ISO-10303-21;
HEADER;
/* Generated by software containing ST-Developer
 * from STEP Tools, Inc. (www.steptools.com) 
 */

FILE_DESCRIPTION(
/* description */ (''),
/* implementation_level */ '2;1');

FILE_NAME(
/* name */ 'ISO 4762 - M3 x 10 - 12.9.step',
/* time_stamp */ '2026-10-15T12:29:06-07:00',
/* author */ (''),
/* organization */ (''),
/* preprocessor_version */ 'ST-DEVELOPER v20.2',
/* originating_system */ 'Autodesk Translation Framework v15.15.0.0',
/* authorisation */ '');

FILE_SCHEMA (('AUTOMOTIVE_DESIGN { 1 0 10303 214 3 1 1 }'));
ENDSEC;

DATA;
#10=MECHANICAL_DESIGN_GEOMETRIC_PRESENTATION_REPRESENTATION('',(#1750),#135282);
#97=TOROIDAL_SURFACE('',#33907,1.5635,0.1);
#98=TOROIDAL_SURFACE('',#34101,2.55,0.2);
#200=(
BOUNDED_CURVE()
B_SPLINE_CURVE(2,(#125959,#125960,#125961),.UNSPECIFIED.,.F.,.F.)
B_SPLINE_CURVE_WITH_KNOTS((3,3),(0.,0.0211644268265626),.UNSPECIFIED.)
CURVE()
GEOMETRIC_REPRESENTATION_ITEM()
RATIONAL_B_SPLINE_CURVE((1.,1.00090979172689,1.00093939181531))
REPRESENTATION_ITEM('')
);
#201=(
BOUNDED_CURVE()
B_SPLINE_CURVE(2,(#125965,#125966,#125967),.UNSPECIFIED.,.F.,.F.)
B_SPLINE_CURVE_WITH_KNOTS((3,3),(0.0225879098005429,0.0437523366271117),
 .UNSPECIFIED.)
CURVE()
GEOMETRIC_REPRESENTATION_ITEM()
RATIONAL_B_SPLINE_CURVE((1.00093939181021,1.00090979172194,1.))
REPRESENTATION_ITEM('')
);
#202=(
BOUNDED_CURVE()
B_SPLINE_CURVE(2,(#126262,#126263,#126264),.UNSPECIFIED.,.F.,.F.)
B_SPLINE_CURVE_WITH_KNOTS((3,3),(0.,0.0211644268265449),.UNSPECIFIED.)
CURVE()
GEOMETRIC_REPRESENTATION_ITEM()
RATIONAL_B_SPLINE_CURVE((1.,1.00090979172393,1.00093939181226))
REPRESENTATION_ITEM('')
);
#203=(
BOUNDED_CURVE()
B_SPLINE_CURVE(2,(#126266,#126267,#126268),.UNSPECIFIED.,.F.,.F.)
B_SPLINE_CURVE_WITH_KNOTS((3,3),(0.0225879098005501,0.0437523366271115),
 .UNSPECIFIED.)
CURVE()
GEOMETRIC_REPRESENTATION_ITEM()
RATIONAL_B_SPLINE_CURVE((1.00093939181012,1.00090979172185,1.))
REPRESENTATION_ITEM('')
);
#204=(
BOUNDED_CURVE()
B_SPLINE_CURVE(2,(#126273,#126274,#126275),.UNSPECIFIED.,.F.,.F.)
B_SPLINE_CURVE_WITH_KNOTS((3,3),(0.0225879098005831,0.0437523366271112),
 .UNSPECIFIED.)
CURVE()
GEOMETRIC_REPRESENTATION_ITEM()
RATIONAL_B_SPLINE_CURVE((1.0009393918114,1.0009097917231,1.))
REPRESENTATION_ITEM('')
);
#205=(
BOUNDED_CURVE()
B_SPLINE_CURVE(2,(#126277,#126278,#126279),.UNSPECIFIED.,.F.,.F.)
B_SPLINE_CURVE_WITH_KNOTS((3,3),(0.,0.0211644268265669),.UNSPECIFIED.)
CURVE()
GEOMETRIC_REPRESENTATION_ITEM()
RATIONAL_B_SPLINE_CURVE((1.,1.00090979172267,1.00093939181096))
REPRESENTATION_ITEM('')
);
#206=(
BOUNDED_CURVE()
B_SPLINE_CURVE(2,(#126280,#126281,#126282),.UNSPECIFIED.,.F.,.F.)
B_SPLINE_CURVE_WITH_KNOTS((3,3),(0.0225879098005253,0.0437523366271112),
 .UNSPECIFIED.)
CURVE()
GEOMETRIC_REPRESENTATION_ITEM()
RATIONAL_B_SPLINE_CURVE((1.00093939180879,1.00090979172056,1.))
REPRESENTATION_ITEM('')
);
#207=(
BOUNDED_CURVE()
B_SPLINE_CURVE(2,(#126284,#126285,#126286),.UNSPECIFIED.,.F.,.F.)
B_SPLINE_CURVE_WITH_KNOTS((3,3),(0.,0.0211644268265721),.UNSPECIFIED.)
CURVE()
GEOMETRIC_REPRESENTATION_ITEM()
RATIONAL_B_SPLINE_CURVE((1.,1.00090979172631,1.00093939181472))
REPRESENTATION_ITEM('')
);
#208=(
BOUNDED_CURVE()
B_SPLINE_CURVE(2,(#126287,#126288,#126289),.UNSPECIFIED.,.F.,.F.)
B_SPLINE_CURVE_WITH_KNOTS((3,3),(0.0225879098005649,0.043752336627111),
 .UNSPECIFIED.)
CURVE()
GEOMETRIC_REPRESENTATION_ITEM()
RATIONAL_B_SPLINE_CURVE((1.00093939180692,1.00090979171876,1.))
REPRESENTATION_ITEM('')
);
#209=(
BOUNDED_CURVE()
B_SPLINE_CURVE(2,(#126291,#126292,#126293),.UNSPECIFIED.,.F.,.F.)
B_SPLINE_CURVE_WITH_KNOTS((3,3),(0.,0.0211644268265702),.UNSPECIFIED.)
CURVE()
GEOMETRIC_REPRESENTATION_ITEM()
RATIONAL_B_SPLINE_CURVE((1.,1.00090979172334,1.00093939181166))
REPRESENTATION_ITEM('')
);
#210=(
BOUNDED_CURVE()
B_SPLINE_CURVE(2,(#126294,#126295,#126296),.UNSPECIFIED.,.F.,.F.)
B_SPLINE_CURVE_WITH_KNOTS((3,3),(0.0225879098005071,0.0437523366271112),
 .UNSPECIFIED.)
CURVE()
GEOMETRIC_REPRESENTATION_ITEM()
RATIONAL_B_SPLINE_CURVE((1.00093939181505,1.00090979172663,1.))
REPRESENTATION_ITEM('')
);
#211=(
BOUNDED_CURVE()
B_SPLINE_CURVE(2,(#126298,#126299,#126300),.UNSPECIFIED.,.F.,.F.)
B_SPLINE_CURVE_WITH_KNOTS((3,3),(0.,0.0211644268265989),.UNSPECIFIED.)
CURVE()
GEOMETRIC_REPRESENTATION_ITEM()
RATIONAL_B_SPLINE_CURVE((1.,1.00090979172892,1.00093939181741))
REPRESENTATION_ITEM('')
);
#212=(
BOUNDED_CURVE()
B_SPLINE_CURVE(2,(#126301,#126302,#126303),.UNSPECIFIED.,.F.,.F.)
B_SPLINE_CURVE_WITH_KNOTS((3,3),(0.0225879098005698,0.043752336627111),
 .UNSPECIFIED.)
CURVE()
GEOMETRIC_REPRESENTATION_ITEM()
RATIONAL_B_SPLINE_CURVE((1.00093939181504,1.00090979172662,1.))
REPRESENTATION_ITEM('')
);
#213=(
BOUNDED_CURVE()
B_SPLINE_CURVE(2,(#126305,#126306,#126307),.UNSPECIFIED.,.F.,.F.)
B_SPLINE_CURVE_WITH_KNOTS((3,3),(0.,0.0211644268265459),.UNSPECIFIED.)
CURVE()
GEOMETRIC_REPRESENTATION_ITEM()
RATIONAL_B_SPLINE_CURVE((1.,1.00090979172781,1.00093939181627))
REPRESENTATION_ITEM('')
);
#214=(
BOUNDED_CURVE()
B_SPLINE_CURVE(2,(#126308,#126309,#126310),.UNSPECIFIED.,.F.,.F.)
B_SPLINE_CURVE_WITH_KNOTS((3,3),(0.0225879098004806,0.043752336627111),
 .UNSPECIFIED.)
CURVE()
GEOMETRIC_REPRESENTATION_ITEM()
RATIONAL_B_SPLINE_CURVE((1.00093939180982,1.00090979172157,1.))
REPRESENTATION_ITEM('')
);
#215=(
BOUNDED_CURVE()
B_SPLINE_CURVE(2,(#126312,#126313,#126314),.UNSPECIFIED.,.F.,.F.)
B_SPLINE_CURVE_WITH_KNOTS((3,3),(0.,0.0211644268265575),.UNSPECIFIED.)
CURVE()
GEOMETRIC_REPRESENTATION_ITEM()
RATIONAL_B_SPLINE_CURVE((1.,1.00090979172714,1.00093939181558))
REPRESENTATION_ITEM('')
);
#216=(
BOUNDED_CURVE()
B_SPLINE_CURVE(2,(#126315,#126316,#126317),.UNSPECIFIED.,.F.,.F.)
B_SPLINE_CURVE_WITH_KNOTS((3,3),(0.0225879098005155,0.0437523366271111),
 .UNSPECIFIED.)
CURVE()
GEOMETRIC_REPRESENTATION_ITEM()
RATIONAL_B_SPLINE_CURVE((1.0009393918136,1.00090979172523,1.))
REPRESENTATION_ITEM('')
);
#217=(
BOUNDED_CURVE()
B_SPLINE_CURVE(2,(#126319,#126320,#126321),.UNSPECIFIED.,.F.,.F.)
B_SPLINE_CURVE_WITH_KNOTS((3,3),(0.,0.0211644268265217),.UNSPECIFIED.)
CURVE()
GEOMETRIC_REPRESENTATION_ITEM()
RATIONAL_B_SPLINE_CURVE((1.,1.00090979172259,1.00093939181088))
REPRESENTATION_ITEM('')
);
#218=(
BOUNDED_CURVE()
B_SPLINE_CURVE(2,(#126322,#126323,#126324),.UNSPECIFIED.,.F.,.F.)
B_SPLINE_CURVE_WITH_KNOTS((3,3),(0.0225879098004986,0.043752336627111),
 .UNSPECIFIED.)
CURVE()
GEOMETRIC_REPRESENTATION_ITEM()
RATIONAL_B_SPLINE_CURVE((1.00093939181162,1.00090979172331,1.))
REPRESENTATION_ITEM('')
);
#219=(
BOUNDED_CURVE()
B_SPLINE_CURVE(2,(#126326,#126327,#126328),.UNSPECIFIED.,.F.,.F.)
B_SPLINE_CURVE_WITH_KNOTS((3,3),(0.,0.0211644268265753),.UNSPECIFIED.)
CURVE()
GEOMETRIC_REPRESENTATION_ITEM()
RATIONAL_B_SPLINE_CURVE((1.,1.00090979172494,1.00093939181331))
REPRESENTATION_ITEM('')
);
#220=(
BOUNDED_CURVE()
B_SPLINE_CURVE(2,(#126329,#126330,#126331),.UNSPECIFIED.,.F.,.F.)
B_SPLINE_CURVE_WITH_KNOTS((3,3),(0.02258790980058,0.043752336627111),
 .UNSPECIFIED.)
CURVE()
GEOMETRIC_REPRESENTATION_ITEM()
RATIONAL_B_SPLINE_CURVE((1.00093939181509,1.00090979172667,1.))
REPRESENTATION_ITEM('')
);
#221=(
BOUNDED_CURVE()
B_SPLINE_CURVE(2,(#126333,#126334,#126335),.UNSPECIFIED.,.F.,.F.)
B_SPLINE_CURVE_WITH_KNOTS((3,3),(0.,0.0211644268265208),.UNSPECIFIED.)
CURVE()
GEOMETRIC_REPRESENTATION_ITEM()
RATIONAL_B_SPLINE_CURVE((1.,1.0009097917237,1.00093939181202))
REPRESENTATION_ITEM('')
);
#222=(
BOUNDED_CURVE()
B_SPLINE_CURVE(2,(#126336,#126337,#126338),.UNSPECIFIED.,.F.,.F.)
B_SPLINE_CURVE_WITH_KNOTS((3,3),(0.022587909800591,0.0437523366271109),
 .UNSPECIFIED.)
CURVE()
GEOMETRIC_REPRESENTATION_ITEM()
RATIONAL_B_SPLINE_CURVE((1.0009393918133,1.00090979172493,1.))
REPRESENTATION_ITEM('')
);
#223=(
BOUNDED_CURVE()
B_SPLINE_CURVE(2,(#126340,#126341,#126342),.UNSPECIFIED.,.F.,.F.)
B_SPLINE_CURVE_WITH_KNOTS((3,3),(0.,0.0211644268265324),.UNSPECIFIED.)
CURVE()
GEOMETRIC_REPRESENTATION_ITEM()
RATIONAL_B_SPLINE_CURVE((1.,1.00090979172547,1.00093939181385))
REPRESENTATION_ITEM('')
);
#224=(
BOUNDED_CURVE()
B_SPLINE_CURVE(2,(#126343,#126344,#126345),.UNSPECIFIED.,.F.,.F.)
B_SPLINE_CURVE_WITH_KNOTS((3,3),(0.0225879098005774,0.0437523366271109),
 .UNSPECIFIED.)
CURVE()
GEOMETRIC_REPRESENTATION_ITEM()
RATIONAL_B_SPLINE_CURVE((1.00093939181154,1.00090979172323,1.))
REPRESENTATION_ITEM('')
);
#225=(
BOUNDED_CURVE()
B_SPLINE_CURVE(2,(#126347,#126348,#126349),.UNSPECIFIED.,.F.,.F.)
B_SPLINE_CURVE_WITH_KNOTS((3,3),(0.,0.0211644268266055),.UNSPECIFIED.)
CURVE()
GEOMETRIC_REPRESENTATION_ITEM()
RATIONAL_B_SPLINE_CURVE((1.,1.00090979172398,1.00093939181232))
REPRESENTATION_ITEM('')
);
#226=(
BOUNDED_CURVE()
B_SPLINE_CURVE(2,(#126350,#126351,#126352),.UNSPECIFIED.,.F.,.F.)
B_SPLINE_CURVE_WITH_KNOTS((3,3),(0.0225879098005268,0.043752336627111),
 .UNSPECIFIED.)
CURVE()
GEOMETRIC_REPRESENTATION_ITEM()
RATIONAL_B_SPLINE_CURVE((1.00093939181403,1.00090979172564,1.))
REPRESENTATION_ITEM('')
);
#227=(
BOUNDED_CURVE()
B_SPLINE_CURVE(2,(#126354,#126355,#126356),.UNSPECIFIED.,.F.,.F.)
B_SPLINE_CURVE_WITH_KNOTS((3,3),(0.,0.0211644268265998),.UNSPECIFIED.)
CURVE()
GEOMETRIC_REPRESENTATION_ITEM()
RATIONAL_B_SPLINE_CURVE((1.,1.00090979172202,1.00093939181029))
REPRESENTATION_ITEM('')
);
#228=(
BOUNDED_CURVE()
B_SPLINE_CURVE(2,(#126357,#126358,#126359),.UNSPECIFIED.,.F.,.F.)
B_SPLINE_CURVE_WITH_KNOTS((3,3),(0.0225879098005115,0.0437523366271109),
 .UNSPECIFIED.)
CURVE()
GEOMETRIC_REPRESENTATION_ITEM()
RATIONAL_B_SPLINE_CURVE((1.00093939181353,1.00090979172516,1.))
REPRESENTATION_ITEM('')
);
#229=(
BOUNDED_CURVE()
B_SPLINE_CURVE(2,(#126361,#126362,#126363),.UNSPECIFIED.,.F.,.F.)
B_SPLINE_CURVE_WITH_KNOTS((3,3),(0.,0.0211644268266192),.UNSPECIFIED.)
CURVE()
GEOMETRIC_REPRESENTATION_ITEM()
RATIONAL_B_SPLINE_CURVE((1.,1.00090979172386,1.00093939181218))
REPRESENTATION_ITEM('')
);
#230=(
BOUNDED_CURVE()
B_SPLINE_CURVE(2,(#126364,#126365,#126366),.UNSPECIFIED.,.F.,.F.)
B_SPLINE_CURVE_WITH_KNOTS((3,3),(0.0225879098005691,0.0437523366271108),
 .UNSPECIFIED.)
CURVE()
GEOMETRIC_REPRESENTATION_ITEM()
RATIONAL_B_SPLINE_CURVE((1.00093939181287,1.00090979172452,1.))
REPRESENTATION_ITEM('')
);
#231=(
BOUNDED_CURVE()
B_SPLINE_CURVE(2,(#126368,#126369,#126370),.UNSPECIFIED.,.F.,.F.)
B_SPLINE_CURVE_WITH_KNOTS((3,3),(0.,0.0211644268265309),.UNSPECIFIED.)
CURVE()
GEOMETRIC_REPRESENTATION_ITEM()
RATIONAL_B_SPLINE_CURVE((1.,1.00090979172246,1.00093939181075))
REPRESENTATION_ITEM('')
);
#232=(
BOUNDED_CURVE()
B_SPLINE_CURVE(2,(#126371,#126372,#126373),.UNSPECIFIED.,.F.,.F.)
B_SPLINE_CURVE_WITH_KNOTS((3,3),(0.0225879098005445,0.0437523366271108),
 .UNSPECIFIED.)
CURVE()
GEOMETRIC_REPRESENTATION_ITEM()
RATIONAL_B_SPLINE_CURVE((1.00093939181122,1.00090979172292,1.))
REPRESENTATION_ITEM('')
);
#233=(
BOUNDED_CURVE()
B_SPLINE_CURVE(2,(#126375,#126376,#126377),.UNSPECIFIED.,.F.,.F.)
B_SPLINE_CURVE_WITH_KNOTS((3,3),(0.,0.0211644268266054),.UNSPECIFIED.)
CURVE()
GEOMETRIC_REPRESENTATION_ITEM()
RATIONAL_B_SPLINE_CURVE((1.,1.0009097917244,1.00093939181275))
REPRESENTATION_ITEM('')
);
#234=(
BOUNDED_CURVE()
B_SPLINE_CURVE(2,(#126378,#126379,#126380),.UNSPECIFIED.,.F.,.F.)
B_SPLINE_CURVE_WITH_KNOTS((3,3),(0.0225879098005202,0.0437523366271108),
 .UNSPECIFIED.)
CURVE()
GEOMETRIC_REPRESENTATION_ITEM()
RATIONAL_B_SPLINE_CURVE((1.00093939181333,1.00090979172497,1.))
REPRESENTATION_ITEM('')
);
#235=(
BOUNDED_CURVE()
B_SPLINE_CURVE(2,(#126382,#126383,#126384),.UNSPECIFIED.,.F.,.F.)
B_SPLINE_CURVE_WITH_KNOTS((3,3),(0.,0.0211644268265328),.UNSPECIFIED.)
CURVE()
GEOMETRIC_REPRESENTATION_ITEM()
RATIONAL_B_SPLINE_CURVE((1.,1.00090979172326,1.00093939181157))
REPRESENTATION_ITEM('')
);
#236=(
BOUNDED_CURVE()
B_SPLINE_CURVE(2,(#126385,#126386,#126387),.UNSPECIFIED.,.F.,.F.)
B_SPLINE_CURVE_WITH_KNOTS((3,3),(0.0225879098004953,0.0437523366271108),
 .UNSPECIFIED.)
CURVE()
GEOMETRIC_REPRESENTATION_ITEM()
RATIONAL_B_SPLINE_CURVE((1.0009393918111,1.00090979172281,1.))
REPRESENTATION_ITEM('')
);
#237=(
BOUNDED_CURVE()
B_SPLINE_CURVE(2,(#126389,#126390,#126391),.UNSPECIFIED.,.F.,.F.)
B_SPLINE_CURVE_WITH_KNOTS((3,3),(0.,0.0211644268265412),.UNSPECIFIED.)
CURVE()
GEOMETRIC_REPRESENTATION_ITEM()
RATIONAL_B_SPLINE_CURVE((1.,1.00090979172431,1.00093939181265))
REPRESENTATION_ITEM('')
);
#238=(
BOUNDED_CURVE()
B_SPLINE_CURVE(2,(#126392,#126393,#126394),.UNSPECIFIED.,.F.,.F.)
B_SPLINE_CURVE_WITH_KNOTS((3,3),(0.0225879098005734,0.0437523366271109),
 .UNSPECIFIED.)
CURVE()
GEOMETRIC_REPRESENTATION_ITEM()
RATIONAL_B_SPLINE_CURVE((1.00093939181328,1.00090979172492,1.))
REPRESENTATION_ITEM('')
);
#239=(
BOUNDED_CURVE()
B_SPLINE_CURVE(2,(#126396,#126397,#126398),.UNSPECIFIED.,.F.,.F.)
B_SPLINE_CURVE_WITH_KNOTS((3,3),(0.,0.0211644268265644),.UNSPECIFIED.)
CURVE()
GEOMETRIC_REPRESENTATION_ITEM()
RATIONAL_B_SPLINE_CURVE((1.,1.00090979172253,1.00093939181082))
REPRESENTATION_ITEM('')
);
#240=(
BOUNDED_CURVE()
B_SPLINE_CURVE(2,(#126399,#126400,#126401),.UNSPECIFIED.,.F.,.F.)
B_SPLINE_CURVE_WITH_KNOTS((3,3),(0.0225879098005465,0.0437523366271109),
 .UNSPECIFIED.)
CURVE()
GEOMETRIC_REPRESENTATION_ITEM()
RATIONAL_B_SPLINE_CURVE((1.00093939181082,1.00090979172253,1.))
REPRESENTATION_ITEM('')
);
#241=(
BOUNDED_CURVE()
B_SPLINE_CURVE(2,(#126403,#126404,#126405),.UNSPECIFIED.,.F.,.F.)
B_SPLINE_CURVE_WITH_KNOTS((3,3),(0.,0.0211644268265949),.UNSPECIFIED.)
CURVE()
GEOMETRIC_REPRESENTATION_ITEM()
RATIONAL_B_SPLINE_CURVE((1.,1.00090979172025,1.00093939180846))
REPRESENTATION_ITEM('')
);
#242=(
BOUNDED_CURVE()
B_SPLINE_CURVE(2,(#126406,#126407,#126408),.UNSPECIFIED.,.F.,.F.)
B_SPLINE_CURVE_WITH_KNOTS((3,3),(0.0225879098005516,0.0437523366271116),
 .UNSPECIFIED.)
CURVE()
GEOMETRIC_REPRESENTATION_ITEM()
RATIONAL_B_SPLINE_CURVE((1.00093939180938,1.00090979172114,1.))
REPRESENTATION_ITEM('')
);
#243=(
BOUNDED_CURVE()
B_SPLINE_CURVE(2,(#126410,#126411,#126412),.UNSPECIFIED.,.F.,.F.)
B_SPLINE_CURVE_WITH_KNOTS((3,3),(0.,0.0211644268265594),.UNSPECIFIED.)
CURVE()
GEOMETRIC_REPRESENTATION_ITEM()
RATIONAL_B_SPLINE_CURVE((1.,1.0009097917224,1.00093939181069))
REPRESENTATION_ITEM('')
);
#244=(
BOUNDED_CURVE()
B_SPLINE_CURVE(2,(#126413,#126414,#126415),.UNSPECIFIED.,.F.,.F.)
B_SPLINE_CURVE_WITH_KNOTS((3,3),(0.0225879098004988,0.0437523366271116),
 .UNSPECIFIED.)
CURVE()
GEOMETRIC_REPRESENTATION_ITEM()
RATIONAL_B_SPLINE_CURVE((1.00093939180876,1.00090979172054,1.))
REPRESENTATION_ITEM('')
);
#245=(
BOUNDED_CURVE()
B_SPLINE_CURVE(2,(#126417,#126418,#126419),.UNSPECIFIED.,.F.,.F.)
B_SPLINE_CURVE_WITH_KNOTS((3,3),(0.,0.0211644268266144),.UNSPECIFIED.)
CURVE()
GEOMETRIC_REPRESENTATION_ITEM()
RATIONAL_B_SPLINE_CURVE((1.,1.00090979172203,1.0009393918103))
REPRESENTATION_ITEM('')
);
#246=(
BOUNDED_CURVE()
B_SPLINE_CURVE(2,(#126420,#126421,#126422),.UNSPECIFIED.,.F.,.F.)
B_SPLINE_CURVE_WITH_KNOTS((3,3),(0.0225879098005803,0.0437523366271115),
 .UNSPECIFIED.)
CURVE()
GEOMETRIC_REPRESENTATION_ITEM()
RATIONAL_B_SPLINE_CURVE((1.00093939181596,1.00090979172751,1.))
REPRESENTATION_ITEM('')
);
#247=(
BOUNDED_CURVE()
B_SPLINE_CURVE(2,(#126424,#126425,#126426),.UNSPECIFIED.,.F.,.F.)
B_SPLINE_CURVE_WITH_KNOTS((3,3),(0.,0.0211644268265443),.UNSPECIFIED.)
CURVE()
GEOMETRIC_REPRESENTATION_ITEM()
RATIONAL_B_SPLINE_CURVE((1.,1.00090979171957,1.00093939180776))
REPRESENTATION_ITEM('')
);
#248=(
BOUNDED_CURVE()
B_SPLINE_CURVE(2,(#126427,#126428,#126429),.UNSPECIFIED.,.F.,.F.)
B_SPLINE_CURVE_WITH_KNOTS((3,3),(0.0225879098005492,0.0437523366271114),
 .UNSPECIFIED.)
CURVE()
GEOMETRIC_REPRESENTATION_ITEM()
RATIONAL_B_SPLINE_CURVE((1.00093939181166,1.00090979172334,1.))
REPRESENTATION_ITEM('')
);
#249=(
BOUNDED_CURVE()
B_SPLINE_CURVE(2,(#126431,#126432,#126433),.UNSPECIFIED.,.F.,.F.)
B_SPLINE_CURVE_WITH_KNOTS((3,3),(0.,0.0211644268265569),.UNSPECIFIED.)
CURVE()
GEOMETRIC_REPRESENTATION_ITEM()
RATIONAL_B_SPLINE_CURVE((1.,1.00090979172576,1.00093939181416))
REPRESENTATION_ITEM('')
);
#250=(
BOUNDED_CURVE()
B_SPLINE_CURVE(2,(#126434,#126435,#126436),.UNSPECIFIED.,.F.,.F.)
B_SPLINE_CURVE_WITH_KNOTS((3,3),(0.0225879098005114,0.0437523366271113),
 .UNSPECIFIED.)
CURVE()
GEOMETRIC_REPRESENTATION_ITEM()
RATIONAL_B_SPLINE_CURVE((1.00093939181229,1.00090979172396,1.))
REPRESENTATION_ITEM('')
);
#251=(
BOUNDED_CURVE()
B_SPLINE_CURVE(2,(#126438,#126439,#126440),.UNSPECIFIED.,.F.,.F.)
B_SPLINE_CURVE_WITH_KNOTS((3,3),(0.,0.021164426826552),.UNSPECIFIED.)
CURVE()
GEOMETRIC_REPRESENTATION_ITEM()
RATIONAL_B_SPLINE_CURVE((1.,1.00090979172362,1.00093939181195))
REPRESENTATION_ITEM('')
);
#252=(
BOUNDED_CURVE()
B_SPLINE_CURVE(2,(#126441,#126442,#126443),.UNSPECIFIED.,.F.,.F.)
B_SPLINE_CURVE_WITH_KNOTS((3,3),(0.0225879098005811,0.0437523366271113),
 .UNSPECIFIED.)
CURVE()
GEOMETRIC_REPRESENTATION_ITEM()
RATIONAL_B_SPLINE_CURVE((1.00093939181488,1.00090979172647,1.))
REPRESENTATION_ITEM('')
);
#253=(
BOUNDED_CURVE()
B_SPLINE_CURVE(2,(#126445,#126446,#126447),.UNSPECIFIED.,.F.,.F.)
B_SPLINE_CURVE_WITH_KNOTS((3,3),(0.,0.0211644268265175),.UNSPECIFIED.)
CURVE()
GEOMETRIC_REPRESENTATION_ITEM()
RATIONAL_B_SPLINE_CURVE((1.,1.00090979172709,1.00093939181552))
REPRESENTATION_ITEM('')
);
#254=(
BOUNDED_CURVE()
B_SPLINE_CURVE(2,(#126448,#126449,#126450),.UNSPECIFIED.,.F.,.F.)
B_SPLINE_CURVE_WITH_KNOTS((3,3),(0.0225879098005324,0.0437523366271115),
 .UNSPECIFIED.)
CURVE()
GEOMETRIC_REPRESENTATION_ITEM()
RATIONAL_B_SPLINE_CURVE((1.00093939180857,1.00090979172035,1.))
REPRESENTATION_ITEM('')
);
#255=(
BOUNDED_CURVE()
B_SPLINE_CURVE(2,(#126452,#126453,#126454),.UNSPECIFIED.,.F.,.F.)
B_SPLINE_CURVE_WITH_KNOTS((3,3),(0.,0.0211644268265537),.UNSPECIFIED.)
CURVE()
GEOMETRIC_REPRESENTATION_ITEM()
RATIONAL_B_SPLINE_CURVE((1.,1.00090979172547,1.00093939181385))
REPRESENTATION_ITEM('')
);
#256=(
BOUNDED_CURVE()
B_SPLINE_CURVE(2,(#126455,#126456,#126457),.UNSPECIFIED.,.F.,.F.)
B_SPLINE_CURVE_WITH_KNOTS((3,3),(0.022587909800574,0.0437523366271114),
 .UNSPECIFIED.)
CURVE()
GEOMETRIC_REPRESENTATION_ITEM()
RATIONAL_B_SPLINE_CURVE((1.00093939181312,1.00090979172476,1.))
REPRESENTATION_ITEM('')
);
#257=(
BOUNDED_CURVE()
B_SPLINE_CURVE(2,(#126459,#126460,#126461),.UNSPECIFIED.,.F.,.F.)
B_SPLINE_CURVE_WITH_KNOTS((3,3),(0.,0.021164426826543),.UNSPECIFIED.)
CURVE()
GEOMETRIC_REPRESENTATION_ITEM()
RATIONAL_B_SPLINE_CURVE((1.,1.00090979172432,1.00093939181266))
REPRESENTATION_ITEM('')
);
#258=(
BOUNDED_CURVE()
B_SPLINE_CURVE(2,(#126462,#126463,#126464),.UNSPECIFIED.,.F.,.F.)
B_SPLINE_CURVE_WITH_KNOTS((3,3),(0.0225879098005786,0.0437523366271112),
 .UNSPECIFIED.)
CURVE()
GEOMETRIC_REPRESENTATION_ITEM()
RATIONAL_B_SPLINE_CURVE((1.00093939181221,1.00090979172388,1.))
REPRESENTATION_ITEM('')
);
#259=(
BOUNDED_CURVE()
B_SPLINE_CURVE(2,(#126466,#126467,#126468),.UNSPECIFIED.,.F.,.F.)
B_SPLINE_CURVE_WITH_KNOTS((3,3),(0.,0.0211644268266067),.UNSPECIFIED.)
CURVE()
GEOMETRIC_REPRESENTATION_ITEM()
RATIONAL_B_SPLINE_CURVE((1.,1.00090979172414,1.00093939181248))
REPRESENTATION_ITEM('')
);
#260=(
BOUNDED_CURVE()
B_SPLINE_CURVE(2,(#126469,#126470,#126471),.UNSPECIFIED.,.F.,.F.)
B_SPLINE_CURVE_WITH_KNOTS((3,3),(0.0225879098005837,0.0437523366271114),
 .UNSPECIFIED.)
CURVE()
GEOMETRIC_REPRESENTATION_ITEM()
RATIONAL_B_SPLINE_CURVE((1.00093939181515,1.00090979172673,1.))
REPRESENTATION_ITEM('')
);
#261=(
BOUNDED_CURVE()
B_SPLINE_CURVE(2,(#126473,#126474,#126475),.UNSPECIFIED.,.F.,.F.)
B_SPLINE_CURVE_WITH_KNOTS((3,3),(0.,0.021164426826571),.UNSPECIFIED.)
CURVE()
GEOMETRIC_REPRESENTATION_ITEM()
RATIONAL_B_SPLINE_CURVE((1.,1.00090979172479,1.00093939181314))
REPRESENTATION_ITEM('')
);
#262=(
BOUNDED_CURVE()
B_SPLINE_CURVE(2,(#126476,#126477,#126478),.UNSPECIFIED.,.F.,.F.)
B_SPLINE_CURVE_WITH_KNOTS((3,3),(0.0225879098005185,0.0437523366271113),
 .UNSPECIFIED.)
CURVE()
GEOMETRIC_REPRESENTATION_ITEM()
RATIONAL_B_SPLINE_CURVE((1.00093939181435,1.00090979172595,1.))
REPRESENTATION_ITEM('')
);
#263=(
BOUNDED_CURVE()
B_SPLINE_CURVE(2,(#126480,#126481,#126482),.UNSPECIFIED.,.F.,.F.)
B_SPLINE_CURVE_WITH_KNOTS((3,3),(0.,0.0211644268264922),.UNSPECIFIED.)
CURVE()
GEOMETRIC_REPRESENTATION_ITEM()
RATIONAL_B_SPLINE_CURVE((1.,1.00090979172566,1.00093939181405))
REPRESENTATION_ITEM('')
);
#264=(
BOUNDED_CURVE()
B_SPLINE_CURVE(2,(#126483,#126484,#126485),.UNSPECIFIED.,.F.,.F.)
B_SPLINE_CURVE_WITH_KNOTS((3,3),(0.0225879098005469,0.0437523366271113),
 .UNSPECIFIED.)
CURVE()
GEOMETRIC_REPRESENTATION_ITEM()
RATIONAL_B_SPLINE_CURVE((1.00093939181638,1.00090979172792,1.))
REPRESENTATION_ITEM('')
);
#265=(
BOUNDED_CURVE()
B_SPLINE_CURVE(2,(#126487,#126488,#126489),.UNSPECIFIED.,.F.,.F.)
B_SPLINE_CURVE_WITH_KNOTS((3,3),(0.,0.021164426826593),.UNSPECIFIED.)
CURVE()
GEOMETRIC_REPRESENTATION_ITEM()
RATIONAL_B_SPLINE_CURVE((1.,1.00090979171923,1.00093939180741))
REPRESENTATION_ITEM('')
);
#266=(
BOUNDED_CURVE()
B_SPLINE_CURVE(2,(#126490,#126491,#126492),.UNSPECIFIED.,.F.,.F.)
B_SPLINE_CURVE_WITH_KNOTS((3,3),(0.0225879098005747,0.0437523366271113),
 .UNSPECIFIED.)
CURVE()
GEOMETRIC_REPRESENTATION_ITEM()
RATIONAL_B_SPLINE_CURVE((1.00093939181217,1.00090979172384,1.))
REPRESENTATION_ITEM('')
);
#267=(
BOUNDED_CURVE()
B_SPLINE_CURVE(2,(#126494,#126495,#126496),.UNSPECIFIED.,.F.,.F.)
B_SPLINE_CURVE_WITH_KNOTS((3,3),(0.,0.0211644268265413),.UNSPECIFIED.)
CURVE()
GEOMETRIC_REPRESENTATION_ITEM()
RATIONAL_B_SPLINE_CURVE((1.,1.00090979172347,1.00093939181179))
REPRESENTATION_ITEM('')
);
#268=(
BOUNDED_CURVE()
B_SPLINE_CURVE(2,(#126497,#126498,#126499),.UNSPECIFIED.,.F.,.F.)
B_SPLINE_CURVE_WITH_KNOTS((3,3),(0.022587909800513,0.043752336627111),
 .UNSPECIFIED.)
CURVE()
GEOMETRIC_REPRESENTATION_ITEM()
RATIONAL_B_SPLINE_CURVE((1.00093939181455,1.00090979172615,1.))
REPRESENTATION_ITEM('')
);
#269=(
BOUNDED_CURVE()
B_SPLINE_CURVE(2,(#126501,#126502,#126503),.UNSPECIFIED.,.F.,.F.)
B_SPLINE_CURVE_WITH_KNOTS((3,3),(0.,0.0211644268266052),.UNSPECIFIED.)
CURVE()
GEOMETRIC_REPRESENTATION_ITEM()
RATIONAL_B_SPLINE_CURVE((1.,1.00090979172484,1.0009393918132))
REPRESENTATION_ITEM('')
);
#270=(
BOUNDED_CURVE()
B_SPLINE_CURVE(2,(#126504,#126505,#126506),.UNSPECIFIED.,.F.,.F.)
B_SPLINE_CURVE_WITH_KNOTS((3,3),(0.0225879098004969,0.043752336627111),
 .UNSPECIFIED.)
CURVE()
GEOMETRIC_REPRESENTATION_ITEM()
RATIONAL_B_SPLINE_CURVE((1.00093939181429,1.0009097917259,1.))
REPRESENTATION_ITEM('')
);
#271=(
BOUNDED_CURVE()
B_SPLINE_CURVE(2,(#126507,#126508,#126509),.UNSPECIFIED.,.F.,.F.)
B_SPLINE_CURVE_WITH_KNOTS((3,3),(0.,0.0211644268265307),.UNSPECIFIED.)
CURVE()
GEOMETRIC_REPRESENTATION_ITEM()
RATIONAL_B_SPLINE_CURVE((1.,1.00090979172321,1.00093939181152))
REPRESENTATION_ITEM('')
);
#272=(
BOUNDED_CURVE()
B_SPLINE_CURVE(2,(#126759,#126760,#126761),.UNSPECIFIED.,.F.,.F.)
B_SPLINE_CURVE_WITH_KNOTS((3,3),(0.,0.0126130588257612),.UNSPECIFIED.)
CURVE()
GEOMETRIC_REPRESENTATION_ITEM()
RATIONAL_B_SPLINE_CURVE((1.,1.00234596681272,1.00329298027596))
REPRESENTATION_ITEM('')
);
#273=(
BOUNDED_CURVE()
B_SPLINE_CURVE(2,(#126765,#126766,#126767),.UNSPECIFIED.,.F.,.F.)
B_SPLINE_CURVE_WITH_KNOTS((3,3),(0.0296897347922144,0.0423027936179771),
 .UNSPECIFIED.)
CURVE()
GEOMETRIC_REPRESENTATION_ITEM()
RATIONAL_B_SPLINE_CURVE((1.00329298027586,1.00234596681265,1.))
REPRESENTATION_ITEM('')
);
#274=(
BOUNDED_CURVE()
B_SPLINE_CURVE(2,(#126769,#126770,#126771),.UNSPECIFIED.,.F.,.F.)
B_SPLINE_CURVE_WITH_KNOTS((3,3),(0.,0.0126130588257635),.UNSPECIFIED.)
CURVE()
GEOMETRIC_REPRESENTATION_ITEM()
RATIONAL_B_SPLINE_CURVE((1.,1.00234596681256,1.00329298027573))
REPRESENTATION_ITEM('')
);
#275=(
BOUNDED_CURVE()
B_SPLINE_CURVE(2,(#126775,#126776,#126777),.UNSPECIFIED.,.F.,.F.)
B_SPLINE_CURVE_WITH_KNOTS((3,3),(0.0296897347922126,0.0423027936179773),
 .UNSPECIFIED.)
CURVE()
GEOMETRIC_REPRESENTATION_ITEM()
RATIONAL_B_SPLINE_CURVE((1.00329298027557,1.00234596681244,1.))
REPRESENTATION_ITEM('')
);
#276=(
BOUNDED_CURVE()
B_SPLINE_CURVE(2,(#126779,#126780,#126781),.UNSPECIFIED.,.F.,.F.)
B_SPLINE_CURVE_WITH_KNOTS((3,3),(0.,0.0126130588257643),.UNSPECIFIED.)
CURVE()
GEOMETRIC_REPRESENTATION_ITEM()
RATIONAL_B_SPLINE_CURVE((1.,1.00234596681249,1.00329298027564))
REPRESENTATION_ITEM('')
);
#277=(
BOUNDED_CURVE()
B_SPLINE_CURVE(2,(#126785,#126786,#126787),.UNSPECIFIED.,.F.,.F.)
B_SPLINE_CURVE_WITH_KNOTS((3,3),(0.029689734792213,0.0423027936179773),
 .UNSPECIFIED.)
CURVE()
GEOMETRIC_REPRESENTATION_ITEM()
RATIONAL_B_SPLINE_CURVE((1.00329298027556,1.00234596681243,1.))
REPRESENTATION_ITEM('')
);
#278=(
BOUNDED_CURVE()
B_SPLINE_CURVE(2,(#126789,#126790,#126791),.UNSPECIFIED.,.F.,.F.)
B_SPLINE_CURVE_WITH_KNOTS((3,3),(0.,0.0126130588257614),.UNSPECIFIED.)
CURVE()
GEOMETRIC_REPRESENTATION_ITEM()
RATIONAL_B_SPLINE_CURVE((1.,1.00234596681274,1.00329298027599))
REPRESENTATION_ITEM('')
);
#279=(
BOUNDED_CURVE()
B_SPLINE_CURVE(2,(#126795,#126796,#126797),.UNSPECIFIED.,.F.,.F.)
B_SPLINE_CURVE_WITH_KNOTS((3,3),(0.0296897347922119,0.0423027936179772),
 .UNSPECIFIED.)
CURVE()
GEOMETRIC_REPRESENTATION_ITEM()
RATIONAL_B_SPLINE_CURVE((1.00329298027552,1.00234596681241,1.))
REPRESENTATION_ITEM('')
);
#280=(
BOUNDED_CURVE()
B_SPLINE_CURVE(2,(#126799,#126800,#126801),.UNSPECIFIED.,.F.,.F.)
B_SPLINE_CURVE_WITH_KNOTS((3,3),(0.,0.0126130588257625),.UNSPECIFIED.)
CURVE()
GEOMETRIC_REPRESENTATION_ITEM()
RATIONAL_B_SPLINE_CURVE((1.,1.00234596681265,1.00329298027587))
REPRESENTATION_ITEM('')
);
#281=(
BOUNDED_CURVE()
B_SPLINE_CURVE(2,(#126805,#126806,#126807),.UNSPECIFIED.,.F.,.F.)
B_SPLINE_CURVE_WITH_KNOTS((3,3),(0.0296897347922142,0.0423027936179773),
 .UNSPECIFIED.)
CURVE()
GEOMETRIC_REPRESENTATION_ITEM()
RATIONAL_B_SPLINE_CURVE((1.00329298027579,1.0023459668126,1.))
REPRESENTATION_ITEM('')
);
#282=(
BOUNDED_CURVE()
B_SPLINE_CURVE(2,(#126809,#126810,#126811),.UNSPECIFIED.,.F.,.F.)
B_SPLINE_CURVE_WITH_KNOTS((3,3),(0.,0.0126130588257623),.UNSPECIFIED.)
CURVE()
GEOMETRIC_REPRESENTATION_ITEM()
RATIONAL_B_SPLINE_CURVE((1.,1.00234596681269,1.00329298027592))
REPRESENTATION_ITEM('')
);
#283=(
BOUNDED_CURVE()
B_SPLINE_CURVE(2,(#126814,#126815,#126816),.UNSPECIFIED.,.F.,.F.)
B_SPLINE_CURVE_WITH_KNOTS((3,3),(0.0296897347922153,0.042302793617977),
 .UNSPECIFIED.)
CURVE()
GEOMETRIC_REPRESENTATION_ITEM()
RATIONAL_B_SPLINE_CURVE((1.00329298027599,1.00234596681274,1.))
REPRESENTATION_ITEM('')
);
#613=B_SPLINE_SURFACE_WITH_KNOTS('',3,3,((#124738,#124739,#124740,#124741,
#124742,#124743,#124744,#124745,#124746,#124747,#124748,#124749,#124750,
#124751,#124752,#124753,#124754,#124755,#124756,#124757,#124758,#124759,
#124760,#124761,#124762,#124763,#124764,#124765,#124766,#124767,#124768,
#124769,#124770,#124771,#124772,#124773,#124774,#124775,#124776,#124777,
#124778,#124779,#124780,#124781,#124782,#124783,#124784,#124785,#124786,
#124787,#124788,#124789,#124790,#124791,#124792,#124793,#124794,#124795,
#124796,#124797,#124798,#124799,#124800,#124801,#124802,#124803,#124804,
#124805,#124806,#124807,#124808,#124809,#124810,#124811,#124812,#124813,
#124814,#124815,#124816,#124817,#124818,#124819,#124820,#124821,#124822,
#124823,#124824,#124825,#124826,#124827,#124828,#124829,#124830,#124831,
#124832,#124833,#124834,#124835,#124836,#124837,#124838,#124839,#124840,
#124841,#124842,#124843,#124844,#124845,#124846,#124847,#124848,#124849,
#124850,#124851,#124852,#124853,#124854,#124855,#124856,#124857,#124858,
#124859,#124860,#124861,#124862,#124863),(#124864,#124865,#124866,#124867,
#124868,#124869,#124870,#124871,#124872,#124873,#124874,#124875,#124876,
#124877,#124878,#124879,#124880,#124881,#124882,#124883,#124884,#124885,
#124886,#124887,#124888,#124889,#124890,#124891,#124892,#124893,#124894,
#124895,#124896,#124897,#124898,#124899,#124900,#124901,#124902,#124903,
#124904,#124905,#124906,#124907,#124908,#124909,#124910,#124911,#124912,
#124913,#124914,#124915,#124916,#124917,#124918,#124919,#124920,#124921,
#124922,#124923,#124924,#124925,#124926,#124927,#124928,#124929,#124930,
#124931,#124932,#124933,#124934,#124935,#124936,#124937,#124938,#124939,
#124940,#124941,#124942,#124943,#124944,#124945,#124946,#124947,#124948,
#124949,#124950,#124951,#124952,#124953,#124954,#124955,#124956,#124957,
#124958,#124959,#124960,#124961,#124962,#124963,#124964,#124965,#124966,
#124967,#124968,#124969,#124970,#124971,#124972,#124973,#124974,#124975,
#124976,#124977,#124978,#124979,#124980,#124981,#124982,#124983,#124984,
#124985,#124986,#124987,#124988,#124989),(#124990,#124991,#124992,#124993,
#124994,#124995,#124996,#124997,#124998,#124999,#125000,#125001,#125002,
#125003,#125004,#125005,#125006,#125007,#125008,#125009,#125010,#125011,
#125012,#125013,#125014,#125015,#125016,#125017,#125018,#125019,#125020,
#125021,#125022,#125023,#125024,#125025,#125026,#125027,#125028,#125029,
#125030,#125031,#125032,#125033,#125034,#125035,#125036,#125037,#125038,
#125039,#125040,#125041,#125042,#125043,#125044,#125045,#125046,#125047,
#125048,#125049,#125050,#125051,#125052,#125053,#125054,#125055,#125056,
#125057,#125058,#125059,#125060,#125061,#125062,#125063,#125064,#125065,
#125066,#125067,#125068,#125069,#125070,#125071,#125072,#125073,#125074,
#125075,#125076,#125077,#125078,#125079,#125080,#125081,#125082,#125083,
#125084,#125085,#125086,#125087,#125088,#125089,#125090,#125091,#125092,
#125093,#125094,#125095,#125096,#125097,#125098,#125099,#125100,#125101,
#125102,#125103,#125104,#125105,#125106,#125107,#125108,#125109,#125110,
#125111,#125112,#125113,#125114,#125115),(#125116,#125117,#125118,#125119,
#125120,#125121,#125122,#125123,#125124,#125125,#125126,#125127,#125128,
#125129,#125130,#125131,#125132,#125133,#125134,#125135,#125136,#125137,
#125138,#125139,#125140,#125141,#125142,#125143,#125144,#125145,#125146,
#125147,#125148,#125149,#125150,#125151,#125152,#125153,#125154,#125155,
#125156,#125157,#125158,#125159,#125160,#125161,#125162,#125163,#125164,
#125165,#125166,#125167,#125168,#125169,#125170,#125171,#125172,#125173,
#125174,#125175,#125176,#125177,#125178,#125179,#125180,#125181,#125182,
#125183,#125184,#125185,#125186,#125187,#125188,#125189,#125190,#125191,
#125192,#125193,#125194,#125195,#125196,#125197,#125198,#125199,#125200,
#125201,#125202,#125203,#125204,#125205,#125206,#125207,#125208,#125209,
#125210,#125211,#125212,#125213,#125214,#125215,#125216,#125217,#125218,
#125219,#125220,#125221,#125222,#125223,#125224,#125225,#125226,#125227,
#125228,#125229,#125230,#125231,#125232,#125233,#125234,#125235,#125236,
#125237,#125238,#125239,#125240,#125241)),.UNSPECIFIED.,.F.,.F.,.F.,(4,
4),(4,1,1,1,1,1,1,1,1,1,1,1,1,1,1,1,1,1,1,1,1,1,1,1,1,1,1,1,1,1,1,1,1,1,
1,1,1,1,1,1,1,1,1,1,1,1,1,1,1,1,1,1,1,1,1,1,1,1,1,1,1,1,1,1,1,1,1,1,1,1,
1,1,1,1,1,1,1,1,1,1,1,1,1,1,1,1,1,1,1,1,1,1,1,1,1,1,1,1,1,1,1,1,1,1,1,1,
1,1,1,1,1,1,1,1,1,1,1,1,1,1,1,1,1,4),(-0.000237865095396134,0.0336171964829504),
(8.30175323816384,9.29457283756397,10.2871095208197,11.2796462040753,12.272182887331,
13.2647195705867,14.2572562538424,15.2497929370981,16.2423296203538,17.2348663036095,
18.2274029868652,19.2199396701209,20.2124763533766,21.2050130366322,22.1975497198879,
23.1900864031436,24.1826230863993,25.175159769655,26.1676964529107,27.1602331361664,
28.1527698194221,29.1453065026778,30.1378431859334,31.1303798691891,32.1229165524448,
33.1154532357005,34.1079899189562,35.1005266022119,36.0930632854676,37.0855999687233,
38.078136651979,39.0706733352347,40.0632100184903,41.055746701746,42.0482833850017,
43.0408200682574,44.0333567515131,45.0258934347688,46.0184301180245,47.0109668012802,
48.0035034845359,48.9960401677916,49.9885768510472,50.9811135343029,51.9736502175586,
52.9661869008143,53.95872358407,54.9512602673257,55.9437969505814,56.9363336338371,
57.9288703170928,58.9214070003484,59.9139436836041,60.9064803668598,61.8990170501155,
62.8915537333712,63.8840904166269,64.8766270998826,65.8691637831383,66.861700466394,
67.8542371496497,68.8467738329053,69.839310516161,70.8318471994167,71.8243838826724,
72.8169205659281,73.8094572491838,74.8019939324395,75.7945306156952,76.7870672989509,
77.7796039822065,78.7721406654622,79.7646773487179,80.7572140319736,81.7497507152293,
82.742287398485,83.7348240817407,84.7273607649964,85.7198974482521,86.7124341315078,
87.7049708147634,88.6975074980191,89.6900441812748,90.6825808645305,91.6751175477862,
92.6676542310419,93.6601909142976,94.6527275975533,95.645264280809,96.6378009640647,
97.6303376473203,98.622874330576,99.6154110138317,100.607947697087,101.600484380343,
102.593021063599,103.585557746854,104.57809443011,105.570631113366,106.563167796622,
107.555704479877,108.548241163133,109.540777846389,110.533314529644,111.5258512129,
112.518387896156,113.510924579411,114.503461262667,115.495997945923,116.488534629178,
117.481071312434,118.47360799569,119.466144678946,120.458681362201,121.451218045457,
122.443754728713,123.436291411968,124.428828095224,125.42136477848,126.413901461735,
127.406438144991,128.398974828247,129.391511511502,130.384286059853),
 .UNSPECIFIED.);
#614=B_SPLINE_SURFACE_WITH_KNOTS('',3,3,((#125425,#125426,#125427,#125428,
#125429,#125430,#125431,#125432,#125433,#125434,#125435,#125436,#125437,
#125438,#125439,#125440,#125441,#125442,#125443,#125444,#125445,#125446,
#125447,#125448,#125449,#125450,#125451,#125452,#125453,#125454,#125455,
#125456,#125457,#125458,#125459,#125460,#125461,#125462,#125463,#125464,
#125465,#125466,#125467,#125468,#125469,#125470,#125471,#125472,#125473,
#125474,#125475,#125476,#125477,#125478,#125479,#125480,#125481,#125482,
#125483,#125484,#125485,#125486,#125487,#125488,#125489,#125490,#125491,
#125492,#125493,#125494,#125495,#125496,#125497,#125498,#125499,#125500,
#125501,#125502,#125503,#125504,#125505,#125506,#125507,#125508,#125509,
#125510,#125511,#125512,#125513,#125514,#125515,#125516,#125517,#125518,
#125519,#125520,#125521,#125522,#125523,#125524,#125525,#125526,#125527,
#125528,#125529,#125530,#125531,#125532,#125533,#125534,#125535,#125536,
#125537,#125538,#125539,#125540,#125541,#125542,#125543,#125544,#125545,
#125546,#125547,#125548,#125549,#125550),(#125551,#125552,#125553,#125554,
#125555,#125556,#125557,#125558,#125559,#125560,#125561,#125562,#125563,
#125564,#125565,#125566,#125567,#125568,#125569,#125570,#125571,#125572,
#125573,#125574,#125575,#125576,#125577,#125578,#125579,#125580,#125581,
#125582,#125583,#125584,#125585,#125586,#125587,#125588,#125589,#125590,
#125591,#125592,#125593,#125594,#125595,#125596,#125597,#125598,#125599,
#125600,#125601,#125602,#125603,#125604,#125605,#125606,#125607,#125608,
#125609,#125610,#125611,#125612,#125613,#125614,#125615,#125616,#125617,
#125618,#125619,#125620,#125621,#125622,#125623,#125624,#125625,#125626,
#125627,#125628,#125629,#125630,#125631,#125632,#125633,#125634,#125635,
#125636,#125637,#125638,#125639,#125640,#125641,#125642,#125643,#125644,
#125645,#125646,#125647,#125648,#125649,#125650,#125651,#125652,#125653,
#125654,#125655,#125656,#125657,#125658,#125659,#125660,#125661,#125662,
#125663,#125664,#125665,#125666,#125667,#125668,#125669,#125670,#125671,
#125672,#125673,#125674,#125675,#125676),(#125677,#125678,#125679,#125680,
#125681,#125682,#125683,#125684,#125685,#125686,#125687,#125688,#125689,
#125690,#125691,#125692,#125693,#125694,#125695,#125696,#125697,#125698,
#125699,#125700,#125701,#125702,#125703,#125704,#125705,#125706,#125707,
#125708,#125709,#125710,#125711,#125712,#125713,#125714,#125715,#125716,
#125717,#125718,#125719,#125720,#125721,#125722,#125723,#125724,#125725,
#125726,#125727,#125728,#125729,#125730,#125731,#125732,#125733,#125734,
#125735,#125736,#125737,#125738,#125739,#125740,#125741,#125742,#125743,
#125744,#125745,#125746,#125747,#125748,#125749,#125750,#125751,#125752,
#125753,#125754,#125755,#125756,#125757,#125758,#125759,#125760,#125761,
#125762,#125763,#125764,#125765,#125766,#125767,#125768,#125769,#125770,
#125771,#125772,#125773,#125774,#125775,#125776,#125777,#125778,#125779,
#125780,#125781,#125782,#125783,#125784,#125785,#125786,#125787,#125788,
#125789,#125790,#125791,#125792,#125793,#125794,#125795,#125796,#125797,
#125798,#125799,#125800,#125801,#125802),(#125803,#125804,#125805,#125806,
#125807,#125808,#125809,#125810,#125811,#125812,#125813,#125814,#125815,
#125816,#125817,#125818,#125819,#125820,#125821,#125822,#125823,#125824,
#125825,#125826,#125827,#125828,#125829,#125830,#125831,#125832,#125833,
#125834,#125835,#125836,#125837,#125838,#125839,#125840,#125841,#125842,
#125843,#125844,#125845,#125846,#125847,#125848,#125849,#125850,#125851,
#125852,#125853,#125854,#125855,#125856,#125857,#125858,#125859,#125860,
#125861,#125862,#125863,#125864,#125865,#125866,#125867,#125868,#125869,
#125870,#125871,#125872,#125873,#125874,#125875,#125876,#125877,#125878,
#125879,#125880,#125881,#125882,#125883,#125884,#125885,#125886,#125887,
#125888,#125889,#125890,#125891,#125892,#125893,#125894,#125895,#125896,
#125897,#125898,#125899,#125900,#125901,#125902,#125903,#125904,#125905,
#125906,#125907,#125908,#125909,#125910,#125911,#125912,#125913,#125914,
#125915,#125916,#125917,#125918,#125919,#125920,#125921,#125922,#125923,
#125924,#125925,#125926,#125927,#125928)),.UNSPECIFIED.,.F.,.F.,.F.,(4,
4),(4,1,1,1,1,1,1,1,1,1,1,1,1,1,1,1,1,1,1,1,1,1,1,1,1,1,1,1,1,1,1,1,1,1,
1,1,1,1,1,1,1,1,1,1,1,1,1,1,1,1,1,1,1,1,1,1,1,1,1,1,1,1,1,1,1,1,1,1,1,1,
1,1,1,1,1,1,1,1,1,1,1,1,1,1,1,1,1,1,1,1,1,1,1,1,1,1,1,1,1,1,1,1,1,1,1,1,
1,1,1,1,1,1,1,1,1,1,1,1,1,1,1,1,1,4),(-0.000612126754026731,0.033233417622924),
(11.6157018977616,12.608476430756,13.6010131140117,14.5935497972674,15.5860864805231,
16.5786231637787,17.5711598470344,18.5636965302901,19.5562332135458,20.5487698968015,
21.5413065800572,22.5338432633129,23.5263799465686,24.5189166298243,25.51145331308,
26.5039899963356,27.4965266795913,28.489063362847,29.4816000461027,30.4741367293584,
31.4666734126141,32.4592100958698,33.4517467791255,34.4442834623812,35.4368201456369,
36.4293568288925,37.4218935121482,38.4144301954039,39.4069668786596,40.3995035619153,
41.392040245171,42.3845769284267,43.3771136116824,44.3696502949381,45.3621869781938,
46.3547236614494,47.3472603447051,48.3397970279608,49.3323337112165,50.3248703944722,
51.3174070777279,52.3099437609836,53.3024804442393,54.295017127495,55.2875538107507,
56.2800904940063,57.272627177262,58.2651638605177,59.2577005437734,60.2502372270291,
61.2427739102848,62.2353105935405,63.2278472767962,64.2203839600519,65.2129206433076,
66.2054573265632,67.1979940098189,68.1905306930746,69.1830673763303,70.175604059586,
71.1681407428417,72.1606774260974,73.1532141093531,74.1457507926088,75.1382874758644,
76.1308241591201,77.1233608423758,78.1158975256315,79.1084342088872,80.1009708921429,
81.0935075753986,82.0860442586543,83.07858094191,84.0711176251657,85.0636543084213,
86.056190991677,87.0487276749327,88.0412643581884,89.0338010414441,90.0263377246998,
91.0188744079555,92.0114110912112,93.0039477744669,93.9964844577226,94.9890211409783,
95.9815578242339,96.9740945074896,97.9666311907453,98.959167874001,99.9517045572567,
100.944241240512,101.936777923768,102.929314607024,103.921851290279,104.914387973535,
105.906924656791,106.899461340047,107.891998023302,108.884534706558,109.877071389814,
110.869608073069,111.862144756325,112.854681439581,113.847218122836,114.839754806092,
115.832291489348,116.824828172603,117.817364855859,118.809901539115,119.80243822237,
120.794974905626,121.787511588882,122.780048272138,123.772584955393,124.765121638649,
125.757658321905,126.75019500516,127.742731688416,128.735268371672,129.727805054927,
130.720341738183,131.712878421439,132.705415104694,133.698346948047),
 .UNSPECIFIED.);
#1553=B_SPLINE_CURVE_WITH_KNOTS('',3,(#107631,#107632,#107633,#107634,#107635,
#107636,#107637,#107638,#107639,#107640,#107641,#107642,#107643,#107644,
#107645,#107646,#107647,#107648,#107649,#107650,#107651,#107652,#107653,
#107654,#107655,#107656,#107657,#107658,#107659,#107660,#107661,#107662,
#107663,#107664,#107665,#107666,#107667,#107668,#107669,#107670,#107671,
#107672,#107673,#107674,#107675,#107676,#107677,#107678,#107679,#107680,
#107681,#107682,#107683,#107684,#107685,#107686,#107687,#107688,#107689,
#107690,#107691,#107692,#107693,#107694,#107695,#107696,#107697,#107698,
#107699,#107700,#107701,#107702,#107703,#107704,#107705,#107706,#107707,
#107708,#107709,#107710,#107711,#107712,#107713,#107714,#107715,#107716,
#107717,#107718,#107719,#107720,#107721,#107722,#107723,#107724,#107725,
#107726,#107727,#107728,#107729,#107730,#107731,#107732,#107733,#107734,
#107735,#107736,#107737,#107738,#107739,#107740,#107741,#107742,#107743,
#107744,#107745,#107746,#107747,#107748,#107749,#107750,#107751,#107752,
#107753,#107754,#107755,#107756),.UNSPECIFIED.,.F.,.F.,(4,2,2,2,2,2,2,2,
2,2,2,2,2,2,2,2,2,2,2,2,2,2,2,2,2,2,2,2,2,2,2,2,2,2,2,2,2,2,2,2,2,2,2,2,
2,2,2,2,2,2,2,2,2,2,2,2,2,2,2,2,2,2,4),(2.76410463468713,2.77789812941896,
2.78029099172256,2.78154043546213,2.78255236827767,2.78378253357171,2.78613322726203,
2.80299114552905,2.84623477508507,2.85146639624688,2.85385187931519,2.85569291033944,
2.85768346019709,2.8608647368197,2.87181382805971,2.89151307140856,2.92219014353228,
2.92546467461625,2.92689529622041,2.92791948796111,2.92800365644322,2.92802691950589,
2.92804697267802,2.92806430741348,2.92807932856926,2.92809237225132,2.92810371941849,
2.92811644168053,2.92812877912382,2.92814074852271,2.9281523656638,2.92816364545057,
2.92817460199015,2.92818524861464,2.92819559790968,2.92820566182541,2.92821545166794,
2.92822497815332,2.92823425145468,2.92824328122277,2.92825207665361,2.92826064643558,
2.92826899886783,2.92827714184007,2.92828508287351,2.92829282915032,2.92830038747757,
2.92830776434548,2.9283149659868,2.92832199832138,2.92958491940801,2.93096879994323,
2.93761211253387,2.94996160565319,2.96335951326714,2.9916822450335,2.99530203860186,
2.99761541079866,2.99946130850531,3.00155231497011,3.00512210431552,3.02061545583317,
3.06019655133367),.UNSPECIFIED.);
#1554=B_SPLINE_CURVE_WITH_KNOTS('',3,(#107759,#107760,#107761,#107762,#107763,
#107764,#107765,#107766,#107767,#107768,#107769,#107770,#107771,#107772,
#107773,#107774,#107775,#107776,#107777,#107778,#107779,#107780,#107781,
#107782,#107783,#107784,#107785,#107786,#107787,#107788,#107789),
 .UNSPECIFIED.,.F.,.F.,(4,3,3,3,3,3,3,3,3,3,4),(0.,0.116094185676976,0.232131701312071,
0.348141226325033,0.464158878026556,0.580220774075408,0.69645813588627,
0.812789557622708,0.92936017010412,0.992536683255691,1.12274180646084),
 .UNSPECIFIED.);
#1555=B_SPLINE_CURVE_WITH_KNOTS('',3,(#107794,#107795,#107796,#107797,#107798,
#107799,#107800,#107801,#107802,#107803,#107804,#107805,#107806,#107807,
#107808,#107809,#107810,#107811,#107812,#107813,#107814,#107815,#107816,
#107817,#107818,#107819,#107820,#107821,#107822,#107823,#107824,#107825,
#107826,#107827,#107828,#107829,#107830,#107831,#107832,#107833,#107834,
#107835,#107836,#107837,#107838,#107839,#107840,#107841,#107842,#107843,
#107844,#107845,#107846,#107847,#107848,#107849,#107850,#107851,#107852,
#107853,#107854,#107855,#107856,#107857,#107858,#107859,#107860,#107861,
#107862,#107863,#107864,#107865,#107866,#107867,#107868,#107869,#107870,
#107871,#107872,#107873,#107874,#107875,#107876,#107877,#107878,#107879,
#107880,#107881,#107882,#107883,#107884,#107885,#107886,#107887,#107888,
#107889,#107890,#107891,#107892,#107893,#107894,#107895,#107896,#107897,
#107898,#107899,#107900,#107901,#107902,#107903,#107904,#107905,#107906,
#107907,#107908,#107909,#107910,#107911,#107912,#107913,#107914,#107915,
#107916,#107917,#107918,#107919,#107920,#107921,#107922,#107923,#107924,
#107925,#107926,#107927,#107928,#107929,#107930,#107931,#107932,#107933,
#107934,#107935,#107936,#107937,#107938,#107939,#107940,#107941,#107942,
#107943,#107944,#107945,#107946,#107947,#107948,#107949,#107950,#107951,
#107952,#107953,#107954,#107955,#107956,#107957,#107958,#107959,#107960,
#107961,#107962,#107963,#107964,#107965,#107966,#107967,#107968,#107969,
#107970,#107971,#107972,#107973,#107974,#107975,#107976,#107977,#107978,
#107979,#107980,#107981,#107982,#107983,#107984,#107985,#107986,#107987,
#107988,#107989,#107990,#107991,#107992,#107993,#107994,#107995,#107996,
#107997,#107998,#107999),.UNSPECIFIED.,.F.,.F.,(4,2,2,2,2,2,2,2,2,2,2,2,
2,2,2,2,2,2,2,2,2,2,2,2,2,2,2,2,2,2,2,2,2,2,2,2,2,2,2,2,2,2,2,2,2,2,2,2,
2,2,2,2,2,2,2,2,2,2,2,2,2,2,2,2,2,2,2,2,2,2,2,2,2,2,2,2,2,2,2,2,2,2,2,2,
2,2,2,2,2,2,2,2,2,2,2,2,2,2,2,2,2,2,4),(1.84269843666847,1.84465206436514,
1.86466744624785,1.88909843978047,1.9044696726718,1.90665505477036,1.90796783409467,
1.90898768484762,1.91015809674146,1.9122323585912,1.92207896927376,1.9452269465831,
1.97433899529737,1.97795641832976,1.98024962844833,1.98206668280837,1.98411096986709,
1.98756517846782,2.00191160002639,2.03460536231984,2.05003291699972,2.05222065299162,
2.05353431007178,2.05455467608111,2.05572572941863,2.05780046852841,2.06763838032658,
2.0907492258872,2.11985991651743,2.12347708723234,2.12577069799239,2.12758844718778,
2.12963392691719,2.13309118363733,2.1474676822273,2.18030996796785,2.19557941550631,
2.19776169421316,2.19907374086217,2.20009333137368,2.2012632832125,2.20333853115487,
2.2132238094026,2.23655464115746,2.26545757916821,2.26907355681657,2.27136517396421,
2.27318051073824,2.27522236239165,2.27867116351496,2.29297117305714,2.32542129106005,
2.33366690394975,2.34180525325721,2.34382697877215,2.34499712305827,2.34591425164786,
2.34719192709616,2.34977952899999,2.37447329543612,2.40897414384731,2.41433829493518,
2.41674135846877,2.41857871311583,2.42054835059226,2.42365963261701,2.43399481303058,
2.45197144537995,2.47961394855035,2.48744011589297,2.48943851321585,2.49060482548682,
2.49152667176838,2.49282038950961,2.49547135894722,2.51680170906175,2.55487684006113,
2.55982438698553,2.56217952473733,2.56400748672678,2.56602509832581,2.56934289824803,
2.58184463659192,2.60541404761194,2.63028997449203,2.63388567973593,2.6352385295489,
2.63620312834631,2.63724143592376,2.63872672719072,2.64253391123869,2.64817938671692,
2.66657909981711,2.70000646731652,2.70544755102859,2.70785350904814,2.70968040878739,
2.71162645737796,2.7146740301476,2.72454162917124,2.74132224400079,2.76169470610199,
2.76410463468713),.UNSPECIFIED.);
#1556=B_SPLINE_CURVE_WITH_KNOTS('',3,(#108000,#108001,#108002,#108003,#108004,
#108005,#108006,#108007,#108008,#108009,#108010,#108011,#108012,#108013,
#108014,#108015,#108016,#108017,#108018,#108019,#108020,#108021,#108022,
#108023,#108024,#108025,#108026,#108027,#108028,#108029,#108030,#108031,
#108032,#108033,#108034,#108035,#108036,#108037,#108038,#108039,#108040,
#108041,#108042,#108043,#108044,#108045,#108046,#108047,#108048,#108049,
#108050,#108051,#108052,#108053,#108054,#108055,#108056,#108057,#108058,
#108059,#108060,#108061,#108062,#108063,#108064,#108065,#108066,#108067,
#108068,#108069,#108070,#108071,#108072,#108073,#108074,#108075,#108076,
#108077,#108078,#108079,#108080,#108081,#108082,#108083,#108084,#108085,
#108086,#108087,#108088,#108089,#108090,#108091,#108092,#108093,#108094,
#108095,#108096,#108097,#108098,#108099,#108100,#108101,#108102,#108103,
#108104,#108105,#108106,#108107,#108108,#108109,#108110,#108111,#108112,
#108113,#108114,#108115,#108116,#108117,#108118,#108119,#108120,#108121,
#108122,#108123,#108124,#108125,#108126,#108127,#108128,#108129,#108130,
#108131,#108132,#108133,#108134,#108135,#108136,#108137,#108138,#108139,
#108140,#108141,#108142,#108143,#108144,#108145,#108146,#108147,#108148,
#108149,#108150,#108151,#108152,#108153,#108154,#108155,#108156,#108157,
#108158,#108159,#108160,#108161,#108162,#108163,#108164,#108165,#108166,
#108167,#108168,#108169,#108170,#108171,#108172,#108173,#108174,#108175,
#108176,#108177,#108178,#108179,#108180,#108181,#108182,#108183,#108184,
#108185,#108186,#108187,#108188,#108189,#108190,#108191,#108192,#108193,
#108194,#108195,#108196,#108197,#108198,#108199,#108200,#108201,#108202,
#108203,#108204,#108205,#108206,#108207,#108208,#108209),.UNSPECIFIED.,
 .F.,.F.,(4,2,2,2,2,2,2,2,2,2,2,2,2,2,2,2,2,2,2,2,2,2,2,2,2,2,2,2,2,2,2,
2,2,2,2,2,2,2,2,2,2,2,2,2,2,2,2,2,2,2,2,2,2,2,2,2,2,2,2,2,2,2,2,2,2,2,2,
2,2,2,2,2,2,2,2,2,2,2,2,2,2,2,2,2,2,2,2,2,2,2,2,2,2,2,2,2,2,2,2,2,2,2,2,
2,4),(0.000399761267031184,0.0354038923493914,0.0475757413653406,0.0507498700600226,
0.052665118299736,0.054389506155791,0.0565945699565813,0.0601266017211276,
0.0900469725943057,0.106246160835366,0.118415915794598,0.124896777653985,
0.126616318895631,0.127551727208082,0.128562730137273,0.129856744256951,
0.131930054904672,0.143969798295755,0.146782220099005,0.183594347104414,
0.195488779260129,0.198784031837144,0.200815362002396,0.202674196585776,
0.205055700711521,0.210174161082761,0.245387517317568,0.267665523710923,
0.270379134128065,0.27170439868395,0.272745129037137,0.273965945445756,
0.27617422487073,0.286798406387755,0.312242333914371,0.33398952117668,0.340471820486383,
0.343097120955262,0.344972310462606,0.346671748477799,0.349365105914915,
0.354370088839332,0.386014049197861,0.411288245845744,0.415452225451261,
0.416999251761255,0.418055054273712,0.419004476870668,0.420311502973881,
0.423621027919398,0.454287009212792,0.470716343632252,0.484712895793224,
0.488126907672694,0.490153489225955,0.49195839668569,0.494240923051114,
0.497850101060658,0.526477617454613,0.547091629527813,0.559923356448015,
0.5621323675004,0.563326159800845,0.564339340622975,0.565627166301655,0.567680293843476,
0.579345217611069,0.591205943481146,0.617373085928431,0.62612762103121,
0.632333551642897,0.634910852335761,0.636773918413517,0.638477516374394,
0.640773585663114,0.645266778309606,0.682999264416808,0.704568513315369,
0.707226533438398,0.708521799455347,0.709541217013154,0.710745881195248,
0.712911733600078,0.723032759100198,0.727043210822709,0.729718387332021,
0.755044277666134,0.773420450493433,0.778249639393888,0.780579516497017,
0.782401446758974,0.784426227990873,0.787788000658176,0.799378632288752,
0.841947045258856,0.848135232477724,0.852218090185299,0.853752224696319,
0.854804710603946,0.855760817272099,0.857083418788338,0.860466964580924,
0.890220433337641,0.910689042243752,0.92190171802025),.UNSPECIFIED.);
#1557=B_SPLINE_CURVE_WITH_KNOTS('',3,(#108214,#108215,#108216,#108217,#108218,
#108219,#108220,#108221,#108222,#108223,#108224,#108225,#108226,#108227,
#108228,#108229,#108230,#108231,#108232,#108233,#108234,#108235,#108236,
#108237,#108238,#108239,#108240,#108241,#108242,#108243,#108244,#108245,
#108246,#108247,#108248,#108249,#108250,#108251,#108252,#108253,#108254,
#108255,#108256,#108257,#108258,#108259,#108260,#108261,#108262,#108263,
#108264,#108265,#108266,#108267,#108268,#108269,#108270,#108271,#108272,
#108273,#108274,#108275,#108276,#108277,#108278,#108279,#108280,#108281,
#108282,#108283,#108284,#108285,#108286,#108287,#108288,#108289,#108290,
#108291,#108292,#108293,#108294,#108295,#108296,#108297,#108298,#108299,
#108300,#108301,#108302,#108303,#108304,#108305,#108306,#108307,#108308,
#108309,#108310,#108311,#108312,#108313,#108314,#108315,#108316,#108317,
#108318,#108319,#108320,#108321,#108322,#108323,#108324,#108325,#108326,
#108327,#108328,#108329,#108330,#108331,#108332,#108333,#108334,#108335,
#108336,#108337,#108338,#108339,#108340,#108341,#108342,#108343,#108344,
#108345,#108346,#108347,#108348,#108349,#108350,#108351,#108352,#108353,
#108354,#108355,#108356,#108357,#108358,#108359,#108360,#108361,#108362,
#108363,#108364,#108365,#108366,#108367,#108368,#108369,#108370,#108371,
#108372,#108373,#108374,#108375,#108376,#108377,#108378,#108379,#108380,
#108381,#108382,#108383,#108384,#108385,#108386,#108387,#108388,#108389,
#108390,#108391,#108392,#108393,#108394,#108395,#108396,#108397,#108398,
#108399,#108400,#108401,#108402,#108403,#108404,#108405,#108406,#108407,
#108408,#108409,#108410,#108411,#108412,#108413,#108414,#108415,#108416,
#108417,#108418,#108419,#108420,#108421,#108422,#108423,#108424,#108425,
#108426,#108427,#108428,#108429,#108430,#108431,#108432,#108433,#108434,
#108435,#108436,#108437,#108438,#108439),.UNSPECIFIED.,.F.,.F.,(4,2,2,2,
2,2,2,2,2,2,2,2,2,2,2,2,2,2,2,2,2,2,2,2,2,2,2,2,2,2,2,2,2,2,2,2,2,2,2,2,
2,2,2,2,2,2,2,2,2,2,2,2,2,2,2,2,2,2,2,2,2,2,2,2,2,2,2,2,2,2,2,2,2,2,2,2,
2,2,2,2,2,2,2,2,2,2,2,2,2,2,2,2,2,2,2,2,2,2,2,2,2,2,2,2,2,2,2,2,2,2,2,2,
4),(0.921274759476541,0.924524411894003,0.955331798003363,0.959422856744768,
0.961603573824362,0.963395822341905,0.965516884118037,0.969223274006393,
0.985857093836077,1.01696676767491,1.03138812448544,1.03366693698771,1.03488127566808,
1.03589622863804,1.03717033314132,1.03917954371989,1.04997318880504,1.05265600228155,
1.08186307806757,1.09977080420862,1.10453584607552,1.10685232120785,1.10867157897424,
1.11070145120502,1.11409077440169,1.12599154243361,1.16095164213714,1.17685574226388,
1.17917915286552,1.18040290371243,1.18141747464084,1.18268080075765,1.18511783643431,
1.20349893626503,1.22149443631757,1.24307009577738,1.24935689449321,1.25194300601702,
1.25380372500567,1.25549917215905,1.25820575250134,1.26478119621306,1.31031020571826,
1.32265634058214,1.32485719315882,1.32605508245878,1.32707145396758,1.32836675455236,
1.33044575510915,1.3426550143206,1.36815018997544,1.39012680899947,1.39540978244704,
1.39782386678021,1.39965605896793,1.40163761979861,1.40480551002242,1.4146607053459,
1.42229412958812,1.45359912969482,1.46807335298029,1.47035423351201,1.4715691418609,
1.47258425799189,1.47385817109101,1.47586635828403,1.48663455185492,1.4896662483066,
1.49249726537156,1.51493078383045,1.53027695283092,1.539414452834,1.54249483493583,
1.54445737325793,1.54629679572344,1.54875777245418,1.55430187765757,1.56186146207899,
1.58293176552634,1.61176482372921,1.61518699948736,1.61651638768316,1.61747468620137,
1.61852595728505,1.62005310375601,1.62408744207596,1.63017736529024,1.65120863598262,
1.68079438459942,1.68637268739585,1.68859338931337,1.6904442269639,1.69235013975978,
1.69516439833821,1.70299321625123,1.71498283316381,1.73443750721181,1.75705093740503,
1.76066437161217,1.76216918606104,1.76320562397846,1.76429856794156,1.76602209698975,
1.77158289560727,1.78110162991792,1.81063415071968,1.81946693363781,1.83015165068634,
1.83341301906289,1.83541489534002,1.8372406717015,1.83961003620665,1.84269843666847),
 .UNSPECIFIED.);
#1558=B_SPLINE_CURVE_WITH_KNOTS('',3,(#108440,#108441,#108442,#108443,#108444,
#108445,#108446,#108447,#108448,#108449,#108450,#108451,#108452,#108453,
#108454,#108455,#108456,#108457,#108458,#108459,#108460,#108461,#108462,
#108463,#108464,#108465,#108466,#108467,#108468,#108469,#108470,#108471,
#108472,#108473,#108474,#108475,#108476,#108477,#108478,#108479,#108480,
#108481,#108482,#108483,#108484,#108485,#108486,#108487,#108488,#108489,
#108490,#108491,#108492,#108493,#108494,#108495,#108496,#108497,#108498,
#108499,#108500,#108501,#108502,#108503,#108504,#108505,#108506,#108507,
#108508,#108509,#108510,#108511,#108512,#108513,#108514,#108515,#108516,
#108517,#108518,#108519,#108520,#108521,#108522,#108523,#108524,#108525,
#108526,#108527,#108528,#108529,#108530,#108531,#108532,#108533,#108534,
#108535,#108536,#108537,#108538,#108539,#108540,#108541,#108542,#108543,
#108544,#108545,#108546,#108547,#108548,#108549,#108550,#108551,#108552,
#108553,#108554,#108555,#108556,#108557,#108558,#108559,#108560,#108561,
#108562,#108563,#108564,#108565,#108566,#108567,#108568,#108569,#108570,
#108571,#108572,#108573,#108574,#108575,#108576,#108577,#108578,#108579,
#108580,#108581,#108582,#108583,#108584,#108585,#108586,#108587,#108588,
#108589,#108590,#108591,#108592,#108593,#108594,#108595,#108596,#108597,
#108598,#108599,#108600,#108601,#108602,#108603,#108604,#108605,#108606,
#108607,#108608,#108609,#108610,#108611,#108612,#108613,#108614,#108615,
#108616,#108617,#108618,#108619,#108620,#108621,#108622,#108623,#108624,
#108625,#108626,#108627,#108628,#108629,#108630,#108631,#108632,#108633,
#108634,#108635,#108636,#108637,#108638,#108639,#108640,#108641,#108642,
#108643,#108644,#108645,#108646,#108647,#108648,#108649,#108650,#108651,
#108652,#108653,#108654,#108655,#108656,#108657,#108658,#108659,#108660,
#108661),.UNSPECIFIED.,.F.,.F.,(4,2,2,2,2,2,2,2,2,2,2,2,2,2,2,2,2,2,2,2,
2,2,2,2,2,2,2,2,2,2,2,2,2,2,2,2,2,2,2,2,2,2,2,2,2,2,2,2,2,2,2,2,2,2,2,2,
2,2,2,2,2,2,2,2,2,2,2,2,2,2,2,2,2,2,2,2,2,2,2,2,2,2,2,2,2,2,2,2,2,2,2,2,
2,2,2,2,2,2,2,2,2,2,2,2,2,2,2,2,2,2,4),(0.92190171802025,0.925097910706482,
0.927084696020978,0.928913322374671,0.931310420781255,0.936506460788974,
0.957770258313368,0.973175329250713,0.983438581459966,0.987675120157475,
0.996629540026158,0.998716171406378,0.999901209099351,1.00091874235883,
1.00223071662206,1.00499115134119,1.00869107710742,1.0180788219129,1.04664205552107,
1.06617808787567,1.06967778928561,1.07193602825733,1.07375094123707,1.07582039705739,
1.07938621299087,1.09542457581823,1.11663680013027,1.13973400610314,1.14334084377314,
1.1446962004824,1.14566180113158,1.14670751565977,1.14820508355772,1.15204259320464,
1.15773686811606,1.17637540657759,1.20917025715405,1.21463650403762,1.21705734362094,
1.21889732206621,1.22085918985489,1.22393588001835,1.23394551071447,1.2510550158773,
1.2582421502029,1.28540020775133,1.28891275600559,1.29025528172181,1.29121699906627,
1.29226492984325,1.29377560286236,1.29770085892672,1.30357069906719,1.32324230488299,
1.35461883827749,1.35959943289312,1.3622793758212,1.36397023229319,1.36583575939953,
1.36844705828791,1.3748904134451,1.39447773337755,1.41469072131754,1.43260620022306,
1.43503697760918,1.43629902294411,1.43731372504564,1.43853906029758,1.44086913857483,
1.45700189907874,1.4934566391852,1.50393811228342,1.50717790998537,1.50917532561174,
1.51100283650529,1.51338278553973,1.51847989878641,1.53893111871115,1.56585252750646,
1.57836549495523,1.58045703992866,1.5817561783554,1.58277289272859,1.58396806217407,
1.58615622409197,1.59821129282421,1.63932058147671,1.64953330184663,1.65274241570116,
1.65473284787755,1.65656191819012,1.65895539784791,1.66412700780667,1.68518352170173,
1.71636277949963,1.72439866040462,1.72641292229441,1.72758191281659,1.72849976478118,
1.72978084749162,1.73190461240497,1.74724716617857,1.76640326878732,1.79352359501647,
1.79716146568833,1.79946075024912,1.80127830738836,1.80331863519332,1.80675518548761,
1.81087512618335,1.84317688118116),.UNSPECIFIED.);
#1559=B_SPLINE_CURVE_WITH_KNOTS('',3,(#108666,#108667,#108668,#108669,#108670,
#108671,#108672,#108673,#108674,#108675,#108676,#108677,#108678,#108679,
#108680,#108681,#108682,#108683,#108684,#108685,#108686,#108687,#108688,
#108689,#108690,#108691,#108692,#108693,#108694,#108695,#108696,#108697,
#108698,#108699,#108700,#108701,#108702,#108703,#108704,#108705,#108706,
#108707,#108708,#108709,#108710,#108711,#108712,#108713,#108714,#108715,
#108716,#108717,#108718,#108719,#108720,#108721,#108722,#108723,#108724,
#108725,#108726,#108727,#108728,#108729,#108730,#108731,#108732,#108733,
#108734,#108735,#108736,#108737,#108738,#108739,#108740,#108741,#108742,
#108743,#108744,#108745,#108746,#108747,#108748,#108749,#108750,#108751,
#108752,#108753,#108754,#108755,#108756,#108757,#108758,#108759,#108760,
#108761,#108762,#108763,#108764,#108765,#108766,#108767,#108768,#108769,
#108770,#108771,#108772,#108773,#108774,#108775,#108776,#108777,#108778,
#108779,#108780,#108781,#108782,#108783,#108784,#108785,#108786,#108787,
#108788,#108789,#108790,#108791,#108792,#108793,#108794,#108795,#108796,
#108797,#108798,#108799,#108800,#108801,#108802,#108803,#108804,#108805,
#108806,#108807,#108808,#108809,#108810,#108811,#108812,#108813,#108814,
#108815,#108816,#108817,#108818,#108819,#108820,#108821,#108822,#108823,
#108824,#108825,#108826,#108827,#108828,#108829,#108830,#108831,#108832,
#108833,#108834,#108835,#108836,#108837,#108838,#108839,#108840,#108841,
#108842,#108843,#108844,#108845,#108846,#108847,#108848,#108849,#108850,
#108851,#108852,#108853,#108854,#108855,#108856,#108857,#108858,#108859,
#108860,#108861,#108862,#108863,#108864,#108865,#108866,#108867,#108868,
#108869,#108870,#108871,#108872,#108873,#108874,#108875,#108876,#108877,
#108878,#108879,#108880,#108881,#108882,#108883,#108884,#108885,#108886,
#108887,#108888,#108889,#108890,#108891,#108892,#108893),.UNSPECIFIED.,
 .F.,.F.,(4,2,2,2,2,2,2,2,2,2,2,2,2,2,2,2,2,2,2,2,2,2,2,2,2,2,2,2,2,2,2,
2,2,2,2,2,2,2,2,2,2,2,2,2,2,2,2,2,2,2,2,2,2,2,2,2,2,2,2,2,2,2,2,2,2,2,2,
2,2,2,2,2,2,2,2,2,2,2,2,2,2,2,2,2,2,2,2,2,2,2,2,2,2,2,2,2,2,2,2,2,2,2,2,
2,2,2,2,2,2,2,2,2,2,4),(4.49376522957252E-6,0.0113749598956965,0.0134880192968926,
0.0148074797055664,0.0158105913397222,0.0168025881782626,0.0179570993091921,
0.0199588523548088,0.0275744334940921,0.0360676976962523,0.0572160554608524,
0.0784496470980371,0.0849223676533522,0.0875381455987711,0.0894043571962459,
0.0910941380961687,0.0933466673929254,0.0988936033675317,0.126711578100134,
0.15507441798845,0.158036127799285,0.159694246096322,0.161135006931926,
0.162159328346036,0.163123845402985,0.164477241892783,0.168074683343924,
0.192464336244554,0.216639861558587,0.224814997892535,0.230701699195563,
0.233221644257129,0.235070576775565,0.237011650843792,0.239993831612372,
0.248373108130774,0.282724568528582,0.30315163536191,0.305735969210109,
0.307013139536424,0.307930581823168,0.309102313519474,0.311128464198215,
0.31930797917579,0.327554693713002,0.35997370661674,0.374270283175109,0.377720789227907,
0.37976413006942,0.381581109297172,0.38387525716595,0.387496190613368,0.415890591675,
0.436204773794535,0.449272756508166,0.451502939303418,0.452706982936574,
0.453722661868401,0.455009545124361,0.457060891247674,0.468707123699906,
0.480836271109797,0.516828243065623,0.522093530004954,0.524504143723025,
0.526335580309462,0.528318145672917,0.531491623640803,0.541397178631337,
0.542970680625468,0.551183071007714,0.58068522568375,0.590195560937992,
0.595753192085045,0.597476286851616,0.598569096853285,0.599605380326054,
0.601110136357807,0.604724377492192,0.62732722199006,0.646761316862511,
0.658778929904398,0.666619693918354,0.669435117988138,0.671340922475368,
0.67319096938632,0.675409888769996,0.680979216055241,0.710960536998371,
0.731661901303821,0.737698859777822,0.741707139166819,0.743230138372334,
0.744280374734848,0.745239226719529,0.746571257485783,0.750011520669876,
0.778505048035367,0.80966618209178,0.813804912842453,0.815995537387778,
0.817629170845031,0.819683532644638,0.823184844153557,0.836310774560698,
0.877142334794315,0.883241525653986,0.887280458946217,0.888808027493967,
0.889859184779243,0.890817113530748,0.892145560971097,0.89556282049056,
0.921274759476541),.UNSPECIFIED.);
#1560=B_SPLINE_CURVE_WITH_KNOTS('',3,(#108895,#108896,#108897,#108898),
 .UNSPECIFIED.,.F.,.F.,(4,4),(1.84317688118116,1.84330550588385),
 .UNSPECIFIED.);
#1561=B_SPLINE_CURVE_WITH_KNOTS('',3,(#108899,#108900,#108901,#108902,#108903,
#108904,#108905,#108906,#108907,#108908,#108909,#108910,#108911,#108912,
#108913,#108914,#108915,#108916,#108917,#108918,#108919,#108920,#108921,
#108922,#108923,#108924,#108925,#108926,#108927,#108928,#108929,#108930,
#108931,#108932,#108933,#108934,#108935,#108936,#108937,#108938,#108939,
#108940,#108941,#108942,#108943,#108944,#108945,#108946,#108947,#108948,
#108949,#108950,#108951,#108952,#108953,#108954,#108955,#108956,#108957,
#108958,#108959,#108960,#108961,#108962,#108963,#108964,#108965,#108966,
#108967,#108968,#108969,#108970,#108971,#108972,#108973,#108974,#108975,
#108976,#108977,#108978,#108979,#108980,#108981,#108982,#108983,#108984,
#108985,#108986,#108987,#108988,#108989,#108990,#108991,#108992,#108993,
#108994,#108995,#108996,#108997,#108998,#108999,#109000,#109001,#109002,
#109003,#109004,#109005,#109006,#109007,#109008,#109009,#109010,#109011,
#109012,#109013,#109014,#109015,#109016,#109017,#109018,#109019,#109020,
#109021,#109022,#109023,#109024,#109025,#109026,#109027,#109028,#109029,
#109030,#109031,#109032,#109033,#109034,#109035,#109036,#109037,#109038,
#109039,#109040,#109041,#109042,#109043,#109044,#109045,#109046,#109047,
#109048,#109049,#109050,#109051,#109052,#109053,#109054,#109055,#109056,
#109057,#109058,#109059,#109060,#109061,#109062,#109063,#109064,#109065,
#109066,#109067,#109068,#109069,#109070,#109071,#109072,#109073,#109074,
#109075,#109076,#109077,#109078,#109079,#109080,#109081,#109082,#109083,
#109084,#109085,#109086,#109087,#109088,#109089,#109090,#109091,#109092,
#109093,#109094,#109095,#109096,#109097,#109098,#109099,#109100,#109101,
#109102,#109103,#109104,#109105,#109106,#109107,#109108,#109109,#109110,
#109111,#109112,#109113,#109114,#109115),.UNSPECIFIED.,.F.,.F.,(4,3,3,3,
3,3,3,3,3,3,3,3,3,3,3,3,3,3,3,3,3,3,3,3,3,3,3,3,3,3,3,3,3,3,3,3,3,3,3,3,
3,3,3,3,3,3,3,3,3,3,3,3,3,3,3,3,3,3,3,3,3,3,3,3,3,3,3,3,3,3,3,3,4),(13.68911242082,
13.8012112614014,13.8476634851164,13.8954754250497,13.8955135655797,13.999451658463,
14.008995850694,14.1222765446835,14.235445226898,14.3485466996653,14.461625665281,
14.5748085635747,14.6880430109893,14.801490990776,14.8880121102273,14.8880502488354,
14.9919884088926,15.0015323678574,15.1148128939076,15.2279814071832,15.3410827103216,
15.4541615059267,15.5673442349873,15.6805785133411,15.7940263264698,15.8805487922504,
15.880586932091,15.9845249283623,15.9940689917698,16.1073494559926,16.220517905967,
16.3336191444456,16.4466978741456,16.5598805358895,16.6731147460388,16.7865624903498,
16.8730854756924,16.8731236153467,16.9770616866453,16.9866057538221,17.099886298756,
17.2130548305512,17.3261561518109,17.4392349651043,17.5524177110341,17.6656520058279,
17.779099834481,17.8656221591762,17.8656602986024,17.9695983715848,17.9791424083181,
18.0924229240761,18.2055914264633,18.3186927181367,18.4317715017191,18.5449542179834,
18.6581884830913,18.7716362823968,18.8581588422516,18.8581969818581,18.9621350335285,
18.9716790865825,19.0849595970672,19.1981280940124,19.311229380085,19.4243081579174,
19.5374908682451,19.6507251273037,19.7641729204494,19.8506955255481,19.8507336651138,
19.9606220100522,19.9722977279996),.UNSPECIFIED.);
#1562=B_SPLINE_CURVE_WITH_KNOTS('',3,(#109120,#109121,#109122,#109123,#109124,
#109125,#109126,#109127,#109128,#109129,#109130,#109131,#109132,#109133,
#109134,#109135,#109136,#109137,#109138,#109139,#109140,#109141,#109142,
#109143,#109144,#109145,#109146,#109147,#109148,#109149,#109150,#109151,
#109152,#109153,#109154,#109155,#109156,#109157,#109158,#109159,#109160,
#109161,#109162,#109163,#109164,#109165,#109166,#109167,#109168,#109169,
#109170,#109171,#109172,#109173,#109174,#109175,#109176,#109177,#109178,
#109179,#109180,#109181,#109182,#109183,#109184,#109185,#109186,#109187,
#109188,#109189,#109190,#109191,#109192,#109193,#109194,#109195,#109196,
#109197,#109198,#109199,#109200,#109201,#109202,#109203,#109204,#109205,
#109206,#109207,#109208,#109209,#109210,#109211,#109212,#109213,#109214,
#109215,#109216,#109217,#109218,#109219,#109220,#109221,#109222,#109223,
#109224,#109225,#109226,#109227,#109228,#109229,#109230,#109231,#109232,
#109233,#109234,#109235,#109236,#109237,#109238,#109239,#109240,#109241,
#109242,#109243,#109244,#109245,#109246,#109247,#109248,#109249,#109250,
#109251,#109252,#109253,#109254,#109255,#109256,#109257,#109258,#109259,
#109260,#109261,#109262,#109263,#109264,#109265,#109266,#109267,#109268,
#109269,#109270,#109271,#109272,#109273,#109274,#109275,#109276,#109277,
#109278,#109279,#109280,#109281,#109282,#109283,#109284,#109285,#109286,
#109287,#109288,#109289,#109290,#109291,#109292,#109293,#109294,#109295,
#109296,#109297,#109298,#109299,#109300,#109301,#109302,#109303,#109304,
#109305,#109306,#109307,#109308,#109309,#109310,#109311,#109312,#109313,
#109314,#109315,#109316,#109317,#109318,#109319,#109320,#109321,#109322,
#109323,#109324,#109325,#109326,#109327,#109328,#109329,#109330,#109331,
#109332,#109333,#109334,#109335,#109336,#109337,#109338,#109339,#109340,
#109341,#109342,#109343,#109344,#109345,#109346,#109347,#109348,#109349,
#109350,#109351,#109352,#109353,#109354,#109355,#109356,#109357,#109358,
#109359,#109360,#109361,#109362,#109363,#109364,#109365,#109366,#109367,
#109368,#109369,#109370,#109371,#109372,#109373,#109374,#109375,#109376,
#109377),.UNSPECIFIED.,.F.,.F.,(4,2,2,2,2,2,2,2,2,2,2,2,2,2,2,2,2,2,2,2,
2,2,2,2,2,2,2,2,2,2,2,2,2,2,2,2,2,2,2,2,2,2,2,2,2,2,2,2,2,2,2,2,2,2,2,2,
2,2,2,2,2,2,2,2,2,2,2,2,2,2,2,2,2,2,2,2,2,2,2,2,2,2,2,2,2,2,2,2,2,2,2,2,
2,2,2,2,2,2,2,2,2,2,2,2,2,2,2,2,2,2,2,2,2,2,2,2,2,2,2,2,2,2,2,2,2,2,2,2,
4),(0.922139440865828,0.953161415715388,0.960070350467286,0.966684456462424,
0.974893849796186,0.983240001336062,0.985280283945809,0.986455441762326,
0.987372658490879,0.988645784439311,0.991208908371169,1.0165377107103,1.05031292538638,
1.05565375139298,1.05787146489727,1.05972153203008,1.06162841902405,1.06444745047457,
1.07231177019854,1.08437694587395,1.10375333853131,1.12632352907967,1.12993886186585,
1.1314439924651,1.13248052705378,1.13357358898686,1.13529706938882,1.14085570542365,
1.15036854728225,1.1798557258133,1.18740497453879,1.19920015955819,1.20258020649556,
1.20460835140601,1.20642847238205,1.2087493603968,1.21353550303919,1.23159331623799,
1.26211195449628,1.27398281603662,1.27604748238435,1.27733851605856,1.27835464359757,
1.27955588455904,1.28177228045122,1.29448592749055,1.31511396218002,1.34360777637861,
1.34723187230794,1.34952719116486,1.35134458534677,1.35338785267183,1.35683692442122,
1.37110761611683,1.40338692627428,1.41159532411027,1.4199426259377,1.42198289882,
1.42315799672873,1.42407513359945,1.42534810609123,1.42791077319943,1.45265599708845,
1.48708157408453,1.49244446000674,1.49484683517825,1.49668361576894,1.49865258852215,
1.50176269713238,1.51209197701971,1.53004901964931,1.55762230298695,1.56557556032801,
1.56758315935155,1.56875071076571,1.5696689337195,1.57095246361897,1.57356834085825,
1.5770218829926,1.61048168844067,1.6347604555478,1.63838350743291,1.64067839881354,
1.64249560152849,1.64453880845312,1.64798815508236,1.66226594370436,1.69458698710231,
1.71045749788657,1.71265232222996,1.71396793566005,1.71498820834799,1.71499796917578,
1.71500738331674,1.71501646633788,1.71502523288589,1.71503369678327,1.71504187112695,
1.7150497682493,1.71505739984063,1.71506477701247,1.71507191024131,1.71507880947977,
1.71508548416404,1.71509194327339,1.71509819529474,1.71510424831747,1.71511011006787,
1.71511578784317,1.71512128870614,1.71512661920111,1.7151317857507,1.71513815154595,
1.71514447543104,1.71515075816516,1.7163638142909,1.71860029211483,1.72150504753066,
1.72809902616017,1.74872291573315,1.77787840905959,1.78346175125323,1.78568304986354,
1.78753384311899,1.78943915203532,1.79225146421474,1.80006782415327,1.81203164969954,
1.84370254741232),.UNSPECIFIED.);
#1563=B_SPLINE_CURVE_WITH_KNOTS('',3,(#109378,#109379,#109380,#109381,#109382,
#109383,#109384,#109385,#109386,#109387,#109388,#109389,#109390,#109391,
#109392,#109393,#109394,#109395,#109396,#109397,#109398,#109399,#109400,
#109401,#109402,#109403,#109404,#109405,#109406,#109407,#109408,#109409,
#109410,#109411,#109412,#109413,#109414,#109415,#109416,#109417,#109418,
#109419,#109420,#109421,#109422,#109423,#109424,#109425,#109426,#109427,
#109428,#109429,#109430,#109431,#109432,#109433,#109434,#109435,#109436,
#109437,#109438,#109439,#109440,#109441,#109442,#109443,#109444,#109445,
#109446,#109447,#109448,#109449,#109450,#109451,#109452,#109453,#109454,
#109455,#109456,#109457,#109458,#109459,#109460,#109461,#109462,#109463,
#109464,#109465,#109466,#109467,#109468,#109469,#109470,#109471,#109472,
#109473,#109474,#109475,#109476,#109477,#109478,#109479,#109480,#109481,
#109482,#109483,#109484,#109485,#109486,#109487,#109488,#109489,#109490,
#109491,#109492,#109493,#109494,#109495,#109496,#109497,#109498,#109499,
#109500,#109501,#109502,#109503,#109504,#109505,#109506,#109507,#109508,
#109509,#109510,#109511,#109512,#109513,#109514,#109515,#109516,#109517,
#109518,#109519,#109520,#109521,#109522,#109523,#109524,#109525,#109526,
#109527,#109528,#109529,#109530,#109531,#109532,#109533,#109534,#109535,
#109536,#109537,#109538,#109539,#109540,#109541,#109542,#109543,#109544,
#109545,#109546,#109547,#109548,#109549),.UNSPECIFIED.,.F.,.F.,(4,3,3,3,
3,3,3,3,3,3,3,3,3,3,3,3,3,3,3,3,3,3,3,3,3,3,3,3,3,3,3,3,3,3,3,3,3,3,3,3,
3,3,3,3,3,3,3,3,3,3,3,3,3,3,3,3,3,4),(19.9723059855781,20.0841134945368,
20.1957886725539,20.3073787092846,20.4189306526368,20.5305707429868,20.6422527284484,
20.7541428742084,20.8432703483695,20.9567524590299,21.0700329756447,21.1832014788343,
21.2963027712539,21.4093815555251,21.5225642723825,21.6357985380314,21.749246337785,
21.8358070316252,21.9492891420776,22.0625696584554,22.1757381613903,22.2888394535383,
22.4019182375211,22.5151009540661,22.6283352193889,22.7417830187978,22.8283437148809,
22.9418258267259,23.0551063445343,23.1682748489219,23.281376142542,23.3944549280137,
23.5076376460622,23.6208719128987,23.7343197138193,23.8208803981366,23.9343625092453,
24.0476430263037,24.1608115299334,24.2739128227892,24.3869916074918,24.5001743247693,
24.6134085908326,24.7268563909863,24.8134170813922,24.9268991925426,25.0401797096401,
25.1533482133074,25.2664495061991,25.3795282909356,25.4927110082443,25.6059452743375,
25.7193930745179,25.8059537646479,25.9278422858354,26.0494238170588,26.1705511115848,
26.2554797039036),.UNSPECIFIED.);
#1564=B_SPLINE_CURVE_WITH_KNOTS('',3,(#109554,#109555,#109556,#109557,#109558,
#109559,#109560,#109561,#109562,#109563,#109564,#109565,#109566,#109567,
#109568,#109569,#109570,#109571,#109572,#109573,#109574,#109575,#109576,
#109577,#109578,#109579,#109580,#109581,#109582,#109583,#109584,#109585,
#109586,#109587,#109588,#109589,#109590,#109591,#109592,#109593,#109594,
#109595,#109596,#109597,#109598,#109599,#109600,#109601,#109602,#109603,
#109604,#109605,#109606,#109607,#109608,#109609,#109610,#109611,#109612,
#109613,#109614,#109615,#109616,#109617,#109618,#109619,#109620,#109621,
#109622,#109623,#109624,#109625,#109626,#109627,#109628,#109629,#109630,
#109631,#109632,#109633,#109634,#109635,#109636,#109637,#109638,#109639,
#109640,#109641,#109642,#109643,#109644,#109645,#109646,#109647,#109648,
#109649,#109650,#109651,#109652,#109653,#109654,#109655,#109656,#109657,
#109658,#109659,#109660,#109661,#109662,#109663,#109664,#109665,#109666,
#109667,#109668,#109669,#109670,#109671,#109672,#109673,#109674,#109675,
#109676,#109677,#109678,#109679,#109680,#109681,#109682,#109683,#109684,
#109685,#109686,#109687,#109688,#109689,#109690,#109691,#109692,#109693,
#109694,#109695,#109696,#109697,#109698,#109699,#109700,#109701,#109702,
#109703,#109704,#109705,#109706,#109707,#109708,#109709,#109710,#109711,
#109712,#109713,#109714,#109715,#109716,#109717,#109718,#109719,#109720,
#109721,#109722,#109723,#109724,#109725,#109726,#109727,#109728,#109729,
#109730,#109731,#109732,#109733,#109734,#109735,#109736,#109737,#109738,
#109739,#109740,#109741,#109742,#109743,#109744,#109745,#109746,#109747,
#109748,#109749,#109750,#109751,#109752,#109753,#109754,#109755,#109756,
#109757,#109758,#109759,#109760,#109761,#109762,#109763,#109764,#109765,
#109766,#109767,#109768,#109769),.UNSPECIFIED.,.F.,.F.,(4,2,2,2,2,2,2,2,
2,2,2,2,2,2,2,2,2,2,2,2,2,2,2,2,2,2,2,2,2,2,2,2,2,2,2,2,2,2,2,2,2,2,2,2,
2,2,2,2,2,2,2,2,2,2,2,2,2,2,2,2,2,2,2,2,2,2,2,2,2,2,2,2,2,2,2,2,2,2,2,2,
2,2,2,2,2,2,2,2,2,2,2,2,2,2,2,2,2,2,2,2,2,2,2,2,2,2,2,4),(0.000558712531683679,
0.0303543092442183,0.0344908609805544,0.0379383069450645,0.0399809976431443,
0.0417981159065078,0.0440934061081103,0.0477180648270099,0.0722622776020328,
0.0749869819963228,0.0997555196939848,0.109640744976087,0.111729543896498,
0.112929512132167,0.11394554448846,0.115237719811978,0.117306602474994,
0.129280893441805,0.16159069337941,0.173521456781318,0.181321319996906,
0.184131206610329,0.186035860048845,0.187886767504216,0.1901090998719,0.195700035767165,
0.224162151874238,0.251968646416803,0.256299670067604,0.257869230894463,
0.258928906962958,0.25987889161532,0.26117623583237,0.2644087444951,0.295713649201497,
0.315229233110872,0.326117443109647,0.329283463224686,0.331264382741658,
0.333096339254328,0.335469727156021,0.340672970701033,0.383827390725163,
0.400434348289794,0.4027761940494,0.404003857700441,0.405018374805607,0.406277533153869,
0.408695045569298,0.425465295124815,0.450301186885433,0.468800406273494,
0.473645282751628,0.475977321239594,0.477798535307081,0.479820042035368,
0.483170537760421,0.494674489184328,0.537285187064901,0.543472809813753,
0.547555230683006,0.549089351604343,0.550141931368141,0.551098731467874,
0.552422454238078,0.555810070167633,0.585506122805496,0.606010993961614,
0.613449518579923,0.61892458051788,0.621373251721448,0.623210667291422,
0.625177860060438,0.62827992972715,0.637591682420103,0.679744683552076,
0.691878018813171,0.694069754170991,0.695265748816941,0.696282408849505,
0.697580506452813,0.699668595383467,0.712092963746128,0.723610343399227,
0.741761877277822,0.755043043057593,0.760680444658789,0.765089551777033,
0.767336044012604,0.769149314631689,0.771225403452858,0.774732502138415,
0.788414230469905,0.821689367773794,0.837233277445426,0.839547220871354,
0.840769214118043,0.841784174592153,0.843050294866388,0.845499287333106,
0.865954505965287,0.894223465796298,0.907998020110397,0.911411386991672,
0.91344696693094,0.915265905747734,0.917574559839485,0.922139440865828),
 .UNSPECIFIED.);
#1565=B_SPLINE_CURVE_WITH_KNOTS('',3,(#109770,#109771,#109772,#109773,#109774,
#109775,#109776,#109777,#109778,#109779,#109780,#109781,#109782,#109783,
#109784,#109785,#109786,#109787,#109788,#109789,#109790,#109791,#109792,
#109793,#109794,#109795,#109796,#109797,#109798,#109799,#109800,#109801,
#109802,#109803,#109804,#109805,#109806,#109807,#109808,#109809,#109810,
#109811,#109812,#109813,#109814,#109815,#109816,#109817,#109818,#109819,
#109820,#109821,#109822,#109823,#109824,#109825,#109826,#109827,#109828,
#109829,#109830,#109831,#109832,#109833,#109834,#109835,#109836,#109837,
#109838,#109839,#109840,#109841,#109842,#109843,#109844,#109845,#109846,
#109847,#109848,#109849,#109850,#109851,#109852,#109853,#109854,#109855,
#109856,#109857,#109858,#109859,#109860,#109861,#109862,#109863,#109864,
#109865,#109866,#109867,#109868,#109869,#109870,#109871,#109872,#109873,
#109874,#109875,#109876,#109877,#109878,#109879,#109880,#109881,#109882,
#109883,#109884,#109885,#109886,#109887,#109888,#109889,#109890,#109891,
#109892,#109893,#109894,#109895,#109896,#109897,#109898,#109899,#109900,
#109901,#109902,#109903,#109904,#109905,#109906,#109907,#109908,#109909,
#109910,#109911,#109912,#109913,#109914,#109915,#109916,#109917,#109918,
#109919,#109920,#109921,#109922,#109923,#109924,#109925,#109926,#109927,
#109928,#109929,#109930,#109931,#109932,#109933,#109934,#109935,#109936,
#109937,#109938,#109939,#109940,#109941,#109942,#109943,#109944,#109945,
#109946,#109947,#109948,#109949,#109950,#109951,#109952,#109953,#109954,
#109955,#109956,#109957,#109958,#109959,#109960,#109961,#109962,#109963,
#109964,#109965,#109966,#109967,#109968,#109969,#109970,#109971,#109972,
#109973,#109974,#109975,#109976,#109977,#109978,#109979,#109980,#109981,
#109982,#109983,#109984,#109985),.UNSPECIFIED.,.F.,.F.,(4,2,2,2,2,2,2,2,
2,2,2,2,2,2,2,2,2,2,2,2,2,2,2,2,2,2,2,2,2,2,2,2,2,2,2,2,2,2,2,2,2,2,2,2,
2,2,2,2,2,2,2,2,2,2,2,2,2,2,2,2,2,2,2,2,2,2,2,2,2,2,2,2,2,2,2,2,2,2,2,2,
2,2,2,2,2,2,2,2,2,2,2,2,2,2,2,2,2,2,2,2,2,2,2,2,2,2,2,4),(0.000422182612240338,
0.00230014374216202,0.00418583338429343,0.00596491858417384,0.00771271525841758,
0.00944973154873033,0.0123777201742667,0.0203870933818239,0.0605627937106026,
0.0761168735771465,0.0784312785091729,0.0796534600410549,0.0806685514793024,
0.0819348271305579,0.0843841171858574,0.104382579937836,0.122576663950065,
0.145280999014369,0.148333427195791,0.150400475656218,0.152373182422382,
0.154111251266834,0.156408944585511,0.160039881871664,0.188059454648603,
0.208139706469626,0.221770721124928,0.22402290215518,0.22523194661011,0.226247751098447,
0.227529630869021,0.229563449268175,0.240844295685968,0.271961541449092,
0.285120828661717,0.290723548969139,0.295111332127361,0.297353697503326,
0.299150220770967,0.301223834663411,0.304719363941605,0.318295246109952,
0.351664099326014,0.367230453884055,0.369545235222495,0.370767506186816,
0.3717826090661,0.37304882042102,0.375497762863803,0.396202945752565,0.420874676465013,
0.437623398785895,0.441230235107616,0.443308258062966,0.445121673007081,
0.447366353046707,0.45082268889384,0.469222142535316,0.498781851827809,
0.508301678022971,0.513863814481442,0.515587939058819,0.516681321811511,
0.517718093990286,0.519223501774321,0.522838988897575,0.545441218887071,
0.5648714408073,0.576898257533913,0.584744207926846,0.587561166042227,0.58946793066542,
0.591318855504727,0.593538768786578,0.599110321217708,0.629067971135241,
0.655538209718973,0.659781068145504,0.661338661539975,0.662396231688496,
0.663348957744016,0.66465598920104,0.667943249240449,0.698920184128574,
0.718618903341301,0.729572069214626,0.732745430682947,0.734728589991012,
0.7365610307643,0.73893281469556,0.744123389930791,0.787185848366582,0.803911791764828,
0.806257447647684,0.807486269168103,0.808501274453993,0.809760479986267,
0.812176543038197,0.829045135785397,0.848700124576346,0.865507978362181,
0.875400958599596,0.878465684826659,0.880425334127053,0.88226703783853,
0.884695712748449,0.890204221494311,0.922002138176677),.UNSPECIFIED.);
#1566=B_SPLINE_CURVE_WITH_KNOTS('',3,(#109991,#109992,#109993,#109994,#109995,
#109996,#109997,#109998,#109999,#110000,#110001,#110002,#110003,#110004,
#110005,#110006,#110007,#110008,#110009,#110010,#110011,#110012,#110013,
#110014,#110015,#110016,#110017,#110018,#110019,#110020,#110021,#110022,
#110023,#110024,#110025,#110026,#110027,#110028,#110029,#110030,#110031,
#110032,#110033,#110034,#110035,#110036,#110037,#110038,#110039,#110040,
#110041,#110042,#110043,#110044,#110045,#110046,#110047,#110048,#110049,
#110050,#110051,#110052,#110053,#110054,#110055,#110056,#110057,#110058,
#110059,#110060,#110061,#110062,#110063,#110064,#110065,#110066,#110067,
#110068,#110069,#110070,#110071,#110072,#110073,#110074,#110075,#110076,
#110077,#110078,#110079,#110080,#110081,#110082,#110083,#110084,#110085,
#110086,#110087,#110088,#110089,#110090,#110091,#110092,#110093,#110094,
#110095,#110096,#110097,#110098,#110099,#110100,#110101,#110102,#110103,
#110104,#110105,#110106,#110107,#110108,#110109,#110110,#110111,#110112,
#110113,#110114,#110115,#110116,#110117,#110118,#110119,#110120,#110121,
#110122,#110123,#110124,#110125,#110126,#110127,#110128,#110129,#110130,
#110131,#110132,#110133,#110134,#110135,#110136,#110137,#110138,#110139,
#110140,#110141,#110142,#110143,#110144,#110145,#110146,#110147,#110148,
#110149,#110150,#110151,#110152,#110153,#110154,#110155,#110156,#110157,
#110158,#110159,#110160,#110161,#110162,#110163,#110164,#110165,#110166,
#110167,#110168,#110169,#110170,#110171,#110172,#110173,#110174,#110175,
#110176,#110177,#110178,#110179,#110180,#110181,#110182,#110183,#110184,
#110185,#110186,#110187,#110188,#110189,#110190,#110191,#110192,#110193,
#110194,#110195,#110196,#110197,#110198,#110199,#110200,#110201,#110202,
#110203,#110204,#110205,#110206,#110207,#110208,#110209,#110210,#110211,
#110212,#110213,#110214),.UNSPECIFIED.,.F.,.F.,(4,2,2,2,2,2,2,2,2,2,2,2,
2,2,2,2,2,2,2,2,2,2,2,2,2,2,2,2,2,2,2,2,2,2,2,2,2,2,2,2,2,2,2,2,2,2,2,2,
2,2,2,2,2,2,2,2,2,2,2,2,2,2,2,2,2,2,2,2,2,2,2,2,2,2,2,2,2,2,2,2,2,2,2,2,
2,2,2,2,2,2,2,2,2,2,2,2,2,2,2,2,2,2,2,2,2,2,2,2,2,2,2,4),(0.921845214926218,
0.933185665857156,0.935222172523389,0.936504811047572,0.937520568875029,
0.93872876108664,0.940977251501902,0.954508611584695,0.9746858515713,1.00275128291823,
1.00638423902856,1.00868241866071,1.01050035102992,1.01254240697938,1.01598502208849,
1.03015970943304,1.06193105216681,1.0651438398602,1.06804116180917,1.07882417672254,
1.08083336064094,1.08210772416984,1.08312306664836,1.08433808483189,1.08661875864089,
1.10107238885954,1.13228481038067,1.14030868481636,1.14997115109598,1.15311647643279,
1.15509335190042,1.15692764237122,1.15935401267431,1.16470319198419,1.18723475045186,
1.21014043551825,1.21406418367441,1.22443762180443,1.22642542353472,1.22769325366856,
1.22870828008019,1.22992878348522,1.23223563398876,1.24753160356075,1.28027254350274,
1.2946783120448,1.29823574932891,1.30032333808449,1.30213552196335,1.30436639474811,
1.30869856533483,1.33898418905266,1.36806827707569,1.37148173088947,1.37280979136644,
1.3737678006107,1.37481945540795,1.37634844367025,1.38039511824596,1.38651004616567,
1.42760127436187,1.44051355085667,1.44400010440247,1.44605156769803,1.44768605707324,
1.44988189646338,1.45404413600022,1.48365278438462,1.51376647404206,1.51712674083966,
1.51844584242256,1.51940148331546,1.52045534013953,1.52199564666969,1.52612004319726,
1.55091898885604,1.58280166889616,1.5877778859282,1.59045675373167,1.59214749492838,
1.59401335279707,1.59662597448919,1.60307703508295,1.62307231559871,1.64531813048479,
1.66084576219238,1.66303683438019,1.66435138813528,1.66537158163238,1.66654118571843,
1.66846205834106,1.67686343368966,1.69507012178042,1.72436877655217,1.73267275384419,
1.73564405921602,1.7375829769771,1.73943344469706,1.7419611656308,1.74760214046776,
1.76677122254198,1.78338583643667,1.79411356416013,1.80656626655906,1.80865522462919,
1.80995349650304,1.81097004575616,1.81216561218554,1.81344047394473,1.81544462514572,
1.8193297147383,1.84320204160076),.UNSPECIFIED.);
#1567=B_SPLINE_CURVE_WITH_KNOTS('',3,(#110215,#110216,#110217,#110218),
 .UNSPECIFIED.,.F.,.F.,(4,4),(0.000429300473710356,0.000558712531683679),
 .UNSPECIFIED.);
#1568=B_SPLINE_CURVE_WITH_KNOTS('',3,(#110219,#110220,#110221,#110222,#110223,
#110224,#110225,#110226,#110227,#110228,#110229,#110230,#110231,#110232,
#110233,#110234,#110235,#110236,#110237,#110238,#110239,#110240,#110241,
#110242,#110243,#110244,#110245,#110246,#110247,#110248,#110249,#110250,
#110251,#110252,#110253,#110254,#110255,#110256,#110257,#110258,#110259,
#110260,#110261,#110262,#110263,#110264,#110265,#110266,#110267,#110268,
#110269,#110270,#110271,#110272,#110273,#110274,#110275,#110276,#110277,
#110278,#110279,#110280,#110281,#110282,#110283,#110284,#110285,#110286,
#110287,#110288,#110289,#110290,#110291,#110292,#110293,#110294,#110295,
#110296,#110297,#110298,#110299,#110300,#110301,#110302,#110303,#110304,
#110305,#110306,#110307,#110308,#110309,#110310,#110311,#110312,#110313,
#110314,#110315,#110316,#110317,#110318,#110319,#110320,#110321,#110322,
#110323,#110324,#110325,#110326,#110327,#110328,#110329,#110330,#110331,
#110332,#110333,#110334,#110335,#110336,#110337,#110338,#110339,#110340,
#110341,#110342,#110343,#110344,#110345,#110346,#110347,#110348,#110349,
#110350,#110351,#110352,#110353,#110354,#110355,#110356,#110357,#110358,
#110359,#110360,#110361,#110362,#110363,#110364,#110365,#110366,#110367,
#110368,#110369,#110370,#110371,#110372,#110373,#110374,#110375,#110376,
#110377,#110378,#110379,#110380,#110381,#110382,#110383,#110384,#110385,
#110386,#110387,#110388,#110389,#110390,#110391,#110392,#110393,#110394,
#110395,#110396,#110397,#110398,#110399,#110400,#110401,#110402,#110403,
#110404,#110405,#110406,#110407,#110408,#110409,#110410,#110411,#110412,
#110413,#110414,#110415,#110416,#110417,#110418,#110419,#110420,#110421,
#110422,#110423,#110424,#110425,#110426,#110427,#110428,#110429,#110430,
#110431,#110432,#110433,#110434,#110435,#110436,#110437,#110438,#110439,
#110440,#110441,#110442,#110443,#110444,#110445,#110446,#110447,#110448,
#110449,#110450,#110451,#110452,#110453,#110454,#110455,#110456,#110457,
#110458,#110459,#110460,#110461,#110462,#110463,#110464,#110465,#110466,
#110467,#110468,#110469,#110470,#110471,#110472,#110473,#110474,#110475,
#110476,#110477,#110478,#110479,#110480,#110481,#110482,#110483,#110484,
#110485,#110486,#110487,#110488,#110489,#110490,#110491,#110492,#110493,
#110494),.UNSPECIFIED.,.F.,.F.,(4,2,2,2,2,2,2,2,2,2,2,2,2,2,2,2,2,2,2,2,
2,2,2,2,2,2,2,2,2,2,2,2,2,2,2,2,2,2,2,2,2,2,2,2,2,2,2,2,2,2,2,2,2,2,2,2,
2,2,2,2,2,2,2,2,2,2,2,2,2,2,2,2,2,2,2,2,2,2,2,2,2,2,2,2,2,2,2,2,2,2,2,2,
2,2,2,2,2,2,2,2,2,2,2,2,2,2,2,2,2,2,2,2,2,2,2,2,2,2,2,2,2,2,2,2,2,2,2,2,
2,2,2,2,2,2,2,2,2,4),(0.922002138176677,0.922131789127635,0.947522296073982,
0.951107738256752,0.95246009871606,0.953424698801019,0.954471051166437,
0.955971641903355,0.959827837521926,0.965558829801141,0.984405314838493,
1.01693479908309,1.02241727387269,1.02484141956543,1.02668239416404,1.02864386627924,
1.03171688262267,1.04168655480851,1.05869036494434,1.08403387757733,1.08547294910327,
1.09535537305435,1.09750584308617,1.09870630086103,1.09972293521332,1.10101614002484,
1.10367941441332,1.12564258133335,1.16317782650648,1.16822549582711,1.17057117842003,
1.17239989543567,1.1743955840034,1.17762575984179,1.18917875409744,1.22429053049902,
1.22664329023082,1.23051604783466,1.24091404874388,1.24290345746829,1.24417193480783,
1.24518722178763,1.24640775246314,1.24871389701591,1.26397302767487,1.29670077320765,
1.31114866054734,1.31470947035549,1.31679813453431,1.31861071051853,1.32084138108904,
1.32517098489071,1.35535253615668,1.38454718897717,1.38795678901901,1.38928441307581,
1.39024245632873,1.39129456816539,1.39282494946702,1.39687957342737,1.40301033806786,
1.44441098533032,1.45702200878654,1.46048904203517,1.46253654019901,1.4641720245021,
1.46637458813808,1.47056779749672,1.50294552046279,1.53001112150995,1.53353160456391,
1.53487545441299,1.535837703354,1.53688577356658,1.53839588895441,1.54231546557355,
1.54817330944218,1.56776889051933,1.59925863869765,1.60423667737684,1.60691637952539,
1.60860759241162,1.61047393050294,1.61308715706424,1.61953944245918,1.63957040158522,
1.65677472958376,1.67723508763838,1.67967792804942,1.68094281037152,1.68195784567911,
1.68196248270823,1.68196706191326,1.68197158408254,1.68197605008116,1.68198046070088,
1.681984816743,1.68198911896023,1.68199336813537,1.68199756508067,1.68200171046563,
1.68200580505263,1.68200984957442,1.68201384473938,1.6820177912015,1.68202168966647,
1.68202554083482,1.68202934537668,1.68203310397398,1.68203681723418,1.6820404857585,
1.68204411019473,1.68204769117382,1.68205122931632,1.68205472513393,1.68205817914971,
1.68330411708186,1.68575853186955,1.68897844193243,1.69663103748635,1.72203223564396,
1.74714377659505,1.75077373163496,1.75307107170837,1.75488901233754,1.75693179059308,
1.76037737167948,1.77459249516826,1.8070163579622,1.81559012311616,1.82354437268877,
1.82555239270934,1.82672023258885,1.82771964005603,1.82871836377646,1.83002418007741,
1.83210346497329,1.84352467432996),.UNSPECIFIED.);
#1569=B_SPLINE_CURVE_WITH_KNOTS('',3,(#110499,#110500,#110501,#110502,#110503,
#110504,#110505,#110506,#110507,#110508,#110509,#110510,#110511,#110512,
#110513,#110514,#110515,#110516,#110517,#110518,#110519,#110520,#110521,
#110522,#110523,#110524,#110525,#110526,#110527,#110528,#110529,#110530,
#110531,#110532,#110533,#110534,#110535,#110536,#110537,#110538,#110539,
#110540,#110541,#110542,#110543,#110544,#110545,#110546,#110547,#110548,
#110549,#110550,#110551,#110552,#110553,#110554,#110555,#110556,#110557,
#110558,#110559,#110560,#110561,#110562,#110563,#110564,#110565,#110566,
#110567,#110568,#110569,#110570,#110571,#110572,#110573,#110574,#110575,
#110576,#110577,#110578,#110579,#110580,#110581,#110582,#110583,#110584,
#110585,#110586,#110587,#110588,#110589,#110590,#110591,#110592,#110593,
#110594,#110595,#110596,#110597,#110598,#110599,#110600,#110601,#110602,
#110603,#110604,#110605,#110606,#110607,#110608,#110609,#110610,#110611,
#110612,#110613,#110614,#110615,#110616,#110617,#110618,#110619,#110620,
#110621,#110622,#110623,#110624,#110625,#110626,#110627,#110628,#110629,
#110630,#110631,#110632,#110633,#110634,#110635,#110636,#110637,#110638,
#110639,#110640,#110641,#110642,#110643,#110644,#110645,#110646,#110647,
#110648,#110649,#110650,#110651,#110652,#110653,#110654,#110655,#110656,
#110657,#110658,#110659,#110660,#110661,#110662,#110663,#110664,#110665,
#110666,#110667,#110668,#110669,#110670,#110671,#110672,#110673,#110674,
#110675,#110676,#110677,#110678,#110679,#110680,#110681,#110682,#110683,
#110684,#110685,#110686,#110687,#110688,#110689,#110690,#110691,#110692,
#110693,#110694,#110695,#110696,#110697,#110698,#110699,#110700,#110701,
#110702,#110703,#110704,#110705,#110706,#110707,#110708,#110709,#110710,
#110711,#110712,#110713,#110714,#110715,#110716,#110717,#110718),
 .UNSPECIFIED.,.F.,.F.,(4,2,2,2,2,2,2,2,2,2,2,2,2,2,2,2,2,2,2,2,2,2,2,2,
2,2,2,2,2,2,2,2,2,2,2,2,2,2,2,2,2,2,2,2,2,2,2,2,2,2,2,2,2,2,2,2,2,2,2,2,
2,2,2,2,2,2,2,2,2,2,2,2,2,2,2,2,2,2,2,2,2,2,2,2,2,2,2,2,2,2,2,2,2,2,2,2,
2,2,2,2,2,2,2,2,2,2,2,2,2,4),(0.000120839695703934,0.0455676436533427,0.0550891343698512,
0.0606516894268146,0.0623756015464489,0.0634687637408005,0.0645052426716709,
0.0660100725110365,0.0696231998186394,0.0922843274643028,0.11181783426619,
0.123748531195746,0.128991447536211,0.131947275537561,0.134467042128502,
0.136293290822903,0.138149296600383,0.140390278001579,0.145738393914182,
0.178654531865889,0.197203053008805,0.202881542233866,0.2067112609413,0.208207442141353,
0.209252673206656,0.21021779473239,0.211572961825374,0.215182553955673,
0.23798700617635,0.257775853028359,0.269464050009548,0.274634044129374,
0.278751377937892,0.280937964967913,0.28273092729656,0.284848010646145,
0.288535174696274,0.304835818766062,0.336246763738113,0.350751084457187,
0.353033153430974,0.354248397109868,0.355263621792299,0.356537457531062,
0.358545132791956,0.369300041246568,0.372381135434078,0.395793388673595,
0.41827561079411,0.423618630137956,0.426043807151103,0.427877834829059,
0.429855041135546,0.433002223332262,0.442681239081158,0.450642903751783,
0.481867211514867,0.496320526560074,0.498600961178106,0.49981587437733,
0.500831138839873,0.502105422197662,0.504114527114491,0.514896962037762,
0.517875751396225,0.520928015401863,0.546031917750097,0.564584962921893,
0.569437533974991,0.571771361674194,0.57359313080324,0.575614391328937,
0.578962458160321,0.590440704604357,0.633092956662107,0.639283455500257,
0.643367517919966,0.644902088369731,0.645954924471855,0.646911916654801,
0.648235851931401,0.651623728291181,0.68133551695141,0.686131394801075,
0.703281597658528,0.713306480015122,0.716385004602834,0.71834737432617,
0.720187349722236,0.722607486460359,0.72806905981282,0.760980090844152,
0.7795390932919,0.785219751408212,0.789050697621132,0.790547193121992,0.791592588955462,
0.792557818540408,0.79391307831307,0.797522445733084,0.820390828525827,
0.855884129541508,0.860702962130679,0.863030339422605,0.864851396346624,
0.866876307473201,0.870240868187866,0.881862739111313,0.886541005314974,
0.921845214926218),.UNSPECIFIED.);
#1570=B_SPLINE_CURVE_WITH_KNOTS('',3,(#110719,#110720,#110721,#110722,#110723,
#110724,#110725,#110726,#110727,#110728,#110729,#110730,#110731,#110732,
#110733,#110734,#110735,#110736,#110737,#110738,#110739,#110740,#110741,
#110742,#110743,#110744,#110745,#110746,#110747,#110748,#110749,#110750,
#110751,#110752,#110753,#110754,#110755,#110756,#110757,#110758,#110759,
#110760,#110761,#110762,#110763,#110764,#110765,#110766,#110767,#110768,
#110769,#110770,#110771,#110772,#110773,#110774,#110775,#110776,#110777,
#110778,#110779,#110780,#110781,#110782,#110783,#110784,#110785,#110786,
#110787,#110788,#110789,#110790,#110791,#110792,#110793,#110794,#110795,
#110796,#110797,#110798,#110799,#110800,#110801,#110802,#110803,#110804,
#110805,#110806,#110807,#110808,#110809,#110810,#110811,#110812,#110813,
#110814,#110815,#110816,#110817,#110818,#110819,#110820,#110821,#110822,
#110823,#110824,#110825,#110826,#110827,#110828,#110829,#110830,#110831,
#110832,#110833,#110834,#110835,#110836,#110837,#110838,#110839,#110840,
#110841,#110842,#110843,#110844,#110845,#110846,#110847,#110848,#110849,
#110850,#110851,#110852,#110853,#110854,#110855,#110856,#110857,#110858,
#110859,#110860,#110861,#110862,#110863,#110864,#110865,#110866,#110867,
#110868,#110869,#110870,#110871,#110872,#110873,#110874,#110875,#110876,
#110877,#110878,#110879,#110880,#110881,#110882,#110883,#110884,#110885,
#110886,#110887,#110888,#110889,#110890,#110891,#110892,#110893,#110894,
#110895,#110896,#110897,#110898,#110899,#110900,#110901,#110902,#110903,
#110904,#110905,#110906,#110907,#110908,#110909,#110910,#110911,#110912,
#110913,#110914,#110915,#110916,#110917,#110918,#110919,#110920,#110921,
#110922,#110923,#110924,#110925,#110926,#110927,#110928,#110929,#110930,
#110931,#110932,#110933,#110934,#110935,#110936,#110937,#110938,#110939,
#110940,#110941,#110942),.UNSPECIFIED.,.F.,.F.,(4,2,2,2,2,2,2,2,2,2,2,2,
2,2,2,2,2,2,2,2,2,2,2,2,2,2,2,2,2,2,2,2,2,2,2,2,2,2,2,2,2,2,2,2,2,2,2,2,
2,2,2,2,2,2,2,2,2,2,2,2,2,2,2,2,2,2,2,2,2,2,2,2,2,2,2,2,2,2,2,2,2,2,2,2,
2,2,2,2,2,2,2,2,2,2,2,2,2,2,2,2,2,2,2,2,2,2,2,2,2,2,2,4),(0.000514184320873031,
0.0322186784840785,0.0441938112098259,0.0520149769162336,0.0548282071910111,
0.0567339135113913,0.058584925666832,0.0608062843752995,0.0663887988403879,
0.0955079519483176,0.116131054964101,0.122725807482339,0.125630989791039,
0.127867940242788,0.129081184927655,0.129087469474058,0.129093795157261,
0.129100162687236,0.129105332954239,0.12911066715257,0.130125491655159,
0.131388692396932,0.133824279512369,0.152326042020472,0.169802716361319,
0.186945709428819,0.196967096278412,0.200045053451801,0.202007194759573,
0.203847055070414,0.20626719230246,0.211729485227269,0.244585891014861,
0.26316690063735,0.268850870124813,0.272683346994358,0.274180000660141,
0.275225365162193,0.276190464971353,0.277545422311956,0.281153050611057,
0.303754126726062,0.323167822089898,0.335205127653032,0.343055631141181,
0.345872903167848,0.347779507116791,0.349629992462675,0.351849037985281,
0.357416552826848,0.387516011876421,0.408126768213905,0.414149747937819,
0.418151385661808,0.419673682560489,0.420724016585175,0.421683429987472,
0.4230168767433,0.426464788019815,0.454854728526462,0.476229340216446,0.483852718275466,
0.489432482782446,0.491899872705768,0.493740452892699,0.495700825152586,
0.498770695782936,0.507824088981048,0.545879449196452,0.562164090828559,
0.564498207136595,0.565724453773425,0.566739303337916,0.568000770185634,
0.570428049355293,0.588063271096944,0.612153720068695,0.625518049369035,
0.631179069301836,0.635602774794257,0.637852301622535,0.63966591321271,
0.641740092682062,0.645238480806698,0.658855391131439,0.692183590060947,
0.707739687045261,0.710054043955779,0.711276173856409,0.712291207313562,
0.713557391756719,0.716006451735459,0.735899551618312,0.752289842697189,
0.76921558000163,0.779153668774858,0.782222909945432,0.784183305095312,
0.786024204184396,0.788449616088973,0.793941003574496,0.826223971212188,
0.845220450467257,0.850976582094028,0.854845481609915,0.856347829444499,
0.857394365138296,0.858358295379293,0.859708608442635,0.863279237442187,
0.889009418862205,0.92191958549341),.UNSPECIFIED.);
#1571=B_SPLINE_CURVE_WITH_KNOTS('',3,(#110947,#110948,#110949,#110950,#110951,
#110952,#110953,#110954,#110955,#110956,#110957,#110958,#110959,#110960,
#110961,#110962,#110963,#110964,#110965,#110966,#110967,#110968,#110969,
#110970,#110971,#110972,#110973,#110974,#110975,#110976,#110977,#110978,
#110979,#110980,#110981,#110982,#110983,#110984,#110985,#110986,#110987,
#110988,#110989,#110990,#110991,#110992,#110993,#110994,#110995,#110996,
#110997,#110998,#110999,#111000,#111001,#111002,#111003,#111004,#111005,
#111006,#111007,#111008,#111009,#111010,#111011,#111012,#111013,#111014,
#111015,#111016,#111017,#111018,#111019,#111020,#111021,#111022,#111023,
#111024,#111025,#111026,#111027,#111028,#111029,#111030,#111031,#111032,
#111033,#111034,#111035,#111036,#111037,#111038,#111039,#111040,#111041,
#111042,#111043,#111044,#111045,#111046,#111047,#111048,#111049,#111050,
#111051,#111052,#111053,#111054,#111055,#111056,#111057,#111058,#111059,
#111060,#111061,#111062,#111063,#111064,#111065,#111066,#111067,#111068,
#111069,#111070,#111071,#111072,#111073,#111074,#111075,#111076,#111077,
#111078,#111079,#111080,#111081,#111082,#111083,#111084,#111085,#111086,
#111087,#111088,#111089,#111090,#111091,#111092,#111093,#111094,#111095,
#111096,#111097,#111098,#111099,#111100,#111101,#111102,#111103,#111104,
#111105,#111106,#111107,#111108,#111109,#111110,#111111,#111112,#111113,
#111114,#111115,#111116,#111117,#111118,#111119,#111120,#111121,#111122,
#111123,#111124,#111125,#111126,#111127,#111128,#111129,#111130,#111131,
#111132,#111133,#111134,#111135,#111136,#111137,#111138,#111139,#111140,
#111141,#111142,#111143,#111144,#111145,#111146,#111147,#111148,#111149,
#111150,#111151,#111152,#111153,#111154,#111155,#111156,#111157,#111158,
#111159,#111160,#111161,#111162,#111163,#111164,#111165,#111166),
 .UNSPECIFIED.,.F.,.F.,(4,2,2,2,2,2,2,2,2,2,2,2,2,2,2,2,2,2,2,2,2,2,2,2,
2,2,2,2,2,2,2,2,2,2,2,2,2,2,2,2,2,2,2,2,2,2,2,2,2,2,2,2,2,2,2,2,2,2,2,2,
2,2,2,2,2,2,2,2,2,2,2,2,2,2,2,2,2,2,2,2,2,2,2,2,2,2,2,2,2,2,2,2,2,2,2,2,
2,2,2,2,2,2,2,2,2,2,2,2,2,4),(0.921832680523177,0.951032977161874,0.956613964824321,
0.958834794682953,0.960685376336237,0.962590651187675,0.965403259289845,
0.973222741326489,0.985193528648157,1.00466256949375,1.02728211220415,1.03089451980252,
1.03239901474863,1.03343526852322,1.03452819312185,1.03625174106495,1.04181307473724,
1.05133349189691,1.08088344459705,1.09930720423002,1.10276358497415,1.10500771165741,
1.10682030213161,1.10889696018903,1.11250033370256,1.12921009882921,1.15376467379925,
1.17459284352664,1.17704051120357,1.17830608984447,1.17932069367457,1.18054234675118,
1.18285589932244,1.19840529777989,1.23170540104789,1.24536155560679,1.2488659448375,
1.25094094518432,1.25275358269939,1.25499970212062,1.25940944287171,1.26504800019322,
1.27833484108479,1.29645189574596,1.3079441886255,1.3203662744993,1.32245360210224,
1.32375122682387,1.32476751161592,1.32596305047816,1.32815392955443,1.3402803704804,
1.38234634198735,1.39172955958175,1.39483971063103,1.39680814837065,1.39864403995622,
1.40108664199351,1.40653098971685,1.41391570893857,1.43417818860011,1.46419454084351,
1.46755899305462,1.46887846251745,1.46983390239858,1.47088698868382,1.47242524014894,
1.47653862276615,1.48279129753188,1.50489476827277,1.533078641905,1.53812330140673,
1.54081968306867,1.54251297446302,1.54437474523794,1.54696870701772,1.5533071112382,
1.57388359825824,1.59919005058039,1.61141087341261,1.61348962208528,1.61478457351595,
1.61580053022497,1.61699775292987,1.61919697917837,1.63152062131788,1.67666546494988,
1.68352406156949,1.68627876436677,1.6879823432206,1.68979762493318,1.69226298490438,
1.69502133739956,1.69976555012603,1.73494159340071,1.75667848637664,1.75912741496879,
1.76039299721527,1.76140725040061,1.76262805668367,1.76493884462942,1.78041538237603,
1.81943088951654,1.82839248411727,1.83144790437885,1.83340414316616,1.83514031364755,
1.8369292665996,1.83974263793472,1.8430958654942),.UNSPECIFIED.);
#1572=B_SPLINE_CURVE_WITH_KNOTS('',3,(#111167,#111168,#111169,#111170,#111171,
#111172,#111173,#111174,#111175,#111176,#111177,#111178,#111179,#111180,
#111181,#111182,#111183,#111184,#111185,#111186,#111187,#111188,#111189,
#111190,#111191,#111192,#111193,#111194,#111195,#111196,#111197,#111198,
#111199,#111200,#111201,#111202,#111203,#111204,#111205,#111206,#111207,
#111208,#111209,#111210,#111211,#111212,#111213,#111214,#111215,#111216,
#111217,#111218,#111219,#111220,#111221,#111222,#111223,#111224,#111225,
#111226,#111227,#111228,#111229,#111230,#111231,#111232,#111233,#111234,
#111235,#111236,#111237,#111238,#111239,#111240,#111241,#111242,#111243,
#111244,#111245,#111246,#111247,#111248,#111249,#111250,#111251,#111252,
#111253,#111254,#111255,#111256,#111257,#111258,#111259,#111260,#111261,
#111262,#111263,#111264,#111265,#111266,#111267,#111268,#111269,#111270,
#111271,#111272,#111273,#111274,#111275,#111276,#111277,#111278,#111279,
#111280,#111281,#111282,#111283,#111284,#111285,#111286,#111287,#111288,
#111289,#111290,#111291,#111292,#111293,#111294,#111295,#111296,#111297,
#111298,#111299,#111300,#111301,#111302,#111303,#111304,#111305,#111306,
#111307,#111308,#111309,#111310,#111311,#111312,#111313,#111314,#111315,
#111316,#111317,#111318,#111319,#111320,#111321,#111322,#111323,#111324,
#111325,#111326,#111327,#111328,#111329,#111330,#111331,#111332,#111333,
#111334,#111335,#111336,#111337,#111338,#111339,#111340,#111341,#111342,
#111343,#111344,#111345,#111346,#111347,#111348,#111349,#111350,#111351,
#111352,#111353,#111354,#111355,#111356,#111357,#111358,#111359,#111360,
#111361,#111362,#111363,#111364,#111365,#111366,#111367,#111368,#111369,
#111370,#111371,#111372,#111373,#111374,#111375,#111376,#111377,#111378,
#111379,#111380,#111381,#111382,#111383,#111384,#111385,#111386,#111387,
#111388),.UNSPECIFIED.,.F.,.F.,(4,2,2,2,2,2,2,2,2,2,2,2,2,2,2,2,2,2,2,2,
2,2,2,2,2,2,2,2,2,2,2,2,2,2,2,2,2,2,2,2,2,2,2,2,2,2,2,2,2,2,2,2,2,2,2,2,
2,2,2,2,2,2,2,2,2,2,2,2,2,2,2,2,2,2,2,2,2,2,2,2,2,2,2,2,2,2,2,2,2,2,2,2,
2,2,2,2,2,2,2,2,2,2,2,2,2,2,2,2,2,2,4),(0.92191958549341,0.926579367833769,
0.928875863602883,0.930693640011219,0.932736764118459,0.936184217644736,
0.95042734325079,0.982562959212838,0.990740527403718,0.999255938185879,
1.00131180928417,1.00249059598165,1.00349985597227,1.0048175583881,1.00760813821281,
1.01136016505699,1.02094585198147,1.04954070246114,1.06876593590375,1.0722541534795,
1.07450846860991,1.0763224809011,1.07839334864441,1.08196775281062,1.09816144265899,
1.13874778937986,1.14518890231943,1.14708014009456,1.14821055385572,1.1492413755653,
1.15065445406444,1.15397162347375,1.16954739234742,1.21221139447352,1.21745110001137,
1.21983165370702,1.22166528737793,1.22364421626648,1.22679880689785,1.23756332287219,
1.25672146928524,1.28857288534043,1.29176477119561,1.29305538694806,1.29400393063906,
1.2950661999706,1.296646940662,1.30105597602291,1.30792658851252,1.33309893351256,
1.35964455106454,1.36329439381451,1.36559766214912,1.36741612785572,1.36945512801421,
1.37288376923044,1.38686559866481,1.40321928976217,1.43395050049501,1.4372587269574,
1.43856919098321,1.43952270479107,1.44057911084322,1.44213151129411,1.44633885271029,
1.47230005894757,1.5028500438719,1.50840757959098,1.51062507526198,1.51247518831042,
1.51438236205098,1.51720228035824,1.52507231738369,1.53714975234297,1.55650603351655,
1.57906168074817,1.58267700494955,1.58418220527175,1.58521881170999,1.5863119908356,
1.58803575348555,1.59359622787261,1.6031136914262,1.63885803511642,1.65174357722761,
1.6552278030918,1.65727880182868,1.65891342369968,1.66111009559181,1.66527613918819,
1.6705231347409,1.6824671921474,1.71470754108742,1.71491367217198,1.72265956845524,
1.72773985981153,1.72946643764562,1.73045147511664,1.73148368286488,1.73290647421248,
1.73615990929275,1.75408663822514,1.7713270689301,1.79629775262752,1.79992631497513,
1.80222306527678,1.80404072239263,1.80608337483517,1.80952921207148,1.81366286783874,
1.84340367613644),.UNSPECIFIED.);
#1573=B_SPLINE_CURVE_WITH_KNOTS('',3,(#111393,#111394,#111395,#111396,#111397,
#111398,#111399,#111400,#111401,#111402,#111403,#111404,#111405,#111406,
#111407,#111408,#111409,#111410,#111411,#111412,#111413,#111414,#111415,
#111416,#111417,#111418,#111419,#111420,#111421,#111422,#111423,#111424,
#111425,#111426,#111427,#111428,#111429,#111430,#111431,#111432,#111433,
#111434,#111435,#111436,#111437,#111438,#111439,#111440,#111441,#111442,
#111443,#111444,#111445,#111446,#111447,#111448,#111449,#111450,#111451,
#111452,#111453,#111454,#111455,#111456,#111457,#111458,#111459,#111460,
#111461,#111462,#111463,#111464,#111465,#111466,#111467,#111468,#111469,
#111470,#111471,#111472,#111473,#111474,#111475,#111476,#111477,#111478,
#111479,#111480,#111481,#111482,#111483,#111484,#111485,#111486,#111487,
#111488,#111489,#111490,#111491,#111492,#111493,#111494,#111495,#111496,
#111497,#111498,#111499,#111500,#111501,#111502,#111503,#111504,#111505,
#111506,#111507,#111508,#111509,#111510,#111511,#111512,#111513,#111514,
#111515,#111516,#111517,#111518,#111519,#111520,#111521,#111522,#111523,
#111524,#111525,#111526,#111527,#111528,#111529,#111530,#111531,#111532,
#111533,#111534,#111535,#111536,#111537,#111538,#111539,#111540,#111541,
#111542,#111543,#111544,#111545,#111546,#111547,#111548,#111549,#111550,
#111551,#111552,#111553,#111554,#111555,#111556,#111557,#111558,#111559,
#111560,#111561,#111562,#111563,#111564,#111565,#111566,#111567,#111568,
#111569,#111570,#111571,#111572,#111573,#111574,#111575,#111576,#111577,
#111578,#111579,#111580,#111581,#111582,#111583,#111584,#111585,#111586,
#111587,#111588,#111589,#111590,#111591,#111592,#111593,#111594,#111595,
#111596,#111597,#111598,#111599,#111600,#111601,#111602,#111603,#111604,
#111605,#111606,#111607,#111608,#111609,#111610,#111611,#111612,#111613,
#111614,#111615,#111616,#111617,#111618,#111619,#111620,#111621,#111622),
 .UNSPECIFIED.,.F.,.F.,(4,2,2,2,2,2,2,2,2,2,2,2,2,2,2,2,2,2,2,2,2,2,2,2,
2,2,2,2,2,2,2,2,2,2,2,2,2,2,2,2,2,2,2,2,2,2,2,2,2,2,2,2,2,2,2,2,2,2,2,2,
2,2,2,2,2,2,2,2,2,2,2,2,2,2,2,2,2,2,2,2,2,2,2,2,2,2,2,2,2,2,2,2,2,2,2,2,
2,2,2,2,2,2,2,2,2,2,2,2,2,2,2,2,2,2,4),(0.000524403676282058,0.00751668207639485,
0.0113220917333589,0.0126923919885938,0.0137134438502507,0.0146856560546402,
0.0158024627757273,0.0176338610187251,0.0235572436620335,0.0317292774025957,
0.0629190299713805,0.0747436182064204,0.0824932672144701,0.0852963038193244,
0.087199523291428,0.0890514882090771,0.0912780477840168,0.0968959088845208,
0.124749431018032,0.153079850951266,0.156040153453738,0.157697703775962,
0.159139527547368,0.160163533982415,0.161128349344055,0.162482965147253,
0.166090118711053,0.188720406112024,0.208188857076231,0.220173763010725,
0.227999130920155,0.230812466176736,0.232717830737024,0.234568191449988,
0.236788378114272,0.242365757688715,0.271877414054598,0.292940725404047,
0.299034741160938,0.303071100156101,0.304598259348679,0.305649312720744,
0.306607289002639,0.307935985517641,0.31135494875589,0.340267299751136,
0.361293718415928,0.372691770276517,0.375906472201909,0.377898041870809,
0.379726599514782,0.382077088086457,0.387155123112346,0.424392673331689,
0.446555411305695,0.449222961363215,0.450516558468262,0.451532680444599,
0.452731539269522,0.454876778672273,0.464687314003478,0.469655157036567,
0.495011818239325,0.51512094469035,0.520174522354779,0.522546042046933,
0.524372094158481,0.526372895206465,0.529629405671474,0.54026954927466,
0.583854497357847,0.590085995000661,0.594189763049214,0.595726956857285,
0.596780110707899,0.597736229173265,0.599057445976145,0.602430473901178,
0.63236765908882,0.662143556569582,0.666309877185375,0.668506388529733,
0.670140751327125,0.672191244277325,0.675674142610747,0.68854877880188,
0.694838975016591,0.724288494827162,0.733791986315476,0.739346995755445,
0.741069891163162,0.742162718616861,0.743199139318214,0.744704276942378,
0.748320550696405,0.770885068432099,0.790249321996064,0.802335872082938,
0.810209181748124,0.813029139720641,0.814935997355287,0.816785536642284,
0.819002010700611,0.824555192305118,0.855207091332126,0.875403468583031,
0.881359477781386,0.885327824467106,0.886844938876926,0.88789408451025,
0.888854296170021,0.890191313290946,0.893664648804961,0.921702227342705,
0.921832680523177),.UNSPECIFIED.);
#1574=B_SPLINE_CURVE_WITH_KNOTS('',3,(#111624,#111625,#111626,#111627),
 .UNSPECIFIED.,.F.,.F.,(4,4),(1.84340367613644,1.84353373193666),
 .UNSPECIFIED.);
#1575=B_SPLINE_CURVE_WITH_KNOTS('',3,(#111628,#111629,#111630,#111631,#111632,
#111633,#111634,#111635,#111636,#111637,#111638,#111639,#111640,#111641,
#111642,#111643,#111644,#111645,#111646,#111647,#111648,#111649,#111650,
#111651,#111652,#111653,#111654,#111655,#111656,#111657,#111658,#111659,
#111660,#111661,#111662,#111663,#111664,#111665,#111666,#111667,#111668,
#111669,#111670,#111671,#111672,#111673,#111674,#111675,#111676,#111677,
#111678,#111679,#111680,#111681,#111682,#111683,#111684,#111685,#111686,
#111687,#111688,#111689,#111690,#111691,#111692,#111693,#111694,#111695,
#111696,#111697,#111698,#111699,#111700,#111701,#111702,#111703,#111704,
#111705,#111706,#111707,#111708,#111709,#111710,#111711,#111712,#111713,
#111714,#111715,#111716,#111717,#111718,#111719,#111720,#111721,#111722,
#111723,#111724,#111725,#111726,#111727,#111728,#111729,#111730,#111731,
#111732,#111733,#111734,#111735,#111736,#111737,#111738,#111739,#111740,
#111741,#111742,#111743,#111744,#111745,#111746,#111747,#111748,#111749,
#111750,#111751,#111752,#111753,#111754,#111755,#111756,#111757,#111758,
#111759,#111760,#111761,#111762,#111763,#111764,#111765,#111766,#111767,
#111768,#111769,#111770,#111771,#111772,#111773,#111774,#111775,#111776,
#111777,#111778,#111779,#111780,#111781,#111782,#111783,#111784,#111785,
#111786,#111787,#111788,#111789,#111790,#111791,#111792,#111793,#111794,
#111795,#111796,#111797,#111798,#111799,#111800,#111801,#111802,#111803,
#111804,#111805,#111806,#111807,#111808,#111809,#111810,#111811,#111812,
#111813,#111814,#111815,#111816,#111817,#111818,#111819,#111820,#111821,
#111822,#111823,#111824,#111825,#111826,#111827,#111828,#111829,#111830,
#111831,#111832,#111833,#111834,#111835,#111836,#111837,#111838,#111839,
#111840,#111841,#111842,#111843,#111844,#111845),.UNSPECIFIED.,.F.,.F.,
(4,2,2,2,2,2,2,2,2,2,2,2,2,2,2,2,2,2,2,2,2,2,2,2,2,2,2,2,2,2,2,2,2,2,2,
2,2,2,2,2,2,2,2,2,2,2,2,2,2,2,2,2,2,2,2,2,2,2,2,2,2,2,2,2,2,2,2,2,2,2,2,
2,2,2,2,2,2,2,2,2,2,2,2,2,2,2,2,2,2,2,2,2,2,2,2,2,2,2,2,2,2,2,2,2,2,2,2,
2,4),(6.16657166538228E-5,0.0272484328133284,0.0295142882092296,0.0308961787740782,
0.0321672258211346,0.0330842569284198,0.0342610005797047,0.0363081468226688,
0.0447109857495129,0.052916879077173,0.0609339267452389,0.085445441451452,
0.0992570511726005,0.102782524613097,0.104842676833897,0.106657902238045,
0.108927669001958,0.112466780138857,0.13318458533275,0.163691858774371,
0.174561965044177,0.176636047923632,0.177840886257816,0.178856890894084,
0.180143772371423,0.182194355555759,0.193821253099834,0.224553919283199,
0.237713117079223,0.243315641515315,0.2477032179675,0.24994541606699,0.251741776054048,
0.253815168820887,0.257310247523331,0.270883160262322,0.304250485817181,
0.31981577171664,0.322130349297808,0.32335250929215,0.324367518067532,0.325633609610802,
0.328082313427743,0.34881019951447,0.373465094409642,0.390203149026289,
0.393809136304438,0.395886854867423,0.397700112982985,0.399944739536755,
0.403401260434524,0.421811111267245,0.451357251626637,0.460874680061493,
0.46643568827762,0.468159584410237,0.469252850716743,0.470289536240179,
0.471794854164713,0.475410346273516,0.498002331568398,0.517416230753731,
0.529455715569027,0.537307413673667,0.540124983715762,0.542031752431276,
0.54388236964757,0.546101539610805,0.551669182782149,0.58178479423145,0.608109877493179,
0.612342555981929,0.613898611939505,0.614955799032749,0.615908691864993,
0.617216608921445,0.620509517806219,0.651422978089403,0.671156585611706,
0.682121419079166,0.685295721641037,0.687278968140453,0.689111150705318,
0.691482122990965,0.696668957248408,0.739753360501173,0.756457718122972,
0.758802667556837,0.760031273689142,0.761046188573503,0.76230539070731,
0.764721750732512,0.781632043115149,0.813105538538973,0.827221935277099,
0.830660582758489,0.832701886267296,0.834520144506229,0.836820089447146,
0.840458525941019,0.868476476245189,0.888588954351692,0.902177372020108,
0.904427982079159,0.905636687484879,0.906652507114882,0.907934786172863,
0.909969940583127,0.921279068844543),.UNSPECIFIED.);
#1576=B_SPLINE_CURVE_WITH_KNOTS('',3,(#111850,#111851,#111852,#111853,#111854,
#111855,#111856,#111857,#111858,#111859,#111860,#111861,#111862,#111863,
#111864,#111865,#111866,#111867,#111868,#111869,#111870,#111871,#111872,
#111873,#111874,#111875,#111876,#111877,#111878,#111879,#111880,#111881,
#111882,#111883,#111884,#111885,#111886,#111887,#111888,#111889,#111890,
#111891,#111892,#111893,#111894,#111895,#111896,#111897,#111898,#111899,
#111900,#111901,#111902,#111903,#111904,#111905,#111906,#111907,#111908,
#111909,#111910,#111911,#111912,#111913,#111914,#111915,#111916,#111917,
#111918,#111919,#111920,#111921,#111922,#111923,#111924,#111925,#111926,
#111927,#111928,#111929,#111930,#111931,#111932,#111933,#111934,#111935,
#111936,#111937,#111938,#111939,#111940,#111941,#111942,#111943,#111944,
#111945,#111946,#111947,#111948,#111949,#111950,#111951,#111952,#111953,
#111954,#111955,#111956,#111957,#111958,#111959,#111960,#111961,#111962,
#111963,#111964,#111965,#111966,#111967,#111968,#111969,#111970,#111971,
#111972,#111973,#111974,#111975,#111976,#111977,#111978,#111979,#111980,
#111981,#111982,#111983,#111984,#111985,#111986,#111987,#111988,#111989,
#111990,#111991,#111992,#111993,#111994,#111995,#111996,#111997,#111998,
#111999,#112000,#112001,#112002,#112003,#112004,#112005,#112006,#112007,
#112008,#112009,#112010,#112011,#112012,#112013,#112014,#112015,#112016,
#112017,#112018,#112019,#112020,#112021,#112022,#112023,#112024,#112025,
#112026,#112027,#112028,#112029,#112030,#112031,#112032,#112033,#112034,
#112035,#112036,#112037,#112038,#112039,#112040,#112041,#112042,#112043,
#112044,#112045,#112046,#112047,#112048,#112049,#112050,#112051,#112052,
#112053,#112054,#112055,#112056,#112057,#112058,#112059,#112060,#112061),
 .UNSPECIFIED.,.F.,.F.,(4,2,2,2,2,2,2,2,2,2,2,2,2,2,2,2,2,2,2,2,2,2,2,2,
2,2,2,2,2,2,2,2,2,2,2,2,2,2,2,2,2,2,2,2,2,2,2,2,2,2,2,2,2,2,2,2,2,2,2,2,
2,2,2,2,2,2,2,2,2,2,2,2,2,2,2,2,2,2,2,2,2,2,2,2,2,2,2,2,2,2,2,2,2,2,2,2,
2,2,2,2,2,2,2,2,2,4),(0.92204535995261,0.953944386918954,0.95987018790377,
0.979899530679955,0.982348226566923,0.983614213939935,0.984629078386282,
0.985850964698843,0.988164738546376,1.00370527446872,1.0369606799699,1.0506787967077,
1.0541883361554,1.05626483944438,1.05807783867503,1.06032317518575,1.06472733276008,
1.07035646215137,1.08360855261257,1.10177243604417,1.11316225765477,1.12570188762382,
1.12779442409456,1.1290937818792,1.13011042979398,1.13130523372803,1.13349182893139,
1.14551235879845,1.18616344411341,1.19679726504982,1.20005312598398,1.2020537874123,
1.20387988115381,1.20625169695481,1.21130686297429,1.23142674796299,1.25690697381001,
1.26148320533421,1.27149992836319,1.2736571738815,1.2748587430236,1.27587461632745,
1.27716465667964,1.27981412365994,1.3013243175951,1.33942839261513,1.3439067861149,
1.34619586496282,1.34789441269299,1.34975202242548,1.35232178109057,1.35850880797521,
1.36723559464952,1.39329615774988,1.4052861720004,1.41688831647583,1.41893689253544,
1.42022287959704,1.42123841319755,1.42244294109354,1.42467574219976,1.43781332829239,
1.45808324160008,1.48647647074121,1.49009267717621,1.49238526541735,1.49420192423637,
1.49624586939909,1.49969975128897,1.51404860004353,1.54676048641741,1.55085297813547,
1.56241799419245,1.56446463347913,1.56575004329047,1.56676555241938,1.56797056103585,
1.5702055808731,1.58340004545195,1.60362472831337,1.63200790695679,1.63562166863319,
1.6379135324401,1.63973013729049,1.64177457066557,1.64523061664596,1.65960986864042,
1.69248745629916,1.70769893000109,1.7098807215789,1.7111924133257,1.71221208110609,
1.7133595224369,1.71529799943006,1.71773545028386,1.72286731565794,1.73849076693741,
1.77587843886736,1.78087576261213,1.78324617375042,1.78507754755572,1.78705954114314,
1.7902310025642,1.8011771707635,1.82085894693048,1.84342048453855),
 .UNSPECIFIED.);
#1577=B_SPLINE_CURVE_WITH_KNOTS('',3,(#112062,#112063,#112064,#112065,#112066,
#112067,#112068,#112069,#112070,#112071,#112072,#112073,#112074,#112075,
#112076,#112077,#112078,#112079,#112080,#112081,#112082,#112083,#112084,
#112085,#112086,#112087,#112088,#112089,#112090,#112091,#112092,#112093,
#112094,#112095,#112096,#112097,#112098,#112099,#112100,#112101,#112102,
#112103,#112104,#112105,#112106,#112107,#112108,#112109,#112110,#112111,
#112112,#112113,#112114,#112115,#112116,#112117,#112118,#112119,#112120,
#112121,#112122,#112123,#112124,#112125,#112126,#112127,#112128,#112129,
#112130,#112131,#112132,#112133,#112134,#112135,#112136,#112137,#112138,
#112139,#112140,#112141,#112142,#112143,#112144,#112145,#112146,#112147,
#112148,#112149,#112150,#112151,#112152,#112153,#112154,#112155,#112156,
#112157,#112158,#112159,#112160,#112161,#112162,#112163,#112164,#112165,
#112166,#112167,#112168,#112169,#112170,#112171,#112172,#112173,#112174,
#112175,#112176,#112177,#112178,#112179,#112180,#112181,#112182,#112183,
#112184,#112185,#112186,#112187,#112188,#112189,#112190,#112191,#112192,
#112193,#112194,#112195,#112196,#112197,#112198,#112199,#112200,#112201,
#112202,#112203,#112204,#112205,#112206,#112207,#112208,#112209,#112210,
#112211,#112212,#112213,#112214,#112215,#112216,#112217,#112218,#112219,
#112220,#112221,#112222,#112223,#112224,#112225,#112226,#112227,#112228,
#112229,#112230,#112231,#112232,#112233,#112234,#112235,#112236,#112237,
#112238,#112239,#112240,#112241,#112242,#112243,#112244,#112245,#112246,
#112247,#112248,#112249,#112250,#112251,#112252,#112253,#112254,#112255,
#112256,#112257,#112258,#112259,#112260,#112261,#112262,#112263,#112264,
#112265,#112266,#112267,#112268,#112269,#112270,#112271,#112272,#112273,
#112274,#112275,#112276,#112277,#112278,#112279,#112280,#112281,#112282,
#112283,#112284,#112285,#112286,#112287,#112288,#112289,#112290,#112291,
#112292,#112293,#112294,#112295,#112296,#112297,#112298,#112299,#112300,
#112301,#112302,#112303,#112304,#112305),.UNSPECIFIED.,.F.,.F.,(4,2,2,2,
2,2,2,2,2,2,2,2,2,2,2,2,2,2,2,2,2,2,2,2,2,2,2,2,2,2,2,2,2,2,2,2,2,2,2,2,
2,2,2,2,2,2,2,2,2,2,2,2,2,2,2,2,2,2,2,2,2,2,2,2,2,2,2,2,2,2,2,2,2,2,2,2,
2,2,2,2,2,2,2,2,2,2,2,2,2,2,2,2,2,2,2,2,2,2,2,2,2,2,2,2,2,2,2,2,2,2,2,2,
2,2,2,2,2,2,2,2,2,4),(0.921279068844543,0.956298513554688,0.972293124115016,
0.975958448726816,0.978070747848119,0.979864192118253,0.982056965369928,
0.98620320628717,1.01623728703387,1.04590538699293,1.04929346749591,1.05061744920304,
1.05157446840378,1.05262733179809,1.05416196739572,1.05824633558653,1.06443816262797,
1.10710918758739,1.11857348029956,1.12191991583858,1.12394079928729,1.12576262055144,
1.12809706706528,1.13295301876023,1.15153109246506,1.17676829009808,1.1799894099863,
1.18261374519873,1.19337193667338,1.19537966756903,1.19665352372206,1.19766875354577,
1.19888400766024,1.20116613989136,1.21567133503768,1.24707561127836,1.26338550538756,
1.26707327250464,1.26919046688631,1.27098339386767,1.27316978410453,1.27728631379281,
1.28245473572016,1.29413751355348,1.31390617178286,1.3366914498755,1.34029951586951,
1.3416544286229,1.3426194628133,1.34366471016383,1.34516112579781,1.34899257446693,
1.35467521278871,1.3732490689044,1.40613629730528,1.41159771901257,1.41401756893816,
1.41585724376237,1.41781921977225,1.42089698861231,1.43091863512013,1.44806122807699,
1.45212210744402,1.48260802533421,1.4859372336422,1.48725109622952,1.48820537481963,
1.48926061103684,1.49080785619653,1.49498039784081,1.52045274305289,1.55155359264667,
1.55709279681286,1.55930716111682,1.56115627166095,1.56306407153006,1.56588805723009,
1.5737905558334,1.5859380868287,1.60521561199562,1.62772447703324,1.63134117722634,
1.63284641856937,1.63388290929275,1.63497582076077,1.63669890094147,1.64225490210686,
1.65176200066512,1.68121966167649,1.69973762996546,1.70319735337777,1.70544264900406,
1.70721130373004,1.70728093234482,1.70733928756684,1.70738865583322,1.70743074575989,
1.70746686300787,1.70749802435037,1.70752503447409,1.70754853921643,1.70756906325468,
1.70761035862912,1.70765059138038,1.7076898441727,1.70772819304422,1.70776570814694,
1.70780245438651,1.70994316417093,1.71236570111559,1.7162799518059,1.72411131713937,
1.76111023988633,1.76526865793287,1.77551277306454,1.77749335770848,1.77875887925639,
1.77977366884035,1.78099584671832,1.78331123888072,1.79891507005206,1.84269217962932),
 .UNSPECIFIED.);
#1578=B_SPLINE_CURVE_WITH_KNOTS('',3,(#112310,#112311,#112312,#112313,#112314,
#112315,#112316,#112317,#112318,#112319,#112320,#112321,#112322,#112323,
#112324,#112325,#112326,#112327,#112328,#112329,#112330,#112331,#112332,
#112333,#112334,#112335,#112336,#112337,#112338,#112339,#112340,#112341,
#112342,#112343,#112344,#112345,#112346,#112347,#112348,#112349,#112350,
#112351,#112352,#112353,#112354,#112355,#112356,#112357,#112358,#112359,
#112360,#112361,#112362,#112363,#112364,#112365,#112366,#112367,#112368,
#112369,#112370,#112371,#112372,#112373,#112374,#112375,#112376,#112377,
#112378,#112379,#112380,#112381,#112382,#112383,#112384,#112385,#112386,
#112387,#112388,#112389,#112390,#112391,#112392,#112393,#112394,#112395,
#112396,#112397,#112398,#112399,#112400,#112401,#112402,#112403,#112404,
#112405,#112406,#112407,#112408,#112409,#112410,#112411,#112412,#112413,
#112414,#112415,#112416,#112417,#112418,#112419,#112420,#112421,#112422,
#112423,#112424,#112425,#112426,#112427,#112428,#112429,#112430,#112431,
#112432,#112433,#112434,#112435,#112436,#112437,#112438,#112439,#112440,
#112441,#112442,#112443,#112444,#112445,#112446,#112447,#112448,#112449,
#112450,#112451,#112452,#112453,#112454,#112455,#112456,#112457,#112458,
#112459,#112460,#112461,#112462,#112463,#112464,#112465,#112466,#112467,
#112468,#112469,#112470,#112471,#112472,#112473,#112474,#112475,#112476,
#112477,#112478,#112479,#112480,#112481,#112482,#112483,#112484,#112485,
#112486,#112487,#112488,#112489,#112490,#112491,#112492,#112493,#112494,
#112495,#112496,#112497,#112498,#112499,#112500,#112501,#112502,#112503,
#112504,#112505,#112506,#112507,#112508,#112509,#112510,#112511,#112512,
#112513,#112514,#112515,#112516,#112517,#112518,#112519,#112520,#112521,
#112522,#112523,#112524,#112525,#112526,#112527,#112528,#112529,#112530,
#112531,#112532,#112533),.UNSPECIFIED.,.F.,.F.,(4,2,2,2,2,2,2,2,2,2,2,2,
2,2,2,2,2,2,2,2,2,2,2,2,2,2,2,2,2,2,2,2,2,2,2,2,2,2,2,2,2,2,2,2,2,2,2,2,
2,2,2,2,2,2,2,2,2,2,2,2,2,2,2,2,2,2,2,2,2,2,2,2,2,2,2,2,2,2,2,2,2,2,2,2,
2,2,2,2,2,2,2,2,2,2,2,2,2,2,2,2,2,2,2,2,2,2,2,2,2,2,2,4),(0.00042260572670247,
0.0301011163856895,0.0332807977237642,0.0353998883783552,0.0374424354602521,
0.039259591213873,0.0415551516259118,0.0451806803513619,0.0698369562847597,
0.0910803951690008,0.10676058206949,0.108894709803408,0.110189664572487,
0.111205885210203,0.112403725382788,0.114544450411237,0.124277673180439,
0.151505312701787,0.168328777751004,0.178197942834237,0.18127583918798,
0.183237594244121,0.185076843302523,0.187495806182267,0.192953773733776,
0.225877582550643,0.244412318308645,0.25008783254676,0.253915826739409,
0.255411532291323,0.256456496776942,0.257421425013085,0.258776391522564,
0.262386014025757,0.285138843196942,0.304841084080135,0.316604957621866,
0.324325912206559,0.327125111226344,0.329027599970107,0.330880288697055,
0.333109452982143,0.338743482302663,0.37603618460946,0.397358616537846,
0.40000275861588,0.401291803267086,0.402307678881092,0.403510169807019,
0.405671291415577,0.415748760984687,0.420254891991418,0.428803100862613,
0.435568472256776,0.467412103385173,0.471518126514989,0.473702117681862,
0.475335338683475,0.477395158773801,0.480920685395639,0.494354713695172,
0.527852304403676,0.543447612934405,0.545762620242868,0.546984679691504,
0.547999410415133,0.54926488815002,0.551711626907463,0.571095249558754,
0.591813168085176,0.611525065672801,0.616528377380245,0.618890600239986,
0.620715590692822,0.622721331930648,0.6259997661454,0.636842210744138,0.680203536013387,
0.686425579781325,0.690524846153533,0.692061475135762,0.693114589652801,
0.694070945117811,0.695392843578168,0.698769440841013,0.728658459991538,
0.733283861022475,0.750432957156993,0.760456792246902,0.763534842372239,
0.765496875372686,0.767336511036852,0.76975616594468,0.775216498756968,
0.808126358361383,0.826678621298388,0.832357661174859,0.836187616663424,
0.837683795815743,0.838728994093165,0.839694060120821,0.841049115496593,
0.844658140300783,0.867491768400454,0.887332640603449,0.898969602078717,
0.906630545277608,0.909421839881593,0.911322953809042,0.913177373116619,
0.915828015176426,0.92204535995261),.UNSPECIFIED.);
#1579=B_SPLINE_CURVE_WITH_KNOTS('',3,(#112534,#112535,#112536,#112537,#112538,
#112539,#112540,#112541,#112542,#112543,#112544,#112545,#112546,#112547,
#112548,#112549,#112550,#112551,#112552,#112553,#112554,#112555,#112556,
#112557,#112558,#112559,#112560,#112561,#112562,#112563,#112564,#112565,
#112566,#112567,#112568,#112569,#112570,#112571,#112572,#112573,#112574,
#112575,#112576,#112577,#112578,#112579,#112580,#112581,#112582,#112583,
#112584,#112585,#112586,#112587,#112588,#112589,#112590,#112591,#112592,
#112593,#112594,#112595,#112596,#112597,#112598,#112599,#112600,#112601,
#112602,#112603,#112604,#112605,#112606,#112607,#112608,#112609,#112610,
#112611,#112612,#112613,#112614,#112615,#112616,#112617,#112618,#112619,
#112620,#112621,#112622,#112623,#112624,#112625,#112626,#112627,#112628,
#112629,#112630,#112631,#112632,#112633,#112634,#112635,#112636,#112637,
#112638,#112639,#112640,#112641,#112642,#112643,#112644,#112645,#112646,
#112647,#112648,#112649,#112650,#112651,#112652,#112653,#112654,#112655,
#112656,#112657,#112658,#112659,#112660,#112661,#112662,#112663,#112664,
#112665,#112666,#112667,#112668,#112669,#112670,#112671,#112672,#112673,
#112674,#112675,#112676,#112677,#112678,#112679,#112680,#112681,#112682,
#112683,#112684,#112685,#112686,#112687,#112688,#112689,#112690,#112691,
#112692,#112693,#112694,#112695,#112696,#112697,#112698,#112699,#112700,
#112701,#112702,#112703,#112704,#112705,#112706,#112707,#112708,#112709,
#112710,#112711,#112712,#112713,#112714,#112715,#112716,#112717,#112718,
#112719,#112720,#112721,#112722,#112723,#112724,#112725,#112726,#112727,
#112728,#112729,#112730,#112731,#112732,#112733,#112734,#112735,#112736,
#112737,#112738,#112739,#112740,#112741,#112742,#112743,#112744,#112745,
#112746,#112747,#112748,#112749,#112750,#112751,#112752,#112753,#112754,
#112755,#112756,#112757),.UNSPECIFIED.,.F.,.F.,(4,2,2,2,2,2,2,2,2,2,2,2,
2,2,2,2,2,2,2,2,2,2,2,2,2,2,2,2,2,2,2,2,2,2,2,2,2,2,2,2,2,2,2,2,2,2,2,2,
2,2,2,2,2,2,2,2,2,2,2,2,2,2,2,2,2,2,2,2,2,2,2,2,2,2,2,2,2,2,2,2,2,2,2,2,
2,2,2,2,2,2,2,2,2,2,2,2,2,2,2,2,2,2,2,2,2,2,2,2,2,2,2,4),(0.000546165661636938,
0.00390012266971836,0.00678607654953448,0.00857512239891336,0.0103140173546196,
0.0122744325894094,0.0153440613668164,0.0244041487964937,0.0654579884993774,
0.0745317781892129,0.0781480578681155,0.0808599340831022,0.0821625136740359,
0.0831796991097723,0.084372843616601,0.0864915158746407,0.0958927265309324,
0.13416601876407,0.144214806203282,0.148873822036611,0.151598743997447,
0.154040525418751,0.155852718339705,0.157795392586238,0.160783012000645,
0.16920173840781,0.212406384429208,0.224612508426159,0.226807752462525,
0.228004653962178,0.22902147307387,0.230319013074906,0.232404771488569,
0.244766080215256,0.269855628021126,0.29203687762002,0.297344791587636,
0.299763868558389,0.301597266764204,0.303577642147319,0.306738233037307,
0.316526758408449,0.324281233702563,0.355554530919044,0.370021825276057,
0.372302999250273,0.373518204052623,0.374533658977692,0.375808138304257,
0.377817486901831,0.388600334413022,0.391569652345019,0.394634644336681,
0.426478646014624,0.440667623624168,0.444111495432347,0.446153953166104,
0.447972035265999,0.450270130576169,0.453902398958874,0.481939901522743,
0.502071770694074,0.515635062022503,0.517884763157456,0.519093281332932,
0.520109122729312,0.521391656299878,0.523427634409899,0.534753787615099,
0.565826598598347,0.578982723177383,0.584584540824968,0.588971767032186,
0.591214021205559,0.593010537723858,0.595084235740598,0.598580125854212,
0.612160842838273,0.645525333867422,0.661090655301423,0.663405409267278,
0.664627675296077,0.665642779546511,0.666908999451296,0.669357977861442,
0.690001954991413,0.714705191471345,0.73148086781269,0.73508922722716,0.737167582655402,
0.738980966940695,0.741225194526251,0.74468004587663,0.763043951053706,
0.792635525159949,0.802159826518154,0.807723774363526,0.809448103288884,
0.810541531955286,0.811578277737538,0.813083541352188,0.816698031446895,
0.839325433925569,0.858800634878303,0.870784839016698,0.878610751186036,
0.881425005868438,0.883331212624748,0.885182563605453,0.887404151786532,
0.892986273077319,0.922131836389314),.UNSPECIFIED.);
#1580=B_SPLINE_CURVE_WITH_KNOTS('',3,(#112762,#112763,#112764,#112765,#112766,
#112767,#112768,#112769,#112770,#112771,#112772,#112773,#112774,#112775,
#112776,#112777,#112778,#112779,#112780,#112781,#112782,#112783,#112784,
#112785,#112786,#112787,#112788,#112789,#112790,#112791,#112792,#112793,
#112794,#112795,#112796,#112797,#112798,#112799,#112800,#112801,#112802,
#112803,#112804,#112805,#112806,#112807,#112808,#112809,#112810,#112811,
#112812,#112813,#112814,#112815,#112816,#112817,#112818,#112819,#112820,
#112821,#112822,#112823,#112824,#112825,#112826,#112827,#112828,#112829,
#112830,#112831,#112832,#112833,#112834,#112835,#112836,#112837,#112838,
#112839,#112840,#112841,#112842,#112843,#112844,#112845,#112846,#112847,
#112848,#112849,#112850,#112851,#112852,#112853,#112854,#112855,#112856,
#112857,#112858,#112859,#112860,#112861,#112862,#112863,#112864,#112865,
#112866,#112867,#112868,#112869,#112870,#112871,#112872,#112873,#112874,
#112875,#112876,#112877,#112878,#112879,#112880,#112881,#112882,#112883,
#112884,#112885,#112886,#112887,#112888,#112889,#112890,#112891,#112892,
#112893,#112894,#112895,#112896,#112897,#112898,#112899,#112900,#112901,
#112902,#112903,#112904,#112905,#112906,#112907,#112908,#112909,#112910,
#112911,#112912,#112913,#112914,#112915,#112916,#112917,#112918,#112919,
#112920,#112921,#112922,#112923,#112924,#112925,#112926,#112927,#112928,
#112929,#112930,#112931,#112932,#112933),.UNSPECIFIED.,.F.,.F.,(4,3,3,3,
3,3,3,3,3,3,3,3,3,3,3,3,3,3,3,3,3,3,3,3,3,3,3,3,3,3,3,3,3,3,3,3,3,3,3,3,
3,3,3,3,3,3,3,3,3,3,3,3,3,3,3,3,3,4),(-79.4902472066036,-79.4029346604552,
-79.2894525492148,-79.1761720320241,-79.0630035282616,-78.949902235273,
-78.8368234504382,-78.7236407330294,-78.6104064668353,-78.4969586665535,
-78.4103979771995,-78.2969158659599,-78.1836353487699,-78.0704668450082,
-77.9573655520203,-77.8442867671862,-77.7311040497783,-77.617869783585,
-77.5044219833039,-77.4178612939438,-77.3043791827041,-77.191098665514,
-77.0779301617523,-76.9648288687643,-76.8517500839302,-76.7385673665221,
-76.6253331003288,-76.5118853000477,-76.4253246106881,-76.3118424994482,
-76.198561982258,-76.0853934784961,-75.9722921855081,-75.8592134006738,
-75.7460306832656,-75.6327964170721,-75.5193486167908,-75.4327879274324,
-75.3193058161927,-75.2060252990027,-75.0928567952409,-74.979755502253,
-74.8666767174189,-74.7534940000109,-74.6402597338175,-74.5268119335365,
-74.4402512441768,-74.326769132937,-74.2134886157468,-74.1003201119849,
-73.9872188189968,-73.8741400341625,-73.7609573167544,-73.6477230505609,
-73.5342752502797,-73.4477145609211,-73.29948869365,-73.2070626855824),
 .UNSPECIFIED.);
#1581=B_SPLINE_CURVE_WITH_KNOTS('',3,(#112934,#112935,#112936,#112937,#112938,
#112939,#112940,#112941,#112942,#112943,#112944,#112945,#112946,#112947,
#112948,#112949,#112950,#112951,#112952,#112953,#112954,#112955,#112956,
#112957,#112958,#112959,#112960,#112961,#112962,#112963,#112964,#112965,
#112966,#112967,#112968,#112969,#112970,#112971,#112972,#112973,#112974,
#112975,#112976,#112977,#112978,#112979,#112980,#112981,#112982,#112983,
#112984,#112985,#112986,#112987,#112988,#112989,#112990,#112991,#112992,
#112993,#112994,#112995,#112996,#112997,#112998,#112999,#113000,#113001,
#113002,#113003,#113004,#113005,#113006,#113007,#113008,#113009,#113010,
#113011,#113012,#113013,#113014,#113015,#113016,#113017,#113018,#113019,
#113020,#113021,#113022,#113023,#113024,#113025,#113026,#113027,#113028,
#113029,#113030,#113031,#113032,#113033,#113034,#113035,#113036,#113037,
#113038,#113039,#113040,#113041,#113042,#113043,#113044,#113045,#113046,
#113047,#113048,#113049,#113050,#113051,#113052,#113053,#113054,#113055,
#113056,#113057,#113058,#113059,#113060,#113061,#113062,#113063,#113064,
#113065,#113066,#113067,#113068,#113069,#113070,#113071,#113072,#113073,
#113074,#113075,#113076,#113077,#113078,#113079,#113080,#113081,#113082,
#113083,#113084,#113085,#113086,#113087,#113088,#113089,#113090,#113091,
#113092,#113093,#113094,#113095,#113096,#113097,#113098,#113099,#113100,
#113101,#113102,#113103,#113104,#113105,#113106,#113107,#113108,#113109,
#113110,#113111,#113112,#113113,#113114,#113115,#113116,#113117,#113118,
#113119,#113120,#113121,#113122,#113123,#113124,#113125,#113126,#113127,
#113128,#113129,#113130,#113131,#113132,#113133,#113134,#113135,#113136,
#113137,#113138,#113139,#113140,#113141,#113142,#113143,#113144,#113145,
#113146,#113147,#113148,#113149,#113150,#113151,#113152,#113153,#113154,
#113155,#113156,#113157,#113158,#113159,#113160,#113161,#113162,#113163,
#113164,#113165,#113166,#113167,#113168,#113169,#113170,#113171,#113172,
#113173,#113174,#113175,#113176,#113177,#113178,#113179,#113180,#113181,
#113182,#113183,#113184,#113185,#113186,#113187,#113188,#113189,#113190,
#113191,#113192,#113193,#113194,#113195,#113196,#113197,#113198,#113199,
#113200,#113201,#113202,#113203,#113204,#113205,#113206,#113207,#113208,
#113209,#113210,#113211,#113212,#113213,#113214,#113215,#113216,#113217,
#113218,#113219,#113220,#113221,#113222,#113223,#113224,#113225,#113226,
#113227,#113228,#113229,#113230,#113231,#113232,#113233,#113234,#113235,
#113236,#113237,#113238,#113239,#113240,#113241,#113242,#113243,#113244,
#113245,#113246,#113247,#113248,#113249,#113250,#113251,#113252,#113253),
 .UNSPECIFIED.,.F.,.F.,(4,2,2,2,2,2,2,2,2,2,2,2,2,2,2,2,2,2,2,2,2,2,2,2,
2,2,2,2,2,2,2,2,2,2,2,2,2,2,2,2,2,2,2,2,2,2,2,2,2,2,2,2,2,2,2,2,2,2,2,2,
2,2,2,2,2,2,2,2,2,2,2,2,2,2,2,2,2,2,2,2,2,2,2,2,2,2,2,2,2,2,2,2,2,2,2,2,
2,2,2,2,2,2,2,2,2,2,2,2,2,2,2,2,2,2,2,2,2,2,2,2,2,2,2,2,2,2,2,2,2,2,2,2,
2,2,2,2,2,2,2,2,2,2,2,2,2,2,2,2,2,2,2,2,2,2,2,2,2,2,2,4),(0.922131836389314,
0.922262170085757,0.950341467134868,0.953812250201056,0.955149235641928,
0.956109698770761,0.957159441304046,0.958677984828669,0.962653258221853,
0.968623082936937,0.988898476370587,1.0194771585668,1.025035006869,1.02725278454895,
1.02910319328668,1.03101073401772,1.03383131248837,1.0417039792166,1.05378620317461,
1.07314302761759,1.09570100249777,1.09931702588588,1.10082249837379,1.10185928713487,
1.10295265336059,1.10467670178362,1.1102380172569,1.11975682410213,1.14928555259909,
1.1580687781151,1.16879530833217,1.17206200219198,1.17406560146509,1.1758919456092,
1.17826062777076,1.18329579101754,1.20325027346598,1.22677310948163,1.22919221591622,
1.2331184869178,1.24348767733223,1.24547536566065,1.24674323280732,1.24775837102777,
1.2489791303374,1.25128681669362,1.26660629154333,1.29932926019654,1.3137175956732,
1.31727403479016,1.31936153458299,1.32117394901371,1.32340550551232,1.32774032121055,
1.35810790355764,1.38708877082697,1.39050536028061,1.39183400845851,1.39279223837166,
1.39384391125911,1.39537257278968,1.39941637160345,1.40552534915469,1.4465091621457,
1.45951469761285,1.46300724388953,1.46506015984343,1.46669467559132,1.46888909806894,
1.47304380537896,1.47827268162891,1.49015584363016,1.50971629540219,1.53239096713076,
1.53599802882937,1.53735287296186,1.5383179313917,1.53936328802267,1.54085999656315,
1.54469293152849,1.55037838201038,1.56896735546875,1.60183747171693,1.60730030490129,
1.6097205060333,1.61156034047385,1.613522383322,1.61660003991939,1.62661931240597,
1.64375508150689,1.6651238541587,1.6798235291184,1.68198585395234,1.6832920578398,
1.68431139056386,1.68431750783836,1.68432354536141,1.68432950428872,1.6843353857784,
1.68434119097933,1.6843469210309,1.68435257705015,1.68435816010519,1.68436367127825,
1.68436911162005,1.68437448215374,1.68437978389931,1.68438501787452,1.68439018510243,
1.68439528649927,1.68440032301204,1.68440529561369,1.684410205242,1.68441505277351,
1.68441983915181,1.68442456520982,1.68442923183469,1.68443383989028,1.68443839017334,
1.6844428835534,1.68444732087386,1.68445170288335,1.6844560303425,1.68446030407582,
1.68446452481658,1.68446869332439,1.68447281030495,1.68447687654171,1.6844808927455,
1.68448485957552,1.68448877771987,1.68449264786284,1.68449647069641,1.68450024689281,
1.68450397708628,1.68450766192792,1.68451130202242,1.68574041043262,1.6881477946098,
1.69128835708962,1.6986691312011,1.71464550614072,1.74734205824822,1.75281341739043,
1.75523502857482,1.75707500900258,1.75903631674563,1.76211095147079,1.77210313640312,
1.78916893192169,1.81240495080333,1.82055865454026,1.82636921980636,1.82818757998944,
1.82930162500055,1.83027254324325,1.83129553930595,1.83267092143667,1.83644440740643,
1.84342118748583),.UNSPECIFIED.);
#1582=B_SPLINE_CURVE_WITH_KNOTS('',3,(#113258,#113259,#113260,#113261,#113262,
#113263,#113264,#113265,#113266,#113267,#113268,#113269,#113270,#113271,
#113272,#113273,#113274,#113275,#113276,#113277,#113278,#113279,#113280,
#113281,#113282,#113283,#113284,#113285,#113286,#113287,#113288,#113289,
#113290,#113291,#113292,#113293,#113294,#113295,#113296,#113297,#113298,
#113299,#113300,#113301,#113302,#113303,#113304,#113305,#113306,#113307,
#113308,#113309,#113310,#113311,#113312,#113313,#113314,#113315,#113316,
#113317,#113318,#113319,#113320,#113321,#113322,#113323,#113324,#113325,
#113326,#113327,#113328,#113329,#113330,#113331,#113332,#113333,#113334,
#113335,#113336,#113337,#113338,#113339,#113340,#113341,#113342,#113343,
#113344,#113345,#113346,#113347,#113348,#113349,#113350,#113351,#113352,
#113353,#113354,#113355,#113356,#113357,#113358,#113359,#113360,#113361,
#113362,#113363,#113364,#113365,#113366,#113367,#113368,#113369,#113370,
#113371,#113372,#113373,#113374,#113375,#113376,#113377,#113378,#113379,
#113380,#113381,#113382,#113383,#113384,#113385,#113386,#113387,#113388,
#113389,#113390,#113391,#113392,#113393,#113394,#113395,#113396,#113397,
#113398,#113399,#113400,#113401,#113402,#113403,#113404,#113405,#113406,
#113407,#113408,#113409,#113410,#113411,#113412,#113413,#113414,#113415,
#113416,#113417,#113418,#113419,#113420,#113421,#113422,#113423,#113424,
#113425,#113426,#113427,#113428,#113429,#113430,#113431,#113432,#113433,
#113434,#113435,#113436,#113437,#113438,#113439,#113440,#113441,#113442,
#113443,#113444,#113445,#113446,#113447,#113448,#113449,#113450,#113451,
#113452,#113453,#113454,#113455,#113456,#113457,#113458,#113459,#113460,
#113461,#113462,#113463,#113464,#113465,#113466,#113467,#113468,#113469,
#113470,#113471,#113472,#113473),.UNSPECIFIED.,.F.,.F.,(4,2,2,2,2,2,2,2,
2,2,2,2,2,2,2,2,2,2,2,2,2,2,2,2,2,2,2,2,2,2,2,2,2,2,2,2,2,2,2,2,2,2,2,2,
2,2,2,2,2,2,2,2,2,2,2,2,2,2,2,2,2,2,2,2,2,2,2,2,2,2,2,2,2,2,2,2,2,2,2,2,
2,2,2,2,2,2,2,2,2,2,2,2,2,2,2,2,2,2,2,2,2,2,2,2,2,2,2,4),(0.921591759352823,
0.932451005728724,0.953455716143075,0.976366610203934,0.979973856661162,
0.981328530542062,0.982293408389913,0.98333849006221,0.984834651001523,
0.98866532264372,0.994346592496436,1.01291284055534,1.04582056293844,1.05128137950628,
1.0537009066155,1.05554030536603,1.05750195193745,1.06057911763692,1.07059771434119,
1.08773255977227,1.09276592323988,1.12219662123457,1.12559555911193,1.12692105028923,
1.12787822561133,1.12893015530899,1.13046154554138,1.13452622632648,1.140678471259,
1.18253560637163,1.19473328878941,1.19815099541947,1.20018702757227,1.20182321982764,
1.20403965530232,1.20830358123231,1.23651008554497,1.26803172634206,1.27125844314878,
1.27255474745746,1.2735044368065,1.27456433436741,1.27613518384404,1.28047580165399,
1.30843253218351,1.33674420380591,1.34234076145022,1.3445638848493,1.34641488861363,
1.34831907072948,1.35112719227294,1.35891516738066,1.37081971445205,1.39035465771498,
1.41300937740942,1.41662003002663,1.41797499925442,1.41893985315528,1.41998464297692,
1.42147994921742,1.42530607778609,1.43097866844299,1.44949767356734,1.48246192319825,
1.48791848245317,1.49033701187813,1.49217600038074,1.49413754481196,1.49721525473794,
1.50724214597301,1.5244001585312,1.52709087482143,1.55780841084992,1.56194937799989,
1.56354002047432,1.56449821992207,1.56554883718642,1.56707422736817,1.57109931492969,
1.57717122925508,1.59809381032237,1.62780648546837,1.63338109654358,1.63560069821129,
1.63745075749925,1.63935600930224,1.64216955366867,1.64999809192461,1.66198887788377,
1.68143276138344,1.70403778883264,1.70764762054688,1.70900244786616,1.70996724045918,
1.71099119132066,1.71241772273805,1.7140658269906,1.71700202569571,1.72369975207093,
1.74763392170442,1.77573293633916,1.77935625475289,1.7816509178983,1.78346769024987,
1.78551015034461,1.78895759645335,1.80321740618225,1.84292101011832),
 .UNSPECIFIED.);
#1583=B_SPLINE_CURVE_WITH_KNOTS('',3,(#113474,#113475,#113476,#113477,#113478,
#113479,#113480,#113481,#113482,#113483,#113484,#113485,#113486,#113487,
#113488,#113489,#113490,#113491,#113492,#113493,#113494,#113495,#113496,
#113497,#113498,#113499,#113500,#113501,#113502,#113503,#113504,#113505,
#113506,#113507,#113508,#113509,#113510,#113511,#113512,#113513,#113514,
#113515,#113516,#113517,#113518,#113519,#113520,#113521,#113522,#113523,
#113524,#113525,#113526,#113527,#113528,#113529,#113530,#113531,#113532,
#113533,#113534,#113535,#113536,#113537,#113538,#113539,#113540,#113541,
#113542,#113543,#113544,#113545,#113546,#113547,#113548,#113549,#113550,
#113551,#113552,#113553,#113554,#113555,#113556,#113557,#113558,#113559,
#113560,#113561,#113562,#113563,#113564,#113565,#113566,#113567,#113568,
#113569,#113570,#113571,#113572,#113573,#113574,#113575,#113576,#113577,
#113578,#113579,#113580,#113581,#113582,#113583,#113584,#113585,#113586,
#113587,#113588,#113589,#113590,#113591,#113592,#113593,#113594,#113595,
#113596,#113597,#113598,#113599,#113600,#113601,#113602,#113603,#113604,
#113605,#113606,#113607,#113608,#113609,#113610,#113611,#113612,#113613,
#113614,#113615,#113616,#113617,#113618,#113619,#113620,#113621,#113622,
#113623,#113624,#113625,#113626,#113627,#113628,#113629,#113630,#113631,
#113632,#113633,#113634,#113635,#113636,#113637,#113638,#113639,#113640,
#113641,#113642,#113643,#113644,#113645,#113646,#113647,#113648,#113649,
#113650,#113651,#113652,#113653,#113654,#113655,#113656,#113657,#113658,
#113659,#113660,#113661,#113662,#113663,#113664,#113665,#113666,#113667,
#113668,#113669,#113670,#113671,#113672,#113673,#113674,#113675,#113676,
#113677,#113678,#113679,#113680,#113681,#113682,#113683,#113684,#113685,
#113686,#113687),.UNSPECIFIED.,.F.,.F.,(4,2,2,2,2,2,2,2,2,2,2,2,2,2,2,2,
2,2,2,2,2,2,2,2,2,2,2,2,2,2,2,2,2,2,2,2,2,2,2,2,2,2,2,2,2,2,2,2,2,2,2,2,
2,2,2,2,2,2,2,2,2,2,2,2,2,2,2,2,2,2,2,2,2,2,2,2,2,2,2,2,2,2,2,2,2,2,2,2,
2,2,2,2,2,2,2,2,2,2,2,2,2,2,2,2,2,2,4),(0.000109611860504862,0.0263881269654468,
0.0435355614439316,0.05355865834799,0.0566368023303898,0.0585989868178459,
0.0604388344481837,0.0628588775380518,0.06832061865916,0.10118776293088,
0.119761227349136,0.125443884151263,0.128062432820324,0.130118113203203,
0.131291991293629,0.132237584239197,0.133496730428177,0.135913359114828,
0.152383169061244,0.171898129053717,0.189060586675483,0.199089603391258,
0.2021684736055,0.204130876260641,0.205970757037948,0.208390594030031,0.213850776542714,
0.246753661562792,0.265303706951211,0.270982385116381,0.274812239740323,
0.276308533428512,0.277353866726805,0.278319114893321,0.279674517853826,
0.283285229677594,0.30638543868713,0.326162905717372,0.343554159226471,
0.347195952955449,0.349281436196038,0.351093955951958,0.353328018428925,
0.35675004901375,0.37436254188906,0.375459878242077,0.404811731646641,0.418851115055208,
0.421117652001306,0.422329674552825,0.423345186629057,0.42462316751018,
0.42664431291382,0.437666477644309,0.467986780511056,0.486994421913833,
0.491906945612887,0.494252276864854,0.496075483284056,0.498090671467135,
0.501410864631099,0.512632538612934,0.555559075955423,0.561761480576038,
0.565851324352278,0.567386772688519,0.568439812674461,0.569396689789914,
0.570720090588666,0.5741046203883,0.603858723941073,0.624323149828154,0.631753289757296,
0.637223847627348,0.639672092902816,0.641509823203909,0.64347795940623,
0.646582817594577,0.655913247034108,0.693651877372063,0.709912694420683,
0.712246415318246,0.713472665446473,0.714487638078821,0.715749407588215,
0.718177689593712,0.735863212713659,0.740573903105931,0.754394197357368,
0.771390049077395,0.781355536111029,0.784427909282053,0.786389102053476,
0.788229905384577,0.790653957208334,0.796136832279431,0.828613414878864,
0.847474370630639,0.853207423647724,0.857064816567798,0.858565484998126,
0.859611768832566,0.860576204130791,0.86192820743607,0.865511464295706,
0.890768502812618,0.921587349549934),.UNSPECIFIED.);
#1584=B_SPLINE_CURVE_WITH_KNOTS('',3,(#113692,#113693,#113694,#113695,#113696,
#113697,#113698,#113699,#113700,#113701,#113702,#113703,#113704,#113705,
#113706,#113707,#113708,#113709,#113710,#113711,#113712,#113713,#113714,
#113715,#113716,#113717,#113718,#113719,#113720,#113721,#113722,#113723,
#113724,#113725,#113726,#113727,#113728,#113729,#113730,#113731,#113732,
#113733,#113734,#113735,#113736,#113737,#113738,#113739,#113740,#113741,
#113742,#113743,#113744,#113745,#113746,#113747,#113748,#113749,#113750,
#113751,#113752,#113753,#113754,#113755,#113756,#113757,#113758,#113759,
#113760,#113761,#113762,#113763,#113764,#113765,#113766,#113767,#113768,
#113769,#113770,#113771,#113772,#113773,#113774,#113775,#113776,#113777,
#113778,#113779,#113780,#113781,#113782,#113783,#113784,#113785,#113786,
#113787,#113788,#113789,#113790,#113791,#113792,#113793,#113794,#113795,
#113796,#113797,#113798,#113799,#113800,#113801,#113802,#113803,#113804,
#113805,#113806,#113807,#113808,#113809,#113810,#113811,#113812,#113813,
#113814,#113815,#113816,#113817,#113818,#113819,#113820,#113821,#113822,
#113823,#113824,#113825,#113826,#113827,#113828,#113829,#113830,#113831,
#113832,#113833,#113834,#113835,#113836,#113837,#113838,#113839,#113840,
#113841,#113842,#113843,#113844,#113845,#113846,#113847,#113848,#113849,
#113850,#113851,#113852,#113853,#113854,#113855,#113856,#113857,#113858,
#113859,#113860,#113861,#113862,#113863,#113864,#113865,#113866,#113867,
#113868,#113869,#113870,#113871,#113872,#113873,#113874,#113875,#113876,
#113877,#113878,#113879,#113880,#113881,#113882,#113883,#113884,#113885,
#113886,#113887,#113888,#113889,#113890,#113891,#113892,#113893,#113894,
#113895,#113896,#113897,#113898,#113899,#113900,#113901,#113902,#113903,
#113904,#113905,#113906,#113907,#113908,#113909,#113910,#113911,#113912,
#113913,#113914,#113915),.UNSPECIFIED.,.F.,.F.,(4,2,2,2,2,2,2,2,2,2,2,2,
2,2,2,2,2,2,2,2,2,2,2,2,2,2,2,2,2,2,2,2,2,2,2,2,2,2,2,2,2,2,2,2,2,2,2,2,
2,2,2,2,2,2,2,2,2,2,2,2,2,2,2,2,2,2,2,2,2,2,2,2,2,2,2,2,2,2,2,2,2,2,2,2,
2,2,2,2,2,2,2,2,2,2,2,2,2,2,2,2,2,2,2,2,2,2,2,2,2,2,2,4),(0.000198811978866998,
0.0283954862359279,0.0316064030563364,0.0337383934111708,0.0357899693485767,
0.037605746168362,0.0398869767492998,0.043465054483826,0.0654303190957778,
0.081868406265388,0.103907372436054,0.106998195689001,0.10839254961266,
0.109420124828639,0.110558297245092,0.112486020649799,0.119303202645729,
0.146043418971801,0.16551955789568,0.172730562032024,0.178035166075126,
0.180475409689357,0.182311305189635,0.184281436606099,0.187397871729397,
0.196828281741222,0.234658021191554,0.250705431602909,0.253032813560649,
0.254257436305559,0.255272026881879,0.256534500806897,0.258967438645604,
0.280964180518072,0.303881875848621,0.321067887211414,0.324697946598246,
0.326780502490072,0.328592687424683,0.330829166362182,0.334260221371775,
0.3520911173789,0.382155354095163,0.391746709178854,0.395500034649312,0.398291351545985,
0.399608941551679,0.400617907413173,0.401796073379795,0.403850243884671,
0.412348503765858,0.420538281671264,0.452699786764226,0.46694790159021,
0.470395009521909,0.472437626159877,0.474254756471682,0.476550166981768,
0.48017522471286,0.508236868600793,0.528404846999591,0.537522573748585,
0.541150237274782,0.54386853254242,0.545172029626903,0.546188895566675,
0.547380436326399,0.549493378571925,0.558817362874415,0.564597320336818,
0.589718467821813,0.609799901134509,0.614849991996206,0.617220866594573,
0.619046841783186,0.621047976847007,0.624305977322694,0.634959865571651,
0.671218027920972,0.687323957967042,0.689652915735876,0.69087787503871,
0.691892463541422,0.693154584731581,0.695585856638271,0.717747344927057,
0.731804901637097,0.748794254131461,0.7587562650741,0.761827466987194,0.763787870036349,
0.765627896862348,0.76805086713259,0.773530982511415,0.806036067956404,
0.824872579154355,0.830600733020784,0.834455321437375,0.835955187772594,
0.837001003623189,0.837965067660832,0.839316615826241,0.842899179995747,
0.868121171148966,0.891692063341524,0.899753690052054,0.905577873637375,
0.908087288679488,0.909934512291451,0.911646912218673,0.91444625202759,
0.921591759352823),.UNSPECIFIED.);
#1585=B_SPLINE_CURVE_WITH_KNOTS('',3,(#113916,#113917,#113918,#113919,#113920,
#113921,#113922,#113923,#113924,#113925,#113926,#113927,#113928,#113929,
#113930,#113931,#113932,#113933,#113934,#113935,#113936,#113937,#113938,
#113939,#113940,#113941,#113942,#113943,#113944,#113945,#113946,#113947,
#113948,#113949,#113950,#113951,#113952,#113953,#113954,#113955,#113956,
#113957,#113958,#113959,#113960,#113961,#113962,#113963,#113964,#113965,
#113966,#113967,#113968,#113969,#113970,#113971,#113972,#113973,#113974,
#113975,#113976,#113977,#113978,#113979,#113980,#113981,#113982,#113983,
#113984,#113985,#113986,#113987,#113988,#113989,#113990,#113991,#113992,
#113993,#113994,#113995,#113996,#113997,#113998,#113999,#114000,#114001,
#114002,#114003,#114004,#114005,#114006,#114007,#114008,#114009,#114010,
#114011,#114012,#114013,#114014,#114015,#114016,#114017,#114018,#114019,
#114020,#114021,#114022,#114023,#114024,#114025,#114026,#114027,#114028,
#114029,#114030,#114031,#114032,#114033,#114034,#114035,#114036,#114037,
#114038,#114039,#114040,#114041,#114042,#114043,#114044,#114045,#114046,
#114047,#114048,#114049,#114050,#114051,#114052,#114053,#114054,#114055,
#114056,#114057,#114058,#114059,#114060,#114061,#114062,#114063,#114064,
#114065,#114066,#114067,#114068,#114069,#114070,#114071,#114072,#114073,
#114074,#114075,#114076,#114077,#114078,#114079,#114080,#114081,#114082,
#114083,#114084,#114085,#114086,#114087,#114088,#114089,#114090,#114091,
#114092,#114093,#114094,#114095,#114096,#114097,#114098,#114099,#114100,
#114101,#114102,#114103,#114104,#114105,#114106,#114107,#114108,#114109,
#114110,#114111,#114112,#114113,#114114,#114115,#114116,#114117,#114118,
#114119,#114120,#114121,#114122,#114123,#114124,#114125,#114126,#114127,
#114128,#114129,#114130,#114131,#114132,#114133,#114134,#114135,#114136,
#114137,#114138,#114139,#114140,#114141,#114142,#114143,#114144,#114145,
#114146,#114147),.UNSPECIFIED.,.F.,.F.,(4,2,2,2,2,2,2,2,2,2,2,2,2,2,2,2,
2,2,2,2,2,2,2,2,2,2,2,2,2,2,2,2,2,2,2,2,2,2,2,2,2,2,2,2,2,2,2,2,2,2,2,2,
2,2,2,2,2,2,2,2,2,2,2,2,2,2,2,2,2,2,2,2,2,2,2,2,2,2,2,2,2,2,2,2,2,2,2,2,
2,2,2,2,2,2,2,2,2,2,2,2,2,2,2,2,2,2,2,2,2,2,2,2,2,2,2,4),(0.921587349549934,
0.927848225935604,0.930506277226033,0.932362447347461,0.934262485923268,
0.937046879929529,0.944654855764119,0.956179016031914,0.976119790601808,
0.999006551264362,1.00261456202173,1.00396967205066,1.00493489843658,1.00598041264886,
1.0074773067909,1.01131050110182,1.01699615802948,1.035584068137,1.0684698968529,
1.07393010396914,1.07635007763632,1.07819010589254,1.08015270860964,1.08323198522045,
1.09326339944928,1.11042939241382,1.11266517609307,1.14230289420144,1.14762851318991,
1.14938739959065,1.15048843423817,1.15153264398836,1.15302269607578,1.15681177358933,
1.16241022530834,1.18050437146567,1.21408716609722,1.21897125945152,1.22162582581713,
1.22348126351797,1.22538197732328,1.22817000982117,1.2358049578323,1.24738566784906,
1.26726622894608,1.29011751618152,1.29372554012558,1.29508060502706,1.29604578740718,
1.29709124048293,1.29858802495532,1.30242081896593,1.30810578354821,1.32669046885014,
1.35957297963994,1.36503593453121,1.36745631431699,1.36929633342315,1.37125862023852,
1.37433675828564,1.38435851182503,1.40149978109816,1.40594514061497,1.43600950766017,
1.43937274097984,1.44069246176694,1.44164835177349,1.44270226206602,1.44424229536991,
1.44836390839828,1.47312325424737,1.50506461958148,1.51057216431694,1.51300031006199,
1.51484156620911,1.51680069573309,1.51986452081341,1.52975399654812,1.54655307288848,
1.56840301909368,1.57443744472218,1.58358301609946,1.58568424907112,1.58687334031403,
1.58789083302052,1.58919868265825,1.5919382733352,1.59560247100879,1.60485626607495,
1.63730049474235,1.65344709160116,1.65712271521926,1.65923722018338,1.66103036315293,
1.66322008699196,1.6673523124602,1.6725455388567,1.68431024001991,1.71487739838729,
1.7184002204474,1.7289625314812,1.73096019601263,1.73223100474799,1.73324612002173,
1.73446400565934,1.73675854429256,1.75162318622948,1.77365622565695,1.79843617363865,
1.80206351893953,1.80435992119323,1.80617756819158,1.80822048854086,1.81033983962556,
1.81351963797243,1.84313775771039),.UNSPECIFIED.);
#1586=B_SPLINE_CURVE_WITH_KNOTS('',3,(#114153,#114154,#114155,#114156,#114157,
#114158,#114159,#114160,#114161,#114162,#114163,#114164,#114165,#114166,
#114167,#114168,#114169,#114170,#114171,#114172,#114173,#114174,#114175,
#114176,#114177,#114178,#114179,#114180,#114181,#114182,#114183,#114184,
#114185,#114186,#114187,#114188,#114189,#114190,#114191,#114192,#114193,
#114194,#114195,#114196,#114197,#114198,#114199,#114200,#114201,#114202,
#114203,#114204,#114205,#114206,#114207,#114208,#114209,#114210,#114211,
#114212,#114213,#114214,#114215,#114216,#114217,#114218,#114219,#114220,
#114221,#114222,#114223,#114224,#114225,#114226,#114227,#114228,#114229,
#114230,#114231,#114232,#114233,#114234,#114235,#114236,#114237,#114238,
#114239,#114240,#114241,#114242,#114243,#114244,#114245,#114246,#114247,
#114248,#114249,#114250,#114251,#114252,#114253,#114254,#114255,#114256,
#114257,#114258,#114259,#114260,#114261,#114262,#114263,#114264,#114265,
#114266,#114267,#114268,#114269,#114270,#114271,#114272,#114273,#114274,
#114275,#114276,#114277,#114278,#114279,#114280,#114281,#114282,#114283,
#114284,#114285,#114286,#114287,#114288,#114289,#114290,#114291,#114292,
#114293,#114294,#114295,#114296,#114297,#114298,#114299,#114300,#114301,
#114302,#114303,#114304,#114305,#114306,#114307,#114308,#114309,#114310,
#114311,#114312,#114313,#114314,#114315,#114316,#114317,#114318,#114319,
#114320,#114321,#114322,#114323,#114324,#114325,#114326,#114327,#114328,
#114329,#114330,#114331,#114332,#114333,#114334,#114335,#114336,#114337,
#114338,#114339,#114340,#114341,#114342,#114343,#114344,#114345,#114346,
#114347,#114348,#114349,#114350,#114351,#114352,#114353,#114354,#114355,
#114356,#114357,#114358,#114359,#114360,#114361,#114362,#114363,#114364,
#114365,#114366,#114367,#114368),.UNSPECIFIED.,.F.,.F.,(4,2,2,2,2,2,2,2,
2,2,2,2,2,2,2,2,2,2,2,2,2,2,2,2,2,2,2,2,2,2,2,2,2,2,2,2,2,2,2,2,2,2,2,2,
2,2,2,2,2,2,2,2,2,2,2,2,2,2,2,2,2,2,2,2,2,2,2,2,2,2,2,2,2,2,2,2,2,2,2,2,
2,2,2,2,2,2,2,2,2,2,2,2,2,2,2,2,2,2,2,2,2,2,2,2,2,2,2,4),(0.922145236069275,
0.930099973352994,0.932107881168367,0.933275599929072,0.93419394686494,
0.935477640186354,0.938093815256887,0.941547728791295,0.975011963371041,
0.999294364481554,1.00291791362147,1.00521311898398,1.00703056970487,1.00907405482704,
1.01252386952128,1.02680357041686,1.05912883335261,1.06734748520995,1.0756397689485,
1.07767547467535,1.07884955548381,1.07976688396211,1.08104139240927,1.08361156963494,
1.10814217453859,1.14280125718349,1.14814571240382,1.15054486463945,1.1523811914005,
1.15435163796943,1.15746825637024,1.16785972826562,1.18598448997868,1.21399147684555,
1.22136533931493,1.22334553194136,1.22449543919053,1.22551994870709,1.22689159252903,
1.22997382566216,1.24341297343242,1.27537607707635,1.27867695058951,1.2914293368863,
1.29490169426795,1.29695004300745,1.29858493621659,1.3007850517688,1.30496798702628,
1.3354708250013,1.36458018818733,1.36799235669982,1.36932014043535,1.37027802268805,
1.37132962277312,1.37285867374941,1.37690633907274,1.38302347743107,1.42416486087504,
1.43702714683815,1.44050835770318,1.44255853625363,1.44419302360988,1.44639017986748,
1.45055935455125,1.48314428569505,1.51002997857825,1.51355800107457,1.51490256321908,
1.51586480265039,1.51691225278267,1.51842044255947,1.52232926517163,1.52816608434368,
1.54763897256609,1.57927344813945,1.5842583527272,1.58693944426067,1.58863050170565,
1.59049582075123,1.59310601413759,1.59954236567784,1.63523166251883,1.65731330519417,
1.65974532615154,1.66100769139675,1.66202239555444,1.66324739410687,1.66557615759469,
1.67898074642236,1.71454529741024,1.72809772908284,1.73159090305039,1.73366357692704,
1.73545956068647,1.73770160019749,1.74181677882735,1.7608609893505,1.77766003033577,
1.78584563173894,1.80288401998028,1.80530153286857,1.80656069248462,1.80757521002481,
1.80880287065332,1.81114470832946,1.81676095143397,1.84353659621564),
 .UNSPECIFIED.);
#1587=B_SPLINE_CURVE_WITH_KNOTS('',3,(#114369,#114370,#114371,#114372),
 .UNSPECIFIED.,.F.,.F.,(4,4),(6.73545010571804E-5,0.000198811978866998),
 .UNSPECIFIED.);
#1588=B_SPLINE_CURVE_WITH_KNOTS('',3,(#114373,#114374,#114375,#114376,#114377,
#114378,#114379,#114380,#114381,#114382,#114383,#114384,#114385,#114386,
#114387,#114388,#114389,#114390,#114391,#114392,#114393,#114394,#114395,
#114396,#114397,#114398,#114399,#114400,#114401,#114402,#114403,#114404,
#114405,#114406,#114407,#114408,#114409,#114410,#114411,#114412,#114413,
#114414,#114415,#114416,#114417,#114418,#114419,#114420,#114421,#114422,
#114423,#114424,#114425,#114426,#114427,#114428,#114429,#114430,#114431,
#114432,#114433,#114434,#114435,#114436,#114437,#114438,#114439,#114440,
#114441,#114442,#114443,#114444,#114445,#114446,#114447,#114448,#114449,
#114450,#114451,#114452,#114453,#114454,#114455,#114456,#114457,#114458,
#114459,#114460,#114461,#114462,#114463,#114464,#114465,#114466,#114467,
#114468,#114469,#114470,#114471,#114472,#114473,#114474,#114475,#114476,
#114477,#114478,#114479,#114480,#114481,#114482,#114483,#114484,#114485,
#114486,#114487,#114488,#114489,#114490,#114491,#114492,#114493,#114494,
#114495,#114496,#114497,#114498,#114499,#114500,#114501,#114502,#114503,
#114504,#114505,#114506,#114507,#114508,#114509,#114510,#114511,#114512,
#114513,#114514,#114515,#114516,#114517,#114518,#114519,#114520,#114521,
#114522,#114523,#114524,#114525,#114526,#114527,#114528,#114529,#114530,
#114531,#114532,#114533,#114534,#114535,#114536,#114537,#114538,#114539,
#114540,#114541,#114542,#114543,#114544),.UNSPECIFIED.,.F.,.F.,(4,3,3,3,
3,3,3,3,3,3,3,3,3,3,3,3,3,3,3,3,3,3,3,3,3,3,3,3,3,3,3,3,3,3,3,3,3,3,3,3,
3,3,3,3,3,3,3,3,3,3,3,3,3,3,3,3,3,4),(89.0873369787636,89.2354843443786,
89.3283014930121,89.4417836042537,89.5550641214456,89.6682326252091,89.7813339181988,
89.8944127030348,90.0075954204445,90.1208296866396,90.2342774869224,90.3208381762678,
90.4343202875066,90.5476008046957,90.6607693084565,90.7738706014435,90.8869493862768,
91.000132103684,91.1133663698766,91.2268141701569,91.3133748595235,91.4268569707589,
91.5401374879445,91.6533059917019,91.7664072846854,91.8794860695152,91.9926687869188,
92.1059030531078,92.2193508533846,92.3059115427791,92.4193936540317,92.5326741712347,
92.6458426750093,92.75894396801,92.8720227528569,92.9852054702775,93.0984397364834,
93.2118875367767,93.2984482260348,93.4119303372638,93.5252108544434,93.6383793581948,
93.7514806511725,93.8645594359965,93.9777421533947,94.0909764195785,94.2044242198503,
94.2909849092905,94.4044670205054,94.5177475376704,94.630916041407,94.7440173343696,
94.8570961191784,94.9702788365611,95.0835131027292,95.1969609029854,95.2835215925462,
95.3705214141547),.UNSPECIFIED.);
#1589=B_SPLINE_CURVE_WITH_KNOTS('',3,(#114549,#114550,#114551,#114552,#114553,
#114554,#114555,#114556,#114557,#114558,#114559,#114560,#114561,#114562,
#114563,#114564,#114565,#114566,#114567,#114568,#114569,#114570,#114571,
#114572,#114573,#114574,#114575,#114576,#114577,#114578,#114579,#114580,
#114581,#114582,#114583,#114584,#114585,#114586,#114587,#114588,#114589,
#114590,#114591,#114592,#114593,#114594,#114595,#114596,#114597,#114598,
#114599,#114600,#114601,#114602,#114603,#114604,#114605,#114606,#114607,
#114608,#114609,#114610,#114611,#114612,#114613,#114614,#114615,#114616,
#114617,#114618,#114619,#114620,#114621,#114622,#114623,#114624,#114625,
#114626,#114627,#114628,#114629,#114630,#114631,#114632,#114633,#114634,
#114635,#114636,#114637,#114638,#114639,#114640,#114641,#114642,#114643,
#114644,#114645,#114646,#114647,#114648,#114649,#114650,#114651,#114652,
#114653,#114654,#114655,#114656,#114657,#114658,#114659,#114660,#114661,
#114662,#114663,#114664,#114665,#114666,#114667,#114668,#114669,#114670,
#114671,#114672,#114673,#114674,#114675,#114676,#114677,#114678,#114679,
#114680,#114681,#114682,#114683,#114684,#114685,#114686,#114687,#114688,
#114689,#114690,#114691,#114692,#114693,#114694,#114695,#114696,#114697,
#114698,#114699,#114700,#114701,#114702,#114703,#114704,#114705,#114706,
#114707,#114708,#114709,#114710,#114711,#114712,#114713,#114714,#114715,
#114716,#114717,#114718,#114719,#114720,#114721,#114722,#114723,#114724,
#114725,#114726,#114727,#114728,#114729,#114730,#114731,#114732,#114733,
#114734,#114735,#114736,#114737,#114738,#114739,#114740,#114741,#114742,
#114743,#114744,#114745,#114746,#114747,#114748,#114749,#114750,#114751,
#114752,#114753,#114754,#114755,#114756,#114757,#114758,#114759,#114760,
#114761,#114762,#114763,#114764,#114765,#114766,#114767,#114768,#114769,
#114770,#114771,#114772),.UNSPECIFIED.,.F.,.F.,(4,2,2,2,2,2,2,2,2,2,2,2,
2,2,2,2,2,2,2,2,2,2,2,2,2,2,2,2,2,2,2,2,2,2,2,2,2,2,2,2,2,2,2,2,2,2,2,2,
2,2,2,2,2,2,2,2,2,2,2,2,2,2,2,2,2,2,2,2,2,2,2,2,2,2,2,2,2,2,2,2,2,2,2,2,
2,2,2,2,2,2,2,2,2,2,2,2,2,2,2,2,2,2,2,2,2,2,2,2,2,2,2,4),(0.000537788205222184,
0.0412154549149923,0.0561747957247499,0.0584711220099246,0.0596893029918871,
0.060704274533989,0.0619743954783404,0.0639700647646533,0.0744953586875274,
0.0781467153376516,0.115351480761497,0.123203538939702,0.127124951214964,
0.129550403514325,0.131718265746167,0.1317534451347,0.131789516174362,0.131826544704866,
0.131864602013896,0.133607805143231,0.135667900055591,0.139194515470624,
0.15258354640383,0.18634241742011,0.200418333636561,0.203572807557997,0.204957268247585,
0.205983489882934,0.207126678393224,0.209076724871123,0.216127982233253,
0.244388027293493,0.262614795684615,0.273042664231492,0.276162824680071,
0.278133902685874,0.279969707770093,0.282366583692268,0.287699205404328,
0.322466448629646,0.34689989462452,0.349453786325807,0.350724937511526,
0.351641830404646,0.352818080377451,0.354863640989318,0.36324906801713,
0.371458992655041,0.392089093937398,0.414815503947171,0.420186664783383,
0.422616735757513,0.424451309421504,0.426426078856524,0.429562858415874,
0.439157656763658,0.480981688445164,0.493091052657945,0.495281734612963,
0.496477505449941,0.49749419105753,0.498792598560036,0.500881714251003,
0.513330926556598,0.524825621125422,0.542986739446269,0.556259330361401,
0.561894294667348,0.56630190007709,0.56854809268396,0.570361345774777,0.572437660303972,
0.57594572966503,0.589640696854087,0.595021855282038,0.624454171199838,
0.633956527963948,0.639511470460461,0.641234610659879,0.642327655677003,
0.643364334865411,0.64486992673883,0.64848777310719,0.671041166307839,0.690381157664352,
0.702497828902728,0.707796369893352,0.711994655500353,0.714198114861535,
0.716008888783038,0.718118420597832,0.72177197136746,0.737592022849622,
0.769415134908327,0.784046995620602,0.786333307739155,0.787549492796133,
0.788564734455465,0.789837623775737,0.791842048642956,0.802531659933779,
0.805805796590242,0.843188169829598,0.851057059875072,0.856774479642902,
0.859265835369003,0.861110288706096,0.862827616286446,0.865189920878605,
0.869962587923911,0.905125916193915,0.922145236069275),.UNSPECIFIED.);
#1590=B_SPLINE_CURVE_WITH_KNOTS('',3,(#114773,#114774,#114775,#114776,#114777,
#114778,#114779,#114780,#114781,#114782,#114783,#114784,#114785,#114786,
#114787,#114788,#114789,#114790,#114791,#114792,#114793,#114794,#114795,
#114796,#114797,#114798,#114799,#114800,#114801,#114802,#114803,#114804,
#114805,#114806,#114807,#114808,#114809,#114810,#114811,#114812,#114813,
#114814,#114815,#114816,#114817,#114818,#114819,#114820,#114821,#114822,
#114823,#114824,#114825,#114826,#114827,#114828,#114829,#114830,#114831,
#114832,#114833,#114834,#114835,#114836,#114837,#114838,#114839,#114840,
#114841,#114842,#114843,#114844,#114845,#114846,#114847,#114848,#114849,
#114850,#114851,#114852,#114853,#114854,#114855,#114856,#114857,#114858,
#114859,#114860,#114861,#114862,#114863,#114864,#114865,#114866,#114867,
#114868,#114869,#114870,#114871,#114872,#114873,#114874,#114875,#114876,
#114877,#114878,#114879,#114880,#114881,#114882,#114883,#114884,#114885,
#114886,#114887,#114888,#114889,#114890,#114891,#114892,#114893,#114894,
#114895,#114896,#114897,#114898,#114899,#114900,#114901,#114902,#114903,
#114904,#114905,#114906,#114907,#114908,#114909,#114910,#114911,#114912,
#114913,#114914,#114915,#114916,#114917,#114918,#114919,#114920,#114921,
#114922,#114923,#114924,#114925,#114926,#114927,#114928,#114929,#114930,
#114931,#114932,#114933,#114934,#114935,#114936,#114937,#114938,#114939,
#114940,#114941,#114942,#114943,#114944,#114945,#114946,#114947,#114948,
#114949,#114950,#114951,#114952,#114953,#114954,#114955,#114956,#114957,
#114958,#114959,#114960,#114961,#114962,#114963,#114964,#114965,#114966,
#114967,#114968,#114969,#114970,#114971,#114972,#114973,#114974,#114975,
#114976,#114977,#114978,#114979,#114980,#114981,#114982,#114983,#114984,
#114985,#114986),.UNSPECIFIED.,.F.,.F.,(4,2,2,2,2,2,2,2,2,2,2,2,2,2,2,2,
2,2,2,2,2,2,2,2,2,2,2,2,2,2,2,2,2,2,2,2,2,2,2,2,2,2,2,2,2,2,2,2,2,2,2,2,
2,2,2,2,2,2,2,2,2,2,2,2,2,2,2,2,2,2,2,2,2,2,2,2,2,2,2,2,2,2,2,2,2,2,2,2,
2,2,2,2,2,2,2,2,2,2,2,2,2,2,2,2,2,2,4),(0.000422832080831237,0.0231641369034323,
0.0436625978087327,0.0548869710746597,0.0580860565639775,0.0600746485661758,
0.0619049612885063,0.0642639773300582,0.0692004724361086,0.10708315407289,
0.122398094458075,0.127468799234693,0.129886156083532,0.131810214369377,
0.132955479732407,0.133976074497356,0.135292642222996,0.137490196673243,
0.153753014059877,0.185763236143005,0.199983313654894,0.203429122416956,
0.205471854552152,0.207289640637777,0.209586632568232,0.213215705162516,
0.241260298620107,0.261402706048461,0.274947525214627,0.277196342734631,
0.278404588326497,0.279420320928489,0.28070286968664,0.282739154045147,
0.294075409440267,0.325133414300778,0.338287209650057,0.343888147688721,
0.348274722900811,0.350516688179482,0.352312994039333,0.354386472121347,
0.357882046811702,0.371462406253757,0.404821914398403,0.420385164382855,
0.422699642218197,0.423921764847353,0.424936751405952,0.426202826256647,
0.428651529042321,0.449278770776321,0.47398498145182,0.490766407620942,
0.494374781822933,0.496452990362262,0.498266155034714,0.500509992687324,
0.503964019263108,0.522315683477168,0.551912871382542,0.561437339141659,
0.567001155497484,0.568725342029325,0.569818656589941,0.570855274256569,
0.572360321741661,0.57597410741078,0.5986064122194,0.618092846594316,0.630062873602365,
0.635317654704643,0.639488477308072,0.641686324221132,0.643321251273812,
0.645371897072596,0.648853705155028,0.661720316766805,0.695742015556085,
0.711458052695675,0.713776952121576,0.715000046187486,0.716015057279447,
0.717280185453477,0.719258972012191,0.729462438497255,0.733739068057952,
0.735978580016645,0.767946736376416,0.782159037315848,0.785604382194395,
0.787647060664827,0.789464935757282,0.791762224734678,0.795392134097783,
0.823393165670096,0.847387041272158,0.857414090942898,0.859499368961179,
0.860672440979104,0.861692302950705,0.863002214592797,0.865176891512479,
0.880201143762242,0.889180545816463,0.910849041034443,0.921801751976425),
 .UNSPECIFIED.);
#1591=B_SPLINE_CURVE_WITH_KNOTS('',3,(#114991,#114992,#114993,#114994,#114995,
#114996,#114997,#114998,#114999,#115000,#115001,#115002,#115003,#115004,
#115005,#115006,#115007,#115008,#115009,#115010,#115011,#115012,#115013,
#115014,#115015,#115016,#115017,#115018,#115019,#115020,#115021,#115022,
#115023,#115024,#115025,#115026,#115027,#115028,#115029,#115030,#115031,
#115032,#115033,#115034,#115035,#115036,#115037,#115038,#115039,#115040,
#115041,#115042,#115043,#115044,#115045,#115046,#115047,#115048,#115049,
#115050,#115051,#115052,#115053,#115054,#115055,#115056,#115057,#115058,
#115059,#115060,#115061,#115062,#115063,#115064,#115065,#115066,#115067,
#115068,#115069,#115070,#115071,#115072,#115073,#115074,#115075,#115076,
#115077,#115078,#115079,#115080,#115081,#115082,#115083,#115084,#115085,
#115086,#115087,#115088,#115089,#115090,#115091,#115092,#115093,#115094,
#115095,#115096,#115097,#115098,#115099,#115100,#115101,#115102,#115103,
#115104,#115105,#115106,#115107,#115108,#115109,#115110,#115111,#115112,
#115113,#115114,#115115,#115116,#115117,#115118,#115119,#115120,#115121,
#115122,#115123,#115124,#115125,#115126,#115127,#115128,#115129,#115130,
#115131,#115132,#115133,#115134,#115135,#115136,#115137,#115138,#115139,
#115140,#115141,#115142,#115143,#115144,#115145,#115146,#115147,#115148,
#115149,#115150,#115151,#115152,#115153,#115154,#115155,#115156,#115157,
#115158,#115159,#115160,#115161,#115162,#115163,#115164,#115165,#115166,
#115167,#115168,#115169,#115170,#115171,#115172,#115173,#115174,#115175,
#115176,#115177,#115178,#115179,#115180,#115181,#115182,#115183,#115184,
#115185,#115186,#115187,#115188,#115189,#115190,#115191,#115192,#115193,
#115194,#115195,#115196,#115197,#115198,#115199,#115200,#115201,#115202,
#115203,#115204,#115205,#115206,#115207,#115208),.UNSPECIFIED.,.F.,.F.,
(4,2,2,2,2,2,2,2,2,2,2,2,2,2,2,2,2,2,2,2,2,2,2,2,2,2,2,2,2,2,2,2,2,2,2,
2,2,2,2,2,2,2,2,2,2,2,2,2,2,2,2,2,2,2,2,2,2,2,2,2,2,2,2,2,2,2,2,2,2,2,2,
2,2,2,2,2,2,2,2,2,2,2,2,2,2,2,2,2,2,2,2,2,2,2,2,2,2,2,2,2,2,2,2,2,2,2,2,
2,4),(0.921725633262079,0.949576255217166,0.953189867214194,0.95548182448934,
0.957298623741511,0.959343404706572,0.962800358457658,0.977188880417411,
1.01011684105481,1.02527247387913,1.02745077460306,1.02876154540852,1.02978121221861,
1.03095299541059,1.0330336272909,1.04298949565247,1.06664950293528,1.09512386101343,
1.09873117438062,1.10102114119684,1.10283762575705,1.10488338552217,1.10834524458052,
1.1228060898948,1.15613479000508,1.16213936875559,1.17130425944584,1.17340635277157,
1.17459539715621,1.17561249366501,1.17691934523928,1.17965512954395,1.18331309507381,
1.19254469668056,1.21260437194532,1.24060620728182,1.24424321226475,1.24654216862674,
1.24835959609691,1.25039990885999,1.2538367333725,1.2679431508107,1.2993808696953,
1.3163034270449,1.31871892067003,1.31997758933872,1.32099203109221,1.32221998760714,
1.32456343325672,1.34123456269813,1.38437212839195,1.38955319235994,1.39192246199284,
1.39375369963911,1.39573628758968,1.39891032291311,1.40988245749201,1.42963928941552,
1.46047494308472,1.46377192978575,1.46508015989422,1.4660328257747,1.46708919018995,
1.46864306126952,1.47286372986537,1.49902919577973,1.52933780257434,1.53490002355417,
1.53711764688994,1.53896719012727,1.54087307551792,1.54368975430288,1.55154167943457,
1.56358226045694,1.58297228379386,1.60554569538321,1.60915913140799,1.61066360284466,
1.61169971870757,1.61279237567419,1.61451527992088,1.62007260117396,1.62958383749003,
1.65907460141803,1.67752748807667,1.68100025182845,1.68324917394677,1.68502060376805,
1.68703021545619,1.68915402035642,1.69234554613468,1.6982002180556,1.71225799480805,
1.73404738345931,1.75283400580711,1.75527494988093,1.75653894226651,1.75755330926194,
1.75877592207479,1.76109470201267,1.77684204839185,1.81265715015851,1.82398332991216,
1.82731730843342,1.82933472530591,1.83110177755749,1.83286177871242,1.83511224080361,
1.84305992990751),.UNSPECIFIED.);
#1592=B_SPLINE_CURVE_WITH_KNOTS('',3,(#115209,#115210,#115211,#115212,#115213,
#115214,#115215,#115216,#115217,#115218,#115219,#115220,#115221,#115222,
#115223,#115224,#115225,#115226,#115227,#115228,#115229,#115230,#115231,
#115232,#115233,#115234,#115235,#115236,#115237,#115238,#115239,#115240,
#115241,#115242,#115243,#115244,#115245,#115246,#115247,#115248,#115249,
#115250,#115251,#115252,#115253,#115254,#115255,#115256,#115257,#115258,
#115259,#115260,#115261,#115262,#115263,#115264,#115265,#115266,#115267,
#115268,#115269,#115270,#115271,#115272,#115273,#115274,#115275,#115276,
#115277,#115278,#115279,#115280,#115281,#115282,#115283,#115284,#115285,
#115286,#115287,#115288,#115289,#115290,#115291,#115292,#115293,#115294,
#115295,#115296,#115297,#115298,#115299,#115300,#115301,#115302,#115303,
#115304,#115305,#115306,#115307,#115308,#115309,#115310,#115311,#115312,
#115313,#115314,#115315,#115316,#115317,#115318,#115319,#115320,#115321,
#115322,#115323,#115324,#115325,#115326,#115327,#115328,#115329,#115330,
#115331,#115332,#115333,#115334,#115335,#115336,#115337,#115338,#115339,
#115340,#115341,#115342,#115343,#115344,#115345,#115346,#115347,#115348,
#115349,#115350,#115351,#115352,#115353,#115354,#115355,#115356,#115357,
#115358,#115359,#115360,#115361,#115362,#115363,#115364,#115365,#115366,
#115367,#115368,#115369,#115370,#115371,#115372,#115373,#115374,#115375,
#115376,#115377,#115378,#115379,#115380,#115381,#115382,#115383,#115384,
#115385,#115386,#115387,#115388,#115389,#115390,#115391,#115392,#115393,
#115394,#115395,#115396,#115397,#115398,#115399,#115400,#115401,#115402,
#115403,#115404,#115405,#115406,#115407,#115408,#115409,#115410,#115411,
#115412,#115413,#115414,#115415,#115416,#115417,#115418,#115419,#115420,
#115421,#115422,#115423,#115424,#115425,#115426,#115427,#115428),
 .UNSPECIFIED.,.F.,.F.,(4,2,2,2,2,2,2,2,2,2,2,2,2,2,2,2,2,2,2,2,2,2,2,2,
2,2,2,2,2,2,2,2,2,2,2,2,2,2,2,2,2,2,2,2,2,2,2,2,2,2,2,2,2,2,2,2,2,2,2,2,
2,2,2,2,2,2,2,2,2,2,2,2,2,2,2,2,2,2,2,2,2,2,2,2,2,2,2,2,2,2,2,2,2,2,2,2,
2,2,2,2,2,2,2,2,2,2,2,2,2,4),(0.921801751976425,0.928993186603278,0.931799776086555,
0.933513930511989,0.935360977569221,0.937866490624144,0.943664922853653,
0.951678557413244,0.974996347806176,1.00053872865013,1.00411662522397,1.00546783791764,
1.00643200709162,1.00747833400396,1.00897961671964,1.01284155746269,1.01858438217066,
1.03750249382329,1.06992173477077,1.07540702596828,1.07783136247779,1.07967207047093,
1.08163286323914,1.0847039876101,1.09465992892944,1.11162999272388,1.12614995724437,
1.14781767982079,1.15026780256958,1.15153420179619,1.15254922408316,1.15377111624988,
1.15608441927888,1.17160134250916,1.20475928986257,1.21857562492971,1.222092484475,
1.22417084648222,1.22598395701949,1.22822748480154,1.23262174380447,1.23823468221565,
1.25142963165657,1.28313123267952,1.29379598527139,1.29579901905504,1.29707148805807,
1.29808671477441,1.29930328279333,1.30159142259594,1.3162792664152,1.34824968955543,
1.36388954038128,1.36753124830872,1.36963806124147,1.37144894710712,1.37365560544599,
1.37786954386904,1.40464023133291,1.43306506373248,1.43987343871292,1.44180067024132,
1.44293895137445,1.44396691933338,1.44536224453262,1.44857756177365,1.46320330103209,
1.49869174918341,1.5100892583887,1.51342827684771,1.51544750400019,1.51726963541232,
1.51960698859986,1.5244782769087,1.54317240282844,1.56862975337683,1.57684023555829,
1.58516213156876,1.58720027071113,1.58837490266454,1.58929214747542,1.59056589853921,
1.59313233728925,1.61596803153528,1.65260613776114,1.6572422425125,1.6595709083241,
1.66127960562939,1.66312985895016,1.66565600363234,1.6714502616477,1.67952631625789,
1.70317477586795,1.72825259225605,1.73183516150597,1.73318677195699,1.73415091259253,
1.73519686428201,1.73669702600259,1.74042786597807,1.76107722766996,1.77771117914622,
1.79997350278526,1.80356050888335,1.80584464387862,1.80766098276403,1.80971133938939,
1.81184137604068,1.81504719542795,1.84332610369432),.UNSPECIFIED.);
#1593=B_SPLINE_CURVE_WITH_KNOTS('',3,(#115433,#115434,#115435,#115436,#115437,
#115438,#115439,#115440,#115441,#115442,#115443,#115444,#115445,#115446,
#115447,#115448,#115449,#115450,#115451,#115452,#115453,#115454,#115455,
#115456,#115457,#115458,#115459,#115460,#115461,#115462,#115463,#115464,
#115465,#115466,#115467,#115468,#115469,#115470,#115471,#115472,#115473,
#115474,#115475,#115476,#115477,#115478,#115479,#115480,#115481,#115482,
#115483,#115484,#115485,#115486,#115487,#115488,#115489,#115490,#115491,
#115492,#115493,#115494,#115495,#115496,#115497,#115498,#115499,#115500,
#115501,#115502,#115503,#115504,#115505,#115506,#115507,#115508,#115509,
#115510,#115511,#115512,#115513,#115514,#115515,#115516,#115517,#115518,
#115519,#115520,#115521,#115522,#115523,#115524,#115525,#115526,#115527,
#115528,#115529,#115530,#115531,#115532,#115533,#115534,#115535,#115536,
#115537,#115538,#115539,#115540,#115541,#115542,#115543,#115544,#115545,
#115546,#115547,#115548,#115549,#115550,#115551,#115552,#115553,#115554,
#115555,#115556,#115557,#115558,#115559,#115560,#115561,#115562,#115563,
#115564,#115565,#115566,#115567,#115568,#115569,#115570,#115571,#115572,
#115573,#115574,#115575,#115576,#115577,#115578,#115579,#115580,#115581,
#115582,#115583,#115584,#115585,#115586,#115587,#115588,#115589,#115590,
#115591,#115592,#115593,#115594,#115595,#115596,#115597,#115598,#115599,
#115600,#115601,#115602,#115603,#115604,#115605,#115606,#115607,#115608,
#115609,#115610,#115611,#115612,#115613,#115614,#115615,#115616,#115617,
#115618,#115619,#115620,#115621,#115622,#115623,#115624,#115625,#115626,
#115627,#115628,#115629,#115630,#115631,#115632,#115633,#115634,#115635,
#115636,#115637,#115638,#115639,#115640,#115641,#115642,#115643,#115644,
#115645,#115646,#115647,#115648,#115649,#115650,#115651,#115652,#115653,
#115654,#115655,#115656),.UNSPECIFIED.,.F.,.F.,(4,2,2,2,2,2,2,2,2,2,2,2,
2,2,2,2,2,2,2,2,2,2,2,2,2,2,2,2,2,2,2,2,2,2,2,2,2,2,2,2,2,2,2,2,2,2,2,2,
2,2,2,2,2,2,2,2,2,2,2,2,2,2,2,2,2,2,2,2,2,2,2,2,2,2,2,2,2,2,2,2,2,2,2,2,
2,2,2,2,2,2,2,2,2,2,2,2,2,2,2,2,2,2,2,2,2,2,2,2,2,2,2,4),(0.000439914180201879,
0.00735087020532558,0.00879393008916023,0.00983800708509203,0.0107902023889067,
0.0117382816365723,0.0130275882263253,0.01621718725617,0.0240737006876381,
0.0379108716697168,0.0731061580349014,0.0793602683738382,0.0819450251709392,
0.0838090885747689,0.085510590644278,0.0882334997756488,0.0948843795411132,
0.130772015818668,0.145473930588226,0.150421452161862,0.152799611216542,
0.154730567995416,0.155860437615718,0.156841086144421,0.158157665395588,
0.160352965110758,0.176187006904382,0.208520885546101,0.222797291091522,
0.226247139492212,0.228290836136495,0.230108600817205,0.232404377937929,
0.236029126876226,0.264458957544217,0.28480559029371,0.297869941583472,
0.300099648808395,0.301303375678287,0.302318362360115,0.303603866209583,
0.305652649347156,0.317276676234962,0.348057424501443,0.361190729862364,
0.366784078240857,0.371164883466434,0.373403934273249,0.375214544850484,
0.377291240551271,0.380808077501874,0.394665311394709,0.427793523003757,
0.443296601352044,0.445607141407924,0.446827423762021,0.44784165043002,
0.449107498159173,0.451555884593169,0.472107645393182,0.496854401237881,
0.513671969233811,0.517282552302813,0.519361337240652,0.521174600788465,
0.52341804635096,0.52687052245169,0.545187862895212,0.574783394540152,0.584307386307393,
0.589871062274551,0.591595546539695,0.592689145907578,0.593725671640217,
0.595230689490728,0.598845268901491,0.621439980894645,0.640861505358724,
0.652888465572059,0.660733547910954,0.663549608345408,0.665455587489115,
0.667305609186157,0.669524262641367,0.675091627330956,0.70521186441497,
0.731540016359414,0.735772252645225,0.737327806530722,0.738384541076538,
0.739336892018181,0.740643902108912,0.743933653044977,0.7748710217023,0.794589057111284,
0.805547360125346,0.808720031622231,0.810702278938135,0.812533543063013,
0.814903322403207,0.820087457920443,0.856387216131039,0.872670943467903,
0.877932337236289,0.881548421551187,0.883010636458946,0.884049347976965,
0.885022626271749,0.886690364274768,0.891347346841458,0.921594694409251,
0.921725633262079),.UNSPECIFIED.);
#1594=B_SPLINE_CURVE_WITH_KNOTS('',3,(#115657,#115658,#115659,#115660,#115661,
#115662,#115663,#115664,#115665,#115666,#115667,#115668,#115669,#115670,
#115671,#115672,#115673,#115674,#115675,#115676,#115677,#115678,#115679,
#115680,#115681,#115682,#115683,#115684,#115685,#115686,#115687,#115688,
#115689,#115690,#115691,#115692,#115693,#115694,#115695,#115696,#115697,
#115698,#115699,#115700,#115701,#115702,#115703,#115704,#115705,#115706,
#115707,#115708,#115709,#115710,#115711,#115712,#115713,#115714,#115715,
#115716,#115717,#115718,#115719,#115720,#115721,#115722,#115723,#115724,
#115725,#115726,#115727,#115728,#115729,#115730,#115731,#115732,#115733,
#115734,#115735,#115736,#115737,#115738,#115739,#115740,#115741,#115742,
#115743,#115744,#115745,#115746,#115747,#115748,#115749,#115750,#115751,
#115752,#115753,#115754,#115755,#115756,#115757,#115758,#115759,#115760,
#115761,#115762,#115763,#115764,#115765,#115766,#115767,#115768,#115769,
#115770,#115771,#115772,#115773,#115774,#115775,#115776,#115777,#115778,
#115779,#115780,#115781,#115782,#115783,#115784,#115785,#115786,#115787,
#115788,#115789,#115790,#115791,#115792,#115793,#115794,#115795,#115796,
#115797,#115798,#115799,#115800,#115801,#115802,#115803,#115804,#115805,
#115806,#115807,#115808,#115809,#115810,#115811,#115812,#115813,#115814,
#115815,#115816,#115817,#115818,#115819,#115820,#115821,#115822,#115823,
#115824,#115825,#115826,#115827,#115828),.UNSPECIFIED.,.F.,.F.,(4,3,3,3,
3,3,3,3,3,3,3,3,3,3,3,3,3,3,3,3,3,3,3,3,3,3,3,3,3,3,3,3,3,3,3,3,3,3,3,3,
3,3,3,3,3,3,3,3,3,3,3,3,3,3,3,3,3,4),(107.936893664275,108.082961511445,
108.18649847487,108.299980162362,108.413260256859,108.526428338887,108.639529211831,
108.752607579042,108.865789885852,108.979023744717,109.092471148062,109.179035158126,
109.292517499002,109.405798239768,109.518966963243,109.632068471743,109.745147467543,
109.858330387305,109.971564851382,110.085012839851,110.171571841382,110.285055033765,
110.398336640939,110.511506239252,110.624608629379,110.737688511965,110.850872319289,
110.964107672719,111.077556542252,111.164108524637,111.277587519026,111.390864923171,
111.504030318546,111.617128513211,111.730204215196,111.843383897961,111.956615151618,
112.07006001287,112.156645207893,112.270129875436,112.383412908333,112.496583901166,
112.609687652534,112.722768860973,112.835953929634,112.949190510518,113.062640537437,
113.149181891149,113.262670135362,113.375956856776,113.489131603515,113.602239166777,
113.715324237775,113.828513215311,113.941753736768,114.055207705859,114.141718574404,
114.220077335694),.UNSPECIFIED.);
#1595=B_SPLINE_CURVE_WITH_KNOTS('',3,(#115834,#115835,#115836,#115837,#115838,
#115839,#115840,#115841,#115842,#115843,#115844,#115845,#115846,#115847,
#115848,#115849,#115850,#115851,#115852,#115853,#115854,#115855,#115856,
#115857,#115858,#115859,#115860,#115861,#115862,#115863,#115864,#115865,
#115866,#115867,#115868,#115869,#115870,#115871,#115872,#115873,#115874,
#115875,#115876,#115877,#115878,#115879,#115880,#115881,#115882,#115883,
#115884,#115885,#115886,#115887,#115888,#115889,#115890,#115891,#115892,
#115893,#115894,#115895,#115896,#115897,#115898,#115899,#115900,#115901,
#115902,#115903,#115904,#115905,#115906,#115907,#115908,#115909,#115910,
#115911,#115912,#115913,#115914,#115915,#115916,#115917,#115918,#115919,
#115920,#115921,#115922,#115923,#115924,#115925,#115926,#115927,#115928,
#115929,#115930,#115931,#115932,#115933,#115934,#115935,#115936,#115937,
#115938,#115939,#115940,#115941,#115942,#115943,#115944,#115945,#115946,
#115947,#115948,#115949,#115950,#115951,#115952,#115953,#115954,#115955,
#115956,#115957,#115958,#115959,#115960,#115961),.UNSPECIFIED.,.F.,.F.,
(4,2,2,2,2,2,2,2,2,2,2,2,2,2,2,2,2,2,2,2,2,2,2,2,2,2,2,2,2,2,2,2,2,2,2,
2,2,2,2,2,2,2,2,2,2,2,2,2,2,2,2,2,2,2,2,2,2,2,2,2,2,2,2,4),(5.09106672909598E-5,
0.0241638658855157,0.0402610837467883,0.0447177340941628,0.0469913146460663,
0.0488360824618075,0.0509655261534932,0.0546261785485025,0.0760251216445918,
0.0930080494465782,0.0989355387576973,0.101616095779122,0.103171951577462,
0.104504145979611,0.104514853444631,0.104525639016062,0.104536506099771,
0.104547458200618,0.104558498952096,0.104569632074016,0.105594347656082,
0.106780654969661,0.108842728681758,0.11774017688508,0.140039196639271,
0.157417603053612,0.160972874249764,0.163043381116964,0.164869773559774,
0.167162963366124,0.171801021217633,0.199299936175907,0.217990666940658,
0.220713933431138,0.222017097616605,0.223034425414255,0.224244351340609,
0.226463601966407,0.23967212336241,0.24541835094314,0.260473127118986,0.2752172229747,
0.278615744141648,0.280636993619903,0.282445322966469,0.284749909850865,
0.289533089930852,0.314228460216545,0.334759859516565,0.337903314582983,
0.339140291152666,0.340165373326709,0.341283659016612,0.343123599689444,
0.3499726812499,0.363844601673138,0.390519682143007,0.395201753085217,0.397500125611384,
0.399323161385334,0.40138188780051,0.404896755452884,0.421487789229422,
0.423925865176554),.UNSPECIFIED.);
#1596=B_SPLINE_CURVE_WITH_KNOTS('',3,(#115964,#115965,#115966,#115967,#115968,
#115969,#115970,#115971,#115972,#115973,#115974,#115975,#115976,#115977,
#115978,#115979,#115980,#115981,#115982,#115983,#115984,#115985,#115986,
#115987,#115988,#115989,#115990,#115991,#115992,#115993,#115994,#115995,
#115996,#115997,#115998,#115999,#116000,#116001,#116002,#116003,#116004,
#116005,#116006,#116007,#116008,#116009,#116010,#116011,#116012,#116013,
#116014,#116015,#116016,#116017,#116018,#116019,#116020,#116021,#116022,
#116023,#116024,#116025,#116026,#116027,#116028,#116029,#116030,#116031,
#116032,#116033,#116034,#116035,#116036,#116037,#116038,#116039,#116040,
#116041,#116042,#116043,#116044,#116045,#116046,#116047,#116048),
 .UNSPECIFIED.,.F.,.F.,(4,3,3,3,3,3,3,3,3,3,3,3,3,3,3,3,3,3,3,3,3,3,3,3,
3,3,3,3,4),(11.6159397475003,11.7280381177179,11.7400068329073,11.8625173551648,
11.985000574511,12.1074989948772,12.2327433538469,12.3554956319205,12.4819860313383,
12.5938879762662,12.608476430756,12.6085211793387,12.7160201566515,12.732543516163,
12.8509131131061,12.9691482104548,13.0873037088547,13.2054343646596,13.3236778484254,
13.4419878521927,13.5543987232013,13.5605159548505,13.6010131140117,13.6010660202626,
13.7087376969109,13.7209698655402,13.8407524390979,13.9603959036733,13.9764226451991),
 .UNSPECIFIED.);
#1597=B_SPLINE_CURVE_WITH_KNOTS('',3,(#116054,#116055,#116056,#116057,#116058,
#116059,#116060,#116061,#116062,#116063,#116064,#116065,#116066,#116067,
#116068,#116069,#116070,#116071,#116072,#116073,#116074,#116075,#116076,
#116077,#116078,#116079,#116080,#116081,#116082,#116083,#116084,#116085,
#116086,#116087,#116088,#116089,#116090,#116091,#116092,#116093,#116094,
#116095,#116096,#116097,#116098,#116099,#116100,#116101,#116102,#116103,
#116104,#116105,#116106,#116107,#116108,#116109,#116110,#116111,#116112,
#116113,#116114,#116115,#116116,#116117,#116118,#116119,#116120,#116121,
#116122,#116123,#116124,#116125,#116126,#116127,#116128,#116129,#116130,
#116131,#116132,#116133,#116134,#116135,#116136,#116137,#116138,#116139,
#116140,#116141,#116142,#116143,#116144,#116145,#116146,#116147,#116148,
#116149,#116150,#116151,#116152,#116153,#116154,#116155,#116156,#116157,
#116158,#116159,#116160,#116161,#116162,#116163,#116164,#116165,#116166,
#116167,#116168,#116169,#116170,#116171,#116172,#116173,#116174,#116175,
#116176,#116177,#116178,#116179,#116180,#116181,#116182,#116183,#116184,
#116185,#116186,#116187,#116188,#116189,#116190,#116191,#116192,#116193,
#116194,#116195,#116196,#116197,#116198,#116199,#116200,#116201,#116202,
#116203,#116204,#116205,#116206,#116207,#116208,#116209,#116210,#116211,
#116212,#116213,#116214,#116215,#116216,#116217,#116218,#116219,#116220,
#116221,#116222,#116223),.UNSPECIFIED.,.F.,.F.,(4,2,2,2,2,2,2,2,2,2,2,2,
2,2,2,2,2,2,2,2,2,2,2,2,2,2,2,2,2,2,2,2,2,2,2,2,2,2,2,2,2,2,2,2,2,2,2,2,
2,2,2,2,2,2,2,2,2,2,2,2,2,2,2,2,2,2,2,2,2,2,2,2,2,2,2,2,2,2,2,2,2,2,2,2,
4),(-0.537557832667611,-0.535822407565533,-0.533634654125646,-0.532427428703531,
-0.531407235965932,-0.530091030383935,-0.527296021085561,-0.523492515533553,
-0.513337621423678,-0.490247128196482,-0.479151045954009,-0.475893689310045,
-0.473893745368097,-0.472063645881055,-0.469672765814631,-0.464476904356826,
-0.457429258263692,-0.436939307823479,-0.43202717347025,-0.418685629751132,
-0.416650093952005,-0.415369771033602,-0.414351691054465,-0.413115744844251,
-0.410726587227658,-0.407622385020085,-0.400191466048869,-0.384364055659647,
-0.362813838478521,-0.359127228137156,-0.357013256213303,-0.355200901098753,
-0.352992086950319,-0.348745846614782,-0.343324203091915,-0.330300118791415,
-0.311929771329025,-0.301326309731941,-0.299179866175964,-0.297981992556847,
-0.296960932217056,-0.29563222951209,-0.292769857080972,-0.274346012216443,
-0.247051904308374,-0.242433765299577,-0.240151119314268,-0.238333560212228,
-0.236273669535154,-0.232738716335032,-0.215622796572841,-0.190654259769387,
-0.183632963573982,-0.181707752431304,-0.18057074189062,-0.179534472604125,
-0.178092968930831,-0.174586179165968,-0.1694481856061,-0.152477628411396,
-0.130236018990756,-0.125473704543816,-0.123133239140147,-0.121386216928384,
-0.119447871239254,-0.11742902584999,-0.11083999507127,-0.101125169307191,
-0.0860054032081894,-0.0800580615520808,-0.0670227603988455,-0.0649914366300091,
-0.0637123042694286,-0.0626946303055396,-0.061458703386694,-0.0590664189302489,
-0.0559563737445437,-0.0485023004235465,-0.0182068521094829,-0.00966129008743767,
-0.00674950767218951,-0.00480121460763317,-0.00306870101462573,-0.00162054454679811,
-9.99999993922529E-7),.UNSPECIFIED.);
#1598=B_SPLINE_CURVE_WITH_KNOTS('',3,(#116224,#116225,#116226,#116227,#116228,
#116229,#116230,#116231,#116232,#116233,#116234,#116235,#116236,#116237,
#116238,#116239,#116240,#116241,#116242,#116243,#116244,#116245,#116246,
#116247,#116248,#116249,#116250,#116251,#116252,#116253,#116254,#116255,
#116256,#116257,#116258,#116259,#116260,#116261,#116262,#116263,#116264,
#116265,#116266,#116267,#116268,#116269,#116270,#116271,#116272,#116273,
#116274,#116275,#116276,#116277,#116278,#116279,#116280,#116281,#116282,
#116283,#116284,#116285,#116286,#116287,#116288,#116289,#116290,#116291,
#116292,#116293,#116294,#116295,#116296,#116297,#116298,#116299,#116300,
#116301,#116302,#116303,#116304,#116305),.UNSPECIFIED.,.F.,.F.,(4,2,2,2,
2,2,2,2,2,2,2,2,2,2,2,2,2,2,2,2,2,2,2,2,2,2,2,2,2,2,2,2,2,2,2,2,2,2,2,2,
4),(0.423925865176554,0.445966310866901,0.453687543410289,0.4556807015525,
0.456835491098318,0.457868929006599,0.459283373692191,0.462623816461385,
0.467436850977327,0.482482956088123,0.507337740573548,0.51202829969512,
0.514378966601517,0.51615821852133,0.516505652530156,0.516613873910271,
0.516692929373497,0.516753226448358,0.516800588070662,0.516838590051585,
0.516869576459979,0.516951159518163,0.517030394606397,0.517107847019529,
0.517184008515704,0.517259315771496,0.517334164442901,0.517408920172034,
0.519810406849302,0.522622828098142,0.545876157858757,0.569321885433324,
0.572016186067571,0.573338107262603,0.574293993891912,0.575357217178122,
0.576948140445213,0.581487184219949,0.588837685997641,0.624889347384345,
0.628477952425298),.UNSPECIFIED.);
#1599=B_SPLINE_CURVE_WITH_KNOTS('',3,(#116306,#116307,#116308,#116309,#116310,
#116311,#116312,#116313,#116314,#116315,#116316,#116317,#116318,#116319,
#116320,#116321,#116322,#116323,#116324,#116325,#116326,#116327,#116328,
#116329,#116330,#116331,#116332,#116333,#116334,#116335,#116336,#116337,
#116338,#116339,#116340,#116341,#116342,#116343,#116344,#116345,#116346,
#116347,#116348,#116349,#116350,#116351,#116352,#116353,#116354,#116355,
#116356,#116357,#116358,#116359,#116360,#116361,#116362,#116363,#116364,
#116365,#116366,#116367,#116368,#116369,#116370,#116371,#116372,#116373,
#116374,#116375,#116376,#116377,#116378,#116379,#116380,#116381,#116382,
#116383,#116384,#116385,#116386,#116387,#116388,#116389,#116390,#116391,
#116392,#116393,#116394,#116395,#116396,#116397,#116398,#116399,#116400,
#116401,#116402,#116403,#116404,#116405,#116406,#116407,#116408,#116409,
#116410,#116411,#116412,#116413,#116414,#116415,#116416,#116417,#116418,
#116419,#116420,#116421,#116422,#116423,#116424,#116425,#116426,#116427,
#116428,#116429,#116430,#116431,#116432,#116433,#116434,#116435,#116436,
#116437,#116438,#116439,#116440,#116441,#116442,#116443,#116444,#116445,
#116446,#116447,#116448,#116449,#116450,#116451,#116452,#116453,#116454,
#116455,#116456,#116457,#116458,#116459,#116460,#116461,#116462,#116463,
#116464,#116465,#116466,#116467,#116468,#116469,#116470,#116471,#116472,
#116473,#116474,#116475,#116476,#116477,#116478,#116479,#116480,#116481,
#116482,#116483,#116484,#116485,#116486,#116487,#116488,#116489,#116490,
#116491,#116492,#116493,#116494,#116495,#116496,#116497,#116498,#116499,
#116500,#116501,#116502,#116503,#116504,#116505,#116506,#116507,#116508,
#116509,#116510,#116511,#116512,#116513,#116514,#116515,#116516,#116517,
#116518,#116519,#116520,#116521,#116522,#116523,#116524,#116525),
 .UNSPECIFIED.,.F.,.F.,(4,2,2,2,2,2,2,2,2,2,2,2,2,2,2,2,2,2,2,2,2,2,2,2,
2,2,2,2,2,2,2,2,2,2,2,2,2,2,2,2,2,2,2,2,2,2,2,2,2,2,2,2,2,2,2,2,2,2,2,2,
2,2,2,2,2,2,2,2,2,2,2,2,2,2,2,2,2,2,2,2,2,2,2,2,2,2,2,2,2,2,2,2,2,2,2,2,
2,2,2,2,2,2,2,2,2,2,2,2,2,4),(-2.96685071646963,-2.96055947965241,-2.95644349840884,
-2.95422512500191,-2.95245698616293,-2.9506211714232,-2.94849416910481,
-2.9448387276036,-2.93163531286041,-2.91649164060133,-2.90029701081475,
-2.89656855353828,-2.8950683705804,-2.89400191143488,-2.89285870437891,
-2.89093544498106,-2.88408124946649,-2.85875094045842,-2.84766371052407,
-2.84277412466187,-2.8388888769862,-2.83728665315147,-2.83547812721969,
-2.83349513943704,-2.83033890944714,-2.82029582524522,-2.7961230389042,
-2.78210744933936,-2.77903582942547,-2.7776689790042,-2.77664590172264,
-2.77548101227555,-2.77345890762965,-2.76479906529147,-2.76248826270108,
-2.74424710289187,-2.7312720169271,-2.72587375428122,-2.72164806535048,
-2.71945405233847,-2.71765619236946,-2.71556208005707,-2.71191866305611,
-2.68955581852852,-2.67199312687268,-2.66599265095168,-2.66207025520308,
-2.66057291134113,-2.65953291497752,-2.65856058829398,-2.65689414832487,
-2.65218513278725,-2.61674971392236,-2.60984982800802,-2.6047346107735,
-2.60235656897141,-2.60052617308624,-2.59851572976238,-2.59521757227466,
-2.58389764061721,-2.56084054661053,-2.55102794106124,-2.54730552337839,
-2.54455550097753,-2.54324554721334,-2.5422241112739,-2.54100845677239,
-2.53878305122664,-2.52575226024882,-2.51985463861266,-2.50478727050801,
-2.49014547046221,-2.48674006043157,-2.48470917714537,-2.48288850132405,
-2.48056271150524,-2.47571313289205,-2.45496249108257,-2.43674492946519,
-2.43141565992467,-2.42781453603598,-2.42635972695186,-2.42532300846213,
-2.42419568442349,-2.42230706918312,-2.41566697987194,-2.39019458588422,
-2.37318972293653,-2.36966523080757,-2.3676104276467,-2.36579679786522,
-2.36351839421594,-2.35890669529677,-2.33160000037571,-2.3124423664972,
-2.31005872141856,-2.30882546361495,-2.30780896923787,-2.30653008426544,
-2.30449694568281,-2.29198510522542,-2.28616183607307,-2.27199621039738,
-2.2573640741646,-2.25307580917052,-2.25085935356893,-2.24904768859936,
-2.24694237793296,-2.24329086251894,-2.22543560030778),.UNSPECIFIED.);
#1600=B_SPLINE_CURVE_WITH_KNOTS('',3,(#116530,#116531,#116532,#116533,#116534,
#116535,#116536,#116537,#116538,#116539,#116540,#116541,#116542,#116543,
#116544,#116545,#116546,#116547,#116548,#116549,#116550,#116551,#116552,
#116553,#116554,#116555,#116556,#116557,#116558,#116559,#116560,#116561,
#116562,#116563,#116564,#116565,#116566,#116567,#116568,#116569,#116570,
#116571,#116572,#116573,#116574,#116575,#116576,#116577,#116578,#116579,
#116580,#116581,#116582,#116583,#116584,#116585,#116586,#116587,#116588,
#116589,#116590,#116591,#116592,#116593,#116594,#116595,#116596,#116597,
#116598,#116599,#116600,#116601,#116602,#116603,#116604,#116605,#116606,
#116607,#116608,#116609,#116610,#116611,#116612,#116613,#116614,#116615,
#116616,#116617,#116618,#116619,#116620,#116621,#116622,#116623,#116624,
#116625,#116626,#116627,#116628,#116629,#116630,#116631,#116632,#116633,
#116634,#116635,#116636,#116637,#116638,#116639,#116640,#116641,#116642,
#116643,#116644,#116645,#116646,#116647,#116648,#116649,#116650,#116651,
#116652,#116653,#116654,#116655,#116656,#116657,#116658,#116659,#116660,
#116661,#116662,#116663,#116664,#116665,#116666,#116667,#116668,#116669,
#116670,#116671,#116672,#116673,#116674,#116675,#116676,#116677,#116678,
#116679,#116680,#116681,#116682,#116683,#116684,#116685,#116686,#116687,
#116688,#116689,#116690,#116691,#116692,#116693,#116694,#116695,#116696,
#116697,#116698,#116699,#116700,#116701,#116702,#116703,#116704,#116705,
#116706,#116707,#116708,#116709,#116710,#116711,#116712,#116713,#116714,
#116715,#116716,#116717,#116718,#116719,#116720,#116721,#116722,#116723,
#116724,#116725,#116726,#116727,#116728,#116729),.UNSPECIFIED.,.F.,.F.,
(4,2,2,2,2,2,2,2,2,2,2,2,2,2,2,2,2,2,2,2,2,2,2,2,2,2,2,2,2,2,2,2,2,2,2,
2,2,2,2,2,2,2,2,2,2,2,2,2,2,2,2,2,2,2,2,2,2,2,2,2,2,2,2,2,2,2,2,2,2,2,2,
2,2,2,2,2,2,2,2,2,2,2,2,2,2,2,2,2,2,2,2,2,2,2,2,2,2,2,2,4),(-1.27961565155533,
-1.27297154738489,-1.25817211112012,-1.25204962479169,-1.23923900027455,
-1.23719605956918,-1.23591369383386,-1.23489572689644,-1.23366200019947,
-1.23128322551577,-1.21220821504543,-1.18480637761599,-1.18020125751498,
-1.17792150087167,-1.17610462027137,-1.17404376132814,-1.17050274441277,
-1.15323151340705,-1.12942437499849,-1.12155796802723,-1.11955841934318,
-1.11840539889111,-1.11737544514129,-1.11597092924467,-1.1126821094562,
-1.10796712845717,-1.09345280017569,-1.06780649672651,-1.06307131797335,
-1.06076646781195,-1.05894714564179,-1.05690204580128,-1.05343427489531,
-1.03770691156908,-1.01401711910753,-1.00454473900329,-1.00246327074327,
-1.00128011226314,-1.00035961713557,-0.999067045670789,-0.996394165447802,
-0.980423173921308,-0.952755332360289,-0.946676309849489,-0.94432164773791,
-0.942606667433677,-0.940757507371457,-0.93823936220053,-0.932301733272365,
-0.923878025266427,-0.892019365888256,-0.886646637842979,-0.884893253039671,
-0.883794326630226,-0.882739625746801,-0.881193921466839,-0.876993428202555,
-0.870408633008915,-0.856039535161199,-0.833524025299349,-0.828687430490428,
-0.826363109590969,-0.824541487119236,-0.822507375886747,-0.819091323474351,
-0.804306172510864,-0.789287267072459,-0.782851102148691,-0.770368449340278,
-0.768335418519258,-0.767055949957634,-0.766037984958139,-0.764801471243592,
-0.762409476468235,-0.759300495607515,-0.751852196982988,-0.736041497487957,
-0.714471002413865,-0.710806290360515,-0.70869725023484,-0.706884661565346,
-0.70466996099924,-0.700394437015238,-0.67882456183225,-0.654118764459058,
-0.651256045966331,-0.649941382691362,-0.648919551934597,-0.647727228259855,
-0.645546341251571,-0.632538709536092,-0.604766886209205,-0.595902137899208,
-0.592889513063825,-0.590942534810059,-0.589092493672625,-0.586570151213908,
-0.580608059708203,-0.547418652798889,-0.537557832667611),.UNSPECIFIED.);
#1601=B_SPLINE_CURVE_WITH_KNOTS('',3,(#116730,#116731,#116732,#116733,#116734,
#116735,#116736,#116737,#116738,#116739,#116740,#116741,#116742,#116743,
#116744,#116745,#116746,#116747,#116748,#116749,#116750,#116751,#116752,
#116753,#116754,#116755,#116756,#116757,#116758,#116759,#116760,#116761,
#116762,#116763,#116764,#116765,#116766,#116767,#116768,#116769,#116770,
#116771,#116772,#116773,#116774,#116775,#116776,#116777,#116778,#116779,
#116780,#116781,#116782,#116783,#116784,#116785,#116786,#116787,#116788,
#116789,#116790,#116791,#116792,#116793,#116794,#116795,#116796,#116797,
#116798,#116799,#116800,#116801,#116802,#116803,#116804,#116805,#116806,
#116807,#116808,#116809,#116810,#116811,#116812,#116813,#116814,#116815,
#116816,#116817,#116818,#116819,#116820,#116821,#116822,#116823,#116824,
#116825,#116826,#116827,#116828,#116829,#116830,#116831,#116832,#116833,
#116834,#116835,#116836,#116837,#116838,#116839,#116840,#116841,#116842,
#116843,#116844,#116845,#116846,#116847,#116848,#116849,#116850,#116851,
#116852,#116853,#116854,#116855,#116856,#116857,#116858,#116859,#116860,
#116861,#116862,#116863,#116864,#116865,#116866,#116867,#116868,#116869,
#116870,#116871,#116872,#116873,#116874,#116875,#116876,#116877,#116878,
#116879,#116880,#116881,#116882,#116883,#116884,#116885,#116886,#116887,
#116888,#116889,#116890,#116891,#116892,#116893,#116894,#116895,#116896,
#116897,#116898,#116899,#116900,#116901,#116902,#116903,#116904,#116905,
#116906,#116907,#116908,#116909,#116910,#116911,#116912,#116913,#116914,
#116915,#116916,#116917,#116918,#116919,#116920,#116921,#116922,#116923,
#116924,#116925,#116926,#116927,#116928,#116929,#116930,#116931,#116932,
#116933,#116934,#116935,#116936,#116937,#116938,#116939,#116940,#116941,
#116942,#116943),.UNSPECIFIED.,.F.,.F.,(4,2,2,2,2,2,2,2,2,2,2,2,2,2,2,2,
2,2,2,2,2,2,2,2,2,2,2,2,2,2,2,2,2,2,2,2,2,2,2,2,2,2,2,2,2,2,2,2,2,2,2,2,
2,2,2,2,2,2,2,2,2,2,2,2,2,2,2,2,2,2,2,2,2,2,2,2,2,2,2,2,2,2,2,2,2,2,2,2,
2,2,2,2,2,2,2,2,2,2,2,2,2,2,2,2,2,2,4),(-2.22543560030778,-2.22346995110092,
-2.19766668743467,-2.19369352880723,-2.19218089423719,-2.19113291758194,
-2.19002472527881,-2.18822657659134,-2.18246509920158,-2.17453946428187,
-2.15761531171578,-2.14023848126831,-2.13596883444132,-2.13375659654113,
-2.13194574075725,-2.12983840606076,-2.1261759035639,-2.10460241237019,
-2.08878669957219,-2.08134069297737,-2.07823339232187,-2.07584309019904,
-2.07460770676217,-2.07359085883657,-2.07231307992573,-2.07028325392101,
-2.0573292418964,-2.05134704593693,-2.03628211938002,-2.02160563381292,
-2.01819874955883,-2.0161680453255,-2.0143482087055,-2.01202444059825,-2.00718266000176,
-1.98640745700003,-1.96823701680219,-1.96291549160832,-1.95931821305553,
-1.95786377303689,-1.95682672861602,-1.9556977767367,-1.95380520587897,
-1.94713648574973,-1.94057297743912,-1.93483669394144,-1.92066836599361,
-1.90462735267213,-1.90114557885655,-1.89909841656881,-1.89728103142439,
-1.89498374134024,-1.89028269729641,-1.86409570078748,-1.84390585352744,
-1.8415628523317,-1.84033701157129,-1.83931941830871,-1.83802977064273,
-1.83596085311572,-1.81957867583272,-1.79844854979183,-1.78691121105397,
-1.78372726249022,-1.78174458661736,-1.77991173483215,-1.77753120883033,
-1.77223997334062,-1.74359891010144,-1.73190742382553,-1.72573211176272,
-1.72395573001499,-1.72285234140212,-1.72181421325108,-1.72029708341537,
-1.71741135408668,-1.69876256518131,-1.68659007488242,-1.67034632885863,
-1.66685429501999,-1.66480483018073,-1.66298766513066,-1.66069370763473,
-1.65601052653078,-1.62954610873251,-1.61557903138443,-1.61096730234711,
-1.60773339236998,-1.60633881514178,-1.60531082600416,-1.60415400827282,
-1.60213497191957,-1.59399314372386,-1.57057663470836,-1.55327373188853,
-1.54973316449134,-1.5476732062146,-1.54585750638439,-1.54357975590212,
-1.53913100716567,-1.51077344741973,-1.49233899208333,-1.49004889907942,
-1.48883402383142,-1.48781555479757,-1.48651205680211,-1.48387134362921),
 .UNSPECIFIED.);
#1602=B_SPLINE_CURVE_WITH_KNOTS('',3,(#116948,#116949,#116950,#116951,#116952,
#116953,#116954,#116955,#116956,#116957,#116958,#116959,#116960,#116961,
#116962,#116963,#116964,#116965,#116966,#116967,#116968,#116969,#116970,
#116971,#116972,#116973,#116974,#116975,#116976,#116977,#116978,#116979,
#116980,#116981,#116982,#116983,#116984,#116985,#116986,#116987,#116988,
#116989,#116990,#116991,#116992,#116993,#116994,#116995,#116996,#116997,
#116998,#116999,#117000,#117001,#117002,#117003,#117004,#117005,#117006,
#117007,#117008,#117009,#117010,#117011,#117012,#117013,#117014,#117015,
#117016,#117017,#117018,#117019,#117020,#117021,#117022,#117023,#117024,
#117025,#117026,#117027,#117028,#117029,#117030,#117031,#117032,#117033,
#117034,#117035,#117036,#117037,#117038,#117039,#117040,#117041,#117042,
#117043,#117044,#117045,#117046,#117047,#117048,#117049,#117050,#117051,
#117052,#117053,#117054,#117055,#117056,#117057,#117058,#117059,#117060,
#117061,#117062,#117063,#117064,#117065,#117066,#117067,#117068,#117069,
#117070,#117071,#117072,#117073,#117074,#117075,#117076,#117077,#117078,
#117079,#117080,#117081,#117082,#117083,#117084,#117085,#117086,#117087,
#117088,#117089,#117090,#117091,#117092,#117093,#117094,#117095,#117096,
#117097,#117098,#117099,#117100,#117101,#117102,#117103,#117104,#117105,
#117106,#117107,#117108,#117109,#117110,#117111,#117112,#117113,#117114,
#117115,#117116,#117117,#117118,#117119,#117120,#117121,#117122,#117123,
#117124,#117125,#117126,#117127,#117128,#117129,#117130,#117131,#117132,
#117133,#117134,#117135,#117136,#117137,#117138,#117139,#117140,#117141,
#117142,#117143,#117144,#117145,#117146,#117147,#117148,#117149,#117150,
#117151),.UNSPECIFIED.,.F.,.F.,(4,2,2,2,2,2,2,2,2,2,2,2,2,2,2,2,2,2,2,2,
2,2,2,2,2,2,2,2,2,2,2,2,2,2,2,2,2,2,2,2,2,2,2,2,2,2,2,2,2,2,2,2,2,2,2,2,
2,2,2,2,2,2,2,2,2,2,2,2,2,2,2,2,2,2,2,2,2,2,2,2,2,2,2,2,2,2,2,2,2,2,2,2,
2,2,2,2,2,2,2,2,2,4),(-2.02159988673811,-2.01023874891081,-2.00476139218147,
-2.00048106180913,-1.99826561944067,-1.99645327508937,-1.9943454811568,
-1.9906853890789,-1.96900276011331,-1.95310248249342,-1.94221870637194,
-1.94012097174003,-1.93894665041687,-1.93792196804332,-1.9365802692999,
-1.93356724722753,-1.91067655430104,-1.88989982509215,-1.88408416831748,
-1.88158630640505,-1.87974060469866,-1.87778569811498,-1.87473488677416,
-1.86555118526279,-1.83804850031722,-1.8262089759111,-1.82337552390372,
-1.82205235419196,-1.82103190246641,-1.8198304039197,-1.8176674096707,-1.80666123908907,
-1.77305041475846,-1.76696226052818,-1.76441982698929,-1.76256667793041,
-1.76085765001004,-1.75852617640153,-1.75259841564563,-1.71899376981925,
-1.70792022772854,-1.70575424469168,-1.70455206256328,-1.70353165673122,
-1.7022093722014,-1.69938073674376,-1.68758403258962,-1.66018665301785,
-1.65089710486703,-1.64783375461423,-1.64587610473106,-1.64403153343535,
-1.64154097548185,-1.63576948054799,-1.61550340513709,-1.59195506464101,
-1.58901572155697,-1.58766662163375,-1.58664094767425,-1.58547091502716,
-1.58339327701468,-1.57293280076989,-1.54813027272964,-1.53445320006987,
-1.53099939773501,-1.52895731307537,-1.52731948571513,-1.52509955957985,
-1.52079742865841,-1.50557223902687,-1.48217508196827,-1.47329301346568,
-1.47124748926732,-1.47007249173212,-1.46915066797477,-1.46784622188022,
-1.46511175757561,-1.44436385079241,-1.41946169081447,-1.41469162418968,
-1.41238009758397,-1.41056005989801,-1.4085189199942,-1.40506957540279,
-1.38968854045139,-1.36869005698206,-1.36317650789737,-1.3558692392975,
-1.35391959916482,-1.35277750305365,-1.35174406844184,-1.35031651507144,
-1.34689030058723,-1.3419096224148,-1.32589075076654,-1.30233948918634,
-1.29752242087111,-1.29520195404796,-1.29338093701748,-1.29134499790602,
-1.2879197982415,-1.27961565155533),.UNSPECIFIED.);
#1603=B_SPLINE_CURVE_WITH_KNOTS('',3,(#117152,#117153,#117154,#117155,#117156,
#117157,#117158,#117159,#117160,#117161,#117162,#117163,#117164,#117165,
#117166,#117167,#117168,#117169,#117170,#117171,#117172,#117173,#117174,
#117175,#117176,#117177,#117178,#117179,#117180,#117181,#117182,#117183,
#117184,#117185,#117186,#117187,#117188,#117189,#117190,#117191,#117192,
#117193,#117194,#117195,#117196,#117197,#117198,#117199,#117200,#117201,
#117202,#117203,#117204,#117205,#117206,#117207,#117208,#117209,#117210,
#117211,#117212,#117213,#117214,#117215,#117216,#117217,#117218,#117219,
#117220,#117221,#117222,#117223,#117224,#117225,#117226,#117227,#117228,
#117229,#117230,#117231,#117232,#117233,#117234,#117235,#117236,#117237,
#117238,#117239,#117240,#117241,#117242,#117243,#117244,#117245,#117246,
#117247,#117248,#117249,#117250,#117251,#117252,#117253,#117254,#117255,
#117256,#117257,#117258,#117259,#117260,#117261,#117262,#117263,#117264,
#117265,#117266,#117267,#117268,#117269,#117270,#117271,#117272,#117273,
#117274,#117275,#117276,#117277,#117278,#117279,#117280,#117281,#117282,
#117283,#117284,#117285,#117286,#117287,#117288,#117289,#117290,#117291,
#117292,#117293,#117294,#117295,#117296,#117297,#117298,#117299,#117300,
#117301,#117302,#117303,#117304,#117305,#117306,#117307,#117308,#117309,
#117310,#117311,#117312,#117313,#117314,#117315,#117316,#117317,#117318,
#117319,#117320,#117321,#117322,#117323,#117324,#117325,#117326,#117327,
#117328,#117329,#117330,#117331,#117332,#117333,#117334,#117335,#117336,
#117337,#117338,#117339,#117340,#117341,#117342,#117343,#117344,#117345,
#117346,#117347,#117348,#117349,#117350,#117351,#117352,#117353,#117354,
#117355,#117356,#117357),.UNSPECIFIED.,.F.,.F.,(4,2,2,2,2,2,2,2,2,2,2,2,
2,2,2,2,2,2,2,2,2,2,2,2,2,2,2,2,2,2,2,2,2,2,2,2,2,2,2,2,2,2,2,2,2,2,2,2,
2,2,2,2,2,2,2,2,2,2,2,2,2,2,2,2,2,2,2,2,2,2,2,2,2,2,2,2,2,2,2,2,2,2,2,2,
2,2,2,2,2,2,2,2,2,2,2,2,2,2,2,2,2,2,4),(-1.48387134362921,-1.48377999702024,
-1.46315723794815,-1.43813415029469,-1.43337170539462,-1.43106250797207,
-1.42924371447017,-1.42720336243635,-1.42375388509515,-1.4083422761872,
-1.38704739695505,-1.37506804135528,-1.37286554620323,-1.37165565777335,
-1.37063677096227,-1.36932683772982,-1.36656102064039,-1.36280830306064,
-1.35286232469363,-1.32972610022241,-1.31846318547549,-1.31517376640477,
-1.31316805463049,-1.31134171861673,-1.30896874229698,-1.30386433522966,
-1.29697777657784,-1.26171163520227,-1.25685812970614,-1.25517188789329,
-1.25419564337877,-1.25315077728875,-1.25165434126708,-1.247788841154,-1.2419201373854,
-1.21962247097283,-1.20193469350586,-1.19832039525319,-1.19622331836809,
-1.19441093373294,-1.19218371788766,-1.18784253369973,-1.17232706365384,
-1.14657216912726,-1.14006904698983,-1.13818127016854,-1.13705305445912,
-1.13601488192044,-1.13455646060163,-1.13093742878364,-1.12557392212731,
-1.10712523158652,-1.08481734015431,-1.08116132413674,-1.07905480238783,
-1.07724293037825,-1.07502729372302,-1.07074417235852,-1.06526128227778,
-1.05199936901524,-1.0329339726823,-1.0233021801812,-1.0212125850191,-1.02002785178597,
-1.01910800514188,-1.01781879106991,-1.01516171667161,-1.01160016095842,
-1.00243615273952,-0.98032154049671,-0.976874022524991,-0.966643428518402,
-0.963476480296804,-0.96149693748438,-0.959661951932099,-0.957229891846341,
-0.951797079031165,-0.927113465870233,-0.907790871667674,-0.904920845167456,
-0.903407487642196,-0.902369759714737,-0.9012644969737,-0.899480953313526,
-0.893236370584017,-0.881336325875826,-0.851477393574428,-0.847588927226387,
-0.845246357168156,-0.843418426218387,-0.841416548376831,-0.838146247005505,
-0.825537529619766,-0.794520541486454,-0.788375703241604,-0.78653492087652,
-0.785416997372842,-0.784373940272735,-0.782888147237172,-0.77909382736156,
-0.773373272137859,-0.752303317712854,-0.741992569555718),.UNSPECIFIED.);
#1604=B_SPLINE_CURVE_WITH_KNOTS('',3,(#117362,#117363,#117364,#117365,#117366,
#117367,#117368,#117369,#117370,#117371,#117372,#117373,#117374,#117375,
#117376,#117377,#117378,#117379,#117380,#117381,#117382,#117383,#117384,
#117385,#117386,#117387,#117388,#117389,#117390,#117391,#117392,#117393,
#117394,#117395,#117396,#117397,#117398,#117399,#117400,#117401,#117402,
#117403,#117404,#117405,#117406,#117407,#117408,#117409,#117410,#117411,
#117412,#117413,#117414,#117415,#117416,#117417,#117418,#117419,#117420,
#117421,#117422,#117423,#117424,#117425,#117426,#117427,#117428,#117429,
#117430,#117431,#117432,#117433,#117434,#117435,#117436,#117437,#117438,
#117439,#117440,#117441,#117442,#117443,#117444,#117445,#117446,#117447,
#117448,#117449,#117450,#117451,#117452,#117453,#117454,#117455,#117456,
#117457,#117458,#117459,#117460,#117461,#117462,#117463,#117464,#117465,
#117466,#117467,#117468,#117469,#117470,#117471,#117472,#117473,#117474,
#117475,#117476,#117477,#117478,#117479,#117480,#117481,#117482,#117483,
#117484,#117485,#117486,#117487,#117488,#117489,#117490,#117491,#117492,
#117493,#117494,#117495,#117496,#117497,#117498,#117499,#117500,#117501,
#117502,#117503,#117504,#117505,#117506,#117507,#117508,#117509,#117510,
#117511,#117512,#117513,#117514,#117515,#117516,#117517,#117518,#117519,
#117520,#117521,#117522,#117523,#117524,#117525,#117526,#117527,#117528,
#117529,#117530,#117531,#117532,#117533,#117534,#117535,#117536,#117537,
#117538,#117539,#117540,#117541,#117542,#117543,#117544,#117545,#117546,
#117547,#117548,#117549,#117550,#117551,#117552,#117553,#117554,#117555,
#117556,#117557,#117558,#117559,#117560,#117561,#117562,#117563,#117564,
#117565,#117566,#117567,#117568,#117569,#117570,#117571,#117572,#117573,
#117574,#117575),.UNSPECIFIED.,.F.,.F.,(4,2,2,2,2,2,2,2,2,2,2,2,2,2,2,2,
2,2,2,2,2,2,2,2,2,2,2,2,2,2,2,2,2,2,2,2,2,2,2,2,2,2,2,2,2,2,2,2,2,2,2,2,
2,2,2,2,2,2,2,2,2,2,2,2,2,2,2,2,2,2,2,2,2,2,2,2,2,2,2,2,2,2,2,2,2,2,2,2,
2,2,2,2,2,2,2,2,2,2,2,2,2,2,2,2,2,2,4),(-2.76333442860709,-2.76333283318913,
-2.76068421758337,-2.75939667777254,-2.75847703137243,-2.75729111816091,
-2.75519622044825,-2.74546055096043,-2.72204380573131,-2.70637394934725,
-2.70291038561152,-2.70086669644073,-2.69904797092557,-2.69674298407476,
-2.6920043013292,-2.66644103123076,-2.65186306973592,-2.64713693765569,
-2.64384289432828,-2.64243781001507,-2.64140809953394,-2.64025606848278,
-2.63825980070012,-2.63042820661761,-2.60660521887019,-2.58935394258163,
-2.58581502241089,-2.58375509013378,-2.58193884709238,-2.57965965269024,
-2.57505486325027,-2.54765370769002,-2.52857370256385,-2.52619431060883,
-2.52496071488969,-2.52394310882237,-2.52266152223482,-2.52062044354352,
-2.50786845093339,-2.50171570027642,-2.48696620136139,-2.47198610863194,
-2.46856010726826,-2.4665244319741,-2.4647041052505,-2.46238514244044,-2.4575735596559,
-2.43384322357729,-2.41794861781208,-2.41298942078168,-2.40957479272484,
-2.40814943301167,-2.40711661658967,-2.40597410768787,-2.40402153207336,
-2.39667421855921,-2.37219136413258,-2.35502329163313,-2.35148777367013,
-2.34942848327379,-2.34761200604477,-2.34533145334806,-2.34072016310816,
-2.31338254103153,-2.29997954768587,-2.2932698555125,-2.29144319627224,
-2.29032841871975,-2.28929572498656,-2.28804280562818,-2.28483351190113,
-2.2669858372421,-2.25102750315509,-2.24205204956476,-2.23583113164242,
-2.23326770717714,-2.23141107475487,-2.22970698791456,-2.22739479686671,
-2.22158245255139,-2.18670116004057,-2.17651391584756,-2.17445007223402,
-2.17328312112535,-2.17225690792152,-2.17090294959828,-2.16782034662982,
-2.14609448340949,-2.12912665379621,-2.12276692297633,-2.11796266727518,
-2.11564478307702,-2.11382422033606,-2.11178715526263,-2.10835608385699,
-2.09512584728045,-2.07301216042403,-2.06387076306505,-2.06031472479081,
-2.05766089717045,-2.05637211286587,-2.05545210550099,-2.05426646501974,
-2.05217370664708,-2.04248713622254,-2.02347769295184,-2.02159988673811),
 .UNSPECIFIED.);
#1605=B_SPLINE_CURVE_WITH_KNOTS('',3,(#117576,#117577,#117578,#117579,#117580,
#117581,#117582,#117583,#117584,#117585,#117586,#117587,#117588,#117589,
#117590,#117591,#117592,#117593,#117594,#117595,#117596,#117597,#117598,
#117599,#117600,#117601,#117602,#117603,#117604,#117605,#117606,#117607,
#117608,#117609,#117610,#117611,#117612,#117613,#117614,#117615,#117616,
#117617,#117618,#117619,#117620,#117621,#117622,#117623,#117624,#117625,
#117626,#117627,#117628,#117629,#117630,#117631,#117632,#117633,#117634,
#117635,#117636,#117637,#117638,#117639,#117640,#117641,#117642,#117643,
#117644,#117645,#117646,#117647,#117648,#117649,#117650,#117651,#117652,
#117653,#117654,#117655,#117656,#117657,#117658,#117659,#117660,#117661,
#117662,#117663,#117664,#117665,#117666,#117667,#117668,#117669,#117670,
#117671,#117672,#117673,#117674,#117675,#117676,#117677,#117678,#117679,
#117680,#117681,#117682,#117683,#117684,#117685,#117686,#117687,#117688,
#117689,#117690,#117691,#117692,#117693,#117694,#117695,#117696,#117697,
#117698,#117699,#117700,#117701,#117702,#117703,#117704,#117705,#117706,
#117707,#117708,#117709,#117710,#117711,#117712,#117713,#117714,#117715,
#117716,#117717,#117718,#117719,#117720,#117721,#117722,#117723,#117724,
#117725,#117726,#117727,#117728,#117729,#117730,#117731,#117732,#117733,
#117734,#117735,#117736,#117737,#117738,#117739,#117740,#117741,#117742,
#117743,#117744,#117745,#117746,#117747,#117748,#117749,#117750,#117751,
#117752,#117753,#117754,#117755,#117756,#117757,#117758,#117759,#117760,
#117761,#117762,#117763,#117764,#117765,#117766,#117767,#117768,#117769,
#117770,#117771,#117772,#117773,#117774,#117775,#117776,#117777,#117778,
#117779,#117780,#117781,#117782,#117783,#117784,#117785,#117786,#117787,
#117788,#117789,#117790,#117791,#117792,#117793,#117794,#117795,#117796,
#117797,#117798,#117799,#117800,#117801,#117802,#117803,#117804,#117805,
#117806,#117807,#117808,#117809,#117810,#117811,#117812,#117813,#117814,
#117815,#117816,#117817,#117818,#117819,#117820,#117821,#117822,#117823,
#117824,#117825,#117826,#117827,#117828,#117829,#117830,#117831),
 .UNSPECIFIED.,.F.,.F.,(4,2,2,2,2,2,2,2,2,2,2,2,2,2,2,2,2,2,2,2,2,2,2,2,
2,2,2,2,2,2,2,2,2,2,2,2,2,2,2,2,2,2,2,2,2,2,2,2,2,2,2,2,2,2,2,2,2,2,2,2,
2,2,2,2,2,2,2,2,2,2,2,2,2,2,2,2,2,2,2,2,2,2,2,2,2,2,2,2,2,2,2,2,2,2,2,2,
2,2,2,2,2,2,2,2,2,2,2,2,2,2,2,2,2,2,2,2,2,2,2,2,2,2,2,2,2,2,2,4),(-0.741992569555718,
-0.73318870284283,-0.729544201474817,-0.72744012484644,-0.725627892883925,
-0.723408709494159,-0.719108690195953,-0.698710957662591,-0.676815334076249,
-0.671082751472562,-0.669287268239637,-0.668179306736096,-0.667130835562251,
-0.665615972295351,-0.661627853229084,-0.635574802920313,-0.615979417880168,
-0.612329099901808,-0.610223693915561,-0.608411508990924,-0.606193886264462,
-0.601901750326023,-0.574660631713768,-0.556146881016924,-0.552949987367722,
-0.551698911756885,-0.55066658726682,-0.549550740848841,-0.547719605691151,
-0.540960731484522,-0.527393877360477,-0.50032045343663,-0.495684922990846,
-0.493399515498577,-0.491582416478181,-0.489525891164254,-0.486003918819416,
-0.469156001182718,-0.443411036230704,-0.436804851844572,-0.434917651980441,
-0.433789425269804,-0.432750961736503,-0.431291737825382,-0.427668733650887,
-0.422297610217772,-0.403800552084539,-0.381543276603508,-0.377887030756206,
-0.375780204774764,-0.373967970320406,-0.371751763604743,-0.367467131324538,
-0.361982062257574,-0.348713292113806,-0.329632105657695,-0.320015336911719,
-0.317926239922814,-0.316741479352543,-0.315821422152957,-0.314531668249012,
-0.311872599352975,-0.308307780362068,-0.299131738821657,-0.276999731355626,
-0.263835630332816,-0.260414487317775,-0.258379646139239,-0.256558803036898,
-0.254237459345754,-0.249414573004908,-0.243021937136065,-0.225901994101888,
-0.204380046542002,-0.201276607848063,-0.199919020965707,-0.198892358721255,
-0.197727576686562,-0.195673638922233,-0.185675182893973,-0.170669577703329,
-0.149049340936359,-0.144188447454653,-0.141859933535519,-0.140038284626923,
-0.139966586884795,-0.139892322074679,-0.139833040363475,-0.13978570294262,
-0.13974788951397,-0.139717673366876,-0.139693520463697,-0.139652268856524,
-0.139612907247453,-0.139575334970087,-0.139539457351,-0.139505185367904,
-0.1394724353068,-0.139441128439938,-0.139411190722675,-0.139382552491046,
-0.13935514818376,-0.139328916082467,-0.139303798069155,-0.139279739377783,
-0.139256688398259,-0.139234596455869,-0.137002123313113,-0.132221133101487,
-0.125843419857235,-0.108793559695371,-0.0871769081942999,-0.0840706230298656,
-0.0827125328941422,-0.0816857959390228,-0.0805212845319382,-0.0784686181302189,
-0.0685069531331131,-0.0556620206200613,-0.0401284664204443,-0.0291025594357174,
-0.0258527632426961,-0.0238549937213871,-0.0220252775992914,-0.0202402506975366,
-0.0179126868020217,-0.0119193789141974,-9.99999999473644E-7),
 .UNSPECIFIED.);
#1606=B_SPLINE_CURVE_WITH_KNOTS('',3,(#117837,#117838,#117839,#117840),
 .UNSPECIFIED.,.F.,.F.,(4,4),(-7.37639246660687E-6,-1.00000002898216E-6),
 .UNSPECIFIED.);
#1607=B_SPLINE_CURVE_WITH_KNOTS('',3,(#117841,#117842,#117843,#117844,#117845,
#117846,#117847,#117848,#117849,#117850,#117851,#117852,#117853,#117854,
#117855,#117856,#117857,#117858,#117859,#117860,#117861,#117862,#117863,
#117864,#117865,#117866,#117867,#117868,#117869,#117870,#117871,#117872,
#117873,#117874,#117875,#117876,#117877,#117878,#117879,#117880,#117881,
#117882,#117883,#117884,#117885,#117886,#117887,#117888,#117889,#117890,
#117891,#117892,#117893,#117894,#117895,#117896,#117897,#117898,#117899,
#117900,#117901,#117902,#117903,#117904,#117905,#117906,#117907,#117908,
#117909,#117910,#117911,#117912,#117913,#117914,#117915,#117916,#117917,
#117918,#117919,#117920,#117921,#117922,#117923,#117924,#117925,#117926,
#117927,#117928,#117929,#117930,#117931,#117932,#117933,#117934,#117935,
#117936,#117937,#117938,#117939,#117940,#117941,#117942,#117943,#117944,
#117945,#117946,#117947,#117948,#117949,#117950,#117951,#117952,#117953,
#117954,#117955,#117956,#117957,#117958,#117959,#117960,#117961,#117962,
#117963,#117964,#117965,#117966,#117967,#117968,#117969,#117970,#117971,
#117972,#117973,#117974,#117975,#117976,#117977,#117978,#117979,#117980,
#117981,#117982,#117983,#117984,#117985,#117986,#117987,#117988,#117989,
#117990,#117991,#117992,#117993,#117994,#117995,#117996,#117997,#117998,
#117999,#118000,#118001,#118002,#118003,#118004,#118005,#118006,#118007,
#118008,#118009,#118010,#118011,#118012,#118013,#118014,#118015,#118016,
#118017,#118018,#118019,#118020,#118021,#118022,#118023,#118024,#118025,
#118026,#118027,#118028,#118029,#118030,#118031,#118032,#118033,#118034,
#118035,#118036,#118037,#118038),.UNSPECIFIED.,.F.,.F.,(4,2,2,2,2,2,2,2,
2,2,2,2,2,2,2,2,2,2,2,2,2,2,2,2,2,2,2,2,2,2,2,2,2,2,2,2,2,2,2,2,2,2,2,2,
2,2,2,2,2,2,2,2,2,2,2,2,2,2,2,2,2,2,2,2,2,2,2,2,2,2,2,2,2,2,2,2,2,2,2,2,
2,2,2,2,2,2,2,2,2,2,2,2,2,2,2,2,2,2,4),(-3.50505994913951,-3.47315403237273,
-3.46775638294582,-3.46412091975709,-3.46266001459946,-3.46162152312737,
-3.46049449643126,-3.45861169729268,-3.45207912793899,-3.42151459665575,
-3.41319486600962,-3.40916149875354,-3.405844748922,-3.40387667570559,-3.40206020637225,
-3.39977588084231,-3.39514355310517,-3.3681740534866,-3.35453116357743,
-3.34775157983184,-3.3459190072022,-3.3448030816471,-3.34377129766263,-3.34252149820814,
-3.33933111088432,-3.32091973657367,-3.3085606603361,-3.2922666791688,-3.28877179370144,
-3.28672145357713,-3.28490398551821,-3.28261027070267,-3.27808552992817,
-3.25045211862615,-3.23210446468634,-3.22939123268064,-3.2280912179084,
-3.2271702655456,-3.22599322079007,-3.2239372834672,-3.21487057319751,-3.1954261927615,
-3.17649417550572,-3.17220033200873,-3.16998265801461,-3.16817081999811,
-3.16606624589857,-3.16241843340655,-3.14299208292389,-3.12218336990926,
-3.11649610308137,-3.11271852186062,-3.11123545095678,-3.11019302404303,
-3.10907437217193,-3.10722972766805,-3.10104586735349,-3.0701072550709,
-3.06175744616636,-3.05585852503814,-3.05334751972596,-3.05150025881259,
-3.04955115883133,-3.04652485756429,-3.03753851975265,-3.00988138395361,
-2.99798279447741,-2.99514317674569,-2.99381919458604,-2.99279906792931,
-2.9915990726788,-2.98944140454965,-2.97854507599638,-2.94491057303494,
-2.93877172904217,-2.93622183601537,-2.93436800015261,-2.93266163317722,
-2.93033888045945,-2.92446095743522,-2.88968186573152,-2.8795037355228,
-2.87744081810128,-2.8762742821151,-2.87524835897929,-2.87389468678925,
-2.87081233432166,-2.84910487704185,-2.83213431964646,-2.82577481456576,
-2.82097102244665,-2.81865364521651,-2.81683360481558,-2.81479725323633,
-2.81136769791102,-2.79805617471201,-2.77598814858421,-2.76688011497481,
-2.76333442860709),.UNSPECIFIED.);
#1608=B_SPLINE_CURVE_WITH_KNOTS('',3,(#118039,#118040,#118041,#118042,#118043,
#118044,#118045,#118046,#118047,#118048,#118049,#118050,#118051,#118052,
#118053,#118054,#118055,#118056,#118057,#118058,#118059,#118060,#118061,
#118062,#118063,#118064,#118065,#118066,#118067,#118068,#118069,#118070,
#118071,#118072,#118073,#118074,#118075,#118076,#118077,#118078,#118079,
#118080,#118081,#118082,#118083,#118084,#118085,#118086,#118087,#118088,
#118089,#118090,#118091,#118092,#118093,#118094,#118095,#118096,#118097,
#118098,#118099,#118100,#118101,#118102,#118103,#118104,#118105,#118106,
#118107,#118108,#118109,#118110,#118111,#118112,#118113,#118114,#118115,
#118116,#118117,#118118,#118119,#118120,#118121,#118122,#118123,#118124,
#118125,#118126,#118127,#118128,#118129,#118130,#118131,#118132,#118133,
#118134,#118135,#118136,#118137,#118138,#118139,#118140,#118141,#118142,
#118143,#118144,#118145,#118146,#118147,#118148,#118149,#118150,#118151,
#118152,#118153,#118154,#118155,#118156,#118157,#118158,#118159,#118160,
#118161,#118162,#118163,#118164,#118165,#118166,#118167,#118168,#118169,
#118170,#118171,#118172,#118173,#118174,#118175,#118176,#118177,#118178,
#118179,#118180,#118181,#118182,#118183,#118184,#118185,#118186,#118187,
#118188,#118189,#118190,#118191,#118192,#118193,#118194,#118195,#118196,
#118197,#118198,#118199,#118200,#118201,#118202,#118203,#118204,#118205,
#118206,#118207,#118208,#118209,#118210,#118211,#118212,#118213,#118214,
#118215,#118216,#118217,#118218,#118219,#118220,#118221,#118222,#118223,
#118224,#118225,#118226,#118227,#118228,#118229,#118230,#118231,#118232,
#118233,#118234,#118235,#118236,#118237,#118238,#118239,#118240,#118241,
#118242,#118243,#118244,#118245,#118246,#118247,#118248,#118249,#118250,
#118251,#118252,#118253,#118254,#118255,#118256,#118257,#118258,#118259,
#118260,#118261,#118262,#118263,#118264,#118265,#118266),.UNSPECIFIED.,
 .F.,.F.,(4,2,2,2,2,2,2,2,2,2,2,2,2,2,2,2,2,2,2,2,2,2,2,2,2,2,2,2,2,2,2,
2,2,2,2,2,2,2,2,2,2,2,2,2,2,2,2,2,2,2,2,2,2,2,2,2,2,2,2,2,2,2,2,2,2,2,2,
2,2,2,2,2,2,2,2,2,2,2,2,2,2,2,2,2,2,2,2,2,2,2,2,2,2,2,2,2,2,2,2,2,2,2,2,
2,2,2,2,2,2,2,2,2,2,4),(-2.96761844200665,-2.93767638030957,-2.93548019648945,
-2.9336592562878,-2.93254600130476,-2.9315131451599,-2.93025844008825,-2.92716409765907,
-2.90650829392983,-2.8888379059781,-2.8823315150323,-2.87749151310647,-2.8753219616522,
-2.87527613194927,-2.87522753684484,-2.87517583173089,-2.87512061413181,
-2.87329858116516,-2.87127510210733,-2.86790350393687,-2.85550729588206,
-2.82989684850021,-2.82244673261111,-2.81933798348305,-2.81694664596374,
-2.81571078257054,-2.81469354533725,-2.81341526634235,-2.8113846499091,
-2.7982052469369,-2.79242601858666,-2.77758943642391,-2.76271667977566,
-2.75929738765832,-2.75726349489495,-2.7554434059559,-2.75312289383221,
-2.74830125028984,-2.72496885149802,-2.708776646864,-2.70376743420223,-2.70032738663267,
-2.69889804992327,-2.69786482227434,-2.69672460861366,-2.69478164684512,
-2.68754275776878,-2.66678912334879,-2.64703561785448,-2.64276764051325,
-2.64055537390903,-2.63874405581574,-2.63663568557671,-2.63297010513757,
-2.61132181153184,-2.59543763763128,-2.58808364660803,-2.58500168474834,
-2.58262637971013,-2.58139379988205,-2.58037641061561,-2.57909434548578,
-2.57705114926448,-2.56325661067326,-2.55807480885457,-2.54290715044706,
-2.52836819659951,-2.52496852603686,-2.52293885483448,-2.52111790244483,
-2.51878988367364,-2.51392857361376,-2.4929891476698,-2.47496368494581,
-2.46966307373379,-2.46607588426237,-2.4646226941432,-2.4635855664214,-2.46245556543585,
-2.46055906021209,-2.45385008040142,-2.44729131397717,-2.42663083758384,
-2.41129714329299,-2.40785189514679,-2.40581236922416,-2.40399327843769,
-2.40168229466265,-2.39691101489519,-2.37205368528113,-2.35125224167795,
-2.348517985985,-2.34721399762815,-2.3461954232727,-2.34498074761048,-2.34275704041747,
-2.32968049854632,-2.32380163528694,-2.30871456669348,-2.29405779654679,
-2.29065093418213,-2.28861962433217,-2.28679885511071,-2.28447335269856,
-2.27962588423449,-2.25870320887828,-2.24064482911579,-2.23533909950807,
-2.23174929490462,-2.23029563194362,-2.22925837447632,-2.22812845793281,
-2.22623254049717,-2.22593322706991),.UNSPECIFIED.);
#1609=B_SPLINE_CURVE_WITH_KNOTS('',3,(#118271,#118272,#118273,#118274,#118275,
#118276,#118277,#118278,#118279,#118280,#118281,#118282,#118283,#118284,
#118285,#118286,#118287,#118288,#118289,#118290,#118291,#118292,#118293,
#118294,#118295,#118296,#118297,#118298,#118299,#118300,#118301,#118302,
#118303,#118304,#118305,#118306,#118307,#118308,#118309,#118310,#118311,
#118312,#118313,#118314,#118315,#118316,#118317,#118318,#118319,#118320,
#118321,#118322,#118323,#118324,#118325,#118326,#118327,#118328,#118329,
#118330,#118331,#118332,#118333,#118334,#118335,#118336,#118337,#118338,
#118339,#118340,#118341,#118342,#118343,#118344,#118345,#118346,#118347,
#118348,#118349,#118350,#118351,#118352,#118353,#118354,#118355,#118356,
#118357,#118358,#118359,#118360,#118361,#118362,#118363,#118364,#118365,
#118366,#118367,#118368,#118369,#118370,#118371,#118372,#118373,#118374,
#118375,#118376,#118377,#118378,#118379,#118380,#118381,#118382,#118383,
#118384,#118385,#118386,#118387,#118388,#118389,#118390,#118391,#118392,
#118393,#118394,#118395,#118396,#118397,#118398,#118399,#118400,#118401,
#118402,#118403,#118404,#118405,#118406,#118407,#118408,#118409,#118410,
#118411,#118412,#118413,#118414,#118415,#118416,#118417,#118418,#118419,
#118420,#118421,#118422,#118423,#118424,#118425,#118426,#118427,#118428,
#118429,#118430,#118431,#118432,#118433,#118434,#118435,#118436,#118437,
#118438,#118439,#118440,#118441,#118442,#118443,#118444,#118445,#118446,
#118447,#118448,#118449,#118450,#118451,#118452,#118453,#118454,#118455,
#118456,#118457,#118458,#118459,#118460,#118461,#118462,#118463,#118464,
#118465,#118466,#118467,#118468,#118469,#118470,#118471,#118472,#118473,
#118474,#118475,#118476,#118477,#118478,#118479,#118480,#118481,#118482,
#118483,#118484,#118485,#118486,#118487,#118488,#118489,#118490,#118491,
#118492,#118493,#118494),.UNSPECIFIED.,.F.,.F.,(4,2,2,2,2,2,2,2,2,2,2,2,
2,2,2,2,2,2,2,2,2,2,2,2,2,2,2,2,2,2,2,2,2,2,2,2,2,2,2,2,2,2,2,2,2,2,2,2,
2,2,2,2,2,2,2,2,2,2,2,2,2,2,2,2,2,2,2,2,2,2,2,2,2,2,2,2,2,2,2,2,2,2,2,2,
2,2,2,2,2,2,2,2,2,2,2,2,2,2,2,2,2,2,2,2,2,2,2,2,2,2,2,4),(-0.742112763578935,
-0.727061281829163,-0.722288707659859,-0.719976552121643,-0.718156277868983,
-0.716115142797653,-0.712666468742061,-0.697302911406439,-0.676462712432556,
-0.66399562117025,-0.661963327744964,-0.660684073406103,-0.659666095868948,
-0.658429341915493,-0.656036286403435,-0.652925557060773,-0.645471068072106,
-0.629664810654427,-0.608098954927716,-0.604434092649939,-0.602324978154874,
-0.600512332017134,-0.598297568700903,-0.594021944671633,-0.572450882452868,
-0.547745965683558,-0.544883050965748,-0.543568324645918,-0.542546455406132,
-0.541354095005308,-0.539173162230857,-0.526165755512889,-0.498395084105655,
-0.48952989129908,-0.486517177448293,-0.484570153612476,-0.482720077252544,
-0.480197699155873,-0.474235583314371,-0.441046239068091,-0.429448447310168,
-0.427260622291499,-0.42605338083039,-0.42503324097333,-0.423717177313737,
-0.420922601092093,-0.417119811234962,-0.406967813557909,-0.383888849225869,
-0.372775422093107,-0.36951646000599,-0.367516230418958,-0.365686331015219,
-0.363296383097122,-0.358105309888169,-0.351066129489304,-0.326977507093747,
-0.312343672992127,-0.310283518804771,-0.308995810007337,-0.307977354236198,
-0.306747568929113,-0.304388912333526,-0.301335672727778,-0.268385915888379,
-0.25576465302906,-0.252376083045881,-0.250347846979684,-0.248524922392752,
-0.246189851639557,-0.241296587464822,-0.234782495934772,-0.217085539253761,
-0.196417331824234,-0.193319624540132,-0.192063716207234,-0.191029941686005,
-0.189915746832888,-0.188093350758696,-0.181437709394761,-0.168221536479482,
-0.140578045065258,-0.136057031252293,-0.133763207470923,-0.131944696436363,
-0.13186632269449,-0.131803688724853,-0.13175369384992,-0.131713823231323,
-0.131682047934474,-0.129585548653185,-0.127332074427384,-0.123815420715499,
-0.117008595736625,-0.0978331338304588,-0.079280032901386,-0.0763948936646742,
-0.0748772570631236,-0.0738383714654832,-0.0727337095512854,-0.0709544215164448,
-0.0647593847788353,-0.0530138957397964,-0.0346913996586432,-0.0218253839118807,
-0.0182147852973583,-0.016117783036972,-0.0143078318254824,-0.0125677029833169,
-0.0103865823899228,-0.00631987000565794,-7.37639246660687E-6),
 .UNSPECIFIED.);
#1610=B_SPLINE_CURVE_WITH_KNOTS('',3,(#118495,#118496,#118497,#118498,#118499,
#118500,#118501,#118502,#118503,#118504,#118505,#118506,#118507,#118508,
#118509,#118510,#118511,#118512,#118513,#118514,#118515,#118516,#118517,
#118518,#118519,#118520,#118521,#118522,#118523,#118524,#118525,#118526,
#118527,#118528,#118529,#118530,#118531,#118532,#118533,#118534,#118535,
#118536,#118537,#118538,#118539,#118540,#118541,#118542,#118543,#118544,
#118545,#118546,#118547,#118548,#118549,#118550,#118551,#118552,#118553,
#118554,#118555,#118556,#118557,#118558,#118559,#118560,#118561,#118562,
#118563,#118564,#118565,#118566,#118567,#118568,#118569,#118570,#118571,
#118572,#118573,#118574,#118575,#118576,#118577,#118578,#118579,#118580,
#118581,#118582,#118583,#118584,#118585,#118586,#118587,#118588,#118589,
#118590,#118591,#118592,#118593,#118594,#118595,#118596,#118597,#118598,
#118599,#118600,#118601,#118602,#118603,#118604,#118605,#118606,#118607,
#118608,#118609,#118610,#118611,#118612,#118613,#118614,#118615,#118616,
#118617,#118618,#118619,#118620,#118621,#118622,#118623,#118624,#118625,
#118626,#118627,#118628,#118629,#118630,#118631,#118632,#118633,#118634,
#118635,#118636,#118637,#118638,#118639,#118640,#118641,#118642,#118643,
#118644,#118645,#118646,#118647,#118648,#118649,#118650,#118651,#118652,
#118653,#118654,#118655,#118656,#118657,#118658,#118659,#118660,#118661,
#118662,#118663,#118664,#118665,#118666,#118667,#118668,#118669,#118670,
#118671,#118672,#118673,#118674,#118675,#118676,#118677,#118678,#118679,
#118680,#118681,#118682,#118683,#118684,#118685,#118686,#118687,#118688,
#118689,#118690,#118691,#118692,#118693,#118694,#118695,#118696),
 .UNSPECIFIED.,.F.,.F.,(4,2,2,2,2,2,2,2,2,2,2,2,2,2,2,2,2,2,2,2,2,2,2,2,
2,2,2,2,2,2,2,2,2,2,2,2,2,2,2,2,2,2,2,2,2,2,2,2,2,2,2,2,2,2,2,2,2,2,2,2,
2,2,2,2,2,2,2,2,2,2,2,2,2,2,2,2,2,2,2,2,2,2,2,2,2,2,2,2,2,2,2,2,2,2,2,2,
2,2,2,2,4),(-2.22593322706991,-2.21953112565396,-2.21297056419295,-2.20668574539589,
-2.19166772652078,-2.1769127101204,-2.17350000824533,-2.17146740944946,
-2.16964684772091,-2.16732348817461,-2.16248752947384,-2.13999724481421,
-2.12559948620941,-2.1157953171276,-2.11375217469596,-2.11258997203901,
-2.11156309561059,-2.11020203273382,-2.10707711764329,-2.08624076422116,
-2.06868339382152,-2.0621998217347,-2.05732433500123,-2.05499349847257,
-2.05317204991695,-2.0511435828802,-2.04775016493561,-2.03503194109297,
-2.00214006565418,-1.99910871877699,-1.99676368690714,-1.99553714979222,
-1.99451915022935,-1.99322922796777,-1.99116040290091,-1.97552361412581,
-1.97214598083311,-1.95683519985974,-1.94248622408338,-1.93909738044412,
-1.93706968354457,-1.93524769324632,-1.93291445424272,-1.92802750292512,
-1.90665816348616,-1.8889938903102,-1.88374754623271,-1.8801872460834,-1.87873810635213,
-1.87770142886847,-1.87656925829213,-1.87466383019428,-1.86785708755501,
-1.86131259863678,-1.84073047145756,-1.8254027251819,-1.82195705553556,
-1.81991706735598,-1.81809743346858,-1.81578558127099,-1.81101185082757,
-1.78617368158807,-1.76534201698589,-1.76260677022686,-1.76130236840509,
-1.76028349954876,-1.75906850665928,-1.75684430159575,-1.74379854502861,
-1.73788596356335,-1.72307132868658,-1.70815857599283,-1.70473603071085,
-1.70270095572413,-1.70088027528091,-1.69855964985648,-1.69374016171822,
-1.6702369877515,-1.64815745880669,-1.64540977591381,-1.64410294295502,
-1.6430838515852,-1.64187059085465,-1.6396544127336,-1.62739774240837,-1.60705133675503,
-1.59105274609926,-1.58757148371704,-1.58552365748868,-1.58370509907058,
-1.58140554079275,-1.5766970335215,-1.5505562822561,-1.53028006958655,-1.52794301035101,
-1.52671798131452,-1.52569967968587,-1.52440740454272,-1.52233113542177,
-1.50493410620379,-1.48402414970713),.UNSPECIFIED.);
#1611=B_SPLINE_CURVE_WITH_KNOTS('',3,(#118701,#118702,#118703,#118704,#118705,
#118706,#118707,#118708,#118709,#118710,#118711,#118712,#118713,#118714,
#118715,#118716,#118717,#118718,#118719,#118720,#118721,#118722,#118723,
#118724,#118725,#118726,#118727,#118728,#118729,#118730,#118731,#118732,
#118733,#118734,#118735,#118736,#118737,#118738,#118739,#118740,#118741,
#118742,#118743,#118744,#118745,#118746,#118747,#118748,#118749,#118750,
#118751,#118752,#118753,#118754,#118755,#118756,#118757,#118758,#118759,
#118760,#118761,#118762,#118763,#118764,#118765,#118766,#118767,#118768,
#118769,#118770,#118771,#118772,#118773,#118774,#118775,#118776,#118777,
#118778,#118779,#118780,#118781,#118782,#118783,#118784,#118785,#118786,
#118787,#118788,#118789,#118790,#118791,#118792,#118793,#118794,#118795,
#118796,#118797,#118798,#118799,#118800,#118801,#118802,#118803,#118804,
#118805,#118806,#118807,#118808,#118809,#118810,#118811,#118812,#118813,
#118814,#118815,#118816,#118817,#118818,#118819,#118820,#118821,#118822,
#118823,#118824,#118825,#118826,#118827,#118828,#118829,#118830,#118831,
#118832,#118833,#118834,#118835,#118836,#118837,#118838,#118839,#118840,
#118841,#118842,#118843,#118844,#118845,#118846,#118847,#118848,#118849,
#118850,#118851,#118852,#118853,#118854,#118855,#118856,#118857,#118858,
#118859,#118860,#118861,#118862,#118863,#118864,#118865,#118866,#118867,
#118868,#118869,#118870,#118871,#118872,#118873,#118874,#118875,#118876,
#118877,#118878,#118879,#118880,#118881,#118882,#118883,#118884,#118885,
#118886,#118887,#118888,#118889,#118890,#118891,#118892,#118893,#118894,
#118895,#118896,#118897,#118898,#118899,#118900,#118901,#118902,#118903,
#118904,#118905,#118906,#118907,#118908,#118909,#118910,#118911,#118912,
#118913,#118914,#118915,#118916,#118917,#118918,#118919,#118920),
 .UNSPECIFIED.,.F.,.F.,(4,2,2,2,2,2,2,2,2,2,2,2,2,2,2,2,2,2,2,2,2,2,2,2,
2,2,2,2,2,2,2,2,2,2,2,2,2,2,2,2,2,2,2,2,2,2,2,2,2,2,2,2,2,2,2,2,2,2,2,2,
2,2,2,2,2,2,2,2,2,2,2,2,2,2,2,2,2,2,2,2,2,2,2,2,2,2,2,2,2,2,2,2,2,2,2,2,
2,2,2,2,2,2,2,2,2,2,2,2,2,4),(-1.48419021204294,-1.48218378775787,-1.48101315824072,
-1.48009053040463,-1.47877941151569,-1.47601000501141,-1.47225160644337,
-1.46228499926441,-1.43911667662998,-1.42789216537953,-1.42460483990733,
-1.42259874951587,-1.42077098719917,-1.41839459796471,-1.41327651641115,
-1.40636693667328,-1.37070917493401,-1.36617581273004,-1.3645333229462,
-1.36356520205338,-1.36251274873407,-1.36097887816494,-1.35686241463103,
-1.35046119277678,-1.33355109572006,-1.31140156200382,-1.30774455349713,
-1.30563705480767,-1.30382409477266,-1.3016068057226,-1.29731940696517,
-1.29183032348863,-1.27854826632138,-1.25943090419546,-1.24986193966554,
-1.24777487645582,-1.2465902982298,-1.24566977766055,-1.24437856481664,
-1.24171353968761,-1.23813870739911,-1.22892416044852,-1.22713125957704,
-1.20301083681601,-1.19311422522434,-1.18998242293793,-1.18800971988834,
-1.18617073171274,-1.18371779040802,-1.17816969209402,-1.15874058175379,
-1.13493115936447,-1.13139254209156,-1.13005000383784,-1.12908852242119,
-1.12802972518176,-1.12646409826591,-1.12212107126218,-1.11522035782837,
-1.07924233184699,-1.07410278051337,-1.07174787986452,-1.06991742105179,
-1.06791993085555,-1.06467304669819,-1.05238585055491,-1.03800737060559,
-1.01696169390139,-1.01384527862247,-1.01248518659566,-1.01145792746855,
-1.01029394739306,-1.00824469117645,-0.998342120341819,-0.983643346582729,
-0.961583123922189,-0.956739850300681,-0.954414240329411,-0.952592443832404,
-0.950559003523848,-0.947146172610424,-0.932416884743305,-0.917357368760218,
-0.911109752915589,-0.904546648676946,-0.897787864690021,-0.895886057620949,
-0.894754397968665,-0.893716891405269,-0.89226475358036,-0.888687907973293,
-0.883409779187262,-0.865538288076789,-0.844397515202518,-0.839545615215156,
-0.837218390249218,-0.835396426255118,-0.833363932830224,-0.829955430603124,
-0.815299054069314,-0.800188327554611,-0.794245652075295,-0.781213164006394,
-0.778987212211267,-0.777771576307993,-0.776752345280325,-0.775447686036176,
-0.772712548625201,-0.751918186273301,-0.742112763578935),.UNSPECIFIED.);
#1612=B_SPLINE_CURVE_WITH_KNOTS('',3,(#118921,#118922,#118923,#118924,#118925,
#118926,#118927,#118928,#118929,#118930,#118931,#118932,#118933,#118934,
#118935,#118936,#118937,#118938,#118939,#118940,#118941,#118942,#118943,
#118944,#118945,#118946,#118947,#118948,#118949,#118950,#118951,#118952,
#118953,#118954,#118955,#118956,#118957,#118958,#118959,#118960,#118961,
#118962,#118963,#118964,#118965,#118966,#118967,#118968,#118969,#118970,
#118971,#118972,#118973,#118974,#118975,#118976,#118977,#118978,#118979,
#118980,#118981,#118982,#118983,#118984,#118985,#118986,#118987,#118988,
#118989,#118990,#118991,#118992,#118993,#118994,#118995,#118996,#118997,
#118998,#118999,#119000,#119001,#119002,#119003,#119004,#119005,#119006,
#119007,#119008,#119009,#119010,#119011,#119012,#119013,#119014,#119015,
#119016,#119017,#119018,#119019,#119020,#119021,#119022,#119023,#119024,
#119025,#119026,#119027,#119028,#119029,#119030,#119031,#119032,#119033,
#119034,#119035,#119036,#119037,#119038,#119039,#119040,#119041,#119042,
#119043,#119044,#119045,#119046,#119047,#119048,#119049,#119050,#119051,
#119052,#119053,#119054,#119055,#119056,#119057,#119058,#119059,#119060,
#119061,#119062,#119063,#119064,#119065,#119066,#119067,#119068,#119069,
#119070,#119071,#119072,#119073,#119074,#119075,#119076,#119077,#119078,
#119079,#119080,#119081,#119082,#119083,#119084,#119085,#119086,#119087,
#119088,#119089,#119090,#119091,#119092,#119093,#119094,#119095,#119096,
#119097,#119098,#119099,#119100,#119101,#119102,#119103,#119104,#119105,
#119106,#119107,#119108,#119109,#119110,#119111,#119112,#119113,#119114,
#119115,#119116,#119117,#119118,#119119,#119120,#119121,#119122,#119123,
#119124,#119125,#119126,#119127,#119128,#119129,#119130,#119131,#119132,
#119133,#119134,#119135,#119136),.UNSPECIFIED.,.F.,.F.,(4,2,2,2,2,2,2,2,
2,2,2,2,2,2,2,2,2,2,2,2,2,2,2,2,2,2,2,2,2,2,2,2,2,2,2,2,2,2,2,2,2,2,2,2,
2,2,2,2,2,2,2,2,2,2,2,2,2,2,2,2,2,2,2,2,2,2,2,2,2,2,2,2,2,2,2,2,2,2,2,2,
2,2,2,2,2,2,2,2,2,2,2,2,2,2,2,2,2,2,2,2,2,2,2,2,2,2,2,4),(-1.48402414970713,
-1.48386902271208,-1.47329677017161,-1.47009145873531,-1.46810329736781,
-1.46627059428127,-1.46385672872211,-1.45852924500984,-1.45124389717394,
-1.42934011570267,-1.41299688403725,-1.41092631703839,-1.40963573774516,
-1.40861750151737,-1.40739101152478,-1.40504699141599,-1.38507466244869,
-1.35863008259914,-1.35394363573545,-1.35164826065279,-1.34983004600115,
-1.34777947376678,-1.34428575295072,-1.32804275936578,-1.31835679519701,
-1.29702186517173,-1.29391946443402,-1.2925620380903,-1.29153537611592,
-1.29037045358503,-1.28831595315114,-1.27830755480595,-1.26327037388336,
-1.24170341859183,-1.23683462937683,-1.23450459447146,-1.23268273424493,
-1.23065273978464,-1.22725419546221,-1.21275462026739,-1.19753334629008,
-1.19256519393886,-1.17852556835761,-1.17647654750295,-1.17519244799117,
-1.17417455072479,-1.17294268915125,-1.17057248190465,-1.16749969414661,
-1.13451096006151,-1.12196447640015,-1.11858174215839,-1.11655531091684,
-1.11473295889365,-1.11239717435145,-1.10749697314075,-1.10097009783791,
-1.08320735078966,-1.06264185319504,-1.05980702702136,-1.05830276994263,
-1.05726665359571,-1.05615823719905,-1.05436068926936,-1.04797011243133,
-1.03561416416639,-1.00655033194157,-1.00256819054537,-1.00019875669666,
-0.99836683666612,-0.996377596164948,-0.993166245935335,-0.981313397103145,
-0.955301253663928,-0.949413257716968,-0.943289635095021,-0.941451072565698,
-0.940333616646599,-0.939290276415498,-0.937803050749906,-0.933999533416799,
-0.928260039157953,-0.907039523288692,-0.888100935658694,-0.884458712495661,
-0.882355104923363,-0.880542778844311,-0.878322851169783,-0.874019351741301,
-0.858781886714686,-0.835176779061912,-0.833679631812814,-0.826304893164126,
-0.824349717177918,-0.823206544320609,-0.822173766398724,-0.820749403607453,
-0.817341491304575,-0.812396317308845,-0.796585544834842,-0.772746656663903,
-0.767937769357755,-0.765619119899626,-0.763798612446761,-0.761762300022572,
-0.758334204017837,-0.743328397463449,-0.741997157565065),.UNSPECIFIED.);
#1613=B_SPLINE_CURVE_WITH_KNOTS('',3,(#119141,#119142,#119143,#119144,#119145,
#119146,#119147,#119148,#119149,#119150,#119151,#119152,#119153,#119154,
#119155,#119156,#119157,#119158,#119159,#119160,#119161,#119162,#119163,
#119164,#119165,#119166,#119167,#119168,#119169,#119170,#119171,#119172,
#119173,#119174,#119175,#119176,#119177,#119178,#119179,#119180,#119181,
#119182,#119183,#119184,#119185,#119186,#119187,#119188,#119189,#119190,
#119191,#119192,#119193,#119194,#119195,#119196,#119197,#119198,#119199,
#119200,#119201,#119202,#119203,#119204,#119205,#119206,#119207,#119208,
#119209,#119210,#119211,#119212,#119213,#119214,#119215,#119216,#119217,
#119218,#119219,#119220,#119221,#119222,#119223,#119224,#119225,#119226,
#119227,#119228,#119229,#119230,#119231,#119232,#119233,#119234,#119235,
#119236,#119237,#119238,#119239,#119240,#119241,#119242,#119243,#119244,
#119245,#119246,#119247,#119248,#119249,#119250,#119251,#119252,#119253,
#119254,#119255,#119256,#119257,#119258,#119259,#119260,#119261,#119262,
#119263,#119264,#119265,#119266,#119267,#119268,#119269,#119270,#119271,
#119272,#119273,#119274,#119275,#119276,#119277,#119278,#119279,#119280,
#119281,#119282,#119283,#119284,#119285,#119286,#119287,#119288,#119289,
#119290,#119291,#119292,#119293,#119294,#119295,#119296,#119297,#119298,
#119299,#119300,#119301,#119302,#119303,#119304,#119305,#119306,#119307,
#119308,#119309,#119310,#119311,#119312,#119313,#119314,#119315,#119316,
#119317,#119318,#119319,#119320,#119321,#119322,#119323,#119324,#119325,
#119326,#119327,#119328,#119329,#119330,#119331,#119332,#119333,#119334,
#119335,#119336,#119337,#119338,#119339,#119340,#119341,#119342,#119343,
#119344,#119345,#119346),.UNSPECIFIED.,.F.,.F.,(4,2,2,2,2,2,2,2,2,2,2,2,
2,2,2,2,2,2,2,2,2,2,2,2,2,2,2,2,2,2,2,2,2,2,2,2,2,2,2,2,2,2,2,2,2,2,2,2,
2,2,2,2,2,2,2,2,2,2,2,2,2,2,2,2,2,2,2,2,2,2,2,2,2,2,2,2,2,2,2,2,2,2,2,2,
2,2,2,2,2,2,2,2,2,2,2,2,2,2,2,2,2,2,4),(-2.22608676643451,-2.20726309333763,
-2.1937123379699,-2.18695881985012,-2.18512815033227,-2.18401241697167,
-2.18298003559482,-2.18172871979647,-2.17853017582475,-2.16075985761862,
-2.14494711928046,-2.13582836423958,-2.12953504509966,-2.12696004683478,
-2.12510121517364,-2.1233993485002,-2.12065573164219,-2.11376224262234,
-2.08689525161069,-2.07146002627653,-2.06863393377325,-2.06731222386601,
-2.06629198356956,-2.06508965528965,-2.06292263589511,-2.05181528796755,
-2.02561483179469,-2.01372958303666,-2.01051548053703,-2.0085254914483,
-2.00669350536859,-2.00432485095476,-2.00034590751655,-1.97124001084136,
-1.9588983175329,-1.95251256562008,-1.95071530670252,-1.94960686956509,
-1.94857054382749,-1.94706568375257,-1.9442289364259,-1.92374976668429,
-1.90904750276677,-1.89661902115088,-1.89336185253027,-1.8913624303113,
-1.88953307745642,-1.88718359411602,-1.88327223080929,-1.853578629355,-1.83681731374779,
-1.83414344894614,-1.83285070285945,-1.83193021346715,-1.83074722401876,
-1.82866644601452,-1.81920397570096,-1.80003238027993,-1.78673538177809,
-1.78124279493265,-1.77695312398073,-1.77473568364263,-1.7729230953229,
-1.77081658769254,-1.76716272455683,-1.74459620798524,-1.72632685790298,
-1.7209886938557,-1.7173823093171,-1.71592556479101,-1.71488738365343,-1.71375782010907,
-1.71186514152084,-1.7052065218983,-1.68402963362545,-1.66400989463197,
-1.65973937647502,-1.65752581492613,-1.65571343598548,-1.65360382095896,
-1.64993602071104,-1.62862459442818,-1.60936723860382,-1.60388647319068,
-1.60020945106807,-1.59874157348474,-1.5977014928129,-1.59657637431063,
-1.59470381433327,-1.58825446612154,-1.58116121273384,-1.5750856244477,
-1.56002521396891,-1.54532294391199,-1.541912198669,-1.53987938693197,-1.53805776791121,
-1.53573185373234,-1.53088599402871,-1.50888621928476,-1.49413085231136,
-1.48421012225063,-1.48419021204294),.UNSPECIFIED.);
#1614=B_SPLINE_CURVE_WITH_KNOTS('',3,(#119347,#119348,#119349,#119350,#119351,
#119352,#119353,#119354,#119355,#119356,#119357,#119358,#119359,#119360,
#119361,#119362,#119363,#119364,#119365,#119366,#119367,#119368,#119369,
#119370,#119371,#119372,#119373,#119374,#119375,#119376,#119377,#119378,
#119379,#119380,#119381,#119382,#119383,#119384,#119385,#119386,#119387,
#119388,#119389,#119390,#119391,#119392,#119393,#119394,#119395,#119396,
#119397,#119398,#119399,#119400,#119401,#119402,#119403,#119404,#119405,
#119406,#119407,#119408,#119409,#119410,#119411,#119412,#119413,#119414,
#119415,#119416,#119417,#119418,#119419,#119420,#119421,#119422,#119423,
#119424,#119425,#119426,#119427,#119428,#119429,#119430,#119431,#119432,
#119433,#119434,#119435,#119436,#119437,#119438,#119439,#119440,#119441,
#119442,#119443,#119444,#119445,#119446,#119447,#119448,#119449,#119450,
#119451,#119452,#119453,#119454,#119455,#119456,#119457,#119458,#119459,
#119460,#119461,#119462,#119463,#119464,#119465,#119466,#119467,#119468,
#119469,#119470,#119471,#119472,#119473,#119474,#119475,#119476,#119477,
#119478,#119479,#119480,#119481,#119482,#119483,#119484,#119485,#119486,
#119487,#119488,#119489,#119490,#119491,#119492,#119493,#119494,#119495,
#119496,#119497,#119498,#119499,#119500,#119501,#119502,#119503,#119504,
#119505,#119506,#119507,#119508,#119509,#119510,#119511,#119512,#119513,
#119514,#119515,#119516,#119517,#119518,#119519,#119520,#119521,#119522,
#119523,#119524,#119525,#119526,#119527,#119528,#119529,#119530,#119531,
#119532,#119533,#119534,#119535,#119536,#119537,#119538,#119539,#119540,
#119541,#119542,#119543,#119544,#119545,#119546,#119547,#119548,#119549,
#119550,#119551,#119552,#119553,#119554,#119555,#119556,#119557,#119558,
#119559,#119560,#119561,#119562,#119563,#119564,#119565,#119566),
 .UNSPECIFIED.,.F.,.F.,(4,2,2,2,2,2,2,2,2,2,2,2,2,2,2,2,2,2,2,2,2,2,2,2,
2,2,2,2,2,2,2,2,2,2,2,2,2,2,2,2,2,2,2,2,2,2,2,2,2,2,2,2,2,2,2,2,2,2,2,2,
2,2,2,2,2,2,2,2,2,2,2,2,2,2,2,2,2,2,2,2,2,2,2,2,2,2,2,2,2,2,2,2,2,2,2,2,
2,2,2,2,2,2,2,2,2,2,2,2,2,4),(-0.741997157565065,-0.728572633296522,-0.722291508979075,
-0.715722384418041,-0.709001205149917,-0.707103099315564,-0.705972493802639,
-0.704935074437573,-0.703481857250529,-0.699896439939264,-0.694600682114955,
-0.676609818948818,-0.653737675961877,-0.650071834712697,-0.647962905077023,
-0.646150865642299,-0.643937416035677,-0.639666211520541,-0.619574407583386,
-0.598283007078139,-0.591766262696187,-0.589880478273266,-0.588752562278465,
-0.587713963648858,-0.586253956617637,-0.582626015483684,-0.577244956375353,
-0.558679987688215,-0.536506076107584,-0.532850532802642,-0.530743861647133,
-0.528931613735612,-0.526715205973186,-0.522429589952349,-0.516942905714233,
-0.503667923990456,-0.48456923586704,-0.474976915285377,-0.472889131984864,
-0.471704667210622,-0.470784564721378,-0.469494392033032,-0.466833179027015,
-0.463264628586587,-0.454073693161898,-0.453215635711422,-0.430301112416084,
-0.418600480856284,-0.415283609643857,-0.413271355113976,-0.411445613406979,
-0.409082723854666,-0.404036991037775,-0.397255230843478,-0.378208812850448,
-0.359479489619188,-0.356595311326521,-0.355078156793945,-0.354039596801582,
-0.352935299794781,-0.351156664812063,-0.344964769249125,-0.333227625140076,
-0.304399024096692,-0.299274495127334,-0.296922794975267,-0.295093330602675,
-0.293095427075587,-0.289844492602138,-0.277495408096522,-0.262975474257854,
-0.242164261102668,-0.239035374043058,-0.237673404462222,-0.236646192914751,
-0.235483992690002,-0.233441733337095,-0.223659387130257,-0.209330127320179,
-0.186759042122723,-0.181923788104845,-0.179600194733689,-0.177779192358314,
-0.175745834492589,-0.172331221563639,-0.157557695393221,-0.142531306356899,
-0.125060732804245,-0.121940415051461,-0.120664111979058,-0.119665820805118,
-0.118599316442255,-0.117478324788082,-0.115847619865693,-0.0990038844796983,
-0.0707289323749749,-0.0652192497652088,-0.0629576091979782,-0.061265790591419,
-0.059397923888038,-0.0567726546030518,-0.0501515511055032,-0.0403676753941963,
-0.0110688761212782,-0.0054956478613353,-0.00375609781177683,-0.0026448724528549,
-0.00167735725160652,-0.000891022296295099,-9.99999999917733E-7),
 .UNSPECIFIED.);
#1615=B_SPLINE_CURVE_WITH_KNOTS('',3,(#119571,#119572,#119573,#119574,#119575,
#119576,#119577,#119578,#119579,#119580,#119581,#119582,#119583,#119584,
#119585,#119586,#119587,#119588,#119589,#119590,#119591,#119592,#119593,
#119594,#119595,#119596,#119597,#119598,#119599,#119600,#119601,#119602,
#119603,#119604,#119605,#119606,#119607,#119608,#119609,#119610,#119611,
#119612,#119613,#119614,#119615,#119616,#119617,#119618,#119619,#119620,
#119621,#119622,#119623,#119624,#119625,#119626,#119627,#119628,#119629,
#119630,#119631,#119632,#119633,#119634,#119635,#119636,#119637,#119638,
#119639,#119640,#119641,#119642,#119643,#119644,#119645,#119646,#119647,
#119648,#119649,#119650,#119651,#119652,#119653,#119654,#119655,#119656,
#119657,#119658,#119659,#119660,#119661,#119662,#119663,#119664,#119665,
#119666,#119667,#119668,#119669,#119670,#119671,#119672,#119673,#119674,
#119675,#119676,#119677,#119678,#119679,#119680,#119681,#119682,#119683,
#119684,#119685,#119686,#119687,#119688,#119689,#119690,#119691,#119692,
#119693,#119694,#119695,#119696,#119697,#119698,#119699,#119700,#119701,
#119702,#119703,#119704,#119705,#119706,#119707,#119708,#119709,#119710,
#119711,#119712,#119713,#119714,#119715,#119716,#119717,#119718,#119719,
#119720,#119721,#119722,#119723,#119724,#119725,#119726,#119727,#119728,
#119729,#119730,#119731,#119732,#119733,#119734,#119735,#119736,#119737,
#119738,#119739,#119740,#119741,#119742,#119743,#119744,#119745,#119746,
#119747,#119748,#119749,#119750,#119751,#119752,#119753,#119754,#119755,
#119756,#119757,#119758,#119759,#119760,#119761,#119762,#119763,#119764,
#119765,#119766,#119767,#119768,#119769,#119770,#119771,#119772,#119773,
#119774,#119775,#119776,#119777,#119778,#119779,#119780,#119781,#119782,
#119783,#119784,#119785,#119786,#119787,#119788,#119789,#119790,#119791,
#119792,#119793,#119794,#119795,#119796,#119797,#119798,#119799,#119800,
#119801,#119802,#119803,#119804,#119805,#119806,#119807,#119808,#119809,
#119810,#119811,#119812,#119813,#119814,#119815,#119816,#119817,#119818,
#119819,#119820,#119821,#119822,#119823,#119824,#119825,#119826,#119827,
#119828,#119829,#119830,#119831,#119832),.UNSPECIFIED.,.F.,.F.,(4,2,2,2,
2,2,2,2,2,2,2,2,2,2,2,2,2,2,2,2,2,2,2,2,2,2,2,2,2,2,2,2,2,2,2,2,2,2,2,2,
2,2,2,2,2,2,2,2,2,2,2,2,2,2,2,2,2,2,2,2,2,2,2,2,2,2,2,2,2,2,2,2,2,2,2,2,
2,2,2,2,2,2,2,2,2,2,2,2,2,2,2,2,2,2,2,2,2,2,2,2,2,2,2,2,2,2,2,2,2,2,2,2,
2,2,2,2,2,2,2,2,2,2,2,2,2,2,2,2,2,2,4),(-2.96774370793825,-2.95691337121733,
-2.95119318194074,-2.94877962072619,-2.94696532202346,-2.94512123982102,
-2.94316545926379,-2.94010786907299,-2.93085947243012,-2.91702940083278,
-2.90086534003985,-2.89041205828235,-2.8883345613625,-2.88716494585088,
-2.88613985631808,-2.88479183023501,-2.88174104500079,-2.8595196773211,
-2.84288406306168,-2.83659729946576,-2.83186882414787,-2.82964656440494,
-2.82962354836739,-2.8295995245032,-2.8295744413791,-2.82954824444592,-2.82952087583186,
-2.82949227411457,-2.82946237408205,-2.82943110648194,-2.82939839773653,
-2.82936416966736,-2.82932833919924,-2.82929081804144,-2.82925151235605,
-2.82921032243071,-2.82918648407176,-2.82915667241775,-2.82911938112325,
-2.82907272063437,-2.82901432083922,-2.82894121110194,-2.82889805228096,
-2.82872855034397,-2.8268972112756,-2.82452938261826,-2.82055180181568,
-2.7914769617933,-2.7791246514421,-2.77273643292514,-2.77093936623985,-2.76983122390776,
-2.76879531921187,-2.76729128510585,-2.76445666280324,-2.74395459894712,
-2.72618437749715,-2.71965726480536,-2.71475679111166,-2.71242126143093,
-2.71059925204096,-2.7085733396414,-2.7051917858923,-2.6926559866327,-2.659656721078,
-2.65658407325577,-2.65421422186697,-2.65298254452811,-2.65196478553647,
-2.65068081852581,-2.64863193766583,-2.63457057553929,-2.62965093275844,
-2.61445773560999,-2.59995507505905,-2.59655693786095,-2.59452721087574,
-2.59270559271037,-2.59037586012033,-2.58550765200907,-2.56392543158225,
-2.54889540567895,-2.53888995871644,-2.53683576545242,-2.53567100647635,
-2.53464445631786,-2.53328713069123,-2.53018466006796,-2.50869152597703,
-2.49158372393118,-2.48519446016765,-2.48037324705607,-2.47805234210953,
-2.47623166198625,-2.47419680551015,-2.47077514189218,-2.45759998322799,
-2.43545671446359,-2.42629105838255,-2.42272910519923,-2.42007196092014,
-2.41878263408276,-2.4178626761167,-2.41667770961938,-2.41458750897691,
-2.40494486365705,-2.38590752884688,-2.37265962288026,-2.36718021266936,
-2.36289876059312,-2.36068327325347,-2.35887115502185,-2.35676392121772,
-2.35310555882761,-2.33101233536977,-2.31237978797182,-2.30698881677355,
-2.303356392832,-2.30189571570355,-2.30085703904073,-2.29972943526284,-2.29784493692715,
-2.29132389915938,-2.2655802373753,-2.24868780790604,-2.24516421743623,
-2.24310736701001,-2.24129033897382,-2.23900548920624,-2.23437273187573,
-2.22608676643451),.UNSPECIFIED.);
#1616=B_SPLINE_CURVE_WITH_KNOTS('',3,(#119833,#119834,#119835,#119836,#119837,
#119838,#119839,#119840,#119841,#119842,#119843,#119844,#119845,#119846,
#119847,#119848,#119849,#119850,#119851,#119852,#119853,#119854,#119855,
#119856,#119857,#119858,#119859,#119860,#119861,#119862,#119863,#119864,
#119865,#119866,#119867,#119868,#119869,#119870,#119871,#119872,#119873,
#119874,#119875,#119876,#119877,#119878,#119879,#119880,#119881,#119882,
#119883,#119884,#119885,#119886,#119887,#119888,#119889,#119890,#119891,
#119892,#119893,#119894,#119895,#119896,#119897,#119898,#119899,#119900,
#119901,#119902,#119903,#119904,#119905,#119906,#119907,#119908,#119909,
#119910,#119911,#119912,#119913,#119914,#119915,#119916,#119917,#119918,
#119919,#119920,#119921,#119922,#119923,#119924,#119925,#119926,#119927,
#119928,#119929,#119930,#119931,#119932,#119933,#119934,#119935,#119936,
#119937,#119938,#119939,#119940,#119941,#119942,#119943,#119944,#119945,
#119946,#119947,#119948,#119949,#119950,#119951,#119952,#119953,#119954,
#119955,#119956,#119957,#119958,#119959,#119960,#119961,#119962,#119963,
#119964,#119965,#119966,#119967,#119968,#119969,#119970,#119971,#119972,
#119973,#119974,#119975,#119976,#119977,#119978,#119979,#119980,#119981,
#119982,#119983,#119984,#119985,#119986,#119987,#119988,#119989,#119990,
#119991,#119992,#119993,#119994,#119995,#119996,#119997,#119998,#119999,
#120000,#120001,#120002,#120003,#120004,#120005,#120006,#120007,#120008,
#120009,#120010,#120011,#120012,#120013,#120014,#120015,#120016,#120017,
#120018,#120019,#120020,#120021,#120022,#120023,#120024,#120025,#120026,
#120027,#120028,#120029,#120030,#120031,#120032,#120033,#120034,#120035,
#120036,#120037,#120038,#120039,#120040,#120041,#120042,#120043,#120044,
#120045,#120046,#120047,#120048,#120049,#120050,#120051,#120052,#120053,
#120054,#120055,#120056,#120057,#120058,#120059,#120060,#120061,#120062,
#120063,#120064,#120065,#120066,#120067,#120068,#120069,#120070,#120071,
#120072,#120073,#120074,#120075,#120076),.UNSPECIFIED.,.F.,.F.,(4,2,2,2,
2,2,2,2,2,2,2,2,2,2,2,2,2,2,2,2,2,2,2,2,2,2,2,2,2,2,2,2,2,2,2,2,2,2,2,2,
2,2,2,2,2,2,2,2,2,2,2,2,2,2,2,2,2,2,2,2,2,2,2,2,2,2,2,2,2,2,2,2,2,2,2,2,
2,2,2,2,2,2,2,2,2,2,2,2,2,2,2,2,2,2,2,2,2,2,2,2,2,2,2,2,2,2,2,2,2,2,2,2,
2,2,2,2,2,2,2,2,2,4),(-2.96786375617954,-2.96378011212947,-2.93841144513886,
-2.91929099895211,-2.91502414866376,-2.91281199116845,-2.91100052850842,
-2.90889172503984,-2.90522471437712,-2.88398853022001,-2.86864283089649,
-2.85684768434756,-2.85530143633461,-2.85396946682291,-2.85395746328359,
-2.8539454580821,-2.85393344738246,-2.85392142729917,-2.85390939387554,
-2.85389734305823,-2.853885270717,-2.85387317263873,-2.85386104450872,-2.85384888189198,
-2.85383668022117,-2.85382443485175,-2.85381214097922,-2.85379979364217,
-2.85379255029808,-2.8537850850793,-2.85377738427235,-2.85376943297857,
-2.8537612150429,-2.85375271278093,-2.85276266139395,-2.85154560427922,
-2.84935661837392,-2.83722774254759,-2.81722281878852,-2.80079809171344,
-2.7972967887381,-2.79524507431375,-2.79342784258526,-2.79113639099924,
-2.78646762546614,-2.75979460067696,-2.74595953704414,-2.74137263781126,
-2.73815166175674,-2.73675915076909,-2.73573129179428,-2.73457306029961,
-2.73254810965919,-2.72432663497843,-2.70137977818497,-2.68371618065551,
-2.68016008967731,-2.67809656907524,-2.67628098234639,-2.67400768311489,
-2.66958142973605,-2.64101270337113,-2.63656659279805,-2.62706253283171,
-2.62341680381072,-2.6207118305187,-2.61941342363992,-2.61849267611034,
-2.61731462257691,-2.61525416760211,-2.60611241832179,-2.58671418373808,
-2.57333631493625,-2.56512093122223,-2.56227796791665,-2.5603673603776,
-2.55851785594919,-2.55589001287662,-2.54972562592053,-2.51530424097516,
-2.50514778971678,-2.50308577858156,-2.50191936374699,-2.50089328894623,
-2.49953911482938,-2.49645440143038,-2.47476441782474,-2.45776926702449,
-2.45140380837669,-2.44659638211607,-2.44427816219535,-2.44245787160905,
-2.4404216766947,-2.43699347410117,-2.4238051775546,-2.40166689409547,-2.39250649030868,
-2.3889458124976,-2.38628940489537,-2.38500026543142,-2.38408037723338,
-2.3828954386582,-2.3808051774687,-2.37116096120318,-2.35211820748262,-2.33886668702043,
-2.33338622950079,-2.32910415154005,-2.32688861386955,-2.32507660019495,
-2.32296966191593,-2.31931228559718,-2.2972224280038,-2.28037895714556,
-2.2738897040351,-2.26973360365978,-2.26819453784391,-2.2671414493785,-2.26604118243269,
-2.26428045255196,-2.2588435727881,-2.2259764122215),.UNSPECIFIED.);
#1617=B_SPLINE_CURVE_WITH_KNOTS('',3,(#120081,#120082,#120083,#120084,#120085,
#120086,#120087,#120088,#120089,#120090,#120091,#120092,#120093,#120094,
#120095,#120096,#120097,#120098,#120099,#120100,#120101,#120102,#120103,
#120104,#120105,#120106,#120107,#120108,#120109,#120110,#120111,#120112,
#120113,#120114,#120115,#120116,#120117,#120118,#120119,#120120,#120121,
#120122,#120123,#120124,#120125,#120126,#120127,#120128,#120129,#120130,
#120131,#120132,#120133,#120134,#120135,#120136,#120137,#120138,#120139,
#120140,#120141,#120142,#120143,#120144,#120145,#120146,#120147,#120148,
#120149,#120150,#120151,#120152,#120153,#120154,#120155,#120156,#120157,
#120158,#120159,#120160,#120161,#120162,#120163,#120164,#120165,#120166,
#120167,#120168,#120169,#120170,#120171,#120172,#120173,#120174,#120175,
#120176,#120177,#120178,#120179,#120180,#120181,#120182,#120183,#120184,
#120185,#120186,#120187,#120188,#120189,#120190,#120191,#120192,#120193,
#120194,#120195,#120196,#120197,#120198,#120199,#120200,#120201,#120202,
#120203,#120204,#120205,#120206,#120207,#120208,#120209,#120210,#120211,
#120212,#120213,#120214,#120215,#120216,#120217,#120218,#120219,#120220,
#120221,#120222,#120223,#120224,#120225,#120226,#120227,#120228,#120229,
#120230,#120231,#120232,#120233,#120234,#120235,#120236,#120237,#120238,
#120239,#120240,#120241,#120242,#120243,#120244,#120245,#120246,#120247,
#120248,#120249,#120250,#120251,#120252,#120253,#120254,#120255,#120256,
#120257,#120258,#120259,#120260,#120261,#120262,#120263,#120264,#120265,
#120266,#120267,#120268,#120269,#120270,#120271,#120272,#120273,#120274,
#120275,#120276,#120277,#120278,#120279,#120280,#120281,#120282,#120283,
#120284,#120285,#120286,#120287,#120288,#120289,#120290,#120291,#120292,
#120293,#120294),.UNSPECIFIED.,.F.,.F.,(4,2,2,2,2,2,2,2,2,2,2,2,2,2,2,2,
2,2,2,2,2,2,2,2,2,2,2,2,2,2,2,2,2,2,2,2,2,2,2,2,2,2,2,2,2,2,2,2,2,2,2,2,
2,2,2,2,2,2,2,2,2,2,2,2,2,2,2,2,2,2,2,2,2,2,2,2,2,2,2,2,2,2,2,2,2,2,2,2,
2,2,2,2,2,2,2,2,2,2,2,2,2,2,2,2,2,2,4),(-0.74213368445771,-0.741060461331361,
-0.739913267852274,-0.738881528423136,-0.73746498088996,-0.734104923777809,
-0.729252868746627,-0.713978510749945,-0.689407102522553,-0.684623742302791,
-0.682309682649795,-0.680489371994206,-0.67844972183358,-0.675007291837811,
-0.659752468392614,-0.645099581600553,-0.638038602406348,-0.62628217224783,
-0.624088265812981,-0.622879857130139,-0.621860134935974,-0.620546416786616,
-0.617763138683222,-0.613980105693608,-0.603909895994989,-0.581115795296927,
-0.569702119864442,-0.566398037747063,-0.564388368144093,-0.562561632247161,
-0.560192693704824,-0.555115080641119,-0.548277159539189,-0.513885374889266,
-0.508253198435443,-0.506468872213815,-0.505363106188769,-0.504312691935271,
-0.502789118743533,-0.498743663735054,-0.492495368135684,-0.466566401205063,
-0.452794176426897,-0.449309095402972,-0.447260050771829,-0.445622959088123,
-0.443412291706371,-0.439157121738554,-0.424311686470956,-0.403979524002424,
-0.391863094776248,-0.389653195630644,-0.388441105957018,-0.387421541700861,
-0.386112214189044,-0.38335273720478,-0.379612047668472,-0.369720065740236,
-0.346651344500311,-0.33524447399746,-0.331940601323955,-0.3299307620635,
-0.32810368053141,-0.325734021066061,-0.320653777535694,-0.313811558375602,
-0.27936170952052,-0.273775642141207,-0.271996509396533,-0.270891768378505,
-0.269840442791227,-0.268312789488573,-0.264240237845529,-0.257934128724755,
-0.231372863825376,-0.218199398417869,-0.214776626821744,-0.212740839503349,
-0.210919154211932,-0.208596732040243,-0.203771525467293,-0.197375655071753,
-0.180244532455095,-0.158730966505941,-0.155627320835404,-0.1542693264795,
-0.153242218763514,-0.152076744565603,-0.150021137204183,-0.140003437519451,
-0.107427986167811,-0.099789382732737,-0.096937101024957,-0.0952149089678628,
-0.0933697957912819,-0.0911703237474851,-0.0861569041583209,-0.0793539652609495,
-0.0606703468593545,-0.0416052063917316,-0.0384147364760087,-0.0371643586513535,
-0.0361318961322054,-0.0350149612168854,-0.0331802271212109,-0.0309635957031294,
-9.99999994588663E-7),.UNSPECIFIED.);
#1618=B_SPLINE_CURVE_WITH_KNOTS('',3,(#120295,#120296,#120297,#120298,#120299,
#120300,#120301,#120302,#120303,#120304,#120305,#120306,#120307,#120308,
#120309,#120310,#120311,#120312,#120313,#120314,#120315,#120316,#120317,
#120318,#120319,#120320,#120321,#120322,#120323,#120324,#120325,#120326,
#120327,#120328,#120329,#120330,#120331,#120332,#120333,#120334,#120335,
#120336,#120337,#120338,#120339,#120340,#120341,#120342,#120343,#120344,
#120345,#120346,#120347,#120348,#120349,#120350,#120351,#120352,#120353,
#120354,#120355,#120356,#120357,#120358,#120359,#120360,#120361,#120362,
#120363,#120364,#120365,#120366,#120367,#120368,#120369,#120370,#120371,
#120372,#120373,#120374,#120375,#120376,#120377,#120378,#120379,#120380,
#120381,#120382,#120383,#120384,#120385,#120386,#120387,#120388,#120389,
#120390,#120391,#120392,#120393,#120394,#120395,#120396,#120397,#120398,
#120399,#120400,#120401,#120402,#120403,#120404,#120405,#120406,#120407,
#120408,#120409,#120410,#120411,#120412,#120413,#120414,#120415,#120416,
#120417,#120418,#120419,#120420,#120421,#120422,#120423,#120424,#120425,
#120426,#120427,#120428,#120429,#120430,#120431,#120432,#120433,#120434,
#120435,#120436,#120437,#120438,#120439,#120440,#120441,#120442,#120443,
#120444,#120445,#120446,#120447,#120448,#120449,#120450,#120451,#120452,
#120453,#120454,#120455,#120456,#120457,#120458,#120459,#120460,#120461,
#120462,#120463,#120464,#120465,#120466,#120467,#120468,#120469,#120470,
#120471,#120472,#120473,#120474,#120475,#120476,#120477,#120478,#120479,
#120480,#120481,#120482,#120483,#120484,#120485,#120486,#120487,#120488,
#120489,#120490,#120491,#120492,#120493,#120494,#120495,#120496,#120497,
#120498,#120499,#120500,#120501,#120502,#120503,#120504,#120505,#120506,
#120507,#120508),.UNSPECIFIED.,.F.,.F.,(4,2,2,2,2,2,2,2,2,2,2,2,2,2,2,2,
2,2,2,2,2,2,2,2,2,2,2,2,2,2,2,2,2,2,2,2,2,2,2,2,2,2,2,2,2,2,2,2,2,2,2,2,
2,2,2,2,2,2,2,2,2,2,2,2,2,2,2,2,2,2,2,2,2,2,2,2,2,2,2,2,2,2,2,2,2,2,2,2,
2,2,2,2,2,2,2,2,2,2,2,2,2,2,2,2,2,2,4),(-2.2259764122215,-2.22425628378077,
-2.21740905304554,-2.21232608992596,-2.20995671416596,-2.20813050011741,
-2.20612227226823,-2.20282260378006,-2.19145154282195,-2.16834133453937,
-2.15843797074299,-2.15469518279821,-2.1519350443964,-2.15062600491296,
-2.14960696389469,-2.1483958697176,-2.14618874234476,-2.13411461014791,
-2.11292307752032,-2.09752380211373,-2.0940745053629,-2.0920338685433,-2.09021457674336,
-2.08790441429328,-2.08313879335939,-2.05812210350068,-2.03745952708545,
-2.03472599290275,-2.03342200053563,-2.03240325553752,-2.03118817642637,
-2.02896324264578,-2.01596972923931,-2.01001250965625,-1.99493413568077,
-1.98025840719109,-1.97684995940238,-1.97481807056782,-1.97299701031433,
-1.97067145059373,-1.96582504370401,-1.94386208011153,-1.92908086965547,
-1.9191527491163,-1.9171026907723,-1.91593886843292,-1.91491217572012,-1.91355344204157,
-1.91044266794885,-1.88932528614479,-1.87194878512497,-1.86550251094958,
-1.86064834204034,-1.85832128657316,-1.85650001406538,-1.85446887765395,
-1.85106408999226,-1.83816812869897,-1.81132451768157,-1.80499344509727,
-1.80091021846368,-1.79938153804988,-1.79833044452903,-1.79722693783769,
-1.79545160635758,-1.78989248233265,-1.75544062518884,-1.74860128995825,
-1.74352274392376,-1.7411541246853,-1.73932795300417,-1.73731923040808,
-1.73401749430364,-1.72247941086814,-1.69945047463344,-1.68960775261839,
-1.68587949384137,-1.68312755324843,-1.68182004825567,-1.68089815279672,
-1.67972595593863,-1.6776916143627,-1.66897074193232,-1.66500010961163,
-1.6447789055654,-1.62878015876585,-1.62529937335927,-1.62325188517156,
-1.62143366189215,-1.61913457459874,-1.61442720270841,-1.58828677187455,
-1.56803155580148,-1.56568690462733,-1.56446043519854,-1.56344241534644,
-1.56215237055494,-1.56008316907118,-1.5443132260124,-1.52965471026575,
-1.51325822354984,-1.50879867441267,-1.50654770813344,-1.50475016736747,
-1.50267628825316,-1.4991657852467,-1.48408042832229),.UNSPECIFIED.);
#1619=B_SPLINE_CURVE_WITH_KNOTS('',3,(#120513,#120514,#120515,#120516,#120517,
#120518,#120519,#120520,#120521,#120522,#120523,#120524,#120525,#120526,
#120527,#120528,#120529,#120530,#120531,#120532,#120533,#120534,#120535,
#120536,#120537,#120538,#120539,#120540,#120541,#120542,#120543,#120544,
#120545,#120546,#120547,#120548,#120549,#120550,#120551,#120552,#120553,
#120554,#120555,#120556,#120557,#120558,#120559,#120560,#120561,#120562,
#120563,#120564,#120565,#120566,#120567,#120568,#120569,#120570,#120571,
#120572,#120573,#120574,#120575,#120576,#120577,#120578,#120579,#120580,
#120581,#120582,#120583,#120584,#120585,#120586,#120587,#120588,#120589,
#120590,#120591,#120592,#120593,#120594,#120595,#120596,#120597,#120598,
#120599,#120600,#120601,#120602,#120603,#120604,#120605,#120606,#120607,
#120608,#120609,#120610,#120611,#120612,#120613,#120614,#120615,#120616,
#120617,#120618,#120619,#120620,#120621,#120622,#120623,#120624,#120625,
#120626,#120627,#120628,#120629,#120630,#120631,#120632,#120633,#120634,
#120635,#120636,#120637,#120638,#120639,#120640,#120641,#120642,#120643,
#120644,#120645,#120646,#120647,#120648,#120649,#120650,#120651,#120652,
#120653,#120654,#120655,#120656,#120657,#120658,#120659,#120660,#120661,
#120662,#120663,#120664,#120665,#120666,#120667,#120668,#120669,#120670,
#120671,#120672,#120673,#120674,#120675,#120676,#120677,#120678,#120679,
#120680,#120681,#120682,#120683,#120684,#120685,#120686,#120687,#120688,
#120689,#120690,#120691,#120692,#120693,#120694,#120695,#120696,#120697,
#120698,#120699,#120700,#120701,#120702,#120703,#120704,#120705,#120706,
#120707,#120708,#120709,#120710,#120711,#120712,#120713,#120714,#120715,
#120716),.UNSPECIFIED.,.F.,.F.,(4,2,2,2,2,2,2,2,2,2,2,2,2,2,2,2,2,2,2,2,
2,2,2,2,2,2,2,2,2,2,2,2,2,2,2,2,2,2,2,2,2,2,2,2,2,2,2,2,2,2,2,2,2,2,2,2,
2,2,2,2,2,2,2,2,2,2,2,2,2,2,2,2,2,2,2,2,2,2,2,2,2,2,2,2,2,2,2,2,2,2,2,2,
2,2,2,2,2,2,2,2,2,4),(-1.48412040656859,-1.48082148178739,-1.46574011190158,
-1.45962859656999,-1.44680686389676,-1.44476382001585,-1.4434814452826,
-1.44246351060667,-1.44122987116206,-1.43885139570483,-1.41849408519134,
-1.39255622452202,-1.38783773326304,-1.38553615482571,-1.38371725275182,
-1.38167035033535,-1.3781938923928,-1.36229547724367,-1.33907177662105,
-1.32934887034997,-1.32725398897561,-1.32606783682932,-1.32514784158701,
-1.32385962122743,-1.32120888197452,-1.31765862536708,-1.30854075520546,
-1.28648398574501,-1.2731842051744,-1.26975462372141,-1.26771780557239,
-1.2658970655478,-1.26357841092839,-1.25877057215442,-1.25240403450815,
-1.23540594709219,-1.21369531991906,-1.2106101871287,-1.20925570946243,
-1.20822936030441,-1.20706253266058,-1.20499956509593,-1.19483020961972,
-1.16017891010646,-1.15420560452021,-1.15186693942054,-1.15015613169257,
-1.14830437428156,-1.14576988545933,-1.13973084436134,-1.13111087709734,
-1.10547618480664,-1.09500491757566,-1.09287013930818,-1.09167502967595,
-1.09065385665762,-1.08932175709915,-1.08644010912123,-1.07417759234089,
-1.0521670197258,-1.03878081073498,-1.03534604319968,-1.03330817432964,
-1.03148774786634,-1.02917120837372,-1.02437412304914,-1.01802602864954,
-1.00111316188268,-0.979274228817487,-0.976497079413082,-0.975155231787754,
-0.974194139420834,-0.973135642989955,-0.971570248014536,-0.967226486820596,
-0.960323152528731,-0.924233981012744,-0.919182874805421,-0.916844410137595,
-0.915016757839911,-0.913012198141236,-0.909730633684257,-0.8969752878299,
-0.864614557572141,-0.859691904762698,-0.857996031461812,-0.857017649022139,
-0.855973612590148,-0.854483314218406,-0.850660632927603,-0.844881660672618,
-0.82334110480409,-0.804783359721267,-0.801147009071279,-0.799044493782142,
-0.797231742973639,-0.795009557879451,-0.790695996527068,-0.775387421492797,
-0.750606962364917,-0.743033356308706,-0.74213368445771),.UNSPECIFIED.);
#1620=B_SPLINE_CURVE_WITH_KNOTS('',3,(#120717,#120718,#120719,#120720,#120721,
#120722,#120723,#120724,#120725,#120726,#120727,#120728,#120729,#120730,
#120731,#120732,#120733,#120734,#120735,#120736,#120737,#120738,#120739,
#120740,#120741,#120742,#120743,#120744,#120745,#120746,#120747,#120748,
#120749,#120750,#120751,#120752,#120753,#120754,#120755,#120756,#120757,
#120758,#120759,#120760,#120761,#120762,#120763,#120764,#120765,#120766,
#120767,#120768,#120769,#120770,#120771,#120772,#120773,#120774,#120775,
#120776,#120777,#120778,#120779,#120780,#120781,#120782,#120783,#120784,
#120785,#120786,#120787,#120788,#120789,#120790,#120791,#120792,#120793,
#120794,#120795,#120796,#120797,#120798,#120799,#120800,#120801,#120802,
#120803,#120804,#120805,#120806,#120807,#120808,#120809,#120810,#120811,
#120812,#120813,#120814,#120815,#120816,#120817,#120818,#120819,#120820,
#120821,#120822,#120823,#120824,#120825,#120826,#120827,#120828,#120829,
#120830,#120831,#120832,#120833,#120834,#120835,#120836,#120837,#120838,
#120839,#120840,#120841,#120842,#120843,#120844,#120845,#120846,#120847,
#120848,#120849,#120850,#120851,#120852,#120853,#120854,#120855,#120856,
#120857,#120858,#120859,#120860,#120861,#120862,#120863,#120864,#120865,
#120866,#120867,#120868,#120869,#120870,#120871,#120872,#120873,#120874,
#120875,#120876,#120877,#120878,#120879,#120880,#120881,#120882,#120883,
#120884,#120885,#120886,#120887,#120888,#120889,#120890,#120891,#120892,
#120893,#120894,#120895,#120896,#120897,#120898,#120899,#120900,#120901,
#120902,#120903,#120904,#120905,#120906,#120907,#120908,#120909,#120910,
#120911,#120912,#120913,#120914,#120915,#120916,#120917,#120918,#120919,
#120920,#120921,#120922,#120923,#120924,#120925,#120926),.UNSPECIFIED.,
 .F.,.F.,(4,2,2,2,2,2,2,2,2,2,2,2,2,2,2,2,2,2,2,2,2,2,2,2,2,2,2,2,2,2,2,
2,2,2,2,2,2,2,2,2,2,2,2,2,2,2,2,2,2,2,2,2,2,2,2,2,2,2,2,2,2,2,2,2,2,2,2,
2,2,2,2,2,2,2,2,2,2,2,2,2,2,2,2,2,2,2,2,2,2,2,2,2,2,2,2,2,2,2,2,2,2,2,2,
2,4),(-1.48408042832229,-1.48376664299265,-1.46114076049178,-1.45054639973923,
-1.4484008663561,-1.44720343557792,-1.44618273513266,-1.44485447556968,
-1.44199291362653,-1.4235726312338,-1.39629157020093,-1.39167501278574,
-1.38939333124003,-1.38757663247404,-1.38551782371353,-1.38198502686217,
-1.36489249373927,-1.33976498747468,-1.33286042335265,-1.33094627999807,
-1.32981214828741,-1.32877614612721,-1.32733141389717,-1.32379881274751,
-1.31860832013949,-1.30130110862416,-1.2794458178099,-1.27459629617925,
-1.27226999993658,-1.27044868397678,-1.26841684067741,-1.26500927844663,
-1.25035576603178,-1.23524420141299,-1.22931597518159,-1.21626791406282,
-1.21404279911828,-1.21282759713475,-1.21180872549969,-1.21050455178258,
-1.20777055250332,-1.18703788587951,-1.16211551129242,-1.15734647651094,
-1.15503547263141,-1.15321586934416,-1.15117524933759,-1.14772688983962,
-1.13235471934567,-1.11143780144199,-1.1076205454009,-1.09873985078699,
-1.09669472316324,-1.09551999073136,-1.09459840878217,-1.09329437668301,
-1.09056107817527,-1.06990751197003,-1.04489968762296,-1.04013433919366,
-1.03782405067679,-1.03600453765067,-1.03396352455051,-1.03051328787816,
-1.01510613239754,-0.993891289332276,-0.981815317663498,-0.979607850191654,
-0.978396577969166,-0.97737738353288,-0.976068154383664,-0.973307619550056,
-0.969564684118706,-0.95966171815368,-0.936579865867218,-0.925201037611923,
-0.921900427748099,-0.919891794237271,-0.918065315730189,-0.915695746899244,
-0.910613014351861,-0.903765701502042,-0.869218524085517,-0.863722291686634,
-0.861954189398518,-0.860852150939333,-0.859799822597651,-0.858265493893037,
-0.854144009175637,-0.847731408440624,-0.830833549532936,-0.808689718737118,
-0.805032781718992,-0.80292566070683,-0.801113233015744,-0.798896866184818,
-0.794612169914818,-0.789127165718284,-0.775859502758688,-0.75678345007552,
-0.747155533671208,-0.745065666409472,-0.743880654051961,-0.742960514511092,
-0.74204764888634),.UNSPECIFIED.);
#1621=B_SPLINE_CURVE_WITH_KNOTS('',3,(#120931,#120932,#120933,#120934,#120935,
#120936,#120937,#120938,#120939,#120940,#120941,#120942,#120943,#120944,
#120945,#120946,#120947,#120948,#120949,#120950,#120951,#120952,#120953,
#120954,#120955,#120956,#120957,#120958,#120959,#120960,#120961,#120962,
#120963,#120964,#120965,#120966,#120967,#120968,#120969,#120970,#120971,
#120972,#120973,#120974,#120975,#120976,#120977,#120978,#120979,#120980,
#120981,#120982,#120983,#120984,#120985,#120986,#120987,#120988,#120989,
#120990,#120991,#120992,#120993,#120994,#120995,#120996,#120997,#120998,
#120999,#121000,#121001,#121002,#121003,#121004,#121005,#121006,#121007,
#121008,#121009,#121010,#121011,#121012,#121013,#121014,#121015,#121016,
#121017,#121018,#121019,#121020,#121021,#121022,#121023,#121024,#121025,
#121026,#121027,#121028,#121029,#121030,#121031,#121032,#121033,#121034,
#121035,#121036,#121037,#121038,#121039,#121040,#121041,#121042,#121043,
#121044,#121045,#121046,#121047,#121048,#121049,#121050,#121051,#121052,
#121053,#121054,#121055,#121056,#121057,#121058,#121059,#121060,#121061,
#121062,#121063,#121064,#121065,#121066,#121067,#121068,#121069,#121070,
#121071,#121072,#121073,#121074,#121075,#121076,#121077,#121078,#121079,
#121080,#121081,#121082,#121083,#121084,#121085,#121086,#121087,#121088,
#121089,#121090,#121091,#121092,#121093,#121094,#121095,#121096,#121097,
#121098,#121099,#121100,#121101,#121102,#121103,#121104,#121105,#121106,
#121107,#121108,#121109,#121110,#121111,#121112,#121113,#121114,#121115,
#121116,#121117,#121118,#121119,#121120,#121121,#121122,#121123,#121124,
#121125,#121126,#121127,#121128,#121129,#121130,#121131,#121132,#121133,
#121134,#121135,#121136,#121137,#121138,#121139,#121140,#121141,#121142,
#121143,#121144),.UNSPECIFIED.,.F.,.F.,(4,2,2,2,2,2,2,2,2,2,2,2,2,2,2,2,
2,2,2,2,2,2,2,2,2,2,2,2,2,2,2,2,2,2,2,2,2,2,2,2,2,2,2,2,2,2,2,2,2,2,2,2,
2,2,2,2,2,2,2,2,2,2,2,2,2,2,2,2,2,2,2,2,2,2,2,2,2,2,2,2,2,2,2,2,2,2,2,2,
2,2,2,2,2,2,2,2,2,2,2,2,2,2,2,2,2,2,4),(-2.22609961801482,-2.22556332767558,
-2.21080189555777,-2.20738749015127,-2.20535379388558,-2.20353218821009,
-2.2012074015045,-2.19636805452909,-2.17552754132884,-2.15790385451442,
-2.15227350392173,-2.14852307968545,-2.14704371560362,-2.14600154677802,
-2.14488065646882,-2.14302754487163,-2.13676884940031,-2.13122332319925,
-2.09748507458848,-2.0916169857361,-2.08911033753154,-2.08726311582116,
-2.0853111594724,-2.08227442410342,-2.07320934779991,-2.04560457994546,
-2.03266082996555,-2.03048206813715,-2.02929026865605,-2.02826846957923,
-2.02695333547304,-2.024087628352,-1.99943236232436,-1.97784586923063,-1.97357138152013,
-1.97135698244195,-1.96954451780279,-1.96743548224453,-1.96377042358467,
-1.94218576237533,-1.92635985520588,-1.91891549606693,-1.91580777306001,
-1.91341673991637,-1.91218047247507,-1.91116257480152,-1.90988302330995,
-1.90784956118684,-1.89535776847603,-1.88895093563702,-1.87395577686803,
-1.85916083006046,-1.85574455991814,-1.85371050838847,-1.85188905360386,
-1.84956510532392,-1.84472992223066,-1.82202909975717,-1.80777706002198,
-1.80121781824838,-1.79702943468748,-1.79548550233807,-1.79443121460751,
-1.79346554220677,-1.7918351220653,-1.78738538641425,-1.75165173785602,
-1.74474065300278,-1.73962138582896,-1.7372449481181,-1.7354173462335,-1.73341162800042,
-1.73012537265356,-1.71891090606944,-1.69571141668826,-1.68574279946609,
-1.68198409700383,-1.67921480268087,-1.67790378212643,-1.67688431170144,
-1.6756740005234,-1.67347138468028,-1.66150733172289,-1.65461876349508,
-1.6398073631068,-1.62476962615438,-1.62133964197631,-1.61930275103474,
-1.61748204878895,-1.6151635832835,-1.61035666076,-1.58642277066181,-1.56530819942813,
-1.56219585771367,-1.56083661460074,-1.55980961468118,-1.55864548475794,
-1.55659497610999,-1.54666410758093,-1.5318732939339,-1.5099507302706,-1.50510418815635,
-1.50277820190063,-1.5009566292511,-1.49892397477586,-1.49551375850441,
-1.48412040656859),.UNSPECIFIED.);
#1622=B_SPLINE_CURVE_WITH_KNOTS('',3,(#121145,#121146,#121147,#121148,#121149,
#121150,#121151,#121152,#121153,#121154,#121155,#121156,#121157,#121158,
#121159,#121160,#121161,#121162,#121163,#121164,#121165,#121166,#121167,
#121168,#121169,#121170,#121171,#121172,#121173,#121174,#121175,#121176,
#121177,#121178,#121179,#121180,#121181,#121182,#121183,#121184,#121185,
#121186,#121187,#121188,#121189,#121190,#121191,#121192,#121193,#121194,
#121195,#121196,#121197,#121198,#121199,#121200,#121201,#121202,#121203,
#121204,#121205,#121206,#121207,#121208,#121209,#121210,#121211,#121212,
#121213,#121214,#121215,#121216,#121217,#121218,#121219,#121220,#121221,
#121222,#121223,#121224,#121225,#121226,#121227,#121228,#121229,#121230,
#121231,#121232,#121233,#121234,#121235,#121236,#121237,#121238,#121239,
#121240,#121241,#121242,#121243,#121244,#121245,#121246,#121247,#121248,
#121249,#121250,#121251,#121252,#121253,#121254,#121255,#121256,#121257,
#121258,#121259,#121260,#121261,#121262,#121263,#121264,#121265,#121266,
#121267,#121268,#121269,#121270,#121271,#121272,#121273,#121274,#121275,
#121276,#121277,#121278,#121279,#121280,#121281,#121282,#121283,#121284,
#121285,#121286,#121287,#121288,#121289,#121290,#121291,#121292,#121293,
#121294,#121295,#121296,#121297,#121298,#121299,#121300,#121301,#121302,
#121303,#121304,#121305,#121306,#121307,#121308,#121309,#121310,#121311,
#121312,#121313,#121314,#121315,#121316,#121317,#121318,#121319,#121320,
#121321,#121322,#121323,#121324,#121325,#121326,#121327,#121328,#121329,
#121330,#121331,#121332,#121333,#121334,#121335,#121336,#121337,#121338,
#121339,#121340,#121341,#121342,#121343,#121344,#121345,#121346,#121347,
#121348,#121349,#121350,#121351,#121352,#121353,#121354,#121355,#121356,
#121357,#121358,#121359,#121360,#121361,#121362,#121363,#121364,#121365,
#121366,#121367,#121368,#121369,#121370,#121371,#121372),.UNSPECIFIED.,
 .F.,.F.,(4,2,2,2,2,2,2,2,2,2,2,2,2,2,2,2,2,2,2,2,2,2,2,2,2,2,2,2,2,2,2,
2,2,2,2,2,2,2,2,2,2,2,2,2,2,2,2,2,2,2,2,2,2,2,2,2,2,2,2,2,2,2,2,2,2,2,2,
2,2,2,2,2,2,2,2,2,2,2,2,2,2,2,2,2,2,2,2,2,2,2,2,2,2,2,2,2,2,2,2,2,2,2,2,
2,2,2,2,2,2,2,2,2,2,4),(-0.74204764888634,-0.741670791865605,-0.739012316314998,
-0.735448644722572,-0.726277726514639,-0.704151134559818,-0.690970543427621,
-0.687548117910528,-0.685512860146582,-0.683691858811255,-0.681370608177842,
-0.676549015115992,-0.670158822644936,-0.653051742934083,-0.631508312556897,
-0.628403527682639,-0.627045618070197,-0.626018821544591,-0.624854014741848,
-0.622800318503052,-0.612809549364189,-0.597830478773235,-0.576171490404625,
-0.571309192892764,-0.568980263000083,-0.567158399832068,-0.56512750846632,
-0.56172531021177,-0.54716850794111,-0.531985435400949,-0.526618440682185,
-0.512984136553094,-0.510943076728187,-0.509661307973488,-0.508643420409092,
-0.507409341360159,-0.505028665738601,-0.501938496769546,-0.494557409918824,
-0.47869437733524,-0.457076808974808,-0.453405307478627,-0.451294929893803,
-0.449482702788917,-0.447270349220692,-0.443005509136648,-0.425901253236259,
-0.408473004259165,-0.401912962552111,-0.395131608666908,-0.393228056902245,
-0.392096150899994,-0.391059047653106,-0.389608388598855,-0.386039746323683,
-0.380777780233697,-0.363011746042743,-0.341732737130473,-0.336880754347417,
-0.334553780609715,-0.332732152642795,-0.330700186805467,-0.327292963617882,
-0.312651624283672,-0.297527702476826,-0.291669261037713,-0.278543052645347,
-0.276317319176379,-0.275101870655147,-0.274082849712495,-0.272778558271081,
-0.270044561968888,-0.249357556165051,-0.224378423698583,-0.21961090779958,
-0.217299980563585,-0.215480146480685,-0.213438963421036,-0.209988906109757,
-0.194592806373508,-0.173490174260136,-0.161291623309227,-0.159078164370229,
-0.157865444820671,-0.156846199323849,-0.155538400039576,-0.152786026073709,
-0.149057693378639,-0.139216379301996,-0.125356799839326,-0.105416407194767,
-0.101751945956182,-0.0996431355881328,-0.0978308038861879,-0.0977586976386119,
-0.0976923001905339,-0.0976308451375815,-0.0975736963287582,-0.0975203211224048,
-0.0974702699703891,-0.097423160629703,-0.0973786658315197,-0.0952050846410103,
-0.0903331681393833,-0.083786017071551,-0.0659268366182135,-0.0454950428270455,
-0.0426547737456153,-0.0411489605696309,-0.0401124249770891,-0.0390042464901762,
-0.0372083444533776,-0.0308374795419021,-9.99999999917733E-7),
 .UNSPECIFIED.);
#1623=B_SPLINE_CURVE_WITH_KNOTS('',3,(#121377,#121378,#121379,#121380,#121381,
#121382,#121383,#121384,#121385,#121386,#121387,#121388,#121389,#121390,
#121391,#121392,#121393,#121394,#121395,#121396,#121397,#121398,#121399,
#121400,#121401,#121402,#121403,#121404,#121405,#121406,#121407,#121408,
#121409,#121410,#121411,#121412,#121413,#121414,#121415,#121416,#121417,
#121418,#121419,#121420,#121421,#121422,#121423,#121424,#121425,#121426,
#121427,#121428,#121429,#121430,#121431,#121432,#121433,#121434,#121435,
#121436,#121437,#121438,#121439,#121440,#121441,#121442,#121443,#121444,
#121445,#121446,#121447,#121448,#121449,#121450,#121451,#121452,#121453,
#121454,#121455,#121456,#121457,#121458,#121459,#121460,#121461,#121462,
#121463,#121464,#121465,#121466,#121467,#121468,#121469,#121470,#121471,
#121472,#121473,#121474,#121475,#121476,#121477,#121478,#121479,#121480,
#121481,#121482,#121483,#121484,#121485,#121486,#121487,#121488,#121489,
#121490,#121491,#121492,#121493,#121494,#121495,#121496,#121497,#121498,
#121499,#121500,#121501,#121502,#121503,#121504,#121505,#121506,#121507,
#121508,#121509,#121510,#121511,#121512,#121513,#121514,#121515,#121516,
#121517,#121518,#121519,#121520,#121521,#121522,#121523,#121524,#121525,
#121526,#121527,#121528,#121529,#121530,#121531,#121532,#121533,#121534,
#121535,#121536,#121537,#121538,#121539,#121540,#121541,#121542,#121543,
#121544,#121545,#121546,#121547,#121548,#121549,#121550,#121551,#121552,
#121553,#121554,#121555,#121556,#121557,#121558,#121559,#121560,#121561,
#121562,#121563,#121564,#121565,#121566,#121567,#121568,#121569,#121570,
#121571,#121572,#121573,#121574,#121575,#121576,#121577,#121578,#121579,
#121580,#121581,#121582,#121583,#121584,#121585,#121586,#121587,#121588,
#121589,#121590,#121591,#121592,#121593,#121594,#121595,#121596),
 .UNSPECIFIED.,.F.,.F.,(4,2,2,2,2,2,2,2,2,2,2,2,2,2,2,2,2,2,2,2,2,2,2,2,
2,2,2,2,2,2,2,2,2,2,2,2,2,2,2,2,2,2,2,2,2,2,2,2,2,2,2,2,2,2,2,2,2,2,2,2,
2,2,2,2,2,2,2,2,2,2,2,2,2,2,2,2,2,2,2,2,2,2,2,2,2,2,2,2,2,2,2,2,2,2,2,2,
2,2,2,2,2,2,2,2,2,2,2,2,2,4),(-2.96804921651682,-2.96740018557415,-2.96636690768878,
-2.9652244441556,-2.96327309443646,-2.95594501532251,-2.95235016748792,
-2.93395364698124,-2.91557597381258,-2.91128095729757,-2.90906245417739,
-2.90724982949593,-2.9051442184243,-2.90149429568817,-2.88201497995418,
-2.85583203712465,-2.85183614570248,-2.85031989175863,-2.84927095635197,
-2.84816299218549,-2.84636837540087,-2.84064565571773,-2.83513624202623,
-2.81674471798401,-2.80371791225676,-2.79829564462427,-2.79404873373829,
-2.79183984473697,-2.79002755182002,-2.78791378799744,-2.7842278770267,
-2.76265490157924,-2.74680552123245,-2.73580893222999,-2.73370582241923,
-2.73253023540477,-2.73150562286161,-2.73016551489865,-2.7271620745997,
-2.70404947525284,-2.68351131196158,-2.67766824547294,-2.67516559838338,
-2.67331889938587,-2.67136526914252,-2.66832130501516,-2.65919749540911,
-2.63163968534097,-2.61977691757225,-2.61694057164501,-2.61561674400291,
-2.61459610465318,-2.6133947619652,-2.61123293034756,-2.60026061716805,
-2.56663224468561,-2.56052505473452,-2.5579793309458,-2.55612540546224,
-2.55418625212886,-2.55120988808159,-2.54263542946784,-2.51733662235103,
-2.51508602961282,-2.50585484299411,-2.50227616797712,-2.49960926619588,
-2.4983178408928,-2.49739745978806,-2.49621344778694,-2.49412828150278,
-2.48458654653846,-2.4654704513213,-2.45219295846012,-2.44670534290785,
-2.44241865517638,-2.44020176127328,-2.43838913146348,-2.43628202441509,
-2.43262571917638,-2.41010828841658,-2.39180159508405,-2.38645778274185,
-2.38284854737319,-2.38139131429905,-2.38035301855822,-2.37922358384149,
-2.37733161982564,-2.37068125132752,-2.36410984526234,-2.35777659506131,
-2.34276442753719,-2.32799245906315,-2.32457748261986,-2.32254368610575,
-2.32072213964739,-2.31839763373028,-2.31355964007905,-2.29270730497905,
-2.27457051600587,-2.26925197284302,-2.26565531310506,-2.26420006447268,
-2.26316209000569,-2.2620318174849,-2.26013611012157,-2.25344495903044,
-2.24688051099489,-2.2405835000354,-2.22609961801482),.UNSPECIFIED.);
#1624=B_SPLINE_CURVE_WITH_KNOTS('',3,(#121597,#121598,#121599,#121600,#121601,
#121602,#121603,#121604,#121605,#121606,#121607,#121608,#121609,#121610,
#121611,#121612,#121613,#121614,#121615,#121616,#121617,#121618,#121619,
#121620,#121621,#121622,#121623,#121624,#121625,#121626,#121627,#121628,
#121629,#121630,#121631,#121632,#121633,#121634,#121635,#121636,#121637,
#121638,#121639,#121640,#121641,#121642,#121643,#121644,#121645,#121646,
#121647,#121648,#121649,#121650,#121651,#121652,#121653,#121654,#121655,
#121656,#121657,#121658,#121659,#121660,#121661,#121662,#121663,#121664,
#121665,#121666,#121667,#121668,#121669,#121670,#121671,#121672,#121673,
#121674,#121675,#121676,#121677,#121678,#121679,#121680,#121681,#121682,
#121683,#121684,#121685,#121686,#121687,#121688,#121689,#121690,#121691,
#121692,#121693,#121694,#121695,#121696,#121697,#121698,#121699,#121700,
#121701,#121702,#121703,#121704,#121705,#121706,#121707,#121708,#121709,
#121710,#121711,#121712,#121713,#121714,#121715,#121716,#121717,#121718,
#121719,#121720,#121721,#121722,#121723,#121724,#121725,#121726,#121727,
#121728,#121729,#121730,#121731,#121732,#121733,#121734,#121735,#121736,
#121737,#121738,#121739,#121740,#121741,#121742,#121743,#121744,#121745,
#121746,#121747,#121748,#121749,#121750,#121751,#121752,#121753,#121754,
#121755,#121756,#121757,#121758,#121759,#121760,#121761,#121762,#121763,
#121764,#121765,#121766,#121767,#121768,#121769,#121770,#121771,#121772,
#121773,#121774,#121775,#121776,#121777,#121778,#121779,#121780,#121781,
#121782,#121783,#121784,#121785,#121786,#121787,#121788,#121789,#121790,
#121791,#121792,#121793,#121794,#121795,#121796,#121797,#121798,#121799,
#121800,#121801,#121802,#121803,#121804,#121805,#121806,#121807,#121808,
#121809,#121810,#121811,#121812,#121813,#121814,#121815,#121816,#121817,
#121818,#121819,#121820,#121821,#121822,#121823,#121824,#121825,#121826,
#121827,#121828,#121829,#121830,#121831,#121832,#121833,#121834,#121835,
#121836,#121837,#121838),.UNSPECIFIED.,.F.,.F.,(4,2,2,2,2,2,2,2,2,2,2,2,
2,2,2,2,2,2,2,2,2,2,2,2,2,2,2,2,2,2,2,2,2,2,2,2,2,2,2,2,2,2,2,2,2,2,2,2,
2,2,2,2,2,2,2,2,2,2,2,2,2,2,2,2,2,2,2,2,2,2,2,2,2,2,2,2,2,2,2,2,2,2,2,2,
2,2,2,2,2,2,2,2,2,2,2,2,2,2,2,2,2,2,2,2,2,2,2,2,2,2,2,2,2,2,2,2,2,2,2,2,
4),(-3.17249826874624,-3.15996572603712,-3.157529950244,-3.15570792548478,
-3.15398958290604,-3.15229751877215,-3.15003259406328,-3.14450001108718,
-3.13163795961908,-3.10262595841067,-3.09812298178249,-3.09653671995918,
-3.09547440212686,-3.09451803466948,-3.09293426290759,-3.08879133768354,
-3.06558234112219,-3.05075155693984,-3.04487784726782,-3.04039185782308,
-3.03815996048887,-3.03813008624643,-3.038098823617,-3.03806609921834,-3.03803183529047,
-3.03799594943884,-3.037958354382,-3.03791895762843,-3.0378776612519,-3.03785330622156,
-3.03782282349539,-3.03778467372763,-3.0377369341454,-3.03767720680599,
-3.03760250894207,-3.03752383761234,-3.0357030316206,-3.03337492711704,
-3.02851240858195,-3.0063911165544,-2.99175817505828,-2.98187903292201,
-2.97983211928711,-2.97866922844905,-2.97764276181246,-2.97628355749059,
-2.97316846357522,-2.95216989591933,-2.94231298690757,-2.92598537941526,
-2.92248908762707,-2.92043861528152,-2.91862145887172,-2.91632872476524,
-2.91165239880608,-2.88508965512769,-2.86523538391448,-2.86288366085681,
-2.86165593334355,-2.86063828518764,-2.85935050180203,-2.85728824587902,
-2.84239039005393,-2.83927346191504,-2.81867833424378,-2.8116151234893,
-2.80641105707509,-2.80401992766183,-2.80219107587269,-2.8001939239654,
-2.79694440017387,-2.78591222668791,-2.76276300193371,-2.75259060918443,
-2.74878399583113,-2.74598797163831,-2.74467225243698,-2.74365287369737,
-2.74244713445332,-2.74026351870955,-2.72873497984704,-2.70290988376886,
-2.69109561439306,-2.68788816846166,-2.6859001556504,-2.6840685702862,-2.68169844644491,
-2.67771255398351,-2.64868002347202,-2.63629863002996,-2.62990104654788,
-2.6281031535377,-2.62699487168615,-2.62595915763727,-2.62445590644093,
-2.6216241247957,-2.60103789025177,-2.58331614647095,-2.57679872877489,
-2.57190382443153,-2.56956941470045,-2.56774763218338,-2.56572131731914,
-2.5623375498601,-2.54976784915376,-2.51678453095886,-2.51226582424226,
-2.51067718289416,-2.5096141517007,-2.50865784006037,-2.50733388925779,
-2.50463059782684,-2.48140117165499,-2.46089262065977,-2.4551090437446,
-2.45261698569481,-2.45077266883969,-2.44881655782831,-2.44575829990954,
-2.43650710435452,-2.43074206186157),.UNSPECIFIED.);
#1625=B_SPLINE_CURVE_WITH_KNOTS('',3,(#121844,#121845,#121846,#121847,#121848,
#121849,#121850,#121851,#121852,#121853,#121854,#121855,#121856,#121857,
#121858,#121859,#121860,#121861,#121862,#121863,#121864,#121865,#121866,
#121867,#121868,#121869,#121870,#121871,#121872,#121873,#121874,#121875,
#121876,#121877,#121878,#121879,#121880,#121881,#121882,#121883,#121884,
#121885,#121886,#121887,#121888,#121889,#121890,#121891,#121892,#121893,
#121894,#121895,#121896,#121897,#121898,#121899,#121900,#121901,#121902,
#121903,#121904,#121905,#121906,#121907,#121908,#121909,#121910,#121911,
#121912,#121913,#121914,#121915,#121916,#121917,#121918,#121919,#121920,
#121921,#121922,#121923,#121924,#121925,#121926,#121927,#121928,#121929,
#121930,#121931,#121932,#121933,#121934,#121935,#121936,#121937,#121938,
#121939,#121940,#121941,#121942,#121943,#121944,#121945,#121946,#121947,
#121948,#121949,#121950,#121951,#121952,#121953,#121954,#121955,#121956,
#121957,#121958,#121959,#121960,#121961,#121962,#121963,#121964,#121965,
#121966,#121967,#121968,#121969,#121970,#121971,#121972,#121973,#121974,
#121975,#121976,#121977,#121978,#121979,#121980,#121981,#121982,#121983,
#121984,#121985,#121986,#121987,#121988,#121989,#121990,#121991,#121992,
#121993,#121994,#121995,#121996,#121997,#121998,#121999,#122000,#122001,
#122002,#122003),.UNSPECIFIED.,.F.,.F.,(4,2,2,2,2,2,2,2,2,2,2,2,2,2,2,2,
2,2,2,2,2,2,2,2,2,2,2,2,2,2,2,2,2,2,2,2,2,2,2,2,2,2,2,2,2,2,2,2,2,2,2,2,
2,2,2,2,2,2,2,2,2,2,2,2,2,2,2,2,2,2,2,2,2,2,2,2,2,2,2,4),(-0.53741600959432,
-0.534484832243604,-0.519854900077587,-0.512786627924429,-0.501043645279421,
-0.498850283075522,-0.497641989366339,-0.496622245743267,-0.49530834754258,
-0.492524155824832,-0.488739511942901,-0.478662573346859,-0.455844798656207,
-0.444459269895697,-0.441157627619831,-0.439148475591579,-0.437321587095685,
-0.434951562703679,-0.429868086290401,-0.423019805479859,-0.388456053145617,
-0.382977631523204,-0.381211419722964,-0.380109634403813,-0.379056725781395,
-0.37752030930671,-0.373385664998653,-0.366944843583964,-0.350032573219157,
-0.327956050256951,-0.324296892333281,-0.322188981340229,-0.320376151089173,
-0.318159630407206,-0.313875681754338,-0.308392189512478,-0.295131263573339,
-0.276072580496971,-0.26642335744724,-0.264332057561692,-0.263146559066483,
-0.262226231407268,-0.260936461599468,-0.258278639091771,-0.254716292615004,
-0.245551357234333,-0.223432343813054,-0.219982607683143,-0.209749035659174,
-0.206580727778321,-0.204600199583779,-0.202764199958113,-0.200330633835428,
-0.194893670207973,-0.17142556703497,-0.150823119788353,-0.147988968339029,
-0.146484558743827,-0.145448079924042,-0.144338981131448,-0.142539753285958,
-0.136218438314228,-0.124042816166063,-0.0947797854898783,-0.0903781093229487,
-0.0881090574085132,-0.0862927524872583,-0.0842239697971216,-0.0810315137100925,
-0.0671218210259667,-0.049808689118311,-0.0336457193529712,-0.0304704048723358,
-0.0292224599991369,-0.0281906302242398,-0.0270726134321287,-0.0259062656496201,
-0.0241633810584764,-0.0209596523026307,-9.99999999362622E-7),
 .UNSPECIFIED.);
#1626=B_SPLINE_CURVE_WITH_KNOTS('',3,(#122004,#122005,#122006,#122007,#122008,
#122009,#122010,#122011,#122012,#122013,#122014,#122015,#122016,#122017,
#122018,#122019,#122020,#122021,#122022,#122023,#122024,#122025,#122026,
#122027,#122028,#122029,#122030,#122031,#122032,#122033,#122034,#122035,
#122036,#122037,#122038,#122039,#122040,#122041,#122042,#122043,#122044,
#122045,#122046,#122047,#122048,#122049,#122050,#122051,#122052,#122053,
#122054,#122055,#122056,#122057,#122058,#122059,#122060,#122061),
 .UNSPECIFIED.,.F.,.F.,(4,2,2,2,2,2,2,2,2,2,2,2,2,2,2,2,2,2,2,2,2,2,2,2,
2,2,2,2,4),(-3.17264791624771,-3.15505568789391,-3.14811105788344,-3.14571795912332,
-3.14348337569644,-3.14166987417207,-3.13957692736989,-3.13598326905043,
-3.11889625329433,-3.0980938169293,-3.08771727849231,-3.08548745148271,
-3.08425564172295,-3.08323758771176,-3.08195301449682,-3.07990273649253,
-3.06579456529562,-3.042135875813,-3.03122600181549,-3.02781438490697,-3.0257814219777,
-3.02395989650779,-3.02163441749417,-3.01679064919694,-2.99317995059097,
-2.97721906467787,-2.97224790087894,-2.9688268726201,-2.96804921651682),
 .UNSPECIFIED.);
#1627=B_SPLINE_CURVE_WITH_KNOTS('',3,(#122062,#122063,#122064,#122065,#122066,
#122067,#122068,#122069,#122070,#122071,#122072,#122073,#122074,#122075,
#122076,#122077,#122078,#122079,#122080,#122081,#122082,#122083,#122084,
#122085,#122086,#122087,#122088,#122089,#122090,#122091,#122092,#122093,
#122094,#122095,#122096,#122097,#122098,#122099,#122100,#122101,#122102,
#122103,#122104,#122105,#122106,#122107,#122108,#122109,#122110,#122111,
#122112,#122113,#122114,#122115,#122116,#122117,#122118,#122119,#122120,
#122121,#122122,#122123,#122124,#122125,#122126,#122127,#122128,#122129,
#122130,#122131,#122132,#122133,#122134,#122135,#122136,#122137,#122138,
#122139,#122140,#122141,#122142,#122143,#122144,#122145,#122146,#122147,
#122148,#122149,#122150,#122151,#122152,#122153,#122154,#122155,#122156,
#122157,#122158,#122159,#122160,#122161,#122162,#122163,#122164,#122165,
#122166,#122167,#122168,#122169,#122170,#122171,#122172,#122173,#122174,
#122175,#122176,#122177,#122178,#122179,#122180,#122181,#122182,#122183,
#122184,#122185,#122186,#122187,#122188,#122189,#122190,#122191,#122192,
#122193,#122194,#122195,#122196,#122197,#122198,#122199,#122200,#122201,
#122202,#122203,#122204,#122205,#122206,#122207,#122208,#122209,#122210,
#122211,#122212,#122213,#122214,#122215,#122216,#122217,#122218,#122219,
#122220,#122221,#122222,#122223,#122224,#122225,#122226,#122227,#122228,
#122229,#122230,#122231,#122232,#122233,#122234,#122235,#122236,#122237,
#122238,#122239,#122240,#122241,#122242,#122243,#122244,#122245,#122246,
#122247,#122248,#122249,#122250,#122251,#122252,#122253,#122254,#122255,
#122256,#122257,#122258,#122259,#122260,#122261,#122262,#122263,#122264,
#122265),.UNSPECIFIED.,.F.,.F.,(4,2,2,2,2,2,2,2,2,2,2,2,2,2,2,2,2,2,2,2,
2,2,2,2,2,2,2,2,2,2,2,2,2,2,2,2,2,2,2,2,2,2,2,2,2,2,2,2,2,2,2,2,2,2,2,2,
2,2,2,2,2,2,2,2,2,2,2,2,2,2,2,2,2,2,2,2,2,2,2,2,2,2,2,2,2,2,2,2,2,2,2,2,
2,2,2,2,2,2,2,2,2,4),(-2.43074206186157,-2.4090569147898,-2.39724404997104,
-2.39441402941403,-2.39309173731544,-2.39207163503482,-2.3908701905365,
-2.38870648531317,-2.37767316280368,-2.34407760162979,-2.33799939804609,
-2.33545901911373,-2.33360665066793,-2.33189784981673,-2.32956593126672,
-2.32363291502396,-2.2889091748288,-2.27873194303697,-2.27666881871534,
-2.27550214106668,-2.27447608853296,-2.27312227022324,-2.27003972310494,
-2.24810593095924,-2.23128039512432,-2.22495134245193,-2.22016500351806,
-2.21785074144045,-2.21603082923062,-2.21399221563774,-2.21055300399553,
-2.19709354860412,-2.17079964462455,-2.16451717080728,-2.16045648992661,
-2.15893104801878,-2.15788056607248,-2.15691112567371,-2.15526036840917,
-2.15066541382706,-2.11510333833867,-2.1082013764317,-2.10308749213984,
-2.10071241106036,-2.09888539526737,-2.09687987329407,-2.09359293297056,
-2.08236515068073,-2.05917242582913,-2.0492084126796,-2.04545104019528,
-2.04268263341402,-2.04137198849434,-2.04035279662942,-2.03914282894785,
-2.03694089838078,-2.02498393131013,-2.01841566722429,-2.0043888570307,
-1.98833699660259,-1.98485346220588,-1.98280534318475,-1.9809871590231,
-1.97868893031814,-1.97398624522421,-1.94777049685608,-1.92757886243888,
-1.92523579783067,-1.92400963582356,-1.92299156692938,-1.92170107468881,
-1.91963043915727,-1.90293500712316,-1.88915843602945,-1.87128125497875,
-1.86771584884128,-1.86564998426402,-1.86383415040595,-1.86156293960789,
-1.85714839721741,-1.82846098495934,-1.81586772974028,-1.80940302599846,
-1.80759847251117,-1.80648848700649,-1.80545315353217,-1.80395335841114,
-1.80033667488877,-1.77661694535968,-1.75713805832133,-1.75165581368674,
-1.74921489748148,-1.747378348378,-1.7456429577935,-1.74271782478029,-1.7345447129076,
-1.70887823035537,-1.69435077256306,-1.69122943348981,-1.68985402446978,
-1.68882815015699,-1.68866836701421),.UNSPECIFIED.);
#1628=B_SPLINE_CURVE_WITH_KNOTS('',3,(#122270,#122271,#122272,#122273,#122274,
#122275,#122276,#122277,#122278,#122279,#122280,#122281,#122282,#122283,
#122284,#122285,#122286,#122287,#122288,#122289,#122290,#122291,#122292,
#122293,#122294,#122295,#122296,#122297,#122298,#122299,#122300,#122301,
#122302,#122303,#122304,#122305,#122306,#122307,#122308,#122309,#122310,
#122311,#122312,#122313,#122314,#122315,#122316,#122317,#122318,#122319,
#122320,#122321,#122322,#122323,#122324,#122325,#122326,#122327,#122328,
#122329,#122330,#122331,#122332,#122333,#122334,#122335,#122336,#122337,
#122338,#122339,#122340,#122341,#122342,#122343,#122344,#122345,#122346,
#122347,#122348,#122349,#122350,#122351,#122352,#122353,#122354,#122355,
#122356,#122357,#122358,#122359,#122360,#122361,#122362,#122363,#122364,
#122365,#122366,#122367,#122368,#122369,#122370,#122371,#122372,#122373,
#122374,#122375,#122376,#122377,#122378,#122379,#122380,#122381,#122382,
#122383,#122384,#122385,#122386,#122387,#122388,#122389,#122390,#122391,
#122392,#122393,#122394,#122395,#122396,#122397,#122398,#122399,#122400,
#122401,#122402,#122403,#122404,#122405,#122406,#122407,#122408,#122409,
#122410,#122411,#122412,#122413,#122414,#122415,#122416,#122417,#122418,
#122419,#122420,#122421,#122422,#122423,#122424,#122425,#122426,#122427,
#122428,#122429,#122430,#122431,#122432,#122433,#122434,#122435,#122436,
#122437,#122438,#122439,#122440,#122441,#122442,#122443,#122444,#122445,
#122446,#122447,#122448,#122449,#122450,#122451,#122452,#122453,#122454,
#122455,#122456,#122457,#122458,#122459,#122460,#122461,#122462,#122463,
#122464,#122465,#122466,#122467,#122468,#122469,#122470,#122471,#122472,
#122473,#122474,#122475,#122476,#122477,#122478,#122479,#122480,#122481),
 .UNSPECIFIED.,.F.,.F.,(4,2,2,2,2,2,2,2,2,2,2,2,2,2,2,2,2,2,2,2,2,2,2,2,
2,2,2,2,2,2,2,2,2,2,2,2,2,2,2,2,2,2,2,2,2,2,2,2,2,2,2,2,2,2,2,2,2,2,2,2,
2,2,2,2,2,2,2,2,2,2,2,2,2,2,2,2,2,2,2,2,2,2,2,2,2,2,2,2,2,2,2,2,2,2,2,2,
2,2,2,2,2,2,2,2,2,4),(-1.27924578165543,-1.27363190609435,-1.2642977297301,
-1.26122973084357,-1.25927146425767,-1.25742796374932,-1.25494140697023,
-1.24919109281031,-1.22936566748064,-1.20529050297461,-1.2023621082489,
-1.20103577987058,-1.20001308664896,-1.19882947187116,-1.19668788578905,
-1.18475869372216,-1.16952282675743,-1.14835190002979,-1.14468473223606,
-1.142575611829,-1.14076373297092,-1.13855087682873,-1.13428204777997,-1.11481019004502,
-1.09451565542147,-1.08661733085815,-1.08461569158226,-1.08346239205533,
-1.08243285547877,-1.08102981810248,-1.07774846564997,-1.07304738312471,
-1.05860561927177,-1.03286582706281,-1.02813720395848,-1.02583395193099,
-1.02401518244914,-1.02196995912114,-1.01850013800645,-1.00272081400972,
-0.97886595052194,-0.969606756653152,-0.967537518435581,-0.966357306748276,
-0.965436626301309,-0.964140581092339,-0.961448788895081,-0.957826721370322,
-0.948419697753517,-0.943730926363833,-0.915317806405154,-0.910876294510142,
-0.908599503501079,-0.906783222421048,-0.904721151758604,-0.901173245196586,
-0.883725870038095,-0.860957991008182,-0.852349631852284,-0.850321839434271,
-0.849151056019276,-0.848228745774727,-0.846918651915113,-0.844153594702399,
-0.840402605742695,-0.830465518135808,-0.807339613158091,-0.796053612439536,
-0.792761304123363,-0.79075446003744,-0.788927490730511,-0.786554248729905,
-0.781451429737925,-0.774568393654032,-0.739380289571229,-0.734456982475254,
-0.732761011859199,-0.731782603874834,-0.730738567977097,-0.729248314777892,
-0.725425990236165,-0.719647779091906,-0.698113708376985,-0.679547984343296,
-0.675911456109227,-0.673808888170751,-0.671996121473987,-0.669773954229791,
-0.665460548821992,-0.650153266734758,-0.625390789732032,-0.617800454356525,
-0.615825747012055,-0.614678148095272,-0.613646521560169,-0.612230784497594,
-0.608875621559339,-0.604033050420835,-0.588812496673201,-0.564165628442818,
-0.559385140058434,-0.557071611044161,-0.55525133964979,-0.553211339052226,
-0.549767352328332,-0.53741600959432),.UNSPECIFIED.);
#1629=B_SPLINE_CURVE_WITH_KNOTS('',3,(#122482,#122483,#122484,#122485,#122486,
#122487,#122488,#122489,#122490,#122491,#122492,#122493,#122494,#122495,
#122496,#122497,#122498,#122499,#122500,#122501,#122502,#122503,#122504,
#122505,#122506,#122507,#122508,#122509,#122510,#122511,#122512,#122513,
#122514,#122515,#122516,#122517,#122518,#122519,#122520,#122521,#122522,
#122523,#122524,#122525,#122526,#122527,#122528,#122529,#122530,#122531,
#122532,#122533,#122534,#122535,#122536,#122537,#122538,#122539,#122540,
#122541,#122542,#122543,#122544,#122545,#122546,#122547,#122548,#122549,
#122550,#122551,#122552,#122553,#122554,#122555,#122556,#122557,#122558,
#122559,#122560,#122561,#122562,#122563,#122564,#122565,#122566,#122567,
#122568,#122569,#122570,#122571,#122572,#122573,#122574,#122575,#122576,
#122577,#122578,#122579,#122580,#122581,#122582,#122583,#122584,#122585,
#122586,#122587,#122588,#122589,#122590,#122591,#122592,#122593,#122594,
#122595,#122596,#122597,#122598,#122599,#122600,#122601,#122602,#122603,
#122604,#122605,#122606,#122607,#122608,#122609,#122610,#122611,#122612,
#122613,#122614,#122615,#122616,#122617,#122618,#122619,#122620,#122621,
#122622,#122623,#122624,#122625,#122626,#122627,#122628,#122629,#122630,
#122631,#122632,#122633,#122634,#122635,#122636,#122637,#122638,#122639,
#122640,#122641,#122642,#122643,#122644,#122645,#122646,#122647,#122648,
#122649,#122650,#122651,#122652,#122653,#122654,#122655,#122656,#122657,
#122658,#122659,#122660,#122661,#122662,#122663,#122664,#122665,#122666,
#122667,#122668,#122669,#122670,#122671,#122672,#122673,#122674,#122675,
#122676,#122677,#122678,#122679,#122680,#122681,#122682,#122683,#122684,
#122685,#122686,#122687,#122688,#122689),.UNSPECIFIED.,.F.,.F.,(4,2,2,2,
2,2,2,2,2,2,2,2,2,2,2,2,2,2,2,2,2,2,2,2,2,2,2,2,2,2,2,2,2,2,2,2,2,2,2,2,
2,2,2,2,2,2,2,2,2,2,2,2,2,2,2,2,2,2,2,2,2,2,2,2,2,2,2,2,2,2,2,2,2,2,2,2,
2,2,2,2,2,2,2,2,2,2,2,2,2,2,2,2,2,2,2,2,2,2,2,2,2,2,2,4),(-1.68866836701421,
-1.68766003423988,-1.6856441604167,-1.67721851905643,-1.65335343849554,
-1.63810952549874,-1.63380486913827,-1.63158465220404,-1.62977223375796,
-1.62766868049812,-1.62402696439383,-1.60219375242694,-1.58623145092022,
-1.57564406792919,-1.57349871134111,-1.57230127023743,-1.57128048908813,
-1.56995203104287,-1.56708970214844,-1.54866551661408,-1.52138662442643,
-1.5167693673048,-1.51448745315367,-1.51267062076208,-1.51061171569116,
-1.50707889302881,-1.48999019440203,-1.46483184721473,-1.45794703092893,
-1.45603453311759,-1.45490071366645,-1.45386448642712,-1.4524187272107,
-1.44888014014972,-1.44367788574291,-1.42629671695579,-1.40454044140624,
-1.39968518745367,-1.39735771198411,-1.39553615420813,-1.3935047444938,
-1.3900996068696,-1.37548984238613,-1.36034594721379,-1.35464908177789,
-1.34135625090745,-1.33932228955552,-1.33804271129841,-1.33702498931849,
-1.33578919905587,-1.33339987244181,-1.33029517854445,-1.32286166325756,
-1.30703877634558,-1.28549539029785,-1.28180856903748,-1.27969487980205,
-1.2778830066361,-1.27567508402203,-1.27143154808291,-1.26601397942529,
-1.25300387770382,-1.23467307055161,-1.22401733820856,-1.22186906649175,
-1.22067096231294,-1.21965025107821,-1.21832270910871,-1.2154653455333,
-1.20341724369821,-1.17519556375446,-1.16678899363816,-1.16383428965986,
-1.16189998836635,-1.16004392430862,-1.15748433761299,-1.15128860406224,
-1.14236223506171,-1.12629683593003,-1.1084254567127,-1.10521449493295,
-1.10396122945004,-1.10292838564219,-1.10181362539722,-1.09998738289662,
-1.09328353553487,-1.07990326569269,-1.05253619241229,-1.04792748526969,
-1.04564728977325,-1.04383068209268,-1.04177080822787,-1.03823322455044,
-1.02103273135173,-0.996631374783848,-0.98920258671719,-0.987242851936966,
-0.986098684347984,-0.98506625075259,-0.983644075971947,-0.980249305024847,
-0.975329701243524,-0.95966761514608,-0.946673080131941),.UNSPECIFIED.);
#1630=B_SPLINE_CURVE_WITH_KNOTS('',3,(#122694,#122695,#122696,#122697,#122698,
#122699,#122700,#122701,#122702,#122703,#122704,#122705,#122706,#122707,
#122708,#122709,#122710,#122711,#122712,#122713,#122714,#122715,#122716,
#122717,#122718,#122719,#122720,#122721,#122722,#122723,#122724,#122725,
#122726,#122727,#122728,#122729,#122730,#122731,#122732,#122733,#122734,
#122735,#122736,#122737,#122738,#122739,#122740,#122741,#122742,#122743,
#122744,#122745,#122746,#122747,#122748,#122749,#122750,#122751,#122752,
#122753,#122754,#122755,#122756,#122757,#122758,#122759,#122760,#122761,
#122762,#122763,#122764,#122765,#122766,#122767,#122768,#122769,#122770,
#122771,#122772,#122773,#122774,#122775,#122776,#122777,#122778,#122779,
#122780,#122781,#122782,#122783,#122784,#122785,#122786,#122787,#122788,
#122789,#122790,#122791,#122792,#122793,#122794,#122795,#122796,#122797,
#122798,#122799,#122800,#122801,#122802,#122803,#122804,#122805,#122806,
#122807,#122808,#122809,#122810,#122811,#122812,#122813,#122814,#122815,
#122816,#122817,#122818,#122819,#122820,#122821,#122822,#122823,#122824,
#122825,#122826,#122827,#122828,#122829,#122830,#122831,#122832,#122833,
#122834,#122835,#122836,#122837,#122838,#122839,#122840,#122841,#122842,
#122843,#122844,#122845,#122846,#122847,#122848,#122849,#122850,#122851,
#122852,#122853,#122854,#122855,#122856,#122857,#122858,#122859,#122860,
#122861,#122862,#122863,#122864,#122865,#122866,#122867,#122868,#122869,
#122870,#122871,#122872,#122873,#122874,#122875,#122876,#122877,#122878,
#122879,#122880,#122881,#122882,#122883,#122884,#122885,#122886,#122887,
#122888,#122889,#122890,#122891,#122892,#122893,#122894,#122895,#122896,
#122897,#122898,#122899,#122900,#122901,#122902,#122903,#122904,#122905),
 .UNSPECIFIED.,.F.,.F.,(4,2,2,2,2,2,2,2,2,2,2,2,2,2,2,2,2,2,2,2,2,2,2,2,
2,2,2,2,2,2,2,2,2,2,2,2,2,2,2,2,2,2,2,2,2,2,2,2,2,2,2,2,2,2,2,2,2,2,2,2,
2,2,2,2,2,2,2,2,2,2,2,2,2,2,2,2,2,2,2,2,2,2,2,2,2,2,2,2,2,2,2,2,2,2,2,2,
2,2,2,2,2,2,2,2,2,4),(-2.02096473940897,-2.0207001392651,-2.01966945009549,
-2.01842486118067,-2.0152685424195,-1.99515219974244,-1.97126241300299,
-1.96583507629916,-1.96340398073594,-1.96156911882332,-1.95958912000209,
-1.95642013419931,-1.94617045210257,-1.92235583906836,-1.9214297946144,
-1.9117088824231,-1.90801016868078,-1.90527499978267,-1.90397068781599,
-1.9029519058378,-1.90173700694308,-1.89951292524769,-1.88642369092045,
-1.88055889265947,-1.86547088755815,-1.85081923536881,-1.84741228612423,
-1.84538070415464,-1.84355954433598,-1.84123332963993,-1.8363835113232,
-1.81566520436901,-1.79745118092209,-1.79212206588293,-1.7885204839487,
-1.78706477697706,-1.7860270171828,-1.78489756770433,-1.78300439878093,
-1.7763360747173,-1.7697705313992,-1.75234065077155,-1.73415217818814,-1.73052424934472,
-1.72842395480023,-1.72661155391675,-1.7243878154464,-1.7200647842999,-1.69003315527847,
-1.67298354502583,-1.67091102683763,-1.66961996453208,-1.66860183748791,
-1.66737604028128,-1.66503484169274,-1.662010158347,-1.62914395437748,-1.6164212327105,
-1.61302751305175,-1.61099881182171,-1.60917710618397,-1.60684586582125,
-1.60196922788607,-1.59548303547423,-1.57791396803449,-1.55707633338049,
-1.55395031816943,-1.55258893341696,-1.55156188425926,-1.55039951748663,
-1.54835615770544,-1.53854999290055,-1.52414341589642,-1.50169758667576,
-1.49686240702736,-1.49453897672409,-1.49271814459168,-1.49068501187754,
-1.48727083626137,-1.47249854911327,-1.45748153307026,-1.45106850387174,
-1.43857029121308,-1.43653712334913,-1.43525790644315,-1.43424036755935,
-1.43300464325958,-1.43061497350352,-1.42750950428366,-1.42007225407143,
-1.40426248153534,-1.38269506585492,-1.37903197992924,-1.37692384113659,
-1.37511200629303,-1.37289820000553,-1.36862431350211,-1.34699163713018,
-1.32238427279142,-1.31951282693004,-1.31819688750572,-1.31717529623337,
-1.31598471622319,-1.3138105949162,-1.30098464557554,-1.27924578165543),
 .UNSPECIFIED.);
#1631=B_SPLINE_CURVE_WITH_KNOTS('',3,(#122906,#122907,#122908,#122909,#122910,
#122911,#122912,#122913,#122914,#122915,#122916,#122917,#122918,#122919,
#122920,#122921,#122922,#122923,#122924,#122925,#122926,#122927,#122928,
#122929,#122930,#122931,#122932,#122933,#122934,#122935,#122936,#122937,
#122938,#122939,#122940,#122941,#122942,#122943,#122944,#122945,#122946,
#122947,#122948,#122949,#122950,#122951,#122952,#122953,#122954,#122955,
#122956,#122957,#122958,#122959,#122960,#122961,#122962,#122963,#122964,
#122965,#122966,#122967,#122968,#122969,#122970,#122971,#122972,#122973,
#122974,#122975,#122976,#122977,#122978,#122979,#122980,#122981,#122982,
#122983,#122984,#122985,#122986,#122987,#122988,#122989,#122990,#122991,
#122992,#122993,#122994,#122995,#122996,#122997,#122998,#122999,#123000,
#123001,#123002,#123003,#123004,#123005,#123006,#123007,#123008,#123009,
#123010,#123011,#123012,#123013,#123014,#123015,#123016,#123017,#123018,
#123019,#123020,#123021,#123022,#123023,#123024,#123025,#123026,#123027,
#123028,#123029,#123030,#123031,#123032,#123033,#123034,#123035,#123036,
#123037,#123038,#123039,#123040,#123041,#123042,#123043,#123044,#123045,
#123046,#123047,#123048,#123049,#123050,#123051,#123052,#123053,#123054,
#123055,#123056,#123057,#123058,#123059,#123060,#123061,#123062,#123063,
#123064,#123065,#123066,#123067,#123068,#123069,#123070,#123071,#123072,
#123073,#123074,#123075,#123076,#123077,#123078,#123079,#123080,#123081,
#123082,#123083,#123084,#123085,#123086,#123087,#123088,#123089,#123090,
#123091,#123092,#123093,#123094,#123095,#123096,#123097,#123098,#123099,
#123100,#123101,#123102,#123103,#123104,#123105,#123106,#123107,#123108,
#123109,#123110,#123111,#123112,#123113,#123114,#123115,#123116,#123117),
 .UNSPECIFIED.,.F.,.F.,(4,2,2,2,2,2,2,2,2,2,2,2,2,2,2,2,2,2,2,2,2,2,2,2,
2,2,2,2,2,2,2,2,2,2,2,2,2,2,2,2,2,2,2,2,2,2,2,2,2,2,2,2,2,2,2,2,2,2,2,2,
2,2,2,2,2,2,2,2,2,2,2,2,2,2,2,2,2,2,2,2,2,2,2,2,2,2,2,2,2,2,2,2,2,2,2,2,
2,2,2,2,2,2,2,2,2,4),(-0.946673080131941,-0.935626006097239,-0.930823601939602,
-0.928506193560378,-0.92668583442944,-0.924648829194281,-0.921217475209467,
-0.906153837844209,-0.891343295666385,-0.884392217971758,-0.87247788876375,
-0.870277544085949,-0.869067839219171,-0.868048471210341,-0.866737101317524,
-0.863965411416058,-0.860202762729112,-0.850217585935452,-0.827024272926127,
-0.815840526288103,-0.81255738436404,-0.810552505904783,-0.80872498722333,
-0.806347692829656,-0.801222818589417,-0.794300799206035,-0.758401741841977,
-0.754063973351398,-0.752451587588511,-0.751489408091924,-0.750431919954055,
-0.748871715256692,-0.744566193094111,-0.737748837531389,-0.713139203061365,
-0.698961982861916,-0.695474001672571,-0.693424537578214,-0.691787821654563,
-0.689578597318098,-0.685329515246036,-0.679903059085688,-0.666860115880548,
-0.648434847417636,-0.637906155227199,-0.635763822650013,-0.634566956589963,
-0.633545930416142,-0.632216197126501,-0.629347641449624,-0.617202843921097,
-0.588483038482858,-0.580546844005023,-0.577653746245591,-0.575924255590045,
-0.574084246106177,-0.571621989604517,-0.566017280792925,-0.551719748590105,
-0.528867530047163,-0.520442056219144,-0.518425922436248,-0.517257660152455,
-0.516231646089653,-0.514856058674415,-0.511734291946429,-0.497205469745065,
-0.471529893004746,-0.463380141304061,-0.460457723407912,-0.458722682847371,
-0.456885568607325,-0.454442313596543,-0.448947912763836,-0.425437939714836,
-0.404965998159196,-0.402126943930736,-0.400621421142603,-0.399584912143404,
-0.398476579557482,-0.396680093219113,-0.390303479771554,-0.377993408307067,
-0.348839715601933,-0.344866157587136,-0.342498903767759,-0.340666992245494,
-0.338676086111014,-0.33545829751017,-0.323532117757917,-0.29712737881507,
-0.286210775684609,-0.28405125746133,-0.282850529357465,-0.281829973841278,
-0.280505733202747,-0.277666635066594,-0.265779840422882,-0.238163707008377,
-0.229121938702919,-0.226088026588155,-0.224136694904447,-0.222289224506927,
-0.219780937754473,-0.213902979691889,-0.204532409010266),.UNSPECIFIED.);
#1632=B_SPLINE_CURVE_WITH_KNOTS('',3,(#123122,#123123,#123124,#123125,#123126,
#123127,#123128,#123129,#123130,#123131,#123132,#123133,#123134,#123135,
#123136,#123137,#123138,#123139,#123140,#123141,#123142,#123143,#123144,
#123145,#123146,#123147,#123148,#123149,#123150,#123151,#123152,#123153,
#123154,#123155,#123156,#123157,#123158,#123159,#123160,#123161,#123162,
#123163,#123164,#123165,#123166,#123167,#123168,#123169,#123170,#123171,
#123172,#123173,#123174,#123175,#123176,#123177,#123178,#123179,#123180,
#123181,#123182,#123183,#123184,#123185,#123186,#123187,#123188,#123189,
#123190,#123191,#123192,#123193,#123194,#123195,#123196,#123197,#123198,
#123199,#123200,#123201,#123202,#123203,#123204,#123205,#123206,#123207,
#123208,#123209,#123210,#123211,#123212,#123213,#123214,#123215,#123216,
#123217,#123218,#123219,#123220,#123221,#123222,#123223,#123224,#123225,
#123226,#123227,#123228,#123229,#123230,#123231,#123232,#123233,#123234,
#123235,#123236,#123237,#123238,#123239,#123240,#123241,#123242,#123243,
#123244,#123245,#123246,#123247,#123248,#123249,#123250,#123251,#123252,
#123253,#123254,#123255,#123256,#123257,#123258,#123259,#123260,#123261,
#123262,#123263,#123264,#123265,#123266,#123267,#123268,#123269,#123270,
#123271,#123272,#123273,#123274,#123275,#123276,#123277,#123278,#123279,
#123280,#123281,#123282,#123283,#123284,#123285,#123286,#123287,#123288,
#123289,#123290,#123291,#123292,#123293,#123294,#123295,#123296,#123297,
#123298,#123299,#123300,#123301,#123302,#123303,#123304,#123305,#123306,
#123307,#123308,#123309,#123310,#123311,#123312,#123313,#123314,#123315,
#123316,#123317,#123318,#123319,#123320,#123321,#123322,#123323),
 .UNSPECIFIED.,.F.,.F.,(4,2,2,2,2,2,2,2,2,2,2,2,2,2,2,2,2,2,2,2,2,2,2,2,
2,2,2,2,2,2,2,2,2,2,2,2,2,2,2,2,2,2,2,2,2,2,2,2,2,2,2,2,2,2,2,2,2,2,2,2,
2,2,2,2,2,2,2,2,2,2,2,2,2,2,2,2,2,2,2,2,2,2,2,2,2,2,2,2,2,2,2,2,2,2,2,2,
2,2,2,2,4),(-2.7627136742397,-2.74760750538693,-2.72756916375101,-2.72523029199539,
-2.72400534826976,-2.72298773880131,-2.72169711456732,-2.71962489439385,
-2.70247686396111,-2.68193471826147,-2.6705609044919,-2.66739090472042,
-2.66541122098641,-2.66357729275388,-2.66118988637063,-2.65585952912302,
-2.61797084562576,-2.61242594454177,-2.60871789594637,-2.60724566909461,
-2.6062052368122,-2.60508256720467,-2.60321981134333,-2.59686203922748,
-2.56610720588711,-2.5577716816043,-2.55188012910689,-2.54937023693817,
-2.54752306269227,-2.54580703469866,-2.54298381485341,-2.53554142777646,
-2.50274358845909,-2.49271029691211,-2.49065471525136,-2.48948967859719,
-2.48846329009461,-2.48710664973158,-2.48400758364922,-2.46256886503251,
-2.44542381011884,-2.43902701285583,-2.43420159701271,-2.43188008523737,
-2.43005954725324,-2.42802549060667,-2.42460672876648,-2.41147393581952,
-2.38487628181305,-2.37856780832695,-2.37449526167128,-2.37296821996719,
-2.37191751645818,-2.37081362773828,-2.36903625070745,-2.36345865803876,
-2.32904303053547,-2.32220734697397,-2.31713105174476,-2.31476298711301,
-2.31293702456317,-2.31092830502834,-2.30762602542793,-2.29596060092727,
-2.27333996513071,-2.26331827752009,-2.25954740692162,-2.25677148058451,
-2.25545948817148,-2.25444959454968,-2.25324483074787,-2.2510659748943,
-2.23965723364532,-2.21858202528268,-2.20244174064115,-2.1989542064734,
-2.19690535746983,-2.19508749950381,-2.19279098579296,-2.18809645651082,
-2.16179099851405,-2.14772072408464,-2.14081765617953,-2.13897415466464,
-2.13785571521514,-2.1368249113606,-2.13557965889867,-2.13241884878729,
-2.11261622874445,-2.10134724215732,-2.08528250050539,-2.08179858226312,
-2.07975044500786,-2.07793236112261,-2.0756344057589,-2.07093275342417,
-2.0447267828665,-2.0305871921962,-2.023664271598,-2.02181900182672,-2.02096473940897),
 .UNSPECIFIED.);
#1633=B_SPLINE_CURVE_WITH_KNOTS('',3,(#123325,#123326,#123327,#123328,#123329,
#123330,#123331,#123332,#123333,#123334,#123335,#123336,#123337,#123338,
#123339,#123340,#123341,#123342,#123343,#123344,#123345,#123346,#123347,
#123348,#123349,#123350,#123351,#123352,#123353,#123354,#123355,#123356,
#123357,#123358,#123359,#123360,#123361,#123362,#123363,#123364,#123365,
#123366,#123367,#123368,#123369,#123370,#123371,#123372,#123373,#123374,
#123375,#123376,#123377,#123378,#123379,#123380,#123381,#123382,#123383,
#123384,#123385,#123386,#123387,#123388,#123389,#123390,#123391,#123392),
 .UNSPECIFIED.,.F.,.F.,(4,2,2,2,2,2,2,2,2,2,2,2,2,2,2,2,2,2,2,2,2,2,2,2,
2,2,2,2,2,2,2,2,2,4),(-0.204532409010266,-0.194924932902125,-0.171058061330753,
-0.167580129499482,-0.166245255876008,-0.165285928558312,-0.164225470541549,
-0.162650657065151,-0.158238086983778,-0.125426654891204,-0.112590818373553,
-0.109184993804583,-0.10715335998345,-0.105414591283973,-0.105351688545113,
-0.105292623790695,-0.105236888767858,-0.105184055192759,-0.105133758874891,
-0.105085687463357,-0.102894543815645,-0.100315808264756,-0.0959954645696802,
-0.0867881052724889,-0.0710444130250007,-0.053306962456332,-0.050147685259005,
-0.0488816456134193,-0.0478455880490776,-0.0467366517880079,-0.044937191567511,
-0.0385279941781553,-0.0261139800210841,-1.0000001292032E-6),
 .UNSPECIFIED.);
#1634=B_SPLINE_CURVE_WITH_KNOTS('',3,(#123393,#123394,#123395,#123396,#123397,
#123398,#123399,#123400,#123401,#123402,#123403,#123404,#123405,#123406,
#123407,#123408,#123409,#123410,#123411,#123412,#123413,#123414,#123415,
#123416,#123417,#123418,#123419,#123420,#123421,#123422,#123423,#123424,
#123425,#123426,#123427,#123428,#123429,#123430,#123431,#123432,#123433,
#123434,#123435,#123436,#123437,#123438,#123439,#123440,#123441,#123442,
#123443,#123444,#123445,#123446,#123447,#123448,#123449,#123450,#123451,
#123452,#123453,#123454,#123455,#123456,#123457,#123458,#123459,#123460,
#123461,#123462,#123463,#123464,#123465,#123466,#123467,#123468,#123469,
#123470,#123471,#123472,#123473,#123474,#123475,#123476,#123477,#123478,
#123479,#123480,#123481,#123482,#123483,#123484,#123485,#123486,#123487,
#123488,#123489,#123490,#123491,#123492,#123493,#123494,#123495,#123496,
#123497,#123498,#123499,#123500,#123501,#123502,#123503,#123504,#123505,
#123506,#123507,#123508,#123509,#123510,#123511,#123512,#123513,#123514,
#123515,#123516,#123517,#123518,#123519,#123520,#123521,#123522,#123523,
#123524,#123525,#123526,#123527,#123528,#123529,#123530,#123531,#123532,
#123533,#123534,#123535,#123536,#123537,#123538,#123539,#123540,#123541,
#123542,#123543,#123544,#123545,#123546,#123547,#123548,#123549,#123550,
#123551,#123552,#123553,#123554,#123555,#123556,#123557,#123558),
 .UNSPECIFIED.,.F.,.F.,(4,2,2,2,2,2,2,2,2,2,2,2,2,2,2,2,2,2,2,2,2,2,2,2,
2,2,2,2,2,2,2,2,2,2,2,2,2,2,2,2,2,2,2,2,2,2,2,2,2,2,2,2,2,2,2,2,2,2,2,2,
2,2,2,2,2,2,2,2,2,2,2,2,2,2,2,2,2,2,2,2,2,2,4),(-1.81503280713751,-1.81069981961972,
-1.80759276479933,-1.80580583034795,-1.80406479795658,-1.80209824698256,
-1.79898871711039,-1.78926359027205,-1.76295057239896,-1.75068537642654,
-1.74780444958829,-1.74647302196291,-1.74546171232084,-1.74427142252917,
-1.74215590334836,-1.73200843122411,-1.71333810717845,-1.70021960555422,
-1.69477478505897,-1.69175866186095,-1.68971040142769,-1.6877555233977,
-1.68602911904562,-1.68370725577307,-1.67887703274963,-1.65855113979732,
-1.64110174187218,-1.63506485100915,-1.63111999738201,-1.62961202629393,
-1.6285652877668,-1.6274559475313,-1.62565240929404,-1.61984272044714,-1.58568991710473,
-1.57887130130342,-1.5738051126339,-1.57143952335733,-1.56961455121706,
-1.56760600912896,-1.5643019264818,-1.55286714756856,-1.52980751085361,
-1.51993809569984,-1.51620413605914,-1.51344930902468,-1.5121416681231,
-1.51122015751256,-1.51004910805787,-1.50801819129573,-1.49933752343943,
-1.47962099595857,-1.46612766114278,-1.45786695651096,-1.4550191289998,
-1.45310805176318,-1.4512601882012,-1.44863828804738,-1.44250965410269,
-1.41489418244456,-1.41178533340499,-1.40252842423068,-1.39894431739321,
-1.39627479936842,-1.3949835313354,-1.39406385318909,-1.39288160338511,
-1.39080144874296,-1.38132764517926,-1.3808517104182,-1.35760121078074,
-1.34195867604981,-1.33849763362988,-1.33645508445692,-1.3346371710014,
-1.33233294992883,-1.32759494175085,-1.30204640962113,-1.28746206108587,
-1.28273540121226,-1.27944140541104,-1.27803671668043,-1.27782408552841),
 .UNSPECIFIED.);
#1635=B_SPLINE_CURVE_WITH_KNOTS('',3,(#123563,#123564,#123565,#123566,#123567,
#123568,#123569,#123570,#123571,#123572,#123573,#123574,#123575,#123576,
#123577,#123578,#123579,#123580,#123581,#123582,#123583,#123584,#123585,
#123586,#123587,#123588,#123589,#123590,#123591,#123592,#123593,#123594,
#123595,#123596,#123597,#123598,#123599,#123600,#123601,#123602,#123603,
#123604,#123605,#123606,#123607,#123608,#123609,#123610,#123611,#123612,
#123613,#123614,#123615,#123616,#123617,#123618,#123619,#123620,#123621,
#123622,#123623,#123624,#123625,#123626,#123627,#123628,#123629,#123630,
#123631,#123632,#123633,#123634,#123635,#123636,#123637,#123638,#123639,
#123640,#123641,#123642,#123643,#123644,#123645,#123646,#123647,#123648,
#123649,#123650,#123651,#123652,#123653,#123654,#123655,#123656,#123657,
#123658,#123659,#123660,#123661,#123662,#123663,#123664,#123665,#123666,
#123667,#123668,#123669,#123670,#123671,#123672,#123673,#123674,#123675,
#123676,#123677,#123678,#123679,#123680,#123681,#123682,#123683,#123684,
#123685,#123686,#123687,#123688,#123689,#123690,#123691,#123692,#123693,
#123694,#123695,#123696,#123697,#123698,#123699,#123700,#123701,#123702,
#123703,#123704,#123705,#123706,#123707,#123708,#123709,#123710,#123711,
#123712,#123713,#123714,#123715,#123716,#123717,#123718,#123719,#123720,
#123721,#123722,#123723,#123724,#123725,#123726,#123727,#123728,#123729,
#123730,#123731,#123732,#123733,#123734,#123735,#123736,#123737,#123738,
#123739,#123740,#123741,#123742,#123743,#123744,#123745,#123746,#123747,
#123748,#123749,#123750,#123751,#123752,#123753,#123754,#123755,#123756,
#123757,#123758,#123759,#123760,#123761,#123762,#123763,#123764,#123765,
#123766,#123767,#123768,#123769,#123770,#123771,#123772,#123773,#123774,
#123775,#123776,#123777,#123778),.UNSPECIFIED.,.F.,.F.,(4,2,2,2,2,2,2,2,
2,2,2,2,2,2,2,2,2,2,2,2,2,2,2,2,2,2,2,2,2,2,2,2,2,2,2,2,2,2,2,2,2,2,2,2,
2,2,2,2,2,2,2,2,2,2,2,2,2,2,2,2,2,2,2,2,2,2,2,2,2,2,2,2,2,2,2,2,2,2,2,2,
2,2,2,2,2,2,2,2,2,2,2,2,2,2,2,2,2,2,2,2,2,2,2,2,2,2,2,4),(-3.50413679931849,
-3.49590987031219,-3.49100908839452,-3.48860580968547,-3.48679049718976,
-3.48505425934406,-3.48333887870094,-3.48100178508058,-3.47507574420192,
-3.46212039058586,-3.4369866640505,-3.4320360545749,-3.42862446149258,-3.42719904529355,
-3.42616712469117,-3.42503194270083,-3.42309244796776,-3.4158099622432,
-3.39508062099519,-3.38118444829873,-3.37554950017391,-3.37246772029541,
-3.36978904110003,-3.36793947953406,-3.36609627761575,-3.36344886980306,
-3.35706623725807,-3.32956258591042,-3.32661252784782,-3.31400625547146,
-3.31109577402588,-3.30976516605439,-3.30875766895029,-3.30757401278248,
-3.30548940801067,-3.29594876245353,-3.27683265978024,-3.26354729792033,
-3.2580546351264,-3.25376292148752,-3.25154251098197,-3.24972643626906,
-3.24761455977581,-3.24394754645604,-3.22281910613394,-3.20751639591832,
-3.19579692305258,-3.19365860294311,-3.19247285593897,-3.1914475180448,
-3.19011509057152,-3.18715699906652,-3.16344576325454,-3.14112639399976,
-3.13685335263498,-3.13463966382662,-3.13282773953272,-3.1307192775451,
-3.12705507922154,-3.10538545893922,-3.0894919765626,-3.07857452758075,
-3.07647644664878,-3.07530268378633,-3.07427947089646,-3.07294077941223,
-3.06993792494916,-3.04689019301246,-3.02631410306661,-3.02047959131481,
-3.01798093165929,-3.01613735335176,-3.01418722248511,-3.01114920317816,
-3.00204915819561,-2.9744754598127,-2.9626146412364,-2.95978073152702,-2.95845876314082,
-2.95743945954545,-2.95623932141187,-2.9540808568736,-2.94316287873158,
-2.90954003559155,-2.90341166898242,-2.90086310015065,-2.89900915166713,
-2.89730192170372,-2.89452753337548,-2.88741260709016,-2.86079519058316,
-2.85865434170654,-2.84532430335765,-2.84259059757052,-2.84128636783062,
-2.84026753860776,-2.83905249035476,-2.83682697913635,-2.82389353315059,
-2.81855228183661,-2.80449603841603,-2.78831602751527,-2.78482726838424,
-2.78277849255522,-2.78096118025786,-2.77866600531978,-2.77397657432156,
-2.7627136742397),.UNSPECIFIED.);
#1636=B_SPLINE_CURVE_WITH_KNOTS('',3,(#123779,#123780,#123781,#123782,#123783,
#123784,#123785,#123786,#123787,#123788,#123789,#123790,#123791,#123792,
#123793,#123794,#123795,#123796,#123797,#123798,#123799,#123800,#123801,
#123802,#123803,#123804,#123805,#123806,#123807,#123808,#123809,#123810,
#123811,#123812,#123813,#123814,#123815,#123816,#123817,#123818,#123819,
#123820,#123821,#123822,#123823,#123824,#123825,#123826,#123827,#123828,
#123829,#123830,#123831,#123832,#123833,#123834,#123835,#123836,#123837,
#123838,#123839,#123840,#123841,#123842,#123843,#123844,#123845,#123846,
#123847,#123848,#123849,#123850,#123851,#123852,#123853,#123854,#123855,
#123856,#123857,#123858,#123859,#123860,#123861,#123862,#123863,#123864,
#123865,#123866,#123867,#123868,#123869,#123870,#123871,#123872,#123873,
#123874,#123875,#123876,#123877,#123878,#123879,#123880,#123881,#123882,
#123883,#123884,#123885,#123886,#123887,#123888,#123889,#123890,#123891,
#123892,#123893,#123894,#123895,#123896,#123897,#123898,#123899,#123900,
#123901,#123902,#123903,#123904,#123905,#123906,#123907,#123908,#123909,
#123910,#123911,#123912,#123913,#123914,#123915,#123916,#123917,#123918,
#123919,#123920,#123921,#123922,#123923,#123924,#123925,#123926,#123927,
#123928,#123929,#123930,#123931,#123932,#123933,#123934,#123935,#123936,
#123937,#123938,#123939,#123940,#123941,#123942,#123943,#123944,#123945,
#123946,#123947,#123948,#123949,#123950,#123951,#123952,#123953,#123954,
#123955,#123956,#123957,#123958,#123959,#123960,#123961,#123962,#123963,
#123964,#123965,#123966,#123967,#123968,#123969,#123970,#123971,#123972,
#123973,#123974,#123975,#123976,#123977,#123978,#123979,#123980),
 .UNSPECIFIED.,.F.,.F.,(4,2,2,2,2,2,2,2,2,2,2,2,2,2,2,2,2,2,2,2,2,2,2,2,
2,2,2,2,2,2,2,2,2,2,2,2,2,2,2,2,2,2,2,2,2,2,2,2,2,2,2,2,2,2,2,2,2,2,2,2,
2,2,2,2,2,2,2,2,2,2,2,2,2,2,2,2,2,2,2,2,2,2,2,2,2,2,2,2,2,2,2,2,2,2,2,2,
2,2,2,2,4),(-1.27782408552841,-1.27700744843732,-1.27585611518679,-1.27386152192946,
-1.26604387234503,-1.24155901253228,-1.22490854839876,-1.22139758046917,
-1.21934425388906,-1.21752803589453,-1.21524113476472,-1.21059333879667,
-1.18369148601385,-1.17001696913576,-1.1632285724226,-1.16139555307866,
-1.16027972848832,-1.15924827904952,-1.15799920069739,-1.15481245546084,
-1.13590214908377,-1.12404871419593,-1.10774680020317,-1.10425208402406,
-1.10220208188184,-1.10038506410701,-1.09809212763459,-1.09356964927776,
-1.06591623509627,-1.05271418884702,-1.04606509809328,-1.04424434984758,
-1.04313117127479,-1.04209849058864,-1.04084400231322,-1.03775008283869,
-1.01709280661423,-0.999424224147688,-0.992918543041473,-0.988030755869076,
-0.985698179287253,-0.983877162069481,-0.981851020003204,-0.978465928688977,
-0.965862976968039,-0.932911646393505,-0.929852129901944,-0.927490350469066,
-0.926260650127288,-0.925243244661346,-0.923958165246924,-0.921904712265766,
-0.907573653906144,-0.884583599093049,-0.873034819418677,-0.869732134957923,
-0.867723486857646,-0.865897800961454,-0.863530408941509,-0.858456908094493,
-0.851625094044048,-0.817300255843636,-0.811620743739196,-0.80983140096965,
-0.808724822179306,-0.807675113362555,-0.806155258474049,-0.802135746087605,
-0.775504484471682,-0.756552995034251,-0.75291093240851,-0.750807102714669,
-0.748994375106247,-0.746773669450533,-0.742467656594624,-0.727214627360076,
-0.703302196578544,-0.694910798872665,-0.692897308279438,-0.691729816029914,
-0.690704786917919,-0.689330380182545,-0.686208874600118,-0.671665160824926,
-0.645948757699798,-0.637840731634461,-0.63492588503852,-0.63319383827778,
-0.631358821769959,-0.628916565289571,-0.623416864518652,-0.59868497174726,
-0.579511699625379,-0.576640082361904,-0.57512701986566,-0.574089986632705,
-0.572985554076917,-0.57120470940897,-0.564984759893283,-0.553162204596557,
-0.536047533639214),.UNSPECIFIED.);
#1637=B_SPLINE_CURVE_WITH_KNOTS('',3,(#123983,#123984,#123985,#123986,#123987,
#123988,#123989,#123990,#123991,#123992,#123993,#123994,#123995,#123996,
#123997,#123998,#123999,#124000,#124001,#124002,#124003,#124004,#124005,
#124006,#124007,#124008,#124009,#124010,#124011,#124012,#124013,#124014,
#124015,#124016,#124017,#124018,#124019,#124020,#124021,#124022,#124023,
#124024,#124025,#124026,#124027,#124028,#124029,#124030,#124031,#124032,
#124033,#124034,#124035,#124036,#124037,#124038,#124039,#124040,#124041,
#124042,#124043,#124044,#124045,#124046,#124047,#124048,#124049,#124050,
#124051,#124052,#124053,#124054,#124055,#124056,#124057,#124058,#124059,
#124060,#124061,#124062,#124063,#124064,#124065,#124066,#124067,#124068,
#124069,#124070,#124071,#124072,#124073,#124074,#124075,#124076,#124077,
#124078,#124079,#124080,#124081,#124082,#124083,#124084,#124085,#124086,
#124087,#124088,#124089,#124090,#124091,#124092,#124093,#124094,#124095,
#124096,#124097,#124098,#124099,#124100,#124101,#124102,#124103,#124104,
#124105,#124106,#124107,#124108,#124109,#124110,#124111,#124112,#124113,
#124114,#124115,#124116,#124117,#124118,#124119,#124120,#124121,#124122,
#124123,#124124,#124125,#124126,#124127,#124128,#124129,#124130,#124131,
#124132,#124133,#124134,#124135,#124136,#124137,#124138,#124139,#124140,
#124141,#124142,#124143,#124144,#124145,#124146,#124147,#124148,#124149,
#124150,#124151,#124152,#124153,#124154,#124155,#124156,#124157,#124158,
#124159,#124160,#124161,#124162,#124163,#124164,#124165,#124166,#124167,
#124168,#124169,#124170,#124171,#124172),.UNSPECIFIED.,.F.,.F.,(4,2,2,2,
2,2,2,2,2,2,2,2,2,2,2,2,2,2,2,2,2,2,2,2,2,2,2,2,2,2,2,2,2,2,2,2,2,2,2,2,
2,2,2,2,2,2,2,2,2,2,2,2,2,2,2,2,2,2,2,2,2,2,2,2,2,2,2,2,2,2,2,2,2,2,2,2,
2,2,2,2,2,2,2,2,2,2,2,2,2,2,2,2,2,2,4),(-0.536047533639214,-0.52399885171329,
-0.5191418345236,-0.51681386044327,-0.51499206653414,-0.512960546072856,
-0.50955554956382,-0.494947057225457,-0.479827449156403,-0.474042924106341,
-0.460859879018046,-0.458631996800147,-0.457415386092451,-0.456393388474596,
-0.455083034564835,-0.452333245550669,-0.44861226264521,-0.438808977029807,
-0.415787915339652,-0.404424222966805,-0.401120959226698,-0.399108661379668,
-0.397277386413001,-0.394899360003346,-0.389788857269007,-0.382897753187339,
-0.347709148442755,-0.342751932427427,-0.341051268531925,-0.340071816487764,
-0.339035557306534,-0.337562497544506,-0.333805206831877,-0.32815082965446,
-0.307574270578932,-0.287646486813658,-0.284003445079414,-0.281908596678359,
-0.280109547254434,-0.277913384027072,-0.273681342470775,-0.268273073581708,
-0.255264360341712,-0.23694535907824,-0.226252973921614,-0.22411121235287,
-0.222918799531449,-0.221909562376785,-0.220589323919137,-0.21777493670625,
-0.213938499391572,-0.203655402571684,-0.180162614763938,-0.169322462829239,
-0.166079711731662,-0.164077142773677,-0.162236891490299,-0.159821276372025,
-0.154522453365636,-0.147292561345917,-0.125699525127139,-0.109176941674625,
-0.106895801112883,-0.105660587506475,-0.104645952324828,-0.104633561435904,
-0.104621312149598,-0.104609199094343,-0.104597217086387,-0.104585361125445,
-0.104573626424971,-0.104562008308446,-0.104550502282346,-0.104539104016455,
-0.104527809305687,-0.104516614067934,-0.104505514375394,-0.104494506409772,
-0.104483586458463,-0.104472750918138,-0.10446199632122,-0.104451319278702,
-0.103118243704271,-0.101561016763444,-0.098876620287455,-0.0929360043824338,
-0.0760446284376168,-0.0563580902694081,-0.0515877124908065,-0.0492537501845121,
-0.0474046239728219,-0.0453179671092674,-0.0417576343573112,-0.0249627090523748,
-9.99999997475243E-7),.UNSPECIFIED.);
#1638=B_SPLINE_CURVE_WITH_KNOTS('',3,(#124176,#124177,#124178,#124179,#124180,
#124181,#124182,#124183,#124184,#124185,#124186,#124187,#124188,#124189,
#124190,#124191,#124192,#124193,#124194,#124195,#124196,#124197,#124198,
#124199,#124200,#124201,#124202,#124203,#124204,#124205,#124206,#124207,
#124208,#124209,#124210,#124211,#124212,#124213,#124214,#124215,#124216,
#124217,#124218,#124219,#124220,#124221,#124222,#124223,#124224,#124225,
#124226,#124227,#124228,#124229,#124230,#124231,#124232,#124233),
 .UNSPECIFIED.,.F.,.F.,(4,2,2,2,2,2,2,2,2,2,2,2,2,2,2,2,2,2,2,2,2,2,2,2,
2,2,2,2,4),(5.15211709134537E-5,0.00655144725415278,0.00869323351133672,
0.0103519278912827,0.0119948184923338,0.0138623089950716,0.0168900595936218,
0.0269226222271582,0.0455925782724488,0.0661451986302976,0.0683674394977015,
0.0695297613193126,0.0705349598656515,0.0718094328174083,0.0738312522614602,
0.085736896500158,0.0932115525345353,0.111958373848329,0.127062062352944,
0.130865085822168,0.133119269195534,0.134933720040114,0.137408194121271,
0.142294210116158,0.162787875320058,0.181511848037067,0.184359249810965,
0.185542544508814,0.186520187542269),.UNSPECIFIED.);
#1639=B_SPLINE_CURVE_WITH_KNOTS('',3,(#124234,#124235,#124236,#124237,#124238,
#124239,#124240,#124241,#124242,#124243,#124244,#124245,#124246,#124247,
#124248,#124249,#124250,#124251,#124252,#124253,#124254,#124255,#124256,
#124257,#124258,#124259,#124260,#124261,#124262,#124263,#124264,#124265,
#124266,#124267,#124268,#124269,#124270,#124271,#124272,#124273,#124274,
#124275,#124276,#124277,#124278,#124279,#124280,#124281,#124282,#124283,
#124284,#124285,#124286,#124287,#124288,#124289,#124290,#124291,#124292,
#124293,#124294,#124295,#124296,#124297,#124298,#124299,#124300),
 .UNSPECIFIED.,.F.,.F.,(4,3,3,3,3,3,3,3,3,3,3,3,3,3,3,3,3,3,3,3,3,3,4),
(127.073099465779,127.192848546177,127.312825622574,127.406393326248,127.406438144991,
127.517358027634,127.530505230398,127.650260561131,127.769899548496,127.889474529566,
128.009037730339,128.128722920694,128.248481837206,128.358789105211,128.368455012374,
128.398921923044,128.398974828247,128.513022470957,128.530246689258,128.653089710286,
128.66777274281,128.79787167666,128.805298587658),.UNSPECIFIED.);
#1640=B_SPLINE_CURVE_WITH_KNOTS('',3,(#124303,#124304,#124305,#124306,#124307,
#124308,#124309,#124310,#124311,#124312,#124313,#124314,#124315,#124316,
#124317,#124318,#124319,#124320,#124321,#124322,#124323,#124324,#124325,
#124326,#124327,#124328,#124329,#124330,#124331,#124332,#124333,#124334,
#124335,#124336,#124337,#124338,#124339,#124340,#124341,#124342,#124343,
#124344,#124345,#124346,#124347,#124348,#124349,#124350,#124351,#124352,
#124353,#124354,#124355,#124356,#124357,#124358,#124359,#124360,#124361,
#124362,#124363,#124364,#124365,#124366,#124367,#124368,#124369,#124370,
#124371,#124372,#124373,#124374,#124375,#124376,#124377,#124378,#124379,
#124380,#124381,#124382,#124383,#124384,#124385,#124386,#124387,#124388,
#124389,#124390,#124391,#124392,#124393,#124394,#124395,#124396,#124397,
#124398,#124399,#124400,#124401,#124402,#124403,#124404,#124405,#124406,
#124407,#124408,#124409,#124410,#124411,#124412,#124413,#124414,#124415,
#124416,#124417,#124418,#124419,#124420,#124421,#124422,#124423,#124424,
#124425,#124426,#124427,#124428,#124429,#124430,#124431,#124432,#124433,
#124434,#124435,#124436,#124437,#124438,#124439,#124440,#124441,#124442,
#124443,#124444,#124445,#124446,#124447,#124448,#124449,#124450,#124451,
#124452,#124453,#124454,#124455,#124456,#124457,#124458,#124459,#124460,
#124461,#124462,#124463,#124464,#124465,#124466,#124467,#124468,#124469,
#124470,#124471,#124472,#124473,#124474,#124475,#124476,#124477,#124478,
#124479,#124480,#124481,#124482,#124483,#124484,#124485,#124486,#124487,
#124488,#124489,#124490,#124491,#124492,#124493,#124494,#124495,#124496,
#124497,#124498),.UNSPECIFIED.,.F.,.F.,(4,3,3,3,3,3,3,3,3,3,3,3,3,3,3,3,
3,3,3,3,3,3,3,3,3,3,3,3,3,3,3,3,3,3,3,3,3,3,3,3,3,3,3,3,3,3,3,3,3,3,3,3,
3,3,3,3,3,3,3,3,3,3,3,3,3,4),(114.220077335694,114.33434957594,114.446371905497,
114.558296674362,114.670170562004,114.786191735918,114.898176860493,115.010235018737,
115.11261136392,115.122481064781,115.134217102282,115.13425525766,115.238194100788,
115.247761589678,115.361066064117,115.474258346336,115.587383199224,115.700485285426,
115.81369072395,115.926947423793,116.040416912324,116.126754127008,116.126791940916,
116.230802571534,116.240305554226,116.353618126926,116.466818999181,116.579952912647,
116.693064509343,116.806280067485,116.919547240532,117.033027640638,117.119289858741,
117.119328624171,117.223112043074,117.232655671037,117.345780955494,117.458794234581,
117.571740577994,117.684664955273,117.79769531587,117.910778123356,118.024077818661,
118.111827279956,118.111865307427,118.215860201835,118.225558196699,118.339047810285,
118.452424216398,118.565731855983,118.679015068459,118.792397641909,118.905829519251,
119.019468834404,119.10436589177,119.104401990683,119.207910461063,119.217456662739,
119.329494590553,119.441426415126,119.553298846381,119.667183976568,119.779143127069,
119.893991247099,120.002398983502,120.00883936713),.UNSPECIFIED.);
#1641=B_SPLINE_CURVE_WITH_KNOTS('',3,(#124501,#124502,#124503,#124504,#124505,
#124506,#124507,#124508,#124509,#124510,#124511,#124512,#124513,#124514,
#124515,#124516,#124517,#124518,#124519,#124520,#124521,#124522,#124523,
#124524,#124525,#124526,#124527,#124528,#124529,#124530,#124531,#124532,
#124533,#124534,#124535,#124536,#124537,#124538,#124539,#124540,#124541,
#124542,#124543,#124544,#124545,#124546,#124547,#124548,#124549,#124550,
#124551,#124552,#124553,#124554,#124555,#124556,#124557,#124558,#124559,
#124560,#124561,#124562,#124563,#124564,#124565,#124566,#124567,#124568,
#124569,#124570,#124571,#124572,#124573,#124574,#124575,#124576,#124577,
#124578,#124579,#124580,#124581,#124582,#124583,#124584,#124585,#124586,
#124587,#124588,#124589,#124590,#124591,#124592,#124593,#124594,#124595,
#124596,#124597,#124598,#124599,#124600,#124601,#124602,#124603,#124604,
#124605,#124606,#124607,#124608,#124609,#124610,#124611,#124612,#124613,
#124614,#124615,#124616,#124617,#124618,#124619,#124620,#124621,#124622,
#124623,#124624,#124625,#124626,#124627,#124628,#124629,#124630,#124631,
#124632,#124633,#124634,#124635,#124636),.UNSPECIFIED.,.F.,.F.,(4,3,3,3,
3,3,3,3,3,3,3,3,3,3,3,3,3,3,3,3,3,3,3,3,3,3,3,3,3,3,3,3,3,3,3,3,3,3,3,3,
3,3,3,3,3,4),(-122.08201204045,-121.965917445828,-121.84987950632,-121.73386954936,
-121.617851459242,-121.501789119903,-121.38555131248,-121.269219443816,
-121.152648388576,-121.089475357194,-120.977120237893,-120.864991994256,
-120.752990586367,-120.641069346948,-120.529181735418,-120.417198453266,
-120.305170328657,-120.19292473749,-120.096938673939,-119.983292274015,
-119.869847663663,-119.756515326666,-119.64325077363,-119.53000961553,-119.416667246722,
-119.303274605463,-119.189672534295,-119.104401990683,-118.990730137739,
-118.877253694146,-118.763885635601,-118.650581534411,-118.537297058507,
-118.423905835679,-118.310461187396,-118.196802551937,-118.111865307427,
-117.996552974004,-117.884544281931,-117.772645207091,-117.660808992061,
-117.548988983923,-117.437070174475,-117.325090175962,-117.212929561234,
-117.189366640045),.UNSPECIFIED.);
#1642=B_SPLINE_CURVE_WITH_KNOTS('',3,(#124641,#124642,#124643,#124644,#124645,
#124646,#124647,#124648,#124649,#124650,#124651,#124652,#124653,#124654,
#124655,#124656,#124657,#124658,#124659,#124660,#124661,#124662,#124663,
#124664,#124665,#124666,#124667,#124668,#124669,#124670,#124671,#124672,
#124673,#124674,#124675,#124676,#124677,#124678,#124679,#124680,#124681,
#124682,#124683,#124684,#124685,#124686,#124687,#124688,#124689,#124690,
#124691,#124692,#124693,#124694,#124695,#124696,#124697,#124698,#124699,
#124700,#124701,#124702,#124703,#124704,#124705,#124706,#124707,#124708,
#124709,#124710,#124711,#124712,#124713,#124714,#124715,#124716,#124717,
#124718,#124719,#124720,#124721,#124722),.UNSPECIFIED.,.F.,.F.,(4,3,3,3,
3,3,3,3,3,3,3,3,3,3,3,3,3,3,3,3,3,3,3,3,3,3,3,4),(-0.272868023033693,-0.262502242400483,
-0.24527561767975,-0.237903293088585,-0.234230035432386,-0.217032391147809,
-0.20548949783366,-0.200475199976904,-0.197081245750112,-0.180328401578601,
-0.16398380749676,-0.154160166781224,-0.14719926789301,-0.144231535113113,
-0.128376931012345,-0.124689244634614,-0.108443690652105,-0.100974559826481,
-0.0956859974770197,-0.0926107843079526,-0.0768446513362621,-0.0611547177757335,
-0.05329672619646,-0.0475077033060932,-0.0447092358393594,-0.0296005801383283,
-0.0148002900691642,0.),.UNSPECIFIED.);
#1643=B_SPLINE_CURVE_WITH_KNOTS('',3,(#124723,#124724,#124725,#124726,#124727,
#124728,#124729,#124730,#124731,#124732,#124733,#124734,#124735,#124736),
 .UNSPECIFIED.,.F.,.F.,(4,2,2,2,2,2,4),(9.99999625904413E-7,0.0430920561884333,
0.0851072847416361,0.126567605991081,0.169373405344057,0.208996427770222,
0.24979679593988),.UNSPECIFIED.);
#1644=B_SPLINE_CURVE_WITH_KNOTS('',3,(#125242,#125243,#125244,#125245,#125246,
#125247),.UNSPECIFIED.,.F.,.F.,(4,2,4),(8.45004561326557E-5,0.00132119826430728,
0.00256099238825395),.UNSPECIFIED.);
#1645=B_SPLINE_CURVE_WITH_KNOTS('',3,(#125249,#125250,#125251,#125252,#125253,
#125254,#125255,#125256,#125257,#125258,#125259,#125260,#125261,#125262,
#125263,#125264,#125265,#125266,#125267,#125268,#125269,#125270,#125271,
#125272,#125273,#125274,#125275,#125276,#125277,#125278,#125279,#125280,
#125281,#125282,#125283,#125284,#125285,#125286,#125287,#125288,#125289,
#125290,#125291,#125292,#125293,#125294,#125295,#125296,#125297,#125298,
#125299,#125300,#125301,#125302,#125303,#125304,#125305,#125306,#125307,
#125308,#125309,#125310,#125311,#125312,#125313,#125314,#125315,#125316,
#125317,#125318,#125319,#125320,#125321,#125322,#125323,#125324,#125325,
#125326,#125327,#125328,#125329,#125330,#125331,#125332,#125333),
 .UNSPECIFIED.,.F.,.F.,(4,3,3,3,3,3,3,3,3,3,3,3,3,3,3,3,3,3,3,3,3,3,3,3,
3,3,3,3,4),(-0.276631791712731,-0.266078274757453,-0.25142944697914,-0.244605027091712,
-0.241150782754899,-0.225852149777011,-0.215097155747404,-0.211769086231776,
-0.208422910451095,-0.192472307416272,-0.176609029381956,-0.16739153228391,
-0.162510949576809,-0.159609420310082,-0.143083140167058,-0.139739040989771,
-0.123776906696283,-0.115962699697761,-0.111035505377364,-0.107829669889836,
-0.0911010363506398,-0.0743724028114436,-0.0648654694233928,-0.0586676892110244,
-0.0555403299923495,-0.0380585004240356,-0.020721803007727,-0.00352182003484276,
0.),.UNSPECIFIED.);
#1646=B_SPLINE_CURVE_WITH_KNOTS('',3,(#125334,#125335,#125336,#125337),
 .UNSPECIFIED.,.F.,.F.,(4,4),(-0.0121033717511618,0.),.UNSPECIFIED.);
#1647=B_SPLINE_CURVE_WITH_KNOTS('',3,(#125342,#125343,#125344,#125345,#125346,
#125347,#125348,#125349,#125350,#125351,#125352,#125353,#125354,#125355,
#125356,#125357,#125358,#125359,#125360,#125361,#125362,#125363,#125364,
#125365,#125366,#125367,#125368,#125369,#125370,#125371,#125372,#125373,
#125374,#125375,#125376,#125377,#125378,#125379,#125380,#125381,#125382,
#125383,#125384,#125385,#125386,#125387,#125388,#125389,#125390,#125391,
#125392,#125393,#125394,#125395,#125396,#125397,#125398,#125399,#125400,
#125401,#125402,#125403,#125404,#125405,#125406,#125407,#125408,#125409,
#125410,#125411,#125412,#125413,#125414,#125415,#125416,#125417,#125418,
#125419,#125420,#125421,#125422,#125423),.UNSPECIFIED.,.F.,.F.,(4,3,3,3,
3,3,3,3,3,3,3,3,3,3,3,3,3,3,3,3,3,3,3,3,3,3,3,4),(-0.272867943863341,-0.262502242400497,
-0.245275617679762,-0.237903297370454,-0.234230038512527,-0.21703119377903,
-0.205489500611459,-0.200475208558893,-0.19708124562454,-0.180335625911279,
-0.163965603178691,-0.154160171865287,-0.14719928547427,-0.144231543166927,
-0.128376945114741,-0.124689244634617,-0.108477769606106,-0.100974564290966,
-0.0956859981647498,-0.0926107839869569,-0.0768294319563884,-0.0611547141438257,
-0.0532967250836255,-0.0475076998648919,-0.0447092326529874,-0.0296829840600132,
-0.0148414920300066,0.),.UNSPECIFIED.);
#1648=B_SPLINE_CURVE_WITH_KNOTS('',3,(#125929,#125930,#125931,#125932,#125933,
#125934),.UNSPECIFIED.,.F.,.F.,(4,2,4),(-0.00251068061179639,-0.00126056420704893,
-1.00000002448055E-6),.UNSPECIFIED.);
#1724=SHAPE_REPRESENTATION_RELATIONSHIP('SRR','None',#135348,#1737);
#1737=ADVANCED_BREP_SHAPE_REPRESENTATION('',(#1763),#135280);
#1750=STYLED_ITEM('',(#135422),#1763);
#1763=MANIFOLD_SOLID_BREP('Body1',#32086);
#1945=CYLINDRICAL_SURFACE('',#33857,1.4635);
#1946=CYLINDRICAL_SURFACE('',#33859,1.4635);
#1947=CYLINDRICAL_SURFACE('',#33860,1.4635);
#1948=CYLINDRICAL_SURFACE('',#33861,1.4635);
#1949=CYLINDRICAL_SURFACE('',#33862,1.4635);
#1950=CYLINDRICAL_SURFACE('',#33863,1.4635);
#1951=CYLINDRICAL_SURFACE('',#33864,1.4635);
#1952=CYLINDRICAL_SURFACE('',#33865,1.4635);
#1953=CYLINDRICAL_SURFACE('',#33866,1.4635);
#1954=CYLINDRICAL_SURFACE('',#33867,1.4635);
#1955=CYLINDRICAL_SURFACE('',#33868,1.4635);
#1956=CYLINDRICAL_SURFACE('',#33869,1.4635);
#1957=CYLINDRICAL_SURFACE('',#33870,1.4635);
#1958=CYLINDRICAL_SURFACE('',#33871,1.4635);
#1959=CYLINDRICAL_SURFACE('',#33872,1.4635);
#1960=CYLINDRICAL_SURFACE('',#33873,1.4635);
#1961=CYLINDRICAL_SURFACE('',#33874,1.4635);
#1962=CYLINDRICAL_SURFACE('',#33875,1.4635);
#1963=CYLINDRICAL_SURFACE('',#33876,1.4635);
#1964=CYLINDRICAL_SURFACE('',#33877,1.17775);
#1965=CYLINDRICAL_SURFACE('',#33879,1.17775);
#1966=CYLINDRICAL_SURFACE('',#33880,1.17775);
#1967=CYLINDRICAL_SURFACE('',#33881,1.17775);
#1968=CYLINDRICAL_SURFACE('',#33882,1.17775);
#1969=CYLINDRICAL_SURFACE('',#33883,1.17775);
#1970=CYLINDRICAL_SURFACE('',#33884,1.17775);
#1971=CYLINDRICAL_SURFACE('',#33885,1.17775);
#1972=CYLINDRICAL_SURFACE('',#33886,1.17775);
#1973=CYLINDRICAL_SURFACE('',#33887,1.17775);
#1974=CYLINDRICAL_SURFACE('',#33888,1.17775);
#1975=CYLINDRICAL_SURFACE('',#33889,1.17775);
#1976=CYLINDRICAL_SURFACE('',#33890,1.17775);
#1977=CYLINDRICAL_SURFACE('',#33891,1.17775);
#1978=CYLINDRICAL_SURFACE('',#33892,1.17775);
#1979=CYLINDRICAL_SURFACE('',#33893,1.17775);
#1980=CYLINDRICAL_SURFACE('',#33894,1.17775);
#1981=CYLINDRICAL_SURFACE('',#33895,1.17775);
#1982=CYLINDRICAL_SURFACE('',#33896,1.17775);
#1983=CYLINDRICAL_SURFACE('',#33897,1.17775);
#1984=CYLINDRICAL_SURFACE('',#33899,1.4635);
#1985=CYLINDRICAL_SURFACE('',#33919,2.75);
#1986=CYLINDRICAL_SURFACE('',#34112,1.39337567297406);
#1987=CYLINDRICAL_SURFACE('',#34114,1.39337567297406);
#1988=CYLINDRICAL_SURFACE('',#34116,1.39337567297406);
#1989=CYLINDRICAL_SURFACE('',#34118,1.39337567297406);
#1990=CYLINDRICAL_SURFACE('',#34120,1.39337567297406);
#1991=CYLINDRICAL_SURFACE('',#34122,1.39337567297406);
#2229=FACE_BOUND('',#6889,.T.);
#2230=FACE_BOUND('',#7004,.T.);
#3207=PLANE('',#33901);
#3208=PLANE('',#33904);
#3209=PLANE('',#33910);
#3210=PLANE('',#33914);
#3211=PLANE('',#33915);
#3212=PLANE('',#33917);
#3213=PLANE('',#33918);
#3214=PLANE('',#33994);
#3215=PLANE('',#33995);
#3216=PLANE('',#33996);
#3217=PLANE('',#33999);
#3218=PLANE('',#34000);
#3219=PLANE('',#34001);
#3220=PLANE('',#34002);
#3221=PLANE('',#34003);
#3222=PLANE('',#34004);
#3223=PLANE('',#34005);
#3224=PLANE('',#34006);
#3225=PLANE('',#34007);
#3226=PLANE('',#34008);
#3227=PLANE('',#34009);
#3228=PLANE('',#34010);
#3229=PLANE('',#34011);
#3230=PLANE('',#34012);
#3231=PLANE('',#34013);
#3232=PLANE('',#34014);
#3233=PLANE('',#34015);
#3234=PLANE('',#34016);
#3235=PLANE('',#34017);
#3236=PLANE('',#34018);
#3237=PLANE('',#34019);
#3238=PLANE('',#34020);
#3239=PLANE('',#34021);
#3240=PLANE('',#34022);
#3241=PLANE('',#34023);
#3242=PLANE('',#34024);
#3243=PLANE('',#34025);
#3244=PLANE('',#34026);
#3245=PLANE('',#34027);
#3246=PLANE('',#34028);
#3247=PLANE('',#34029);
#3248=PLANE('',#34030);
#3249=PLANE('',#34031);
#3250=PLANE('',#34032);
#3251=PLANE('',#34033);
#3252=PLANE('',#34034);
#3253=PLANE('',#34035);
#3254=PLANE('',#34036);
#3255=PLANE('',#34037);
#3256=PLANE('',#34038);
#3257=PLANE('',#34039);
#3258=PLANE('',#34040);
#3259=PLANE('',#34041);
#3260=PLANE('',#34042);
#3261=PLANE('',#34043);
#3262=PLANE('',#34044);
#3263=PLANE('',#34045);
#3264=PLANE('',#34046);
#3265=PLANE('',#34047);
#3266=PLANE('',#34048);
#3267=PLANE('',#34049);
#3268=PLANE('',#34050);
#3269=PLANE('',#34051);
#3270=PLANE('',#34052);
#3271=PLANE('',#34053);
#3272=PLANE('',#34054);
#3273=PLANE('',#34055);
#3274=PLANE('',#34056);
#3275=PLANE('',#34057);
#3276=PLANE('',#34058);
#3277=PLANE('',#34059);
#3278=PLANE('',#34060);
#3279=PLANE('',#34061);
#3280=PLANE('',#34062);
#3281=PLANE('',#34063);
#3282=PLANE('',#34064);
#3283=PLANE('',#34065);
#3284=PLANE('',#34066);
#3285=PLANE('',#34067);
#3286=PLANE('',#34068);
#3287=PLANE('',#34069);
#3288=PLANE('',#34070);
#3289=PLANE('',#34071);
#3290=PLANE('',#34072);
#3291=PLANE('',#34073);
#3292=PLANE('',#34074);
#3293=PLANE('',#34075);
#3294=PLANE('',#34076);
#3295=PLANE('',#34077);
#3296=PLANE('',#34078);
#3297=PLANE('',#34079);
#3298=PLANE('',#34080);
#3299=PLANE('',#34081);
#3300=PLANE('',#34082);
#3301=PLANE('',#34083);
#3302=PLANE('',#34084);
#3303=PLANE('',#34085);
#3304=PLANE('',#34086);
#3305=PLANE('',#34087);
#3306=PLANE('',#34088);
#3307=PLANE('',#34089);
#3308=PLANE('',#34090);
#3309=PLANE('',#34091);
#3310=PLANE('',#34092);
#3311=PLANE('',#34093);
#3312=PLANE('',#34094);
#3313=PLANE('',#34095);
#3314=PLANE('',#34096);
#3315=PLANE('',#34097);
#3316=PLANE('',#34098);
#3317=PLANE('',#34099);
#3318=PLANE('',#34100);
#3319=PLANE('',#34103);
#3320=PLANE('',#34124);
#3321=PLANE('',#34125);
#3322=PLANE('',#34126);
#3323=PLANE('',#34127);
#3324=PLANE('',#34128);
#3325=PLANE('',#34129);
#3326=PLANE('',#34130);
#3327=PLANE('',#34131);
#3328=PLANE('',#34132);
#3329=PLANE('',#34133);
#3330=PLANE('',#34135);
#3331=PLANE('',#34137);
#3332=PLANE('',#34139);
#3333=PLANE('',#34141);
#3334=PLANE('',#34143);
#3335=PLANE('',#34146);
#3336=PLANE('',#34147);
#3337=PLANE('',#34148);
#4876=FACE_OUTER_BOUND('',#6843,.T.);
#4877=FACE_OUTER_BOUND('',#6844,.T.);
#4878=FACE_OUTER_BOUND('',#6845,.T.);
#4879=FACE_OUTER_BOUND('',#6846,.T.);
#4880=FACE_OUTER_BOUND('',#6847,.T.);
#4881=FACE_OUTER_BOUND('',#6848,.T.);
#4882=FACE_OUTER_BOUND('',#6849,.T.);
#4883=FACE_OUTER_BOUND('',#6850,.T.);
#4884=FACE_OUTER_BOUND('',#6851,.T.);
#4885=FACE_OUTER_BOUND('',#6852,.T.);
#4886=FACE_OUTER_BOUND('',#6853,.T.);
#4887=FACE_OUTER_BOUND('',#6854,.T.);
#4888=FACE_OUTER_BOUND('',#6855,.T.);
#4889=FACE_OUTER_BOUND('',#6856,.T.);
#4890=FACE_OUTER_BOUND('',#6857,.T.);
#4891=FACE_OUTER_BOUND('',#6858,.T.);
#4892=FACE_OUTER_BOUND('',#6859,.T.);
#4893=FACE_OUTER_BOUND('',#6860,.T.);
#4894=FACE_OUTER_BOUND('',#6861,.T.);
#4895=FACE_OUTER_BOUND('',#6862,.T.);
#4896=FACE_OUTER_BOUND('',#6863,.T.);
#4897=FACE_OUTER_BOUND('',#6864,.T.);
#4898=FACE_OUTER_BOUND('',#6865,.T.);
#4899=FACE_OUTER_BOUND('',#6866,.T.);
#4900=FACE_OUTER_BOUND('',#6867,.T.);
#4901=FACE_OUTER_BOUND('',#6868,.T.);
#4902=FACE_OUTER_BOUND('',#6869,.T.);
#4903=FACE_OUTER_BOUND('',#6870,.T.);
#4904=FACE_OUTER_BOUND('',#6871,.T.);
#4905=FACE_OUTER_BOUND('',#6872,.T.);
#4906=FACE_OUTER_BOUND('',#6873,.T.);
#4907=FACE_OUTER_BOUND('',#6874,.T.);
#4908=FACE_OUTER_BOUND('',#6875,.T.);
#4909=FACE_OUTER_BOUND('',#6876,.T.);
#4910=FACE_OUTER_BOUND('',#6877,.T.);
#4911=FACE_OUTER_BOUND('',#6878,.T.);
#4912=FACE_OUTER_BOUND('',#6879,.T.);
#4913=FACE_OUTER_BOUND('',#6880,.T.);
#4914=FACE_OUTER_BOUND('',#6881,.T.);
#4915=FACE_OUTER_BOUND('',#6882,.T.);
#4916=FACE_OUTER_BOUND('',#6883,.T.);
#4917=FACE_OUTER_BOUND('',#6884,.T.);
#4918=FACE_OUTER_BOUND('',#6885,.T.);
#4919=FACE_OUTER_BOUND('',#6886,.T.);
#4920=FACE_OUTER_BOUND('',#6887,.T.);
#4921=FACE_OUTER_BOUND('',#6888,.T.);
#4922=FACE_OUTER_BOUND('',#6890,.T.);
#4923=FACE_OUTER_BOUND('',#6891,.T.);
#4924=FACE_OUTER_BOUND('',#6892,.T.);
#4925=FACE_OUTER_BOUND('',#6893,.T.);
#4926=FACE_OUTER_BOUND('',#6894,.T.);
#4927=FACE_OUTER_BOUND('',#6895,.T.);
#4928=FACE_OUTER_BOUND('',#6896,.T.);
#4929=FACE_OUTER_BOUND('',#6897,.T.);
#4930=FACE_OUTER_BOUND('',#6898,.T.);
#4931=FACE_OUTER_BOUND('',#6899,.T.);
#4932=FACE_OUTER_BOUND('',#6900,.T.);
#4933=FACE_OUTER_BOUND('',#6901,.T.);
#4934=FACE_OUTER_BOUND('',#6902,.T.);
#4935=FACE_OUTER_BOUND('',#6903,.T.);
#4936=FACE_OUTER_BOUND('',#6904,.T.);
#4937=FACE_OUTER_BOUND('',#6905,.T.);
#4938=FACE_OUTER_BOUND('',#6906,.T.);
#4939=FACE_OUTER_BOUND('',#6907,.T.);
#4940=FACE_OUTER_BOUND('',#6908,.T.);
#4941=FACE_OUTER_BOUND('',#6909,.T.);
#4942=FACE_OUTER_BOUND('',#6910,.T.);
#4943=FACE_OUTER_BOUND('',#6911,.T.);
#4944=FACE_OUTER_BOUND('',#6912,.T.);
#4945=FACE_OUTER_BOUND('',#6913,.T.);
#4946=FACE_OUTER_BOUND('',#6914,.T.);
#4947=FACE_OUTER_BOUND('',#6915,.T.);
#4948=FACE_OUTER_BOUND('',#6916,.T.);
#4949=FACE_OUTER_BOUND('',#6917,.T.);
#4950=FACE_OUTER_BOUND('',#6918,.T.);
#4951=FACE_OUTER_BOUND('',#6919,.T.);
#4952=FACE_OUTER_BOUND('',#6920,.T.);
#4953=FACE_OUTER_BOUND('',#6921,.T.);
#4954=FACE_OUTER_BOUND('',#6922,.T.);
#4955=FACE_OUTER_BOUND('',#6923,.T.);
#4956=FACE_OUTER_BOUND('',#6924,.T.);
#4957=FACE_OUTER_BOUND('',#6925,.T.);
#4958=FACE_OUTER_BOUND('',#6926,.T.);
#4959=FACE_OUTER_BOUND('',#6927,.T.);
#4960=FACE_OUTER_BOUND('',#6928,.T.);
#4961=FACE_OUTER_BOUND('',#6929,.T.);
#4962=FACE_OUTER_BOUND('',#6930,.T.);
#4963=FACE_OUTER_BOUND('',#6931,.T.);
#4964=FACE_OUTER_BOUND('',#6932,.T.);
#4965=FACE_OUTER_BOUND('',#6933,.T.);
#4966=FACE_OUTER_BOUND('',#6934,.T.);
#4967=FACE_OUTER_BOUND('',#6935,.T.);
#4968=FACE_OUTER_BOUND('',#6936,.T.);
#4969=FACE_OUTER_BOUND('',#6937,.T.);
#4970=FACE_OUTER_BOUND('',#6938,.T.);
#4971=FACE_OUTER_BOUND('',#6939,.T.);
#4972=FACE_OUTER_BOUND('',#6940,.T.);
#4973=FACE_OUTER_BOUND('',#6941,.T.);
#4974=FACE_OUTER_BOUND('',#6942,.T.);
#4975=FACE_OUTER_BOUND('',#6943,.T.);
#4976=FACE_OUTER_BOUND('',#6944,.T.);
#4977=FACE_OUTER_BOUND('',#6945,.T.);
#4978=FACE_OUTER_BOUND('',#6946,.T.);
#4979=FACE_OUTER_BOUND('',#6947,.T.);
#4980=FACE_OUTER_BOUND('',#6948,.T.);
#4981=FACE_OUTER_BOUND('',#6949,.T.);
#4982=FACE_OUTER_BOUND('',#6950,.T.);
#4983=FACE_OUTER_BOUND('',#6951,.T.);
#4984=FACE_OUTER_BOUND('',#6952,.T.);
#4985=FACE_OUTER_BOUND('',#6953,.T.);
#4986=FACE_OUTER_BOUND('',#6954,.T.);
#4987=FACE_OUTER_BOUND('',#6955,.T.);
#4988=FACE_OUTER_BOUND('',#6956,.T.);
#4989=FACE_OUTER_BOUND('',#6957,.T.);
#4990=FACE_OUTER_BOUND('',#6958,.T.);
#4991=FACE_OUTER_BOUND('',#6959,.T.);
#4992=FACE_OUTER_BOUND('',#6960,.T.);
#4993=FACE_OUTER_BOUND('',#6961,.T.);
#4994=FACE_OUTER_BOUND('',#6962,.T.);
#4995=FACE_OUTER_BOUND('',#6963,.T.);
#4996=FACE_OUTER_BOUND('',#6964,.T.);
#4997=FACE_OUTER_BOUND('',#6965,.T.);
#4998=FACE_OUTER_BOUND('',#6966,.T.);
#4999=FACE_OUTER_BOUND('',#6967,.T.);
#5000=FACE_OUTER_BOUND('',#6968,.T.);
#5001=FACE_OUTER_BOUND('',#6969,.T.);
#5002=FACE_OUTER_BOUND('',#6970,.T.);
#5003=FACE_OUTER_BOUND('',#6971,.T.);
#5004=FACE_OUTER_BOUND('',#6972,.T.);
#5005=FACE_OUTER_BOUND('',#6973,.T.);
#5006=FACE_OUTER_BOUND('',#6974,.T.);
#5007=FACE_OUTER_BOUND('',#6975,.T.);
#5008=FACE_OUTER_BOUND('',#6976,.T.);
#5009=FACE_OUTER_BOUND('',#6977,.T.);
#5010=FACE_OUTER_BOUND('',#6978,.T.);
#5011=FACE_OUTER_BOUND('',#6979,.T.);
#5012=FACE_OUTER_BOUND('',#6980,.T.);
#5013=FACE_OUTER_BOUND('',#6981,.T.);
#5014=FACE_OUTER_BOUND('',#6982,.T.);
#5015=FACE_OUTER_BOUND('',#6983,.T.);
#5016=FACE_OUTER_BOUND('',#6984,.T.);
#5017=FACE_OUTER_BOUND('',#6985,.T.);
#5018=FACE_OUTER_BOUND('',#6986,.T.);
#5019=FACE_OUTER_BOUND('',#6987,.T.);
#5020=FACE_OUTER_BOUND('',#6988,.T.);
#5021=FACE_OUTER_BOUND('',#6989,.T.);
#5022=FACE_OUTER_BOUND('',#6990,.T.);
#5023=FACE_OUTER_BOUND('',#6991,.T.);
#5024=FACE_OUTER_BOUND('',#6992,.T.);
#5025=FACE_OUTER_BOUND('',#6993,.T.);
#5026=FACE_OUTER_BOUND('',#6994,.T.);
#5027=FACE_OUTER_BOUND('',#6995,.T.);
#5028=FACE_OUTER_BOUND('',#6996,.T.);
#5029=FACE_OUTER_BOUND('',#6997,.T.);
#5030=FACE_OUTER_BOUND('',#6998,.T.);
#5031=FACE_OUTER_BOUND('',#6999,.T.);
#5032=FACE_OUTER_BOUND('',#7000,.T.);
#5033=FACE_OUTER_BOUND('',#7001,.T.);
#5034=FACE_OUTER_BOUND('',#7002,.T.);
#5035=FACE_OUTER_BOUND('',#7003,.T.);
#5036=FACE_OUTER_BOUND('',#7005,.T.);
#5037=FACE_OUTER_BOUND('',#7006,.T.);
#5038=FACE_OUTER_BOUND('',#7007,.T.);
#5039=FACE_OUTER_BOUND('',#7008,.T.);
#5040=FACE_OUTER_BOUND('',#7009,.T.);
#5041=FACE_OUTER_BOUND('',#7010,.T.);
#5042=FACE_OUTER_BOUND('',#7011,.T.);
#5043=FACE_OUTER_BOUND('',#7012,.T.);
#5044=FACE_OUTER_BOUND('',#7013,.T.);
#5045=FACE_OUTER_BOUND('',#7014,.T.);
#5046=FACE_OUTER_BOUND('',#7015,.T.);
#5047=FACE_OUTER_BOUND('',#7016,.T.);
#5048=FACE_OUTER_BOUND('',#7017,.T.);
#5049=FACE_OUTER_BOUND('',#7018,.T.);
#5050=FACE_OUTER_BOUND('',#7019,.T.);
#5051=FACE_OUTER_BOUND('',#7020,.T.);
#5052=FACE_OUTER_BOUND('',#7021,.T.);
#5053=FACE_OUTER_BOUND('',#7022,.T.);
#5054=FACE_OUTER_BOUND('',#7023,.T.);
#5055=FACE_OUTER_BOUND('',#7024,.T.);
#5056=FACE_OUTER_BOUND('',#7025,.T.);
#5057=FACE_OUTER_BOUND('',#7026,.T.);
#5058=FACE_OUTER_BOUND('',#7027,.T.);
#5059=FACE_OUTER_BOUND('',#7028,.T.);
#5060=FACE_OUTER_BOUND('',#7029,.T.);
#5061=FACE_OUTER_BOUND('',#7030,.T.);
#6843=EDGE_LOOP('',(#28936,#28937,#28938,#28939));
#6844=EDGE_LOOP('',(#28940,#28941,#28942,#28943));
#6845=EDGE_LOOP('',(#28944,#28945,#28946,#28947));
#6846=EDGE_LOOP('',(#28948,#28949,#28950,#28951,#28952));
#6847=EDGE_LOOP('',(#28953,#28954,#28955,#28956));
#6848=EDGE_LOOP('',(#28957,#28958,#28959,#28960));
#6849=EDGE_LOOP('',(#28961,#28962,#28963,#28964,#28965));
#6850=EDGE_LOOP('',(#28966,#28967,#28968,#28969));
#6851=EDGE_LOOP('',(#28970,#28971,#28972,#28973));
#6852=EDGE_LOOP('',(#28974,#28975,#28976,#28977,#28978));
#6853=EDGE_LOOP('',(#28979,#28980,#28981,#28982));
#6854=EDGE_LOOP('',(#28983,#28984,#28985,#28986));
#6855=EDGE_LOOP('',(#28987,#28988,#28989,#28990));
#6856=EDGE_LOOP('',(#28991,#28992,#28993,#28994));
#6857=EDGE_LOOP('',(#28995,#28996,#28997,#28998));
#6858=EDGE_LOOP('',(#28999,#29000,#29001,#29002,#29003));
#6859=EDGE_LOOP('',(#29004,#29005,#29006,#29007));
#6860=EDGE_LOOP('',(#29008,#29009,#29010,#29011));
#6861=EDGE_LOOP('',(#29012,#29013,#29014,#29015));
#6862=EDGE_LOOP('',(#29016,#29017,#29018,#29019));
#6863=EDGE_LOOP('',(#29020,#29021,#29022,#29023,#29024));
#6864=EDGE_LOOP('',(#29025,#29026,#29027,#29028));
#6865=EDGE_LOOP('',(#29029,#29030,#29031,#29032));
#6866=EDGE_LOOP('',(#29033,#29034,#29035,#29036));
#6867=EDGE_LOOP('',(#29037,#29038,#29039,#29040,#29041));
#6868=EDGE_LOOP('',(#29042,#29043,#29044,#29045));
#6869=EDGE_LOOP('',(#29046,#29047,#29048,#29049));
#6870=EDGE_LOOP('',(#29050,#29051,#29052,#29053));
#6871=EDGE_LOOP('',(#29054,#29055,#29056,#29057));
#6872=EDGE_LOOP('',(#29058,#29059,#29060,#29061));
#6873=EDGE_LOOP('',(#29062,#29063,#29064,#29065));
#6874=EDGE_LOOP('',(#29066,#29067,#29068,#29069));
#6875=EDGE_LOOP('',(#29070,#29071,#29072,#29073));
#6876=EDGE_LOOP('',(#29074,#29075,#29076,#29077,#29078));
#6877=EDGE_LOOP('',(#29079,#29080,#29081,#29082));
#6878=EDGE_LOOP('',(#29083,#29084,#29085,#29086));
#6879=EDGE_LOOP('',(#29087,#29088,#29089,#29090,#29091));
#6880=EDGE_LOOP('',(#29092,#29093,#29094,#29095));
#6881=EDGE_LOOP('',(#29096,#29097,#29098,#29099,#29100));
#6882=EDGE_LOOP('',(#29101,#29102,#29103,#29104));
#6883=EDGE_LOOP('',(#29105,#29106,#29107,#29108,#29109));
#6884=EDGE_LOOP('',(#29110,#29111,#29112,#29113,#29114,#29115,#29116,#29117,
#29118,#29119,#29120,#29121,#29122,#29123,#29124,#29125,#29126,#29127,#29128,
#29129,#29130,#29131,#29132,#29133,#29134,#29135,#29136,#29137,#29138,#29139,
#29140,#29141,#29142,#29143,#29144,#29145,#29146,#29147,#29148,#29149,#29150,
#29151,#29152,#29153,#29154,#29155,#29156,#29157,#29158,#29159));
#6885=EDGE_LOOP('',(#29160,#29161,#29162,#29163,#29164,#29165));
#6886=EDGE_LOOP('',(#29166,#29167,#29168,#29169,#29170,#29171,#29172,#29173,
#29174,#29175,#29176,#29177,#29178,#29179,#29180,#29181,#29182,#29183,#29184,
#29185,#29186,#29187,#29188,#29189,#29190,#29191,#29192,#29193,#29194,#29195,
#29196,#29197,#29198,#29199,#29200,#29201,#29202,#29203,#29204,#29205,#29206,
#29207,#29208,#29209,#29210,#29211));
#6887=EDGE_LOOP('',(#29212,#29213,#29214,#29215,#29216,#29217,#29218));
#6888=EDGE_LOOP('',(#29219));
#6889=EDGE_LOOP('',(#29220));
#6890=EDGE_LOOP('',(#29221,#29222,#29223,#29224,#29225,#29226,#29227));
#6891=EDGE_LOOP('',(#29228));
#6892=EDGE_LOOP('',(#29229,#29230,#29231));
#6893=EDGE_LOOP('',(#29232,#29233,#29234,#29235));
#6894=EDGE_LOOP('',(#29236,#29237,#29238,#29239));
#6895=EDGE_LOOP('',(#29240,#29241,#29242,#29243,#29244,#29245,#29246,#29247,
#29248,#29249,#29250,#29251,#29252,#29253,#29254,#29255,#29256,#29257,#29258,
#29259,#29260,#29261,#29262,#29263,#29264,#29265,#29266,#29267,#29268,#29269,
#29270,#29271,#29272,#29273,#29274,#29275,#29276,#29277,#29278,#29279,#29280,
#29281,#29282,#29283,#29284,#29285,#29286,#29287,#29288,#29289,#29290,#29291,
#29292,#29293,#29294,#29295,#29296,#29297,#29298,#29299,#29300,#29301,#29302,
#29303,#29304,#29305,#29306,#29307,#29308,#29309,#29310,#29311,#29312,#29313,
#29314,#29315,#29316,#29317,#29318,#29319,#29320,#29321,#29322,#29323,#29324,
#29325,#29326,#29327,#29328,#29329,#29330,#29331,#29332,#29333,#29334,#29335,
#29336,#29337,#29338,#29339,#29340,#29341,#29342,#29343,#29344,#29345,#29346,
#29347,#29348,#29349,#29350,#29351,#29352,#29353,#29354,#29355,#29356,#29357,
#29358,#29359,#29360,#29361,#29362,#29363,#29364,#29365,#29366,#29367,#29368,
#29369,#29370,#29371,#29372,#29373,#29374,#29375,#29376,#29377,#29378,#29379,
#29380,#29381,#29382,#29383,#29384,#29385,#29386,#29387,#29388));
#6896=EDGE_LOOP('',(#29389,#29390,#29391,#29392));
#6897=EDGE_LOOP('',(#29393,#29394,#29395,#29396));
#6898=EDGE_LOOP('',(#29397,#29398,#29399));
#6899=EDGE_LOOP('',(#29400,#29401,#29402,#29403,#29404,#29405,#29406,#29407,
#29408,#29409,#29410,#29411,#29412,#29413,#29414,#29415,#29416,#29417,#29418,
#29419,#29420,#29421,#29422,#29423,#29424,#29425,#29426,#29427,#29428,#29429,
#29430,#29431,#29432,#29433,#29434,#29435,#29436,#29437,#29438,#29439,#29440,
#29441,#29442,#29443,#29444,#29445,#29446,#29447,#29448,#29449,#29450,#29451,
#29452,#29453,#29454,#29455,#29456,#29457,#29458,#29459,#29460,#29461,#29462,
#29463,#29464,#29465,#29466,#29467,#29468,#29469,#29470,#29471,#29472,#29473,
#29474,#29475,#29476,#29477,#29478,#29479,#29480,#29481,#29482,#29483,#29484,
#29485,#29486,#29487,#29488,#29489,#29490,#29491,#29492,#29493,#29494,#29495,
#29496,#29497,#29498,#29499,#29500,#29501,#29502,#29503,#29504,#29505,#29506,
#29507,#29508,#29509,#29510));
#6900=EDGE_LOOP('',(#29511,#29512,#29513));
#6901=EDGE_LOOP('',(#29514,#29515,#29516,#29517));
#6902=EDGE_LOOP('',(#29518,#29519,#29520,#29521));
#6903=EDGE_LOOP('',(#29522,#29523,#29524,#29525));
#6904=EDGE_LOOP('',(#29526,#29527,#29528,#29529));
#6905=EDGE_LOOP('',(#29530,#29531,#29532));
#6906=EDGE_LOOP('',(#29533,#29534,#29535));
#6907=EDGE_LOOP('',(#29536,#29537,#29538,#29539));
#6908=EDGE_LOOP('',(#29540,#29541,#29542,#29543));
#6909=EDGE_LOOP('',(#29544,#29545,#29546,#29547));
#6910=EDGE_LOOP('',(#29548,#29549,#29550,#29551));
#6911=EDGE_LOOP('',(#29552,#29553,#29554));
#6912=EDGE_LOOP('',(#29555,#29556,#29557));
#6913=EDGE_LOOP('',(#29558,#29559,#29560,#29561));
#6914=EDGE_LOOP('',(#29562,#29563,#29564,#29565));
#6915=EDGE_LOOP('',(#29566,#29567,#29568,#29569));
#6916=EDGE_LOOP('',(#29570,#29571,#29572,#29573));
#6917=EDGE_LOOP('',(#29574,#29575,#29576));
#6918=EDGE_LOOP('',(#29577,#29578,#29579));
#6919=EDGE_LOOP('',(#29580,#29581,#29582,#29583));
#6920=EDGE_LOOP('',(#29584,#29585,#29586,#29587));
#6921=EDGE_LOOP('',(#29588,#29589,#29590,#29591));
#6922=EDGE_LOOP('',(#29592,#29593,#29594,#29595));
#6923=EDGE_LOOP('',(#29596,#29597,#29598));
#6924=EDGE_LOOP('',(#29599,#29600,#29601));
#6925=EDGE_LOOP('',(#29602,#29603,#29604,#29605));
#6926=EDGE_LOOP('',(#29606,#29607,#29608,#29609));
#6927=EDGE_LOOP('',(#29610,#29611,#29612,#29613));
#6928=EDGE_LOOP('',(#29614,#29615,#29616,#29617));
#6929=EDGE_LOOP('',(#29618,#29619,#29620));
#6930=EDGE_LOOP('',(#29621,#29622,#29623));
#6931=EDGE_LOOP('',(#29624,#29625,#29626,#29627));
#6932=EDGE_LOOP('',(#29628,#29629,#29630,#29631));
#6933=EDGE_LOOP('',(#29632,#29633,#29634,#29635));
#6934=EDGE_LOOP('',(#29636,#29637,#29638,#29639));
#6935=EDGE_LOOP('',(#29640,#29641,#29642));
#6936=EDGE_LOOP('',(#29643,#29644,#29645));
#6937=EDGE_LOOP('',(#29646,#29647,#29648,#29649));
#6938=EDGE_LOOP('',(#29650,#29651,#29652,#29653));
#6939=EDGE_LOOP('',(#29654,#29655,#29656,#29657));
#6940=EDGE_LOOP('',(#29658,#29659,#29660,#29661));
#6941=EDGE_LOOP('',(#29662,#29663,#29664));
#6942=EDGE_LOOP('',(#29665,#29666,#29667));
#6943=EDGE_LOOP('',(#29668,#29669,#29670,#29671));
#6944=EDGE_LOOP('',(#29672,#29673,#29674,#29675));
#6945=EDGE_LOOP('',(#29676,#29677,#29678,#29679));
#6946=EDGE_LOOP('',(#29680,#29681,#29682,#29683));
#6947=EDGE_LOOP('',(#29684,#29685,#29686,#29687));
#6948=EDGE_LOOP('',(#29688,#29689,#29690));
#6949=EDGE_LOOP('',(#29691,#29692,#29693,#29694));
#6950=EDGE_LOOP('',(#29695,#29696,#29697,#29698));
#6951=EDGE_LOOP('',(#29699,#29700,#29701,#29702));
#6952=EDGE_LOOP('',(#29703,#29704,#29705,#29706));
#6953=EDGE_LOOP('',(#29707,#29708,#29709));
#6954=EDGE_LOOP('',(#29710,#29711,#29712));
#6955=EDGE_LOOP('',(#29713,#29714,#29715,#29716));
#6956=EDGE_LOOP('',(#29717,#29718,#29719,#29720));
#6957=EDGE_LOOP('',(#29721,#29722,#29723,#29724));
#6958=EDGE_LOOP('',(#29725,#29726,#29727,#29728));
#6959=EDGE_LOOP('',(#29729,#29730,#29731));
#6960=EDGE_LOOP('',(#29732,#29733,#29734));
#6961=EDGE_LOOP('',(#29735,#29736,#29737,#29738));
#6962=EDGE_LOOP('',(#29739,#29740,#29741,#29742));
#6963=EDGE_LOOP('',(#29743,#29744,#29745,#29746));
#6964=EDGE_LOOP('',(#29747,#29748,#29749,#29750));
#6965=EDGE_LOOP('',(#29751,#29752,#29753));
#6966=EDGE_LOOP('',(#29754,#29755,#29756));
#6967=EDGE_LOOP('',(#29757,#29758,#29759,#29760));
#6968=EDGE_LOOP('',(#29761,#29762,#29763,#29764));
#6969=EDGE_LOOP('',(#29765,#29766,#29767,#29768));
#6970=EDGE_LOOP('',(#29769,#29770,#29771,#29772));
#6971=EDGE_LOOP('',(#29773,#29774,#29775));
#6972=EDGE_LOOP('',(#29776,#29777,#29778));
#6973=EDGE_LOOP('',(#29779,#29780,#29781,#29782));
#6974=EDGE_LOOP('',(#29783,#29784,#29785,#29786));
#6975=EDGE_LOOP('',(#29787,#29788,#29789,#29790));
#6976=EDGE_LOOP('',(#29791,#29792,#29793,#29794));
#6977=EDGE_LOOP('',(#29795,#29796,#29797));
#6978=EDGE_LOOP('',(#29798,#29799,#29800));
#6979=EDGE_LOOP('',(#29801,#29802,#29803,#29804));
#6980=EDGE_LOOP('',(#29805,#29806,#29807,#29808));
#6981=EDGE_LOOP('',(#29809,#29810,#29811,#29812));
#6982=EDGE_LOOP('',(#29813,#29814,#29815,#29816));
#6983=EDGE_LOOP('',(#29817,#29818,#29819));
#6984=EDGE_LOOP('',(#29820,#29821,#29822));
#6985=EDGE_LOOP('',(#29823,#29824,#29825,#29826));
#6986=EDGE_LOOP('',(#29827,#29828,#29829,#29830));
#6987=EDGE_LOOP('',(#29831,#29832,#29833,#29834));
#6988=EDGE_LOOP('',(#29835,#29836,#29837,#29838));
#6989=EDGE_LOOP('',(#29839,#29840,#29841));
#6990=EDGE_LOOP('',(#29842,#29843,#29844));
#6991=EDGE_LOOP('',(#29845,#29846,#29847,#29848));
#6992=EDGE_LOOP('',(#29849,#29850,#29851,#29852));
#6993=EDGE_LOOP('',(#29853,#29854,#29855,#29856));
#6994=EDGE_LOOP('',(#29857,#29858,#29859,#29860));
#6995=EDGE_LOOP('',(#29861,#29862,#29863));
#6996=EDGE_LOOP('',(#29864,#29865,#29866));
#6997=EDGE_LOOP('',(#29867,#29868,#29869,#29870));
#6998=EDGE_LOOP('',(#29871,#29872,#29873,#29874));
#6999=EDGE_LOOP('',(#29875,#29876,#29877,#29878));
#7000=EDGE_LOOP('',(#29879,#29880,#29881,#29882));
#7001=EDGE_LOOP('',(#29883,#29884,#29885));
#7002=EDGE_LOOP('',(#29886,#29887,#29888,#29889,#29890));
#7003=EDGE_LOOP('',(#29891));
#7004=EDGE_LOOP('',(#29892));
#7005=EDGE_LOOP('',(#29893,#29894,#29895,#29896,#29897,#29898,#29899,#29900,
#29901,#29902,#29903,#29904,#29905,#29906,#29907,#29908,#29909,#29910,#29911,
#29912,#29913));
#7006=EDGE_LOOP('',(#29914,#29915,#29916,#29917));
#7007=EDGE_LOOP('',(#29918,#29919,#29920,#29921));
#7008=EDGE_LOOP('',(#29922,#29923,#29924,#29925));
#7009=EDGE_LOOP('',(#29926,#29927,#29928,#29929));
#7010=EDGE_LOOP('',(#29930,#29931,#29932,#29933));
#7011=EDGE_LOOP('',(#29934,#29935,#29936,#29937));
#7012=EDGE_LOOP('',(#29938,#29939,#29940,#29941,#29942,#29943,#29944,#29945));
#7013=EDGE_LOOP('',(#29946,#29947,#29948,#29949,#29950,#29951,#29952,#29953));
#7014=EDGE_LOOP('',(#29954,#29955,#29956,#29957,#29958,#29959,#29960,#29961));
#7015=EDGE_LOOP('',(#29962,#29963));
#7016=EDGE_LOOP('',(#29964,#29965));
#7017=EDGE_LOOP('',(#29966,#29967));
#7018=EDGE_LOOP('',(#29968,#29969));
#7019=EDGE_LOOP('',(#29970,#29971));
#7020=EDGE_LOOP('',(#29972,#29973));
#7021=EDGE_LOOP('',(#29974,#29975));
#7022=EDGE_LOOP('',(#29976,#29977));
#7023=EDGE_LOOP('',(#29978,#29979));
#7024=EDGE_LOOP('',(#29980,#29981));
#7025=EDGE_LOOP('',(#29982,#29983));
#7026=EDGE_LOOP('',(#29984,#29985));
#7027=EDGE_LOOP('',(#29986,#29987,#29988,#29989,#29990,#29991,#29992,#29993));
#7028=EDGE_LOOP('',(#29994,#29995,#29996,#29997,#29998,#29999,#30000,#30001));
#7029=EDGE_LOOP('',(#30002,#30003,#30004,#30005,#30006,#30007,#30008,#30009));
#7030=EDGE_LOOP('',(#30010,#30011,#30012,#30013,#30014,#30015,#30016,#30017));
#9623=LINE('',#107629,#12460);
#9624=LINE('',#107793,#12461);
#9625=LINE('',#108213,#12462);
#9626=LINE('',#108665,#12463);
#9627=LINE('',#109119,#12464);
#9628=LINE('',#109553,#12465);
#9629=LINE('',#109989,#12466);
#9630=LINE('',#110498,#12467);
#9631=LINE('',#110946,#12468);
#9632=LINE('',#111392,#12469);
#9633=LINE('',#111849,#12470);
#9634=LINE('',#112309,#12471);
#9635=LINE('',#112761,#12472);
#9636=LINE('',#113257,#12473);
#9637=LINE('',#113691,#12474);
#9638=LINE('',#114151,#12475);
#9639=LINE('',#114548,#12476);
#9640=LINE('',#114990,#12477);
#9641=LINE('',#115432,#12478);
#9642=LINE('',#115832,#12479);
#9643=LINE('',#116052,#12480);
#9644=LINE('',#116529,#12481);
#9645=LINE('',#116947,#12482);
#9646=LINE('',#117361,#12483);
#9647=LINE('',#117835,#12484);
#9648=LINE('',#118270,#12485);
#9649=LINE('',#118700,#12486);
#9650=LINE('',#119140,#12487);
#9651=LINE('',#119570,#12488);
#9652=LINE('',#120080,#12489);
#9653=LINE('',#120512,#12490);
#9654=LINE('',#120930,#12491);
#9655=LINE('',#121376,#12492);
#9656=LINE('',#121842,#12493);
#9657=LINE('',#122269,#12494);
#9658=LINE('',#122693,#12495);
#9659=LINE('',#123121,#12496);
#9660=LINE('',#123562,#12497);
#9661=LINE('',#125944,#12498);
#9662=LINE('',#125952,#12499);
#9663=LINE('',#125953,#12500);
#9664=LINE('',#125956,#12501);
#9665=LINE('',#125958,#12502);
#9666=LINE('',#125964,#12503);
#9667=LINE('',#125973,#12504);
#9668=LINE('',#125980,#12505);
#9669=LINE('',#125984,#12506);
#9670=LINE('',#125988,#12507);
#9671=LINE('',#125992,#12508);
#9672=LINE('',#125996,#12509);
#9673=LINE('',#126000,#12510);
#9674=LINE('',#126004,#12511);
#9675=LINE('',#126008,#12512);
#9676=LINE('',#126012,#12513);
#9677=LINE('',#126016,#12514);
#9678=LINE('',#126020,#12515);
#9679=LINE('',#126024,#12516);
#9680=LINE('',#126028,#12517);
#9681=LINE('',#126032,#12518);
#9682=LINE('',#126036,#12519);
#9683=LINE('',#126040,#12520);
#9684=LINE('',#126044,#12521);
#9685=LINE('',#126048,#12522);
#9686=LINE('',#126052,#12523);
#9687=LINE('',#126056,#12524);
#9688=LINE('',#126060,#12525);
#9689=LINE('',#126064,#12526);
#9690=LINE('',#126068,#12527);
#9691=LINE('',#126072,#12528);
#9692=LINE('',#126076,#12529);
#9693=LINE('',#126080,#12530);
#9694=LINE('',#126084,#12531);
#9695=LINE('',#126088,#12532);
#9696=LINE('',#126092,#12533);
#9697=LINE('',#126096,#12534);
#9698=LINE('',#126100,#12535);
#9699=LINE('',#126104,#12536);
#9700=LINE('',#126108,#12537);
#9701=LINE('',#126113,#12538);
#9702=LINE('',#126117,#12539);
#9703=LINE('',#126121,#12540);
#9704=LINE('',#126125,#12541);
#9705=LINE('',#126129,#12542);
#9706=LINE('',#126133,#12543);
#9707=LINE('',#126137,#12544);
#9708=LINE('',#126141,#12545);
#9709=LINE('',#126145,#12546);
#9710=LINE('',#126149,#12547);
#9711=LINE('',#126153,#12548);
#9712=LINE('',#126157,#12549);
#9713=LINE('',#126161,#12550);
#9714=LINE('',#126165,#12551);
#9715=LINE('',#126169,#12552);
#9716=LINE('',#126173,#12553);
#9717=LINE('',#126177,#12554);
#9718=LINE('',#126181,#12555);
#9719=LINE('',#126185,#12556);
#9720=LINE('',#126189,#12557);
#9721=LINE('',#126193,#12558);
#9722=LINE('',#126197,#12559);
#9723=LINE('',#126201,#12560);
#9724=LINE('',#126205,#12561);
#9725=LINE('',#126209,#12562);
#9726=LINE('',#126213,#12563);
#9727=LINE('',#126217,#12564);
#9728=LINE('',#126221,#12565);
#9729=LINE('',#126225,#12566);
#9730=LINE('',#126229,#12567);
#9731=LINE('',#126233,#12568);
#9732=LINE('',#126237,#12569);
#9733=LINE('',#126241,#12570);
#9734=LINE('',#126245,#12571);
#9735=LINE('',#126249,#12572);
#9736=LINE('',#126253,#12573);
#9737=LINE('',#126256,#12574);
#9738=LINE('',#126259,#12575);
#9739=LINE('',#126261,#12576);
#9740=LINE('',#126269,#12577);
#9741=LINE('',#126511,#12578);
#9742=LINE('',#126515,#12579);
#9743=LINE('',#126516,#12580);
#9744=LINE('',#126518,#12581);
#9745=LINE('',#126522,#12582);
#9746=LINE('',#126523,#12583);
#9747=LINE('',#126525,#12584);
#9748=LINE('',#126529,#12585);
#9749=LINE('',#126530,#12586);
#9750=LINE('',#126532,#12587);
#9751=LINE('',#126536,#12588);
#9752=LINE('',#126537,#12589);
#9753=LINE('',#126539,#12590);
#9754=LINE('',#126543,#12591);
#9755=LINE('',#126544,#12592);
#9756=LINE('',#126546,#12593);
#9757=LINE('',#126550,#12594);
#9758=LINE('',#126551,#12595);
#9759=LINE('',#126553,#12596);
#9760=LINE('',#126557,#12597);
#9761=LINE('',#126558,#12598);
#9762=LINE('',#126560,#12599);
#9763=LINE('',#126564,#12600);
#9764=LINE('',#126565,#12601);
#9765=LINE('',#126567,#12602);
#9766=LINE('',#126571,#12603);
#9767=LINE('',#126572,#12604);
#9768=LINE('',#126574,#12605);
#9769=LINE('',#126578,#12606);
#9770=LINE('',#126579,#12607);
#9771=LINE('',#126581,#12608);
#9772=LINE('',#126585,#12609);
#9773=LINE('',#126586,#12610);
#9774=LINE('',#126588,#12611);
#9775=LINE('',#126592,#12612);
#9776=LINE('',#126593,#12613);
#9777=LINE('',#126595,#12614);
#9778=LINE('',#126599,#12615);
#9779=LINE('',#126600,#12616);
#9780=LINE('',#126602,#12617);
#9781=LINE('',#126606,#12618);
#9782=LINE('',#126607,#12619);
#9783=LINE('',#126609,#12620);
#9784=LINE('',#126613,#12621);
#9785=LINE('',#126614,#12622);
#9786=LINE('',#126616,#12623);
#9787=LINE('',#126620,#12624);
#9788=LINE('',#126621,#12625);
#9789=LINE('',#126623,#12626);
#9790=LINE('',#126627,#12627);
#9791=LINE('',#126628,#12628);
#9792=LINE('',#126630,#12629);
#9793=LINE('',#126634,#12630);
#9794=LINE('',#126635,#12631);
#9795=LINE('',#126637,#12632);
#9796=LINE('',#126641,#12633);
#9797=LINE('',#126642,#12634);
#9798=LINE('',#126644,#12635);
#9799=LINE('',#126648,#12636);
#9800=LINE('',#126649,#12637);
#9801=LINE('',#126651,#12638);
#9802=LINE('',#126655,#12639);
#9803=LINE('',#126656,#12640);
#9804=LINE('',#126658,#12641);
#9805=LINE('',#126662,#12642);
#9806=LINE('',#126663,#12643);
#9807=LINE('',#126665,#12644);
#9808=LINE('',#126669,#12645);
#9809=LINE('',#126670,#12646);
#9810=LINE('',#126672,#12647);
#9811=LINE('',#126676,#12648);
#9812=LINE('',#126677,#12649);
#9813=LINE('',#126679,#12650);
#9814=LINE('',#126683,#12651);
#9815=LINE('',#126684,#12652);
#9816=LINE('',#126686,#12653);
#9817=LINE('',#126690,#12654);
#9818=LINE('',#126691,#12655);
#9819=LINE('',#126693,#12656);
#9820=LINE('',#126697,#12657);
#9821=LINE('',#126698,#12658);
#9822=LINE('',#126700,#12659);
#9823=LINE('',#126704,#12660);
#9824=LINE('',#126705,#12661);
#9825=LINE('',#126707,#12662);
#9826=LINE('',#126711,#12663);
#9827=LINE('',#126712,#12664);
#9828=LINE('',#126714,#12665);
#9829=LINE('',#126718,#12666);
#9830=LINE('',#126719,#12667);
#9831=LINE('',#126721,#12668);
#9832=LINE('',#126725,#12669);
#9833=LINE('',#126726,#12670);
#9834=LINE('',#126728,#12671);
#9835=LINE('',#126732,#12672);
#9836=LINE('',#126733,#12673);
#9837=LINE('',#126735,#12674);
#9838=LINE('',#126739,#12675);
#9839=LINE('',#126740,#12676);
#9840=LINE('',#126742,#12677);
#9841=LINE('',#126746,#12678);
#9842=LINE('',#126747,#12679);
#9843=LINE('',#126749,#12680);
#9844=LINE('',#126817,#12681);
#9845=LINE('',#126820,#12682);
#9846=LINE('',#126822,#12683);
#9847=LINE('',#126826,#12684);
#9848=LINE('',#126829,#12685);
#9849=LINE('',#126832,#12686);
#9850=LINE('',#126834,#12687);
#9851=LINE('',#126838,#12688);
#9852=LINE('',#126841,#12689);
#9853=LINE('',#126844,#12690);
#9854=LINE('',#126846,#12691);
#9855=LINE('',#126850,#12692);
#9856=LINE('',#126853,#12693);
#9857=LINE('',#126855,#12694);
#9858=LINE('',#126857,#12695);
#9859=LINE('',#126859,#12696);
#9860=LINE('',#126860,#12697);
#9861=LINE('',#126862,#12698);
#9862=LINE('',#126864,#12699);
#9863=LINE('',#126865,#12700);
#9864=LINE('',#126867,#12701);
#9865=LINE('',#126869,#12702);
#9866=LINE('',#126870,#12703);
#9867=LINE('',#126874,#12704);
#9868=LINE('',#126877,#12705);
#9869=LINE('',#126879,#12706);
#9870=LINE('',#126883,#12707);
#9871=LINE('',#126886,#12708);
#9872=LINE('',#126895,#12709);
#9873=LINE('',#126899,#12710);
#9874=LINE('',#126901,#12711);
#9875=LINE('',#126902,#12712);
#12460=VECTOR('',#40029,1.4635);
#12461=VECTOR('',#40034,1.4635);
#12462=VECTOR('',#40037,1.4635);
#12463=VECTOR('',#40040,1.4635);
#12464=VECTOR('',#40043,1.4635);
#12465=VECTOR('',#40046,1.4635);
#12466=VECTOR('',#40049,1.4635);
#12467=VECTOR('',#40052,1.4635);
#12468=VECTOR('',#40055,1.4635);
#12469=VECTOR('',#40058,1.4635);
#12470=VECTOR('',#40061,1.4635);
#12471=VECTOR('',#40064,1.4635);
#12472=VECTOR('',#40067,1.4635);
#12473=VECTOR('',#40070,1.4635);
#12474=VECTOR('',#40073,1.4635);
#12475=VECTOR('',#40076,1.4635);
#12476=VECTOR('',#40079,1.4635);
#12477=VECTOR('',#40082,1.4635);
#12478=VECTOR('',#40085,1.4635);
#12479=VECTOR('',#40088,1.17775);
#12480=VECTOR('',#40093,1.17775);
#12481=VECTOR('',#40096,1.17775);
#12482=VECTOR('',#40099,1.17775);
#12483=VECTOR('',#40102,1.17775);
#12484=VECTOR('',#40105,1.17775);
#12485=VECTOR('',#40108,1.17775);
#12486=VECTOR('',#40111,1.17775);
#12487=VECTOR('',#40114,1.17775);
#12488=VECTOR('',#40117,1.17775);
#12489=VECTOR('',#40120,1.17775);
#12490=VECTOR('',#40123,1.17775);
#12491=VECTOR('',#40126,1.17775);
#12492=VECTOR('',#40129,1.17775);
#12493=VECTOR('',#40132,1.17775);
#12494=VECTOR('',#40135,1.17775);
#12495=VECTOR('',#40138,1.17775);
#12496=VECTOR('',#40141,1.17775);
#12497=VECTOR('',#40144,1.17775);
#12498=VECTOR('',#40177,1.2885);
#12499=VECTOR('',#40186,10.);
#12500=VECTOR('',#40187,10.);
#12501=VECTOR('',#40190,10.);
#12502=VECTOR('',#40191,10.);
#12503=VECTOR('',#40194,10.);
#12504=VECTOR('',#40199,2.75);
#12505=VECTOR('',#40206,10.);
#12506=VECTOR('',#40209,10.);
#12507=VECTOR('',#40212,10.);
#12508=VECTOR('',#40215,10.);
#12509=VECTOR('',#40218,10.);
#12510=VECTOR('',#40221,10.);
#12511=VECTOR('',#40224,10.);
#12512=VECTOR('',#40227,10.);
#12513=VECTOR('',#40230,10.);
#12514=VECTOR('',#40233,10.);
#12515=VECTOR('',#40236,10.);
#12516=VECTOR('',#40239,10.);
#12517=VECTOR('',#40242,10.);
#12518=VECTOR('',#40245,10.);
#12519=VECTOR('',#40248,10.);
#12520=VECTOR('',#40251,10.);
#12521=VECTOR('',#40254,10.);
#12522=VECTOR('',#40257,10.);
#12523=VECTOR('',#40260,10.);
#12524=VECTOR('',#40263,10.);
#12525=VECTOR('',#40266,10.);
#12526=VECTOR('',#40269,10.);
#12527=VECTOR('',#40272,10.);
#12528=VECTOR('',#40275,10.);
#12529=VECTOR('',#40278,10.);
#12530=VECTOR('',#40281,10.);
#12531=VECTOR('',#40284,10.);
#12532=VECTOR('',#40287,10.);
#12533=VECTOR('',#40290,10.);
#12534=VECTOR('',#40293,10.);
#12535=VECTOR('',#40296,10.);
#12536=VECTOR('',#40299,10.);
#12537=VECTOR('',#40302,10.);
#12538=VECTOR('',#40307,10.);
#12539=VECTOR('',#40310,10.);
#12540=VECTOR('',#40313,10.);
#12541=VECTOR('',#40316,10.);
#12542=VECTOR('',#40319,10.);
#12543=VECTOR('',#40322,10.);
#12544=VECTOR('',#40325,10.);
#12545=VECTOR('',#40328,10.);
#12546=VECTOR('',#40331,10.);
#12547=VECTOR('',#40334,10.);
#12548=VECTOR('',#40337,10.);
#12549=VECTOR('',#40340,10.);
#12550=VECTOR('',#40343,10.);
#12551=VECTOR('',#40346,10.);
#12552=VECTOR('',#40349,10.);
#12553=VECTOR('',#40352,10.);
#12554=VECTOR('',#40355,10.);
#12555=VECTOR('',#40358,10.);
#12556=VECTOR('',#40361,10.);
#12557=VECTOR('',#40364,10.);
#12558=VECTOR('',#40367,10.);
#12559=VECTOR('',#40370,10.);
#12560=VECTOR('',#40373,10.);
#12561=VECTOR('',#40376,10.);
#12562=VECTOR('',#40379,10.);
#12563=VECTOR('',#40382,10.);
#12564=VECTOR('',#40385,10.);
#12565=VECTOR('',#40388,10.);
#12566=VECTOR('',#40391,10.);
#12567=VECTOR('',#40394,10.);
#12568=VECTOR('',#40397,10.);
#12569=VECTOR('',#40400,10.);
#12570=VECTOR('',#40403,10.);
#12571=VECTOR('',#40406,10.);
#12572=VECTOR('',#40409,10.);
#12573=VECTOR('',#40412,10.);
#12574=VECTOR('',#40415,10.);
#12575=VECTOR('',#40418,10.);
#12576=VECTOR('',#40419,10.);
#12577=VECTOR('',#40422,10.);
#12578=VECTOR('',#40427,2.6);
#12579=VECTOR('',#40432,10.);
#12580=VECTOR('',#40433,10.);
#12581=VECTOR('',#40436,10.);
#12582=VECTOR('',#40441,10.);
#12583=VECTOR('',#40442,10.);
#12584=VECTOR('',#40445,10.);
#12585=VECTOR('',#40450,10.);
#12586=VECTOR('',#40451,10.);
#12587=VECTOR('',#40454,10.);
#12588=VECTOR('',#40459,10.);
#12589=VECTOR('',#40460,10.);
#12590=VECTOR('',#40463,10.);
#12591=VECTOR('',#40468,10.);
#12592=VECTOR('',#40469,10.);
#12593=VECTOR('',#40472,10.);
#12594=VECTOR('',#40477,10.);
#12595=VECTOR('',#40478,10.);
#12596=VECTOR('',#40481,10.);
#12597=VECTOR('',#40486,10.);
#12598=VECTOR('',#40487,10.);
#12599=VECTOR('',#40490,10.);
#12600=VECTOR('',#40495,10.);
#12601=VECTOR('',#40496,10.);
#12602=VECTOR('',#40499,10.);
#12603=VECTOR('',#40504,10.);
#12604=VECTOR('',#40505,10.);
#12605=VECTOR('',#40508,10.);
#12606=VECTOR('',#40513,10.);
#12607=VECTOR('',#40514,10.);
#12608=VECTOR('',#40517,10.);
#12609=VECTOR('',#40522,10.);
#12610=VECTOR('',#40523,10.);
#12611=VECTOR('',#40526,10.);
#12612=VECTOR('',#40531,10.);
#12613=VECTOR('',#40532,10.);
#12614=VECTOR('',#40535,10.);
#12615=VECTOR('',#40540,10.);
#12616=VECTOR('',#40541,10.);
#12617=VECTOR('',#40544,10.);
#12618=VECTOR('',#40549,10.);
#12619=VECTOR('',#40550,10.);
#12620=VECTOR('',#40553,10.);
#12621=VECTOR('',#40558,10.);
#12622=VECTOR('',#40559,10.);
#12623=VECTOR('',#40562,10.);
#12624=VECTOR('',#40567,10.);
#12625=VECTOR('',#40568,10.);
#12626=VECTOR('',#40571,10.);
#12627=VECTOR('',#40576,10.);
#12628=VECTOR('',#40577,10.);
#12629=VECTOR('',#40580,10.);
#12630=VECTOR('',#40585,10.);
#12631=VECTOR('',#40586,10.);
#12632=VECTOR('',#40589,10.);
#12633=VECTOR('',#40594,10.);
#12634=VECTOR('',#40595,10.);
#12635=VECTOR('',#40598,10.);
#12636=VECTOR('',#40603,10.);
#12637=VECTOR('',#40604,10.);
#12638=VECTOR('',#40607,10.);
#12639=VECTOR('',#40612,10.);
#12640=VECTOR('',#40613,9.99999999999999);
#12641=VECTOR('',#40616,10.);
#12642=VECTOR('',#40621,10.);
#12643=VECTOR('',#40622,10.);
#12644=VECTOR('',#40625,10.);
#12645=VECTOR('',#40630,10.);
#12646=VECTOR('',#40631,10.);
#12647=VECTOR('',#40634,10.);
#12648=VECTOR('',#40639,10.);
#12649=VECTOR('',#40640,10.);
#12650=VECTOR('',#40643,10.);
#12651=VECTOR('',#40648,10.);
#12652=VECTOR('',#40649,10.);
#12653=VECTOR('',#40652,10.);
#12654=VECTOR('',#40657,10.);
#12655=VECTOR('',#40658,10.);
#12656=VECTOR('',#40661,10.);
#12657=VECTOR('',#40666,10.);
#12658=VECTOR('',#40667,10.);
#12659=VECTOR('',#40670,10.);
#12660=VECTOR('',#40675,10.);
#12661=VECTOR('',#40676,10.);
#12662=VECTOR('',#40679,10.);
#12663=VECTOR('',#40684,9.99999999999999);
#12664=VECTOR('',#40685,10.);
#12665=VECTOR('',#40688,10.);
#12666=VECTOR('',#40693,10.);
#12667=VECTOR('',#40694,10.);
#12668=VECTOR('',#40697,10.);
#12669=VECTOR('',#40702,10.);
#12670=VECTOR('',#40703,10.);
#12671=VECTOR('',#40706,10.);
#12672=VECTOR('',#40711,10.);
#12673=VECTOR('',#40712,10.);
#12674=VECTOR('',#40715,10.);
#12675=VECTOR('',#40720,10.);
#12676=VECTOR('',#40721,10.);
#12677=VECTOR('',#40724,10.);
#12678=VECTOR('',#40729,10.);
#12679=VECTOR('',#40730,10.);
#12680=VECTOR('',#40733,10.);
#12681=VECTOR('',#40758,1.49337567297406);
#12682=VECTOR('',#40761,10.);
#12683=VECTOR('',#40762,10.);
#12684=VECTOR('',#40767,10.);
#12685=VECTOR('',#40770,10.);
#12686=VECTOR('',#40773,10.);
#12687=VECTOR('',#40774,10.);
#12688=VECTOR('',#40779,10.);
#12689=VECTOR('',#40782,10.);
#12690=VECTOR('',#40785,10.);
#12691=VECTOR('',#40786,10.);
#12692=VECTOR('',#40791,10.);
#12693=VECTOR('',#40794,10.);
#12694=VECTOR('',#40797,10.);
#12695=VECTOR('',#40798,10.);
#12696=VECTOR('',#40799,10.);
#12697=VECTOR('',#40800,10.);
#12698=VECTOR('',#40803,10.);
#12699=VECTOR('',#40804,10.);
#12700=VECTOR('',#40805,10.);
#12701=VECTOR('',#40808,10.);
#12702=VECTOR('',#40809,10.);
#12703=VECTOR('',#40810,10.);
#12704=VECTOR('',#40817,10.);
#12705=VECTOR('',#40822,10.);
#12706=VECTOR('',#40825,10.);
#12707=VECTOR('',#40828,10.);
#12708=VECTOR('',#40833,10.);
#12709=VECTOR('',#40850,10.);
#12710=VECTOR('',#40855,0.721687836487032);
#12711=VECTOR('',#40858,10.);
#12712=VECTOR('',#40859,10.);
#13119=CIRCLE('',#33858,1.4635);
#13120=CIRCLE('',#33878,1.17775);
#13121=CIRCLE('',#33898,1.17775);
#13122=CIRCLE('',#33900,1.4635);
#13123=CIRCLE('',#33902,1.4635);
#13124=CIRCLE('',#33903,1.4635);
#13125=CIRCLE('',#33905,1.4635);
#13126=CIRCLE('',#33906,1.4635);
#13127=CIRCLE('',#33908,1.5635);
#13128=CIRCLE('',#33909,0.1);
#13129=CIRCLE('',#33911,2.55);
#13130=CIRCLE('',#33913,1.1135);
#13131=CIRCLE('',#33916,2.75);
#13132=CIRCLE('',#33920,2.75);
#13133=CIRCLE('',#33921,2.75);
#13134=CIRCLE('',#33922,2.75);
#13135=CIRCLE('',#33923,2.75);
#13136=CIRCLE('',#33924,2.75);
#13137=CIRCLE('',#33925,2.75);
#13138=CIRCLE('',#33926,2.75);
#13139=CIRCLE('',#33927,2.75);
#13140=CIRCLE('',#33928,2.75);
#13141=CIRCLE('',#33929,2.75);
#13142=CIRCLE('',#33930,2.75);
#13143=CIRCLE('',#33931,2.75);
#13144=CIRCLE('',#33932,2.75);
#13145=CIRCLE('',#33933,2.75);
#13146=CIRCLE('',#33934,2.75);
#13147=CIRCLE('',#33935,2.75);
#13148=CIRCLE('',#33936,2.75);
#13149=CIRCLE('',#33937,2.75);
#13150=CIRCLE('',#33938,2.75);
#13151=CIRCLE('',#33939,2.75);
#13152=CIRCLE('',#33940,2.75);
#13153=CIRCLE('',#33941,2.75);
#13154=CIRCLE('',#33942,2.75);
#13155=CIRCLE('',#33943,2.75);
#13156=CIRCLE('',#33944,2.75);
#13157=CIRCLE('',#33945,2.75);
#13158=CIRCLE('',#33946,2.75);
#13159=CIRCLE('',#33947,2.75);
#13160=CIRCLE('',#33948,2.75);
#13161=CIRCLE('',#33949,2.75);
#13162=CIRCLE('',#33950,2.75);
#13163=CIRCLE('',#33951,2.75);
#13164=CIRCLE('',#33952,2.75);
#13165=CIRCLE('',#33953,2.75);
#13166=CIRCLE('',#33954,2.75);
#13167=CIRCLE('',#33955,2.75);
#13168=CIRCLE('',#33956,2.75);
#13169=CIRCLE('',#33957,2.75);
#13170=CIRCLE('',#33958,2.75);
#13171=CIRCLE('',#33959,2.75);
#13172=CIRCLE('',#33960,2.75);
#13173=CIRCLE('',#33961,2.75);
#13174=CIRCLE('',#33962,2.75);
#13175=CIRCLE('',#33963,2.75);
#13176=CIRCLE('',#33964,2.75);
#13177=CIRCLE('',#33965,2.75);
#13178=CIRCLE('',#33966,2.75);
#13179=CIRCLE('',#33967,2.75);
#13180=CIRCLE('',#33968,2.75);
#13181=CIRCLE('',#33969,2.75);
#13182=CIRCLE('',#33970,2.75);
#13183=CIRCLE('',#33971,2.75);
#13184=CIRCLE('',#33972,2.75);
#13185=CIRCLE('',#33973,2.75);
#13186=CIRCLE('',#33974,2.75);
#13187=CIRCLE('',#33975,2.75);
#13188=CIRCLE('',#33976,2.75);
#13189=CIRCLE('',#33977,2.75);
#13190=CIRCLE('',#33978,2.75);
#13191=CIRCLE('',#33979,2.75);
#13192=CIRCLE('',#33980,2.75);
#13193=CIRCLE('',#33981,2.75);
#13194=CIRCLE('',#33982,2.75);
#13195=CIRCLE('',#33983,2.75);
#13196=CIRCLE('',#33984,2.75);
#13197=CIRCLE('',#33985,2.75);
#13198=CIRCLE('',#33986,2.75);
#13199=CIRCLE('',#33987,2.75);
#13200=CIRCLE('',#33988,2.75);
#13201=CIRCLE('',#33989,2.75);
#13202=CIRCLE('',#33990,2.75);
#13203=CIRCLE('',#33991,2.75);
#13204=CIRCLE('',#33992,2.75);
#13205=CIRCLE('',#33993,2.75);
#13206=CIRCLE('',#33998,2.45);
#13207=CIRCLE('',#34102,0.2);
#13208=CIRCLE('',#34104,1.59337567297406);
#13209=CIRCLE('',#34106,1.39337567297406);
#13210=CIRCLE('',#34107,1.39337567297406);
#13211=CIRCLE('',#34108,1.39337567297406);
#13212=CIRCLE('',#34109,1.39337567297406);
#13213=CIRCLE('',#34110,1.39337567297406);
#13214=CIRCLE('',#34111,1.39337567297406);
#13215=CIRCLE('',#34113,1.39337567297406);
#13216=CIRCLE('',#34115,1.39337567297406);
#13217=CIRCLE('',#34117,1.39337567297406);
#13218=CIRCLE('',#34119,1.39337567297406);
#13219=CIRCLE('',#34121,1.39337567297406);
#13220=CIRCLE('',#34123,1.39337567297406);
#13221=CIRCLE('',#34134,1.44337567297406);
#13222=CIRCLE('',#34136,1.44337567297406);
#13223=CIRCLE('',#34138,1.44337567297406);
#13224=CIRCLE('',#34140,1.44337567297406);
#13225=CIRCLE('',#34142,1.44337567297406);
#13226=CIRCLE('',#34144,1.44337567297406);
#15899=VERTEX_POINT('',#107627);
#15900=VERTEX_POINT('',#107628);
#15901=VERTEX_POINT('',#107630);
#15902=VERTEX_POINT('',#107757);
#15903=VERTEX_POINT('',#107791);
#15904=VERTEX_POINT('',#107792);
#15905=VERTEX_POINT('',#108211);
#15906=VERTEX_POINT('',#108212);
#15907=VERTEX_POINT('',#108663);
#15908=VERTEX_POINT('',#108664);
#15909=VERTEX_POINT('',#108894);
#15910=VERTEX_POINT('',#109117);
#15911=VERTEX_POINT('',#109118);
#15912=VERTEX_POINT('',#109551);
#15913=VERTEX_POINT('',#109552);
#15914=VERTEX_POINT('',#109987);
#15915=VERTEX_POINT('',#109988);
#15916=VERTEX_POINT('',#109990);
#15917=VERTEX_POINT('',#110496);
#15918=VERTEX_POINT('',#110497);
#15919=VERTEX_POINT('',#110944);
#15920=VERTEX_POINT('',#110945);
#15921=VERTEX_POINT('',#111390);
#15922=VERTEX_POINT('',#111391);
#15923=VERTEX_POINT('',#111623);
#15924=VERTEX_POINT('',#111847);
#15925=VERTEX_POINT('',#111848);
#15926=VERTEX_POINT('',#112307);
#15927=VERTEX_POINT('',#112308);
#15928=VERTEX_POINT('',#112759);
#15929=VERTEX_POINT('',#112760);
#15930=VERTEX_POINT('',#113255);
#15931=VERTEX_POINT('',#113256);
#15932=VERTEX_POINT('',#113689);
#15933=VERTEX_POINT('',#113690);
#15934=VERTEX_POINT('',#114149);
#15935=VERTEX_POINT('',#114150);
#15936=VERTEX_POINT('',#114152);
#15937=VERTEX_POINT('',#114546);
#15938=VERTEX_POINT('',#114547);
#15939=VERTEX_POINT('',#114988);
#15940=VERTEX_POINT('',#114989);
#15941=VERTEX_POINT('',#115430);
#15942=VERTEX_POINT('',#115431);
#15943=VERTEX_POINT('',#115830);
#15944=VERTEX_POINT('',#115831);
#15945=VERTEX_POINT('',#115833);
#15946=VERTEX_POINT('',#115962);
#15947=VERTEX_POINT('',#116050);
#15948=VERTEX_POINT('',#116051);
#15949=VERTEX_POINT('',#116053);
#15950=VERTEX_POINT('',#116527);
#15951=VERTEX_POINT('',#116528);
#15952=VERTEX_POINT('',#116945);
#15953=VERTEX_POINT('',#116946);
#15954=VERTEX_POINT('',#117359);
#15955=VERTEX_POINT('',#117360);
#15956=VERTEX_POINT('',#117833);
#15957=VERTEX_POINT('',#117834);
#15958=VERTEX_POINT('',#117836);
#15959=VERTEX_POINT('',#118268);
#15960=VERTEX_POINT('',#118269);
#15961=VERTEX_POINT('',#118698);
#15962=VERTEX_POINT('',#118699);
#15963=VERTEX_POINT('',#119138);
#15964=VERTEX_POINT('',#119139);
#15965=VERTEX_POINT('',#119568);
#15966=VERTEX_POINT('',#119569);
#15967=VERTEX_POINT('',#120078);
#15968=VERTEX_POINT('',#120079);
#15969=VERTEX_POINT('',#120510);
#15970=VERTEX_POINT('',#120511);
#15971=VERTEX_POINT('',#120928);
#15972=VERTEX_POINT('',#120929);
#15973=VERTEX_POINT('',#121374);
#15974=VERTEX_POINT('',#121375);
#15975=VERTEX_POINT('',#121840);
#15976=VERTEX_POINT('',#121841);
#15977=VERTEX_POINT('',#121843);
#15978=VERTEX_POINT('',#122267);
#15979=VERTEX_POINT('',#122268);
#15980=VERTEX_POINT('',#122691);
#15981=VERTEX_POINT('',#122692);
#15982=VERTEX_POINT('',#123119);
#15983=VERTEX_POINT('',#123120);
#15984=VERTEX_POINT('',#123324);
#15985=VERTEX_POINT('',#123560);
#15986=VERTEX_POINT('',#123561);
#15987=VERTEX_POINT('',#123982);
#15988=VERTEX_POINT('',#124173);
#15989=VERTEX_POINT('',#124175);
#15990=VERTEX_POINT('',#124302);
#15991=VERTEX_POINT('',#124499);
#15992=VERTEX_POINT('',#124638);
#15993=VERTEX_POINT('',#124639);
#15994=VERTEX_POINT('',#125248);
#15995=VERTEX_POINT('',#125339);
#15996=VERTEX_POINT('',#125340);
#15997=VERTEX_POINT('',#125936);
#15998=VERTEX_POINT('',#125940);
#15999=VERTEX_POINT('',#125943);
#16000=VERTEX_POINT('',#125948);
#16001=VERTEX_POINT('',#125949);
#16002=VERTEX_POINT('',#125951);
#16003=VERTEX_POINT('',#125955);
#16004=VERTEX_POINT('',#125957);
#16005=VERTEX_POINT('',#125963);
#16006=VERTEX_POINT('',#125969);
#16007=VERTEX_POINT('',#125970);
#16008=VERTEX_POINT('',#125972);
#16009=VERTEX_POINT('',#125974);
#16010=VERTEX_POINT('',#125977);
#16011=VERTEX_POINT('',#125979);
#16012=VERTEX_POINT('',#125981);
#16013=VERTEX_POINT('',#125983);
#16014=VERTEX_POINT('',#125985);
#16015=VERTEX_POINT('',#125987);
#16016=VERTEX_POINT('',#125989);
#16017=VERTEX_POINT('',#125991);
#16018=VERTEX_POINT('',#125993);
#16019=VERTEX_POINT('',#125995);
#16020=VERTEX_POINT('',#125997);
#16021=VERTEX_POINT('',#125999);
#16022=VERTEX_POINT('',#126001);
#16023=VERTEX_POINT('',#126003);
#16024=VERTEX_POINT('',#126005);
#16025=VERTEX_POINT('',#126007);
#16026=VERTEX_POINT('',#126009);
#16027=VERTEX_POINT('',#126011);
#16028=VERTEX_POINT('',#126013);
#16029=VERTEX_POINT('',#126015);
#16030=VERTEX_POINT('',#126017);
#16031=VERTEX_POINT('',#126019);
#16032=VERTEX_POINT('',#126021);
#16033=VERTEX_POINT('',#126023);
#16034=VERTEX_POINT('',#126025);
#16035=VERTEX_POINT('',#126027);
#16036=VERTEX_POINT('',#126029);
#16037=VERTEX_POINT('',#126031);
#16038=VERTEX_POINT('',#126033);
#16039=VERTEX_POINT('',#126035);
#16040=VERTEX_POINT('',#126037);
#16041=VERTEX_POINT('',#126039);
#16042=VERTEX_POINT('',#126041);
#16043=VERTEX_POINT('',#126043);
#16044=VERTEX_POINT('',#126045);
#16045=VERTEX_POINT('',#126047);
#16046=VERTEX_POINT('',#126049);
#16047=VERTEX_POINT('',#126051);
#16048=VERTEX_POINT('',#126053);
#16049=VERTEX_POINT('',#126055);
#16050=VERTEX_POINT('',#126057);
#16051=VERTEX_POINT('',#126059);
#16052=VERTEX_POINT('',#126061);
#16053=VERTEX_POINT('',#126063);
#16054=VERTEX_POINT('',#126065);
#16055=VERTEX_POINT('',#126067);
#16056=VERTEX_POINT('',#126069);
#16057=VERTEX_POINT('',#126071);
#16058=VERTEX_POINT('',#126073);
#16059=VERTEX_POINT('',#126075);
#16060=VERTEX_POINT('',#126077);
#16061=VERTEX_POINT('',#126079);
#16062=VERTEX_POINT('',#126081);
#16063=VERTEX_POINT('',#126083);
#16064=VERTEX_POINT('',#126085);
#16065=VERTEX_POINT('',#126087);
#16066=VERTEX_POINT('',#126089);
#16067=VERTEX_POINT('',#126091);
#16068=VERTEX_POINT('',#126093);
#16069=VERTEX_POINT('',#126095);
#16070=VERTEX_POINT('',#126097);
#16071=VERTEX_POINT('',#126099);
#16072=VERTEX_POINT('',#126101);
#16073=VERTEX_POINT('',#126103);
#16074=VERTEX_POINT('',#126105);
#16075=VERTEX_POINT('',#126107);
#16076=VERTEX_POINT('',#126110);
#16077=VERTEX_POINT('',#126112);
#16078=VERTEX_POINT('',#126114);
#16079=VERTEX_POINT('',#126116);
#16080=VERTEX_POINT('',#126118);
#16081=VERTEX_POINT('',#126120);
#16082=VERTEX_POINT('',#126122);
#16083=VERTEX_POINT('',#126124);
#16084=VERTEX_POINT('',#126126);
#16085=VERTEX_POINT('',#126128);
#16086=VERTEX_POINT('',#126130);
#16087=VERTEX_POINT('',#126132);
#16088=VERTEX_POINT('',#126134);
#16089=VERTEX_POINT('',#126136);
#16090=VERTEX_POINT('',#126138);
#16091=VERTEX_POINT('',#126140);
#16092=VERTEX_POINT('',#126142);
#16093=VERTEX_POINT('',#126144);
#16094=VERTEX_POINT('',#126146);
#16095=VERTEX_POINT('',#126148);
#16096=VERTEX_POINT('',#126150);
#16097=VERTEX_POINT('',#126152);
#16098=VERTEX_POINT('',#126154);
#16099=VERTEX_POINT('',#126156);
#16100=VERTEX_POINT('',#126158);
#16101=VERTEX_POINT('',#126160);
#16102=VERTEX_POINT('',#126162);
#16103=VERTEX_POINT('',#126164);
#16104=VERTEX_POINT('',#126166);
#16105=VERTEX_POINT('',#126168);
#16106=VERTEX_POINT('',#126170);
#16107=VERTEX_POINT('',#126172);
#16108=VERTEX_POINT('',#126174);
#16109=VERTEX_POINT('',#126176);
#16110=VERTEX_POINT('',#126178);
#16111=VERTEX_POINT('',#126180);
#16112=VERTEX_POINT('',#126182);
#16113=VERTEX_POINT('',#126184);
#16114=VERTEX_POINT('',#126186);
#16115=VERTEX_POINT('',#126188);
#16116=VERTEX_POINT('',#126190);
#16117=VERTEX_POINT('',#126192);
#16118=VERTEX_POINT('',#126194);
#16119=VERTEX_POINT('',#126196);
#16120=VERTEX_POINT('',#126198);
#16121=VERTEX_POINT('',#126200);
#16122=VERTEX_POINT('',#126202);
#16123=VERTEX_POINT('',#126204);
#16124=VERTEX_POINT('',#126206);
#16125=VERTEX_POINT('',#126208);
#16126=VERTEX_POINT('',#126210);
#16127=VERTEX_POINT('',#126212);
#16128=VERTEX_POINT('',#126214);
#16129=VERTEX_POINT('',#126216);
#16130=VERTEX_POINT('',#126218);
#16131=VERTEX_POINT('',#126220);
#16132=VERTEX_POINT('',#126222);
#16133=VERTEX_POINT('',#126224);
#16134=VERTEX_POINT('',#126226);
#16135=VERTEX_POINT('',#126228);
#16136=VERTEX_POINT('',#126230);
#16137=VERTEX_POINT('',#126232);
#16138=VERTEX_POINT('',#126234);
#16139=VERTEX_POINT('',#126236);
#16140=VERTEX_POINT('',#126238);
#16141=VERTEX_POINT('',#126240);
#16142=VERTEX_POINT('',#126242);
#16143=VERTEX_POINT('',#126244);
#16144=VERTEX_POINT('',#126246);
#16145=VERTEX_POINT('',#126248);
#16146=VERTEX_POINT('',#126250);
#16147=VERTEX_POINT('',#126252);
#16148=VERTEX_POINT('',#126254);
#16149=VERTEX_POINT('',#126258);
#16150=VERTEX_POINT('',#126260);
#16151=VERTEX_POINT('',#126272);
#16152=VERTEX_POINT('',#126276);
#16153=VERTEX_POINT('',#126283);
#16154=VERTEX_POINT('',#126290);
#16155=VERTEX_POINT('',#126297);
#16156=VERTEX_POINT('',#126304);
#16157=VERTEX_POINT('',#126311);
#16158=VERTEX_POINT('',#126318);
#16159=VERTEX_POINT('',#126325);
#16160=VERTEX_POINT('',#126332);
#16161=VERTEX_POINT('',#126339);
#16162=VERTEX_POINT('',#126346);
#16163=VERTEX_POINT('',#126353);
#16164=VERTEX_POINT('',#126360);
#16165=VERTEX_POINT('',#126367);
#16166=VERTEX_POINT('',#126374);
#16167=VERTEX_POINT('',#126381);
#16168=VERTEX_POINT('',#126388);
#16169=VERTEX_POINT('',#126395);
#16170=VERTEX_POINT('',#126402);
#16171=VERTEX_POINT('',#126409);
#16172=VERTEX_POINT('',#126416);
#16173=VERTEX_POINT('',#126423);
#16174=VERTEX_POINT('',#126430);
#16175=VERTEX_POINT('',#126437);
#16176=VERTEX_POINT('',#126444);
#16177=VERTEX_POINT('',#126451);
#16178=VERTEX_POINT('',#126458);
#16179=VERTEX_POINT('',#126465);
#16180=VERTEX_POINT('',#126472);
#16181=VERTEX_POINT('',#126479);
#16182=VERTEX_POINT('',#126486);
#16183=VERTEX_POINT('',#126493);
#16184=VERTEX_POINT('',#126500);
#16185=VERTEX_POINT('',#126510);
#16186=VERTEX_POINT('',#126514);
#16187=VERTEX_POINT('',#126521);
#16188=VERTEX_POINT('',#126528);
#16189=VERTEX_POINT('',#126535);
#16190=VERTEX_POINT('',#126542);
#16191=VERTEX_POINT('',#126549);
#16192=VERTEX_POINT('',#126556);
#16193=VERTEX_POINT('',#126563);
#16194=VERTEX_POINT('',#126570);
#16195=VERTEX_POINT('',#126577);
#16196=VERTEX_POINT('',#126584);
#16197=VERTEX_POINT('',#126591);
#16198=VERTEX_POINT('',#126598);
#16199=VERTEX_POINT('',#126605);
#16200=VERTEX_POINT('',#126612);
#16201=VERTEX_POINT('',#126619);
#16202=VERTEX_POINT('',#126626);
#16203=VERTEX_POINT('',#126633);
#16204=VERTEX_POINT('',#126640);
#16205=VERTEX_POINT('',#126647);
#16206=VERTEX_POINT('',#126654);
#16207=VERTEX_POINT('',#126661);
#16208=VERTEX_POINT('',#126668);
#16209=VERTEX_POINT('',#126675);
#16210=VERTEX_POINT('',#126682);
#16211=VERTEX_POINT('',#126689);
#16212=VERTEX_POINT('',#126696);
#16213=VERTEX_POINT('',#126703);
#16214=VERTEX_POINT('',#126710);
#16215=VERTEX_POINT('',#126717);
#16216=VERTEX_POINT('',#126724);
#16217=VERTEX_POINT('',#126731);
#16218=VERTEX_POINT('',#126738);
#16219=VERTEX_POINT('',#126745);
#16220=VERTEX_POINT('',#126754);
#16221=VERTEX_POINT('',#126757);
#16222=VERTEX_POINT('',#126758);
#16223=VERTEX_POINT('',#126762);
#16224=VERTEX_POINT('',#126764);
#16225=VERTEX_POINT('',#126768);
#16226=VERTEX_POINT('',#126772);
#16227=VERTEX_POINT('',#126774);
#16228=VERTEX_POINT('',#126778);
#16229=VERTEX_POINT('',#126782);
#16230=VERTEX_POINT('',#126784);
#16231=VERTEX_POINT('',#126788);
#16232=VERTEX_POINT('',#126792);
#16233=VERTEX_POINT('',#126794);
#16234=VERTEX_POINT('',#126798);
#16235=VERTEX_POINT('',#126802);
#16236=VERTEX_POINT('',#126804);
#16237=VERTEX_POINT('',#126808);
#16238=VERTEX_POINT('',#126812);
#16239=VERTEX_POINT('',#126819);
#16240=VERTEX_POINT('',#126821);
#16241=VERTEX_POINT('',#126825);
#16242=VERTEX_POINT('',#126827);
#16243=VERTEX_POINT('',#126831);
#16244=VERTEX_POINT('',#126833);
#16245=VERTEX_POINT('',#126837);
#16246=VERTEX_POINT('',#126839);
#16247=VERTEX_POINT('',#126843);
#16248=VERTEX_POINT('',#126845);
#16249=VERTEX_POINT('',#126849);
#16250=VERTEX_POINT('',#126851);
#16251=VERTEX_POINT('',#126856);
#16252=VERTEX_POINT('',#126858);
#16253=VERTEX_POINT('',#126863);
#16254=VERTEX_POINT('',#126868);
#16255=VERTEX_POINT('',#126881);
#16256=VERTEX_POINT('',#126882);
#16257=VERTEX_POINT('',#126898);
#20319=EDGE_CURVE('',#15899,#15900,#9623,.T.);
#20320=EDGE_CURVE('',#15899,#15901,#1553,.T.);
#20321=EDGE_CURVE('',#15902,#15901,#13119,.T.);
#20322=EDGE_CURVE('',#15902,#15900,#1554,.T.);
#20323=EDGE_CURVE('',#15903,#15904,#9624,.T.);
#20324=EDGE_CURVE('',#15903,#15899,#1555,.T.);
#20325=EDGE_CURVE('',#15900,#15904,#1556,.T.);
#20326=EDGE_CURVE('',#15905,#15906,#9625,.T.);
#20327=EDGE_CURVE('',#15905,#15903,#1557,.T.);
#20328=EDGE_CURVE('',#15904,#15906,#1558,.T.);
#20329=EDGE_CURVE('',#15907,#15908,#9626,.T.);
#20330=EDGE_CURVE('',#15907,#15905,#1559,.T.);
#20331=EDGE_CURVE('',#15906,#15909,#1560,.T.);
#20332=EDGE_CURVE('',#15909,#15908,#1561,.T.);
#20333=EDGE_CURVE('',#15910,#15911,#9627,.T.);
#20334=EDGE_CURVE('',#15910,#15907,#1562,.T.);
#20335=EDGE_CURVE('',#15908,#15911,#1563,.T.);
#20336=EDGE_CURVE('',#15912,#15913,#9628,.T.);
#20337=EDGE_CURVE('',#15912,#15910,#1564,.T.);
#20338=EDGE_CURVE('',#15911,#15913,#1565,.T.);
#20339=EDGE_CURVE('',#15914,#15915,#9629,.T.);
#20340=EDGE_CURVE('',#15914,#15916,#1566,.T.);
#20341=EDGE_CURVE('',#15916,#15912,#1567,.T.);
#20342=EDGE_CURVE('',#15913,#15915,#1568,.T.);
#20343=EDGE_CURVE('',#15917,#15918,#9630,.T.);
#20344=EDGE_CURVE('',#15917,#15914,#1569,.T.);
#20345=EDGE_CURVE('',#15915,#15918,#1570,.T.);
#20346=EDGE_CURVE('',#15919,#15920,#9631,.T.);
#20347=EDGE_CURVE('',#15919,#15917,#1571,.T.);
#20348=EDGE_CURVE('',#15918,#15920,#1572,.T.);
#20349=EDGE_CURVE('',#15921,#15922,#9632,.T.);
#20350=EDGE_CURVE('',#15921,#15919,#1573,.T.);
#20351=EDGE_CURVE('',#15920,#15923,#1574,.T.);
#20352=EDGE_CURVE('',#15923,#15922,#1575,.T.);
#20353=EDGE_CURVE('',#15924,#15925,#9633,.T.);
#20354=EDGE_CURVE('',#15924,#15921,#1576,.T.);
#20355=EDGE_CURVE('',#15922,#15925,#1577,.T.);
#20356=EDGE_CURVE('',#15926,#15927,#9634,.T.);
#20357=EDGE_CURVE('',#15926,#15924,#1578,.T.);
#20358=EDGE_CURVE('',#15925,#15927,#1579,.T.);
#20359=EDGE_CURVE('',#15928,#15929,#9635,.T.);
#20360=EDGE_CURVE('',#15928,#15926,#1580,.T.);
#20361=EDGE_CURVE('',#15927,#15929,#1581,.T.);
#20362=EDGE_CURVE('',#15930,#15931,#9636,.T.);
#20363=EDGE_CURVE('',#15930,#15928,#1582,.T.);
#20364=EDGE_CURVE('',#15929,#15931,#1583,.T.);
#20365=EDGE_CURVE('',#15932,#15933,#9637,.T.);
#20366=EDGE_CURVE('',#15932,#15930,#1584,.T.);
#20367=EDGE_CURVE('',#15931,#15933,#1585,.T.);
#20368=EDGE_CURVE('',#15934,#15935,#9638,.T.);
#20369=EDGE_CURVE('',#15934,#15936,#1586,.T.);
#20370=EDGE_CURVE('',#15936,#15932,#1587,.T.);
#20371=EDGE_CURVE('',#15933,#15935,#1588,.T.);
#20372=EDGE_CURVE('',#15937,#15938,#9639,.T.);
#20373=EDGE_CURVE('',#15937,#15934,#1589,.T.);
#20374=EDGE_CURVE('',#15935,#15938,#1590,.T.);
#20375=EDGE_CURVE('',#15939,#15940,#9640,.T.);
#20376=EDGE_CURVE('',#15939,#15937,#1591,.T.);
#20377=EDGE_CURVE('',#15938,#15940,#1592,.T.);
#20378=EDGE_CURVE('',#15941,#15942,#9641,.T.);
#20379=EDGE_CURVE('',#15941,#15939,#1593,.T.);
#20380=EDGE_CURVE('',#15940,#15942,#1594,.T.);
#20381=EDGE_CURVE('',#15943,#15944,#9642,.T.);
#20382=EDGE_CURVE('',#15945,#15943,#1595,.T.);
#20383=EDGE_CURVE('',#15946,#15945,#13120,.T.);
#20384=EDGE_CURVE('',#15946,#15944,#1596,.T.);
#20385=EDGE_CURVE('',#15947,#15948,#9643,.T.);
#20386=EDGE_CURVE('',#15949,#15947,#1597,.F.);
#20387=EDGE_CURVE('',#15943,#15949,#1598,.T.);
#20388=EDGE_CURVE('',#15944,#15948,#1599,.T.);
#20389=EDGE_CURVE('',#15950,#15951,#9644,.T.);
#20390=EDGE_CURVE('',#15947,#15950,#1600,.F.);
#20391=EDGE_CURVE('',#15948,#15951,#1601,.T.);
#20392=EDGE_CURVE('',#15952,#15953,#9645,.T.);
#20393=EDGE_CURVE('',#15950,#15952,#1602,.F.);
#20394=EDGE_CURVE('',#15951,#15953,#1603,.T.);
#20395=EDGE_CURVE('',#15954,#15955,#9646,.T.);
#20396=EDGE_CURVE('',#15952,#15954,#1604,.F.);
#20397=EDGE_CURVE('',#15953,#15955,#1605,.T.);
#20398=EDGE_CURVE('',#15956,#15957,#9647,.T.);
#20399=EDGE_CURVE('',#15958,#15956,#1606,.F.);
#20400=EDGE_CURVE('',#15954,#15958,#1607,.F.);
#20401=EDGE_CURVE('',#15955,#15957,#1608,.T.);
#20402=EDGE_CURVE('',#15959,#15960,#9648,.T.);
#20403=EDGE_CURVE('',#15956,#15959,#1609,.F.);
#20404=EDGE_CURVE('',#15957,#15960,#1610,.T.);
#20405=EDGE_CURVE('',#15961,#15962,#9649,.T.);
#20406=EDGE_CURVE('',#15959,#15961,#1611,.F.);
#20407=EDGE_CURVE('',#15960,#15962,#1612,.T.);
#20408=EDGE_CURVE('',#15963,#15964,#9650,.T.);
#20409=EDGE_CURVE('',#15961,#15963,#1613,.F.);
#20410=EDGE_CURVE('',#15962,#15964,#1614,.T.);
#20411=EDGE_CURVE('',#15965,#15966,#9651,.T.);
#20412=EDGE_CURVE('',#15963,#15965,#1615,.F.);
#20413=EDGE_CURVE('',#15964,#15966,#1616,.T.);
#20414=EDGE_CURVE('',#15967,#15968,#9652,.T.);
#20415=EDGE_CURVE('',#15965,#15967,#1617,.F.);
#20416=EDGE_CURVE('',#15966,#15968,#1618,.T.);
#20417=EDGE_CURVE('',#15969,#15970,#9653,.T.);
#20418=EDGE_CURVE('',#15967,#15969,#1619,.F.);
#20419=EDGE_CURVE('',#15968,#15970,#1620,.T.);
#20420=EDGE_CURVE('',#15971,#15972,#9654,.T.);
#20421=EDGE_CURVE('',#15969,#15971,#1621,.F.);
#20422=EDGE_CURVE('',#15970,#15972,#1622,.T.);
#20423=EDGE_CURVE('',#15973,#15974,#9655,.T.);
#20424=EDGE_CURVE('',#15971,#15973,#1623,.F.);
#20425=EDGE_CURVE('',#15972,#15974,#1624,.T.);
#20426=EDGE_CURVE('',#15975,#15976,#9656,.T.);
#20427=EDGE_CURVE('',#15977,#15975,#1625,.F.);
#20428=EDGE_CURVE('',#15973,#15977,#1626,.F.);
#20429=EDGE_CURVE('',#15974,#15976,#1627,.T.);
#20430=EDGE_CURVE('',#15978,#15979,#9657,.T.);
#20431=EDGE_CURVE('',#15975,#15978,#1628,.F.);
#20432=EDGE_CURVE('',#15976,#15979,#1629,.T.);
#20433=EDGE_CURVE('',#15980,#15981,#9658,.T.);
#20434=EDGE_CURVE('',#15978,#15980,#1630,.F.);
#20435=EDGE_CURVE('',#15979,#15981,#1631,.T.);
#20436=EDGE_CURVE('',#15982,#15983,#9659,.T.);
#20437=EDGE_CURVE('',#15980,#15982,#1632,.F.);
#20438=EDGE_CURVE('',#15981,#15984,#1633,.T.);
#20439=EDGE_CURVE('',#15984,#15983,#1634,.T.);
#20440=EDGE_CURVE('',#15985,#15986,#9660,.T.);
#20441=EDGE_CURVE('',#15982,#15985,#1635,.F.);
#20442=EDGE_CURVE('',#15983,#15986,#1636,.T.);
#20443=EDGE_CURVE('',#15986,#15987,#1637,.T.);
#20444=EDGE_CURVE('',#15988,#15987,#13121,.T.);
#20445=EDGE_CURVE('',#15989,#15988,#1638,.T.);
#20446=EDGE_CURVE('',#15985,#15989,#1639,.T.);
#20447=EDGE_CURVE('',#15942,#15990,#1640,.T.);
#20448=EDGE_CURVE('',#15991,#15990,#13122,.T.);
#20449=EDGE_CURVE('',#15991,#15941,#1641,.T.);
#20450=EDGE_CURVE('',#15992,#15993,#13123,.T.);
#20451=EDGE_CURVE('',#15992,#15988,#1642,.T.);
#20452=EDGE_CURVE('',#15987,#15991,#1643,.T.);
#20453=EDGE_CURVE('',#15993,#15991,#13124,.T.);
#20454=EDGE_CURVE('',#15990,#15992,#1644,.T.);
#20455=EDGE_CURVE('',#15994,#15902,#1645,.T.);
#20456=EDGE_CURVE('',#15994,#15945,#1646,.T.);
#20457=EDGE_CURVE('',#15995,#15996,#13125,.T.);
#20458=EDGE_CURVE('',#15995,#15946,#1647,.T.);
#20459=EDGE_CURVE('',#15996,#15902,#13126,.T.);
#20460=EDGE_CURVE('',#15901,#15995,#1648,.T.);
#20461=EDGE_CURVE('',#15997,#15997,#13127,.T.);
#20462=EDGE_CURVE('',#15997,#15996,#13128,.T.);
#20463=EDGE_CURVE('',#15998,#15998,#13129,.T.);
#20464=EDGE_CURVE('',#15993,#15999,#9661,.T.);
#20465=EDGE_CURVE('',#15999,#15999,#13130,.T.);
#20466=EDGE_CURVE('',#16000,#16001,#13131,.T.);
#20467=EDGE_CURVE('',#16002,#16000,#9662,.T.);
#20468=EDGE_CURVE('',#16001,#16002,#9663,.T.);
#20469=EDGE_CURVE('',#16001,#16003,#9664,.T.);
#20470=EDGE_CURVE('',#16004,#16002,#9665,.T.);
#20471=EDGE_CURVE('',#16003,#16004,#200,.T.);
#20472=EDGE_CURVE('',#16005,#16000,#9666,.T.);
#20473=EDGE_CURVE('',#16004,#16005,#201,.T.);
#20474=EDGE_CURVE('',#16006,#16007,#13132,.T.);
#20475=EDGE_CURVE('',#16007,#16008,#9667,.T.);
#20476=EDGE_CURVE('',#16009,#16008,#13133,.T.);
#20477=EDGE_CURVE('',#16008,#16009,#13134,.T.);
#20478=EDGE_CURVE('',#16007,#16010,#13135,.T.);
#20479=EDGE_CURVE('',#16010,#16011,#9668,.T.);
#20480=EDGE_CURVE('',#16012,#16011,#13136,.T.);
#20481=EDGE_CURVE('',#16012,#16013,#9669,.T.);
#20482=EDGE_CURVE('',#16013,#16014,#13137,.T.);
#20483=EDGE_CURVE('',#16014,#16015,#9670,.T.);
#20484=EDGE_CURVE('',#16016,#16015,#13138,.T.);
#20485=EDGE_CURVE('',#16016,#16017,#9671,.T.);
#20486=EDGE_CURVE('',#16017,#16018,#13139,.T.);
#20487=EDGE_CURVE('',#16018,#16019,#9672,.T.);
#20488=EDGE_CURVE('',#16020,#16019,#13140,.T.);
#20489=EDGE_CURVE('',#16020,#16021,#9673,.T.);
#20490=EDGE_CURVE('',#16021,#16022,#13141,.T.);
#20491=EDGE_CURVE('',#16022,#16023,#9674,.T.);
#20492=EDGE_CURVE('',#16024,#16023,#13142,.T.);
#20493=EDGE_CURVE('',#16024,#16025,#9675,.T.);
#20494=EDGE_CURVE('',#16025,#16026,#13143,.T.);
#20495=EDGE_CURVE('',#16026,#16027,#9676,.T.);
#20496=EDGE_CURVE('',#16028,#16027,#13144,.T.);
#20497=EDGE_CURVE('',#16028,#16029,#9677,.T.);
#20498=EDGE_CURVE('',#16029,#16030,#13145,.T.);
#20499=EDGE_CURVE('',#16030,#16031,#9678,.T.);
#20500=EDGE_CURVE('',#16032,#16031,#13146,.T.);
#20501=EDGE_CURVE('',#16032,#16033,#9679,.T.);
#20502=EDGE_CURVE('',#16033,#16034,#13147,.T.);
#20503=EDGE_CURVE('',#16034,#16035,#9680,.T.);
#20504=EDGE_CURVE('',#16036,#16035,#13148,.T.);
#20505=EDGE_CURVE('',#16036,#16037,#9681,.T.);
#20506=EDGE_CURVE('',#16037,#16038,#13149,.T.);
#20507=EDGE_CURVE('',#16038,#16039,#9682,.T.);
#20508=EDGE_CURVE('',#16040,#16039,#13150,.T.);
#20509=EDGE_CURVE('',#16040,#16041,#9683,.T.);
#20510=EDGE_CURVE('',#16041,#16042,#13151,.T.);
#20511=EDGE_CURVE('',#16042,#16043,#9684,.T.);
#20512=EDGE_CURVE('',#16044,#16043,#13152,.T.);
#20513=EDGE_CURVE('',#16044,#16045,#9685,.T.);
#20514=EDGE_CURVE('',#16045,#16046,#13153,.T.);
#20515=EDGE_CURVE('',#16046,#16047,#9686,.T.);
#20516=EDGE_CURVE('',#16048,#16047,#13154,.T.);
#20517=EDGE_CURVE('',#16048,#16049,#9687,.T.);
#20518=EDGE_CURVE('',#16049,#16050,#13155,.T.);
#20519=EDGE_CURVE('',#16050,#16051,#9688,.T.);
#20520=EDGE_CURVE('',#16052,#16051,#13156,.T.);
#20521=EDGE_CURVE('',#16052,#16053,#9689,.T.);
#20522=EDGE_CURVE('',#16053,#16054,#13157,.T.);
#20523=EDGE_CURVE('',#16054,#16055,#9690,.T.);
#20524=EDGE_CURVE('',#16056,#16055,#13158,.T.);
#20525=EDGE_CURVE('',#16056,#16057,#9691,.T.);
#20526=EDGE_CURVE('',#16057,#16058,#13159,.T.);
#20527=EDGE_CURVE('',#16058,#16059,#9692,.T.);
#20528=EDGE_CURVE('',#16060,#16059,#13160,.T.);
#20529=EDGE_CURVE('',#16060,#16061,#9693,.T.);
#20530=EDGE_CURVE('',#16061,#16062,#13161,.T.);
#20531=EDGE_CURVE('',#16062,#16063,#9694,.T.);
#20532=EDGE_CURVE('',#16064,#16063,#13162,.T.);
#20533=EDGE_CURVE('',#16064,#16065,#9695,.T.);
#20534=EDGE_CURVE('',#16065,#16066,#13163,.T.);
#20535=EDGE_CURVE('',#16066,#16067,#9696,.T.);
#20536=EDGE_CURVE('',#16068,#16067,#13164,.T.);
#20537=EDGE_CURVE('',#16068,#16069,#9697,.T.);
#20538=EDGE_CURVE('',#16069,#16070,#13165,.T.);
#20539=EDGE_CURVE('',#16070,#16071,#9698,.T.);
#20540=EDGE_CURVE('',#16072,#16071,#13166,.T.);
#20541=EDGE_CURVE('',#16072,#16073,#9699,.T.);
#20542=EDGE_CURVE('',#16073,#16074,#13167,.T.);
#20543=EDGE_CURVE('',#16074,#16075,#9700,.T.);
#20544=EDGE_CURVE('',#16005,#16075,#13168,.T.);
#20545=EDGE_CURVE('',#16076,#16003,#13169,.T.);
#20546=EDGE_CURVE('',#16076,#16077,#9701,.T.);
#20547=EDGE_CURVE('',#16077,#16078,#13170,.T.);
#20548=EDGE_CURVE('',#16078,#16079,#9702,.T.);
#20549=EDGE_CURVE('',#16080,#16079,#13171,.T.);
#20550=EDGE_CURVE('',#16080,#16081,#9703,.T.);
#20551=EDGE_CURVE('',#16081,#16082,#13172,.T.);
#20552=EDGE_CURVE('',#16082,#16083,#9704,.T.);
#20553=EDGE_CURVE('',#16084,#16083,#13173,.T.);
#20554=EDGE_CURVE('',#16084,#16085,#9705,.T.);
#20555=EDGE_CURVE('',#16085,#16086,#13174,.T.);
#20556=EDGE_CURVE('',#16086,#16087,#9706,.T.);
#20557=EDGE_CURVE('',#16088,#16087,#13175,.T.);
#20558=EDGE_CURVE('',#16088,#16089,#9707,.T.);
#20559=EDGE_CURVE('',#16089,#16090,#13176,.T.);
#20560=EDGE_CURVE('',#16090,#16091,#9708,.T.);
#20561=EDGE_CURVE('',#16092,#16091,#13177,.T.);
#20562=EDGE_CURVE('',#16092,#16093,#9709,.T.);
#20563=EDGE_CURVE('',#16093,#16094,#13178,.T.);
#20564=EDGE_CURVE('',#16094,#16095,#9710,.T.);
#20565=EDGE_CURVE('',#16096,#16095,#13179,.T.);
#20566=EDGE_CURVE('',#16096,#16097,#9711,.T.);
#20567=EDGE_CURVE('',#16097,#16098,#13180,.T.);
#20568=EDGE_CURVE('',#16098,#16099,#9712,.T.);
#20569=EDGE_CURVE('',#16100,#16099,#13181,.T.);
#20570=EDGE_CURVE('',#16100,#16101,#9713,.T.);
#20571=EDGE_CURVE('',#16101,#16102,#13182,.T.);
#20572=EDGE_CURVE('',#16102,#16103,#9714,.T.);
#20573=EDGE_CURVE('',#16104,#16103,#13183,.T.);
#20574=EDGE_CURVE('',#16104,#16105,#9715,.T.);
#20575=EDGE_CURVE('',#16105,#16106,#13184,.T.);
#20576=EDGE_CURVE('',#16106,#16107,#9716,.T.);
#20577=EDGE_CURVE('',#16108,#16107,#13185,.T.);
#20578=EDGE_CURVE('',#16108,#16109,#9717,.T.);
#20579=EDGE_CURVE('',#16109,#16110,#13186,.T.);
#20580=EDGE_CURVE('',#16110,#16111,#9718,.T.);
#20581=EDGE_CURVE('',#16112,#16111,#13187,.T.);
#20582=EDGE_CURVE('',#16112,#16113,#9719,.T.);
#20583=EDGE_CURVE('',#16113,#16114,#13188,.T.);
#20584=EDGE_CURVE('',#16114,#16115,#9720,.T.);
#20585=EDGE_CURVE('',#16116,#16115,#13189,.T.);
#20586=EDGE_CURVE('',#16116,#16117,#9721,.T.);
#20587=EDGE_CURVE('',#16117,#16118,#13190,.T.);
#20588=EDGE_CURVE('',#16118,#16119,#9722,.T.);
#20589=EDGE_CURVE('',#16120,#16119,#13191,.T.);
#20590=EDGE_CURVE('',#16120,#16121,#9723,.T.);
#20591=EDGE_CURVE('',#16121,#16122,#13192,.T.);
#20592=EDGE_CURVE('',#16122,#16123,#9724,.T.);
#20593=EDGE_CURVE('',#16124,#16123,#13193,.T.);
#20594=EDGE_CURVE('',#16124,#16125,#9725,.T.);
#20595=EDGE_CURVE('',#16125,#16126,#13194,.T.);
#20596=EDGE_CURVE('',#16126,#16127,#9726,.T.);
#20597=EDGE_CURVE('',#16128,#16127,#13195,.T.);
#20598=EDGE_CURVE('',#16128,#16129,#9727,.T.);
#20599=EDGE_CURVE('',#16129,#16130,#13196,.T.);
#20600=EDGE_CURVE('',#16130,#16131,#9728,.T.);
#20601=EDGE_CURVE('',#16132,#16131,#13197,.T.);
#20602=EDGE_CURVE('',#16132,#16133,#9729,.T.);
#20603=EDGE_CURVE('',#16133,#16134,#13198,.T.);
#20604=EDGE_CURVE('',#16134,#16135,#9730,.T.);
#20605=EDGE_CURVE('',#16136,#16135,#13199,.T.);
#20606=EDGE_CURVE('',#16136,#16137,#9731,.T.);
#20607=EDGE_CURVE('',#16137,#16138,#13200,.T.);
#20608=EDGE_CURVE('',#16138,#16139,#9732,.T.);
#20609=EDGE_CURVE('',#16140,#16139,#13201,.T.);
#20610=EDGE_CURVE('',#16140,#16141,#9733,.T.);
#20611=EDGE_CURVE('',#16141,#16142,#13202,.T.);
#20612=EDGE_CURVE('',#16142,#16143,#9734,.T.);
#20613=EDGE_CURVE('',#16144,#16143,#13203,.T.);
#20614=EDGE_CURVE('',#16144,#16145,#9735,.T.);
#20615=EDGE_CURVE('',#16145,#16146,#13204,.T.);
#20616=EDGE_CURVE('',#16146,#16147,#9736,.T.);
#20617=EDGE_CURVE('',#16148,#16147,#13205,.T.);
#20618=EDGE_CURVE('',#16148,#16006,#9737,.T.);
#20619=EDGE_CURVE('',#16074,#16149,#9738,.T.);
#20620=EDGE_CURVE('',#16150,#16149,#9739,.T.);
#20621=EDGE_CURVE('',#16075,#16150,#202,.T.);
#20622=EDGE_CURVE('',#16150,#16072,#203,.T.);
#20623=EDGE_CURVE('',#16149,#16073,#9740,.T.);
#20624=EDGE_CURVE('',#16151,#16148,#204,.T.);
#20625=EDGE_CURVE('',#16147,#16152,#205,.T.);
#20626=EDGE_CURVE('',#16152,#16144,#206,.T.);
#20627=EDGE_CURVE('',#16143,#16153,#207,.T.);
#20628=EDGE_CURVE('',#16153,#16140,#208,.T.);
#20629=EDGE_CURVE('',#16139,#16154,#209,.T.);
#20630=EDGE_CURVE('',#16154,#16136,#210,.T.);
#20631=EDGE_CURVE('',#16135,#16155,#211,.T.);
#20632=EDGE_CURVE('',#16155,#16132,#212,.T.);
#20633=EDGE_CURVE('',#16131,#16156,#213,.T.);
#20634=EDGE_CURVE('',#16156,#16128,#214,.T.);
#20635=EDGE_CURVE('',#16127,#16157,#215,.T.);
#20636=EDGE_CURVE('',#16157,#16124,#216,.T.);
#20637=EDGE_CURVE('',#16123,#16158,#217,.T.);
#20638=EDGE_CURVE('',#16158,#16120,#218,.T.);
#20639=EDGE_CURVE('',#16119,#16159,#219,.T.);
#20640=EDGE_CURVE('',#16159,#16116,#220,.T.);
#20641=EDGE_CURVE('',#16115,#16160,#221,.T.);
#20642=EDGE_CURVE('',#16160,#16112,#222,.T.);
#20643=EDGE_CURVE('',#16111,#16161,#223,.T.);
#20644=EDGE_CURVE('',#16161,#16108,#224,.T.);
#20645=EDGE_CURVE('',#16107,#16162,#225,.T.);
#20646=EDGE_CURVE('',#16162,#16104,#226,.T.);
#20647=EDGE_CURVE('',#16103,#16163,#227,.T.);
#20648=EDGE_CURVE('',#16163,#16100,#228,.T.);
#20649=EDGE_CURVE('',#16099,#16164,#229,.T.);
#20650=EDGE_CURVE('',#16164,#16096,#230,.T.);
#20651=EDGE_CURVE('',#16095,#16165,#231,.T.);
#20652=EDGE_CURVE('',#16165,#16092,#232,.T.);
#20653=EDGE_CURVE('',#16091,#16166,#233,.T.);
#20654=EDGE_CURVE('',#16166,#16088,#234,.T.);
#20655=EDGE_CURVE('',#16087,#16167,#235,.T.);
#20656=EDGE_CURVE('',#16167,#16084,#236,.T.);
#20657=EDGE_CURVE('',#16083,#16168,#237,.T.);
#20658=EDGE_CURVE('',#16168,#16080,#238,.T.);
#20659=EDGE_CURVE('',#16079,#16169,#239,.T.);
#20660=EDGE_CURVE('',#16169,#16076,#240,.T.);
#20661=EDGE_CURVE('',#16071,#16170,#241,.T.);
#20662=EDGE_CURVE('',#16170,#16068,#242,.T.);
#20663=EDGE_CURVE('',#16067,#16171,#243,.T.);
#20664=EDGE_CURVE('',#16171,#16064,#244,.T.);
#20665=EDGE_CURVE('',#16063,#16172,#245,.T.);
#20666=EDGE_CURVE('',#16172,#16060,#246,.T.);
#20667=EDGE_CURVE('',#16059,#16173,#247,.T.);
#20668=EDGE_CURVE('',#16173,#16056,#248,.T.);
#20669=EDGE_CURVE('',#16055,#16174,#249,.T.);
#20670=EDGE_CURVE('',#16174,#16052,#250,.T.);
#20671=EDGE_CURVE('',#16051,#16175,#251,.T.);
#20672=EDGE_CURVE('',#16175,#16048,#252,.T.);
#20673=EDGE_CURVE('',#16047,#16176,#253,.T.);
#20674=EDGE_CURVE('',#16176,#16044,#254,.T.);
#20675=EDGE_CURVE('',#16043,#16177,#255,.T.);
#20676=EDGE_CURVE('',#16177,#16040,#256,.T.);
#20677=EDGE_CURVE('',#16039,#16178,#257,.T.);
#20678=EDGE_CURVE('',#16178,#16036,#258,.T.);
#20679=EDGE_CURVE('',#16035,#16179,#259,.T.);
#20680=EDGE_CURVE('',#16179,#16032,#260,.T.);
#20681=EDGE_CURVE('',#16031,#16180,#261,.T.);
#20682=EDGE_CURVE('',#16180,#16028,#262,.T.);
#20683=EDGE_CURVE('',#16027,#16181,#263,.T.);
#20684=EDGE_CURVE('',#16181,#16024,#264,.T.);
#20685=EDGE_CURVE('',#16023,#16182,#265,.T.);
#20686=EDGE_CURVE('',#16182,#16020,#266,.T.);
#20687=EDGE_CURVE('',#16019,#16183,#267,.T.);
#20688=EDGE_CURVE('',#16183,#16016,#268,.T.);
#20689=EDGE_CURVE('',#16015,#16184,#269,.T.);
#20690=EDGE_CURVE('',#16184,#16012,#270,.T.);
#20691=EDGE_CURVE('',#16011,#16151,#271,.T.);
#20692=EDGE_CURVE('',#16151,#16185,#9741,.T.);
#20693=EDGE_CURVE('',#16185,#16185,#13206,.T.);
#20694=EDGE_CURVE('',#16186,#16069,#9742,.T.);
#20695=EDGE_CURVE('',#16070,#16186,#9743,.T.);
#20696=EDGE_CURVE('',#16170,#16186,#9744,.T.);
#20697=EDGE_CURVE('',#16066,#16187,#9745,.T.);
#20698=EDGE_CURVE('',#16171,#16187,#9746,.T.);
#20699=EDGE_CURVE('',#16187,#16065,#9747,.T.);
#20700=EDGE_CURVE('',#16188,#16061,#9748,.T.);
#20701=EDGE_CURVE('',#16062,#16188,#9749,.T.);
#20702=EDGE_CURVE('',#16172,#16188,#9750,.T.);
#20703=EDGE_CURVE('',#16058,#16189,#9751,.T.);
#20704=EDGE_CURVE('',#16173,#16189,#9752,.T.);
#20705=EDGE_CURVE('',#16189,#16057,#9753,.T.);
#20706=EDGE_CURVE('',#16190,#16053,#9754,.T.);
#20707=EDGE_CURVE('',#16054,#16190,#9755,.T.);
#20708=EDGE_CURVE('',#16174,#16190,#9756,.T.);
#20709=EDGE_CURVE('',#16050,#16191,#9757,.T.);
#20710=EDGE_CURVE('',#16175,#16191,#9758,.T.);
#20711=EDGE_CURVE('',#16191,#16049,#9759,.T.);
#20712=EDGE_CURVE('',#16192,#16045,#9760,.T.);
#20713=EDGE_CURVE('',#16046,#16192,#9761,.T.);
#20714=EDGE_CURVE('',#16176,#16192,#9762,.T.);
#20715=EDGE_CURVE('',#16042,#16193,#9763,.T.);
#20716=EDGE_CURVE('',#16177,#16193,#9764,.T.);
#20717=EDGE_CURVE('',#16193,#16041,#9765,.T.);
#20718=EDGE_CURVE('',#16194,#16037,#9766,.T.);
#20719=EDGE_CURVE('',#16038,#16194,#9767,.T.);
#20720=EDGE_CURVE('',#16178,#16194,#9768,.T.);
#20721=EDGE_CURVE('',#16034,#16195,#9769,.T.);
#20722=EDGE_CURVE('',#16179,#16195,#9770,.T.);
#20723=EDGE_CURVE('',#16195,#16033,#9771,.T.);
#20724=EDGE_CURVE('',#16196,#16029,#9772,.T.);
#20725=EDGE_CURVE('',#16030,#16196,#9773,.T.);
#20726=EDGE_CURVE('',#16180,#16196,#9774,.T.);
#20727=EDGE_CURVE('',#16026,#16197,#9775,.T.);
#20728=EDGE_CURVE('',#16181,#16197,#9776,.T.);
#20729=EDGE_CURVE('',#16197,#16025,#9777,.T.);
#20730=EDGE_CURVE('',#16198,#16021,#9778,.T.);
#20731=EDGE_CURVE('',#16022,#16198,#9779,.T.);
#20732=EDGE_CURVE('',#16182,#16198,#9780,.T.);
#20733=EDGE_CURVE('',#16018,#16199,#9781,.T.);
#20734=EDGE_CURVE('',#16183,#16199,#9782,.T.);
#20735=EDGE_CURVE('',#16199,#16017,#9783,.T.);
#20736=EDGE_CURVE('',#16200,#16013,#9784,.T.);
#20737=EDGE_CURVE('',#16014,#16200,#9785,.T.);
#20738=EDGE_CURVE('',#16184,#16200,#9786,.T.);
#20739=EDGE_CURVE('',#16010,#16201,#9787,.T.);
#20740=EDGE_CURVE('',#16151,#16201,#9788,.T.);
#20741=EDGE_CURVE('',#16201,#16006,#9789,.T.);
#20742=EDGE_CURVE('',#16202,#16145,#9790,.T.);
#20743=EDGE_CURVE('',#16146,#16202,#9791,.T.);
#20744=EDGE_CURVE('',#16152,#16202,#9792,.T.);
#20745=EDGE_CURVE('',#16142,#16203,#9793,.T.);
#20746=EDGE_CURVE('',#16153,#16203,#9794,.T.);
#20747=EDGE_CURVE('',#16203,#16141,#9795,.T.);
#20748=EDGE_CURVE('',#16204,#16137,#9796,.T.);
#20749=EDGE_CURVE('',#16138,#16204,#9797,.T.);
#20750=EDGE_CURVE('',#16154,#16204,#9798,.T.);
#20751=EDGE_CURVE('',#16134,#16205,#9799,.T.);
#20752=EDGE_CURVE('',#16155,#16205,#9800,.T.);
#20753=EDGE_CURVE('',#16205,#16133,#9801,.T.);
#20754=EDGE_CURVE('',#16206,#16129,#9802,.T.);
#20755=EDGE_CURVE('',#16130,#16206,#9803,.T.);
#20756=EDGE_CURVE('',#16156,#16206,#9804,.T.);
#20757=EDGE_CURVE('',#16126,#16207,#9805,.T.);
#20758=EDGE_CURVE('',#16157,#16207,#9806,.T.);
#20759=EDGE_CURVE('',#16207,#16125,#9807,.T.);
#20760=EDGE_CURVE('',#16208,#16121,#9808,.T.);
#20761=EDGE_CURVE('',#16122,#16208,#9809,.T.);
#20762=EDGE_CURVE('',#16158,#16208,#9810,.T.);
#20763=EDGE_CURVE('',#16118,#16209,#9811,.T.);
#20764=EDGE_CURVE('',#16159,#16209,#9812,.T.);
#20765=EDGE_CURVE('',#16209,#16117,#9813,.T.);
#20766=EDGE_CURVE('',#16210,#16113,#9814,.T.);
#20767=EDGE_CURVE('',#16114,#16210,#9815,.T.);
#20768=EDGE_CURVE('',#16160,#16210,#9816,.T.);
#20769=EDGE_CURVE('',#16110,#16211,#9817,.T.);
#20770=EDGE_CURVE('',#16161,#16211,#9818,.T.);
#20771=EDGE_CURVE('',#16211,#16109,#9819,.T.);
#20772=EDGE_CURVE('',#16212,#16105,#9820,.T.);
#20773=EDGE_CURVE('',#16106,#16212,#9821,.T.);
#20774=EDGE_CURVE('',#16162,#16212,#9822,.T.);
#20775=EDGE_CURVE('',#16102,#16213,#9823,.T.);
#20776=EDGE_CURVE('',#16163,#16213,#9824,.T.);
#20777=EDGE_CURVE('',#16213,#16101,#9825,.T.);
#20778=EDGE_CURVE('',#16214,#16097,#9826,.T.);
#20779=EDGE_CURVE('',#16098,#16214,#9827,.T.);
#20780=EDGE_CURVE('',#16164,#16214,#9828,.T.);
#20781=EDGE_CURVE('',#16094,#16215,#9829,.T.);
#20782=EDGE_CURVE('',#16165,#16215,#9830,.T.);
#20783=EDGE_CURVE('',#16215,#16093,#9831,.T.);
#20784=EDGE_CURVE('',#16216,#16089,#9832,.T.);
#20785=EDGE_CURVE('',#16090,#16216,#9833,.T.);
#20786=EDGE_CURVE('',#16166,#16216,#9834,.T.);
#20787=EDGE_CURVE('',#16086,#16217,#9835,.T.);
#20788=EDGE_CURVE('',#16167,#16217,#9836,.T.);
#20789=EDGE_CURVE('',#16217,#16085,#9837,.T.);
#20790=EDGE_CURVE('',#16218,#16081,#9838,.T.);
#20791=EDGE_CURVE('',#16082,#16218,#9839,.T.);
#20792=EDGE_CURVE('',#16168,#16218,#9840,.T.);
#20793=EDGE_CURVE('',#16078,#16219,#9841,.T.);
#20794=EDGE_CURVE('',#16169,#16219,#9842,.T.);
#20795=EDGE_CURVE('',#16219,#16077,#9843,.T.);
#20796=EDGE_CURVE('',#15998,#16009,#13207,.T.);
#20797=EDGE_CURVE('',#16220,#16220,#13208,.T.);
#20798=EDGE_CURVE('',#16221,#16222,#272,.T.);
#20799=EDGE_CURVE('',#16223,#16221,#13209,.T.);
#20800=EDGE_CURVE('',#16224,#16223,#273,.T.);
#20801=EDGE_CURVE('',#16225,#16224,#274,.T.);
#20802=EDGE_CURVE('',#16226,#16225,#13210,.T.);
#20803=EDGE_CURVE('',#16227,#16226,#275,.T.);
#20804=EDGE_CURVE('',#16228,#16227,#276,.T.);
#20805=EDGE_CURVE('',#16229,#16228,#13211,.T.);
#20806=EDGE_CURVE('',#16230,#16229,#277,.T.);
#20807=EDGE_CURVE('',#16231,#16230,#278,.T.);
#20808=EDGE_CURVE('',#16232,#16231,#13212,.T.);
#20809=EDGE_CURVE('',#16233,#16232,#279,.T.);
#20810=EDGE_CURVE('',#16234,#16233,#280,.T.);
#20811=EDGE_CURVE('',#16235,#16234,#13213,.T.);
#20812=EDGE_CURVE('',#16236,#16235,#281,.T.);
#20813=EDGE_CURVE('',#16237,#16236,#282,.T.);
#20814=EDGE_CURVE('',#16238,#16237,#13214,.T.);
#20815=EDGE_CURVE('',#16222,#16238,#283,.T.);
#20816=EDGE_CURVE('',#16222,#16220,#9844,.T.);
#20817=EDGE_CURVE('',#16238,#16239,#9845,.T.);
#20818=EDGE_CURVE('',#16240,#16237,#9846,.T.);
#20819=EDGE_CURVE('',#16239,#16240,#13215,.T.);
#20820=EDGE_CURVE('',#16241,#16234,#9847,.T.);
#20821=EDGE_CURVE('',#16242,#16241,#13216,.T.);
#20822=EDGE_CURVE('',#16235,#16242,#9848,.T.);
#20823=EDGE_CURVE('',#16223,#16243,#9849,.T.);
#20824=EDGE_CURVE('',#16244,#16221,#9850,.T.);
#20825=EDGE_CURVE('',#16243,#16244,#13217,.T.);
#20826=EDGE_CURVE('',#16245,#16231,#9851,.T.);
#20827=EDGE_CURVE('',#16246,#16245,#13218,.T.);
#20828=EDGE_CURVE('',#16232,#16246,#9852,.T.);
#20829=EDGE_CURVE('',#16226,#16247,#9853,.T.);
#20830=EDGE_CURVE('',#16248,#16225,#9854,.T.);
#20831=EDGE_CURVE('',#16247,#16248,#13219,.T.);
#20832=EDGE_CURVE('',#16249,#16228,#9855,.T.);
#20833=EDGE_CURVE('',#16250,#16249,#13220,.T.);
#20834=EDGE_CURVE('',#16229,#16250,#9856,.T.);
#20835=EDGE_CURVE('',#16248,#16247,#9857,.T.);
#20836=EDGE_CURVE('',#16224,#16251,#9858,.T.);
#20837=EDGE_CURVE('',#16251,#16252,#9859,.T.);
#20838=EDGE_CURVE('',#16227,#16252,#9860,.T.);
#20839=EDGE_CURVE('',#16244,#16243,#9861,.T.);
#20840=EDGE_CURVE('',#16222,#16253,#9862,.T.);
#20841=EDGE_CURVE('',#16253,#16251,#9863,.T.);
#20842=EDGE_CURVE('',#16240,#16239,#9864,.T.);
#20843=EDGE_CURVE('',#16236,#16254,#9865,.T.);
#20844=EDGE_CURVE('',#16254,#16253,#9866,.T.);
#20845=EDGE_CURVE('',#16241,#16242,#9867,.T.);
#20846=EDGE_CURVE('',#16245,#16246,#9868,.T.);
#20847=EDGE_CURVE('',#16249,#16250,#9869,.T.);
#20848=EDGE_CURVE('',#16255,#16256,#9870,.T.);
#20849=EDGE_CURVE('',#16256,#16255,#13221,.T.);
#20850=EDGE_CURVE('',#16256,#16254,#9871,.T.);
#20851=EDGE_CURVE('',#16254,#16256,#13222,.T.);
#20852=EDGE_CURVE('',#16253,#16254,#13223,.T.);
#20853=EDGE_CURVE('',#16251,#16253,#13224,.T.);
#20854=EDGE_CURVE('',#16252,#16251,#13225,.T.);
#20855=EDGE_CURVE('',#16252,#16255,#9872,.T.);
#20856=EDGE_CURVE('',#16255,#16252,#13226,.T.);
#20857=EDGE_CURVE('',#16257,#16253,#9873,.T.);
#20858=EDGE_CURVE('',#16230,#16255,#9874,.T.);
#20859=EDGE_CURVE('',#16233,#16256,#9875,.T.);
#28936=ORIENTED_EDGE('',*,*,#20319,.F.);
#28937=ORIENTED_EDGE('',*,*,#20320,.T.);
#28938=ORIENTED_EDGE('',*,*,#20321,.F.);
#28939=ORIENTED_EDGE('',*,*,#20322,.T.);
#28940=ORIENTED_EDGE('',*,*,#20323,.F.);
#28941=ORIENTED_EDGE('',*,*,#20324,.T.);
#28942=ORIENTED_EDGE('',*,*,#20319,.T.);
#28943=ORIENTED_EDGE('',*,*,#20325,.T.);
#28944=ORIENTED_EDGE('',*,*,#20326,.F.);
#28945=ORIENTED_EDGE('',*,*,#20327,.T.);
#28946=ORIENTED_EDGE('',*,*,#20323,.T.);
#28947=ORIENTED_EDGE('',*,*,#20328,.T.);
#28948=ORIENTED_EDGE('',*,*,#20329,.F.);
#28949=ORIENTED_EDGE('',*,*,#20330,.T.);
#28950=ORIENTED_EDGE('',*,*,#20326,.T.);
#28951=ORIENTED_EDGE('',*,*,#20331,.T.);
#28952=ORIENTED_EDGE('',*,*,#20332,.T.);
#28953=ORIENTED_EDGE('',*,*,#20333,.F.);
#28954=ORIENTED_EDGE('',*,*,#20334,.T.);
#28955=ORIENTED_EDGE('',*,*,#20329,.T.);
#28956=ORIENTED_EDGE('',*,*,#20335,.T.);
#28957=ORIENTED_EDGE('',*,*,#20336,.F.);
#28958=ORIENTED_EDGE('',*,*,#20337,.T.);
#28959=ORIENTED_EDGE('',*,*,#20333,.T.);
#28960=ORIENTED_EDGE('',*,*,#20338,.T.);
#28961=ORIENTED_EDGE('',*,*,#20339,.F.);
#28962=ORIENTED_EDGE('',*,*,#20340,.T.);
#28963=ORIENTED_EDGE('',*,*,#20341,.T.);
#28964=ORIENTED_EDGE('',*,*,#20336,.T.);
#28965=ORIENTED_EDGE('',*,*,#20342,.T.);
#28966=ORIENTED_EDGE('',*,*,#20343,.F.);
#28967=ORIENTED_EDGE('',*,*,#20344,.T.);
#28968=ORIENTED_EDGE('',*,*,#20339,.T.);
#28969=ORIENTED_EDGE('',*,*,#20345,.T.);
#28970=ORIENTED_EDGE('',*,*,#20346,.F.);
#28971=ORIENTED_EDGE('',*,*,#20347,.T.);
#28972=ORIENTED_EDGE('',*,*,#20343,.T.);
#28973=ORIENTED_EDGE('',*,*,#20348,.T.);
#28974=ORIENTED_EDGE('',*,*,#20349,.F.);
#28975=ORIENTED_EDGE('',*,*,#20350,.T.);
#28976=ORIENTED_EDGE('',*,*,#20346,.T.);
#28977=ORIENTED_EDGE('',*,*,#20351,.T.);
#28978=ORIENTED_EDGE('',*,*,#20352,.T.);
#28979=ORIENTED_EDGE('',*,*,#20353,.F.);
#28980=ORIENTED_EDGE('',*,*,#20354,.T.);
#28981=ORIENTED_EDGE('',*,*,#20349,.T.);
#28982=ORIENTED_EDGE('',*,*,#20355,.T.);
#28983=ORIENTED_EDGE('',*,*,#20356,.F.);
#28984=ORIENTED_EDGE('',*,*,#20357,.T.);
#28985=ORIENTED_EDGE('',*,*,#20353,.T.);
#28986=ORIENTED_EDGE('',*,*,#20358,.T.);
#28987=ORIENTED_EDGE('',*,*,#20359,.F.);
#28988=ORIENTED_EDGE('',*,*,#20360,.T.);
#28989=ORIENTED_EDGE('',*,*,#20356,.T.);
#28990=ORIENTED_EDGE('',*,*,#20361,.T.);
#28991=ORIENTED_EDGE('',*,*,#20362,.F.);
#28992=ORIENTED_EDGE('',*,*,#20363,.T.);
#28993=ORIENTED_EDGE('',*,*,#20359,.T.);
#28994=ORIENTED_EDGE('',*,*,#20364,.T.);
#28995=ORIENTED_EDGE('',*,*,#20365,.F.);
#28996=ORIENTED_EDGE('',*,*,#20366,.T.);
#28997=ORIENTED_EDGE('',*,*,#20362,.T.);
#28998=ORIENTED_EDGE('',*,*,#20367,.T.);
#28999=ORIENTED_EDGE('',*,*,#20368,.F.);
#29000=ORIENTED_EDGE('',*,*,#20369,.T.);
#29001=ORIENTED_EDGE('',*,*,#20370,.T.);
#29002=ORIENTED_EDGE('',*,*,#20365,.T.);
#29003=ORIENTED_EDGE('',*,*,#20371,.T.);
#29004=ORIENTED_EDGE('',*,*,#20372,.F.);
#29005=ORIENTED_EDGE('',*,*,#20373,.T.);
#29006=ORIENTED_EDGE('',*,*,#20368,.T.);
#29007=ORIENTED_EDGE('',*,*,#20374,.T.);
#29008=ORIENTED_EDGE('',*,*,#20375,.F.);
#29009=ORIENTED_EDGE('',*,*,#20376,.T.);
#29010=ORIENTED_EDGE('',*,*,#20372,.T.);
#29011=ORIENTED_EDGE('',*,*,#20377,.T.);
#29012=ORIENTED_EDGE('',*,*,#20378,.F.);
#29013=ORIENTED_EDGE('',*,*,#20379,.T.);
#29014=ORIENTED_EDGE('',*,*,#20375,.T.);
#29015=ORIENTED_EDGE('',*,*,#20380,.T.);
#29016=ORIENTED_EDGE('',*,*,#20381,.F.);
#29017=ORIENTED_EDGE('',*,*,#20382,.F.);
#29018=ORIENTED_EDGE('',*,*,#20383,.F.);
#29019=ORIENTED_EDGE('',*,*,#20384,.T.);
#29020=ORIENTED_EDGE('',*,*,#20385,.F.);
#29021=ORIENTED_EDGE('',*,*,#20386,.F.);
#29022=ORIENTED_EDGE('',*,*,#20387,.F.);
#29023=ORIENTED_EDGE('',*,*,#20381,.T.);
#29024=ORIENTED_EDGE('',*,*,#20388,.T.);
#29025=ORIENTED_EDGE('',*,*,#20389,.F.);
#29026=ORIENTED_EDGE('',*,*,#20390,.F.);
#29027=ORIENTED_EDGE('',*,*,#20385,.T.);
#29028=ORIENTED_EDGE('',*,*,#20391,.T.);
#29029=ORIENTED_EDGE('',*,*,#20392,.F.);
#29030=ORIENTED_EDGE('',*,*,#20393,.F.);
#29031=ORIENTED_EDGE('',*,*,#20389,.T.);
#29032=ORIENTED_EDGE('',*,*,#20394,.T.);
#29033=ORIENTED_EDGE('',*,*,#20395,.F.);
#29034=ORIENTED_EDGE('',*,*,#20396,.F.);
#29035=ORIENTED_EDGE('',*,*,#20392,.T.);
#29036=ORIENTED_EDGE('',*,*,#20397,.T.);
#29037=ORIENTED_EDGE('',*,*,#20398,.F.);
#29038=ORIENTED_EDGE('',*,*,#20399,.F.);
#29039=ORIENTED_EDGE('',*,*,#20400,.F.);
#29040=ORIENTED_EDGE('',*,*,#20395,.T.);
#29041=ORIENTED_EDGE('',*,*,#20401,.T.);
#29042=ORIENTED_EDGE('',*,*,#20402,.F.);
#29043=ORIENTED_EDGE('',*,*,#20403,.F.);
#29044=ORIENTED_EDGE('',*,*,#20398,.T.);
#29045=ORIENTED_EDGE('',*,*,#20404,.T.);
#29046=ORIENTED_EDGE('',*,*,#20405,.F.);
#29047=ORIENTED_EDGE('',*,*,#20406,.F.);
#29048=ORIENTED_EDGE('',*,*,#20402,.T.);
#29049=ORIENTED_EDGE('',*,*,#20407,.T.);
#29050=ORIENTED_EDGE('',*,*,#20408,.F.);
#29051=ORIENTED_EDGE('',*,*,#20409,.F.);
#29052=ORIENTED_EDGE('',*,*,#20405,.T.);
#29053=ORIENTED_EDGE('',*,*,#20410,.T.);
#29054=ORIENTED_EDGE('',*,*,#20411,.F.);
#29055=ORIENTED_EDGE('',*,*,#20412,.F.);
#29056=ORIENTED_EDGE('',*,*,#20408,.T.);
#29057=ORIENTED_EDGE('',*,*,#20413,.T.);
#29058=ORIENTED_EDGE('',*,*,#20414,.F.);
#29059=ORIENTED_EDGE('',*,*,#20415,.F.);
#29060=ORIENTED_EDGE('',*,*,#20411,.T.);
#29061=ORIENTED_EDGE('',*,*,#20416,.T.);
#29062=ORIENTED_EDGE('',*,*,#20417,.F.);
#29063=ORIENTED_EDGE('',*,*,#20418,.F.);
#29064=ORIENTED_EDGE('',*,*,#20414,.T.);
#29065=ORIENTED_EDGE('',*,*,#20419,.T.);
#29066=ORIENTED_EDGE('',*,*,#20420,.F.);
#29067=ORIENTED_EDGE('',*,*,#20421,.F.);
#29068=ORIENTED_EDGE('',*,*,#20417,.T.);
#29069=ORIENTED_EDGE('',*,*,#20422,.T.);
#29070=ORIENTED_EDGE('',*,*,#20423,.F.);
#29071=ORIENTED_EDGE('',*,*,#20424,.F.);
#29072=ORIENTED_EDGE('',*,*,#20420,.T.);
#29073=ORIENTED_EDGE('',*,*,#20425,.T.);
#29074=ORIENTED_EDGE('',*,*,#20426,.F.);
#29075=ORIENTED_EDGE('',*,*,#20427,.F.);
#29076=ORIENTED_EDGE('',*,*,#20428,.F.);
#29077=ORIENTED_EDGE('',*,*,#20423,.T.);
#29078=ORIENTED_EDGE('',*,*,#20429,.T.);
#29079=ORIENTED_EDGE('',*,*,#20430,.F.);
#29080=ORIENTED_EDGE('',*,*,#20431,.F.);
#29081=ORIENTED_EDGE('',*,*,#20426,.T.);
#29082=ORIENTED_EDGE('',*,*,#20432,.T.);
#29083=ORIENTED_EDGE('',*,*,#20433,.F.);
#29084=ORIENTED_EDGE('',*,*,#20434,.F.);
#29085=ORIENTED_EDGE('',*,*,#20430,.T.);
#29086=ORIENTED_EDGE('',*,*,#20435,.T.);
#29087=ORIENTED_EDGE('',*,*,#20436,.F.);
#29088=ORIENTED_EDGE('',*,*,#20437,.F.);
#29089=ORIENTED_EDGE('',*,*,#20433,.T.);
#29090=ORIENTED_EDGE('',*,*,#20438,.T.);
#29091=ORIENTED_EDGE('',*,*,#20439,.T.);
#29092=ORIENTED_EDGE('',*,*,#20440,.F.);
#29093=ORIENTED_EDGE('',*,*,#20441,.F.);
#29094=ORIENTED_EDGE('',*,*,#20436,.T.);
#29095=ORIENTED_EDGE('',*,*,#20442,.T.);
#29096=ORIENTED_EDGE('',*,*,#20440,.T.);
#29097=ORIENTED_EDGE('',*,*,#20443,.T.);
#29098=ORIENTED_EDGE('',*,*,#20444,.F.);
#29099=ORIENTED_EDGE('',*,*,#20445,.F.);
#29100=ORIENTED_EDGE('',*,*,#20446,.F.);
#29101=ORIENTED_EDGE('',*,*,#20378,.T.);
#29102=ORIENTED_EDGE('',*,*,#20447,.T.);
#29103=ORIENTED_EDGE('',*,*,#20448,.F.);
#29104=ORIENTED_EDGE('',*,*,#20449,.T.);
#29105=ORIENTED_EDGE('',*,*,#20450,.F.);
#29106=ORIENTED_EDGE('',*,*,#20451,.T.);
#29107=ORIENTED_EDGE('',*,*,#20444,.T.);
#29108=ORIENTED_EDGE('',*,*,#20452,.T.);
#29109=ORIENTED_EDGE('',*,*,#20453,.F.);
#29110=ORIENTED_EDGE('',*,*,#20451,.F.);
#29111=ORIENTED_EDGE('',*,*,#20454,.F.);
#29112=ORIENTED_EDGE('',*,*,#20447,.F.);
#29113=ORIENTED_EDGE('',*,*,#20380,.F.);
#29114=ORIENTED_EDGE('',*,*,#20377,.F.);
#29115=ORIENTED_EDGE('',*,*,#20374,.F.);
#29116=ORIENTED_EDGE('',*,*,#20371,.F.);
#29117=ORIENTED_EDGE('',*,*,#20367,.F.);
#29118=ORIENTED_EDGE('',*,*,#20364,.F.);
#29119=ORIENTED_EDGE('',*,*,#20361,.F.);
#29120=ORIENTED_EDGE('',*,*,#20358,.F.);
#29121=ORIENTED_EDGE('',*,*,#20355,.F.);
#29122=ORIENTED_EDGE('',*,*,#20352,.F.);
#29123=ORIENTED_EDGE('',*,*,#20351,.F.);
#29124=ORIENTED_EDGE('',*,*,#20348,.F.);
#29125=ORIENTED_EDGE('',*,*,#20345,.F.);
#29126=ORIENTED_EDGE('',*,*,#20342,.F.);
#29127=ORIENTED_EDGE('',*,*,#20338,.F.);
#29128=ORIENTED_EDGE('',*,*,#20335,.F.);
#29129=ORIENTED_EDGE('',*,*,#20332,.F.);
#29130=ORIENTED_EDGE('',*,*,#20331,.F.);
#29131=ORIENTED_EDGE('',*,*,#20328,.F.);
#29132=ORIENTED_EDGE('',*,*,#20325,.F.);
#29133=ORIENTED_EDGE('',*,*,#20322,.F.);
#29134=ORIENTED_EDGE('',*,*,#20455,.F.);
#29135=ORIENTED_EDGE('',*,*,#20456,.T.);
#29136=ORIENTED_EDGE('',*,*,#20382,.T.);
#29137=ORIENTED_EDGE('',*,*,#20387,.T.);
#29138=ORIENTED_EDGE('',*,*,#20386,.T.);
#29139=ORIENTED_EDGE('',*,*,#20390,.T.);
#29140=ORIENTED_EDGE('',*,*,#20393,.T.);
#29141=ORIENTED_EDGE('',*,*,#20396,.T.);
#29142=ORIENTED_EDGE('',*,*,#20400,.T.);
#29143=ORIENTED_EDGE('',*,*,#20399,.T.);
#29144=ORIENTED_EDGE('',*,*,#20403,.T.);
#29145=ORIENTED_EDGE('',*,*,#20406,.T.);
#29146=ORIENTED_EDGE('',*,*,#20409,.T.);
#29147=ORIENTED_EDGE('',*,*,#20412,.T.);
#29148=ORIENTED_EDGE('',*,*,#20415,.T.);
#29149=ORIENTED_EDGE('',*,*,#20418,.T.);
#29150=ORIENTED_EDGE('',*,*,#20421,.T.);
#29151=ORIENTED_EDGE('',*,*,#20424,.T.);
#29152=ORIENTED_EDGE('',*,*,#20428,.T.);
#29153=ORIENTED_EDGE('',*,*,#20427,.T.);
#29154=ORIENTED_EDGE('',*,*,#20431,.T.);
#29155=ORIENTED_EDGE('',*,*,#20434,.T.);
#29156=ORIENTED_EDGE('',*,*,#20437,.T.);
#29157=ORIENTED_EDGE('',*,*,#20441,.T.);
#29158=ORIENTED_EDGE('',*,*,#20446,.T.);
#29159=ORIENTED_EDGE('',*,*,#20445,.T.);
#29160=ORIENTED_EDGE('',*,*,#20457,.F.);
#29161=ORIENTED_EDGE('',*,*,#20458,.T.);
#29162=ORIENTED_EDGE('',*,*,#20383,.T.);
#29163=ORIENTED_EDGE('',*,*,#20456,.F.);
#29164=ORIENTED_EDGE('',*,*,#20455,.T.);
#29165=ORIENTED_EDGE('',*,*,#20459,.F.);
#29166=ORIENTED_EDGE('',*,*,#20452,.F.);
#29167=ORIENTED_EDGE('',*,*,#20443,.F.);
#29168=ORIENTED_EDGE('',*,*,#20442,.F.);
#29169=ORIENTED_EDGE('',*,*,#20439,.F.);
#29170=ORIENTED_EDGE('',*,*,#20438,.F.);
#29171=ORIENTED_EDGE('',*,*,#20435,.F.);
#29172=ORIENTED_EDGE('',*,*,#20432,.F.);
#29173=ORIENTED_EDGE('',*,*,#20429,.F.);
#29174=ORIENTED_EDGE('',*,*,#20425,.F.);
#29175=ORIENTED_EDGE('',*,*,#20422,.F.);
#29176=ORIENTED_EDGE('',*,*,#20419,.F.);
#29177=ORIENTED_EDGE('',*,*,#20416,.F.);
#29178=ORIENTED_EDGE('',*,*,#20413,.F.);
#29179=ORIENTED_EDGE('',*,*,#20410,.F.);
#29180=ORIENTED_EDGE('',*,*,#20407,.F.);
#29181=ORIENTED_EDGE('',*,*,#20404,.F.);
#29182=ORIENTED_EDGE('',*,*,#20401,.F.);
#29183=ORIENTED_EDGE('',*,*,#20397,.F.);
#29184=ORIENTED_EDGE('',*,*,#20394,.F.);
#29185=ORIENTED_EDGE('',*,*,#20391,.F.);
#29186=ORIENTED_EDGE('',*,*,#20388,.F.);
#29187=ORIENTED_EDGE('',*,*,#20384,.F.);
#29188=ORIENTED_EDGE('',*,*,#20458,.F.);
#29189=ORIENTED_EDGE('',*,*,#20460,.F.);
#29190=ORIENTED_EDGE('',*,*,#20320,.F.);
#29191=ORIENTED_EDGE('',*,*,#20324,.F.);
#29192=ORIENTED_EDGE('',*,*,#20327,.F.);
#29193=ORIENTED_EDGE('',*,*,#20330,.F.);
#29194=ORIENTED_EDGE('',*,*,#20334,.F.);
#29195=ORIENTED_EDGE('',*,*,#20337,.F.);
#29196=ORIENTED_EDGE('',*,*,#20341,.F.);
#29197=ORIENTED_EDGE('',*,*,#20340,.F.);
#29198=ORIENTED_EDGE('',*,*,#20344,.F.);
#29199=ORIENTED_EDGE('',*,*,#20347,.F.);
#29200=ORIENTED_EDGE('',*,*,#20350,.F.);
#29201=ORIENTED_EDGE('',*,*,#20354,.F.);
#29202=ORIENTED_EDGE('',*,*,#20357,.F.);
#29203=ORIENTED_EDGE('',*,*,#20360,.F.);
#29204=ORIENTED_EDGE('',*,*,#20363,.F.);
#29205=ORIENTED_EDGE('',*,*,#20366,.F.);
#29206=ORIENTED_EDGE('',*,*,#20370,.F.);
#29207=ORIENTED_EDGE('',*,*,#20369,.F.);
#29208=ORIENTED_EDGE('',*,*,#20373,.F.);
#29209=ORIENTED_EDGE('',*,*,#20376,.F.);
#29210=ORIENTED_EDGE('',*,*,#20379,.F.);
#29211=ORIENTED_EDGE('',*,*,#20449,.F.);
#29212=ORIENTED_EDGE('',*,*,#20461,.T.);
#29213=ORIENTED_EDGE('',*,*,#20462,.T.);
#29214=ORIENTED_EDGE('',*,*,#20459,.T.);
#29215=ORIENTED_EDGE('',*,*,#20321,.T.);
#29216=ORIENTED_EDGE('',*,*,#20460,.T.);
#29217=ORIENTED_EDGE('',*,*,#20457,.T.);
#29218=ORIENTED_EDGE('',*,*,#20462,.F.);
#29219=ORIENTED_EDGE('',*,*,#20463,.F.);
#29220=ORIENTED_EDGE('',*,*,#20461,.F.);
#29221=ORIENTED_EDGE('',*,*,#20450,.T.);
#29222=ORIENTED_EDGE('',*,*,#20464,.T.);
#29223=ORIENTED_EDGE('',*,*,#20465,.T.);
#29224=ORIENTED_EDGE('',*,*,#20464,.F.);
#29225=ORIENTED_EDGE('',*,*,#20453,.T.);
#29226=ORIENTED_EDGE('',*,*,#20448,.T.);
#29227=ORIENTED_EDGE('',*,*,#20454,.T.);
#29228=ORIENTED_EDGE('',*,*,#20465,.F.);
#29229=ORIENTED_EDGE('',*,*,#20466,.F.);
#29230=ORIENTED_EDGE('',*,*,#20467,.F.);
#29231=ORIENTED_EDGE('',*,*,#20468,.F.);
#29232=ORIENTED_EDGE('',*,*,#20469,.F.);
#29233=ORIENTED_EDGE('',*,*,#20468,.T.);
#29234=ORIENTED_EDGE('',*,*,#20470,.F.);
#29235=ORIENTED_EDGE('',*,*,#20471,.F.);
#29236=ORIENTED_EDGE('',*,*,#20472,.F.);
#29237=ORIENTED_EDGE('',*,*,#20473,.F.);
#29238=ORIENTED_EDGE('',*,*,#20470,.T.);
#29239=ORIENTED_EDGE('',*,*,#20467,.T.);
#29240=ORIENTED_EDGE('',*,*,#20474,.T.);
#29241=ORIENTED_EDGE('',*,*,#20475,.T.);
#29242=ORIENTED_EDGE('',*,*,#20476,.F.);
#29243=ORIENTED_EDGE('',*,*,#20477,.F.);
#29244=ORIENTED_EDGE('',*,*,#20475,.F.);
#29245=ORIENTED_EDGE('',*,*,#20478,.T.);
#29246=ORIENTED_EDGE('',*,*,#20479,.T.);
#29247=ORIENTED_EDGE('',*,*,#20480,.F.);
#29248=ORIENTED_EDGE('',*,*,#20481,.T.);
#29249=ORIENTED_EDGE('',*,*,#20482,.T.);
#29250=ORIENTED_EDGE('',*,*,#20483,.T.);
#29251=ORIENTED_EDGE('',*,*,#20484,.F.);
#29252=ORIENTED_EDGE('',*,*,#20485,.T.);
#29253=ORIENTED_EDGE('',*,*,#20486,.T.);
#29254=ORIENTED_EDGE('',*,*,#20487,.T.);
#29255=ORIENTED_EDGE('',*,*,#20488,.F.);
#29256=ORIENTED_EDGE('',*,*,#20489,.T.);
#29257=ORIENTED_EDGE('',*,*,#20490,.T.);
#29258=ORIENTED_EDGE('',*,*,#20491,.T.);
#29259=ORIENTED_EDGE('',*,*,#20492,.F.);
#29260=ORIENTED_EDGE('',*,*,#20493,.T.);
#29261=ORIENTED_EDGE('',*,*,#20494,.T.);
#29262=ORIENTED_EDGE('',*,*,#20495,.T.);
#29263=ORIENTED_EDGE('',*,*,#20496,.F.);
#29264=ORIENTED_EDGE('',*,*,#20497,.T.);
#29265=ORIENTED_EDGE('',*,*,#20498,.T.);
#29266=ORIENTED_EDGE('',*,*,#20499,.T.);
#29267=ORIENTED_EDGE('',*,*,#20500,.F.);
#29268=ORIENTED_EDGE('',*,*,#20501,.T.);
#29269=ORIENTED_EDGE('',*,*,#20502,.T.);
#29270=ORIENTED_EDGE('',*,*,#20503,.T.);
#29271=ORIENTED_EDGE('',*,*,#20504,.F.);
#29272=ORIENTED_EDGE('',*,*,#20505,.T.);
#29273=ORIENTED_EDGE('',*,*,#20506,.T.);
#29274=ORIENTED_EDGE('',*,*,#20507,.T.);
#29275=ORIENTED_EDGE('',*,*,#20508,.F.);
#29276=ORIENTED_EDGE('',*,*,#20509,.T.);
#29277=ORIENTED_EDGE('',*,*,#20510,.T.);
#29278=ORIENTED_EDGE('',*,*,#20511,.T.);
#29279=ORIENTED_EDGE('',*,*,#20512,.F.);
#29280=ORIENTED_EDGE('',*,*,#20513,.T.);
#29281=ORIENTED_EDGE('',*,*,#20514,.T.);
#29282=ORIENTED_EDGE('',*,*,#20515,.T.);
#29283=ORIENTED_EDGE('',*,*,#20516,.F.);
#29284=ORIENTED_EDGE('',*,*,#20517,.T.);
#29285=ORIENTED_EDGE('',*,*,#20518,.T.);
#29286=ORIENTED_EDGE('',*,*,#20519,.T.);
#29287=ORIENTED_EDGE('',*,*,#20520,.F.);
#29288=ORIENTED_EDGE('',*,*,#20521,.T.);
#29289=ORIENTED_EDGE('',*,*,#20522,.T.);
#29290=ORIENTED_EDGE('',*,*,#20523,.T.);
#29291=ORIENTED_EDGE('',*,*,#20524,.F.);
#29292=ORIENTED_EDGE('',*,*,#20525,.T.);
#29293=ORIENTED_EDGE('',*,*,#20526,.T.);
#29294=ORIENTED_EDGE('',*,*,#20527,.T.);
#29295=ORIENTED_EDGE('',*,*,#20528,.F.);
#29296=ORIENTED_EDGE('',*,*,#20529,.T.);
#29297=ORIENTED_EDGE('',*,*,#20530,.T.);
#29298=ORIENTED_EDGE('',*,*,#20531,.T.);
#29299=ORIENTED_EDGE('',*,*,#20532,.F.);
#29300=ORIENTED_EDGE('',*,*,#20533,.T.);
#29301=ORIENTED_EDGE('',*,*,#20534,.T.);
#29302=ORIENTED_EDGE('',*,*,#20535,.T.);
#29303=ORIENTED_EDGE('',*,*,#20536,.F.);
#29304=ORIENTED_EDGE('',*,*,#20537,.T.);
#29305=ORIENTED_EDGE('',*,*,#20538,.T.);
#29306=ORIENTED_EDGE('',*,*,#20539,.T.);
#29307=ORIENTED_EDGE('',*,*,#20540,.F.);
#29308=ORIENTED_EDGE('',*,*,#20541,.T.);
#29309=ORIENTED_EDGE('',*,*,#20542,.T.);
#29310=ORIENTED_EDGE('',*,*,#20543,.T.);
#29311=ORIENTED_EDGE('',*,*,#20544,.F.);
#29312=ORIENTED_EDGE('',*,*,#20472,.T.);
#29313=ORIENTED_EDGE('',*,*,#20466,.T.);
#29314=ORIENTED_EDGE('',*,*,#20469,.T.);
#29315=ORIENTED_EDGE('',*,*,#20545,.F.);
#29316=ORIENTED_EDGE('',*,*,#20546,.T.);
#29317=ORIENTED_EDGE('',*,*,#20547,.T.);
#29318=ORIENTED_EDGE('',*,*,#20548,.T.);
#29319=ORIENTED_EDGE('',*,*,#20549,.F.);
#29320=ORIENTED_EDGE('',*,*,#20550,.T.);
#29321=ORIENTED_EDGE('',*,*,#20551,.T.);
#29322=ORIENTED_EDGE('',*,*,#20552,.T.);
#29323=ORIENTED_EDGE('',*,*,#20553,.F.);
#29324=ORIENTED_EDGE('',*,*,#20554,.T.);
#29325=ORIENTED_EDGE('',*,*,#20555,.T.);
#29326=ORIENTED_EDGE('',*,*,#20556,.T.);
#29327=ORIENTED_EDGE('',*,*,#20557,.F.);
#29328=ORIENTED_EDGE('',*,*,#20558,.T.);
#29329=ORIENTED_EDGE('',*,*,#20559,.T.);
#29330=ORIENTED_EDGE('',*,*,#20560,.T.);
#29331=ORIENTED_EDGE('',*,*,#20561,.F.);
#29332=ORIENTED_EDGE('',*,*,#20562,.T.);
#29333=ORIENTED_EDGE('',*,*,#20563,.T.);
#29334=ORIENTED_EDGE('',*,*,#20564,.T.);
#29335=ORIENTED_EDGE('',*,*,#20565,.F.);
#29336=ORIENTED_EDGE('',*,*,#20566,.T.);
#29337=ORIENTED_EDGE('',*,*,#20567,.T.);
#29338=ORIENTED_EDGE('',*,*,#20568,.T.);
#29339=ORIENTED_EDGE('',*,*,#20569,.F.);
#29340=ORIENTED_EDGE('',*,*,#20570,.T.);
#29341=ORIENTED_EDGE('',*,*,#20571,.T.);
#29342=ORIENTED_EDGE('',*,*,#20572,.T.);
#29343=ORIENTED_EDGE('',*,*,#20573,.F.);
#29344=ORIENTED_EDGE('',*,*,#20574,.T.);
#29345=ORIENTED_EDGE('',*,*,#20575,.T.);
#29346=ORIENTED_EDGE('',*,*,#20576,.T.);
#29347=ORIENTED_EDGE('',*,*,#20577,.F.);
#29348=ORIENTED_EDGE('',*,*,#20578,.T.);
#29349=ORIENTED_EDGE('',*,*,#20579,.T.);
#29350=ORIENTED_EDGE('',*,*,#20580,.T.);
#29351=ORIENTED_EDGE('',*,*,#20581,.F.);
#29352=ORIENTED_EDGE('',*,*,#20582,.T.);
#29353=ORIENTED_EDGE('',*,*,#20583,.T.);
#29354=ORIENTED_EDGE('',*,*,#20584,.T.);
#29355=ORIENTED_EDGE('',*,*,#20585,.F.);
#29356=ORIENTED_EDGE('',*,*,#20586,.T.);
#29357=ORIENTED_EDGE('',*,*,#20587,.T.);
#29358=ORIENTED_EDGE('',*,*,#20588,.T.);
#29359=ORIENTED_EDGE('',*,*,#20589,.F.);
#29360=ORIENTED_EDGE('',*,*,#20590,.T.);
#29361=ORIENTED_EDGE('',*,*,#20591,.T.);
#29362=ORIENTED_EDGE('',*,*,#20592,.T.);
#29363=ORIENTED_EDGE('',*,*,#20593,.F.);
#29364=ORIENTED_EDGE('',*,*,#20594,.T.);
#29365=ORIENTED_EDGE('',*,*,#20595,.T.);
#29366=ORIENTED_EDGE('',*,*,#20596,.T.);
#29367=ORIENTED_EDGE('',*,*,#20597,.F.);
#29368=ORIENTED_EDGE('',*,*,#20598,.T.);
#29369=ORIENTED_EDGE('',*,*,#20599,.T.);
#29370=ORIENTED_EDGE('',*,*,#20600,.T.);
#29371=ORIENTED_EDGE('',*,*,#20601,.F.);
#29372=ORIENTED_EDGE('',*,*,#20602,.T.);
#29373=ORIENTED_EDGE('',*,*,#20603,.T.);
#29374=ORIENTED_EDGE('',*,*,#20604,.T.);
#29375=ORIENTED_EDGE('',*,*,#20605,.F.);
#29376=ORIENTED_EDGE('',*,*,#20606,.T.);
#29377=ORIENTED_EDGE('',*,*,#20607,.T.);
#29378=ORIENTED_EDGE('',*,*,#20608,.T.);
#29379=ORIENTED_EDGE('',*,*,#20609,.F.);
#29380=ORIENTED_EDGE('',*,*,#20610,.T.);
#29381=ORIENTED_EDGE('',*,*,#20611,.T.);
#29382=ORIENTED_EDGE('',*,*,#20612,.T.);
#29383=ORIENTED_EDGE('',*,*,#20613,.F.);
#29384=ORIENTED_EDGE('',*,*,#20614,.T.);
#29385=ORIENTED_EDGE('',*,*,#20615,.T.);
#29386=ORIENTED_EDGE('',*,*,#20616,.T.);
#29387=ORIENTED_EDGE('',*,*,#20617,.F.);
#29388=ORIENTED_EDGE('',*,*,#20618,.T.);
#29389=ORIENTED_EDGE('',*,*,#20543,.F.);
#29390=ORIENTED_EDGE('',*,*,#20619,.T.);
#29391=ORIENTED_EDGE('',*,*,#20620,.F.);
#29392=ORIENTED_EDGE('',*,*,#20621,.F.);
#29393=ORIENTED_EDGE('',*,*,#20622,.F.);
#29394=ORIENTED_EDGE('',*,*,#20620,.T.);
#29395=ORIENTED_EDGE('',*,*,#20623,.T.);
#29396=ORIENTED_EDGE('',*,*,#20541,.F.);
#29397=ORIENTED_EDGE('',*,*,#20542,.F.);
#29398=ORIENTED_EDGE('',*,*,#20623,.F.);
#29399=ORIENTED_EDGE('',*,*,#20619,.F.);
#29400=ORIENTED_EDGE('',*,*,#20624,.T.);
#29401=ORIENTED_EDGE('',*,*,#20617,.T.);
#29402=ORIENTED_EDGE('',*,*,#20625,.T.);
#29403=ORIENTED_EDGE('',*,*,#20626,.T.);
#29404=ORIENTED_EDGE('',*,*,#20613,.T.);
#29405=ORIENTED_EDGE('',*,*,#20627,.T.);
#29406=ORIENTED_EDGE('',*,*,#20628,.T.);
#29407=ORIENTED_EDGE('',*,*,#20609,.T.);
#29408=ORIENTED_EDGE('',*,*,#20629,.T.);
#29409=ORIENTED_EDGE('',*,*,#20630,.T.);
#29410=ORIENTED_EDGE('',*,*,#20605,.T.);
#29411=ORIENTED_EDGE('',*,*,#20631,.T.);
#29412=ORIENTED_EDGE('',*,*,#20632,.T.);
#29413=ORIENTED_EDGE('',*,*,#20601,.T.);
#29414=ORIENTED_EDGE('',*,*,#20633,.T.);
#29415=ORIENTED_EDGE('',*,*,#20634,.T.);
#29416=ORIENTED_EDGE('',*,*,#20597,.T.);
#29417=ORIENTED_EDGE('',*,*,#20635,.T.);
#29418=ORIENTED_EDGE('',*,*,#20636,.T.);
#29419=ORIENTED_EDGE('',*,*,#20593,.T.);
#29420=ORIENTED_EDGE('',*,*,#20637,.T.);
#29421=ORIENTED_EDGE('',*,*,#20638,.T.);
#29422=ORIENTED_EDGE('',*,*,#20589,.T.);
#29423=ORIENTED_EDGE('',*,*,#20639,.T.);
#29424=ORIENTED_EDGE('',*,*,#20640,.T.);
#29425=ORIENTED_EDGE('',*,*,#20585,.T.);
#29426=ORIENTED_EDGE('',*,*,#20641,.T.);
#29427=ORIENTED_EDGE('',*,*,#20642,.T.);
#29428=ORIENTED_EDGE('',*,*,#20581,.T.);
#29429=ORIENTED_EDGE('',*,*,#20643,.T.);
#29430=ORIENTED_EDGE('',*,*,#20644,.T.);
#29431=ORIENTED_EDGE('',*,*,#20577,.T.);
#29432=ORIENTED_EDGE('',*,*,#20645,.T.);
#29433=ORIENTED_EDGE('',*,*,#20646,.T.);
#29434=ORIENTED_EDGE('',*,*,#20573,.T.);
#29435=ORIENTED_EDGE('',*,*,#20647,.T.);
#29436=ORIENTED_EDGE('',*,*,#20648,.T.);
#29437=ORIENTED_EDGE('',*,*,#20569,.T.);
#29438=ORIENTED_EDGE('',*,*,#20649,.T.);
#29439=ORIENTED_EDGE('',*,*,#20650,.T.);
#29440=ORIENTED_EDGE('',*,*,#20565,.T.);
#29441=ORIENTED_EDGE('',*,*,#20651,.T.);
#29442=ORIENTED_EDGE('',*,*,#20652,.T.);
#29443=ORIENTED_EDGE('',*,*,#20561,.T.);
#29444=ORIENTED_EDGE('',*,*,#20653,.T.);
#29445=ORIENTED_EDGE('',*,*,#20654,.T.);
#29446=ORIENTED_EDGE('',*,*,#20557,.T.);
#29447=ORIENTED_EDGE('',*,*,#20655,.T.);
#29448=ORIENTED_EDGE('',*,*,#20656,.T.);
#29449=ORIENTED_EDGE('',*,*,#20553,.T.);
#29450=ORIENTED_EDGE('',*,*,#20657,.T.);
#29451=ORIENTED_EDGE('',*,*,#20658,.T.);
#29452=ORIENTED_EDGE('',*,*,#20549,.T.);
#29453=ORIENTED_EDGE('',*,*,#20659,.T.);
#29454=ORIENTED_EDGE('',*,*,#20660,.T.);
#29455=ORIENTED_EDGE('',*,*,#20545,.T.);
#29456=ORIENTED_EDGE('',*,*,#20471,.T.);
#29457=ORIENTED_EDGE('',*,*,#20473,.T.);
#29458=ORIENTED_EDGE('',*,*,#20544,.T.);
#29459=ORIENTED_EDGE('',*,*,#20621,.T.);
#29460=ORIENTED_EDGE('',*,*,#20622,.T.);
#29461=ORIENTED_EDGE('',*,*,#20540,.T.);
#29462=ORIENTED_EDGE('',*,*,#20661,.T.);
#29463=ORIENTED_EDGE('',*,*,#20662,.T.);
#29464=ORIENTED_EDGE('',*,*,#20536,.T.);
#29465=ORIENTED_EDGE('',*,*,#20663,.T.);
#29466=ORIENTED_EDGE('',*,*,#20664,.T.);
#29467=ORIENTED_EDGE('',*,*,#20532,.T.);
#29468=ORIENTED_EDGE('',*,*,#20665,.T.);
#29469=ORIENTED_EDGE('',*,*,#20666,.T.);
#29470=ORIENTED_EDGE('',*,*,#20528,.T.);
#29471=ORIENTED_EDGE('',*,*,#20667,.T.);
#29472=ORIENTED_EDGE('',*,*,#20668,.T.);
#29473=ORIENTED_EDGE('',*,*,#20524,.T.);
#29474=ORIENTED_EDGE('',*,*,#20669,.T.);
#29475=ORIENTED_EDGE('',*,*,#20670,.T.);
#29476=ORIENTED_EDGE('',*,*,#20520,.T.);
#29477=ORIENTED_EDGE('',*,*,#20671,.T.);
#29478=ORIENTED_EDGE('',*,*,#20672,.T.);
#29479=ORIENTED_EDGE('',*,*,#20516,.T.);
#29480=ORIENTED_EDGE('',*,*,#20673,.T.);
#29481=ORIENTED_EDGE('',*,*,#20674,.T.);
#29482=ORIENTED_EDGE('',*,*,#20512,.T.);
#29483=ORIENTED_EDGE('',*,*,#20675,.T.);
#29484=ORIENTED_EDGE('',*,*,#20676,.T.);
#29485=ORIENTED_EDGE('',*,*,#20508,.T.);
#29486=ORIENTED_EDGE('',*,*,#20677,.T.);
#29487=ORIENTED_EDGE('',*,*,#20678,.T.);
#29488=ORIENTED_EDGE('',*,*,#20504,.T.);
#29489=ORIENTED_EDGE('',*,*,#20679,.T.);
#29490=ORIENTED_EDGE('',*,*,#20680,.T.);
#29491=ORIENTED_EDGE('',*,*,#20500,.T.);
#29492=ORIENTED_EDGE('',*,*,#20681,.T.);
#29493=ORIENTED_EDGE('',*,*,#20682,.T.);
#29494=ORIENTED_EDGE('',*,*,#20496,.T.);
#29495=ORIENTED_EDGE('',*,*,#20683,.T.);
#29496=ORIENTED_EDGE('',*,*,#20684,.T.);
#29497=ORIENTED_EDGE('',*,*,#20492,.T.);
#29498=ORIENTED_EDGE('',*,*,#20685,.T.);
#29499=ORIENTED_EDGE('',*,*,#20686,.T.);
#29500=ORIENTED_EDGE('',*,*,#20488,.T.);
#29501=ORIENTED_EDGE('',*,*,#20687,.T.);
#29502=ORIENTED_EDGE('',*,*,#20688,.T.);
#29503=ORIENTED_EDGE('',*,*,#20484,.T.);
#29504=ORIENTED_EDGE('',*,*,#20689,.T.);
#29505=ORIENTED_EDGE('',*,*,#20690,.T.);
#29506=ORIENTED_EDGE('',*,*,#20480,.T.);
#29507=ORIENTED_EDGE('',*,*,#20691,.T.);
#29508=ORIENTED_EDGE('',*,*,#20692,.T.);
#29509=ORIENTED_EDGE('',*,*,#20693,.T.);
#29510=ORIENTED_EDGE('',*,*,#20692,.F.);
#29511=ORIENTED_EDGE('',*,*,#20538,.F.);
#29512=ORIENTED_EDGE('',*,*,#20694,.F.);
#29513=ORIENTED_EDGE('',*,*,#20695,.F.);
#29514=ORIENTED_EDGE('',*,*,#20539,.F.);
#29515=ORIENTED_EDGE('',*,*,#20695,.T.);
#29516=ORIENTED_EDGE('',*,*,#20696,.F.);
#29517=ORIENTED_EDGE('',*,*,#20661,.F.);
#29518=ORIENTED_EDGE('',*,*,#20537,.F.);
#29519=ORIENTED_EDGE('',*,*,#20662,.F.);
#29520=ORIENTED_EDGE('',*,*,#20696,.T.);
#29521=ORIENTED_EDGE('',*,*,#20694,.T.);
#29522=ORIENTED_EDGE('',*,*,#20535,.F.);
#29523=ORIENTED_EDGE('',*,*,#20697,.T.);
#29524=ORIENTED_EDGE('',*,*,#20698,.F.);
#29525=ORIENTED_EDGE('',*,*,#20663,.F.);
#29526=ORIENTED_EDGE('',*,*,#20664,.F.);
#29527=ORIENTED_EDGE('',*,*,#20698,.T.);
#29528=ORIENTED_EDGE('',*,*,#20699,.T.);
#29529=ORIENTED_EDGE('',*,*,#20533,.F.);
#29530=ORIENTED_EDGE('',*,*,#20534,.F.);
#29531=ORIENTED_EDGE('',*,*,#20699,.F.);
#29532=ORIENTED_EDGE('',*,*,#20697,.F.);
#29533=ORIENTED_EDGE('',*,*,#20530,.F.);
#29534=ORIENTED_EDGE('',*,*,#20700,.F.);
#29535=ORIENTED_EDGE('',*,*,#20701,.F.);
#29536=ORIENTED_EDGE('',*,*,#20531,.F.);
#29537=ORIENTED_EDGE('',*,*,#20701,.T.);
#29538=ORIENTED_EDGE('',*,*,#20702,.F.);
#29539=ORIENTED_EDGE('',*,*,#20665,.F.);
#29540=ORIENTED_EDGE('',*,*,#20529,.F.);
#29541=ORIENTED_EDGE('',*,*,#20666,.F.);
#29542=ORIENTED_EDGE('',*,*,#20702,.T.);
#29543=ORIENTED_EDGE('',*,*,#20700,.T.);
#29544=ORIENTED_EDGE('',*,*,#20527,.F.);
#29545=ORIENTED_EDGE('',*,*,#20703,.T.);
#29546=ORIENTED_EDGE('',*,*,#20704,.F.);
#29547=ORIENTED_EDGE('',*,*,#20667,.F.);
#29548=ORIENTED_EDGE('',*,*,#20668,.F.);
#29549=ORIENTED_EDGE('',*,*,#20704,.T.);
#29550=ORIENTED_EDGE('',*,*,#20705,.T.);
#29551=ORIENTED_EDGE('',*,*,#20525,.F.);
#29552=ORIENTED_EDGE('',*,*,#20526,.F.);
#29553=ORIENTED_EDGE('',*,*,#20705,.F.);
#29554=ORIENTED_EDGE('',*,*,#20703,.F.);
#29555=ORIENTED_EDGE('',*,*,#20522,.F.);
#29556=ORIENTED_EDGE('',*,*,#20706,.F.);
#29557=ORIENTED_EDGE('',*,*,#20707,.F.);
#29558=ORIENTED_EDGE('',*,*,#20523,.F.);
#29559=ORIENTED_EDGE('',*,*,#20707,.T.);
#29560=ORIENTED_EDGE('',*,*,#20708,.F.);
#29561=ORIENTED_EDGE('',*,*,#20669,.F.);
#29562=ORIENTED_EDGE('',*,*,#20521,.F.);
#29563=ORIENTED_EDGE('',*,*,#20670,.F.);
#29564=ORIENTED_EDGE('',*,*,#20708,.T.);
#29565=ORIENTED_EDGE('',*,*,#20706,.T.);
#29566=ORIENTED_EDGE('',*,*,#20519,.F.);
#29567=ORIENTED_EDGE('',*,*,#20709,.T.);
#29568=ORIENTED_EDGE('',*,*,#20710,.F.);
#29569=ORIENTED_EDGE('',*,*,#20671,.F.);
#29570=ORIENTED_EDGE('',*,*,#20672,.F.);
#29571=ORIENTED_EDGE('',*,*,#20710,.T.);
#29572=ORIENTED_EDGE('',*,*,#20711,.T.);
#29573=ORIENTED_EDGE('',*,*,#20517,.F.);
#29574=ORIENTED_EDGE('',*,*,#20518,.F.);
#29575=ORIENTED_EDGE('',*,*,#20711,.F.);
#29576=ORIENTED_EDGE('',*,*,#20709,.F.);
#29577=ORIENTED_EDGE('',*,*,#20514,.F.);
#29578=ORIENTED_EDGE('',*,*,#20712,.F.);
#29579=ORIENTED_EDGE('',*,*,#20713,.F.);
#29580=ORIENTED_EDGE('',*,*,#20515,.F.);
#29581=ORIENTED_EDGE('',*,*,#20713,.T.);
#29582=ORIENTED_EDGE('',*,*,#20714,.F.);
#29583=ORIENTED_EDGE('',*,*,#20673,.F.);
#29584=ORIENTED_EDGE('',*,*,#20513,.F.);
#29585=ORIENTED_EDGE('',*,*,#20674,.F.);
#29586=ORIENTED_EDGE('',*,*,#20714,.T.);
#29587=ORIENTED_EDGE('',*,*,#20712,.T.);
#29588=ORIENTED_EDGE('',*,*,#20511,.F.);
#29589=ORIENTED_EDGE('',*,*,#20715,.T.);
#29590=ORIENTED_EDGE('',*,*,#20716,.F.);
#29591=ORIENTED_EDGE('',*,*,#20675,.F.);
#29592=ORIENTED_EDGE('',*,*,#20676,.F.);
#29593=ORIENTED_EDGE('',*,*,#20716,.T.);
#29594=ORIENTED_EDGE('',*,*,#20717,.T.);
#29595=ORIENTED_EDGE('',*,*,#20509,.F.);
#29596=ORIENTED_EDGE('',*,*,#20510,.F.);
#29597=ORIENTED_EDGE('',*,*,#20717,.F.);
#29598=ORIENTED_EDGE('',*,*,#20715,.F.);
#29599=ORIENTED_EDGE('',*,*,#20506,.F.);
#29600=ORIENTED_EDGE('',*,*,#20718,.F.);
#29601=ORIENTED_EDGE('',*,*,#20719,.F.);
#29602=ORIENTED_EDGE('',*,*,#20507,.F.);
#29603=ORIENTED_EDGE('',*,*,#20719,.T.);
#29604=ORIENTED_EDGE('',*,*,#20720,.F.);
#29605=ORIENTED_EDGE('',*,*,#20677,.F.);
#29606=ORIENTED_EDGE('',*,*,#20505,.F.);
#29607=ORIENTED_EDGE('',*,*,#20678,.F.);
#29608=ORIENTED_EDGE('',*,*,#20720,.T.);
#29609=ORIENTED_EDGE('',*,*,#20718,.T.);
#29610=ORIENTED_EDGE('',*,*,#20503,.F.);
#29611=ORIENTED_EDGE('',*,*,#20721,.T.);
#29612=ORIENTED_EDGE('',*,*,#20722,.F.);
#29613=ORIENTED_EDGE('',*,*,#20679,.F.);
#29614=ORIENTED_EDGE('',*,*,#20680,.F.);
#29615=ORIENTED_EDGE('',*,*,#20722,.T.);
#29616=ORIENTED_EDGE('',*,*,#20723,.T.);
#29617=ORIENTED_EDGE('',*,*,#20501,.F.);
#29618=ORIENTED_EDGE('',*,*,#20502,.F.);
#29619=ORIENTED_EDGE('',*,*,#20723,.F.);
#29620=ORIENTED_EDGE('',*,*,#20721,.F.);
#29621=ORIENTED_EDGE('',*,*,#20498,.F.);
#29622=ORIENTED_EDGE('',*,*,#20724,.F.);
#29623=ORIENTED_EDGE('',*,*,#20725,.F.);
#29624=ORIENTED_EDGE('',*,*,#20499,.F.);
#29625=ORIENTED_EDGE('',*,*,#20725,.T.);
#29626=ORIENTED_EDGE('',*,*,#20726,.F.);
#29627=ORIENTED_EDGE('',*,*,#20681,.F.);
#29628=ORIENTED_EDGE('',*,*,#20497,.F.);
#29629=ORIENTED_EDGE('',*,*,#20682,.F.);
#29630=ORIENTED_EDGE('',*,*,#20726,.T.);
#29631=ORIENTED_EDGE('',*,*,#20724,.T.);
#29632=ORIENTED_EDGE('',*,*,#20495,.F.);
#29633=ORIENTED_EDGE('',*,*,#20727,.T.);
#29634=ORIENTED_EDGE('',*,*,#20728,.F.);
#29635=ORIENTED_EDGE('',*,*,#20683,.F.);
#29636=ORIENTED_EDGE('',*,*,#20684,.F.);
#29637=ORIENTED_EDGE('',*,*,#20728,.T.);
#29638=ORIENTED_EDGE('',*,*,#20729,.T.);
#29639=ORIENTED_EDGE('',*,*,#20493,.F.);
#29640=ORIENTED_EDGE('',*,*,#20494,.F.);
#29641=ORIENTED_EDGE('',*,*,#20729,.F.);
#29642=ORIENTED_EDGE('',*,*,#20727,.F.);
#29643=ORIENTED_EDGE('',*,*,#20490,.F.);
#29644=ORIENTED_EDGE('',*,*,#20730,.F.);
#29645=ORIENTED_EDGE('',*,*,#20731,.F.);
#29646=ORIENTED_EDGE('',*,*,#20491,.F.);
#29647=ORIENTED_EDGE('',*,*,#20731,.T.);
#29648=ORIENTED_EDGE('',*,*,#20732,.F.);
#29649=ORIENTED_EDGE('',*,*,#20685,.F.);
#29650=ORIENTED_EDGE('',*,*,#20489,.F.);
#29651=ORIENTED_EDGE('',*,*,#20686,.F.);
#29652=ORIENTED_EDGE('',*,*,#20732,.T.);
#29653=ORIENTED_EDGE('',*,*,#20730,.T.);
#29654=ORIENTED_EDGE('',*,*,#20487,.F.);
#29655=ORIENTED_EDGE('',*,*,#20733,.T.);
#29656=ORIENTED_EDGE('',*,*,#20734,.F.);
#29657=ORIENTED_EDGE('',*,*,#20687,.F.);
#29658=ORIENTED_EDGE('',*,*,#20688,.F.);
#29659=ORIENTED_EDGE('',*,*,#20734,.T.);
#29660=ORIENTED_EDGE('',*,*,#20735,.T.);
#29661=ORIENTED_EDGE('',*,*,#20485,.F.);
#29662=ORIENTED_EDGE('',*,*,#20486,.F.);
#29663=ORIENTED_EDGE('',*,*,#20735,.F.);
#29664=ORIENTED_EDGE('',*,*,#20733,.F.);
#29665=ORIENTED_EDGE('',*,*,#20482,.F.);
#29666=ORIENTED_EDGE('',*,*,#20736,.F.);
#29667=ORIENTED_EDGE('',*,*,#20737,.F.);
#29668=ORIENTED_EDGE('',*,*,#20483,.F.);
#29669=ORIENTED_EDGE('',*,*,#20737,.T.);
#29670=ORIENTED_EDGE('',*,*,#20738,.F.);
#29671=ORIENTED_EDGE('',*,*,#20689,.F.);
#29672=ORIENTED_EDGE('',*,*,#20481,.F.);
#29673=ORIENTED_EDGE('',*,*,#20690,.F.);
#29674=ORIENTED_EDGE('',*,*,#20738,.T.);
#29675=ORIENTED_EDGE('',*,*,#20736,.T.);
#29676=ORIENTED_EDGE('',*,*,#20479,.F.);
#29677=ORIENTED_EDGE('',*,*,#20739,.T.);
#29678=ORIENTED_EDGE('',*,*,#20740,.F.);
#29679=ORIENTED_EDGE('',*,*,#20691,.F.);
#29680=ORIENTED_EDGE('',*,*,#20624,.F.);
#29681=ORIENTED_EDGE('',*,*,#20740,.T.);
#29682=ORIENTED_EDGE('',*,*,#20741,.T.);
#29683=ORIENTED_EDGE('',*,*,#20618,.F.);
#29684=ORIENTED_EDGE('',*,*,#20474,.F.);
#29685=ORIENTED_EDGE('',*,*,#20741,.F.);
#29686=ORIENTED_EDGE('',*,*,#20739,.F.);
#29687=ORIENTED_EDGE('',*,*,#20478,.F.);
#29688=ORIENTED_EDGE('',*,*,#20615,.F.);
#29689=ORIENTED_EDGE('',*,*,#20742,.F.);
#29690=ORIENTED_EDGE('',*,*,#20743,.F.);
#29691=ORIENTED_EDGE('',*,*,#20616,.F.);
#29692=ORIENTED_EDGE('',*,*,#20743,.T.);
#29693=ORIENTED_EDGE('',*,*,#20744,.F.);
#29694=ORIENTED_EDGE('',*,*,#20625,.F.);
#29695=ORIENTED_EDGE('',*,*,#20614,.F.);
#29696=ORIENTED_EDGE('',*,*,#20626,.F.);
#29697=ORIENTED_EDGE('',*,*,#20744,.T.);
#29698=ORIENTED_EDGE('',*,*,#20742,.T.);
#29699=ORIENTED_EDGE('',*,*,#20612,.F.);
#29700=ORIENTED_EDGE('',*,*,#20745,.T.);
#29701=ORIENTED_EDGE('',*,*,#20746,.F.);
#29702=ORIENTED_EDGE('',*,*,#20627,.F.);
#29703=ORIENTED_EDGE('',*,*,#20628,.F.);
#29704=ORIENTED_EDGE('',*,*,#20746,.T.);
#29705=ORIENTED_EDGE('',*,*,#20747,.T.);
#29706=ORIENTED_EDGE('',*,*,#20610,.F.);
#29707=ORIENTED_EDGE('',*,*,#20611,.F.);
#29708=ORIENTED_EDGE('',*,*,#20747,.F.);
#29709=ORIENTED_EDGE('',*,*,#20745,.F.);
#29710=ORIENTED_EDGE('',*,*,#20607,.F.);
#29711=ORIENTED_EDGE('',*,*,#20748,.F.);
#29712=ORIENTED_EDGE('',*,*,#20749,.F.);
#29713=ORIENTED_EDGE('',*,*,#20608,.F.);
#29714=ORIENTED_EDGE('',*,*,#20749,.T.);
#29715=ORIENTED_EDGE('',*,*,#20750,.F.);
#29716=ORIENTED_EDGE('',*,*,#20629,.F.);
#29717=ORIENTED_EDGE('',*,*,#20606,.F.);
#29718=ORIENTED_EDGE('',*,*,#20630,.F.);
#29719=ORIENTED_EDGE('',*,*,#20750,.T.);
#29720=ORIENTED_EDGE('',*,*,#20748,.T.);
#29721=ORIENTED_EDGE('',*,*,#20604,.F.);
#29722=ORIENTED_EDGE('',*,*,#20751,.T.);
#29723=ORIENTED_EDGE('',*,*,#20752,.F.);
#29724=ORIENTED_EDGE('',*,*,#20631,.F.);
#29725=ORIENTED_EDGE('',*,*,#20632,.F.);
#29726=ORIENTED_EDGE('',*,*,#20752,.T.);
#29727=ORIENTED_EDGE('',*,*,#20753,.T.);
#29728=ORIENTED_EDGE('',*,*,#20602,.F.);
#29729=ORIENTED_EDGE('',*,*,#20603,.F.);
#29730=ORIENTED_EDGE('',*,*,#20753,.F.);
#29731=ORIENTED_EDGE('',*,*,#20751,.F.);
#29732=ORIENTED_EDGE('',*,*,#20599,.F.);
#29733=ORIENTED_EDGE('',*,*,#20754,.F.);
#29734=ORIENTED_EDGE('',*,*,#20755,.F.);
#29735=ORIENTED_EDGE('',*,*,#20600,.F.);
#29736=ORIENTED_EDGE('',*,*,#20755,.T.);
#29737=ORIENTED_EDGE('',*,*,#20756,.F.);
#29738=ORIENTED_EDGE('',*,*,#20633,.F.);
#29739=ORIENTED_EDGE('',*,*,#20598,.F.);
#29740=ORIENTED_EDGE('',*,*,#20634,.F.);
#29741=ORIENTED_EDGE('',*,*,#20756,.T.);
#29742=ORIENTED_EDGE('',*,*,#20754,.T.);
#29743=ORIENTED_EDGE('',*,*,#20596,.F.);
#29744=ORIENTED_EDGE('',*,*,#20757,.T.);
#29745=ORIENTED_EDGE('',*,*,#20758,.F.);
#29746=ORIENTED_EDGE('',*,*,#20635,.F.);
#29747=ORIENTED_EDGE('',*,*,#20636,.F.);
#29748=ORIENTED_EDGE('',*,*,#20758,.T.);
#29749=ORIENTED_EDGE('',*,*,#20759,.T.);
#29750=ORIENTED_EDGE('',*,*,#20594,.F.);
#29751=ORIENTED_EDGE('',*,*,#20595,.F.);
#29752=ORIENTED_EDGE('',*,*,#20759,.F.);
#29753=ORIENTED_EDGE('',*,*,#20757,.F.);
#29754=ORIENTED_EDGE('',*,*,#20591,.F.);
#29755=ORIENTED_EDGE('',*,*,#20760,.F.);
#29756=ORIENTED_EDGE('',*,*,#20761,.F.);
#29757=ORIENTED_EDGE('',*,*,#20592,.F.);
#29758=ORIENTED_EDGE('',*,*,#20761,.T.);
#29759=ORIENTED_EDGE('',*,*,#20762,.F.);
#29760=ORIENTED_EDGE('',*,*,#20637,.F.);
#29761=ORIENTED_EDGE('',*,*,#20590,.F.);
#29762=ORIENTED_EDGE('',*,*,#20638,.F.);
#29763=ORIENTED_EDGE('',*,*,#20762,.T.);
#29764=ORIENTED_EDGE('',*,*,#20760,.T.);
#29765=ORIENTED_EDGE('',*,*,#20588,.F.);
#29766=ORIENTED_EDGE('',*,*,#20763,.T.);
#29767=ORIENTED_EDGE('',*,*,#20764,.F.);
#29768=ORIENTED_EDGE('',*,*,#20639,.F.);
#29769=ORIENTED_EDGE('',*,*,#20640,.F.);
#29770=ORIENTED_EDGE('',*,*,#20764,.T.);
#29771=ORIENTED_EDGE('',*,*,#20765,.T.);
#29772=ORIENTED_EDGE('',*,*,#20586,.F.);
#29773=ORIENTED_EDGE('',*,*,#20587,.F.);
#29774=ORIENTED_EDGE('',*,*,#20765,.F.);
#29775=ORIENTED_EDGE('',*,*,#20763,.F.);
#29776=ORIENTED_EDGE('',*,*,#20583,.F.);
#29777=ORIENTED_EDGE('',*,*,#20766,.F.);
#29778=ORIENTED_EDGE('',*,*,#20767,.F.);
#29779=ORIENTED_EDGE('',*,*,#20584,.F.);
#29780=ORIENTED_EDGE('',*,*,#20767,.T.);
#29781=ORIENTED_EDGE('',*,*,#20768,.F.);
#29782=ORIENTED_EDGE('',*,*,#20641,.F.);
#29783=ORIENTED_EDGE('',*,*,#20582,.F.);
#29784=ORIENTED_EDGE('',*,*,#20642,.F.);
#29785=ORIENTED_EDGE('',*,*,#20768,.T.);
#29786=ORIENTED_EDGE('',*,*,#20766,.T.);
#29787=ORIENTED_EDGE('',*,*,#20580,.F.);
#29788=ORIENTED_EDGE('',*,*,#20769,.T.);
#29789=ORIENTED_EDGE('',*,*,#20770,.F.);
#29790=ORIENTED_EDGE('',*,*,#20643,.F.);
#29791=ORIENTED_EDGE('',*,*,#20644,.F.);
#29792=ORIENTED_EDGE('',*,*,#20770,.T.);
#29793=ORIENTED_EDGE('',*,*,#20771,.T.);
#29794=ORIENTED_EDGE('',*,*,#20578,.F.);
#29795=ORIENTED_EDGE('',*,*,#20579,.F.);
#29796=ORIENTED_EDGE('',*,*,#20771,.F.);
#29797=ORIENTED_EDGE('',*,*,#20769,.F.);
#29798=ORIENTED_EDGE('',*,*,#20575,.F.);
#29799=ORIENTED_EDGE('',*,*,#20772,.F.);
#29800=ORIENTED_EDGE('',*,*,#20773,.F.);
#29801=ORIENTED_EDGE('',*,*,#20576,.F.);
#29802=ORIENTED_EDGE('',*,*,#20773,.T.);
#29803=ORIENTED_EDGE('',*,*,#20774,.F.);
#29804=ORIENTED_EDGE('',*,*,#20645,.F.);
#29805=ORIENTED_EDGE('',*,*,#20574,.F.);
#29806=ORIENTED_EDGE('',*,*,#20646,.F.);
#29807=ORIENTED_EDGE('',*,*,#20774,.T.);
#29808=ORIENTED_EDGE('',*,*,#20772,.T.);
#29809=ORIENTED_EDGE('',*,*,#20572,.F.);
#29810=ORIENTED_EDGE('',*,*,#20775,.T.);
#29811=ORIENTED_EDGE('',*,*,#20776,.F.);
#29812=ORIENTED_EDGE('',*,*,#20647,.F.);
#29813=ORIENTED_EDGE('',*,*,#20648,.F.);
#29814=ORIENTED_EDGE('',*,*,#20776,.T.);
#29815=ORIENTED_EDGE('',*,*,#20777,.T.);
#29816=ORIENTED_EDGE('',*,*,#20570,.F.);
#29817=ORIENTED_EDGE('',*,*,#20571,.F.);
#29818=ORIENTED_EDGE('',*,*,#20777,.F.);
#29819=ORIENTED_EDGE('',*,*,#20775,.F.);
#29820=ORIENTED_EDGE('',*,*,#20567,.F.);
#29821=ORIENTED_EDGE('',*,*,#20778,.F.);
#29822=ORIENTED_EDGE('',*,*,#20779,.F.);
#29823=ORIENTED_EDGE('',*,*,#20568,.F.);
#29824=ORIENTED_EDGE('',*,*,#20779,.T.);
#29825=ORIENTED_EDGE('',*,*,#20780,.F.);
#29826=ORIENTED_EDGE('',*,*,#20649,.F.);
#29827=ORIENTED_EDGE('',*,*,#20566,.F.);
#29828=ORIENTED_EDGE('',*,*,#20650,.F.);
#29829=ORIENTED_EDGE('',*,*,#20780,.T.);
#29830=ORIENTED_EDGE('',*,*,#20778,.T.);
#29831=ORIENTED_EDGE('',*,*,#20564,.F.);
#29832=ORIENTED_EDGE('',*,*,#20781,.T.);
#29833=ORIENTED_EDGE('',*,*,#20782,.F.);
#29834=ORIENTED_EDGE('',*,*,#20651,.F.);
#29835=ORIENTED_EDGE('',*,*,#20652,.F.);
#29836=ORIENTED_EDGE('',*,*,#20782,.T.);
#29837=ORIENTED_EDGE('',*,*,#20783,.T.);
#29838=ORIENTED_EDGE('',*,*,#20562,.F.);
#29839=ORIENTED_EDGE('',*,*,#20563,.F.);
#29840=ORIENTED_EDGE('',*,*,#20783,.F.);
#29841=ORIENTED_EDGE('',*,*,#20781,.F.);
#29842=ORIENTED_EDGE('',*,*,#20559,.F.);
#29843=ORIENTED_EDGE('',*,*,#20784,.F.);
#29844=ORIENTED_EDGE('',*,*,#20785,.F.);
#29845=ORIENTED_EDGE('',*,*,#20560,.F.);
#29846=ORIENTED_EDGE('',*,*,#20785,.T.);
#29847=ORIENTED_EDGE('',*,*,#20786,.F.);
#29848=ORIENTED_EDGE('',*,*,#20653,.F.);
#29849=ORIENTED_EDGE('',*,*,#20558,.F.);
#29850=ORIENTED_EDGE('',*,*,#20654,.F.);
#29851=ORIENTED_EDGE('',*,*,#20786,.T.);
#29852=ORIENTED_EDGE('',*,*,#20784,.T.);
#29853=ORIENTED_EDGE('',*,*,#20556,.F.);
#29854=ORIENTED_EDGE('',*,*,#20787,.T.);
#29855=ORIENTED_EDGE('',*,*,#20788,.F.);
#29856=ORIENTED_EDGE('',*,*,#20655,.F.);
#29857=ORIENTED_EDGE('',*,*,#20656,.F.);
#29858=ORIENTED_EDGE('',*,*,#20788,.T.);
#29859=ORIENTED_EDGE('',*,*,#20789,.T.);
#29860=ORIENTED_EDGE('',*,*,#20554,.F.);
#29861=ORIENTED_EDGE('',*,*,#20555,.F.);
#29862=ORIENTED_EDGE('',*,*,#20789,.F.);
#29863=ORIENTED_EDGE('',*,*,#20787,.F.);
#29864=ORIENTED_EDGE('',*,*,#20551,.F.);
#29865=ORIENTED_EDGE('',*,*,#20790,.F.);
#29866=ORIENTED_EDGE('',*,*,#20791,.F.);
#29867=ORIENTED_EDGE('',*,*,#20552,.F.);
#29868=ORIENTED_EDGE('',*,*,#20791,.T.);
#29869=ORIENTED_EDGE('',*,*,#20792,.F.);
#29870=ORIENTED_EDGE('',*,*,#20657,.F.);
#29871=ORIENTED_EDGE('',*,*,#20550,.F.);
#29872=ORIENTED_EDGE('',*,*,#20658,.F.);
#29873=ORIENTED_EDGE('',*,*,#20792,.T.);
#29874=ORIENTED_EDGE('',*,*,#20790,.T.);
#29875=ORIENTED_EDGE('',*,*,#20548,.F.);
#29876=ORIENTED_EDGE('',*,*,#20793,.T.);
#29877=ORIENTED_EDGE('',*,*,#20794,.F.);
#29878=ORIENTED_EDGE('',*,*,#20659,.F.);
#29879=ORIENTED_EDGE('',*,*,#20660,.F.);
#29880=ORIENTED_EDGE('',*,*,#20794,.T.);
#29881=ORIENTED_EDGE('',*,*,#20795,.T.);
#29882=ORIENTED_EDGE('',*,*,#20546,.F.);
#29883=ORIENTED_EDGE('',*,*,#20547,.F.);
#29884=ORIENTED_EDGE('',*,*,#20795,.F.);
#29885=ORIENTED_EDGE('',*,*,#20793,.F.);
#29886=ORIENTED_EDGE('',*,*,#20463,.T.);
#29887=ORIENTED_EDGE('',*,*,#20796,.T.);
#29888=ORIENTED_EDGE('',*,*,#20476,.T.);
#29889=ORIENTED_EDGE('',*,*,#20477,.T.);
#29890=ORIENTED_EDGE('',*,*,#20796,.F.);
#29891=ORIENTED_EDGE('',*,*,#20693,.F.);
#29892=ORIENTED_EDGE('',*,*,#20797,.T.);
#29893=ORIENTED_EDGE('',*,*,#20798,.F.);
#29894=ORIENTED_EDGE('',*,*,#20799,.F.);
#29895=ORIENTED_EDGE('',*,*,#20800,.F.);
#29896=ORIENTED_EDGE('',*,*,#20801,.F.);
#29897=ORIENTED_EDGE('',*,*,#20802,.F.);
#29898=ORIENTED_EDGE('',*,*,#20803,.F.);
#29899=ORIENTED_EDGE('',*,*,#20804,.F.);
#29900=ORIENTED_EDGE('',*,*,#20805,.F.);
#29901=ORIENTED_EDGE('',*,*,#20806,.F.);
#29902=ORIENTED_EDGE('',*,*,#20807,.F.);
#29903=ORIENTED_EDGE('',*,*,#20808,.F.);
#29904=ORIENTED_EDGE('',*,*,#20809,.F.);
#29905=ORIENTED_EDGE('',*,*,#20810,.F.);
#29906=ORIENTED_EDGE('',*,*,#20811,.F.);
#29907=ORIENTED_EDGE('',*,*,#20812,.F.);
#29908=ORIENTED_EDGE('',*,*,#20813,.F.);
#29909=ORIENTED_EDGE('',*,*,#20814,.F.);
#29910=ORIENTED_EDGE('',*,*,#20815,.F.);
#29911=ORIENTED_EDGE('',*,*,#20816,.T.);
#29912=ORIENTED_EDGE('',*,*,#20797,.F.);
#29913=ORIENTED_EDGE('',*,*,#20816,.F.);
#29914=ORIENTED_EDGE('',*,*,#20817,.F.);
#29915=ORIENTED_EDGE('',*,*,#20814,.T.);
#29916=ORIENTED_EDGE('',*,*,#20818,.F.);
#29917=ORIENTED_EDGE('',*,*,#20819,.F.);
#29918=ORIENTED_EDGE('',*,*,#20820,.F.);
#29919=ORIENTED_EDGE('',*,*,#20821,.F.);
#29920=ORIENTED_EDGE('',*,*,#20822,.F.);
#29921=ORIENTED_EDGE('',*,*,#20811,.T.);
#29922=ORIENTED_EDGE('',*,*,#20823,.F.);
#29923=ORIENTED_EDGE('',*,*,#20799,.T.);
#29924=ORIENTED_EDGE('',*,*,#20824,.F.);
#29925=ORIENTED_EDGE('',*,*,#20825,.F.);
#29926=ORIENTED_EDGE('',*,*,#20826,.F.);
#29927=ORIENTED_EDGE('',*,*,#20827,.F.);
#29928=ORIENTED_EDGE('',*,*,#20828,.F.);
#29929=ORIENTED_EDGE('',*,*,#20808,.T.);
#29930=ORIENTED_EDGE('',*,*,#20829,.F.);
#29931=ORIENTED_EDGE('',*,*,#20802,.T.);
#29932=ORIENTED_EDGE('',*,*,#20830,.F.);
#29933=ORIENTED_EDGE('',*,*,#20831,.F.);
#29934=ORIENTED_EDGE('',*,*,#20832,.F.);
#29935=ORIENTED_EDGE('',*,*,#20833,.F.);
#29936=ORIENTED_EDGE('',*,*,#20834,.F.);
#29937=ORIENTED_EDGE('',*,*,#20805,.T.);
#29938=ORIENTED_EDGE('',*,*,#20803,.T.);
#29939=ORIENTED_EDGE('',*,*,#20829,.T.);
#29940=ORIENTED_EDGE('',*,*,#20835,.F.);
#29941=ORIENTED_EDGE('',*,*,#20830,.T.);
#29942=ORIENTED_EDGE('',*,*,#20801,.T.);
#29943=ORIENTED_EDGE('',*,*,#20836,.T.);
#29944=ORIENTED_EDGE('',*,*,#20837,.T.);
#29945=ORIENTED_EDGE('',*,*,#20838,.F.);
#29946=ORIENTED_EDGE('',*,*,#20800,.T.);
#29947=ORIENTED_EDGE('',*,*,#20823,.T.);
#29948=ORIENTED_EDGE('',*,*,#20839,.F.);
#29949=ORIENTED_EDGE('',*,*,#20824,.T.);
#29950=ORIENTED_EDGE('',*,*,#20798,.T.);
#29951=ORIENTED_EDGE('',*,*,#20840,.T.);
#29952=ORIENTED_EDGE('',*,*,#20841,.T.);
#29953=ORIENTED_EDGE('',*,*,#20836,.F.);
#29954=ORIENTED_EDGE('',*,*,#20815,.T.);
#29955=ORIENTED_EDGE('',*,*,#20817,.T.);
#29956=ORIENTED_EDGE('',*,*,#20842,.F.);
#29957=ORIENTED_EDGE('',*,*,#20818,.T.);
#29958=ORIENTED_EDGE('',*,*,#20813,.T.);
#29959=ORIENTED_EDGE('',*,*,#20843,.T.);
#29960=ORIENTED_EDGE('',*,*,#20844,.T.);
#29961=ORIENTED_EDGE('',*,*,#20840,.F.);
#29962=ORIENTED_EDGE('',*,*,#20819,.T.);
#29963=ORIENTED_EDGE('',*,*,#20842,.T.);
#29964=ORIENTED_EDGE('',*,*,#20825,.T.);
#29965=ORIENTED_EDGE('',*,*,#20839,.T.);
#29966=ORIENTED_EDGE('',*,*,#20821,.T.);
#29967=ORIENTED_EDGE('',*,*,#20845,.T.);
#29968=ORIENTED_EDGE('',*,*,#20831,.T.);
#29969=ORIENTED_EDGE('',*,*,#20835,.T.);
#29970=ORIENTED_EDGE('',*,*,#20827,.T.);
#29971=ORIENTED_EDGE('',*,*,#20846,.T.);
#29972=ORIENTED_EDGE('',*,*,#20833,.T.);
#29973=ORIENTED_EDGE('',*,*,#20847,.T.);
#29974=ORIENTED_EDGE('',*,*,#20848,.F.);
#29975=ORIENTED_EDGE('',*,*,#20849,.F.);
#29976=ORIENTED_EDGE('',*,*,#20850,.F.);
#29977=ORIENTED_EDGE('',*,*,#20851,.F.);
#29978=ORIENTED_EDGE('',*,*,#20844,.F.);
#29979=ORIENTED_EDGE('',*,*,#20852,.F.);
#29980=ORIENTED_EDGE('',*,*,#20841,.F.);
#29981=ORIENTED_EDGE('',*,*,#20853,.F.);
#29982=ORIENTED_EDGE('',*,*,#20837,.F.);
#29983=ORIENTED_EDGE('',*,*,#20854,.F.);
#29984=ORIENTED_EDGE('',*,*,#20855,.F.);
#29985=ORIENTED_EDGE('',*,*,#20856,.F.);
#29986=ORIENTED_EDGE('',*,*,#20857,.T.);
#29987=ORIENTED_EDGE('',*,*,#20852,.T.);
#29988=ORIENTED_EDGE('',*,*,#20851,.T.);
#29989=ORIENTED_EDGE('',*,*,#20849,.T.);
#29990=ORIENTED_EDGE('',*,*,#20856,.T.);
#29991=ORIENTED_EDGE('',*,*,#20854,.T.);
#29992=ORIENTED_EDGE('',*,*,#20853,.T.);
#29993=ORIENTED_EDGE('',*,*,#20857,.F.);
#29994=ORIENTED_EDGE('',*,*,#20807,.T.);
#29995=ORIENTED_EDGE('',*,*,#20858,.T.);
#29996=ORIENTED_EDGE('',*,*,#20848,.T.);
#29997=ORIENTED_EDGE('',*,*,#20859,.F.);
#29998=ORIENTED_EDGE('',*,*,#20809,.T.);
#29999=ORIENTED_EDGE('',*,*,#20828,.T.);
#30000=ORIENTED_EDGE('',*,*,#20846,.F.);
#30001=ORIENTED_EDGE('',*,*,#20826,.T.);
#30002=ORIENTED_EDGE('',*,*,#20804,.T.);
#30003=ORIENTED_EDGE('',*,*,#20838,.T.);
#30004=ORIENTED_EDGE('',*,*,#20855,.T.);
#30005=ORIENTED_EDGE('',*,*,#20858,.F.);
#30006=ORIENTED_EDGE('',*,*,#20806,.T.);
#30007=ORIENTED_EDGE('',*,*,#20834,.T.);
#30008=ORIENTED_EDGE('',*,*,#20847,.F.);
#30009=ORIENTED_EDGE('',*,*,#20832,.T.);
#30010=ORIENTED_EDGE('',*,*,#20810,.T.);
#30011=ORIENTED_EDGE('',*,*,#20859,.T.);
#30012=ORIENTED_EDGE('',*,*,#20850,.T.);
#30013=ORIENTED_EDGE('',*,*,#20843,.F.);
#30014=ORIENTED_EDGE('',*,*,#20812,.T.);
#30015=ORIENTED_EDGE('',*,*,#20822,.T.);
#30016=ORIENTED_EDGE('',*,*,#20845,.F.);
#30017=ORIENTED_EDGE('',*,*,#20820,.T.);
#30314=CONICAL_SURFACE('',#33912,1.2885,0.78539816339745);
#30315=CONICAL_SURFACE('',#33997,2.6,0.785398163397448);
#30316=CONICAL_SURFACE('',#34105,1.49337567297406,0.785398163397449);
#30317=CONICAL_SURFACE('',#34145,0.721687836487032,1.02974425867665);
#31851=ADVANCED_FACE('',(#4876),#1945,.T.);
#31852=ADVANCED_FACE('',(#4877),#1946,.T.);
#31853=ADVANCED_FACE('',(#4878),#1947,.T.);
#31854=ADVANCED_FACE('',(#4879),#1948,.T.);
#31855=ADVANCED_FACE('',(#4880),#1949,.T.);
#31856=ADVANCED_FACE('',(#4881),#1950,.T.);
#31857=ADVANCED_FACE('',(#4882),#1951,.T.);
#31858=ADVANCED_FACE('',(#4883),#1952,.T.);
#31859=ADVANCED_FACE('',(#4884),#1953,.T.);
#31860=ADVANCED_FACE('',(#4885),#1954,.T.);
#31861=ADVANCED_FACE('',(#4886),#1955,.T.);
#31862=ADVANCED_FACE('',(#4887),#1956,.T.);
#31863=ADVANCED_FACE('',(#4888),#1957,.T.);
#31864=ADVANCED_FACE('',(#4889),#1958,.T.);
#31865=ADVANCED_FACE('',(#4890),#1959,.T.);
#31866=ADVANCED_FACE('',(#4891),#1960,.T.);
#31867=ADVANCED_FACE('',(#4892),#1961,.T.);
#31868=ADVANCED_FACE('',(#4893),#1962,.T.);
#31869=ADVANCED_FACE('',(#4894),#1963,.T.);
#31870=ADVANCED_FACE('',(#4895),#1964,.T.);
#31871=ADVANCED_FACE('',(#4896),#1965,.T.);
#31872=ADVANCED_FACE('',(#4897),#1966,.T.);
#31873=ADVANCED_FACE('',(#4898),#1967,.T.);
#31874=ADVANCED_FACE('',(#4899),#1968,.T.);
#31875=ADVANCED_FACE('',(#4900),#1969,.T.);
#31876=ADVANCED_FACE('',(#4901),#1970,.T.);
#31877=ADVANCED_FACE('',(#4902),#1971,.T.);
#31878=ADVANCED_FACE('',(#4903),#1972,.T.);
#31879=ADVANCED_FACE('',(#4904),#1973,.T.);
#31880=ADVANCED_FACE('',(#4905),#1974,.T.);
#31881=ADVANCED_FACE('',(#4906),#1975,.T.);
#31882=ADVANCED_FACE('',(#4907),#1976,.T.);
#31883=ADVANCED_FACE('',(#4908),#1977,.T.);
#31884=ADVANCED_FACE('',(#4909),#1978,.T.);
#31885=ADVANCED_FACE('',(#4910),#1979,.T.);
#31886=ADVANCED_FACE('',(#4911),#1980,.T.);
#31887=ADVANCED_FACE('',(#4912),#1981,.T.);
#31888=ADVANCED_FACE('',(#4913),#1982,.T.);
#31889=ADVANCED_FACE('',(#4914),#1983,.T.);
#31890=ADVANCED_FACE('',(#4915),#1984,.T.);
#31891=ADVANCED_FACE('',(#4916),#3207,.F.);
#31892=ADVANCED_FACE('',(#4917),#613,.F.);
#31893=ADVANCED_FACE('',(#4918),#3208,.T.);
#31894=ADVANCED_FACE('',(#4919),#614,.F.);
#31895=ADVANCED_FACE('',(#4920),#97,.F.);
#31896=ADVANCED_FACE('',(#4921,#2229),#3209,.T.);
#31897=ADVANCED_FACE('',(#4922),#30314,.T.);
#31898=ADVANCED_FACE('',(#4923),#3210,.T.);
#31899=ADVANCED_FACE('',(#4924),#3211,.F.);
#31900=ADVANCED_FACE('',(#4925),#3212,.F.);
#31901=ADVANCED_FACE('',(#4926),#3213,.F.);
#31902=ADVANCED_FACE('',(#4927),#1985,.T.);
#31903=ADVANCED_FACE('',(#4928),#3214,.F.);
#31904=ADVANCED_FACE('',(#4929),#3215,.F.);
#31905=ADVANCED_FACE('',(#4930),#3216,.F.);
#31906=ADVANCED_FACE('',(#4931),#30315,.T.);
#31907=ADVANCED_FACE('',(#4932),#3217,.F.);
#31908=ADVANCED_FACE('',(#4933),#3218,.F.);
#31909=ADVANCED_FACE('',(#4934),#3219,.F.);
#31910=ADVANCED_FACE('',(#4935),#3220,.F.);
#31911=ADVANCED_FACE('',(#4936),#3221,.F.);
#31912=ADVANCED_FACE('',(#4937),#3222,.F.);
#31913=ADVANCED_FACE('',(#4938),#3223,.F.);
#31914=ADVANCED_FACE('',(#4939),#3224,.F.);
#31915=ADVANCED_FACE('',(#4940),#3225,.F.);
#31916=ADVANCED_FACE('',(#4941),#3226,.F.);
#31917=ADVANCED_FACE('',(#4942),#3227,.F.);
#31918=ADVANCED_FACE('',(#4943),#3228,.F.);
#31919=ADVANCED_FACE('',(#4944),#3229,.F.);
#31920=ADVANCED_FACE('',(#4945),#3230,.F.);
#31921=ADVANCED_FACE('',(#4946),#3231,.F.);
#31922=ADVANCED_FACE('',(#4947),#3232,.F.);
#31923=ADVANCED_FACE('',(#4948),#3233,.F.);
#31924=ADVANCED_FACE('',(#4949),#3234,.F.);
#31925=ADVANCED_FACE('',(#4950),#3235,.F.);
#31926=ADVANCED_FACE('',(#4951),#3236,.F.);
#31927=ADVANCED_FACE('',(#4952),#3237,.F.);
#31928=ADVANCED_FACE('',(#4953),#3238,.F.);
#31929=ADVANCED_FACE('',(#4954),#3239,.F.);
#31930=ADVANCED_FACE('',(#4955),#3240,.F.);
#31931=ADVANCED_FACE('',(#4956),#3241,.F.);
#31932=ADVANCED_FACE('',(#4957),#3242,.F.);
#31933=ADVANCED_FACE('',(#4958),#3243,.F.);
#31934=ADVANCED_FACE('',(#4959),#3244,.F.);
#31935=ADVANCED_FACE('',(#4960),#3245,.F.);
#31936=ADVANCED_FACE('',(#4961),#3246,.F.);
#31937=ADVANCED_FACE('',(#4962),#3247,.F.);
#31938=ADVANCED_FACE('',(#4963),#3248,.F.);
#31939=ADVANCED_FACE('',(#4964),#3249,.F.);
#31940=ADVANCED_FACE('',(#4965),#3250,.F.);
#31941=ADVANCED_FACE('',(#4966),#3251,.F.);
#31942=ADVANCED_FACE('',(#4967),#3252,.F.);
#31943=ADVANCED_FACE('',(#4968),#3253,.F.);
#31944=ADVANCED_FACE('',(#4969),#3254,.F.);
#31945=ADVANCED_FACE('',(#4970),#3255,.F.);
#31946=ADVANCED_FACE('',(#4971),#3256,.F.);
#31947=ADVANCED_FACE('',(#4972),#3257,.F.);
#31948=ADVANCED_FACE('',(#4973),#3258,.F.);
#31949=ADVANCED_FACE('',(#4974),#3259,.F.);
#31950=ADVANCED_FACE('',(#4975),#3260,.F.);
#31951=ADVANCED_FACE('',(#4976),#3261,.F.);
#31952=ADVANCED_FACE('',(#4977),#3262,.F.);
#31953=ADVANCED_FACE('',(#4978),#3263,.F.);
#31954=ADVANCED_FACE('',(#4979),#3264,.F.);
#31955=ADVANCED_FACE('',(#4980),#3265,.F.);
#31956=ADVANCED_FACE('',(#4981),#3266,.F.);
#31957=ADVANCED_FACE('',(#4982),#3267,.F.);
#31958=ADVANCED_FACE('',(#4983),#3268,.F.);
#31959=ADVANCED_FACE('',(#4984),#3269,.F.);
#31960=ADVANCED_FACE('',(#4985),#3270,.F.);
#31961=ADVANCED_FACE('',(#4986),#3271,.F.);
#31962=ADVANCED_FACE('',(#4987),#3272,.F.);
#31963=ADVANCED_FACE('',(#4988),#3273,.F.);
#31964=ADVANCED_FACE('',(#4989),#3274,.F.);
#31965=ADVANCED_FACE('',(#4990),#3275,.F.);
#31966=ADVANCED_FACE('',(#4991),#3276,.F.);
#31967=ADVANCED_FACE('',(#4992),#3277,.F.);
#31968=ADVANCED_FACE('',(#4993),#3278,.F.);
#31969=ADVANCED_FACE('',(#4994),#3279,.F.);
#31970=ADVANCED_FACE('',(#4995),#3280,.F.);
#31971=ADVANCED_FACE('',(#4996),#3281,.F.);
#31972=ADVANCED_FACE('',(#4997),#3282,.F.);
#31973=ADVANCED_FACE('',(#4998),#3283,.F.);
#31974=ADVANCED_FACE('',(#4999),#3284,.F.);
#31975=ADVANCED_FACE('',(#5000),#3285,.F.);
#31976=ADVANCED_FACE('',(#5001),#3286,.F.);
#31977=ADVANCED_FACE('',(#5002),#3287,.F.);
#31978=ADVANCED_FACE('',(#5003),#3288,.F.);
#31979=ADVANCED_FACE('',(#5004),#3289,.F.);
#31980=ADVANCED_FACE('',(#5005),#3290,.F.);
#31981=ADVANCED_FACE('',(#5006),#3291,.F.);
#31982=ADVANCED_FACE('',(#5007),#3292,.F.);
#31983=ADVANCED_FACE('',(#5008),#3293,.F.);
#31984=ADVANCED_FACE('',(#5009),#3294,.F.);
#31985=ADVANCED_FACE('',(#5010),#3295,.F.);
#31986=ADVANCED_FACE('',(#5011),#3296,.F.);
#31987=ADVANCED_FACE('',(#5012),#3297,.F.);
#31988=ADVANCED_FACE('',(#5013),#3298,.F.);
#31989=ADVANCED_FACE('',(#5014),#3299,.F.);
#31990=ADVANCED_FACE('',(#5015),#3300,.F.);
#31991=ADVANCED_FACE('',(#5016),#3301,.F.);
#31992=ADVANCED_FACE('',(#5017),#3302,.F.);
#31993=ADVANCED_FACE('',(#5018),#3303,.F.);
#31994=ADVANCED_FACE('',(#5019),#3304,.F.);
#31995=ADVANCED_FACE('',(#5020),#3305,.F.);
#31996=ADVANCED_FACE('',(#5021),#3306,.F.);
#31997=ADVANCED_FACE('',(#5022),#3307,.F.);
#31998=ADVANCED_FACE('',(#5023),#3308,.F.);
#31999=ADVANCED_FACE('',(#5024),#3309,.F.);
#32000=ADVANCED_FACE('',(#5025),#3310,.F.);
#32001=ADVANCED_FACE('',(#5026),#3311,.F.);
#32002=ADVANCED_FACE('',(#5027),#3312,.F.);
#32003=ADVANCED_FACE('',(#5028),#3313,.F.);
#32004=ADVANCED_FACE('',(#5029),#3314,.F.);
#32005=ADVANCED_FACE('',(#5030),#3315,.F.);
#32006=ADVANCED_FACE('',(#5031),#3316,.F.);
#32007=ADVANCED_FACE('',(#5032),#3317,.F.);
#32008=ADVANCED_FACE('',(#5033),#3318,.F.);
#32009=ADVANCED_FACE('',(#5034),#98,.T.);
#32010=ADVANCED_FACE('',(#5035,#2230),#3319,.F.);
#32011=ADVANCED_FACE('',(#5036),#30316,.F.);
#32012=ADVANCED_FACE('',(#5037),#1986,.T.);
#32013=ADVANCED_FACE('',(#5038),#1987,.T.);
#32014=ADVANCED_FACE('',(#5039),#1988,.T.);
#32015=ADVANCED_FACE('',(#5040),#1989,.T.);
#32016=ADVANCED_FACE('',(#5041),#1990,.T.);
#32017=ADVANCED_FACE('',(#5042),#1991,.T.);
#32018=ADVANCED_FACE('',(#5043),#3320,.F.);
#32019=ADVANCED_FACE('',(#5044),#3321,.F.);
#32020=ADVANCED_FACE('',(#5045),#3322,.F.);
#32021=ADVANCED_FACE('',(#5046),#3323,.F.);
#32022=ADVANCED_FACE('',(#5047),#3324,.F.);
#32023=ADVANCED_FACE('',(#5048),#3325,.F.);
#32024=ADVANCED_FACE('',(#5049),#3326,.F.);
#32025=ADVANCED_FACE('',(#5050),#3327,.F.);
#32026=ADVANCED_FACE('',(#5051),#3328,.F.);
#32027=ADVANCED_FACE('',(#5052),#3329,.F.);
#32028=ADVANCED_FACE('',(#5053),#3330,.F.);
#32029=ADVANCED_FACE('',(#5054),#3331,.F.);
#32030=ADVANCED_FACE('',(#5055),#3332,.F.);
#32031=ADVANCED_FACE('',(#5056),#3333,.F.);
#32032=ADVANCED_FACE('',(#5057),#3334,.F.);
#32033=ADVANCED_FACE('',(#5058),#30317,.F.);
#32034=ADVANCED_FACE('',(#5059),#3335,.F.);
#32035=ADVANCED_FACE('',(#5060),#3336,.F.);
#32036=ADVANCED_FACE('',(#5061),#3337,.F.);
#32086=CLOSED_SHELL('',(#31851,#31852,#31853,#31854,#31855,#31856,#31857,
#31858,#31859,#31860,#31861,#31862,#31863,#31864,#31865,#31866,#31867,#31868,
#31869,#31870,#31871,#31872,#31873,#31874,#31875,#31876,#31877,#31878,#31879,
#31880,#31881,#31882,#31883,#31884,#31885,#31886,#31887,#31888,#31889,#31890,
#31891,#31892,#31893,#31894,#31895,#31896,#31897,#31898,#31899,#31900,#31901,
#31902,#31903,#31904,#31905,#31906,#31907,#31908,#31909,#31910,#31911,#31912,
#31913,#31914,#31915,#31916,#31917,#31918,#31919,#31920,#31921,#31922,#31923,
#31924,#31925,#31926,#31927,#31928,#31929,#31930,#31931,#31932,#31933,#31934,
#31935,#31936,#31937,#31938,#31939,#31940,#31941,#31942,#31943,#31944,#31945,
#31946,#31947,#31948,#31949,#31950,#31951,#31952,#31953,#31954,#31955,#31956,
#31957,#31958,#31959,#31960,#31961,#31962,#31963,#31964,#31965,#31966,#31967,
#31968,#31969,#31970,#31971,#31972,#31973,#31974,#31975,#31976,#31977,#31978,
#31979,#31980,#31981,#31982,#31983,#31984,#31985,#31986,#31987,#31988,#31989,
#31990,#31991,#31992,#31993,#31994,#31995,#31996,#31997,#31998,#31999,#32000,
#32001,#32002,#32003,#32004,#32005,#32006,#32007,#32008,#32009,#32010,#32011,
#32012,#32013,#32014,#32015,#32016,#32017,#32018,#32019,#32020,#32021,#32022,
#32023,#32024,#32025,#32026,#32027,#32028,#32029,#32030,#32031,#32032,#32033,
#32034,#32035,#32036));
#33856=AXIS2_PLACEMENT_3D('',#107625,#40025,#40026);
#33857=AXIS2_PLACEMENT_3D('',#107626,#40027,#40028);
#33858=AXIS2_PLACEMENT_3D('',#107758,#40030,#40031);
#33859=AXIS2_PLACEMENT_3D('',#107790,#40032,#40033);
#33860=AXIS2_PLACEMENT_3D('',#108210,#40035,#40036);
#33861=AXIS2_PLACEMENT_3D('',#108662,#40038,#40039);
#33862=AXIS2_PLACEMENT_3D('',#109116,#40041,#40042);
#33863=AXIS2_PLACEMENT_3D('',#109550,#40044,#40045);
#33864=AXIS2_PLACEMENT_3D('',#109986,#40047,#40048);
#33865=AXIS2_PLACEMENT_3D('',#110495,#40050,#40051);
#33866=AXIS2_PLACEMENT_3D('',#110943,#40053,#40054);
#33867=AXIS2_PLACEMENT_3D('',#111389,#40056,#40057);
#33868=AXIS2_PLACEMENT_3D('',#111846,#40059,#40060);
#33869=AXIS2_PLACEMENT_3D('',#112306,#40062,#40063);
#33870=AXIS2_PLACEMENT_3D('',#112758,#40065,#40066);
#33871=AXIS2_PLACEMENT_3D('',#113254,#40068,#40069);
#33872=AXIS2_PLACEMENT_3D('',#113688,#40071,#40072);
#33873=AXIS2_PLACEMENT_3D('',#114148,#40074,#40075);
#33874=AXIS2_PLACEMENT_3D('',#114545,#40077,#40078);
#33875=AXIS2_PLACEMENT_3D('',#114987,#40080,#40081);
#33876=AXIS2_PLACEMENT_3D('',#115429,#40083,#40084);
#33877=AXIS2_PLACEMENT_3D('',#115829,#40086,#40087);
#33878=AXIS2_PLACEMENT_3D('',#115963,#40089,#40090);
#33879=AXIS2_PLACEMENT_3D('',#116049,#40091,#40092);
#33880=AXIS2_PLACEMENT_3D('',#116526,#40094,#40095);
#33881=AXIS2_PLACEMENT_3D('',#116944,#40097,#40098);
#33882=AXIS2_PLACEMENT_3D('',#117358,#40100,#40101);
#33883=AXIS2_PLACEMENT_3D('',#117832,#40103,#40104);
#33884=AXIS2_PLACEMENT_3D('',#118267,#40106,#40107);
#33885=AXIS2_PLACEMENT_3D('',#118697,#40109,#40110);
#33886=AXIS2_PLACEMENT_3D('',#119137,#40112,#40113);
#33887=AXIS2_PLACEMENT_3D('',#119567,#40115,#40116);
#33888=AXIS2_PLACEMENT_3D('',#120077,#40118,#40119);
#33889=AXIS2_PLACEMENT_3D('',#120509,#40121,#40122);
#33890=AXIS2_PLACEMENT_3D('',#120927,#40124,#40125);
#33891=AXIS2_PLACEMENT_3D('',#121373,#40127,#40128);
#33892=AXIS2_PLACEMENT_3D('',#121839,#40130,#40131);
#33893=AXIS2_PLACEMENT_3D('',#122266,#40133,#40134);
#33894=AXIS2_PLACEMENT_3D('',#122690,#40136,#40137);
#33895=AXIS2_PLACEMENT_3D('',#123118,#40139,#40140);
#33896=AXIS2_PLACEMENT_3D('',#123559,#40142,#40143);
#33897=AXIS2_PLACEMENT_3D('',#123981,#40145,#40146);
#33898=AXIS2_PLACEMENT_3D('',#124174,#40147,#40148);
#33899=AXIS2_PLACEMENT_3D('',#124301,#40149,#40150);
#33900=AXIS2_PLACEMENT_3D('',#124500,#40151,#40152);
#33901=AXIS2_PLACEMENT_3D('',#124637,#40153,#40154);
#33902=AXIS2_PLACEMENT_3D('',#124640,#40155,#40156);
#33903=AXIS2_PLACEMENT_3D('',#124737,#40157,#40158);
#33904=AXIS2_PLACEMENT_3D('',#125338,#40159,#40160);
#33905=AXIS2_PLACEMENT_3D('',#125341,#40161,#40162);
#33906=AXIS2_PLACEMENT_3D('',#125424,#40163,#40164);
#33907=AXIS2_PLACEMENT_3D('',#125935,#40165,#40166);
#33908=AXIS2_PLACEMENT_3D('',#125937,#40167,#40168);
#33909=AXIS2_PLACEMENT_3D('',#125938,#40169,#40170);
#33910=AXIS2_PLACEMENT_3D('',#125939,#40171,#40172);
#33911=AXIS2_PLACEMENT_3D('',#125941,#40173,#40174);
#33912=AXIS2_PLACEMENT_3D('',#125942,#40175,#40176);
#33913=AXIS2_PLACEMENT_3D('',#125945,#40178,#40179);
#33914=AXIS2_PLACEMENT_3D('',#125946,#40180,#40181);
#33915=AXIS2_PLACEMENT_3D('',#125947,#40182,#40183);
#33916=AXIS2_PLACEMENT_3D('',#125950,#40184,#40185);
#33917=AXIS2_PLACEMENT_3D('',#125954,#40188,#40189);
#33918=AXIS2_PLACEMENT_3D('',#125962,#40192,#40193);
#33919=AXIS2_PLACEMENT_3D('',#125968,#40195,#40196);
#33920=AXIS2_PLACEMENT_3D('',#125971,#40197,#40198);
#33921=AXIS2_PLACEMENT_3D('',#125975,#40200,#40201);
#33922=AXIS2_PLACEMENT_3D('',#125976,#40202,#40203);
#33923=AXIS2_PLACEMENT_3D('',#125978,#40204,#40205);
#33924=AXIS2_PLACEMENT_3D('',#125982,#40207,#40208);
#33925=AXIS2_PLACEMENT_3D('',#125986,#40210,#40211);
#33926=AXIS2_PLACEMENT_3D('',#125990,#40213,#40214);
#33927=AXIS2_PLACEMENT_3D('',#125994,#40216,#40217);
#33928=AXIS2_PLACEMENT_3D('',#125998,#40219,#40220);
#33929=AXIS2_PLACEMENT_3D('',#126002,#40222,#40223);
#33930=AXIS2_PLACEMENT_3D('',#126006,#40225,#40226);
#33931=AXIS2_PLACEMENT_3D('',#126010,#40228,#40229);
#33932=AXIS2_PLACEMENT_3D('',#126014,#40231,#40232);
#33933=AXIS2_PLACEMENT_3D('',#126018,#40234,#40235);
#33934=AXIS2_PLACEMENT_3D('',#126022,#40237,#40238);
#33935=AXIS2_PLACEMENT_3D('',#126026,#40240,#40241);
#33936=AXIS2_PLACEMENT_3D('',#126030,#40243,#40244);
#33937=AXIS2_PLACEMENT_3D('',#126034,#40246,#40247);
#33938=AXIS2_PLACEMENT_3D('',#126038,#40249,#40250);
#33939=AXIS2_PLACEMENT_3D('',#126042,#40252,#40253);
#33940=AXIS2_PLACEMENT_3D('',#126046,#40255,#40256);
#33941=AXIS2_PLACEMENT_3D('',#126050,#40258,#40259);
#33942=AXIS2_PLACEMENT_3D('',#126054,#40261,#40262);
#33943=AXIS2_PLACEMENT_3D('',#126058,#40264,#40265);
#33944=AXIS2_PLACEMENT_3D('',#126062,#40267,#40268);
#33945=AXIS2_PLACEMENT_3D('',#126066,#40270,#40271);
#33946=AXIS2_PLACEMENT_3D('',#126070,#40273,#40274);
#33947=AXIS2_PLACEMENT_3D('',#126074,#40276,#40277);
#33948=AXIS2_PLACEMENT_3D('',#126078,#40279,#40280);
#33949=AXIS2_PLACEMENT_3D('',#126082,#40282,#40283);
#33950=AXIS2_PLACEMENT_3D('',#126086,#40285,#40286);
#33951=AXIS2_PLACEMENT_3D('',#126090,#40288,#40289);
#33952=AXIS2_PLACEMENT_3D('',#126094,#40291,#40292);
#33953=AXIS2_PLACEMENT_3D('',#126098,#40294,#40295);
#33954=AXIS2_PLACEMENT_3D('',#126102,#40297,#40298);
#33955=AXIS2_PLACEMENT_3D('',#126106,#40300,#40301);
#33956=AXIS2_PLACEMENT_3D('',#126109,#40303,#40304);
#33957=AXIS2_PLACEMENT_3D('',#126111,#40305,#40306);
#33958=AXIS2_PLACEMENT_3D('',#126115,#40308,#40309);
#33959=AXIS2_PLACEMENT_3D('',#126119,#40311,#40312);
#33960=AXIS2_PLACEMENT_3D('',#126123,#40314,#40315);
#33961=AXIS2_PLACEMENT_3D('',#126127,#40317,#40318);
#33962=AXIS2_PLACEMENT_3D('',#126131,#40320,#40321);
#33963=AXIS2_PLACEMENT_3D('',#126135,#40323,#40324);
#33964=AXIS2_PLACEMENT_3D('',#126139,#40326,#40327);
#33965=AXIS2_PLACEMENT_3D('',#126143,#40329,#40330);
#33966=AXIS2_PLACEMENT_3D('',#126147,#40332,#40333);
#33967=AXIS2_PLACEMENT_3D('',#126151,#40335,#40336);
#33968=AXIS2_PLACEMENT_3D('',#126155,#40338,#40339);
#33969=AXIS2_PLACEMENT_3D('',#126159,#40341,#40342);
#33970=AXIS2_PLACEMENT_3D('',#126163,#40344,#40345);
#33971=AXIS2_PLACEMENT_3D('',#126167,#40347,#40348);
#33972=AXIS2_PLACEMENT_3D('',#126171,#40350,#40351);
#33973=AXIS2_PLACEMENT_3D('',#126175,#40353,#40354);
#33974=AXIS2_PLACEMENT_3D('',#126179,#40356,#40357);
#33975=AXIS2_PLACEMENT_3D('',#126183,#40359,#40360);
#33976=AXIS2_PLACEMENT_3D('',#126187,#40362,#40363);
#33977=AXIS2_PLACEMENT_3D('',#126191,#40365,#40366);
#33978=AXIS2_PLACEMENT_3D('',#126195,#40368,#40369);
#33979=AXIS2_PLACEMENT_3D('',#126199,#40371,#40372);
#33980=AXIS2_PLACEMENT_3D('',#126203,#40374,#40375);
#33981=AXIS2_PLACEMENT_3D('',#126207,#40377,#40378);
#33982=AXIS2_PLACEMENT_3D('',#126211,#40380,#40381);
#33983=AXIS2_PLACEMENT_3D('',#126215,#40383,#40384);
#33984=AXIS2_PLACEMENT_3D('',#126219,#40386,#40387);
#33985=AXIS2_PLACEMENT_3D('',#126223,#40389,#40390);
#33986=AXIS2_PLACEMENT_3D('',#126227,#40392,#40393);
#33987=AXIS2_PLACEMENT_3D('',#126231,#40395,#40396);
#33988=AXIS2_PLACEMENT_3D('',#126235,#40398,#40399);
#33989=AXIS2_PLACEMENT_3D('',#126239,#40401,#40402);
#33990=AXIS2_PLACEMENT_3D('',#126243,#40404,#40405);
#33991=AXIS2_PLACEMENT_3D('',#126247,#40407,#40408);
#33992=AXIS2_PLACEMENT_3D('',#126251,#40410,#40411);
#33993=AXIS2_PLACEMENT_3D('',#126255,#40413,#40414);
#33994=AXIS2_PLACEMENT_3D('',#126257,#40416,#40417);
#33995=AXIS2_PLACEMENT_3D('',#126265,#40420,#40421);
#33996=AXIS2_PLACEMENT_3D('',#126270,#40423,#40424);
#33997=AXIS2_PLACEMENT_3D('',#126271,#40425,#40426);
#33998=AXIS2_PLACEMENT_3D('',#126512,#40428,#40429);
#33999=AXIS2_PLACEMENT_3D('',#126513,#40430,#40431);
#34000=AXIS2_PLACEMENT_3D('',#126517,#40434,#40435);
#34001=AXIS2_PLACEMENT_3D('',#126519,#40437,#40438);
#34002=AXIS2_PLACEMENT_3D('',#126520,#40439,#40440);
#34003=AXIS2_PLACEMENT_3D('',#126524,#40443,#40444);
#34004=AXIS2_PLACEMENT_3D('',#126526,#40446,#40447);
#34005=AXIS2_PLACEMENT_3D('',#126527,#40448,#40449);
#34006=AXIS2_PLACEMENT_3D('',#126531,#40452,#40453);
#34007=AXIS2_PLACEMENT_3D('',#126533,#40455,#40456);
#34008=AXIS2_PLACEMENT_3D('',#126534,#40457,#40458);
#34009=AXIS2_PLACEMENT_3D('',#126538,#40461,#40462);
#34010=AXIS2_PLACEMENT_3D('',#126540,#40464,#40465);
#34011=AXIS2_PLACEMENT_3D('',#126541,#40466,#40467);
#34012=AXIS2_PLACEMENT_3D('',#126545,#40470,#40471);
#34013=AXIS2_PLACEMENT_3D('',#126547,#40473,#40474);
#34014=AXIS2_PLACEMENT_3D('',#126548,#40475,#40476);
#34015=AXIS2_PLACEMENT_3D('',#126552,#40479,#40480);
#34016=AXIS2_PLACEMENT_3D('',#126554,#40482,#40483);
#34017=AXIS2_PLACEMENT_3D('',#126555,#40484,#40485);
#34018=AXIS2_PLACEMENT_3D('',#126559,#40488,#40489);
#34019=AXIS2_PLACEMENT_3D('',#126561,#40491,#40492);
#34020=AXIS2_PLACEMENT_3D('',#126562,#40493,#40494);
#34021=AXIS2_PLACEMENT_3D('',#126566,#40497,#40498);
#34022=AXIS2_PLACEMENT_3D('',#126568,#40500,#40501);
#34023=AXIS2_PLACEMENT_3D('',#126569,#40502,#40503);
#34024=AXIS2_PLACEMENT_3D('',#126573,#40506,#40507);
#34025=AXIS2_PLACEMENT_3D('',#126575,#40509,#40510);
#34026=AXIS2_PLACEMENT_3D('',#126576,#40511,#40512);
#34027=AXIS2_PLACEMENT_3D('',#126580,#40515,#40516);
#34028=AXIS2_PLACEMENT_3D('',#126582,#40518,#40519);
#34029=AXIS2_PLACEMENT_3D('',#126583,#40520,#40521);
#34030=AXIS2_PLACEMENT_3D('',#126587,#40524,#40525);
#34031=AXIS2_PLACEMENT_3D('',#126589,#40527,#40528);
#34032=AXIS2_PLACEMENT_3D('',#126590,#40529,#40530);
#34033=AXIS2_PLACEMENT_3D('',#126594,#40533,#40534);
#34034=AXIS2_PLACEMENT_3D('',#126596,#40536,#40537);
#34035=AXIS2_PLACEMENT_3D('',#126597,#40538,#40539);
#34036=AXIS2_PLACEMENT_3D('',#126601,#40542,#40543);
#34037=AXIS2_PLACEMENT_3D('',#126603,#40545,#40546);
#34038=AXIS2_PLACEMENT_3D('',#126604,#40547,#40548);
#34039=AXIS2_PLACEMENT_3D('',#126608,#40551,#40552);
#34040=AXIS2_PLACEMENT_3D('',#126610,#40554,#40555);
#34041=AXIS2_PLACEMENT_3D('',#126611,#40556,#40557);
#34042=AXIS2_PLACEMENT_3D('',#126615,#40560,#40561);
#34043=AXIS2_PLACEMENT_3D('',#126617,#40563,#40564);
#34044=AXIS2_PLACEMENT_3D('',#126618,#40565,#40566);
#34045=AXIS2_PLACEMENT_3D('',#126622,#40569,#40570);
#34046=AXIS2_PLACEMENT_3D('',#126624,#40572,#40573);
#34047=AXIS2_PLACEMENT_3D('',#126625,#40574,#40575);
#34048=AXIS2_PLACEMENT_3D('',#126629,#40578,#40579);
#34049=AXIS2_PLACEMENT_3D('',#126631,#40581,#40582);
#34050=AXIS2_PLACEMENT_3D('',#126632,#40583,#40584);
#34051=AXIS2_PLACEMENT_3D('',#126636,#40587,#40588);
#34052=AXIS2_PLACEMENT_3D('',#126638,#40590,#40591);
#34053=AXIS2_PLACEMENT_3D('',#126639,#40592,#40593);
#34054=AXIS2_PLACEMENT_3D('',#126643,#40596,#40597);
#34055=AXIS2_PLACEMENT_3D('',#126645,#40599,#40600);
#34056=AXIS2_PLACEMENT_3D('',#126646,#40601,#40602);
#34057=AXIS2_PLACEMENT_3D('',#126650,#40605,#40606);
#34058=AXIS2_PLACEMENT_3D('',#126652,#40608,#40609);
#34059=AXIS2_PLACEMENT_3D('',#126653,#40610,#40611);
#34060=AXIS2_PLACEMENT_3D('',#126657,#40614,#40615);
#34061=AXIS2_PLACEMENT_3D('',#126659,#40617,#40618);
#34062=AXIS2_PLACEMENT_3D('',#126660,#40619,#40620);
#34063=AXIS2_PLACEMENT_3D('',#126664,#40623,#40624);
#34064=AXIS2_PLACEMENT_3D('',#126666,#40626,#40627);
#34065=AXIS2_PLACEMENT_3D('',#126667,#40628,#40629);
#34066=AXIS2_PLACEMENT_3D('',#126671,#40632,#40633);
#34067=AXIS2_PLACEMENT_3D('',#126673,#40635,#40636);
#34068=AXIS2_PLACEMENT_3D('',#126674,#40637,#40638);
#34069=AXIS2_PLACEMENT_3D('',#126678,#40641,#40642);
#34070=AXIS2_PLACEMENT_3D('',#126680,#40644,#40645);
#34071=AXIS2_PLACEMENT_3D('',#126681,#40646,#40647);
#34072=AXIS2_PLACEMENT_3D('',#126685,#40650,#40651);
#34073=AXIS2_PLACEMENT_3D('',#126687,#40653,#40654);
#34074=AXIS2_PLACEMENT_3D('',#126688,#40655,#40656);
#34075=AXIS2_PLACEMENT_3D('',#126692,#40659,#40660);
#34076=AXIS2_PLACEMENT_3D('',#126694,#40662,#40663);
#34077=AXIS2_PLACEMENT_3D('',#126695,#40664,#40665);
#34078=AXIS2_PLACEMENT_3D('',#126699,#40668,#40669);
#34079=AXIS2_PLACEMENT_3D('',#126701,#40671,#40672);
#34080=AXIS2_PLACEMENT_3D('',#126702,#40673,#40674);
#34081=AXIS2_PLACEMENT_3D('',#126706,#40677,#40678);
#34082=AXIS2_PLACEMENT_3D('',#126708,#40680,#40681);
#34083=AXIS2_PLACEMENT_3D('',#126709,#40682,#40683);
#34084=AXIS2_PLACEMENT_3D('',#126713,#40686,#40687);
#34085=AXIS2_PLACEMENT_3D('',#126715,#40689,#40690);
#34086=AXIS2_PLACEMENT_3D('',#126716,#40691,#40692);
#34087=AXIS2_PLACEMENT_3D('',#126720,#40695,#40696);
#34088=AXIS2_PLACEMENT_3D('',#126722,#40698,#40699);
#34089=AXIS2_PLACEMENT_3D('',#126723,#40700,#40701);
#34090=AXIS2_PLACEMENT_3D('',#126727,#40704,#40705);
#34091=AXIS2_PLACEMENT_3D('',#126729,#40707,#40708);
#34092=AXIS2_PLACEMENT_3D('',#126730,#40709,#40710);
#34093=AXIS2_PLACEMENT_3D('',#126734,#40713,#40714);
#34094=AXIS2_PLACEMENT_3D('',#126736,#40716,#40717);
#34095=AXIS2_PLACEMENT_3D('',#126737,#40718,#40719);
#34096=AXIS2_PLACEMENT_3D('',#126741,#40722,#40723);
#34097=AXIS2_PLACEMENT_3D('',#126743,#40725,#40726);
#34098=AXIS2_PLACEMENT_3D('',#126744,#40727,#40728);
#34099=AXIS2_PLACEMENT_3D('',#126748,#40731,#40732);
#34100=AXIS2_PLACEMENT_3D('',#126750,#40734,#40735);
#34101=AXIS2_PLACEMENT_3D('',#126751,#40736,#40737);
#34102=AXIS2_PLACEMENT_3D('',#126752,#40738,#40739);
#34103=AXIS2_PLACEMENT_3D('',#126753,#40740,#40741);
#34104=AXIS2_PLACEMENT_3D('',#126755,#40742,#40743);
#34105=AXIS2_PLACEMENT_3D('',#126756,#40744,#40745);
#34106=AXIS2_PLACEMENT_3D('',#126763,#40746,#40747);
#34107=AXIS2_PLACEMENT_3D('',#126773,#40748,#40749);
#34108=AXIS2_PLACEMENT_3D('',#126783,#40750,#40751);
#34109=AXIS2_PLACEMENT_3D('',#126793,#40752,#40753);
#34110=AXIS2_PLACEMENT_3D('',#126803,#40754,#40755);
#34111=AXIS2_PLACEMENT_3D('',#126813,#40756,#40757);
#34112=AXIS2_PLACEMENT_3D('',#126818,#40759,#40760);
#34113=AXIS2_PLACEMENT_3D('',#126823,#40763,#40764);
#34114=AXIS2_PLACEMENT_3D('',#126824,#40765,#40766);
#34115=AXIS2_PLACEMENT_3D('',#126828,#40768,#40769);
#34116=AXIS2_PLACEMENT_3D('',#126830,#40771,#40772);
#34117=AXIS2_PLACEMENT_3D('',#126835,#40775,#40776);
#34118=AXIS2_PLACEMENT_3D('',#126836,#40777,#40778);
#34119=AXIS2_PLACEMENT_3D('',#126840,#40780,#40781);
#34120=AXIS2_PLACEMENT_3D('',#126842,#40783,#40784);
#34121=AXIS2_PLACEMENT_3D('',#126847,#40787,#40788);
#34122=AXIS2_PLACEMENT_3D('',#126848,#40789,#40790);
#34123=AXIS2_PLACEMENT_3D('',#126852,#40792,#40793);
#34124=AXIS2_PLACEMENT_3D('',#126854,#40795,#40796);
#34125=AXIS2_PLACEMENT_3D('',#126861,#40801,#40802);
#34126=AXIS2_PLACEMENT_3D('',#126866,#40806,#40807);
#34127=AXIS2_PLACEMENT_3D('',#126871,#40811,#40812);
#34128=AXIS2_PLACEMENT_3D('',#126872,#40813,#40814);
#34129=AXIS2_PLACEMENT_3D('',#126873,#40815,#40816);
#34130=AXIS2_PLACEMENT_3D('',#126875,#40818,#40819);
#34131=AXIS2_PLACEMENT_3D('',#126876,#40820,#40821);
#34132=AXIS2_PLACEMENT_3D('',#126878,#40823,#40824);
#34133=AXIS2_PLACEMENT_3D('',#126880,#40826,#40827);
#34134=AXIS2_PLACEMENT_3D('',#126884,#40829,#40830);
#34135=AXIS2_PLACEMENT_3D('',#126885,#40831,#40832);
#34136=AXIS2_PLACEMENT_3D('',#126887,#40834,#40835);
#34137=AXIS2_PLACEMENT_3D('',#126888,#40836,#40837);
#34138=AXIS2_PLACEMENT_3D('',#126889,#40838,#40839);
#34139=AXIS2_PLACEMENT_3D('',#126890,#40840,#40841);
#34140=AXIS2_PLACEMENT_3D('',#126891,#40842,#40843);
#34141=AXIS2_PLACEMENT_3D('',#126892,#40844,#40845);
#34142=AXIS2_PLACEMENT_3D('',#126893,#40846,#40847);
#34143=AXIS2_PLACEMENT_3D('',#126894,#40848,#40849);
#34144=AXIS2_PLACEMENT_3D('',#126896,#40851,#40852);
#34145=AXIS2_PLACEMENT_3D('',#126897,#40853,#40854);
#34146=AXIS2_PLACEMENT_3D('',#126900,#40856,#40857);
#34147=AXIS2_PLACEMENT_3D('',#126903,#40860,#40861);
#34148=AXIS2_PLACEMENT_3D('',#126904,#40862,#40863);
#40025=DIRECTION('axis',(0.,0.,1.));
#40026=DIRECTION('refdir',(1.,0.,0.));
#40027=DIRECTION('center_axis',(0.,1.,0.));
#40028=DIRECTION('ref_axis',(1.,0.,0.));
#40029=DIRECTION('',(0.,-1.,0.));
#40030=DIRECTION('center_axis',(0.,-1.,0.));
#40031=DIRECTION('ref_axis',(1.,0.,0.));
#40032=DIRECTION('center_axis',(0.,1.,0.));
#40033=DIRECTION('ref_axis',(1.,0.,0.));
#40034=DIRECTION('',(0.,-1.,0.));
#40035=DIRECTION('center_axis',(0.,1.,0.));
#40036=DIRECTION('ref_axis',(1.,0.,0.));
#40037=DIRECTION('',(0.,-1.,0.));
#40038=DIRECTION('center_axis',(0.,1.,0.));
#40039=DIRECTION('ref_axis',(1.,0.,0.));
#40040=DIRECTION('',(0.,-1.,0.));
#40041=DIRECTION('center_axis',(0.,1.,0.));
#40042=DIRECTION('ref_axis',(1.,0.,0.));
#40043=DIRECTION('',(0.,-1.,0.));
#40044=DIRECTION('center_axis',(0.,1.,0.));
#40045=DIRECTION('ref_axis',(1.,0.,0.));
#40046=DIRECTION('',(0.,-1.,0.));
#40047=DIRECTION('center_axis',(0.,1.,0.));
#40048=DIRECTION('ref_axis',(1.,0.,0.));
#40049=DIRECTION('',(0.,-1.,0.));
#40050=DIRECTION('center_axis',(0.,1.,0.));
#40051=DIRECTION('ref_axis',(1.,0.,0.));
#40052=DIRECTION('',(0.,-1.,0.));
#40053=DIRECTION('center_axis',(0.,1.,0.));
#40054=DIRECTION('ref_axis',(1.,0.,0.));
#40055=DIRECTION('',(0.,-1.,0.));
#40056=DIRECTION('center_axis',(0.,1.,0.));
#40057=DIRECTION('ref_axis',(1.,0.,0.));
#40058=DIRECTION('',(0.,-1.,0.));
#40059=DIRECTION('center_axis',(0.,1.,0.));
#40060=DIRECTION('ref_axis',(1.,0.,0.));
#40061=DIRECTION('',(0.,-1.,0.));
#40062=DIRECTION('center_axis',(0.,1.,0.));
#40063=DIRECTION('ref_axis',(1.,0.,0.));
#40064=DIRECTION('',(0.,-1.,0.));
#40065=DIRECTION('center_axis',(0.,1.,0.));
#40066=DIRECTION('ref_axis',(1.,0.,0.));
#40067=DIRECTION('',(0.,-1.,0.));
#40068=DIRECTION('center_axis',(0.,1.,0.));
#40069=DIRECTION('ref_axis',(1.,0.,0.));
#40070=DIRECTION('',(0.,-1.,0.));
#40071=DIRECTION('center_axis',(0.,1.,0.));
#40072=DIRECTION('ref_axis',(1.,0.,0.));
#40073=DIRECTION('',(0.,-1.,0.));
#40074=DIRECTION('center_axis',(0.,1.,0.));
#40075=DIRECTION('ref_axis',(1.,0.,0.));
#40076=DIRECTION('',(0.,-1.,0.));
#40077=DIRECTION('center_axis',(0.,1.,0.));
#40078=DIRECTION('ref_axis',(1.,0.,0.));
#40079=DIRECTION('',(0.,-1.,0.));
#40080=DIRECTION('center_axis',(0.,1.,0.));
#40081=DIRECTION('ref_axis',(1.,0.,0.));
#40082=DIRECTION('',(0.,-1.,0.));
#40083=DIRECTION('center_axis',(0.,1.,0.));
#40084=DIRECTION('ref_axis',(1.,0.,0.));
#40085=DIRECTION('',(0.,-1.,0.));
#40086=DIRECTION('center_axis',(0.,1.,0.));
#40087=DIRECTION('ref_axis',(-0.160348714496653,0.,0.987060428625964));
#40088=DIRECTION('',(0.,-1.,0.));
#40089=DIRECTION('center_axis',(0.,-1.,0.));
#40090=DIRECTION('ref_axis',(1.,0.,-1.41399663505645E-13));
#40091=DIRECTION('center_axis',(0.,1.,0.));
#40092=DIRECTION('ref_axis',(-0.160348714496653,0.,0.987060428625964));
#40093=DIRECTION('',(0.,-1.,0.));
#40094=DIRECTION('center_axis',(0.,1.,0.));
#40095=DIRECTION('ref_axis',(-0.160348714496653,0.,0.987060428625964));
#40096=DIRECTION('',(0.,-1.,0.));
#40097=DIRECTION('center_axis',(0.,1.,0.));
#40098=DIRECTION('ref_axis',(-0.160348714496653,0.,0.987060428625964));
#40099=DIRECTION('',(0.,-1.,0.));
#40100=DIRECTION('center_axis',(0.,1.,0.));
#40101=DIRECTION('ref_axis',(-0.160348714496653,0.,0.987060428625964));
#40102=DIRECTION('',(0.,-1.,0.));
#40103=DIRECTION('center_axis',(0.,1.,0.));
#40104=DIRECTION('ref_axis',(-0.160348714496653,0.,0.987060428625964));
#40105=DIRECTION('',(0.,-1.,0.));
#40106=DIRECTION('center_axis',(0.,1.,0.));
#40107=DIRECTION('ref_axis',(-0.160348714496653,0.,0.987060428625964));
#40108=DIRECTION('',(0.,-1.,0.));
#40109=DIRECTION('center_axis',(0.,1.,0.));
#40110=DIRECTION('ref_axis',(-0.160348714496653,0.,0.987060428625964));
#40111=DIRECTION('',(0.,-1.,0.));
#40112=DIRECTION('center_axis',(0.,1.,0.));
#40113=DIRECTION('ref_axis',(-0.160348714496653,0.,0.987060428625964));
#40114=DIRECTION('',(0.,-1.,0.));
#40115=DIRECTION('center_axis',(0.,1.,0.));
#40116=DIRECTION('ref_axis',(-0.160348714496653,0.,0.987060428625964));
#40117=DIRECTION('',(0.,-1.,0.));
#40118=DIRECTION('center_axis',(0.,1.,0.));
#40119=DIRECTION('ref_axis',(-0.160348714496653,0.,0.987060428625964));
#40120=DIRECTION('',(0.,-1.,0.));
#40121=DIRECTION('center_axis',(0.,1.,0.));
#40122=DIRECTION('ref_axis',(-0.160348714496653,0.,0.987060428625964));
#40123=DIRECTION('',(0.,-1.,0.));
#40124=DIRECTION('center_axis',(0.,1.,0.));
#40125=DIRECTION('ref_axis',(-0.160348714496653,0.,0.987060428625964));
#40126=DIRECTION('',(0.,-1.,0.));
#40127=DIRECTION('center_axis',(0.,1.,0.));
#40128=DIRECTION('ref_axis',(-0.160348714496653,0.,0.987060428625964));
#40129=DIRECTION('',(0.,-1.,0.));
#40130=DIRECTION('center_axis',(0.,1.,0.));
#40131=DIRECTION('ref_axis',(-0.160348714496653,0.,0.987060428625964));
#40132=DIRECTION('',(0.,-1.,0.));
#40133=DIRECTION('center_axis',(0.,1.,0.));
#40134=DIRECTION('ref_axis',(-0.160348714496653,0.,0.987060428625964));
#40135=DIRECTION('',(0.,-1.,0.));
#40136=DIRECTION('center_axis',(0.,1.,0.));
#40137=DIRECTION('ref_axis',(-0.160348714496653,0.,0.987060428625964));
#40138=DIRECTION('',(0.,-1.,0.));
#40139=DIRECTION('center_axis',(0.,1.,0.));
#40140=DIRECTION('ref_axis',(-0.160348714496653,0.,0.987060428625964));
#40141=DIRECTION('',(0.,-1.,0.));
#40142=DIRECTION('center_axis',(0.,1.,0.));
#40143=DIRECTION('ref_axis',(-0.160348714496653,0.,0.987060428625964));
#40144=DIRECTION('',(0.,-1.,0.));
#40145=DIRECTION('center_axis',(0.,1.,0.));
#40146=DIRECTION('ref_axis',(-0.160348714496653,0.,0.987060428625964));
#40147=DIRECTION('center_axis',(0.,1.,0.));
#40148=DIRECTION('ref_axis',(1.,0.,-1.41399663505645E-13));
#40149=DIRECTION('center_axis',(0.,1.,0.));
#40150=DIRECTION('ref_axis',(1.,0.,0.));
#40151=DIRECTION('center_axis',(0.,1.,0.));
#40152=DIRECTION('ref_axis',(1.,0.,0.));
#40153=DIRECTION('center_axis',(0.,1.,0.));
#40154=DIRECTION('ref_axis',(0.,0.,1.));
#40155=DIRECTION('center_axis',(0.,1.,0.));
#40156=DIRECTION('ref_axis',(1.,0.,0.));
#40157=DIRECTION('center_axis',(0.,1.,0.));
#40158=DIRECTION('ref_axis',(1.,0.,0.));
#40159=DIRECTION('center_axis',(0.,1.,0.));
#40160=DIRECTION('ref_axis',(0.,0.,1.));
#40161=DIRECTION('center_axis',(0.,-1.,0.));
#40162=DIRECTION('ref_axis',(1.,0.,0.));
#40163=DIRECTION('center_axis',(0.,-1.,0.));
#40164=DIRECTION('ref_axis',(1.,0.,0.));
#40165=DIRECTION('center_axis',(0.,-1.,0.));
#40166=DIRECTION('ref_axis',(0.,0.,-1.));
#40167=DIRECTION('center_axis',(0.,1.,0.));
#40168=DIRECTION('ref_axis',(1.,0.,0.));
#40169=DIRECTION('center_axis',(1.,0.,0.));
#40170=DIRECTION('ref_axis',(0.,0.,1.));
#40171=DIRECTION('center_axis',(0.,1.,0.));
#40172=DIRECTION('ref_axis',(1.,0.,0.));
#40173=DIRECTION('center_axis',(0.,-1.,0.));
#40174=DIRECTION('ref_axis',(1.,0.,0.));
#40175=DIRECTION('center_axis',(0.,-1.,0.));
#40176=DIRECTION('ref_axis',(1.,0.,0.));
#40177=DIRECTION('',(0.707106781186549,0.707106781186546,8.65956056235495E-17));
#40178=DIRECTION('center_axis',(0.,-1.,0.));
#40179=DIRECTION('ref_axis',(1.,0.,0.));
#40180=DIRECTION('center_axis',(0.,1.,0.));
#40181=DIRECTION('ref_axis',(1.,0.,0.));
#40182=DIRECTION('center_axis',(0.,1.,0.));
#40183=DIRECTION('ref_axis',(-0.17364817766693,0.,0.984807753012208));
#40184=DIRECTION('center_axis',(0.,1.,0.));
#40185=DIRECTION('ref_axis',(1.,0.,0.));
#40186=DIRECTION('',(0.869726513699833,0.,0.49353398197848));
#40187=DIRECTION('',(-0.986074150277955,0.,0.166306254102512));
#40188=DIRECTION('center_axis',(-0.166306254102512,0.,-0.986074150277955));
#40189=DIRECTION('ref_axis',(-0.986074150277955,0.,0.166306254102512));
#40190=DIRECTION('',(0.,-1.,0.));
#40191=DIRECTION('',(0.,1.,0.));
#40192=DIRECTION('center_axis',(-0.49353398197848,0.,0.869726513699833));
#40193=DIRECTION('ref_axis',(0.869726513699833,0.,0.49353398197848));
#40194=DIRECTION('',(0.,1.,0.));
#40195=DIRECTION('center_axis',(0.,-1.,0.));
#40196=DIRECTION('ref_axis',(1.,0.,0.));
#40197=DIRECTION('center_axis',(0.,1.,0.));
#40198=DIRECTION('ref_axis',(1.,0.,0.));
#40199=DIRECTION('',(0.,1.,0.));
#40200=DIRECTION('center_axis',(0.,1.,0.));
#40201=DIRECTION('ref_axis',(1.,0.,0.));
#40202=DIRECTION('center_axis',(0.,1.,0.));
#40203=DIRECTION('ref_axis',(1.,0.,0.));
#40204=DIRECTION('center_axis',(0.,1.,0.));
#40205=DIRECTION('ref_axis',(1.,0.,0.));
#40206=DIRECTION('',(0.,-1.,0.));
#40207=DIRECTION('center_axis',(0.,-1.,0.));
#40208=DIRECTION('ref_axis',(1.,0.,0.));
#40209=DIRECTION('',(0.,1.,0.));
#40210=DIRECTION('center_axis',(0.,1.,0.));
#40211=DIRECTION('ref_axis',(1.,0.,0.));
#40212=DIRECTION('',(0.,-1.,0.));
#40213=DIRECTION('center_axis',(0.,-1.,0.));
#40214=DIRECTION('ref_axis',(1.,0.,0.));
#40215=DIRECTION('',(0.,1.,0.));
#40216=DIRECTION('center_axis',(0.,1.,0.));
#40217=DIRECTION('ref_axis',(1.,0.,0.));
#40218=DIRECTION('',(0.,-1.,0.));
#40219=DIRECTION('center_axis',(0.,-1.,0.));
#40220=DIRECTION('ref_axis',(1.,0.,0.));
#40221=DIRECTION('',(0.,1.,0.));
#40222=DIRECTION('center_axis',(0.,1.,0.));
#40223=DIRECTION('ref_axis',(1.,0.,0.));
#40224=DIRECTION('',(0.,-1.,0.));
#40225=DIRECTION('center_axis',(0.,-1.,0.));
#40226=DIRECTION('ref_axis',(1.,0.,0.));
#40227=DIRECTION('',(0.,1.,0.));
#40228=DIRECTION('center_axis',(0.,1.,0.));
#40229=DIRECTION('ref_axis',(1.,0.,0.));
#40230=DIRECTION('',(0.,-1.,0.));
#40231=DIRECTION('center_axis',(0.,-1.,0.));
#40232=DIRECTION('ref_axis',(1.,0.,0.));
#40233=DIRECTION('',(0.,1.,0.));
#40234=DIRECTION('center_axis',(0.,1.,0.));
#40235=DIRECTION('ref_axis',(1.,0.,0.));
#40236=DIRECTION('',(0.,-1.,0.));
#40237=DIRECTION('center_axis',(0.,-1.,0.));
#40238=DIRECTION('ref_axis',(1.,0.,0.));
#40239=DIRECTION('',(0.,1.,0.));
#40240=DIRECTION('center_axis',(0.,1.,0.));
#40241=DIRECTION('ref_axis',(1.,0.,0.));
#40242=DIRECTION('',(0.,-1.,0.));
#40243=DIRECTION('center_axis',(0.,-1.,0.));
#40244=DIRECTION('ref_axis',(1.,0.,0.));
#40245=DIRECTION('',(0.,1.,0.));
#40246=DIRECTION('center_axis',(0.,1.,0.));
#40247=DIRECTION('ref_axis',(1.,0.,0.));
#40248=DIRECTION('',(0.,-1.,0.));
#40249=DIRECTION('center_axis',(0.,-1.,0.));
#40250=DIRECTION('ref_axis',(1.,0.,0.));
#40251=DIRECTION('',(0.,1.,0.));
#40252=DIRECTION('center_axis',(0.,1.,0.));
#40253=DIRECTION('ref_axis',(1.,0.,0.));
#40254=DIRECTION('',(0.,-1.,0.));
#40255=DIRECTION('center_axis',(0.,-1.,0.));
#40256=DIRECTION('ref_axis',(1.,0.,0.));
#40257=DIRECTION('',(0.,1.,0.));
#40258=DIRECTION('center_axis',(0.,1.,0.));
#40259=DIRECTION('ref_axis',(1.,0.,0.));
#40260=DIRECTION('',(0.,-1.,0.));
#40261=DIRECTION('center_axis',(0.,-1.,0.));
#40262=DIRECTION('ref_axis',(1.,0.,0.));
#40263=DIRECTION('',(0.,1.,0.));
#40264=DIRECTION('center_axis',(0.,1.,0.));
#40265=DIRECTION('ref_axis',(1.,0.,0.));
#40266=DIRECTION('',(0.,-1.,0.));
#40267=DIRECTION('center_axis',(0.,-1.,0.));
#40268=DIRECTION('ref_axis',(1.,0.,0.));
#40269=DIRECTION('',(0.,1.,0.));
#40270=DIRECTION('center_axis',(0.,1.,0.));
#40271=DIRECTION('ref_axis',(1.,0.,0.));
#40272=DIRECTION('',(0.,-1.,0.));
#40273=DIRECTION('center_axis',(0.,-1.,0.));
#40274=DIRECTION('ref_axis',(1.,0.,0.));
#40275=DIRECTION('',(0.,1.,0.));
#40276=DIRECTION('center_axis',(0.,1.,0.));
#40277=DIRECTION('ref_axis',(1.,0.,0.));
#40278=DIRECTION('',(0.,-1.,0.));
#40279=DIRECTION('center_axis',(0.,-1.,0.));
#40280=DIRECTION('ref_axis',(1.,0.,0.));
#40281=DIRECTION('',(0.,1.,0.));
#40282=DIRECTION('center_axis',(0.,1.,0.));
#40283=DIRECTION('ref_axis',(1.,0.,0.));
#40284=DIRECTION('',(0.,-1.,0.));
#40285=DIRECTION('center_axis',(0.,-1.,0.));
#40286=DIRECTION('ref_axis',(1.,0.,0.));
#40287=DIRECTION('',(0.,1.,0.));
#40288=DIRECTION('center_axis',(0.,1.,0.));
#40289=DIRECTION('ref_axis',(1.,0.,0.));
#40290=DIRECTION('',(0.,-1.,0.));
#40291=DIRECTION('center_axis',(0.,-1.,0.));
#40292=DIRECTION('ref_axis',(1.,0.,0.));
#40293=DIRECTION('',(0.,1.,0.));
#40294=DIRECTION('center_axis',(0.,1.,0.));
#40295=DIRECTION('ref_axis',(1.,0.,0.));
#40296=DIRECTION('',(0.,-1.,0.));
#40297=DIRECTION('center_axis',(0.,-1.,0.));
#40298=DIRECTION('ref_axis',(1.,0.,0.));
#40299=DIRECTION('',(0.,1.,0.));
#40300=DIRECTION('center_axis',(0.,1.,0.));
#40301=DIRECTION('ref_axis',(1.,0.,0.));
#40302=DIRECTION('',(0.,-1.,0.));
#40303=DIRECTION('center_axis',(0.,-1.,0.));
#40304=DIRECTION('ref_axis',(1.,0.,0.));
#40305=DIRECTION('center_axis',(0.,-1.,0.));
#40306=DIRECTION('ref_axis',(1.,0.,0.));
#40307=DIRECTION('',(0.,1.,0.));
#40308=DIRECTION('center_axis',(0.,1.,0.));
#40309=DIRECTION('ref_axis',(1.,0.,0.));
#40310=DIRECTION('',(0.,-1.,0.));
#40311=DIRECTION('center_axis',(0.,-1.,0.));
#40312=DIRECTION('ref_axis',(1.,0.,0.));
#40313=DIRECTION('',(0.,1.,0.));
#40314=DIRECTION('center_axis',(0.,1.,0.));
#40315=DIRECTION('ref_axis',(1.,0.,0.));
#40316=DIRECTION('',(0.,-1.,0.));
#40317=DIRECTION('center_axis',(0.,-1.,0.));
#40318=DIRECTION('ref_axis',(1.,0.,0.));
#40319=DIRECTION('',(0.,1.,0.));
#40320=DIRECTION('center_axis',(0.,1.,0.));
#40321=DIRECTION('ref_axis',(1.,0.,0.));
#40322=DIRECTION('',(0.,-1.,0.));
#40323=DIRECTION('center_axis',(0.,-1.,0.));
#40324=DIRECTION('ref_axis',(1.,0.,0.));
#40325=DIRECTION('',(0.,1.,0.));
#40326=DIRECTION('center_axis',(0.,1.,0.));
#40327=DIRECTION('ref_axis',(1.,0.,0.));
#40328=DIRECTION('',(0.,-1.,0.));
#40329=DIRECTION('center_axis',(0.,-1.,0.));
#40330=DIRECTION('ref_axis',(1.,0.,0.));
#40331=DIRECTION('',(0.,1.,0.));
#40332=DIRECTION('center_axis',(0.,1.,0.));
#40333=DIRECTION('ref_axis',(1.,0.,0.));
#40334=DIRECTION('',(0.,-1.,0.));
#40335=DIRECTION('center_axis',(0.,-1.,0.));
#40336=DIRECTION('ref_axis',(1.,0.,0.));
#40337=DIRECTION('',(0.,1.,0.));
#40338=DIRECTION('center_axis',(0.,1.,0.));
#40339=DIRECTION('ref_axis',(1.,0.,0.));
#40340=DIRECTION('',(0.,-1.,0.));
#40341=DIRECTION('center_axis',(0.,-1.,0.));
#40342=DIRECTION('ref_axis',(1.,0.,0.));
#40343=DIRECTION('',(0.,1.,0.));
#40344=DIRECTION('center_axis',(0.,1.,0.));
#40345=DIRECTION('ref_axis',(1.,0.,0.));
#40346=DIRECTION('',(0.,-1.,0.));
#40347=DIRECTION('center_axis',(0.,-1.,0.));
#40348=DIRECTION('ref_axis',(1.,0.,0.));
#40349=DIRECTION('',(0.,1.,0.));
#40350=DIRECTION('center_axis',(0.,1.,0.));
#40351=DIRECTION('ref_axis',(1.,0.,0.));
#40352=DIRECTION('',(0.,-1.,0.));
#40353=DIRECTION('center_axis',(0.,-1.,0.));
#40354=DIRECTION('ref_axis',(1.,0.,0.));
#40355=DIRECTION('',(0.,1.,0.));
#40356=DIRECTION('center_axis',(0.,1.,0.));
#40357=DIRECTION('ref_axis',(1.,0.,0.));
#40358=DIRECTION('',(0.,-1.,0.));
#40359=DIRECTION('center_axis',(0.,-1.,0.));
#40360=DIRECTION('ref_axis',(1.,0.,0.));
#40361=DIRECTION('',(0.,1.,0.));
#40362=DIRECTION('center_axis',(0.,1.,0.));
#40363=DIRECTION('ref_axis',(1.,0.,0.));
#40364=DIRECTION('',(0.,-1.,0.));
#40365=DIRECTION('center_axis',(0.,-1.,0.));
#40366=DIRECTION('ref_axis',(1.,0.,0.));
#40367=DIRECTION('',(0.,1.,0.));
#40368=DIRECTION('center_axis',(0.,1.,0.));
#40369=DIRECTION('ref_axis',(1.,0.,0.));
#40370=DIRECTION('',(0.,-1.,0.));
#40371=DIRECTION('center_axis',(0.,-1.,0.));
#40372=DIRECTION('ref_axis',(1.,0.,0.));
#40373=DIRECTION('',(0.,1.,0.));
#40374=DIRECTION('center_axis',(0.,1.,0.));
#40375=DIRECTION('ref_axis',(1.,0.,0.));
#40376=DIRECTION('',(0.,-1.,0.));
#40377=DIRECTION('center_axis',(0.,-1.,0.));
#40378=DIRECTION('ref_axis',(1.,0.,0.));
#40379=DIRECTION('',(0.,1.,0.));
#40380=DIRECTION('center_axis',(0.,1.,0.));
#40381=DIRECTION('ref_axis',(1.,0.,0.));
#40382=DIRECTION('',(0.,-1.,0.));
#40383=DIRECTION('center_axis',(0.,-1.,0.));
#40384=DIRECTION('ref_axis',(1.,0.,0.));
#40385=DIRECTION('',(0.,1.,0.));
#40386=DIRECTION('center_axis',(0.,1.,0.));
#40387=DIRECTION('ref_axis',(1.,0.,0.));
#40388=DIRECTION('',(0.,-1.,0.));
#40389=DIRECTION('center_axis',(0.,-1.,0.));
#40390=DIRECTION('ref_axis',(1.,0.,0.));
#40391=DIRECTION('',(0.,1.,0.));
#40392=DIRECTION('center_axis',(0.,1.,0.));
#40393=DIRECTION('ref_axis',(1.,0.,0.));
#40394=DIRECTION('',(0.,-1.,0.));
#40395=DIRECTION('center_axis',(0.,-1.,0.));
#40396=DIRECTION('ref_axis',(1.,0.,0.));
#40397=DIRECTION('',(0.,1.,0.));
#40398=DIRECTION('center_axis',(0.,1.,0.));
#40399=DIRECTION('ref_axis',(1.,0.,0.));
#40400=DIRECTION('',(0.,-1.,0.));
#40401=DIRECTION('center_axis',(0.,-1.,0.));
#40402=DIRECTION('ref_axis',(1.,0.,0.));
#40403=DIRECTION('',(0.,1.,0.));
#40404=DIRECTION('center_axis',(0.,1.,0.));
#40405=DIRECTION('ref_axis',(1.,0.,0.));
#40406=DIRECTION('',(0.,-1.,0.));
#40407=DIRECTION('center_axis',(0.,-1.,0.));
#40408=DIRECTION('ref_axis',(1.,0.,0.));
#40409=DIRECTION('',(0.,1.,0.));
#40410=DIRECTION('center_axis',(0.,1.,0.));
#40411=DIRECTION('ref_axis',(1.,0.,0.));
#40412=DIRECTION('',(0.,-1.,0.));
#40413=DIRECTION('center_axis',(0.,-1.,0.));
#40414=DIRECTION('ref_axis',(1.,0.,0.));
#40415=DIRECTION('',(0.,1.,0.));
#40416=DIRECTION('center_axis',(0.0074502908256619,0.,-0.99997224619817));
#40417=DIRECTION('ref_axis',(-0.99997224619817,0.,-0.0074502908256619));
#40418=DIRECTION('',(-0.99997224619817,0.,-0.0074502908256619));
#40419=DIRECTION('',(0.,1.,0.));
#40420=DIRECTION('center_axis',(-0.637062515999984,0.,0.770812137104606));
#40421=DIRECTION('ref_axis',(0.770812137104606,0.,0.637062515999984));
#40422=DIRECTION('',(0.770812137104606,0.,0.637062515999984));
#40423=DIRECTION('center_axis',(0.,1.,0.));
#40424=DIRECTION('ref_axis',(-0.342020143325669,0.,0.939692620785908));
#40425=DIRECTION('center_axis',(0.,1.,0.));
#40426=DIRECTION('ref_axis',(1.,0.,0.));
#40427=DIRECTION('',(0.707106781186547,-0.707106781186548,-8.65956056235493E-17));
#40428=DIRECTION('center_axis',(0.,1.,0.));
#40429=DIRECTION('ref_axis',(1.,0.,0.));
#40430=DIRECTION('center_axis',(0.,1.,0.));
#40431=DIRECTION('ref_axis',(-0.5,0.,0.866025403784438));
#40432=DIRECTION('',(0.648477023773219,0.,0.761234227842015));
#40433=DIRECTION('',(-0.983486691428025,0.,-0.180980462437127));
#40434=DIRECTION('center_axis',(0.180980462437127,0.,-0.983486691428025));
#40435=DIRECTION('ref_axis',(-0.983486691428025,0.,-0.180980462437127));
#40436=DIRECTION('',(0.,1.,0.));
#40437=DIRECTION('center_axis',(-0.761234227842015,0.,0.648477023773219));
#40438=DIRECTION('ref_axis',(0.648477023773219,0.,0.761234227842015));
#40439=DIRECTION('center_axis',(0.349011634277972,0.,-0.937118391207119));
#40440=DIRECTION('ref_axis',(-0.937118391207119,0.,-0.349011634277972));
#40441=DIRECTION('',(-0.937118391207119,0.,-0.349011634277972));
#40442=DIRECTION('',(0.,1.,0.));
#40443=DIRECTION('center_axis',(-0.862276222874172,0.,0.506438264219689));
#40444=DIRECTION('ref_axis',(0.506438264219689,0.,0.862276222874172));
#40445=DIRECTION('',(0.506438264219689,0.,0.862276222874172));
#40446=DIRECTION('center_axis',(0.,1.,0.));
#40447=DIRECTION('ref_axis',(-0.64278760968654,0.,0.766044443118978));
#40448=DIRECTION('center_axis',(0.,1.,0.));
#40449=DIRECTION('ref_axis',(-0.766044443118978,0.,0.642787609686539));
#40450=DIRECTION('',(0.349011634277972,0.,0.937118391207119));
#40451=DIRECTION('',(-0.862276222874171,0.,-0.50643826421969));
#40452=DIRECTION('center_axis',(0.50643826421969,0.,-0.862276222874171));
#40453=DIRECTION('ref_axis',(-0.862276222874171,0.,-0.50643826421969));
#40454=DIRECTION('',(0.,1.,0.));
#40455=DIRECTION('center_axis',(-0.937118391207119,0.,0.349011634277972));
#40456=DIRECTION('ref_axis',(0.349011634277972,0.,0.937118391207119));
#40457=DIRECTION('center_axis',(0.648477023773219,0.,-0.761234227842014));
#40458=DIRECTION('ref_axis',(-0.761234227842014,0.,-0.648477023773219));
#40459=DIRECTION('',(-0.761234227842014,0.,-0.648477023773219));
#40460=DIRECTION('',(0.,1.,0.));
#40461=DIRECTION('center_axis',(-0.983486691428025,0.,0.180980462437126));
#40462=DIRECTION('ref_axis',(0.180980462437126,0.,0.983486691428025));
#40463=DIRECTION('',(0.180980462437126,0.,0.983486691428025));
#40464=DIRECTION('center_axis',(0.,1.,0.));
#40465=DIRECTION('ref_axis',(-0.866025403784439,0.,0.5));
#40466=DIRECTION('center_axis',(0.,1.,0.));
#40467=DIRECTION('ref_axis',(-0.939692620785909,0.,0.342020143325668));
#40468=DIRECTION('',(0.00745029082566051,0.,0.99997224619817));
#40469=DIRECTION('',(-0.637062515999983,0.,-0.770812137104607));
#40470=DIRECTION('center_axis',(0.770812137104607,0.,-0.637062515999983));
#40471=DIRECTION('ref_axis',(-0.637062515999983,0.,-0.770812137104607));
#40472=DIRECTION('',(0.,1.,0.));
#40473=DIRECTION('center_axis',(-0.99997224619817,0.,0.00745029082566051));
#40474=DIRECTION('ref_axis',(0.00745029082566051,0.,0.99997224619817));
#40475=DIRECTION('center_axis',(0.869726513699833,0.,-0.49353398197848));
#40476=DIRECTION('ref_axis',(-0.49353398197848,0.,-0.869726513699833));
#40477=DIRECTION('',(-0.49353398197848,0.,-0.869726513699833));
#40478=DIRECTION('',(0.,1.,0.));
#40479=DIRECTION('center_axis',(-0.986074150277955,0.,-0.166306254102513));
#40480=DIRECTION('ref_axis',(-0.166306254102513,0.,0.986074150277955));
#40481=DIRECTION('',(-0.166306254102513,0.,0.986074150277955));
#40482=DIRECTION('center_axis',(0.,1.,0.));
#40483=DIRECTION('ref_axis',(-0.984807753012208,0.,0.17364817766693));
#40484=DIRECTION('center_axis',(0.,1.,0.));
#40485=DIRECTION('ref_axis',(-1.,0.,-1.83697019872103E-16));
#40486=DIRECTION('',(-0.335009667654806,0.,0.94221469027914));
#40487=DIRECTION('',(-0.335009667654806,0.,-0.94221469027914));
#40488=DIRECTION('center_axis',(0.94221469027914,0.,-0.335009667654806));
#40489=DIRECTION('ref_axis',(-0.335009667654806,0.,-0.94221469027914));
#40490=DIRECTION('',(0.,1.,0.));
#40491=DIRECTION('center_axis',(-0.94221469027914,0.,-0.335009667654806));
#40492=DIRECTION('ref_axis',(-0.335009667654806,0.,0.94221469027914));
#40493=DIRECTION('center_axis',(0.986074150277955,0.,-0.166306254102512));
#40494=DIRECTION('ref_axis',(-0.166306254102512,0.,-0.986074150277955));
#40495=DIRECTION('',(-0.166306254102512,0.,-0.986074150277955));
#40496=DIRECTION('',(0.,1.,0.));
#40497=DIRECTION('center_axis',(-0.869726513699833,0.,-0.49353398197848));
#40498=DIRECTION('ref_axis',(-0.49353398197848,0.,0.869726513699833));
#40499=DIRECTION('',(-0.49353398197848,0.,0.869726513699833));
#40500=DIRECTION('center_axis',(0.,1.,0.));
#40501=DIRECTION('ref_axis',(-0.984807753012208,0.,-0.17364817766693));
#40502=DIRECTION('center_axis',(0.,1.,0.));
#40503=DIRECTION('ref_axis',(-0.939692620785908,0.,-0.342020143325669));
#40504=DIRECTION('',(-0.637062515999984,0.,0.770812137104606));
#40505=DIRECTION('',(0.00745029082566179,0.,-0.99997224619817));
#40506=DIRECTION('center_axis',(0.99997224619817,0.,0.00745029082566179));
#40507=DIRECTION('ref_axis',(0.00745029082566179,0.,-0.99997224619817));
#40508=DIRECTION('',(0.,1.,0.));
#40509=DIRECTION('center_axis',(-0.770812137104606,0.,-0.637062515999984));
#40510=DIRECTION('ref_axis',(-0.637062515999984,0.,0.770812137104606));
#40511=DIRECTION('center_axis',(0.983486691428025,0.,0.180980462437127));
#40512=DIRECTION('ref_axis',(0.180980462437127,0.,-0.983486691428025));
#40513=DIRECTION('',(0.180980462437127,0.,-0.983486691428025));
#40514=DIRECTION('',(0.,1.,0.));
#40515=DIRECTION('center_axis',(-0.648477023773219,0.,-0.761234227842015));
#40516=DIRECTION('ref_axis',(-0.761234227842015,0.,0.648477023773219));
#40517=DIRECTION('',(-0.761234227842015,0.,0.648477023773219));
#40518=DIRECTION('center_axis',(0.,1.,0.));
#40519=DIRECTION('ref_axis',(-0.866025403784438,0.,-0.5));
#40520=DIRECTION('center_axis',(0.,1.,0.));
#40521=DIRECTION('ref_axis',(-0.766044443118978,0.,-0.642787609686539));
#40522=DIRECTION('',(-0.862276222874172,0.,0.506438264219689));
#40523=DIRECTION('',(0.349011634277972,0.,-0.937118391207119));
#40524=DIRECTION('center_axis',(0.937118391207119,0.,0.349011634277972));
#40525=DIRECTION('ref_axis',(0.349011634277972,0.,-0.937118391207119));
#40526=DIRECTION('',(0.,1.,0.));
#40527=DIRECTION('center_axis',(-0.506438264219689,0.,-0.862276222874172));
#40528=DIRECTION('ref_axis',(-0.862276222874172,0.,0.506438264219689));
#40529=DIRECTION('center_axis',(0.862276222874171,0.,0.50643826421969));
#40530=DIRECTION('ref_axis',(0.50643826421969,0.,-0.862276222874171));
#40531=DIRECTION('',(0.50643826421969,0.,-0.862276222874171));
#40532=DIRECTION('',(0.,1.,0.));
#40533=DIRECTION('center_axis',(-0.349011634277972,0.,-0.937118391207119));
#40534=DIRECTION('ref_axis',(-0.937118391207119,0.,0.349011634277972));
#40535=DIRECTION('',(-0.937118391207119,0.,0.349011634277972));
#40536=DIRECTION('center_axis',(0.,1.,0.));
#40537=DIRECTION('ref_axis',(-0.642787609686539,0.,-0.766044443118978));
#40538=DIRECTION('center_axis',(0.,1.,0.));
#40539=DIRECTION('ref_axis',(-0.5,0.,-0.866025403784439));
#40540=DIRECTION('',(-0.983486691428025,0.,0.180980462437126));
#40541=DIRECTION('',(0.648477023773219,0.,-0.761234227842014));
#40542=DIRECTION('center_axis',(0.761234227842014,0.,0.648477023773219));
#40543=DIRECTION('ref_axis',(0.648477023773219,0.,-0.761234227842014));
#40544=DIRECTION('',(0.,1.,0.));
#40545=DIRECTION('center_axis',(-0.180980462437126,0.,-0.983486691428025));
#40546=DIRECTION('ref_axis',(-0.983486691428025,0.,0.180980462437126));
#40547=DIRECTION('center_axis',(0.637062515999983,0.,0.770812137104607));
#40548=DIRECTION('ref_axis',(0.770812137104607,0.,-0.637062515999983));
#40549=DIRECTION('',(0.770812137104607,0.,-0.637062515999983));
#40550=DIRECTION('',(0.,1.,0.));
#40551=DIRECTION('center_axis',(-0.00745029082566107,0.,-0.99997224619817));
#40552=DIRECTION('ref_axis',(-0.99997224619817,0.,0.00745029082566107));
#40553=DIRECTION('',(-0.99997224619817,0.,0.00745029082566107));
#40554=DIRECTION('center_axis',(0.,1.,0.));
#40555=DIRECTION('ref_axis',(-0.342020143325669,0.,-0.939692620785908));
#40556=DIRECTION('center_axis',(0.,1.,0.));
#40557=DIRECTION('ref_axis',(-0.17364817766693,0.,-0.984807753012208));
#40558=DIRECTION('',(-0.986074150277955,0.,-0.166306254102513));
#40559=DIRECTION('',(0.869726513699833,0.,-0.49353398197848));
#40560=DIRECTION('center_axis',(0.49353398197848,0.,0.869726513699833));
#40561=DIRECTION('ref_axis',(0.869726513699833,0.,-0.49353398197848));
#40562=DIRECTION('',(0.,1.,0.));
#40563=DIRECTION('center_axis',(0.166306254102513,0.,-0.986074150277955));
#40564=DIRECTION('ref_axis',(-0.986074150277955,0.,-0.166306254102513));
#40565=DIRECTION('center_axis',(0.335009667654806,0.,0.94221469027914));
#40566=DIRECTION('ref_axis',(0.94221469027914,0.,-0.335009667654806));
#40567=DIRECTION('',(0.94221469027914,0.,-0.335009667654806));
#40568=DIRECTION('',(0.,1.,0.));
#40569=DIRECTION('center_axis',(0.335009667654806,0.,-0.94221469027914));
#40570=DIRECTION('ref_axis',(-0.94221469027914,0.,-0.335009667654806));
#40571=DIRECTION('',(-0.94221469027914,0.,-0.335009667654806));
#40572=DIRECTION('center_axis',(0.,1.,0.));
#40573=DIRECTION('ref_axis',(1.22464679914735E-16,0.,-1.));
#40574=DIRECTION('center_axis',(0.,1.,0.));
#40575=DIRECTION('ref_axis',(0.173648177666931,0.,-0.984807753012208));
#40576=DIRECTION('',(-0.869726513699832,0.,-0.493533981978481));
#40577=DIRECTION('',(0.986074150277955,0.,-0.166306254102512));
#40578=DIRECTION('center_axis',(0.166306254102512,0.,0.986074150277955));
#40579=DIRECTION('ref_axis',(0.986074150277955,0.,-0.166306254102512));
#40580=DIRECTION('',(0.,1.,0.));
#40581=DIRECTION('center_axis',(0.493533981978481,0.,-0.869726513699832));
#40582=DIRECTION('ref_axis',(-0.869726513699832,0.,-0.493533981978481));
#40583=DIRECTION('center_axis',(-0.00745029082566129,0.,0.99997224619817));
#40584=DIRECTION('ref_axis',(0.99997224619817,0.,0.00745029082566129));
#40585=DIRECTION('',(0.99997224619817,0.,0.00745029082566129));
#40586=DIRECTION('',(0.,1.,0.));
#40587=DIRECTION('center_axis',(0.637062515999983,0.,-0.770812137104607));
#40588=DIRECTION('ref_axis',(-0.770812137104607,0.,-0.637062515999983));
#40589=DIRECTION('',(-0.770812137104607,0.,-0.637062515999983));
#40590=DIRECTION('center_axis',(0.,1.,0.));
#40591=DIRECTION('ref_axis',(0.342020143325669,0.,-0.939692620785908));
#40592=DIRECTION('center_axis',(0.,1.,0.));
#40593=DIRECTION('ref_axis',(0.5,0.,-0.866025403784439));
#40594=DIRECTION('',(-0.648477023773219,0.,-0.761234227842014));
#40595=DIRECTION('',(0.983486691428025,0.,0.180980462437126));
#40596=DIRECTION('center_axis',(-0.180980462437126,0.,0.983486691428025));
#40597=DIRECTION('ref_axis',(0.983486691428025,0.,0.180980462437126));
#40598=DIRECTION('',(0.,1.,0.));
#40599=DIRECTION('center_axis',(0.761234227842014,0.,-0.648477023773219));
#40600=DIRECTION('ref_axis',(-0.648477023773219,0.,-0.761234227842014));
#40601=DIRECTION('center_axis',(-0.349011634277972,0.,0.937118391207119));
#40602=DIRECTION('ref_axis',(0.937118391207119,0.,0.349011634277972));
#40603=DIRECTION('',(0.937118391207119,0.,0.349011634277972));
#40604=DIRECTION('',(0.,1.,0.));
#40605=DIRECTION('center_axis',(0.862276222874172,0.,-0.506438264219689));
#40606=DIRECTION('ref_axis',(-0.506438264219689,0.,-0.862276222874172));
#40607=DIRECTION('',(-0.506438264219689,0.,-0.862276222874172));
#40608=DIRECTION('center_axis',(0.,1.,0.));
#40609=DIRECTION('ref_axis',(0.642787609686539,0.,-0.766044443118978));
#40610=DIRECTION('center_axis',(0.,1.,0.));
#40611=DIRECTION('ref_axis',(0.766044443118978,0.,-0.642787609686539));
#40612=DIRECTION('',(-0.349011634277972,0.,-0.937118391207119));
#40613=DIRECTION('',(0.862276222874172,0.,0.506438264219689));
#40614=DIRECTION('center_axis',(-0.50643826421969,0.,0.862276222874171));
#40615=DIRECTION('ref_axis',(0.862276222874171,0.,0.50643826421969));
#40616=DIRECTION('',(0.,1.,0.));
#40617=DIRECTION('center_axis',(0.937118391207119,0.,-0.349011634277972));
#40618=DIRECTION('ref_axis',(-0.349011634277972,0.,-0.937118391207119));
#40619=DIRECTION('center_axis',(-0.648477023773219,0.,0.761234227842014));
#40620=DIRECTION('ref_axis',(0.761234227842014,0.,0.648477023773219));
#40621=DIRECTION('',(0.761234227842014,0.,0.648477023773219));
#40622=DIRECTION('',(0.,1.,0.));
#40623=DIRECTION('center_axis',(0.983486691428025,0.,-0.180980462437126));
#40624=DIRECTION('ref_axis',(-0.180980462437126,0.,-0.983486691428025));
#40625=DIRECTION('',(-0.180980462437126,0.,-0.983486691428025));
#40626=DIRECTION('center_axis',(0.,1.,0.));
#40627=DIRECTION('ref_axis',(0.866025403784439,0.,-0.5));
#40628=DIRECTION('center_axis',(0.,1.,0.));
#40629=DIRECTION('ref_axis',(0.939692620785908,0.,-0.342020143325669));
#40630=DIRECTION('',(-0.00745029082566112,0.,-0.99997224619817));
#40631=DIRECTION('',(0.637062515999983,0.,0.770812137104607));
#40632=DIRECTION('center_axis',(-0.770812137104607,0.,0.637062515999983));
#40633=DIRECTION('ref_axis',(0.637062515999983,0.,0.770812137104607));
#40634=DIRECTION('',(0.,1.,0.));
#40635=DIRECTION('center_axis',(0.99997224619817,0.,-0.00745029082566112));
#40636=DIRECTION('ref_axis',(-0.00745029082566112,0.,-0.99997224619817));
#40637=DIRECTION('center_axis',(-0.869726513699833,0.,0.49353398197848));
#40638=DIRECTION('ref_axis',(0.49353398197848,0.,0.869726513699833));
#40639=DIRECTION('',(0.49353398197848,0.,0.869726513699833));
#40640=DIRECTION('',(0.,1.,0.));
#40641=DIRECTION('center_axis',(0.986074150277955,0.,0.166306254102512));
#40642=DIRECTION('ref_axis',(0.166306254102512,0.,-0.986074150277955));
#40643=DIRECTION('',(0.166306254102512,0.,-0.986074150277955));
#40644=DIRECTION('center_axis',(0.,1.,0.));
#40645=DIRECTION('ref_axis',(0.984807753012208,0.,-0.17364817766693));
#40646=DIRECTION('center_axis',(0.,1.,0.));
#40647=DIRECTION('ref_axis',(1.,0.,6.12323399573677E-17));
#40648=DIRECTION('',(0.335009667654806,0.,-0.94221469027914));
#40649=DIRECTION('',(0.335009667654806,0.,0.94221469027914));
#40650=DIRECTION('center_axis',(-0.94221469027914,0.,0.335009667654806));
#40651=DIRECTION('ref_axis',(0.335009667654806,0.,0.94221469027914));
#40652=DIRECTION('',(0.,1.,0.));
#40653=DIRECTION('center_axis',(0.94221469027914,0.,0.335009667654806));
#40654=DIRECTION('ref_axis',(0.335009667654806,0.,-0.94221469027914));
#40655=DIRECTION('center_axis',(-0.986074150277955,0.,0.166306254102512));
#40656=DIRECTION('ref_axis',(0.166306254102512,0.,0.986074150277955));
#40657=DIRECTION('',(0.166306254102512,0.,0.986074150277955));
#40658=DIRECTION('',(0.,1.,0.));
#40659=DIRECTION('center_axis',(0.869726513699833,0.,0.49353398197848));
#40660=DIRECTION('ref_axis',(0.49353398197848,0.,-0.869726513699833));
#40661=DIRECTION('',(0.49353398197848,0.,-0.869726513699833));
#40662=DIRECTION('center_axis',(0.,1.,0.));
#40663=DIRECTION('ref_axis',(0.984807753012208,0.,0.17364817766693));
#40664=DIRECTION('center_axis',(0.,1.,0.));
#40665=DIRECTION('ref_axis',(0.939692620785908,0.,0.342020143325669));
#40666=DIRECTION('',(0.637062515999983,0.,-0.770812137104607));
#40667=DIRECTION('',(-0.00745029082566129,0.,0.99997224619817));
#40668=DIRECTION('center_axis',(-0.99997224619817,0.,-0.00745029082566129));
#40669=DIRECTION('ref_axis',(-0.00745029082566129,0.,0.99997224619817));
#40670=DIRECTION('',(0.,1.,0.));
#40671=DIRECTION('center_axis',(0.770812137104607,0.,0.637062515999983));
#40672=DIRECTION('ref_axis',(0.637062515999983,0.,-0.770812137104607));
#40673=DIRECTION('center_axis',(-0.983486691428025,0.,-0.180980462437126));
#40674=DIRECTION('ref_axis',(-0.180980462437126,0.,0.983486691428025));
#40675=DIRECTION('',(-0.180980462437126,0.,0.983486691428025));
#40676=DIRECTION('',(0.,1.,0.));
#40677=DIRECTION('center_axis',(0.648477023773219,0.,0.761234227842014));
#40678=DIRECTION('ref_axis',(0.761234227842014,0.,-0.648477023773219));
#40679=DIRECTION('',(0.761234227842014,0.,-0.648477023773219));
#40680=DIRECTION('center_axis',(0.,1.,0.));
#40681=DIRECTION('ref_axis',(0.866025403784439,0.,0.5));
#40682=DIRECTION('center_axis',(0.,1.,0.));
#40683=DIRECTION('ref_axis',(0.766044443118978,0.,0.642787609686539));
#40684=DIRECTION('',(0.862276222874172,0.,-0.506438264219689));
#40685=DIRECTION('',(-0.349011634277972,0.,0.937118391207119));
#40686=DIRECTION('center_axis',(-0.937118391207119,0.,-0.349011634277972));
#40687=DIRECTION('ref_axis',(-0.349011634277972,0.,0.937118391207119));
#40688=DIRECTION('',(0.,1.,0.));
#40689=DIRECTION('center_axis',(0.50643826421969,0.,0.862276222874171));
#40690=DIRECTION('ref_axis',(0.862276222874171,0.,-0.50643826421969));
#40691=DIRECTION('center_axis',(-0.862276222874171,0.,-0.50643826421969));
#40692=DIRECTION('ref_axis',(-0.50643826421969,0.,0.862276222874171));
#40693=DIRECTION('',(-0.50643826421969,0.,0.862276222874171));
#40694=DIRECTION('',(0.,1.,0.));
#40695=DIRECTION('center_axis',(0.349011634277972,0.,0.937118391207119));
#40696=DIRECTION('ref_axis',(0.937118391207119,0.,-0.349011634277972));
#40697=DIRECTION('',(0.937118391207119,0.,-0.349011634277972));
#40698=DIRECTION('center_axis',(0.,1.,0.));
#40699=DIRECTION('ref_axis',(0.642787609686539,0.,0.766044443118978));
#40700=DIRECTION('center_axis',(0.,1.,0.));
#40701=DIRECTION('ref_axis',(0.5,0.,0.866025403784439));
#40702=DIRECTION('',(0.983486691428025,0.,-0.180980462437126));
#40703=DIRECTION('',(-0.648477023773219,0.,0.761234227842014));
#40704=DIRECTION('center_axis',(-0.761234227842014,0.,-0.648477023773219));
#40705=DIRECTION('ref_axis',(-0.648477023773219,0.,0.761234227842014));
#40706=DIRECTION('',(0.,1.,0.));
#40707=DIRECTION('center_axis',(0.180980462437126,0.,0.983486691428025));
#40708=DIRECTION('ref_axis',(0.983486691428025,0.,-0.180980462437126));
#40709=DIRECTION('center_axis',(-0.637062515999983,0.,-0.770812137104607));
#40710=DIRECTION('ref_axis',(-0.770812137104607,0.,0.637062515999983));
#40711=DIRECTION('',(-0.770812137104607,0.,0.637062515999983));
#40712=DIRECTION('',(0.,1.,0.));
#40713=DIRECTION('center_axis',(0.00745029082566112,0.,0.99997224619817));
#40714=DIRECTION('ref_axis',(0.99997224619817,0.,-0.00745029082566112));
#40715=DIRECTION('',(0.99997224619817,0.,-0.00745029082566112));
#40716=DIRECTION('center_axis',(0.,1.,0.));
#40717=DIRECTION('ref_axis',(0.342020143325669,0.,0.939692620785908));
#40718=DIRECTION('center_axis',(0.,1.,0.));
#40719=DIRECTION('ref_axis',(0.17364817766693,0.,0.984807753012208));
#40720=DIRECTION('',(0.986074150277955,0.,0.166306254102512));
#40721=DIRECTION('',(-0.869726513699833,0.,0.49353398197848));
#40722=DIRECTION('center_axis',(-0.49353398197848,0.,-0.869726513699833));
#40723=DIRECTION('ref_axis',(-0.869726513699833,0.,0.49353398197848));
#40724=DIRECTION('',(0.,1.,0.));
#40725=DIRECTION('center_axis',(-0.166306254102512,0.,0.986074150277955));
#40726=DIRECTION('ref_axis',(0.986074150277955,0.,0.166306254102512));
#40727=DIRECTION('center_axis',(-0.335009667654806,0.,-0.94221469027914));
#40728=DIRECTION('ref_axis',(-0.94221469027914,0.,0.335009667654806));
#40729=DIRECTION('',(-0.94221469027914,0.,0.335009667654806));
#40730=DIRECTION('',(0.,1.,0.));
#40731=DIRECTION('center_axis',(-0.335009667654806,0.,0.94221469027914));
#40732=DIRECTION('ref_axis',(0.94221469027914,0.,0.335009667654806));
#40733=DIRECTION('',(0.94221469027914,0.,0.335009667654806));
#40734=DIRECTION('center_axis',(0.,1.,0.));
#40735=DIRECTION('ref_axis',(0.,0.,1.));
#40736=DIRECTION('center_axis',(0.,1.,0.));
#40737=DIRECTION('ref_axis',(0.,0.,1.));
#40738=DIRECTION('center_axis',(-1.,0.,0.));
#40739=DIRECTION('ref_axis',(0.,0.,-1.));
#40740=DIRECTION('center_axis',(0.,1.,0.));
#40741=DIRECTION('ref_axis',(1.,0.,0.));
#40742=DIRECTION('center_axis',(0.,1.,0.));
#40743=DIRECTION('ref_axis',(1.,0.,0.));
#40744=DIRECTION('center_axis',(0.,-1.,0.));
#40745=DIRECTION('ref_axis',(1.,0.,0.));
#40746=DIRECTION('center_axis',(0.,-1.,0.));
#40747=DIRECTION('ref_axis',(1.,0.,0.));
#40748=DIRECTION('center_axis',(0.,-1.,0.));
#40749=DIRECTION('ref_axis',(1.,0.,0.));
#40750=DIRECTION('center_axis',(0.,-1.,0.));
#40751=DIRECTION('ref_axis',(1.,0.,0.));
#40752=DIRECTION('center_axis',(0.,-1.,0.));
#40753=DIRECTION('ref_axis',(1.,0.,0.));
#40754=DIRECTION('center_axis',(0.,-1.,0.));
#40755=DIRECTION('ref_axis',(1.,0.,0.));
#40756=DIRECTION('center_axis',(0.,-1.,0.));
#40757=DIRECTION('ref_axis',(1.,0.,0.));
#40758=DIRECTION('',(-0.707106781186548,-0.707106781186547,-8.65956056235494E-17));
#40759=DIRECTION('center_axis',(0.,-1.,0.));
#40760=DIRECTION('ref_axis',(1.,0.,0.));
#40761=DIRECTION('',(0.,-1.,0.));
#40762=DIRECTION('',(0.,1.,0.));
#40763=DIRECTION('center_axis',(0.,-1.,0.));
#40764=DIRECTION('ref_axis',(1.,0.,0.));
#40765=DIRECTION('center_axis',(0.,-1.,0.));
#40766=DIRECTION('ref_axis',(1.,0.,0.));
#40767=DIRECTION('',(0.,1.,0.));
#40768=DIRECTION('center_axis',(0.,-1.,0.));
#40769=DIRECTION('ref_axis',(1.,0.,0.));
#40770=DIRECTION('',(0.,-1.,0.));
#40771=DIRECTION('center_axis',(0.,-1.,0.));
#40772=DIRECTION('ref_axis',(1.,0.,0.));
#40773=DIRECTION('',(0.,-1.,0.));
#40774=DIRECTION('',(0.,1.,0.));
#40775=DIRECTION('center_axis',(0.,-1.,0.));
#40776=DIRECTION('ref_axis',(1.,0.,0.));
#40777=DIRECTION('center_axis',(0.,-1.,0.));
#40778=DIRECTION('ref_axis',(1.,0.,0.));
#40779=DIRECTION('',(0.,1.,0.));
#40780=DIRECTION('center_axis',(0.,-1.,0.));
#40781=DIRECTION('ref_axis',(1.,0.,0.));
#40782=DIRECTION('',(0.,-1.,0.));
#40783=DIRECTION('center_axis',(0.,-1.,0.));
#40784=DIRECTION('ref_axis',(1.,0.,0.));
#40785=DIRECTION('',(0.,-1.,0.));
#40786=DIRECTION('',(0.,1.,0.));
#40787=DIRECTION('center_axis',(0.,-1.,0.));
#40788=DIRECTION('ref_axis',(1.,0.,0.));
#40789=DIRECTION('center_axis',(0.,-1.,0.));
#40790=DIRECTION('ref_axis',(1.,0.,0.));
#40791=DIRECTION('',(0.,1.,0.));
#40792=DIRECTION('center_axis',(0.,-1.,0.));
#40793=DIRECTION('ref_axis',(1.,0.,0.));
#40794=DIRECTION('',(0.,-1.,0.));
#40795=DIRECTION('center_axis',(0.,0.,1.));
#40796=DIRECTION('ref_axis',(1.,0.,0.));
#40797=DIRECTION('',(1.,0.,0.));
#40798=DIRECTION('',(0.,1.,0.));
#40799=DIRECTION('',(1.,0.,0.));
#40800=DIRECTION('',(0.,1.,0.));
#40801=DIRECTION('center_axis',(-0.866025403784439,0.,0.499999999999999));
#40802=DIRECTION('ref_axis',(0.499999999999999,0.,0.866025403784439));
#40803=DIRECTION('',(0.499999999999999,0.,0.866025403784439));
#40804=DIRECTION('',(0.,1.,0.));
#40805=DIRECTION('',(0.499999999999999,0.,0.866025403784439));
#40806=DIRECTION('center_axis',(-0.866025403784439,0.,-0.499999999999999));
#40807=DIRECTION('ref_axis',(-0.499999999999999,0.,0.866025403784439));
#40808=DIRECTION('',(-0.499999999999999,0.,0.866025403784439));
#40809=DIRECTION('',(0.,1.,0.));
#40810=DIRECTION('',(-0.499999999999999,0.,0.866025403784439));
#40811=DIRECTION('center_axis',(0.,1.,0.));
#40812=DIRECTION('ref_axis',(1.,0.,0.));
#40813=DIRECTION('center_axis',(0.,1.,0.));
#40814=DIRECTION('ref_axis',(1.,0.,0.));
#40815=DIRECTION('center_axis',(0.,1.,0.));
#40816=DIRECTION('ref_axis',(1.,0.,0.));
#40817=DIRECTION('',(-1.,0.,0.));
#40818=DIRECTION('center_axis',(0.,1.,0.));
#40819=DIRECTION('ref_axis',(1.,0.,0.));
#40820=DIRECTION('center_axis',(0.,1.,0.));
#40821=DIRECTION('ref_axis',(1.,0.,0.));
#40822=DIRECTION('',(-0.499999999999999,0.,-0.866025403784439));
#40823=DIRECTION('center_axis',(0.,1.,0.));
#40824=DIRECTION('ref_axis',(1.,0.,0.));
#40825=DIRECTION('',(0.5,0.,-0.866025403784439));
#40826=DIRECTION('center_axis',(0.,-1.,0.));
#40827=DIRECTION('ref_axis',(0.,0.,-1.));
#40828=DIRECTION('',(-0.499999999999999,0.,-0.866025403784439));
#40829=DIRECTION('center_axis',(0.,-1.,0.));
#40830=DIRECTION('ref_axis',(1.,0.,0.));
#40831=DIRECTION('center_axis',(0.,-1.,0.));
#40832=DIRECTION('ref_axis',(0.,0.,-1.));
#40833=DIRECTION('',(-1.,0.,0.));
#40834=DIRECTION('center_axis',(0.,-1.,0.));
#40835=DIRECTION('ref_axis',(1.,0.,0.));
#40836=DIRECTION('center_axis',(0.,-1.,0.));
#40837=DIRECTION('ref_axis',(0.,0.,-1.));
#40838=DIRECTION('center_axis',(0.,-1.,0.));
#40839=DIRECTION('ref_axis',(1.,0.,0.));
#40840=DIRECTION('center_axis',(0.,-1.,0.));
#40841=DIRECTION('ref_axis',(0.,0.,-1.));
#40842=DIRECTION('center_axis',(0.,-1.,0.));
#40843=DIRECTION('ref_axis',(1.,0.,0.));
#40844=DIRECTION('center_axis',(0.,-1.,0.));
#40845=DIRECTION('ref_axis',(0.,0.,-1.));
#40846=DIRECTION('center_axis',(0.,-1.,0.));
#40847=DIRECTION('ref_axis',(1.,0.,0.));
#40848=DIRECTION('center_axis',(0.,-1.,0.));
#40849=DIRECTION('ref_axis',(0.,0.,-1.));
#40850=DIRECTION('',(0.5,0.,-0.866025403784439));
#40851=DIRECTION('center_axis',(0.,-1.,0.));
#40852=DIRECTION('ref_axis',(1.,0.,0.));
#40853=DIRECTION('center_axis',(0.,-1.,0.));
#40854=DIRECTION('ref_axis',(1.,0.,0.));
#40855=DIRECTION('',(-0.85716730070211,-0.515038074910058,-1.04972719113862E-16));
#40856=DIRECTION('center_axis',(0.866025403784439,0.,-0.499999999999999));
#40857=DIRECTION('ref_axis',(-0.499999999999999,0.,-0.866025403784439));
#40858=DIRECTION('',(0.,1.,0.));
#40859=DIRECTION('',(0.,1.,0.));
#40860=DIRECTION('center_axis',(0.866025403784439,0.,0.5));
#40861=DIRECTION('ref_axis',(0.5,0.,-0.866025403784439));
#40862=DIRECTION('center_axis',(0.,0.,-1.));
#40863=DIRECTION('ref_axis',(-1.,0.,0.));
#107625=CARTESIAN_POINT('',(0.,0.,0.));
#107626=CARTESIAN_POINT('Origin',(-10.,3.5,11.));
#107627=CARTESIAN_POINT('',(-11.4635,3.76156981780296,11.0000000019885));
#107628=CARTESIAN_POINT('',(-11.4634991533828,3.68934495415709,10.9984258183648));
#107629=CARTESIAN_POINT('',(-11.4635,3.5,11.));
#107630=CARTESIAN_POINT('',(-9.36565826844269,3.60066707712968,9.6811206205771));
#107631=CARTESIAN_POINT('Ctrl Pts',(-11.4635,3.76156981780296,11.0000000019885));
#107632=CARTESIAN_POINT('Ctrl Pts',(-11.4635000000624,3.75928323455344,
10.9540845300718));
#107633=CARTESIAN_POINT('Ctrl Pts',(-11.4613391785855,3.7569468082902,10.9081937237433));
#107634=CARTESIAN_POINT('Ctrl Pts',(-11.4562760707715,3.75407978255904,
10.8545499913958));
#107635=CARTESIAN_POINT('Ctrl Pts',(-11.4554628663213,3.75365277919035,
10.8466261482596));
#107636=CARTESIAN_POINT('Ctrl Pts',(-11.4541266745868,3.75299753308779,
10.8345758123366));
#107637=CARTESIAN_POINT('Ctrl Pts',(-11.453650698948,3.75277181702621,10.8304441325523));
#107638=CARTESIAN_POINT('Ctrl Pts',(-11.4527573751666,3.75236150731869,
10.8229700458294));
#107639=CARTESIAN_POINT('Ctrl Pts',(-11.4523460931523,3.7521772514568,10.8196269951759));
#107640=CARTESIAN_POINT('Ctrl Pts',(-11.4514092663413,3.75176756419203,
10.8122231170571));
#107641=CARTESIAN_POINT('Ctrl Pts',(-11.4508782205965,3.75154183540335,
10.8081630787565));
#107642=CARTESIAN_POINT('Ctrl Pts',(-11.4492828561814,3.75088213419359,
10.796351600552));
#107643=CARTESIAN_POINT('Ctrl Pts',(-11.4481734220193,3.75044577390274,
10.7886065230668));
#107644=CARTESIAN_POINT('Ctrl Pts',(-11.4386008915863,3.74685556954419,
10.7253950659656));
#107645=CARTESIAN_POINT('Ctrl Pts',(-11.4270172341977,3.74355475161639,
10.6704533723633));
#107646=CARTESIAN_POINT('Ctrl Pts',(-11.3745844567709,3.73160803816701,
10.4774514069699));
#107647=CARTESIAN_POINT('Ctrl Pts',(-11.3165714936372,3.7228421766896,10.3448701326712));
#107648=CARTESIAN_POINT('Ctrl Pts',(-11.230883367043,3.71380732535996,10.2081277259522));
#107649=CARTESIAN_POINT('Ctrl Pts',(-11.2213726482237,3.71284163789666,
10.1935358331985));
#107650=CARTESIAN_POINT('Ctrl Pts',(-11.2071489353362,3.71144945541935,
10.1725419843163));
#107651=CARTESIAN_POINT('Ctrl Pts',(-11.2026409287824,3.71101545406395,
10.1660035253833));
#107652=CARTESIAN_POINT('Ctrl Pts',(-11.1945597899482,3.71025002039912,
10.1544843431643));
#107653=CARTESIAN_POINT('Ctrl Pts',(-11.1910081967787,3.70991779345025,
10.149488804016));
#107654=CARTESIAN_POINT('Ctrl Pts',(-11.183551393156,3.70922881005415,10.1391386469318));
#107655=CARTESIAN_POINT('Ctrl Pts',(-11.1796409781286,3.70887226102982,
10.1337879392841));
#107656=CARTESIAN_POINT('Ctrl Pts',(-11.1693867808877,3.70794942744629,
10.1199551197653));
#107657=CARTESIAN_POINT('Ctrl Pts',(-11.1629869634305,3.70738529574889,
10.1115149043245));
#107658=CARTESIAN_POINT('Ctrl Pts',(-11.1341557265686,3.70489468741467,
10.0743369878939));
#107659=CARTESIAN_POINT('Ctrl Pts',(-11.1107459145355,3.70300644783047,
10.0463727059592));
#107660=CARTESIAN_POINT('Ctrl Pts',(-11.0423592439328,3.69781349960447,
9.97062045404308));
#107661=CARTESIAN_POINT('Ctrl Pts',(-10.9951780407876,3.69459183261759,
9.92493885221194));
#107662=CARTESIAN_POINT('Ctrl Pts',(-10.8670877841723,3.68640728329733,
9.81660338351391));
#107663=CARTESIAN_POINT('Ctrl Pts',(-10.7824025313501,3.68150410237404,
9.75898836082052));
#107664=CARTESIAN_POINT('Ctrl Pts',(-10.6828185260105,3.67553997822639,
9.70550783553445));
#107665=CARTESIAN_POINT('Ctrl Pts',(-10.6731568845148,3.67495926161974,
9.70045742720849));
#107666=CARTESIAN_POINT('Ctrl Pts',(-10.6591947605846,3.6741158372041,9.69335651332966));
#107667=CARTESIAN_POINT('Ctrl Pts',(-10.6549390623499,3.67385820065167,
9.69121821643585));
#107668=CARTESIAN_POINT('Ctrl Pts',(-10.6476190029936,3.67341396908673,
9.68758485905051));
#107669=CARTESIAN_POINT('Ctrl Pts',(-10.6445597469403,3.67322798585676,
9.68607967989761));
#107670=CARTESIAN_POINT('Ctrl Pts',(-10.6412433593453,3.6730260062026,9.68446235986725));
#107671=CARTESIAN_POINT('Ctrl Pts',(-10.6409914789954,3.67301066358095,
9.68433961359115));
#107672=CARTESIAN_POINT('Ctrl Pts',(-10.6406699375262,3.67299107491475,
9.68418303432902));
#107673=CARTESIAN_POINT('Ctrl Pts',(-10.6406003087526,3.67298683288301,
9.68414913442919));
#107674=CARTESIAN_POINT('Ctrl Pts',(-10.6404706537734,3.67297893352799,
9.68408602252596));
#107675=CARTESIAN_POINT('Ctrl Pts',(-10.6404106282497,3.67297527628957,
9.684056809098));
#107676=CARTESIAN_POINT('Ctrl Pts',(-10.6402987106879,3.67296845713685,
9.68400235014591));
#107677=CARTESIAN_POINT('Ctrl Pts',(-10.6402468191287,3.67296529528336,
9.68397710357088));
#107678=CARTESIAN_POINT('Ctrl Pts',(-10.6401499589466,3.67295939322996,
9.68392998569179));
#107679=CARTESIAN_POINT('Ctrl Pts',(-10.6401049906925,3.6729566530758,9.6839081136216));
#107680=CARTESIAN_POINT('Ctrl Pts',(-10.6400209719959,3.67295153324019,
9.68386725316521));
#107681=CARTESIAN_POINT('Ctrl Pts',(-10.639981921824,3.67294915359248,9.68384826420967));
#107682=CARTESIAN_POINT('Ctrl Pts',(-10.6399088988077,3.67294470360158,
9.68381275927257));
#107683=CARTESIAN_POINT('Ctrl Pts',(-10.6398749262358,3.67294263328786,
9.68379624290097));
#107684=CARTESIAN_POINT('Ctrl Pts',(-10.639802862946,3.67293824161285,9.683761211497));
#107685=CARTESIAN_POINT('Ctrl Pts',(-10.6397647720017,3.67293592022751,
9.68374269677266));
#107686=CARTESIAN_POINT('Ctrl Pts',(-10.6396897405693,3.67293134747059,
9.68370623054835));
#107687=CARTESIAN_POINT('Ctrl Pts',(-10.6396528001962,3.672929096109,9.6836882789825));
#107688=CARTESIAN_POINT('Ctrl Pts',(-10.6395800200727,3.67292466037136,
9.68365291449727));
#107689=CARTESIAN_POINT('Ctrl Pts',(-10.6395441803077,3.67292247599718,
9.68363550145781));
#107690=CARTESIAN_POINT('Ctrl Pts',(-10.6394735542032,3.67291817136605,
9.68360119075929));
#107691=CARTESIAN_POINT('Ctrl Pts',(-10.6394387678749,3.67291605111234,
9.68358429300076));
#107692=CARTESIAN_POINT('Ctrl Pts',(-10.6393702040009,3.67291187200881,
9.68355099086755));
#107693=CARTESIAN_POINT('Ctrl Pts',(-10.639336426533,3.67290981316611,9.68353458643304));
#107694=CARTESIAN_POINT('Ctrl Pts',(-10.6392698382736,3.67290575432521,
9.6835022502093));
#107695=CARTESIAN_POINT('Ctrl Pts',(-10.6392370275452,3.67290375433308,
9.68348631835994));
#107696=CARTESIAN_POINT('Ctrl Pts',(-10.6391723331431,3.67289981078479,
9.68345490779823));
#107697=CARTESIAN_POINT('Ctrl Pts',(-10.6391404494302,3.67289786722832,
9.68343942898236));
#107698=CARTESIAN_POINT('Ctrl Pts',(-10.6390775712215,3.67289403425102,
9.68340890586767));
#107699=CARTESIAN_POINT('Ctrl Pts',(-10.6390465768076,3.67289214483712,
9.68339386152979));
#107700=CARTESIAN_POINT('Ctrl Pts',(-10.6389854416086,3.67288841798128,
9.68336418986316));
#107701=CARTESIAN_POINT('Ctrl Pts',(-10.6389553008488,3.67288658054267,
9.68334956247316));
#107702=CARTESIAN_POINT('Ctrl Pts',(-10.6388958392237,3.67288295558627,
9.68332070811273));
#107703=CARTESIAN_POINT('Ctrl Pts',(-10.6388665183607,3.6728811680703,9.68330648107476));
#107704=CARTESIAN_POINT('Ctrl Pts',(-10.6388086643959,3.67287764100519,
9.68327841162284));
#107705=CARTESIAN_POINT('Ctrl Pts',(-10.6387801313542,3.67287590146129,
9.68326456917388));
#107706=CARTESIAN_POINT('Ctrl Pts',(-10.638723822775,3.67287246850038,9.6832372540307));
#107707=CARTESIAN_POINT('Ctrl Pts',(-10.6386960472265,3.67287077508415,
9.68322378127099));
#107708=CARTESIAN_POINT('Ctrl Pts',(-10.6386412245604,3.67286743261041,
9.68319719122579));
#107709=CARTESIAN_POINT('Ctrl Pts',(-10.6386141775498,3.6728657835608,9.68318407393591));
#107710=CARTESIAN_POINT('Ctrl Pts',(-10.6385607848509,3.67286252817158,
9.68315818151615));
#107711=CARTESIAN_POINT('Ctrl Pts',(-10.6385344390814,3.6728609218283,9.68314540629411));
#107712=CARTESIAN_POINT('Ctrl Pts',(-10.6384824225997,3.67285775025418,
9.68312018511746));
#107713=CARTESIAN_POINT('Ctrl Pts',(-10.6384567519562,3.67285618502872,
9.68310773914664));
#107714=CARTESIAN_POINT('Ctrl Pts',(-10.6384060609823,3.67285309418509,
9.68308316432884));
#107715=CARTESIAN_POINT('Ctrl Pts',(-10.6383810406905,3.67285156857039,
9.68307103545405));
#107716=CARTESIAN_POINT('Ctrl Pts',(-10.6383316268515,3.67284855551457,
9.68304708326534));
#107717=CARTESIAN_POINT('Ctrl Pts',(-10.638307233336,3.67284706807643,9.68303525992313));
#107718=CARTESIAN_POINT('Ctrl Pts',(-10.6382590505208,3.67284413000316,
9.68301190775047));
#107719=CARTESIAN_POINT('Ctrl Pts',(-10.6382352612765,3.67284267937239,
9.68300037890587));
#107720=CARTESIAN_POINT('Ctrl Pts',(-10.6381882657558,3.67283981362117,
9.68297760530938));
#107721=CARTESIAN_POINT('Ctrl Pts',(-10.6381650594227,3.67283839849819,
9.68296636049148));
#107722=CARTESIAN_POINT('Ctrl Pts',(-10.6381192093571,3.67283560252335,
9.6829441449648));
#107723=CARTESIAN_POINT('Ctrl Pts',(-10.6380965655761,3.6728342216694,9.68293317419612));
#107724=CARTESIAN_POINT('Ctrl Pts',(-10.6380518209419,3.67283149303557,
9.68291149712869));
#107725=CARTESIAN_POINT('Ctrl Pts',(-10.6380297201757,3.67283014526182,
9.68290079083785));
#107726=CARTESIAN_POINT('Ctrl Pts',(-10.6379860431233,3.67282748166586,
9.68287963368769));
#107727=CARTESIAN_POINT('Ctrl Pts',(-10.6379644668303,3.67282616584401,
9.68286918279287));
#107728=CARTESIAN_POINT('Ctrl Pts',(-10.6379218210235,3.67282356507472,
9.68284852776526));
#107729=CARTESIAN_POINT('Ctrl Pts',(-10.637900751503,3.67282228012761,9.68283832359883));
#107730=CARTESIAN_POINT('Ctrl Pts',(-10.6340957948628,3.67259022807093,
9.68099566011124));
#107731=CARTESIAN_POINT('Ctrl Pts',(-10.630304075875,3.67235849603446,9.67917953651132));
#107732=CARTESIAN_POINT('Ctrl Pts',(-10.6223412854083,3.67187091114326,
9.67540768643617));
#107733=CARTESIAN_POINT('Ctrl Pts',(-10.6181687044318,3.67161487634773,
9.67345526858665));
#107734=CARTESIAN_POINT('Ctrl Pts',(-10.5939129155798,3.67012370939006,
9.66224488605167));
#107735=CARTESIAN_POINT('Ctrl Pts',(-10.5736321125373,3.66886583557573,
9.65342382575651));
#107736=CARTESIAN_POINT('Ctrl Pts',(-10.5151047183265,3.66522010217662,
9.62952964509481));
#107737=CARTESIAN_POINT('Ctrl Pts',(-10.4764133352891,3.66279159045909,
9.61560416173461));
#107738=CARTESIAN_POINT('Ctrl Pts',(-10.394635829856,3.65768531922315,9.59000600742252));
#107739=CARTESIAN_POINT('Ctrl Pts',(-10.3514957064976,3.65500670078497,
9.57863753186562));
#107740=CARTESIAN_POINT('Ctrl Pts',(-10.2157524381356,3.64671647490178,
9.54942482909924));
#107741=CARTESIAN_POINT('Ctrl Pts',(-10.1218888162979,3.64119769998302,
9.5385399617413));
#107742=CARTESIAN_POINT('Ctrl Pts',(-10.0155701495009,3.63528987767549,
9.53653321439832));
#107743=CARTESIAN_POINT('Ctrl Pts',(-10.0035193113381,3.6346248433307,9.53645461687845));
#107744=CARTESIAN_POINT('Ctrl Pts',(-9.98376715523786,3.63354214859706,
9.53656976272105));
#107745=CARTESIAN_POINT('Ctrl Pts',(-9.97606606332483,3.6331218491377,9.53667545144304));
#107746=CARTESIAN_POINT('Ctrl Pts',(-9.96222203785887,3.63236949464247,
9.5369747636302));
#107747=CARTESIAN_POINT('Ctrl Pts',(-9.95607884911573,3.63203677767909,
9.53714629892512));
#107748=CARTESIAN_POINT('Ctrl Pts',(-9.94297929968529,3.6313296623974,9.53759466833822));
#107749=CARTESIAN_POINT('Ctrl Pts',(-9.93602345000046,3.63095560527962,
9.53788245423457));
#107750=CARTESIAN_POINT('Ctrl Pts',(-9.91719855108318,3.629946993374,9.53879589745609));
#107751=CARTESIAN_POINT('Ctrl Pts',(-9.90533450443742,3.62931533774236,
9.53951653070841));
#107752=CARTESIAN_POINT('Ctrl Pts',(-9.84203160136382,3.6259648265879,9.54413623488598));
#107753=CARTESIAN_POINT('Ctrl Pts',(-9.79081467319214,3.62332573743453,
9.55060856387685));
#107754=CARTESIAN_POINT('Ctrl Pts',(-9.61033444665143,3.61414547291448,
9.5831847917179));
#107755=CARTESIAN_POINT('Ctrl Pts',(-9.48440197132043,3.60801057640892,
9.62400730170195));
#107756=CARTESIAN_POINT('Ctrl Pts',(-9.36564806195114,3.60128744213858,
9.68112552959212));
#107757=CARTESIAN_POINT('',(-10.6340070945752,3.6,9.68095972236316));
#107758=CARTESIAN_POINT('Origin',(-10.,3.6,11.));
#107759=CARTESIAN_POINT('Ctrl Pts',(-10.6340070945752,3.6,9.68095972236315));
#107760=CARTESIAN_POINT('Ctrl Pts',(-10.6850513968777,3.60307949391912,
9.70549456814919));
#107761=CARTESIAN_POINT('Ctrl Pts',(-10.7347103886682,3.60615898783824,
9.7330158864931));
#107762=CARTESIAN_POINT('Ctrl Pts',(-10.7826290695724,3.60923848175736,
9.76334160357025));
#107763=CARTESIAN_POINT('Ctrl Pts',(-10.8305243595235,3.61231647245693,
9.79365251749729));
#107764=CARTESIAN_POINT('Ctrl Pts',(-10.8766806071727,3.6153944631565,9.82676485276805));
#107765=CARTESIAN_POINT('Ctrl Pts',(-10.9207691913895,3.61847245385607,
9.86245160710065));
#107766=CARTESIAN_POINT('Ctrl Pts',(-10.9648471405381,3.62154970208133,
9.89812975305819));
#107767=CARTESIAN_POINT('Ctrl Pts',(-11.0068580336482,3.62462695030659,
9.93638077499454));
#107768=CARTESIAN_POINT('Ctrl Pts',(-11.0465054999892,3.62770419853185,
9.97693671334934));
#107769=CARTESIAN_POINT('Ctrl Pts',(-11.0861557437108,3.63078166232422,
10.017495492725));
#107770=CARTESIAN_POINT('Ctrl Pts',(-11.1234418877901,3.63385912611659,
10.0603591562058));
#107771=CARTESIAN_POINT('Ctrl Pts',(-11.158105019341,3.63693658990896,10.1052234836691));
#107772=CARTESIAN_POINT('Ctrl Pts',(-11.1927813699806,3.64001522731909,
10.1501049205366));
#107773=CARTESIAN_POINT('Ctrl Pts',(-11.2248324210782,3.64309386472922,
10.1969881460308));
#107774=CARTESIAN_POINT('Ctrl Pts',(-11.2540412311563,3.64617250213935,
10.2455380456511));
#107775=CARTESIAN_POINT('Ctrl Pts',(-11.2832941999661,3.64925579392338,
10.2941613444267));
#107776=CARTESIAN_POINT('Ctrl Pts',(-11.3096960963109,3.65233908570741,
10.3444559234168));
#107777=CARTESIAN_POINT('Ctrl Pts',(-11.3330752825907,3.65542237749143,
10.3960608135369));
#107778=CARTESIAN_POINT('Ctrl Pts',(-11.3564733874392,3.65850816429248,
10.4477074626237));
#107779=CARTESIAN_POINT('Ctrl Pts',(-11.376843732178,3.66159395109352,10.5006660748198));
#107780=CARTESIAN_POINT('Ctrl Pts',(-11.3940634951727,3.66467973789456,
10.5545572748076));
#107781=CARTESIAN_POINT('Ctrl Pts',(-11.4113186639751,3.66777186942717,
10.6085592812834));
#107782=CARTESIAN_POINT('Ctrl Pts',(-11.4254101882224,3.67086400095979,
10.6634972277376));
#107783=CARTESIAN_POINT('Ctrl Pts',(-11.4362657981855,3.6739561324924,10.718978991955));
#107784=CARTESIAN_POINT('Ctrl Pts',(-11.4421490956222,3.67563194155163,
10.7490478432044));
#107785=CARTESIAN_POINT('Ctrl Pts',(-11.447082837701,3.67730775061086,10.7792762882384));
#107786=CARTESIAN_POINT('Ctrl Pts',(-11.4510618967054,3.67898355967009,
10.8096014130053));
#107787=CARTESIAN_POINT('Ctrl Pts',(-11.4592626321064,3.68243735783242,
10.8721006933471));
#107788=CARTESIAN_POINT('Ctrl Pts',(-11.4634311218865,3.68589115599475,
10.9351776930672));
#107789=CARTESIAN_POINT('Ctrl Pts',(-11.4634991533828,3.68934495415709,
10.9984258183648));
#107790=CARTESIAN_POINT('Origin',(-10.,3.5,11.));
#107791=CARTESIAN_POINT('',(-11.4635,4.25936781471288,11.0000000001943));
#107792=CARTESIAN_POINT('',(-11.4634999508678,4.19066505394721,10.9996207769711));
#107793=CARTESIAN_POINT('',(-11.4635,3.5,11.));
#107794=CARTESIAN_POINT('Ctrl Pts',(-11.4635,4.25936781471288,11.0000000001943));
#107795=CARTESIAN_POINT('Ctrl Pts',(-11.4635000000009,4.25902532594864,
10.9934975786898));
#107796=CARTESIAN_POINT('Ctrl Pts',(-11.4634566640214,4.25868411486387,
10.9869950464565));
#107797=CARTESIAN_POINT('Ctrl Pts',(-11.4624819664045,4.25486105431314,
10.9138761111745));
#107798=CARTESIAN_POINT('Ctrl Pts',(-11.4570462164854,4.25151849227137,
10.8473945935954));
#107799=CARTESIAN_POINT('Ctrl Pts',(-11.4349561851339,4.24423808160547,
10.7010888593856));
#107800=CARTESIAN_POINT('Ctrl Pts',(-11.4161317145643,4.24034623495184,
10.6218235698782));
#107801=CARTESIAN_POINT('Ctrl Pts',(-11.3748965878244,4.23377647577659,
10.4959068745586));
#107802=CARTESIAN_POINT('Ctrl Pts',(-11.3564340745739,4.23118570966055,
10.4481520862128));
#107803=CARTESIAN_POINT('Ctrl Pts',(-11.3325366186803,4.22807649401993,
10.394829516972));
#107804=CARTESIAN_POINT('Ctrl Pts',(-11.3295125724275,4.22768684870793,
10.3882145235923));
#107805=CARTESIAN_POINT('Ctrl Pts',(-11.3245933241023,4.22705857471218,
10.3776625798055));
#107806=CARTESIAN_POINT('Ctrl Pts',(-11.3227295443383,4.22682177218674,
10.373711016886));
#107807=CARTESIAN_POINT('Ctrl Pts',(-11.319386514376,4.2263990950339,10.3667046537964));
#107808=CARTESIAN_POINT('Ctrl Pts',(-11.3179142970722,4.22621364818248,
10.3636465799442));
#107809=CARTESIAN_POINT('Ctrl Pts',(-11.3147296349514,4.22581394181117,
10.3570898904234));
#107810=CARTESIAN_POINT('Ctrl Pts',(-11.3130138844915,4.22559948891633,
10.3535930380753));
#107811=CARTESIAN_POINT('Ctrl Pts',(-11.3082188104421,4.22500268554567,
10.3439181110308));
#107812=CARTESIAN_POINT('Ctrl Pts',(-11.3051097448193,4.22461857645875,
10.3377549915668));
#107813=CARTESIAN_POINT('Ctrl Pts',(-11.2869922682685,4.22239740661244,
10.3024637258214));
#107814=CARTESIAN_POINT('Ctrl Pts',(-11.2710535368334,4.22050982010397,
10.2738260923971));
#107815=CARTESIAN_POINT('Ctrl Pts',(-11.2144743116127,4.21407730220086,
10.1797460725453));
#107816=CARTESIAN_POINT('Ctrl Pts',(-11.1696328919382,4.20940319389579,
10.1169809133202));
#107817=CARTESIAN_POINT('Ctrl Pts',(-11.0577195639985,4.19897244948248,
9.98390776972589));
#107818=CARTESIAN_POINT('Ctrl Pts',(-10.9881634055467,4.19328350564014,
9.91613991937271));
#107819=CARTESIAN_POINT('Ctrl Pts',(-10.902996436888,4.18722905409278,9.84822978531838));
#107820=CARTESIAN_POINT('Ctrl Pts',(-10.8934909156783,4.18656443193835,
9.84084030945967));
#107821=CARTESIAN_POINT('Ctrl Pts',(-10.8778119624781,4.18548594264641,
9.82895915447156));
#107822=CARTESIAN_POINT('Ctrl Pts',(-10.8716927900577,4.18506936017406,
9.82439709671948));
#107823=CARTESIAN_POINT('Ctrl Pts',(-10.8606614008153,4.18432599134863,
9.81630629857245));
#107824=CARTESIAN_POINT('Ctrl Pts',(-10.8557625012729,4.18399852730871,
9.81275976795615));
#107825=CARTESIAN_POINT('Ctrl Pts',(-10.8453055400798,4.18330509621986,
9.80528786251275));
#107826=CARTESIAN_POINT('Ctrl Pts',(-10.8397417909755,4.18293944414606,
9.80137066856863));
#107827=CARTESIAN_POINT('Ctrl Pts',(-10.8247039285546,4.18195984130277,
9.79093926206517));
#107828=CARTESIAN_POINT('Ctrl Pts',(-10.8151799319174,4.18134860991019,
9.78449758273484));
#107829=CARTESIAN_POINT('Ctrl Pts',(-10.7657127214036,4.17821941567478,
9.75188273989734));
#107830=CARTESIAN_POINT('Ctrl Pts',(-10.7245799218045,4.17576991415896,
9.72756250009926));
#107831=CARTESIAN_POINT('Ctrl Pts',(-10.5860427122453,4.16790447436724,
9.65455133606497));
#107832=CARTESIAN_POINT('Ctrl Pts',(-10.4844024470744,4.16275036782057,
9.61470892577944));
#107833=CARTESIAN_POINT('Ctrl Pts',(-10.3296849698857,4.15480856973996,
9.57319322343475));
#107834=CARTESIAN_POINT('Ctrl Pts',(-10.2794212567143,4.15220878469236,
9.56250477510039));
#107835=CARTESIAN_POINT('Ctrl Pts',(-10.22151324667,4.1490892384097,9.55334276700885));
#107836=CARTESIAN_POINT('Ctrl Pts',(-10.2143130980492,4.14869917941742,
9.55225860045987));
#107837=CARTESIAN_POINT('Ctrl Pts',(-10.2027772842615,4.14807033150747,
9.55060952895859));
#107838=CARTESIAN_POINT('Ctrl Pts',(-10.1984465687697,4.14783337280801,
9.55001023351723));
#107839=CARTESIAN_POINT('Ctrl Pts',(-10.1907474716124,4.14741044648355,
9.54897995063021));
#107840=CARTESIAN_POINT('Ctrl Pts',(-10.1873801946584,4.14722490719728,
9.54854127029223));
#107841=CARTESIAN_POINT('Ctrl Pts',(-10.1801450014133,4.14682499289747,
9.5476242850908));
#107842=CARTESIAN_POINT('Ctrl Pts',(-10.1762767539655,4.14661042436716,
9.54714971725238));
#107843=CARTESIAN_POINT('Ctrl Pts',(-10.1655501883383,4.14601342115145,
9.54587722026402));
#107844=CARTESIAN_POINT('Ctrl Pts',(-10.158688138685,4.14562922905592,9.54511237745438));
#107845=CARTESIAN_POINT('Ctrl Pts',(-10.1192591053765,4.14340963137147,
9.54099988621677));
#107846=CARTESIAN_POINT('Ctrl Pts',(-10.0865946246977,4.14152384108607,
9.53869745653475));
#107847=CARTESIAN_POINT('Ctrl Pts',(-9.97703812012236,4.13510086996666,
9.53466107879946));
#107848=CARTESIAN_POINT('Ctrl Pts',(-9.90009195140336,4.13043505181022,
9.53789082686124));
#107849=CARTESIAN_POINT('Ctrl Pts',(-9.72760709132496,4.12001305109543,
9.55881457973886));
#107850=CARTESIAN_POINT('Ctrl Pts',(-9.63283846661595,4.11432459966961,
9.57999605338088));
#107851=CARTESIAN_POINT('Ctrl Pts',(-9.5294153479113,4.10827049964071,9.61416910888153));
#107852=CARTESIAN_POINT('Ctrl Pts',(-9.51803155698666,4.1076059269297,9.61808697610765));
#107853=CARTESIAN_POINT('Ctrl Pts',(-9.49951013454301,4.10652741164867,
9.62471805842435));
#107854=CARTESIAN_POINT('Ctrl Pts',(-9.49234325988269,4.1061107562891,9.62734739954439));
#107855=CARTESIAN_POINT('Ctrl Pts',(-9.47953373417776,4.1053671883899,9.63216093048103));
#107856=CARTESIAN_POINT('Ctrl Pts',(-9.47388347253239,4.10503959868816,
9.63432424968306));
#107857=CARTESIAN_POINT('Ctrl Pts',(-9.46190380532984,4.10434582774548,
9.63899629416874));
#107858=CARTESIAN_POINT('Ctrl Pts',(-9.45557814944251,4.10397996220359,
9.64151427951083));
#107859=CARTESIAN_POINT('Ctrl Pts',(-9.43860860061271,4.10299960445534,
9.64840672941961));
#107860=CARTESIAN_POINT('Ctrl Pts',(-9.42799823294832,4.10238783645299,
9.6528627906235));
#107861=CARTESIAN_POINT('Ctrl Pts',(-9.37354193673367,4.09925284569418,
9.67649232937693));
#107862=CARTESIAN_POINT('Ctrl Pts',(-9.33060098972898,4.09679837199659,
9.69768367318154));
#107863=CARTESIAN_POINT('Ctrl Pts',(-9.19321779772954,4.08890377083662,
9.77407641669106));
#107864=CARTESIAN_POINT('Ctrl Pts',(-9.10392339858117,4.08372818152984,
9.8377471299721));
#107865=CARTESIAN_POINT('Ctrl Pts',(-8.98472230561747,4.07578415129803,
9.94471464098695));
#107866=CARTESIAN_POINT('Ctrl Pts',(-8.94868865692762,4.07320954238742,
9.98060828185785));
#107867=CARTESIAN_POINT('Ctrl Pts',(-8.90972642669894,4.07011876376522,
10.0236862493227));
#107868=CARTESIAN_POINT('Ctrl Pts',(-8.90489459937282,4.06972965837293,
10.0291090886872));
#107869=CARTESIAN_POINT('Ctrl Pts',(-8.89722285460441,4.06910205929221,
10.0378493436846));
#107870=CARTESIAN_POINT('Ctrl Pts',(-8.894357013495,4.06886538443477,10.0411439611423));
#107871=CARTESIAN_POINT('Ctrl Pts',(-8.88929047445153,4.06844288072918,
10.0470214514402));
#107872=CARTESIAN_POINT('Ctrl Pts',(-8.8870839602853,4.06825747885049,10.0495992147901));
#107873=CARTESIAN_POINT('Ctrl Pts',(-8.88236472824535,4.06785789790903,
10.0551514355703));
#107874=CARTESIAN_POINT('Ctrl Pts',(-8.87985495103988,4.06764352568938,
10.0581282046149));
#107875=CARTESIAN_POINT('Ctrl Pts',(-8.87292647403023,4.06704661440199,
10.0664127173652));
#107876=CARTESIAN_POINT('Ctrl Pts',(-8.86853347967118,4.06666231205731,
10.0717417079311));
#107877=CARTESIAN_POINT('Ctrl Pts',(-8.84343365158452,4.06443367406926,
10.1026323475469));
#107878=CARTESIAN_POINT('Ctrl Pts',(-8.82355702798911,4.06253835793603,
10.1288536075467));
#107879=CARTESIAN_POINT('Ctrl Pts',(-8.75979856923863,4.05606133986969,
10.2191293539086));
#107880=CARTESIAN_POINT('Ctrl Pts',(-8.72013237741204,4.0513485978988,10.2859993770333));
#107881=CARTESIAN_POINT('Ctrl Pts',(-8.64362129402592,4.04092436659841,
10.4420422886716));
#107882=CARTESIAN_POINT('Ctrl Pts',(-8.60989244312836,4.03527841007388,
10.5323608541549));
#107883=CARTESIAN_POINT('Ctrl Pts',(-8.5821864869836,4.02926290781066,10.6369822019807));
#107884=CARTESIAN_POINT('Ctrl Pts',(-8.57924924226182,4.02859855366428,
10.6486534817777));
#107885=CARTESIAN_POINT('Ctrl Pts',(-8.57468616676362,4.02752062677492,
10.667778838211));
#107886=CARTESIAN_POINT('Ctrl Pts',(-8.57297410343424,4.02710433720996,
10.6752115809375));
#107887=CARTESIAN_POINT('Ctrl Pts',(-8.57001003934691,4.02636157421692,
10.688555832201));
#107888=CARTESIAN_POINT('Ctrl Pts',(-8.56873640419713,4.02603442281965,
10.6944623131808));
#107889=CARTESIAN_POINT('Ctrl Pts',(-8.56610798219057,4.02534174409984,
10.707028807842));
#107890=CARTESIAN_POINT('Ctrl Pts',(-8.56476293228192,4.02497653071097,
10.713690727108));
#107891=CARTESIAN_POINT('Ctrl Pts',(-8.56127089511812,4.0239983324744,10.7316297529902));
#107892=CARTESIAN_POINT('Ctrl Pts',(-8.55921007983556,4.02338805989919,
10.7429232748398));
#107893=CARTESIAN_POINT('Ctrl Pts',(-8.54928908673348,4.02026797403415,
10.8011638252084));
#107894=CARTESIAN_POINT('Ctrl Pts',(-8.54358942585577,4.01782622003179,
10.8484519850405));
#107895=CARTESIAN_POINT('Ctrl Pts',(-8.5325229658762,4.01000866402875,11.0036926808674));
#107896=CARTESIAN_POINT('Ctrl Pts',(-8.53679592890457,4.00489055417382,
11.1119614298076));
#107897=CARTESIAN_POINT('Ctrl Pts',(-8.55704725225737,3.99818067615685,
11.2459127323938));
#107898=CARTESIAN_POINT('Ctrl Pts',(-8.56191310014219,3.996805822727,11.2729315930196));
#107899=CARTESIAN_POINT('Ctrl Pts',(-8.57308492715497,3.99402019825296,
11.3263119500431));
#107900=CARTESIAN_POINT('Ctrl Pts',(-8.57936908408791,3.99261066355084,
11.3526666056775));
#107901=CARTESIAN_POINT('Ctrl Pts',(-8.58812228222338,3.99080398171295,
11.3853295179107));
#107902=CARTESIAN_POINT('Ctrl Pts',(-8.58990882809027,3.99044217328389,
11.3918168076613));
#107903=CARTESIAN_POINT('Ctrl Pts',(-8.59279987395277,3.98986703356222,
11.4020388310042));
#107904=CARTESIAN_POINT('Ctrl Pts',(-8.59387467687242,3.9896553567237,11.4057819504665));
#107905=CARTESIAN_POINT('Ctrl Pts',(-8.5958184862173,3.98927622996159,11.4124510184772));
#107906=CARTESIAN_POINT('Ctrl Pts',(-8.59668172021969,3.98910911245706,
11.4153785880219));
#107907=CARTESIAN_POINT('Ctrl Pts',(-8.59876944473903,3.98870791238855,
11.4223781019532));
#107908=CARTESIAN_POINT('Ctrl Pts',(-8.60000252178603,3.98847334163494,
11.4264474059822));
#107909=CARTESIAN_POINT('Ctrl Pts',(-8.60378642450302,3.98776077456913,
11.4387414441541));
#107910=CARTESIAN_POINT('Ctrl Pts',(-8.60639207964714,3.9872797837346,11.4469489459745));
#107911=CARTESIAN_POINT('Ctrl Pts',(-8.63462513418686,3.98217099433124,
11.5332319088467));
#107912=CARTESIAN_POINT('Ctrl Pts',(-8.66671036991323,3.97723783834088,
11.6090328708078));
#107913=CARTESIAN_POINT('Ctrl Pts',(-8.75845258664613,3.96538526579975,
11.78330611747));
#107914=CARTESIAN_POINT('Ctrl Pts',(-8.82369721348791,3.9585232195873,11.8782531834745));
#107915=CARTESIAN_POINT('Ctrl Pts',(-8.9111459972959,3.95109034780991,11.9780326845613));
#107916=CARTESIAN_POINT('Ctrl Pts',(-8.92315794942276,3.95010006756871,
11.9912427597698));
#107917=CARTESIAN_POINT('Ctrl Pts',(-8.940897279623,3.94868066041328,12.0100483405166));
#107918=CARTESIAN_POINT('Ctrl Pts',(-8.9464332485259,3.94824354657535,12.0158215031291));
#107919=CARTESIAN_POINT('Ctrl Pts',(-8.95628511663903,3.94747578526157,
12.0259283076081));
#107920=CARTESIAN_POINT('Ctrl Pts',(-8.96058133922653,3.94714430608266,
12.0302807866332));
#107921=CARTESIAN_POINT('Ctrl Pts',(-8.96953945878527,3.94645992398107,
12.0392431400338));
#107922=CARTESIAN_POINT('Ctrl Pts',(-8.97420530939773,3.94610720486851,
12.0438488807047));
#107923=CARTESIAN_POINT('Ctrl Pts',(-8.9863210046459,3.94520078887457,12.0556488032474));
#107924=CARTESIAN_POINT('Ctrl Pts',(-8.99381661482084,3.94464912917223,
12.0627956078895));
#107925=CARTESIAN_POINT('Ctrl Pts',(-9.02653713770173,3.94227909849936,
12.0933370319047));
#107926=CARTESIAN_POINT('Ctrl Pts',(-9.05250769171143,3.94049470240947,
12.1159186232665));
#107927=CARTESIAN_POINT('Ctrl Pts',(-9.12576854130143,3.93568956595658,
12.1752161718429));
#107928=CARTESIAN_POINT('Ctrl Pts',(-9.17455328394296,3.93273692379298,
12.2099802036993));
#107929=CARTESIAN_POINT('Ctrl Pts',(-9.30341362858846,3.92531926392359,
12.2903757537293));
#107930=CARTESIAN_POINT('Ctrl Pts',(-9.38590987885403,3.9209171720759,12.3316128621035));
#107931=CARTESIAN_POINT('Ctrl Pts',(-9.49601912626406,3.91487561606458,
12.374232236855));
#107932=CARTESIAN_POINT('Ctrl Pts',(-9.52056010450624,3.91351825491526,
12.38298524485));
#107933=CARTESIAN_POINT('Ctrl Pts',(-9.55164247914391,3.9117706456984,12.393144653948));
#107934=CARTESIAN_POINT('Ctrl Pts',(-9.55797878562638,3.91141292060233,
12.3951679956314));
#107935=CARTESIAN_POINT('Ctrl Pts',(-9.56803441446307,3.91084258175971,
12.3983036336196));
#107936=CARTESIAN_POINT('Ctrl Pts',(-9.57174482424624,3.91063156799455,
12.3994444692852));
#107937=CARTESIAN_POINT('Ctrl Pts',(-9.57839588900365,3.91025223444002,
12.4014605370903));
#107938=CARTESIAN_POINT('Ctrl Pts',(-9.58133480962992,3.91008423502295,
12.4023412998281));
#107939=CARTESIAN_POINT('Ctrl Pts',(-9.58840476613533,3.90967919080898,
12.4044358840081));
#107940=CARTESIAN_POINT('Ctrl Pts',(-9.59253839710264,3.9094416391885,12.4056407186875));
#107941=CARTESIAN_POINT('Ctrl Pts',(-9.60515815376641,3.90871430699387,
12.4092586718527));
#107942=CARTESIAN_POINT('Ctrl Pts',(-9.61366068163934,3.90822138155659,
12.4116132654143));
#107943=CARTESIAN_POINT('Ctrl Pts',(-9.69076257099488,3.90372869431454,
12.4322162328003));
#107944=CARTESIAN_POINT('Ctrl Pts',(-9.76057753616558,3.89950218620623,
12.4455262284206));
#107945=CARTESIAN_POINT('Ctrl Pts',(-9.95691335943876,3.88763480977903,
12.4683409039926));
#107946=CARTESIAN_POINT('Ctrl Pts',(-10.0841446359608,3.88001851236018,
12.4665648414931));
#107947=CARTESIAN_POINT('Ctrl Pts',(-10.2258664341384,3.87201545602908,
12.4460593981653));
#107948=CARTESIAN_POINT('Ctrl Pts',(-10.2421237150076,3.87110352171542,
12.4434263287684));
#107949=CARTESIAN_POINT('Ctrl Pts',(-10.2660498092042,3.86977004226315,
12.4391355753332));
#107950=CARTESIAN_POINT('Ctrl Pts',(-10.2737549047943,3.86934193695376,
12.4376897998497));
#107951=CARTESIAN_POINT('Ctrl Pts',(-10.2874192760727,3.86858499270221,
12.4350119977767));
#107952=CARTESIAN_POINT('Ctrl Pts',(-10.2933831394414,3.86825539129264,
12.4338045923533));
#107953=CARTESIAN_POINT('Ctrl Pts',(-10.3059135382311,3.86756444081787,
12.4311863135084));
#107954=CARTESIAN_POINT('Ctrl Pts',(-10.3124782529998,3.86720335429075,
12.4297673588015));
#107955=CARTESIAN_POINT('Ctrl Pts',(-10.3298118674834,3.86625220851928,
12.4258956349346));
#107956=CARTESIAN_POINT('Ctrl Pts',(-10.3405632804195,3.86566457962419,
12.4233660423615));
#107957=CARTESIAN_POINT('Ctrl Pts',(-10.3916863954531,3.86288038728586,
12.4107253678329));
#107958=CARTESIAN_POINT('Ctrl Pts',(-10.4316450224197,3.86073480563761,
12.3990165384748));
#107959=CARTESIAN_POINT('Ctrl Pts',(-10.5453478444627,3.85466331358175,
12.3603623278659));
#107960=CARTESIAN_POINT('Ctrl Pts',(-10.6174939661687,3.8508592225807,12.329169638352));
#107961=CARTESIAN_POINT('Ctrl Pts',(-10.7599315977409,3.84300715496183,
12.2534737244739));
#107962=CARTESIAN_POINT('Ctrl Pts',(-10.829631671141,3.83896904898374,12.2084703806387));
#107963=CARTESIAN_POINT('Ctrl Pts',(-10.9046129472499,3.83398200278471,
12.1505002974353));
#107964=CARTESIAN_POINT('Ctrl Pts',(-10.9139919238802,3.83334560005462,
12.143063543176));
#107965=CARTESIAN_POINT('Ctrl Pts',(-10.9267722504251,3.83245928562767,
12.1326719401305));
#107966=CARTESIAN_POINT('Ctrl Pts',(-10.9302529952138,3.83221591042099,
12.1298149812878));
#107967=CARTESIAN_POINT('Ctrl Pts',(-10.9361927939819,3.83179707565793,
12.1248935998925));
#107968=CARTESIAN_POINT('Ctrl Pts',(-10.9386583627342,3.83162217119824,
12.1228370479482));
#107969=CARTESIAN_POINT('Ctrl Pts',(-10.9437637601388,3.83125776928576,
12.1185500251627));
#107970=CARTESIAN_POINT('Ctrl Pts',(-10.9464024512624,3.83106817517489,
12.1163183206741));
#107971=CARTESIAN_POINT('Ctrl Pts',(-10.9527964197624,3.83060573594224,
12.110871581779));
#107972=CARTESIAN_POINT('Ctrl Pts',(-10.9565433359189,3.83033219467308,
12.1076468452401));
#107973=CARTESIAN_POINT('Ctrl Pts',(-10.9698358896328,3.82935289191924,
12.0960890278877));
#107974=CARTESIAN_POINT('Ctrl Pts',(-10.9792892852846,3.82863997268335,
12.0876512691742));
#107975=CARTESIAN_POINT('Ctrl Pts',(-11.0024848172464,3.82685202884115,
12.0664002238586));
#107976=CARTESIAN_POINT('Ctrl Pts',(-11.0160917886559,3.82576853830024,
12.0534432420865));
#107977=CARTESIAN_POINT('Ctrl Pts',(-11.0729656139498,3.82110377664866,
11.9971589985293));
#107978=CARTESIAN_POINT('Ctrl Pts',(-11.1137383944983,3.81741652752482,
11.951402828134));
#107979=CARTESIAN_POINT('Ctrl Pts',(-11.2201695803576,3.80702796518297,
11.8157142820872));
#107980=CARTESIAN_POINT('Ctrl Pts',(-11.2786261614965,3.80038812963448,
11.7206431311604));
#107981=CARTESIAN_POINT('Ctrl Pts',(-11.3334206405127,3.79313696006048,
11.6034481191542));
#107982=CARTESIAN_POINT('Ctrl Pts',(-11.3407862042801,3.79213211684076,
11.586900871452));
#107983=CARTESIAN_POINT('Ctrl Pts',(-11.3509633628391,3.79069792132813,
11.562844899132));
#107984=CARTESIAN_POINT('Ctrl Pts',(-11.3540231980191,3.79026023683922,
11.5554435804096));
#107985=CARTESIAN_POINT('Ctrl Pts',(-11.3592993561836,3.78949379697774,
11.5423785510346));
#107986=CARTESIAN_POINT('Ctrl Pts',(-11.3615413983233,3.78916418528113,
11.5367254927325));
#107987=CARTESIAN_POINT('Ctrl Pts',(-11.3660988510201,3.7884858883677,11.5250220419829));
#107988=CARTESIAN_POINT('Ctrl Pts',(-11.3684094582083,3.78813736897251,
11.5189699142211));
#107989=CARTESIAN_POINT('Ctrl Pts',(-11.3742353039344,3.78724644782813,
11.5034009356227));
#107990=CARTESIAN_POINT('Ctrl Pts',(-11.3776919402571,3.78670599183501,
11.4938624274722));
#107991=CARTESIAN_POINT('Ctrl Pts',(-11.3919194069026,3.78442904277287,
11.4532898603045));
#107992=CARTESIAN_POINT('Ctrl Pts',(-11.4017433432576,3.78272355128406,
11.4219326286449));
#107993=CARTESIAN_POINT('Ctrl Pts',(-11.4254024569034,3.7781939191404,11.3364243790323));
#107994=CARTESIAN_POINT('Ctrl Pts',(-11.4372059870598,3.77542855920324,
11.2817677902986));
#107995=CARTESIAN_POINT('Ctrl Pts',(-11.4563573860184,3.76937853245025,
11.1595518662736));
#107996=CARTESIAN_POINT('Ctrl Pts',(-11.4621865884358,3.76611769224654,
11.0918890488679));
#107997=CARTESIAN_POINT('Ctrl Pts',(-11.4634340406339,3.76236728451616,
11.0160449865655));
#107998=CARTESIAN_POINT('Ctrl Pts',(-11.4634999999891,3.76196931788923,
11.0080221175165));
#107999=CARTESIAN_POINT('Ctrl Pts',(-11.4635,3.76156981780296,11.0000000019885));
#108000=CARTESIAN_POINT('Ctrl Pts',(-11.463499196434,3.68866743805058,10.9984663647852));
#108001=CARTESIAN_POINT('Ctrl Pts',(-11.463621240977,3.6956372676389,11.1149295816248));
#108002=CARTESIAN_POINT('Ctrl Pts',(-11.4498399904823,3.70278005779937,
11.2310163054424));
#108003=CARTESIAN_POINT('Ctrl Pts',(-11.4129076953229,3.71185718108644,
11.3836211223003));
#108004=CARTESIAN_POINT('Ctrl Pts',(-11.4017475418727,3.71415130090118,
11.4225844559022));
#108005=CARTESIAN_POINT('Ctrl Pts',(-11.3856556268055,3.71697531498198,
11.4710651396683));
#108006=CARTESIAN_POINT('Ctrl Pts',(-11.3822186554584,3.71755570624248,
11.4810566277026));
#108007=CARTESIAN_POINT('Ctrl Pts',(-11.3765347233692,3.71848032778269,
11.4970161484804));
#108008=CARTESIAN_POINT('Ctrl Pts',(-11.3743564835665,3.71882691806274,
11.5030081057587));
#108009=CARTESIAN_POINT('Ctrl Pts',(-11.3701427470647,3.71948297752731,
11.5143676246052));
#108010=CARTESIAN_POINT('Ctrl Pts',(-11.3681146947118,3.71979269826478,
11.5197378031813));
#108011=CARTESIAN_POINT('Ctrl Pts',(-11.3634213391418,3.72049597253914,
11.5319477278626));
#108012=CARTESIAN_POINT('Ctrl Pts',(-11.3607360545594,3.72088881792799,
11.5387796635389));
#108013=CARTESIAN_POINT('Ctrl Pts',(-11.3536159952689,3.72190629038651,
11.556501790686));
#108014=CARTESIAN_POINT('Ctrl Pts',(-11.3491011302877,3.72252809222464,
11.5673593721522));
#108015=CARTESIAN_POINT('Ctrl Pts',(-11.3051046072282,3.72837529935472,
11.6696687992457));
#108016=CARTESIAN_POINT('Ctrl Pts',(-11.256513512871,3.73324548612767,11.7569223344702));
#108017=CARTESIAN_POINT('Ctrl Pts',(-11.1685222763326,3.74064261708535,
11.8827781795316));
#108018=CARTESIAN_POINT('Ctrl Pts',(-11.135196436116,3.74321973909345,11.9252407374178));
#108019=CARTESIAN_POINT('Ctrl Pts',(-11.0728646023674,3.74783544669981,
11.9962106531898));
#108020=CARTESIAN_POINT('Ctrl Pts',(-11.0448741788817,3.749847015431,12.0255299351027));
#108021=CARTESIAN_POINT('Ctrl Pts',(-11.0001720952386,3.7530384120377,12.0686222624175));
#108022=CARTESIAN_POINT('Ctrl Pts',(-10.9843102853539,3.75416713610228,
12.0832501643586));
#108023=CARTESIAN_POINT('Ctrl Pts',(-10.963839295049,3.75562816907438,12.1013077803014));
#108024=CARTESIAN_POINT('Ctrl Pts',(-10.9595246345129,3.75593634644207,
12.1050689965284));
#108025=CARTESIAN_POINT('Ctrl Pts',(-10.9528290768421,3.75641514750095,
12.1108369345323));
#108026=CARTESIAN_POINT('Ctrl Pts',(-10.9504636472347,3.75658441330433,
12.1128615365692));
#108027=CARTESIAN_POINT('Ctrl Pts',(-10.9455282033141,3.75693781611274,
12.1170586337432));
#108028=CARTESIAN_POINT('Ctrl Pts',(-10.9429571554539,3.75712204125014,
12.1192298141948));
#108029=CARTESIAN_POINT('Ctrl Pts',(-10.9370783850132,3.7575435147962,12.1241596423967));
#108030=CARTESIAN_POINT('Ctrl Pts',(-10.9337659419453,3.75778116799584,
12.1269125813249));
#108031=CARTESIAN_POINT('Ctrl Pts',(-10.9251148130383,3.75840217944588,
12.1340381184093));
#108032=CARTESIAN_POINT('Ctrl Pts',(-10.9197573273043,3.75878708573071,
12.138387599381));
#108033=CARTESIAN_POINT('Ctrl Pts',(-10.8830815549875,3.76142306602123,
12.1677349648958));
#108034=CARTESIAN_POINT('Ctrl Pts',(-10.8507811116043,3.7637492708968,12.1914734371027));
#108035=CARTESIAN_POINT('Ctrl Pts',(-10.8097879617422,3.76666827161838,
12.2190829739189));
#108036=CARTESIAN_POINT('Ctrl Pts',(-10.8019755757595,3.76722316004374,
12.2242365016237));
#108037=CARTESIAN_POINT('Ctrl Pts',(-10.69121846531,3.77506507994747,12.2957835330226));
#108038=CARTESIAN_POINT('Ctrl Pts',(-10.5803652448107,3.78255814372612,
12.3490815733773));
#108039=CARTESIAN_POINT('Ctrl Pts',(-10.4266191962654,3.79189938242241,
12.4004983582289));
#108040=CARTESIAN_POINT('Ctrl Pts',(-10.3885772971929,3.7941370682623,12.4115267224502));
#108041=CARTESIAN_POINT('Ctrl Pts',(-10.3394813975757,3.79693295931095,
12.4236238825763));
#108042=CARTESIAN_POINT('Ctrl Pts',(-10.3288011646216,3.79753574982269,
12.4261284589795));
#108043=CARTESIAN_POINT('Ctrl Pts',(-10.3114929758665,3.79850408520259,
12.4299825538055));
#108044=CARTESIAN_POINT('Ctrl Pts',(-10.3048821937036,3.79887193584947,
12.4314065908261));
#108045=CARTESIAN_POINT('Ctrl Pts',(-10.2922034062061,3.7995736842926,12.4340459242474));
#108046=CARTESIAN_POINT('Ctrl Pts',(-10.2861371111975,3.79990780552745,
12.4352686503338));
#108047=CARTESIAN_POINT('Ctrl Pts',(-10.2722813720362,3.8006673057545,12.4379700841435));
#108048=CARTESIAN_POINT('Ctrl Pts',(-10.2644872656801,3.80109191475134,
12.439424050798));
#108049=CARTESIAN_POINT('Ctrl Pts',(-10.239905312291,3.80242311536301,12.4438033343177));
#108050=CARTESIAN_POINT('Ctrl Pts',(-10.2230776622916,3.80332268643314,
12.4464988816223));
#108051=CARTESIAN_POINT('Ctrl Pts',(-10.0901368362225,3.81034577827223,
12.4654189154367));
#108052=CARTESIAN_POINT('Ctrl Pts',(-9.97250560790931,3.8160138269401,12.4679316482423));
#108053=CARTESIAN_POINT('Ctrl Pts',(-9.78201139466121,3.82540972126106,
12.4490740294538));
#108054=CARTESIAN_POINT('Ctrl Pts',(-9.70886459319882,3.82908485480946,
12.436165848386));
#108055=CARTESIAN_POINT('Ctrl Pts',(-9.62826925642121,3.83350188429057,
12.415531739621));
#108056=CARTESIAN_POINT('Ctrl Pts',(-9.61953928920874,3.83398532889747,
12.4132103492714));
#108057=CARTESIAN_POINT('Ctrl Pts',(-9.60657894204175,3.83471124576169,
12.4096352656766));
#108058=CARTESIAN_POINT('Ctrl Pts',(-9.60233168046534,3.83495045552813,
12.4084429763839));
#108059=CARTESIAN_POINT('Ctrl Pts',(-9.59475888137071,3.83537942334854,
12.4062801594041));
#108060=CARTESIAN_POINT('Ctrl Pts',(-9.59143124362136,3.83556877251293,
12.4053169827976));
#108061=CARTESIAN_POINT('Ctrl Pts',(-9.58420765318586,3.83598171672622,
12.4031983066168));
#108062=CARTESIAN_POINT('Ctrl Pts',(-9.58031308018908,3.83620555537564,
12.4020383917323));
#108063=CARTESIAN_POINT('Ctrl Pts',(-9.5693876366974,3.83683676838281,12.398734882277));
#108064=CARTESIAN_POINT('Ctrl Pts',(-9.56236810983725,3.83724614241533,
12.3965545469196));
#108065=CARTESIAN_POINT('Ctrl Pts',(-9.52167520326802,3.83964038914278,
12.3835780042865));
#108066=CARTESIAN_POINT('Ctrl Pts',(-9.4883878354657,3.84168281737915,12.3716177748839));
#108067=CARTESIAN_POINT('Ctrl Pts',(-9.37697068751281,3.84873355475861,
12.3269652007139));
#108068=CARTESIAN_POINT('Ctrl Pts',(-9.3012557911328,3.85388244858191,12.2887042258911));
#108069=CARTESIAN_POINT('Ctrl Pts',(-9.16775115568061,3.86325361129794,
12.2059982852506));
#108070=CARTESIAN_POINT('Ctrl Pts',(-9.10913407821677,3.86749056508258,
12.1633701473067));
#108071=CARTESIAN_POINT('Ctrl Pts',(-9.03744416317425,3.87278480940935,
12.1026259900027));
#108072=CARTESIAN_POINT('Ctrl Pts',(-9.02129202632319,3.87398641071349,
12.0883145611338));
#108073=CARTESIAN_POINT('Ctrl Pts',(-8.99905040742021,3.87565425777772,
12.0677118228095));
#108074=CARTESIAN_POINT('Ctrl Pts',(-8.99269240572417,3.87613261406625,
12.0617156109641));
#108075=CARTESIAN_POINT('Ctrl Pts',(-8.98188559552157,3.87694853633377,
12.0513392776563));
#108076=CARTESIAN_POINT('Ctrl Pts',(-8.97741045390739,3.87728726918689,
12.0469870291625));
#108077=CARTESIAN_POINT('Ctrl Pts',(-8.96893285390491,3.87793065615391,
12.0386360271323));
#108078=CARTESIAN_POINT('Ctrl Pts',(-8.96492547785753,3.87823552324564,
12.0346424461863));
#108079=CARTESIAN_POINT('Ctrl Pts',(-8.95462702312118,3.87902097647494,
12.024259725397));
#108080=CARTESIAN_POINT('Ctrl Pts',(-8.94837127075439,3.87950003373344,
12.0178357757858));
#108081=CARTESIAN_POINT('Ctrl Pts',(-8.93066024863424,3.88086225438437,
11.9993109539905));
#108082=CARTESIAN_POINT('Ctrl Pts',(-8.91935187918126,3.88173924583813,
11.9870712004773));
#108083=CARTESIAN_POINT('Ctrl Pts',(-8.83809280218324,3.88810205326599,
11.8960487144789));
#108084=CARTESIAN_POINT('Ctrl Pts',(-8.77662140943615,3.89322482133122,
11.8101104680997));
#108085=CARTESIAN_POINT('Ctrl Pts',(-8.68360118630223,3.9024459828006,11.6449873227817));
#108086=CARTESIAN_POINT('Ctrl Pts',(-8.64870170330079,3.90653652346817,
11.5682467422017));
#108087=CARTESIAN_POINT('Ctrl Pts',(-8.61596075125646,3.91167409351744,
11.4758778841439));
#108088=CARTESIAN_POINT('Ctrl Pts',(-8.61151562744227,3.91240937872692,
11.4627477955098));
#108089=CARTESIAN_POINT('Ctrl Pts',(-8.60567595994616,3.91343178394463,
11.4446563174431));
#108090=CARTESIAN_POINT('Ctrl Pts',(-8.60411998255951,3.91371013400223,
11.439747364546));
#108091=CARTESIAN_POINT('Ctrl Pts',(-8.60154577770961,3.91418093506458,
11.4314746681681));
#108092=CARTESIAN_POINT('Ctrl Pts',(-8.60051368832493,3.91437259543914,
11.4281152461787));
#108093=CARTESIAN_POINT('Ctrl Pts',(-8.59857652184909,3.91473795727468,
11.4217279597367));
#108094=CARTESIAN_POINT('Ctrl Pts',(-8.59766913271872,3.91491152229669,
11.4187008183829));
#108095=CARTESIAN_POINT('Ctrl Pts',(-8.59553592826119,3.91532534752545,
11.4114995111017));
#108096=CARTESIAN_POINT('Ctrl Pts',(-8.594318911974,3.91556610414029,11.4073227887311));
#108097=CARTESIAN_POINT('Ctrl Pts',(-8.59008618251765,3.91642001660049,
11.3925514217248));
#108098=CARTESIAN_POINT('Ctrl Pts',(-8.58717155649628,3.91703856224464,
11.3819284826828));
#108099=CARTESIAN_POINT('Ctrl Pts',(-8.55848488315195,3.92344567725704,
11.2725496680797));
#108100=CARTESIAN_POINT('Ctrl Pts',(-8.5429925246425,3.92966933800374,11.1713942574521));
#108101=CARTESIAN_POINT('Ctrl Pts',(-8.53555432041782,3.93907835791392,
11.0148450370401));
#108102=CARTESIAN_POINT('Ctrl Pts',(-8.53602172434667,3.94233009204437,
10.9601267404747));
#108103=CARTESIAN_POINT('Ctrl Pts',(-8.54255641551234,3.94821150146611,
10.8590726087786));
#108104=CARTESIAN_POINT('Ctrl Pts',(-8.54778053460093,3.95085910693208,
10.8127524802944));
#108105=CARTESIAN_POINT('Ctrl Pts',(-8.5570171799708,3.95406748731553,10.755537359413));
#108106=CARTESIAN_POINT('Ctrl Pts',(-8.55895903372659,3.95469251157409,
10.7443393942694));
#108107=CARTESIAN_POINT('Ctrl Pts',(-8.56226119614032,3.95568201495197,
10.7265317302962));
#108108=CARTESIAN_POINT('Ctrl Pts',(-8.56353709283855,3.95604914069399,
10.7199070134034));
#108109=CARTESIAN_POINT('Ctrl Pts',(-8.56603587246791,3.95674049784029,
10.7073991913873));
#108110=CARTESIAN_POINT('Ctrl Pts',(-8.5672492641077,3.95706502196616,10.701514351197));
#108111=CARTESIAN_POINT('Ctrl Pts',(-8.57007916288314,3.95779735714886,
10.6882045715526));
#108112=CARTESIAN_POINT('Ctrl Pts',(-8.57171733135342,3.9582044711808,10.6807843815936));
#108113=CARTESIAN_POINT('Ctrl Pts',(-8.57609484049765,3.95925065853,10.6616647843114));
#108114=CARTESIAN_POINT('Ctrl Pts',(-8.57892063142789,3.95988697663107,
10.6499856274233));
#108115=CARTESIAN_POINT('Ctrl Pts',(-8.60544254377412,3.96553144806429,
10.5459895131117));
#108116=CARTESIAN_POINT('Ctrl Pts',(-8.63796046277498,3.97023393713507,
10.456155233466));
#108117=CARTESIAN_POINT('Ctrl Pts',(-8.70853018395964,3.97821463661005,
10.3081550364451));
#108118=CARTESIAN_POINT('Ctrl Pts',(-8.74239373723112,3.98151936158128,
10.2483555113975));
#108119=CARTESIAN_POINT('Ctrl Pts',(-8.80393878236052,3.98708753192422,
10.1555504170636));
#108120=CARTESIAN_POINT('Ctrl Pts',(-8.82909687958725,3.98927145510715,
10.1209989820992));
#108121=CARTESIAN_POINT('Ctrl Pts',(-8.86031214068976,3.9919410486122,10.0818508238769));
#108122=CARTESIAN_POINT('Ctrl Pts',(-8.86493985477081,3.99233586806212,
10.0761359469759));
#108123=CARTESIAN_POINT('Ctrl Pts',(-8.87213436590156,3.99294864472083,
10.0673869220076));
#108124=CARTESIAN_POINT('Ctrl Pts',(-8.87467084891018,3.99316449014423,
10.0643278657751));
#108125=CARTESIAN_POINT('Ctrl Pts',(-8.87938298240759,3.99356519843441,
10.0586918016619));
#108126=CARTESIAN_POINT('Ctrl Pts',(-8.88155511353874,3.99374981059857,
10.0561119454562));
#108127=CARTESIAN_POINT('Ctrl Pts',(-8.88650834740058,3.99417053990146,
10.0502700568117));
#108128=CARTESIAN_POINT('Ctrl Pts',(-8.88929488574262,3.99440704605749,
10.0470127106798));
#108129=CARTESIAN_POINT('Ctrl Pts',(-8.89656081382891,3.99502315628839,
10.0385943030978));
#108130=CARTESIAN_POINT('Ctrl Pts',(-8.9010620644707,3.99540426977056,10.033452348914));
#108131=CARTESIAN_POINT('Ctrl Pts',(-8.93137626248471,3.997966037854,9.99930875767027));
#108132=CARTESIAN_POINT('Ctrl Pts',(-8.95829661271478,4.00021727456717,
9.97131481010969));
#108133=CARTESIAN_POINT('Ctrl Pts',(-9.01476431686176,4.00483553466987,
9.91708687833304));
#108134=CARTESIAN_POINT('Ctrl Pts',(-9.04432665826587,4.00720196757216,
9.89091098341901));
#108135=CARTESIAN_POINT('Ctrl Pts',(-9.14238211038541,4.01481228537688,
9.81092229343975));
#108136=CARTESIAN_POINT('Ctrl Pts',(-9.21463854369616,4.02005723328906,
9.76200797819362));
#108137=CARTESIAN_POINT('Ctrl Pts',(-9.31630753092358,4.02678853680713,
9.70568712541951));
#108138=CARTESIAN_POINT('Ctrl Pts',(-9.34221204166076,4.028453545645,9.69233170412443));
#108139=CARTESIAN_POINT('Ctrl Pts',(-9.38713387223544,4.03125533436954,
9.67084460889202));
#108140=CARTESIAN_POINT('Ctrl Pts',(-9.40595567378044,4.03240451475936,
9.66232651833249));
#108141=CARTESIAN_POINT('Ctrl Pts',(-9.4328413834886,4.03401203140198,9.65083842456283));
#108142=CARTESIAN_POINT('Ctrl Pts',(-9.44076017347881,4.03448140244391,
9.64753681243631));
#108143=CARTESIAN_POINT('Ctrl Pts',(-9.45445269465086,4.03528607529179,
9.64196875920419));
#108144=CARTESIAN_POINT('Ctrl Pts',(-9.46021258359201,4.0356224761713,9.63966906229667));
#108145=CARTESIAN_POINT('Ctrl Pts',(-9.47126711829713,4.03626416858958,
9.63533668920751));
#108146=CARTESIAN_POINT('Ctrl Pts',(-9.47655929078084,4.03656965277777,
9.63329804376216));
#108147=CARTESIAN_POINT('Ctrl Pts',(-9.48901175725161,4.03728450134231,
9.62858405639713));
#108148=CARTESIAN_POINT('Ctrl Pts',(-9.49618146244723,4.03769303320538,
9.62593393216179));
#108149=CARTESIAN_POINT('Ctrl Pts',(-9.51744230244507,4.03889570352381,
9.61826411138814));
#108150=CARTESIAN_POINT('Ctrl Pts',(-9.53159022115626,4.03968466774092,
9.61340406110895));
#108151=CARTESIAN_POINT('Ctrl Pts',(-9.66522824689856,4.0470375110941,9.56977603257737));
#108152=CARTESIAN_POINT('Ctrl Pts',(-9.78916358041345,4.05305366763034,
9.54632788019479));
#108153=CARTESIAN_POINT('Ctrl Pts',(-9.98626834889587,4.06271385989675,
9.53480347257085));
#108154=CARTESIAN_POINT('Ctrl Pts',(-10.0581630668327,4.06627188786413,
9.53589475367225));
#108155=CARTESIAN_POINT('Ctrl Pts',(-10.13849097072,4.07055353624185,9.54304056907519));
#108156=CARTESIAN_POINT('Ctrl Pts',(-10.1472963951161,4.07102708668872,
9.54390443420741));
#108157=CARTESIAN_POINT('Ctrl Pts',(-10.1603799693482,4.07173767184036,
9.54530790095667));
#108158=CARTESIAN_POINT('Ctrl Pts',(-10.1646646012093,4.07197148761062,
9.54578667117222));
#108159=CARTESIAN_POINT('Ctrl Pts',(-10.1723173902641,4.07239119254161,
9.54667605814397));
#108160=CARTESIAN_POINT('Ctrl Pts',(-10.1756863076899,4.07257668293792,
9.5470794639753));
#108161=CARTESIAN_POINT('Ctrl Pts',(-10.1830333490986,4.07298282061103,
9.54798515154535));
#108162=CARTESIAN_POINT('Ctrl Pts',(-10.1870107608459,4.07320371222326,
9.54849205942315));
#108163=CARTESIAN_POINT('Ctrl Pts',(-10.1981330115468,4.07382417329191,
9.54995602666162));
#108164=CARTESIAN_POINT('Ctrl Pts',(-10.2052728377477,4.07422567425499,
9.55094952722314));
#108165=CARTESIAN_POINT('Ctrl Pts',(-10.245732920231,4.07651796416436,9.55688453663883));
#108166=CARTESIAN_POINT('Ctrl Pts',(-10.2788798819815,4.07846148918611,
9.56292220646131));
#108167=CARTESIAN_POINT('Ctrl Pts',(-10.3248256160433,4.08122089493624,
9.57294055013334));
#108168=CARTESIAN_POINT('Ctrl Pts',(-10.3378250692537,4.08200905211992,
9.57596188145257));
#108169=CARTESIAN_POINT('Ctrl Pts',(-10.359423469749,4.08332920311354,9.58129415943564));
#108170=CARTESIAN_POINT('Ctrl Pts',(-10.3680460893823,4.08385909095779,
9.58350659526353));
#108171=CARTESIAN_POINT('Ctrl Pts',(-10.4580812322691,4.08941878995923,
9.60748586870029));
#108172=CARTESIAN_POINT('Ctrl Pts',(-10.5374941053354,4.09454000816576,
9.63616891079823));
#108173=CARTESIAN_POINT('Ctrl Pts',(-10.6695066184319,4.10313123968146,
9.69718279713107));
#108174=CARTESIAN_POINT('Ctrl Pts',(-10.7233582545682,4.10666334508523,
9.72629436327319));
#108175=CARTESIAN_POINT('Ctrl Pts',(-10.7888688175068,4.11097741989449,
9.76720780475711));
#108176=CARTESIAN_POINT('Ctrl Pts',(-10.8023611620632,4.11186716641689,
9.77594640547207));
#108177=CARTESIAN_POINT('Ctrl Pts',(-10.8221460892521,4.11317413300904,
9.78922826210136));
#108178=CARTESIAN_POINT('Ctrl Pts',(-10.8285506048574,4.11359756888372,
9.79360193477379));
#108179=CARTESIAN_POINT('Ctrl Pts',(-10.8399010241364,4.1143487416071,9.80148621226924));
#108180=CARTESIAN_POINT('Ctrl Pts',(-10.8448604049933,4.11467720897415,
9.80497701807492));
#108181=CARTESIAN_POINT('Ctrl Pts',(-10.855285330716,4.11536826922182,9.81241224298774));
#108182=CARTESIAN_POINT('Ctrl Pts',(-10.8607456251433,4.11573058121202,
9.81636380234019));
#108183=CARTESIAN_POINT('Ctrl Pts',(-10.8751987505641,4.11669067126526,
9.82697628744257));
#108184=CARTESIAN_POINT('Ctrl Pts',(-10.8841429056887,4.11728592215926,
9.83370294746339));
#108185=CARTESIAN_POINT('Ctrl Pts',(-10.9235781566369,4.11991652789749,
9.86407552476082));
#108186=CARTESIAN_POINT('Ctrl Pts',(-10.9532054970541,4.12190881011942,
9.88882016212099));
#108187=CARTESIAN_POINT('Ctrl Pts',(-11.0869203946385,4.13104799140508,
10.0097869329715));
#108188=CARTESIAN_POINT('Ctrl Pts',(-11.177637315422,4.13761157382644,10.1196129677356));
#108189=CARTESIAN_POINT('Ctrl Pts',(-11.261835914936,4.14586013438316,10.2583621581496));
#108190=CARTESIAN_POINT('Ctrl Pts',(-11.2721489751241,4.14692115500028,
10.2761951376949));
#108191=CARTESIAN_POINT('Ctrl Pts',(-11.2886352955542,4.148714180465,10.3061441044475));
#108192=CARTESIAN_POINT('Ctrl Pts',(-11.2950224275119,4.14943522350565,
10.3181394461627));
#108193=CARTESIAN_POINT('Ctrl Pts',(-11.3035781319548,4.15044067137346,
10.3347614152334));
#108194=CARTESIAN_POINT('Ctrl Pts',(-11.3058910894315,4.15071665862096,
10.3393134012605));
#108195=CARTESIAN_POINT('Ctrl Pts',(-11.3097505403178,4.15118443888823,
10.3470083906919));
#108196=CARTESIAN_POINT('Ctrl Pts',(-11.3113096791728,4.15137546105613,
10.3501450587294));
#108197=CARTESIAN_POINT('Ctrl Pts',(-11.3142636463107,4.15174136690262,
10.3561417522695));
#108198=CARTESIAN_POINT('Ctrl Pts',(-11.3156604320297,4.15191612230184,
10.3590007781777));
#108199=CARTESIAN_POINT('Ctrl Pts',(-11.3189671380646,4.15233395755997,
10.3658254867663));
#108200=CARTESIAN_POINT('Ctrl Pts',(-11.3208685018215,4.15257754800281,
10.3697952519955));
#108201=CARTESIAN_POINT('Ctrl Pts',(-11.3275701156708,4.15344792844247,
10.3839507887112));
#108202=CARTESIAN_POINT('Ctrl Pts',(-11.332270563974,4.1540803382153,10.3941830544954));
#108203=CARTESIAN_POINT('Ctrl Pts',(-11.3771424094568,4.16033032924802,
10.4949115674403));
#108204=CARTESIAN_POINT('Ctrl Pts',(-11.4081476016286,4.16635450413496,
10.5892038508825));
#108205=CARTESIAN_POINT('Ctrl Pts',(-11.4440125546357,4.17638952254871,
10.7524149019133));
#108206=CARTESIAN_POINT('Ctrl Pts',(-11.4539698137171,4.18043414813969,
10.8198779079293));
#108207=CARTESIAN_POINT('Ctrl Pts',(-11.4620531741787,4.18649632257071,
10.9249991086533));
#108208=CARTESIAN_POINT('Ctrl Pts',(-11.463490280705,4.18860247107709,10.9623016056446));
#108209=CARTESIAN_POINT('Ctrl Pts',(-11.4634999508678,4.1906650539568,10.9996207771448));
#108210=CARTESIAN_POINT('Origin',(-10.,3.5,11.));
#108211=CARTESIAN_POINT('',(-11.4635,4.76071734372175,11.0000000323785));
#108212=CARTESIAN_POINT('',(-11.4635,4.68907309470234,10.9999999999272));
#108213=CARTESIAN_POINT('',(-11.4635,3.5,11.));
#108214=CARTESIAN_POINT('Ctrl Pts',(-11.4635,4.76071734372175,11.0000000323785));
#108215=CARTESIAN_POINT('Ctrl Pts',(-11.4635000002391,4.76006698159341,
10.9891917017201));
#108216=CARTESIAN_POINT('Ctrl Pts',(-11.4633802669752,4.75941670604928,
10.9783811577407));
#108217=CARTESIAN_POINT('Ctrl Pts',(-11.4608690620626,4.752607847583,10.8650820461834));
#108218=CARTESIAN_POINT('Ctrl Pts',(-11.4478351442589,4.74656325652258,
10.7631010660844));
#108219=CARTESIAN_POINT('Ctrl Pts',(-11.4211108031141,4.74010366942665,
10.6500546192025));
#108220=CARTESIAN_POINT('Ctrl Pts',(-11.4177930959355,4.73935224505105,
10.6368465353151));
#108221=CARTESIAN_POINT('Ctrl Pts',(-11.412424909794,4.73820923513488,10.6166713970486));
#108222=CARTESIAN_POINT('Ctrl Pts',(-11.4105061850128,4.73781348121368,
10.6096703337811));
#108223=CARTESIAN_POINT('Ctrl Pts',(-11.406915733191,4.7370955043669,10.5969417364871));
#108224=CARTESIAN_POINT('Ctrl Pts',(-11.4052609281689,4.73677274802698,
10.5912096267016));
#108225=CARTESIAN_POINT('Ctrl Pts',(-11.4015712498716,4.73607046762362,
10.5787160860028));
#108226=CARTESIAN_POINT('Ctrl Pts',(-11.3995223967472,4.73569140208005,
10.5719589178161));
#108227=CARTESIAN_POINT('Ctrl Pts',(-11.3937591309399,4.73465421774199,
10.5534353657643));
#108228=CARTESIAN_POINT('Ctrl Pts',(-11.3899446512638,4.73399933662033,
10.5417005713136));
#108229=CARTESIAN_POINT('Ctrl Pts',(-11.3681989230111,4.7304306400058,10.4775725621268));
#108230=CARTESIAN_POINT('Ctrl Pts',(-11.347452685443,4.72761013312772,10.4261787380737));
#108231=CARTESIAN_POINT('Ctrl Pts',(-11.2796825450749,4.71968911358206,
10.2823830850725));
#108232=CARTESIAN_POINT('Ctrl Pts',(-11.2257038705031,4.71477976942153,
10.1936439323859));
#108233=CARTESIAN_POINT('Ctrl Pts',(-11.1336575211577,4.70723622624622,
10.073200018029));
#108234=CARTESIAN_POINT('Ctrl Pts',(-11.1026458974866,4.70479473939584,
10.0365121891736));
#108235=CARTESIAN_POINT('Ctrl Pts',(-11.0647150253019,4.7018322776016,9.99587266438407));
#108236=CARTESIAN_POINT('Ctrl Pts',(-11.0594962623898,4.70142515934709,
9.99036766280083));
#108237=CARTESIAN_POINT('Ctrl Pts',(-11.0514314465998,4.70079628440902,
9.98199189525893));
#108238=CARTESIAN_POINT('Ctrl Pts',(-11.0486158245668,4.70057677771146,
9.97909185531299));
#108239=CARTESIAN_POINT('Ctrl Pts',(-11.0434249600661,4.70017210252978,
9.97378948767722));
#108240=CARTESIAN_POINT('Ctrl Pts',(-11.0410533824669,4.69998721224627,
9.97138368808151));
#108241=CARTESIAN_POINT('Ctrl Pts',(-11.0356859204814,4.69956875410312,
9.96597635021488));
#108242=CARTESIAN_POINT('Ctrl Pts',(-11.0326853259841,4.69933482551563,
9.96297962856517));
#108243=CARTESIAN_POINT('Ctrl Pts',(-11.024919562509,4.69872951547363,9.95529101603052));
#108244=CARTESIAN_POINT('Ctrl Pts',(-11.0201352341605,4.6983567066261,9.95061871972146));
#108245=CARTESIAN_POINT('Ctrl Pts',(-10.9894467185593,4.69596707211208,
9.92105702099918));
#108246=CARTESIAN_POINT('Ctrl Pts',(-10.962667327796,4.69388972184353,9.897097475539));
#108247=CARTESIAN_POINT('Ctrl Pts',(-10.9281680873675,4.6912517443498,9.8684453375328));
#108248=CARTESIAN_POINT('Ctrl Pts',(-10.921248221818,4.69072443692526,9.86280447493264));
#108249=CARTESIAN_POINT('Ctrl Pts',(-10.8383863882249,4.68443548817276,
9.79651071882984));
#108250=CARTESIAN_POINT('Ctrl Pts',(-10.7566352107316,4.67850216854922,
9.74350370590314));
#108251=CARTESIAN_POINT('Ctrl Pts',(-10.6172501684215,4.66925078563945,
9.67169804983092));
#108252=CARTESIAN_POINT('Ctrl Pts',(-10.5626498788265,4.66581263197997,
9.64766487386264));
#108253=CARTESIAN_POINT('Ctrl Pts',(-10.4918509223742,4.66159898933973,
9.6215347379253));
#108254=CARTESIAN_POINT('Ctrl Pts',(-10.4768827225729,4.66072126629397,
9.61628517924777));
#108255=CARTESIAN_POINT('Ctrl Pts',(-10.4545148306403,4.65942861226279,
9.60884653020689));
#108256=CARTESIAN_POINT('Ctrl Pts',(-10.4471787314659,4.65900765322553,
9.60647106485552));
#108257=CARTESIAN_POINT('Ctrl Pts',(-10.4340480977753,4.65825944463588,
9.60233366879131));
#108258=CARTESIAN_POINT('Ctrl Pts',(-10.4282607947573,4.65793148252047,
9.6005495300752));
#108259=CARTESIAN_POINT('Ctrl Pts',(-10.4159929889272,4.65724003472574,
9.59685077673134));
#108260=CARTESIAN_POINT('Ctrl Pts',(-10.4095099511158,4.65687684069734,
9.59494501473441));
#108261=CARTESIAN_POINT('Ctrl Pts',(-10.3921672217811,4.65591102019841,
9.58997715490186));
#108262=CARTESIAN_POINT('Ctrl Pts',(-10.3812848112144,4.65531097944266,
9.5869955924605));
#108263=CARTESIAN_POINT('Ctrl Pts',(-10.3320399407606,4.65262149741239,
9.57411383494212));
#108264=CARTESIAN_POINT('Ctrl Pts',(-10.2933179613259,4.65057764995032,
9.56564760151899));
#108265=CARTESIAN_POINT('Ctrl Pts',(-10.1396706078471,4.64267910493585,
9.53853744075819));
#108266=CARTESIAN_POINT('Ctrl Pts',(-10.0230472469863,4.63717882680453,
9.53205979938233));
#108267=CARTESIAN_POINT('Ctrl Pts',(-9.85404747007822,4.62879073839662,
9.54283364612742));
#108268=CARTESIAN_POINT('Ctrl Pts',(-9.80143167727726,4.62611251383239,
9.54906738447881));
#108269=CARTESIAN_POINT('Ctrl Pts',(-9.74165540250956,4.62288071416184,
9.55946186045097));
#108270=CARTESIAN_POINT('Ctrl Pts',(-9.73404667231101,4.62246578347306,
9.56084716417637));
#108271=CARTESIAN_POINT('Ctrl Pts',(-9.72244795156883,4.6218273316654,9.5630540364959));
#108272=CARTESIAN_POINT('Ctrl Pts',(-9.71844970297724,4.62160616826766,
9.56383208814206));
#108273=CARTESIAN_POINT('Ctrl Pts',(-9.71114276646304,4.6211999236078,9.56528568964215));
#108274=CARTESIAN_POINT('Ctrl Pts',(-9.70783312258723,4.62101513547982,
9.56595600873118));
#108275=CARTESIAN_POINT('Ctrl Pts',(-9.70040759446,4.62059878870618,9.56748671178977));
#108276=CARTESIAN_POINT('Ctrl Pts',(-9.69629311219602,4.62036688624542,
9.56835337608942));
#108277=CARTESIAN_POINT('Ctrl Pts',(-9.68425279616956,4.6196848482562,9.57094375773924));
#108278=CARTESIAN_POINT('Ctrl Pts',(-9.6763376186338,4.6192321402102,9.57271562150901));
#108279=CARTESIAN_POINT('Ctrl Pts',(-9.60885389582452,4.61533765066677,
9.58841249154717));
#108280=CARTESIAN_POINT('Ctrl Pts',(-9.55020314037553,4.61172316716515,
9.60599286747066));
#108281=CARTESIAN_POINT('Ctrl Pts',(-9.43666180945782,4.60447625328042,
9.64793939549272));
#108282=CARTESIAN_POINT('Ctrl Pts',(-9.38181816847751,4.60085288924654,
9.67211852207918));
#108283=CARTESIAN_POINT('Ctrl Pts',(-9.26481640147025,4.59299486197849,
9.73252544513172));
#108284=CARTESIAN_POINT('Ctrl Pts',(-9.20352680122065,4.58879503422589,
9.77011411323021));
#108285=CARTESIAN_POINT('Ctrl Pts',(-9.12825352236983,4.58357504836204,
9.8242754797133));
#108286=CARTESIAN_POINT('Ctrl Pts',(-9.11153256352299,4.58241063860529,
9.83685953277936));
#108287=CARTESIAN_POINT('Ctrl Pts',(-9.08832142522019,4.58078663799147,
9.85512073914929));
#108288=CARTESIAN_POINT('Ctrl Pts',(-9.08160326408213,4.58031565453016,
9.86050283654933));
#108289=CARTESIAN_POINT('Ctrl Pts',(-9.0701335027491,4.57950982044025,9.86985889911455));
#108290=CARTESIAN_POINT('Ctrl Pts',(-9.06535897941183,4.57917384902404,
9.87380429103717));
#108291=CARTESIAN_POINT('Ctrl Pts',(-9.05628205722691,4.57853405959313,
9.88140242061531));
#108292=CARTESIAN_POINT('Ctrl Pts',(-9.05197546924879,4.57823004168493,
9.88504996056674));
#108293=CARTESIAN_POINT('Ctrl Pts',(-9.04084887665433,4.57744328819505,
9.89458489986472));
#108294=CARTESIAN_POINT('Ctrl Pts',(-9.03406188954293,4.57696211743715,
9.90051057637646));
#108295=CARTESIAN_POINT('Ctrl Pts',(-9.01097518708037,4.57532054962892,
9.92104621064389));
#108296=CARTESIAN_POINT('Ctrl Pts',(-8.99494833670773,4.57417267339318,
9.93595931486271));
#108297=CARTESIAN_POINT('Ctrl Pts',(-8.87064410368156,4.56518419476819,
10.0569407878142));
#108298=CARTESIAN_POINT('Ctrl Pts',(-8.77912095313951,4.55815464699216,
10.1788699898861));
#108299=CARTESIAN_POINT('Ctrl Pts',(-8.68864390469351,4.54849552282197,
10.3489498082288));
#108300=CARTESIAN_POINT('Ctrl Pts',(-8.67088137798294,4.54638986834393,
10.386025823709));
#108301=CARTESIAN_POINT('Ctrl Pts',(-8.6518199071518,4.54380766849645,10.4305297735395));
#108302=CARTESIAN_POINT('Ctrl Pts',(-8.64898669464144,4.54341430415586,
10.4372843116696));
#108303=CARTESIAN_POINT('Ctrl Pts',(-8.64468998516335,4.54280231069275,
10.4477474251766));
#108304=CARTESIAN_POINT('Ctrl Pts',(-8.64319069908793,4.54258574736916,
10.4514412858155));
#108305=CARTESIAN_POINT('Ctrl Pts',(-8.64044728142347,4.5421837665463,10.4582804267795));
#108306=CARTESIAN_POINT('Ctrl Pts',(-8.63919894571175,4.54199860030833,
10.4614239324142));
#108307=CARTESIAN_POINT('Ctrl Pts',(-8.63638449297455,4.5415759715976,10.468583421798));
#108308=CARTESIAN_POINT('Ctrl Pts',(-8.63482522089789,4.54133811583802,
10.4726019983709));
#108309=CARTESIAN_POINT('Ctrl Pts',(-8.63080962526865,4.54071590388535,
10.4830881784182));
#108310=CARTESIAN_POINT('Ctrl Pts',(-8.6283813980002,4.54032998820244,10.4895663408298));
#108311=CARTESIAN_POINT('Ctrl Pts',(-8.61200965341005,4.53766157520196,
10.5342042929301));
#108312=CARTESIAN_POINT('Ctrl Pts',(-8.59961554425191,4.5353018501579,10.5729102311699));
#108313=CARTESIAN_POINT('Ctrl Pts',(-8.56636470243833,4.52788959179638,
10.6938674780609));
#108314=CARTESIAN_POINT('Ctrl Pts',(-8.5510342191019,4.52272421054177,10.7774562479718));
#108315=CARTESIAN_POINT('Ctrl Pts',(-8.53613052030939,4.51331459876314,
10.9346951991438));
#108316=CARTESIAN_POINT('Ctrl Pts',(-8.53469512208989,4.50905315354574,
11.007909207974));
#108317=CARTESIAN_POINT('Ctrl Pts',(-8.53971172793616,4.50397343010813,
11.0984860436277));
#108318=CARTESIAN_POINT('Ctrl Pts',(-8.54100021829184,4.50299854921395,
11.1160216054971));
#108319=CARTESIAN_POINT('Ctrl Pts',(-8.54333744580792,4.50159234978565,
11.1415309200178));
#108320=CARTESIAN_POINT('Ctrl Pts',(-8.54413636693365,4.50115336236033,
11.1495255282902));
#108321=CARTESIAN_POINT('Ctrl Pts',(-8.54565738394172,4.50038478772996,
11.1635756343457));
#108322=CARTESIAN_POINT('Ctrl Pts',(-8.54635156481252,4.50005434347198,
11.1696339042389));
#108323=CARTESIAN_POINT('Ctrl Pts',(-8.547875307817,4.49936895495072,11.1822350761924));
#108324=CARTESIAN_POINT('Ctrl Pts',(-8.54871127520404,4.49901421769615,
11.1887770745228));
#108325=CARTESIAN_POINT('Ctrl Pts',(-8.55099855944523,4.49809590150956,
11.2057625900771));
#108326=CARTESIAN_POINT('Ctrl Pts',(-8.55251857745293,4.49753446808652,
11.2161965710375));
#108327=CARTESIAN_POINT('Ctrl Pts',(-8.55923042448646,4.49524038417566,
11.2590197917275));
#108328=CARTESIAN_POINT('Ctrl Pts',(-8.5653978762397,4.49353813545569,11.2912476205234));
#108329=CARTESIAN_POINT('Ctrl Pts',(-8.57825573472954,4.49056676660924,
11.3480246231672));
#108330=CARTESIAN_POINT('Ctrl Pts',(-8.58451252818077,4.48928696024296,
11.3726569293875));
#108331=CARTESIAN_POINT('Ctrl Pts',(-8.61968510283551,4.48282390277454,
11.4974164339687));
#108332=CARTESIAN_POINT('Ctrl Pts',(-8.65859282370361,4.47788582042177,
11.594405370506));
#108333=CARTESIAN_POINT('Ctrl Pts',(-8.73006742722019,4.47030391446386,
11.7289889325994));
#108334=CARTESIAN_POINT('Ctrl Pts',(-8.7547514087074,4.46785440218498,11.7703951560246));
#108335=CARTESIAN_POINT('Ctrl Pts',(-8.78563341847975,4.46488283143444,
11.8168253661177));
#108336=CARTESIAN_POINT('Ctrl Pts',(-8.78988642461653,4.46447542905982,
11.8231129951655));
#108337=CARTESIAN_POINT('Ctrl Pts',(-8.79647932256232,4.46384620767094,
11.8326983704181));
#108338=CARTESIAN_POINT('Ctrl Pts',(-8.79878435103489,4.46362664257924,
11.8360200721278));
#108339=CARTESIAN_POINT('Ctrl Pts',(-8.8030405039941,4.46322191608363,11.8420995350851));
#108340=CARTESIAN_POINT('Ctrl Pts',(-8.80498743780961,4.46303703343914,
11.8448601290615));
#108341=CARTESIAN_POINT('Ctrl Pts',(-8.80939919697607,4.46261866491626,
11.8510698852408));
#108342=CARTESIAN_POINT('Ctrl Pts',(-8.81186944573324,4.46238481897063,
11.854515071148));
#108343=CARTESIAN_POINT('Ctrl Pts',(-8.8182721689715,4.46177985643482,11.8633633308517));
#108344=CARTESIAN_POINT('Ctrl Pts',(-8.82222670286482,4.46140731505097,
11.8687502315531));
#108345=CARTESIAN_POINT('Ctrl Pts',(-8.84761937332365,4.45902312630088,
11.9028483084829));
#108346=CARTESIAN_POINT('Ctrl Pts',(-8.87006748617596,4.45695125976555,
11.9307890713788));
#108347=CARTESIAN_POINT('Ctrl Pts',(-8.90011803659311,4.45425074797896,
11.9655017641984));
#108348=CARTESIAN_POINT('Ctrl Pts',(-8.90679840846839,4.4536547185935,11.9730592296928));
#108349=CARTESIAN_POINT('Ctrl Pts',(-8.91986679995594,4.45249787000394,
11.9875389773571));
#108350=CARTESIAN_POINT('Ctrl Pts',(-8.92624461799343,4.45193735657752,
11.9944698776333));
#108351=CARTESIAN_POINT('Ctrl Pts',(-8.98375394072611,4.44692228004805,
12.0557681631929));
#108352=CARTESIAN_POINT('Ctrl Pts',(-9.03890816475989,4.44239233869295,
12.1062122084702));
#108353=CARTESIAN_POINT('Ctrl Pts',(-9.13786892075807,4.43492025791827,
12.1837098897234));
#108354=CARTESIAN_POINT('Ctrl Pts',(-9.17968930443782,4.43193188163528,
12.2130664512608));
#108355=CARTESIAN_POINT('Ctrl Pts',(-9.24872740868775,4.42728275583539,
12.2563224986996));
#108356=CARTESIAN_POINT('Ctrl Pts',(-9.27499100648203,4.42557472228268,
12.2716598909955));
#108357=CARTESIAN_POINT('Ctrl Pts',(-9.31072379647752,4.42332952796018,
12.2910598941398));
#108358=CARTESIAN_POINT('Ctrl Pts',(-9.31978407134148,4.42276679088924,
12.2958563318792));
#108359=CARTESIAN_POINT('Ctrl Pts',(-9.3346982753956,4.421850959482,12.3035522709367));
#108360=CARTESIAN_POINT('Ctrl Pts',(-9.34052243956966,4.42149590429826,
12.306508422106));
#108361=CARTESIAN_POINT('Ctrl Pts',(-9.35184348905517,4.42081067609336,
12.3121596178073));
#108362=CARTESIAN_POINT('Ctrl Pts',(-9.35733787023911,4.42048034632237,
12.3148593513447));
#108363=CARTESIAN_POINT('Ctrl Pts',(-9.37022258487034,4.4197108169443,12.3210903605723));
#108364=CARTESIAN_POINT('Ctrl Pts',(-9.37762598433645,4.41927256146422,
12.3245942479525));
#108365=CARTESIAN_POINT('Ctrl Pts',(-9.40180256049737,4.4178537538849,12.3357891112053));
#108366=CARTESIAN_POINT('Ctrl Pts',(-9.41869219883564,4.4168818188004,12.3432252255225));
#108367=CARTESIAN_POINT('Ctrl Pts',(-9.45893437620366,4.41460800038661,
12.3600416678689));
#108368=CARTESIAN_POINT('Ctrl Pts',(-9.4823973497858,4.4133150597027,12.3691431381006));
#108369=CARTESIAN_POINT('Ctrl Pts',(-9.57210490072127,4.40847764844481,
12.4013054761191));
#108370=CARTESIAN_POINT('Ctrl Pts',(-9.63974446153239,4.40505063387864,
12.4201999940375));
#108371=CARTESIAN_POINT('Ctrl Pts',(-9.80253993073046,4.39696478013528,
12.4532909300598));
#108372=CARTESIAN_POINT('Ctrl Pts',(-9.89824112606891,4.39233986708645,
12.4631082288743));
#108373=CARTESIAN_POINT('Ctrl Pts',(-10.0055896289308,4.3866834839278,12.4635336432352));
#108374=CARTESIAN_POINT('Ctrl Pts',(-10.0169787531758,4.38607733689636,
12.4634458223974));
#108375=CARTESIAN_POINT('Ctrl Pts',(-10.0327886102945,4.38522613525996,
12.4631393404871));
#108376=CARTESIAN_POINT('Ctrl Pts',(-10.0372114085697,4.3849869492825,12.4630335377909));
#108377=CARTESIAN_POINT('Ctrl Pts',(-10.0448213691902,4.38457346982709,
12.4628169622198));
#108378=CARTESIAN_POINT('Ctrl Pts',(-10.0480088006151,4.38439970082249,
12.4627158215997));
#108379=CARTESIAN_POINT('Ctrl Pts',(-10.0546920904973,4.38403407879386,
12.4624818849986));
#108380=CARTESIAN_POINT('Ctrl Pts',(-10.0581878259649,4.38384210577452,
12.4623469714208));
#108381=CARTESIAN_POINT('Ctrl Pts',(-10.0667602993354,4.38336959491487,
12.4619853410258));
#108382=CARTESIAN_POINT('Ctrl Pts',(-10.0718363817969,4.38308830523951,
12.4617447135627));
#108383=CARTESIAN_POINT('Ctrl Pts',(-10.0903169807852,4.3820590050995,12.4607721623199));
#108384=CARTESIAN_POINT('Ctrl Pts',(-10.1037121135729,4.38130297595579,
12.4598822687781));
#108385=CARTESIAN_POINT('Ctrl Pts',(-10.1372907698024,4.37938590431397,
12.4571870465033));
#108386=CARTESIAN_POINT('Ctrl Pts',(-10.1574522302599,4.37821498034552,
12.4551465795295));
#108387=CARTESIAN_POINT('Ctrl Pts',(-10.2470186685465,4.37294292897814,
12.4441987617279));
#108388=CARTESIAN_POINT('Ctrl Pts',(-10.315772420299,4.36871200208075,12.4307394415528));
#108389=CARTESIAN_POINT('Ctrl Pts',(-10.4782865807458,4.35858787967845,
12.3866368580609));
#108390=CARTESIAN_POINT('Ctrl Pts',(-10.5704465860408,4.35275828229026,
12.3513385778554));
#108391=CARTESIAN_POINT('Ctrl Pts',(-10.6749533804014,4.34619544065918,
12.2986973359208));
#108392=CARTESIAN_POINT('Ctrl Pts',(-10.6913720895069,4.34516497975277,
12.2900315942557));
#108393=CARTESIAN_POINT('Ctrl Pts',(-10.7140910824816,4.3437394343945,12.2774822085547));
#108394=CARTESIAN_POINT('Ctrl Pts',(-10.7205330482661,4.34333525461376,
12.2738598809937));
#108395=CARTESIAN_POINT('Ctrl Pts',(-10.7322933918196,4.34259737620842,
12.267129266984));
#108396=CARTESIAN_POINT('Ctrl Pts',(-10.7376200867129,4.34226315801337,
12.2640359173036));
#108397=CARTESIAN_POINT('Ctrl Pts',(-10.7483921359397,4.34158720515927,
12.2576890295778));
#108398=CARTESIAN_POINT('Ctrl Pts',(-10.7538361872963,4.34124555015794,
12.2544335329991));
#108399=CARTESIAN_POINT('Ctrl Pts',(-10.767266193376,4.34040253110171,12.2462835015279));
#108400=CARTESIAN_POINT('Ctrl Pts',(-10.7752267137763,4.33990267595804,
12.2413474636006));
#108401=CARTESIAN_POINT('Ctrl Pts',(-10.8051513274522,4.33802249945004,
12.2223921321279));
#108402=CARTESIAN_POINT('Ctrl Pts',(-10.8267877255677,4.33666080295548,
12.207863133798));
#108403=CARTESIAN_POINT('Ctrl Pts',(-10.8805507232855,4.33326098006719,
12.1696389640808));
#108404=CARTESIAN_POINT('Ctrl Pts',(-10.9121177413857,4.33124982275521,
12.145192735519));
#108405=CARTESIAN_POINT('Ctrl Pts',(-10.9921859330042,4.32605204862986,
12.0777724094825));
#108406=CARTESIAN_POINT('Ctrl Pts',(-11.0389018818581,4.32292138961851,
12.032816249364));
#108407=CARTESIAN_POINT('Ctrl Pts',(-11.1331478777198,4.3160944600365,11.9292335494198));
#108408=CARTESIAN_POINT('Ctrl Pts',(-11.1794325066448,4.31239862987386,
11.8697331038137));
#108409=CARTESIAN_POINT('Ctrl Pts',(-11.2275618969624,4.30780627260153,
11.7969119597719));
#108410=CARTESIAN_POINT('Ctrl Pts',(-11.234068844469,4.30716691251265,11.7867979100659));
#108411=CARTESIAN_POINT('Ctrl Pts',(-11.2431077156103,4.30625040892505,
11.772360367902));
#108412=CARTESIAN_POINT('Ctrl Pts',(-11.2457433860401,4.30597962197698,
11.7681020408617));
#108413=CARTESIAN_POINT('Ctrl Pts',(-11.2501573060547,4.30551996480853,
11.7608882026661));
#108414=CARTESIAN_POINT('Ctrl Pts',(-11.2519470852066,4.30533183135619,
11.7579397353729));
#108415=CARTESIAN_POINT('Ctrl Pts',(-11.255602759857,4.30494389355082,11.7518691299748));
#108416=CARTESIAN_POINT('Ctrl Pts',(-11.2574674582387,4.30474401929378,
11.7487463322423));
#108417=CARTESIAN_POINT('Ctrl Pts',(-11.2622426092817,4.30422707498271,
11.7406812689536));
#108418=CARTESIAN_POINT('Ctrl Pts',(-11.2651356557008,4.30390892658485,
11.7357288340929));
#108419=CARTESIAN_POINT('Ctrl Pts',(-11.277239274818,4.30255716276801,11.7147268760488));
#108420=CARTESIAN_POINT('Ctrl Pts',(-11.28617374447,4.30150777462773,11.6985210852964));
#108421=CARTESIAN_POINT('Ctrl Pts',(-11.309560960176,4.29862514904188,11.6541295645834));
#108422=CARTESIAN_POINT('Ctrl Pts',(-11.3234094925998,4.29676644455017,
11.6256376684137));
#108423=CARTESIAN_POINT('Ctrl Pts',(-11.3763842363113,4.28905422820884,
11.5070037375033));
#108424=CARTESIAN_POINT('Ctrl Pts',(-11.4073107495677,4.28305745858354,
11.4134788135742));
#108425=CARTESIAN_POINT('Ctrl Pts',(-11.4350097033341,4.27554249598131,
11.2888652974904));
#108426=CARTESIAN_POINT('Ctrl Pts',(-11.4405213853676,4.27383108191672,
11.259989026018));
#108427=CARTESIAN_POINT('Ctrl Pts',(-11.4507711367393,4.2701016011383,11.1958558255877));
#108428=CARTESIAN_POINT('Ctrl Pts',(-11.4551013009719,4.26809586376428,
11.1605518728364));
#108429=CARTESIAN_POINT('Ctrl Pts',(-11.459069417551,4.2655294348156,11.1143087612984));
#108430=CARTESIAN_POINT('Ctrl Pts',(-11.4598770673208,4.26493298247324,
11.1034843723839));
#108431=CARTESIAN_POINT('Ctrl Pts',(-11.4609860347905,4.26397641895943,
11.0860025924325));
#108432=CARTESIAN_POINT('Ctrl Pts',(-11.4613624250568,4.26361400115722,
11.0793505162485));
#108433=CARTESIAN_POINT('Ctrl Pts',(-11.4619952223012,4.26292372639437,
11.0666269105991));
#108434=CARTESIAN_POINT('Ctrl Pts',(-11.4622592649713,4.26259564050504,
11.0605559145251));
#108435=CARTESIAN_POINT('Ctrl Pts',(-11.4627790706779,4.2618444537934,11.0466028848607));
#108436=CARTESIAN_POINT('Ctrl Pts',(-11.4630089543204,4.26142215982443,
11.0387200381982));
#108437=CARTESIAN_POINT('Ctrl Pts',(-11.4633916991168,4.26045385918552,
11.0205584834817));
#108438=CARTESIAN_POINT('Ctrl Pts',(-11.4634999999986,4.25990923949891,
11.0102793802479));
#108439=CARTESIAN_POINT('Ctrl Pts',(-11.4635,4.25936781471288,11.0000000001943));
#108440=CARTESIAN_POINT('Ctrl Pts',(-11.4634999508678,4.1906650539568,10.9996207771448));
#108441=CARTESIAN_POINT('Ctrl Pts',(-11.4635027073645,4.19125299678564,
11.0102586717368));
#108442=CARTESIAN_POINT('Ctrl Pts',(-11.4633894767784,4.19183736043388,
11.0208964674618));
#108443=CARTESIAN_POINT('Ctrl Pts',(-11.4630177869332,4.19277917313937,
11.038143611353));
#108444=CARTESIAN_POINT('Ctrl Pts',(-11.4628304973372,4.19313880559912,
11.0447539721701));
#108445=CARTESIAN_POINT('Ctrl Pts',(-11.4623847929826,4.19382678807775,
11.0574457460763));
#108446=CARTESIAN_POINT('Ctrl Pts',(-11.462133231498,4.19415534252685,11.0635272490928));
#108447=CARTESIAN_POINT('Ctrl Pts',(-11.4614642418366,4.1949118984824,11.0775769476081));
#108448=CARTESIAN_POINT('Ctrl Pts',(-11.4610195731432,4.19533904961798,
11.0855436921553));
#108449=CARTESIAN_POINT('Ctrl Pts',(-11.4594046954425,4.19668585455684,
11.1107670124031));
#108450=CARTESIAN_POINT('Ctrl Pts',(-11.4579937014578,4.19759807587921,
11.1280070143655));
#108451=CARTESIAN_POINT('Ctrl Pts',(-11.4492537410059,4.20219873302817,
11.2156529495561));
#108452=CARTESIAN_POINT('Ctrl Pts',(-11.4371292417829,4.20573662907436,
11.2854883125994));
#108453=CARTESIAN_POINT('Ctrl Pts',(-11.4075844070937,4.21172667476086,
11.4039416860583));
#108454=CARTESIAN_POINT('Ctrl Pts',(-11.3925649089516,4.21420695202438,
11.453018478542));
#108455=CARTESIAN_POINT('Ctrl Pts',(-11.3632979534051,4.21837900901593,
11.5333090216644));
#108456=CARTESIAN_POINT('Ctrl Pts',(-11.3504754216913,4.22005673416179,
11.564991872712));
#108457=CARTESIAN_POINT('Ctrl Pts',(-11.330810666419,4.22247075492003,11.6090764668431));
#108458=CARTESIAN_POINT('Ctrl Pts',(-11.3248792541956,4.22318125671054,
11.6218730715134));
#108459=CARTESIAN_POINT('Ctrl Pts',(-11.3058385451146,4.22541460586849,
11.6614427630739));
#108460=CARTESIAN_POINT('Ctrl Pts',(-11.2920963094104,4.22696038963874,
11.6879009581243));
#108461=CARTESIAN_POINT('Ctrl Pts',(-11.274168729513,4.22892237210212,11.719982317872));
#108462=CARTESIAN_POINT('Ctrl Pts',(-11.2707375725481,4.22929560577588,
11.7260210101884));
#108463=CARTESIAN_POINT('Ctrl Pts',(-11.2652907127421,4.22988494870316,
11.7354503516548));
#108464=CARTESIAN_POINT('Ctrl Pts',(-11.2633040191641,4.23009926539293,
11.738857741328));
#108465=CARTESIAN_POINT('Ctrl Pts',(-11.2595859380812,4.23049925262188,
11.7451758076356));
#108466=CARTESIAN_POINT('Ctrl Pts',(-11.2578582013422,4.23068469251387,
11.7480885403933));
#108467=CARTESIAN_POINT('Ctrl Pts',(-11.2538796788197,4.23111072076019,
11.7547430475418));
#108468=CARTESIAN_POINT('Ctrl Pts',(-11.2516222499169,4.23135172895555,
11.7584807573541));
#108469=CARTESIAN_POINT('Ctrl Pts',(-11.2445633976118,4.23210298617417,
11.7700510388611));
#108470=CARTESIAN_POINT('Ctrl Pts',(-11.2397050161034,4.23261670820045,
11.7778483897551));
#108471=CARTESIAN_POINT('Ctrl Pts',(-11.2281639899435,4.23382838740645,
11.7959881152876));
#108472=CARTESIAN_POINT('Ctrl Pts',(-11.2214236564232,4.23452949560012,
11.8062928121524));
#108473=CARTESIAN_POINT('Ctrl Pts',(-11.19712487554,4.23703087890603,11.8424370801194));
#108474=CARTESIAN_POINT('Ctrl Pts',(-11.1788706641113,4.2388632731865,11.8677971810766));
#108475=CARTESIAN_POINT('Ctrl Pts',(-11.1018566529653,4.24635550263498,
11.9678724344192));
#108476=CARTESIAN_POINT('Ctrl Pts',(-11.0366934559322,4.25215340792624,
12.0373684494402));
#108477=CARTESIAN_POINT('Ctrl Pts',(-10.9163831261478,4.26160123827869,
12.1429350258821));
#108478=CARTESIAN_POINT('Ctrl Pts',(-10.8647109117015,4.26534512552799,
12.1825122853686));
#108479=CARTESIAN_POINT('Ctrl Pts',(-10.8008733870488,4.26960309813988,
12.2249774492004));
#108480=CARTESIAN_POINT('Ctrl Pts',(-10.7910980123733,4.27024573145171,
12.2313130710421));
#108481=CARTESIAN_POINT('Ctrl Pts',(-10.7748918506384,4.27129600320372,
12.2415439454792));
#108482=CARTESIAN_POINT('Ctrl Pts',(-10.7685049666905,4.27170612109958,
12.2455074740235));
#108483=CARTESIAN_POINT('Ctrl Pts',(-10.7569303214436,4.27244262711917,
12.2525674566509));
#108484=CARTESIAN_POINT('Ctrl Pts',(-10.751753416213,4.27276963983353,12.2556813081762));
#108485=CARTESIAN_POINT('Ctrl Pts',(-10.7406324770407,4.27346707039785,
12.2622770043287));
#108486=CARTESIAN_POINT('Ctrl Pts',(-10.7346828267279,4.27383713431826,
12.2657491252309));
#108487=CARTESIAN_POINT('Ctrl Pts',(-10.7184151731367,4.27484081446469,
12.2750893216377));
#108488=CARTESIAN_POINT('Ctrl Pts',(-10.7080498214554,4.27547147499225,
12.2808741548062));
#108489=CARTESIAN_POINT('Ctrl Pts',(-10.6506813350237,4.27891528209451,
12.3119818981885));
#108490=CARTESIAN_POINT('Ctrl Pts',(-10.6023877125966,4.28164167132618,
12.3348455088745));
#108491=CARTESIAN_POINT('Ctrl Pts',(-10.4875609921858,4.28783735645884,
12.3817033197719));
#108492=CARTESIAN_POINT('Ctrl Pts',(-10.420325975879,4.29125219786606,12.403618980909));
#108493=CARTESIAN_POINT('Ctrl Pts',(-10.2771246201473,4.29844200637088,
12.4390788668867));
#108494=CARTESIAN_POINT('Ctrl Pts',(-10.2011447474074,4.30221214224991,
12.4516488240615));
#108495=CARTESIAN_POINT('Ctrl Pts',(-10.112576159206,4.30688909545454,12.459213147033));
#108496=CARTESIAN_POINT('Ctrl Pts',(-10.100601713755,4.30752741606844,12.4600875580106));
#108497=CARTESIAN_POINT('Ctrl Pts',(-10.0841151733023,4.30841612886615,
12.4610876907105));
#108498=CARTESIAN_POINT('Ctrl Pts',(-10.0796109167686,4.30865994437959,
12.461340036809));
#108499=CARTESIAN_POINT('Ctrl Pts',(-10.0718959075772,4.30907939793572,
12.4617364871842));
#108500=CARTESIAN_POINT('Ctrl Pts',(-10.0686856869701,4.30925447807271,
12.4618908493761));
#108501=CARTESIAN_POINT('Ctrl Pts',(-10.0619979617401,4.30962039834609,
12.4621903490625));
#108502=CARTESIAN_POINT('Ctrl Pts',(-10.0585204327042,4.30981134273063,
12.4623336562643));
#108503=CARTESIAN_POINT('Ctrl Pts',(-10.0500617043155,4.31027737588285,
12.4626520157003));
#108504=CARTESIAN_POINT('Ctrl Pts',(-10.0450800768072,4.31055316982355,
12.4628140273009));
#108505=CARTESIAN_POINT('Ctrl Pts',(-10.0273307201407,4.31154032086842,
12.4633005167618));
#108506=CARTESIAN_POINT('Ctrl Pts',(-10.0145600471893,4.31225888096742,
12.4634832944315));
#108507=CARTESIAN_POINT('Ctrl Pts',(-9.98283890601908,4.31406163315034,
12.4635220723229));
#108508=CARTESIAN_POINT('Ctrl Pts',(-9.96389084247117,4.31515434596721,
12.4631771691707));
#108509=CARTESIAN_POINT('Ctrl Pts',(-9.88297682892465,4.31987390022469,
12.4601317210455));
#108510=CARTESIAN_POINT('Ctrl Pts',(-9.82121186205631,4.32360756779023,
12.4538614626365));
#108511=CARTESIAN_POINT('Ctrl Pts',(-9.65239117560432,4.33390627374144,
12.4258006583493));
#108512=CARTESIAN_POINT('Ctrl Pts',(-9.54706966550362,4.34040884773393,
12.395922924126));
#108513=CARTESIAN_POINT('Ctrl Pts',(-9.42919808313093,4.34754690018117,
12.3477197155518));
#108514=CARTESIAN_POINT('Ctrl Pts',(-9.4124875137565,4.34855645308008,12.3405194441713));
#108515=CARTESIAN_POINT('Ctrl Pts',(-9.38857552538606,4.34999809638388,
12.3296831549033));
#108516=CARTESIAN_POINT('Ctrl Pts',(-9.38126354408988,4.35043852947603,
12.3262964911135));
#108517=CARTESIAN_POINT('Ctrl Pts',(-9.36844373688849,4.3512101073188,12.3202296952608));
#108518=CARTESIAN_POINT('Ctrl Pts',(-9.36292411481005,4.3515421107202,12.3175750755878));
#108519=CARTESIAN_POINT('Ctrl Pts',(-9.35155387096724,4.35222566786066,
12.3120184891237));
#108520=CARTESIAN_POINT('Ctrl Pts',(-9.34570567568064,4.35257705179822,
12.3091118504968));
#108521=CARTESIAN_POINT('Ctrl Pts',(-9.33073637664173,4.35347606570667,
12.3015465206673));
#108522=CARTESIAN_POINT('Ctrl Pts',(-9.32164428256312,4.35402172131619,
12.2968310108645));
#108523=CARTESIAN_POINT('Ctrl Pts',(-9.28318524384873,4.35632895778256,
12.2763695257117));
#108524=CARTESIAN_POINT('Ctrl Pts',(-9.25431004452896,4.35805879535214,
12.2597179324156));
#108525=CARTESIAN_POINT('Ctrl Pts',(-9.17768256559356,4.36266759721873,
12.2119698606601));
#108526=CARTESIAN_POINT('Ctrl Pts',(-9.13113600827753,4.36548558557964,
12.1790474537085));
#108527=CARTESIAN_POINT('Ctrl Pts',(-9.06792739507211,4.36944187511943,
12.1285590632618));
#108528=CARTESIAN_POINT('Ctrl Pts',(-9.04959881169916,4.37060630122378,
12.1131677744841));
#108529=CARTESIAN_POINT('Ctrl Pts',(-8.96385440927159,4.37617070434543,
12.037502478922));
#108530=CARTESIAN_POINT('Ctrl Pts',(-8.90175186074244,4.38054913836327,
11.971522668923));
#108531=CARTESIAN_POINT('Ctrl Pts',(-8.83894846368413,4.38592479157026,
11.8910265424341));
#108532=CARTESIAN_POINT('Ctrl Pts',(-8.8318668714319,4.38654675365553,11.881722148035));
#108533=CARTESIAN_POINT('Ctrl Pts',(-8.82223408834294,4.3874164853401,11.8687460372733));
#108534=CARTESIAN_POINT('Ctrl Pts',(-8.81958691330211,4.3876580410826,11.8651457470532));
#108535=CARTESIAN_POINT('Ctrl Pts',(-8.81507186845236,4.38807454162844,
11.8589457609359));
#108536=CARTESIAN_POINT('Ctrl Pts',(-8.81319594684265,4.38824894444864,
11.8563519347607));
#108537=CARTESIAN_POINT('Ctrl Pts',(-8.80929378889067,4.38861461406567,
11.8509189944278));
#108538=CARTESIAN_POINT('Ctrl Pts',(-8.80726918133989,4.38880599259048,
11.8480787756091));
#108539=CARTESIAN_POINT('Ctrl Pts',(-8.80235086006076,4.38927490761548,
11.8411266665044));
#108540=CARTESIAN_POINT('Ctrl Pts',(-8.79946815837098,4.38955317055933,
11.8370070652155));
#108541=CARTESIAN_POINT('Ctrl Pts',(-8.7891719422427,4.39055921897083,11.8221303669832));
#108542=CARTESIAN_POINT('Ctrl Pts',(-8.78188153140228,4.39129456988115,
11.8112892814181));
#108543=CARTESIAN_POINT('Ctrl Pts',(-8.76405427341029,4.39314834541059,
11.7839974664613));
#108544=CARTESIAN_POINT('Ctrl Pts',(-8.753700028478,4.39427588787582,11.767430897717));
#108545=CARTESIAN_POINT('Ctrl Pts',(-8.71010388074995,4.39923549520253,
11.6944678142483));
#108546=CARTESIAN_POINT('Ctrl Pts',(-8.68033651541236,4.40318424201987,
11.6360857662842));
#108547=CARTESIAN_POINT('Ctrl Pts',(-8.61349356452003,4.41340422112537,
11.4799295966039));
#108548=CARTESIAN_POINT('Ctrl Pts',(-8.58279132160847,4.41960936200771,
11.3798137658191));
#108549=CARTESIAN_POINT('Ctrl Pts',(-8.55986463368865,4.42639467067139,
11.2609927101217));
#108550=CARTESIAN_POINT('Ctrl Pts',(-8.55700059874931,4.42731571203824,
11.2446626811821));
#108551=CARTESIAN_POINT('Ctrl Pts',(-8.55302306296479,4.42871907721364,
11.2194756706173));
#108552=CARTESIAN_POINT('Ctrl Pts',(-8.55171214278256,4.42920750387156,
11.2106516410122));
#108553=CARTESIAN_POINT('Ctrl Pts',(-8.54970580714675,4.4299999942246,11.1962413903572));
#108554=CARTESIAN_POINT('Ctrl Pts',(-8.54896180845184,4.43030556452011,
11.1906622590033));
#108555=CARTESIAN_POINT('Ctrl Pts',(-8.5474646733417,4.43094616816877,11.1789188044287));
#108556=CARTESIAN_POINT('Ctrl Pts',(-8.54671854818662,4.43128097748929,
11.1727536894348));
#108557=CARTESIAN_POINT('Ctrl Pts',(-8.54502222741896,4.43208153777317,
11.1579477573861));
#108558=CARTESIAN_POINT('Ctrl Pts',(-8.54410972596326,4.4325461109285,11.1493028034469));
#108559=CARTESIAN_POINT('Ctrl Pts',(-8.54121285508634,4.43414892854893,
11.1192996527263));
#108560=CARTESIAN_POINT('Ctrl Pts',(-8.53962098862819,4.43527505851465,
11.0979058031575));
#108561=CARTESIAN_POINT('Ctrl Pts',(-8.53509199129682,4.43977162261828,
11.0113630567045));
#108562=CARTESIAN_POINT('Ctrl Pts',(-8.53604006145651,4.44302476659197,
10.9460835370252));
#108563=CARTESIAN_POINT('Ctrl Pts',(-8.54680819821287,4.44952643021242,
10.8140017619516));
#108564=CARTESIAN_POINT('Ctrl Pts',(-8.55689734880188,4.45276409907855,
10.7473812312367));
#108565=CARTESIAN_POINT('Ctrl Pts',(-8.5845086068357,4.45901648981022,10.6234704505779));
#108566=CARTESIAN_POINT('Ctrl Pts',(-8.60102853696015,4.46201036422626,
10.5661016692836));
#108567=CARTESIAN_POINT('Ctrl Pts',(-8.62370958719293,4.4656129085021,10.5022827863349));
#108568=CARTESIAN_POINT('Ctrl Pts',(-8.62648242959269,4.46604654272255,
10.4946810877714));
#108569=CARTESIAN_POINT('Ctrl Pts',(-8.63079036824818,4.46671071561686,
10.4831684197133));
#108570=CARTESIAN_POINT('Ctrl Pts',(-8.6322795489361,4.46693865547146,10.4792403002204));
#108571=CARTESIAN_POINT('Ctrl Pts',(-8.63499649072198,4.46735166425808,
10.4721656723265));
#108572=CARTESIAN_POINT('Ctrl Pts',(-8.63621825226574,4.4675363803055,10.469016947591));
#108573=CARTESIAN_POINT('Ctrl Pts',(-8.63893946360308,4.46794560473289,
10.4620751900769));
#108574=CARTESIAN_POINT('Ctrl Pts',(-8.6404438572736,4.46817039661519,10.4582842269078));
#108575=CARTESIAN_POINT('Ctrl Pts',(-8.64485485056415,4.46882525345754,
10.4473029554661));
#108576=CARTESIAN_POINT('Ctrl Pts',(-8.6478027395085,4.46925765648791,10.4401295127875));
#108577=CARTESIAN_POINT('Ctrl Pts',(-8.67161106243556,4.47270724495156,
10.3834789321));
#108578=CARTESIAN_POINT('Ctrl Pts',(-8.69512131459534,4.47585912464434,
10.335164750206));
#108579=CARTESIAN_POINT('Ctrl Pts',(-8.78022628121704,4.48629403921791,
10.1822589838222));
#108580=CARTESIAN_POINT('Ctrl Pts',(-8.85218456131881,4.49369470354615,
10.0839894264824));
#108581=CARTESIAN_POINT('Ctrl Pts',(-8.95939012754774,4.50265881845623,
9.97034933335254));
#108582=CARTESIAN_POINT('Ctrl Pts',(-8.98423156756091,4.50462588743857,
9.94583484148541));
#108583=CARTESIAN_POINT('Ctrl Pts',(-9.01786948140973,4.50715121315438,
9.91493400650963));
#108584=CARTESIAN_POINT('Ctrl Pts',(-9.02589244845073,4.50774380653366,
9.90772574300453));
#108585=CARTESIAN_POINT('Ctrl Pts',(-9.03898964353153,4.50869581524709,
9.89621761201574));
#108586=CARTESIAN_POINT('Ctrl Pts',(-9.04401468049101,4.50905749535994,
9.89186258245043));
#108587=CARTESIAN_POINT('Ctrl Pts',(-9.05369392921946,4.50974741740859,
9.88358874728664));
#108588=CARTESIAN_POINT('Ctrl Pts',(-9.05834322823138,4.51007587987322,
9.87966442951265));
#108589=CARTESIAN_POINT('Ctrl Pts',(-9.06910340430252,4.51082941860507,
9.87069642864418));
#108590=CARTESIAN_POINT('Ctrl Pts',(-9.07523106938769,4.51125367234545,
9.86567312626953));
#108591=CARTESIAN_POINT('Ctrl Pts',(-9.09460976853472,4.51258043315257,
9.85004837179759));
#108592=CARTESIAN_POINT('Ctrl Pts',(-9.10800482151908,4.51347583936298,
9.83962727915443));
#108593=CARTESIAN_POINT('Ctrl Pts',(-9.17604020212013,4.51792154576474,
9.78857154048586));
#108594=CARTESIAN_POINT('Ctrl Pts',(-9.23329027237463,4.52133336940978,
9.75155049149914));
#108595=CARTESIAN_POINT('Ctrl Pts',(-9.37140400765338,4.52908766400374,
9.67533560828199));
#108596=CARTESIAN_POINT('Ctrl Pts',(-9.45370185317432,4.53336269262486,
9.63932898951885));
#108597=CARTESIAN_POINT('Ctrl Pts',(-9.57831253845299,4.53993716880449,
9.5979487231896));
#108598=CARTESIAN_POINT('Ctrl Pts',(-9.6183924081122,4.54206851476162,9.58651382446483));
#108599=CARTESIAN_POINT('Ctrl Pts',(-9.66567293564811,4.54465834111858,
9.5751820656132));
#108600=CARTESIAN_POINT('Ctrl Pts',(-9.67245545022669,4.54503165386277,
9.57360759387172));
#108601=CARTESIAN_POINT('Ctrl Pts',(-9.68346842367236,4.54564109254178,
9.57113376597176));
#108602=CARTESIAN_POINT('Ctrl Pts',(-9.68769216435107,4.54587560621555,
9.5702046410822));
#108603=CARTESIAN_POINT('Ctrl Pts',(-9.69522856534511,4.54629553421421,
9.56858179505312));
#108604=CARTESIAN_POINT('Ctrl Pts',(-9.69853958525993,4.5464805387279,9.56788082797028));
#108605=CARTESIAN_POINT('Ctrl Pts',(-9.70574813404548,4.54688446053319,
9.56638083234857));
#108606=CARTESIAN_POINT('Ctrl Pts',(-9.70964644350608,4.54710361226988,
9.56558622080727));
#108607=CARTESIAN_POINT('Ctrl Pts',(-9.7206908268142,4.5477264225081,9.56338185666804));
#108608=CARTESIAN_POINT('Ctrl Pts',(-9.72784415191331,4.54813208929254,
9.56200956405307));
#108609=CARTESIAN_POINT('Ctrl Pts',(-9.7744704762348,4.55078976391258,9.55342514274144));
#108610=CARTESIAN_POINT('Ctrl Pts',(-9.81421268169529,4.55311748327766,
9.54778620047079));
#108611=CARTESIAN_POINT('Ctrl Pts',(-9.99026490805148,4.56356191432461,
9.53015123061777));
#108612=CARTESIAN_POINT('Ctrl Pts',(-10.12766917171,4.57198130819257,9.53567044634369));
#108613=CARTESIAN_POINT('Ctrl Pts',(-10.2957513812052,4.58177402193593,
9.56629179590992));
#108614=CARTESIAN_POINT('Ctrl Pts',(-10.3289777944741,4.58368954345081,
9.57354916964442));
#108615=CARTESIAN_POINT('Ctrl Pts',(-10.3722756687432,4.58615952588042,
9.58459997551297));
#108616=CARTESIAN_POINT('Ctrl Pts',(-10.3825989798174,4.58674648353971,
9.5873555181993));
#108617=CARTESIAN_POINT('Ctrl Pts',(-10.399275183982,4.58769166096452,9.59200302004895));
#108618=CARTESIAN_POINT('Ctrl Pts',(-10.4056468954956,4.58805208702374,
9.59382548512793));
#108619=CARTESIAN_POINT('Ctrl Pts',(-10.4178497370601,4.58874105931627,
9.59740564135852));
#108620=CARTESIAN_POINT('Ctrl Pts',(-10.4236826931945,4.58906981439859,
9.59915657024715));
#108621=CARTESIAN_POINT('Ctrl Pts',(-10.4371230409777,4.58982608123282,
9.60328270304028));
#108622=CARTESIAN_POINT('Ctrl Pts',(-10.4447223382625,4.59025274953959,
9.60568374970993));
#108623=CARTESIAN_POINT('Ctrl Pts',(-10.468678635121,4.59159510281259,9.61346867616115));
#108624=CARTESIAN_POINT('Ctrl Pts',(-10.4849607406408,4.59250344029012,
9.61907933331101));
#108625=CARTESIAN_POINT('Ctrl Pts',(-10.5670173406499,4.59706606919631,
9.64898564152315));
#108626=CARTESIAN_POINT('Ctrl Pts',(-10.6310866773151,4.60057298233745,
9.6776991751375));
#108627=CARTESIAN_POINT('Ctrl Pts',(-10.7843200184807,4.60911327662862,
9.76005778247237));
#108628=CARTESIAN_POINT('Ctrl Pts',(-10.8702841163474,4.61403648628601,
9.81880710697756));
#108629=CARTESIAN_POINT('Ctrl Pts',(-10.9696661131851,4.6207100064064,9.9035074692363));
#108630=CARTESIAN_POINT('Ctrl Pts',(-10.9895502016247,4.62210286893229,
9.92141830819711));
#108631=CARTESIAN_POINT('Ctrl Pts',(-11.0137888928878,4.62389076601552,
9.94448623635616));
#108632=CARTESIAN_POINT('Ctrl Pts',(-11.0186149126043,4.62425138369602,
9.9491427875409));
#108633=CARTESIAN_POINT('Ctrl Pts',(-11.026190752231,4.62482518483648,9.95655381693644));
#108634=CARTESIAN_POINT('Ctrl Pts',(-11.0289619389371,4.62503673070563,
9.95928643497953));
#108635=CARTESIAN_POINT('Ctrl Pts',(-11.0338893927735,4.62541591633545,
9.96418422925124));
#108636=CARTESIAN_POINT('Ctrl Pts',(-11.0360498150024,4.62558322626069,
9.96634514091118));
#108637=CARTESIAN_POINT('Ctrl Pts',(-11.0412093646059,4.62598532784425,
9.97153828552069));
#108638=CARTESIAN_POINT('Ctrl Pts',(-11.044202001053,4.62622061221306,9.97457685848739));
#108639=CARTESIAN_POINT('Ctrl Pts',(-11.0521202808657,4.62684853915885,
9.98268728974459));
#108640=CARTESIAN_POINT('Ctrl Pts',(-11.057022465169,4.62724287806036,9.98778177256818));
#108641=CARTESIAN_POINT('Ctrl Pts',(-11.0970331405352,4.63050618427771,
10.029969557));
#108642=CARTESIAN_POINT('Ctrl Pts',(-11.1302117223681,4.63349764678874,
10.0688387602574));
#108643=CARTESIAN_POINT('Ctrl Pts',(-11.2000881254833,4.64033335998983,
10.1599490224313));
#108644=CARTESIAN_POINT('Ctrl Pts',(-11.2355408333677,4.64419583671292,
10.2130209581761));
#108645=CARTESIAN_POINT('Ctrl Pts',(-11.3125525732878,4.65341506154098,
10.3464056780626));
#108646=CARTESIAN_POINT('Ctrl Pts',(-11.3503623881414,4.65869589762568,
10.4285932223123));
#108647=CARTESIAN_POINT('Ctrl Pts',(-11.3843846726457,4.6643883727835,10.5251758135023));
#108648=CARTESIAN_POINT('Ctrl Pts',(-11.3882667257769,4.66505704095535,
10.5366486857993));
#108649=CARTESIAN_POINT('Ctrl Pts',(-11.3943693745582,4.66614079482623,
10.5554497808251));
#108650=CARTESIAN_POINT('Ctrl Pts',(-11.3966756164454,4.66655863937244,
10.5627494132611));
#108651=CARTESIAN_POINT('Ctrl Pts',(-11.4007022320805,4.6673034707351,10.575851292));
#108652=CARTESIAN_POINT('Ctrl Pts',(-11.4024440793121,4.66763114480397,
10.5816467098561));
#108653=CARTESIAN_POINT('Ctrl Pts',(-11.4060649000288,4.66832420622651,
10.5939705737451));
#108654=CARTESIAN_POINT('Ctrl Pts',(-11.4079344685314,4.66868928470783,
10.6005016489165));
#108655=CARTESIAN_POINT('Ctrl Pts',(-11.4128307836232,4.66966540194885,
10.6180676096622));
#108656=CARTESIAN_POINT('Ctrl Pts',(-11.4157737390103,4.67027375629095,
10.6291254879061));
#108657=CARTESIAN_POINT('Ctrl Pts',(-11.4219591890349,4.67160270119403,
10.653514067914));
#108658=CARTESIAN_POINT('Ctrl Pts',(-11.4251445537587,4.67232148261649,
10.6668582082903));
#108659=CARTESIAN_POINT('Ctrl Pts',(-11.4516421134135,4.67862788827222,
10.7852060970909));
#108660=CARTESIAN_POINT('Ctrl Pts',(-11.4634999999947,4.68383528789043,
10.8924348128952));
#108661=CARTESIAN_POINT('Ctrl Pts',(-11.4635,4.68907309470234,10.9999999999272));
#108662=CARTESIAN_POINT('Origin',(-10.,3.5,11.));
#108663=CARTESIAN_POINT('',(-11.4634997956549,5.26158527077303,10.9993582019504));
#108664=CARTESIAN_POINT('',(-11.4634997007504,5.18934561127431,10.9990641028533));
#108665=CARTESIAN_POINT('',(-11.4635,3.5,11.));
#108666=CARTESIAN_POINT('Ctrl Pts',(-11.4634997029717,5.26158526069413,
10.9990675828864));
#108667=CARTESIAN_POINT('Ctrl Pts',(-11.4634755855665,5.25968973270024,
10.9612134778287));
#108668=CARTESIAN_POINT('Ctrl Pts',(-11.4619828030479,5.25775673629656,
10.9233772234463));
#108669=CARTESIAN_POINT('Ctrl Pts',(-11.4584757697762,5.25538245818981,
10.8786321633612));
#108670=CARTESIAN_POINT('Ctrl Pts',(-11.4578756337479,5.25500801283252,
10.8716241626151));
#108671=CARTESIAN_POINT('Ctrl Pts',(-11.4568187498724,5.25439557666695,
10.8602478310136));
#108672=CARTESIAN_POINT('Ctrl Pts',(-11.4563928059141,5.25415915729695,
10.8558766756243));
#108673=CARTESIAN_POINT('Ctrl Pts',(-11.4556084282691,5.25374115395404,
10.8481859647311));
#108674=CARTESIAN_POINT('Ctrl Pts',(-11.4552582955775,5.25356001426152,
10.8448655729414));
#108675=CARTESIAN_POINT('Ctrl Pts',(-11.4545393244097,5.2531984936987,10.8382640875099));
#108676=CARTESIAN_POINT('Ctrl Pts',(-11.4541707448213,5.25301812810379,
10.8349830420699));
#108677=CARTESIAN_POINT('Ctrl Pts',(-11.4533491675055,5.25262647843925,
10.8278860456633));
#108678=CARTESIAN_POINT('Ctrl Pts',(-11.4528922506856,5.25241498772293,
10.8240706870113));
#108679=CARTESIAN_POINT('Ctrl Pts',(-11.4516020577256,5.25183460390441,
10.8136452198963));
#108680=CARTESIAN_POINT('Ctrl Pts',(-11.450738671356,5.25146410332905,10.8070390141617));
#108681=CARTESIAN_POINT('Ctrl Pts',(-11.4463740830346,5.24967334045397,
10.7753298421207));
#108682=CARTESIAN_POINT('Ctrl Pts',(-11.4422664340985,5.24822337335784,
10.7503161085175));
#108683=CARTESIAN_POINT('Ctrl Pts',(-11.432208964507,5.2451094017854,10.6976615065569));
#108684=CARTESIAN_POINT('Ctrl Pts',(-11.4261033503335,5.24344063725012,
10.6700603364372));
#108685=CARTESIAN_POINT('Ctrl Pts',(-11.4020201583697,5.23756598700445,
10.5744135924869));
#108686=CARTESIAN_POINT('Ctrl Pts',(-11.3799380833125,5.23329688406164,
10.5075008576346));
#108687=CARTESIAN_POINT('Ctrl Pts',(-11.3262091045415,5.22488178422601,
10.3771084134679));
#108688=CARTESIAN_POINT('Ctrl Pts',(-11.2945926722418,5.22074794160887,
10.3138102291102));
#108689=CARTESIAN_POINT('Ctrl Pts',(-11.2475274387565,5.21555244173908,
10.2345121605794));
#108690=CARTESIAN_POINT('Ctrl Pts',(-11.2361240249181,5.21435285740232,
10.2162310245885));
#108691=CARTESIAN_POINT('Ctrl Pts',(-11.2195507175855,5.21268894207907,
10.1909239206587));
#108692=CARTESIAN_POINT('Ctrl Pts',(-11.2147157502599,5.21221245147419,
10.183682840087));
#108693=CARTESIAN_POINT('Ctrl Pts',(-11.2063209485273,5.21140011377993,
10.1713501304063));
#108694=CARTESIAN_POINT('Ctrl Pts',(-11.2027928244289,5.21106309918862,
10.1662372877235));
#108695=CARTESIAN_POINT('Ctrl Pts',(-11.1960082256191,5.21042325002653,
10.1565379607346));
#108696=CARTESIAN_POINT('Ctrl Pts',(-11.1927576607588,5.2101202016491,10.1519474949386));
#108697=CARTESIAN_POINT('Ctrl Pts',(-11.185112366485,5.20941549545192,10.1412816819709));
#108698=CARTESIAN_POINT('Ctrl Pts',(-11.1806972297308,5.20901461968196,
10.1352211118231));
#108699=CARTESIAN_POINT('Ctrl Pts',(-11.1652488632197,5.2076325935004,10.1143543133129));
#108700=CARTESIAN_POINT('Ctrl Pts',(-11.1539819002871,5.20666040374123,
10.099722815278));
#108701=CARTESIAN_POINT('Ctrl Pts',(-11.0845615281312,5.20087216071541,
10.0130174974246));
#108702=CARTESIAN_POINT('Ctrl Pts',(-11.0199504829938,5.1963264719403,9.94638174895592));
#108703=CARTESIAN_POINT('Ctrl Pts',(-10.8776070953851,5.187219542736,9.82502956587028));
#108704=CARTESIAN_POINT('Ctrl Pts',(-10.7999921545526,5.18267587510986,
9.77087090758914));
#108705=CARTESIAN_POINT('Ctrl Pts',(-10.7091215358131,5.17721887130485,
9.71973592940985));
#108706=CARTESIAN_POINT('Ctrl Pts',(-10.7004813714721,5.17669861591017,
9.71498821730293));
#108707=CARTESIAN_POINT('Ctrl Pts',(-10.6869305407729,5.17587949513585,
9.70771940247305));
#108708=CARTESIAN_POINT('Ctrl Pts',(-10.6820523209375,5.17558398153923,
9.7051380999356));
#108709=CARTESIAN_POINT('Ctrl Pts',(-10.6729084221052,5.17502866328178,
9.70036562752736));
#108710=CARTESIAN_POINT('Ctrl Pts',(-10.6686463321352,5.17476925925277,
9.69816770362909));
#108711=CARTESIAN_POINT('Ctrl Pts',(-10.6613358253865,5.17432322927632,
9.6944431075811));
#108712=CARTESIAN_POINT('Ctrl Pts',(-10.6582926921947,5.17413723934396,
9.6929060460299));
#108713=CARTESIAN_POINT('Ctrl Pts',(-10.6523737345066,5.1737748122666,9.68994234247756));
#108714=CARTESIAN_POINT('Ctrl Pts',(-10.6494985542266,5.17359845765963,
9.68851451279253));
#108715=CARTESIAN_POINT('Ctrl Pts',(-10.6425777975542,5.17317327613372,
9.68510596848749));
#108716=CARTESIAN_POINT('Ctrl Pts',(-10.6385277540514,5.17292389951705,
9.6831344615964));
#108717=CARTESIAN_POINT('Ctrl Pts',(-10.623679497607,5.17200777221127,9.67599113149921));
#108718=CARTESIAN_POINT('Ctrl Pts',(-10.6128273229477,5.17133461093226,
9.670933314999));
#108719=CARTESIAN_POINT('Ctrl Pts',(-10.5279299822661,5.16604763741605,
9.63262648224487));
#108720=CARTESIAN_POINT('Ctrl Pts',(-10.4513021691369,5.16116135257995,
9.60545897853463));
#108721=CARTESIAN_POINT('Ctrl Pts',(-10.2950371137817,5.15143650110048,
9.56429241358354));
#108722=CARTESIAN_POINT('Ctrl Pts',(-10.2156849653794,5.146616058383,9.55024642308321));
#108723=CARTESIAN_POINT('Ctrl Pts',(-10.1084849545359,5.14039966155635,
9.54027280730143));
#108724=CARTESIAN_POINT('Ctrl Pts',(-10.0813289834433,5.13884880970364,
9.53850823091632));
#108725=CARTESIAN_POINT('Ctrl Pts',(-10.0345590566641,5.13621966845268,
9.53677691553001));
#108726=CARTESIAN_POINT('Ctrl Pts',(-10.0149665836054,5.13513084938983,
9.53644536257446));
#108727=CARTESIAN_POINT('Ctrl Pts',(-9.98698501833215,5.13359315332902,
9.53653383584459));
#108728=CARTESIAN_POINT('Ctrl Pts',(-9.97859763327772,5.13313445152896,
9.5366324637465));
#108729=CARTESIAN_POINT('Ctrl Pts',(-9.96405831972226,5.13234304401249,
9.53692846308017));
#108730=CARTESIAN_POINT('Ctrl Pts',(-9.95790599179437,5.13200932014684,
9.53709254475892));
#108731=CARTESIAN_POINT('Ctrl Pts',(-9.94529709641476,5.1313276891745,9.53750843084473));
#108732=CARTESIAN_POINT('Ctrl Pts',(-9.93884078912077,5.13097991180341,
9.53776419471243));
#108733=CARTESIAN_POINT('Ctrl Pts',(-9.92246994645456,5.13010113859548,
9.53852133593707));
#108734=CARTESIAN_POINT('Ctrl Pts',(-9.91255834330463,5.12957194529207,
9.53908085169949));
#108735=CARTESIAN_POINT('Ctrl Pts',(-9.87482127681209,5.12756733489161,
9.54159656254414));
#108736=CARTESIAN_POINT('Ctrl Pts',(-9.8470472076702,5.12611330053042,9.54424731715029));
#108737=CARTESIAN_POINT('Ctrl Pts',(-9.70587784545216,5.11880542912622,
9.56180568138952));
#108738=CARTESIAN_POINT('Ctrl Pts',(-9.59444050458146,5.11334769004883,
9.58917291230778));
#108739=CARTESIAN_POINT('Ctrl Pts',(-9.42362480176881,5.10441388646958,
9.65305945564372));
#108740=CARTESIAN_POINT('Ctrl Pts',(-9.36167182601259,5.101031704483,9.68129142481616));
#108741=CARTESIAN_POINT('Ctrl Pts',(-9.29435299519216,5.09696263609527,
9.71782663053099));
#108742=CARTESIAN_POINT('Ctrl Pts',(-9.28682914321674,5.09650202379302,
9.72199625713897));
#108743=CARTESIAN_POINT('Ctrl Pts',(-9.27564287051461,5.09580778722608,
9.72832509301882));
#108744=CARTESIAN_POINT('Ctrl Pts',(-9.27195225977204,5.09557719671801,
9.73043440220299));
#108745=CARTESIAN_POINT('Ctrl Pts',(-9.26562649824601,5.09517920826371,
9.734086442988));
#108746=CARTESIAN_POINT('Ctrl Pts',(-9.26298691447873,5.09501230575518,
9.73562138364736));
#108747=CARTESIAN_POINT('Ctrl Pts',(-9.25698700810334,5.09463101081404,
9.73913555350665));
#108748=CARTESIAN_POINT('Ctrl Pts',(-9.25362983904458,5.09441629474183,
9.74111992601837));
#108749=CARTESIAN_POINT('Ctrl Pts',(-9.24448934092962,5.09382803741676,
9.74657215320588));
#108750=CARTESIAN_POINT('Ctrl Pts',(-9.23872205751056,5.09345285803131,
9.75006655624689));
#108751=CARTESIAN_POINT('Ctrl Pts',(-9.20979566049898,5.09155163031159,
9.76786754949988));
#108752=CARTESIAN_POINT('Ctrl Pts',(-9.18701607253434,5.08999118940386,
9.7827776626815));
#108753=CARTESIAN_POINT('Ctrl Pts',(-9.14213434512544,5.08680802435196,
9.81397646491837));
#108754=CARTESIAN_POINT('Ctrl Pts',(-9.12004753578345,5.08518550233335,
9.83026975367048));
#108755=CARTESIAN_POINT('Ctrl Pts',(-9.01346194010103,5.07711991938126,
9.91362495883535));
#108756=CARTESIAN_POINT('Ctrl Pts',(-8.93608773617328,5.07054206553634,
9.98927607798419));
#108757=CARTESIAN_POINT('Ctrl Pts',(-8.83758630149709,5.06150619392063,
10.1095561121911));
#108758=CARTESIAN_POINT('Ctrl Pts',(-8.80925235217324,5.05880050826366,
10.1478165229008));
#108759=CARTESIAN_POINT('Ctrl Pts',(-8.77645351344813,5.0555296940229,10.1969444928169));
#108760=CARTESIAN_POINT('Ctrl Pts',(-8.77018908075466,5.05489792044144,
10.2065711967732));
#108761=CARTESIAN_POINT('Ctrl Pts',(-8.76039619594998,5.05389864445903,
10.2220148338608));
#108762=CARTESIAN_POINT('Ctrl Pts',(-8.75679394712738,5.05352845164113,
10.2277842127883));
#108763=CARTESIAN_POINT('Ctrl Pts',(-8.75006465730026,5.05283183558244,
10.2387310140819));
#108764=CARTESIAN_POINT('Ctrl Pts',(-8.74692924692391,5.05250511342552,
10.2439031020124));
#108765=CARTESIAN_POINT('Ctrl Pts',(-8.73990769015482,5.05176846833726,
10.2556493174005));
#108766=CARTESIAN_POINT('Ctrl Pts',(-8.73604074017696,5.05135924068338,
10.2622347524337));
#108767=CARTESIAN_POINT('Ctrl Pts',(-8.72620367741579,5.05030878366628,
10.2792916925588));
#108768=CARTESIAN_POINT('Ctrl Pts',(-8.72031100372346,5.04967029942666,
10.2898073359778));
#108769=CARTESIAN_POINT('Ctrl Pts',(-8.66936308286706,5.04406355405327,
10.3834187975242));
#108770=CARTESIAN_POINT('Ctrl Pts',(-8.63232514855251,5.03939311447577,
10.4706275187085));
#108771=CARTESIAN_POINT('Ctrl Pts',(-8.5836573710158,5.0314876418374,10.6253263373739));
#108772=CARTESIAN_POINT('Ctrl Pts',(-8.5678579871171,5.0282259393576,10.6911710418615));
#108773=CARTESIAN_POINT('Ctrl Pts',(-8.549470926683,5.0226690827907,10.8007754380119));
#108774=CARTESIAN_POINT('Ctrl Pts',(-8.54419044154288,5.02044590578664,
10.843977898029));
#108775=CARTESIAN_POINT('Ctrl Pts',(-8.54027073440169,5.01773083054033,
10.8947487349756));
#108776=CARTESIAN_POINT('Ctrl Pts',(-8.53975564997126,5.01733225976145,
10.9021542477164));
#108777=CARTESIAN_POINT('Ctrl Pts',(-8.53904928581138,5.01671387287829,
10.9135631910024));
#108778=CARTESIAN_POINT('Ctrl Pts',(-8.53881806813722,5.01649619147403,
10.9175641312434));
#108779=CARTESIAN_POINT('Ctrl Pts',(-8.5384221115899,5.01609320076966,10.9249416591144));
#108780=CARTESIAN_POINT('Ctrl Pts',(-8.53825263613581,5.01590815301889,
10.928317910064));
#108781=CARTESIAN_POINT('Ctrl Pts',(-8.53789495387849,5.0154871710431,10.9359732125391));
#108782=CARTESIAN_POINT('Ctrl Pts',(-8.53771383417716,5.01525085628491,
10.9402525004867));
#108783=CARTESIAN_POINT('Ctrl Pts',(-8.53729274356122,5.0146352972543,10.9513549110742));
#108784=CARTESIAN_POINT('Ctrl Pts',(-8.53708173196008,5.01425454615045,
10.9581789513449));
#108785=CARTESIAN_POINT('Ctrl Pts',(-8.5359916359523,5.01169682256599,11.0037528201883));
#108786=CARTESIAN_POINT('Ctrl Pts',(-8.53660458914721,5.00944947749499,
11.0425201051546));
#108787=CARTESIAN_POINT('Ctrl Pts',(-8.54099486081677,5.00478280293501,
11.1215122312014));
#108788=CARTESIAN_POINT('Ctrl Pts',(-8.54490058019728,5.00236223813583,
11.1616993806745));
#108789=CARTESIAN_POINT('Ctrl Pts',(-8.56696475193314,4.99273178500378,
11.3202876460314));
#108790=CARTESIAN_POINT('Ctrl Pts',(-8.59796787395804,4.9855527947838,11.4364512222269));
#108791=CARTESIAN_POINT('Ctrl Pts',(-8.64934541078253,4.97786394070211,
11.5638009987782));
#108792=CARTESIAN_POINT('Ctrl Pts',(-8.65619384643042,4.97689220511196,
11.5799348623083));
#108793=CARTESIAN_POINT('Ctrl Pts',(-8.66659808387112,4.97548965641671,
11.6032710555377));
#108794=CARTESIAN_POINT('Ctrl Pts',(-8.66992579261374,4.97505123054245,
11.6105728808316));
#108795=CARTESIAN_POINT('Ctrl Pts',(-8.67588715520685,4.97428329456737,
11.6233735560062));
#108796=CARTESIAN_POINT('Ctrl Pts',(-8.67849541015373,4.97395293199002,
11.6288839611913));
#108797=CARTESIAN_POINT('Ctrl Pts',(-8.68399875609455,4.97326738486312,
11.6403253320366));
#108798=CARTESIAN_POINT('Ctrl Pts',(-8.6868996909777,4.97291240976163,11.6462533444407));
#108799=CARTESIAN_POINT('Ctrl Pts',(-8.69454824430736,4.97199277000197,
11.6616188974231));
#108800=CARTESIAN_POINT('Ctrl Pts',(-8.6993581710419,4.97143026259548,11.6710251056552));
#108801=CARTESIAN_POINT('Ctrl Pts',(-8.71959996188531,4.96912600634019,
11.7095740906443));
#108802=CARTESIAN_POINT('Ctrl Pts',(-8.73591332439671,4.96741500709989,
11.7382443600286));
#108803=CARTESIAN_POINT('Ctrl Pts',(-8.75592542847624,4.96546474548255,
11.7708035772006));
#108804=CARTESIAN_POINT('Ctrl Pts',(-8.75869256791548,4.96519812670549,
11.7752519293319));
#108805=CARTESIAN_POINT('Ctrl Pts',(-8.77605019957874,4.96354421552162,
11.8028242212755));
#108806=CARTESIAN_POINT('Ctrl Pts',(-8.79126281992638,4.96217528399169,
11.8255509437413));
#108807=CARTESIAN_POINT('Ctrl Pts',(-8.86401032068164,4.95594935304557,
11.9279055733614));
#108808=CARTESIAN_POINT('Ctrl Pts',(-8.92883005670084,4.9512839532081,12.0020353917433));
#108809=CARTESIAN_POINT('Ctrl Pts',(-9.02371395851486,4.94481269803343,
12.0907338686076));
#108810=CARTESIAN_POINT('Ctrl Pts',(-9.04753887886299,4.9432114755027,12.1115990312943));
#108811=CARTESIAN_POINT('Ctrl Pts',(-9.08632673136406,4.94060796013744,
12.1434053114422));
#108812=CARTESIAN_POINT('Ctrl Pts',(-9.10085367148046,4.9396335569343,12.1548637865274));
#108813=CARTESIAN_POINT('Ctrl Pts',(-9.12016310113909,4.93833359319286,
12.1695093753298));
#108814=CARTESIAN_POINT('Ctrl Pts',(-9.12475323281289,4.9380242274341,12.1729485248401));
#108815=CARTESIAN_POINT('Ctrl Pts',(-9.13228720623301,4.93751567952162,
12.1785244965391));
#108816=CARTESIAN_POINT('Ctrl Pts',(-9.13521905212088,4.93731758864125,
12.1806775143976));
#108817=CARTESIAN_POINT('Ctrl Pts',(-9.14094660622165,4.93693017280231,
12.1848507982467));
#108818=CARTESIAN_POINT('Ctrl Pts',(-9.14374147298838,4.93674092313489,
12.1868721420564));
#108819=CARTESIAN_POINT('Ctrl Pts',(-9.15061203303867,4.9362752494116,12.1918042690779));
#108820=CARTESIAN_POINT('Ctrl Pts',(-9.15469555582124,4.93599809475877,
12.1947040342125));
#108821=CARTESIAN_POINT('Ctrl Pts',(-9.16863735566406,4.93505078028545,
12.2044970345653));
#108822=CARTESIAN_POINT('Ctrl Pts',(-9.17856544750274,4.93437439213182,
12.2112894822088));
#108823=CARTESIAN_POINT('Ctrl Pts',(-9.25117887590748,4.92942100961916,
12.2596657529805));
#108824=CARTESIAN_POINT('Ctrl Pts',(-9.31689934892642,4.92490967114821,
12.2964808148705));
#108825=CARTESIAN_POINT('Ctrl Pts',(-9.4438347339112,4.91649359397749,12.3552469547261));
#108826=CARTESIAN_POINT('Ctrl Pts',(-9.50425752596735,4.91260104888622,
12.3784971344845));
#108827=CARTESIAN_POINT('Ctrl Pts',(-9.60421650183225,4.90644809066128,
12.4095343557478));
#108828=CARTESIAN_POINT('Ctrl Pts',(-9.64288269011412,4.9041331906841,12.4198236844504));
#108829=CARTESIAN_POINT('Ctrl Pts',(-9.70739660982814,4.90038528060468,
12.4341884506568));
#108830=CARTESIAN_POINT('Ctrl Pts',(-9.73301708663121,4.89892589713732,
12.4391780647415));
#108831=CARTESIAN_POINT('Ctrl Pts',(-9.76800160948269,4.8969714786752,12.445024850324));
#108832=CARTESIAN_POINT('Ctrl Pts',(-9.77725948387391,4.89645789234265,
12.4464808119842));
#108833=CARTESIAN_POINT('Ctrl Pts',(-9.79280679586059,4.89560130172806,
12.4487730911937));
#108834=CARTESIAN_POINT('Ctrl Pts',(-9.79908875064772,4.89525680376032,
12.449657602763));
#108835=CARTESIAN_POINT('Ctrl Pts',(-9.81147995074967,4.89458038906313,
12.4513202148215));
#108836=CARTESIAN_POINT('Ctrl Pts',(-9.81758874477589,4.89424840603649,
12.4521006543883));
#108837=CARTESIAN_POINT('Ctrl Pts',(-9.83103491461209,4.89352086359869,
12.4537323027876));
#108838=CARTESIAN_POINT('Ctrl Pts',(-9.83837420046035,4.89312583683215,
12.4545665718233));
#108839=CARTESIAN_POINT('Ctrl Pts',(-9.86415595162818,4.89174524857921,
12.4572996823306));
#108840=CARTESIAN_POINT('Ctrl Pts',(-9.88262830129421,4.89076879311007,
12.4589036618054));
#108841=CARTESIAN_POINT('Ctrl Pts',(-10.0007090555364,4.88459951236762,
12.4668994038411));
#108842=CARTESIAN_POINT('Ctrl Pts',(-10.1007213423544,4.87972693026157,
12.4634384122665));
#108843=CARTESIAN_POINT('Ctrl Pts',(-10.2678917957476,4.87151565336667,
12.4404224677659));
#108844=CARTESIAN_POINT('Ctrl Pts',(-10.3354189620596,4.8681719934354,12.4262102986747));
#108845=CARTESIAN_POINT('Ctrl Pts',(-10.4210140868126,4.86364294751704,
12.40177861866));
#108846=CARTESIAN_POINT('Ctrl Pts',(-10.4402232318274,4.86260677039464,
12.395865178525));
#108847=CARTESIAN_POINT('Ctrl Pts',(-10.4719723016849,4.86085200656935,
12.3853708618621));
#108848=CARTESIAN_POINT('Ctrl Pts',(-10.4845826095537,4.86014378911869,
12.3810104808462));
#108849=CARTESIAN_POINT('Ctrl Pts',(-10.5018990546098,4.85915344031472,
12.3747564467042));
#108850=CARTESIAN_POINT('Ctrl Pts',(-10.5066579673278,4.85887939794238,
12.373009705496));
#108851=CARTESIAN_POINT('Ctrl Pts',(-10.5146829359345,4.85841395632396,
12.3700167682107));
#108852=CARTESIAN_POINT('Ctrl Pts',(-10.5179538264672,4.85822330989188,
12.3687835121437));
#108853=CARTESIAN_POINT('Ctrl Pts',(-10.5242024590992,4.85785725383048,
12.3664019237951));
#108854=CARTESIAN_POINT('Ctrl Pts',(-10.5271809090208,4.85768196700306,
12.365255552722));
#108855=CARTESIAN_POINT('Ctrl Pts',(-10.5342879153417,4.8572618262478,12.3624934235686));
#108856=CARTESIAN_POINT('Ctrl Pts',(-10.5384129012509,4.85701645025387,
12.3608686389492));
#108857=CARTESIAN_POINT('Ctrl Pts',(-10.5531646978716,4.85613364067106,
12.3549805063869));
#108858=CARTESIAN_POINT('Ctrl Pts',(-10.5637485015492,4.85549038716004,
12.3506113305621));
#108859=CARTESIAN_POINT('Ctrl Pts',(-10.6615021365235,4.84946440876787,
12.3089077829852));
#108860=CARTESIAN_POINT('Ctrl Pts',(-10.7448953321199,4.84370913233129,
12.2633104177998));
#108861=CARTESIAN_POINT('Ctrl Pts',(-10.9090151852976,4.83177891169248,
12.1516404715025));
#108862=CARTESIAN_POINT('Ctrl Pts',(-10.9883152594438,4.82565873900936,
12.0843541723756));
#108863=CARTESIAN_POINT('Ctrl Pts',(-11.0693445868901,4.8191227575577,11.9992618241951));
#108864=CARTESIAN_POINT('Ctrl Pts',(-11.0787037384997,4.81836239790206,
11.9891513036427));
#108865=CARTESIAN_POINT('Ctrl Pts',(-11.0927965728734,4.81720872523634,
11.9734891247832));
#108866=CARTESIAN_POINT('Ctrl Pts',(-11.0976336567299,4.81681112244816,
11.9680319127218));
#108867=CARTESIAN_POINT('Ctrl Pts',(-11.1060064907584,4.81611994398244,
11.9584422081271));
#108868=CARTESIAN_POINT('Ctrl Pts',(-11.1095603410807,4.81582562811086,
11.9543257695994));
#108869=CARTESIAN_POINT('Ctrl Pts',(-11.1175313959552,4.81516330106177,
11.9449881477051));
#108870=CARTESIAN_POINT('Ctrl Pts',(-11.1219351306993,4.81479584016562,
11.9397555985006));
#108871=CARTESIAN_POINT('Ctrl Pts',(-11.1337447976585,4.81380605208387,
11.9255219314478));
#108872=CARTESIAN_POINT('Ctrl Pts',(-11.1410802224491,4.81318654519539,
11.9164627914667));
#108873=CARTESIAN_POINT('Ctrl Pts',(-11.1753981465701,4.81026415733355,
11.8730297758536));
#108874=CARTESIAN_POINT('Ctrl Pts',(-11.2009416210287,4.80801749314418,
11.837544909161));
#108875=CARTESIAN_POINT('Ctrl Pts',(-11.2992659116678,4.79896335548206,
11.6871848714425));
#108876=CARTESIAN_POINT('Ctrl Pts',(-11.3574454588929,4.79264724596364,
11.5636049577396));
#108877=CARTESIAN_POINT('Ctrl Pts',(-11.4037531167807,4.78470173335965,
11.4143931677321));
#108878=CARTESIAN_POINT('Ctrl Pts',(-11.4093668779,4.78365530825791,11.3948790263124));
#108879=CARTESIAN_POINT('Ctrl Pts',(-11.4180199275808,4.7818847734404,11.3622602506343));
#108880=CARTESIAN_POINT('Ctrl Pts',(-11.4212878688681,4.78117127378845,
11.3492188034843));
#108881=CARTESIAN_POINT('Ctrl Pts',(-11.4255433633915,4.78017470792175,
11.3311860824075));
#108882=CARTESIAN_POINT('Ctrl Pts',(-11.4266853493238,4.77989986441022,
11.3262315352193));
#108883=CARTESIAN_POINT('Ctrl Pts',(-11.4285695120784,4.77943345855209,
11.317857892444));
#108884=CARTESIAN_POINT('Ctrl Pts',(-11.4293252997111,4.77924265632408,
11.3144418514934));
#108885=CARTESIAN_POINT('Ctrl Pts',(-11.4307464106937,4.77887662150018,
11.3079076545134));
#108886=CARTESIAN_POINT('Ctrl Pts',(-11.4314138045369,4.77870151384946,
11.3047899854013));
#108887=CARTESIAN_POINT('Ctrl Pts',(-11.4329823902885,4.77828222544987,
11.297343687328));
#108888=CARTESIAN_POINT('Ctrl Pts',(-11.4338741585712,4.7780375272814,11.293013132166));
#108889=CARTESIAN_POINT('Ctrl Pts',(-11.4369896913701,4.77715970790461,
11.2775287902159));
#108890=CARTESIAN_POINT('Ctrl Pts',(-11.4391029861991,4.77652085037875,
11.2663534897693));
#108891=CARTESIAN_POINT('Ctrl Pts',(-11.4560043752805,4.77102517608869,
11.1708964297008));
#108892=CARTESIAN_POINT('Ctrl Pts',(-11.463499998108,4.76586314678454,11.0855178363557));
#108893=CARTESIAN_POINT('Ctrl Pts',(-11.4635,4.76071734372175,11.0000000323785));
#108894=CARTESIAN_POINT('',(-11.4635901039152,4.6891878772753,11.0012825185114));
#108895=CARTESIAN_POINT('Ctrl Pts',(-11.4635,4.68907309470234,10.9999999999272));
#108896=CARTESIAN_POINT('Ctrl Pts',(-11.4635,4.68909395150544,11.0004283215526));
#108897=CARTESIAN_POINT('Ctrl Pts',(-11.4634998119651,4.68911480929044,
11.0008566484887));
#108898=CARTESIAN_POINT('Ctrl Pts',(-11.4634994358813,4.68913566809525,
11.0012849806131));
#108899=CARTESIAN_POINT('Ctrl Pts',(-11.4635901039152,4.6891878772753,11.0012825185114));
#108900=CARTESIAN_POINT('Ctrl Pts',(-11.4636777388583,4.69192656168224,
11.0559186640038));
#108901=CARTESIAN_POINT('Ctrl Pts',(-11.4607004171936,4.69466807467494,
11.1104470385295));
#108902=CARTESIAN_POINT('Ctrl Pts',(-11.4546742551396,4.6974780640643,11.1645633069226));
#108903=CARTESIAN_POINT('Ctrl Pts',(-11.4521770961465,4.69864248516869,
11.1869883471191));
#108904=CARTESIAN_POINT('Ctrl Pts',(-11.4491562647747,4.69981866476636,
11.2093432254121));
#108905=CARTESIAN_POINT('Ctrl Pts',(-11.4456120588868,4.70101127414283,
11.2316087754002));
#108906=CARTESIAN_POINT('Ctrl Pts',(-11.4419641095429,4.70223879272668,
11.2545260666185));
#108907=CARTESIAN_POINT('Ctrl Pts',(-11.4377624835256,4.70348395493515,
11.2773470170919));
#108908=CARTESIAN_POINT('Ctrl Pts',(-11.4330092972674,4.70475224144607,
11.3000478316342));
#108909=CARTESIAN_POINT('Ctrl Pts',(-11.4330055055567,4.7047532531833,11.3000659405228));
#108910=CARTESIAN_POINT('Ctrl Pts',(-11.433001713495,4.70475426493525,11.3000840493352));
#108911=CARTESIAN_POINT('Ctrl Pts',(-11.4329979210824,4.70475527670191,
11.3001021580711));
#108912=CARTESIAN_POINT('Ctrl Pts',(-11.4226630846898,4.70751247744201,
11.3494509081483));
#108913=CARTESIAN_POINT('Ctrl Pts',(-11.4096940881357,4.71038302461506,
11.3983377215902));
#108914=CARTESIAN_POINT('Ctrl Pts',(-11.3941777570286,4.71330675141998,
11.4464751367945));
#108915=CARTESIAN_POINT('Ctrl Pts',(-11.3927529584519,4.71357522479565,
11.4508953905386));
#108916=CARTESIAN_POINT('Ctrl Pts',(-11.3913067089278,4.71384414658019,
11.4553093023841));
#108917=CARTESIAN_POINT('Ctrl Pts',(-11.3898390930296,4.71411347018816,
11.4597166362923));
#108918=CARTESIAN_POINT('Ctrl Pts',(-11.3724198559226,4.71731009117817,
11.5120275947979));
#108919=CARTESIAN_POINT('Ctrl Pts',(-11.3519864902487,4.72056269471266,
11.5634159156947));
#108920=CARTESIAN_POINT('Ctrl Pts',(-11.3286919207662,4.72380664698362,
11.6135342257182));
#108921=CARTESIAN_POINT('Ctrl Pts',(-11.305420384918,4.7270473916396,11.6636029788341));
#108922=CARTESIAN_POINT('Ctrl Pts',(-11.2792935959025,4.73027916828496,
11.7124044339615));
#108923=CARTESIAN_POINT('Ctrl Pts',(-11.2504954040596,4.7334578634879,11.75961562067));
#108924=CARTESIAN_POINT('Ctrl Pts',(-11.2217143150982,4.73663467090403,
11.8067987692526));
#108925=CARTESIAN_POINT('Ctrl Pts',(-11.1902650975266,4.73975832445199,
11.8523936230707));
#108926=CARTESIAN_POINT('Ctrl Pts',(-11.156359763586,4.7428085445757,11.8960989536284));
#108927=CARTESIAN_POINT('Ctrl Pts',(-11.1224611767944,4.74585815770673,
11.9397955868414));
#108928=CARTESIAN_POINT('Ctrl Pts',(-11.0861074410123,4.74883437026357,
11.9816034092265));
#108929=CARTESIAN_POINT('Ctrl Pts',(-11.0475382901878,4.75174162379175,
12.0212422055306));
#108930=CARTESIAN_POINT('Ctrl Pts',(-11.0089336898426,4.75465154942293,
12.0609174344837));
#108931=CARTESIAN_POINT('Ctrl Pts',(-10.9681095032209,4.75749251768213,
12.0984194850311));
#108932=CARTESIAN_POINT('Ctrl Pts',(-10.9253348492182,4.76029276749457,
12.1334897620612));
#108933=CARTESIAN_POINT('Ctrl Pts',(-10.8825407135108,4.76309429268005,
12.1685760118397));
#108934=CARTESIAN_POINT('Ctrl Pts',(-10.8377941693208,4.76585535578055,
12.2012279601467));
#108935=CARTESIAN_POINT('Ctrl Pts',(-10.7913954152356,4.76862491232382,
12.2312125760717));
#108936=CARTESIAN_POINT('Ctrl Pts',(-10.7449091644897,4.77139969157089,
12.2612537356219));
#108937=CARTESIAN_POINT('Ctrl Pts',(-10.6967642821325,4.77418351636668,
12.2886169451701));
#108938=CARTESIAN_POINT('Ctrl Pts',(-10.6472962190233,4.77704033974134,
12.3131002464411));
#108939=CARTESIAN_POINT('Ctrl Pts',(-10.6095693929895,4.77921909653291,
12.3317724399682));
#108940=CARTESIAN_POINT('Ctrl Pts',(-10.5710736568645,4.78144073976509,
12.3487701007965));
#108941=CARTESIAN_POINT('Ctrl Pts',(-10.5319715987086,4.7837358552565,12.3640199685171));
#108942=CARTESIAN_POINT('Ctrl Pts',(-10.5319543624768,4.78373686694603,
12.3640266906761));
#108943=CARTESIAN_POINT('Ctrl Pts',(-10.531937126127,4.78373787864983,12.364033412496));
#108944=CARTESIAN_POINT('Ctrl Pts',(-10.5319198896591,4.78373889036791,
12.3640401339767));
#108945=CARTESIAN_POINT('Ctrl Pts',(-10.4849457905787,4.78649609942676,
12.3823580109954));
#108946=CARTESIAN_POINT('Ctrl Pts',(-10.4369187753071,4.78936665361016,
12.398217521904));
#108947=CARTESIAN_POINT('Ctrl Pts',(-10.3881270251176,4.79229038588681,
12.4115342578971));
#108948=CARTESIAN_POINT('Ctrl Pts',(-10.3836467989776,4.79255885302975,
12.4127570463493));
#108949=CARTESIAN_POINT('Ctrl Pts',(-10.3791601595532,4.79282776854608,
12.4139584062387));
#108950=CARTESIAN_POINT('Ctrl Pts',(-10.3746673507138,4.7930970858537,12.4151382793806));
#108951=CARTESIAN_POINT('Ctrl Pts',(-10.3213406599093,4.79629370545296,
12.4291425988338));
#108952=CARTESIAN_POINT('Ctrl Pts',(-10.2671391755717,4.79954630567773,
12.4401185686787));
#108953=CARTESIAN_POINT('Ctrl Pts',(-10.2124373755102,4.80279025309127,
12.4480043869183));
#108954=CARTESIAN_POINT('Ctrl Pts',(-10.1577896650668,4.80603099286124,
12.4558824075919));
#108955=CARTESIAN_POINT('Ctrl Pts',(-10.1026426195312,4.80926276308256,
12.4606767426257));
#108956=CARTESIAN_POINT('Ctrl Pts',(-10.0473671845871,4.81244145074323,
12.4623648252431));
#108957=CARTESIAN_POINT('Ctrl Pts',(-9.99212457740991,4.81561825059936,
12.4640519053179));
#108958=CARTESIAN_POINT('Ctrl Pts',(-9.93675371764679,4.81874189547464,
12.4626365536171));
#108959=CARTESIAN_POINT('Ctrl Pts',(-9.88162273653403,4.82179210620845,
12.4581316699812));
#108960=CARTESIAN_POINT('Ctrl Pts',(-9.8265027266688,4.82484170994024,12.4536276828321));
#108961=CARTESIAN_POINT('Ctrl Pts',(-9.77162252759448,4.8278179123832,12.4460353632545));
#108962=CARTESIAN_POINT('Ctrl Pts',(-9.71734782564662,4.83072515541604,
12.4354023108552));
#108963=CARTESIAN_POINT('Ctrl Pts',(-9.66302323850774,4.83363507056626,
12.4247594853604));
#108964=CARTESIAN_POINT('Ctrl Pts',(-9.60930534586025,4.83647602796213,
12.4110701644286));
#108965=CARTESIAN_POINT('Ctrl Pts',(-9.55655778992746,4.83927626678178,
12.3944183719835));
#108966=CARTESIAN_POINT('Ctrl Pts',(-9.50378621001815,4.84207778097562,
12.3777589954473));
#108967=CARTESIAN_POINT('Ctrl Pts',(-9.45198602283035,4.84483883295526,
12.3581341401879));
#108968=CARTESIAN_POINT('Ctrl Pts',(-9.40151644989201,4.84760837841011,
12.335667829337));
#108969=CARTESIAN_POINT('Ctrl Pts',(-9.35095170251484,4.8503831466144,12.3131591519986));
#108970=CARTESIAN_POINT('Ctrl Pts',(-9.30172295088496,4.85316696040023,
12.2877978380731));
#108971=CARTESIAN_POINT('Ctrl Pts',(-9.25418266356744,4.85602377286918,
12.2597544147948));
#108972=CARTESIAN_POINT('Ctrl Pts',(-9.21792543860034,4.85820255844705,
12.2383667294437));
#108973=CARTESIAN_POINT('Ctrl Pts',(-9.1826502608637,4.86042423198564,12.2154198526192));
#108974=CARTESIAN_POINT('Ctrl Pts',(-9.14850735228077,4.86271938086069,
12.1910099010785));
#108975=CARTESIAN_POINT('Ctrl Pts',(-9.14849230179559,4.86272039258188,
12.1909991409638));
#108976=CARTESIAN_POINT('Ctrl Pts',(-9.14847725152997,4.86272140431735,
12.1909883805648));
#108977=CARTESIAN_POINT('Ctrl Pts',(-9.14846220148391,4.8627224160671,12.1909776198815));
#108978=CARTESIAN_POINT('Ctrl Pts',(-9.10744809109168,4.86547961798553,
12.1616528025972));
#108979=CARTESIAN_POINT('Ctrl Pts',(-9.06791715830832,4.8683501659533,12.1301026005958));
#108980=CARTESIAN_POINT('Ctrl Pts',(-9.03009759816841,4.87127389294877,
12.0965222052036));
#108981=CARTESIAN_POINT('Ctrl Pts',(-9.02662483274124,4.87154236296774,
12.0934386993216));
#108982=CARTESIAN_POINT('Ctrl Pts',(-9.02316650693239,4.87181128137922,
12.0903381103193));
#108983=CARTESIAN_POINT('Ctrl Pts',(-9.01972280276393,4.87208060159934,
12.0872206106208));
#108984=CARTESIAN_POINT('Ctrl Pts',(-8.97884876513542,4.8752772190418,12.0502183613705));
#108985=CARTESIAN_POINT('Ctrl Pts',(-8.94003257657952,4.87852981825204,
12.010828350913));
#108986=CARTESIAN_POINT('Ctrl Pts',(-8.90353066838096,4.88177376548853,
11.9693303933416));
#108987=CARTESIAN_POINT('Ctrl Pts',(-8.86706485408297,4.88501450503768,
11.9278734698756));
#108988=CARTESIAN_POINT('Ctrl Pts',(-8.83290844136806,4.8882462758721,11.884312954634));
#108989=CARTESIAN_POINT('Ctrl Pts',(-8.80128307475971,4.89142496464193,
11.8389471485505));
#108990=CARTESIAN_POINT('Ctrl Pts',(-8.76967649066713,4.89460176556735,
11.7936082855212));
#108991=CARTESIAN_POINT('Ctrl Pts',(-8.74059782794154,4.89772541200718,
11.7464663345094));
#108992=CARTESIAN_POINT('Ctrl Pts',(-8.71423749251512,4.90077562445434,
11.6978366244731));
#108993=CARTESIAN_POINT('Ctrl Pts',(-8.68788240317584,4.90382522986521,
11.6492165924508));
#108994=CARTESIAN_POINT('Ctrl Pts',(-8.66424459950063,4.9068014341363,11.5991094002226));
#108995=CARTESIAN_POINT('Ctrl Pts',(-8.64348409300462,4.90970867880946,
11.5478472950859));
#108996=CARTESIAN_POINT('Ctrl Pts',(-8.62270450527309,4.91261859556678,
11.4965380743212));
#108997=CARTESIAN_POINT('Ctrl Pts',(-8.60480769478582,4.91545955438148,
11.444071793711));
#108998=CARTESIAN_POINT('Ctrl Pts',(-8.5899220535533,4.91825979412484,11.3907988970815));
#108999=CARTESIAN_POINT('Ctrl Pts',(-8.57502963273937,4.92106130922161,
11.3375017376113));
#109000=CARTESIAN_POINT('Ctrl Pts',(-8.56315147659081,4.92382236160641,
11.2833972028079));
#109001=CARTESIAN_POINT('Ctrl Pts',(-8.55438006501671,4.9265919067251,11.2288538967451));
#109002=CARTESIAN_POINT('Ctrl Pts',(-8.54559211254022,4.92936667458076,
11.1742077343183));
#109003=CARTESIAN_POINT('Ctrl Pts',(-8.53992320908011,4.93215048726976,
11.1191211960121));
#109004=CARTESIAN_POINT('Ctrl Pts',(-8.53742320045547,4.93500729776356,
11.0639826484335));
#109005=CARTESIAN_POINT('Ctrl Pts',(-8.53551652341311,4.93718609624019,
11.0219302323813));
#109006=CARTESIAN_POINT('Ctrl Pts',(-8.53545231415658,4.93940778273591,
10.9798479931522));
#109007=CARTESIAN_POINT('Ctrl Pts',(-8.53723218952537,4.94170294524313,
10.9379142664522));
#109008=CARTESIAN_POINT('Ctrl Pts',(-8.53723297410106,4.94170395695931,
10.9378957819092));
#109009=CARTESIAN_POINT('Ctrl Pts',(-8.53723375903481,4.94170496868977,
10.9378772973948));
#109010=CARTESIAN_POINT('Ctrl Pts',(-8.53723454432658,4.94170598043451,
10.9378588129088));
#109011=CARTESIAN_POINT('Ctrl Pts',(-8.53937461911631,4.94446318416237,
10.8874849473202));
#109012=CARTESIAN_POINT('Ctrl Pts',(-8.54418892528037,4.94733373376795,
10.8371367959789));
#109013=CARTESIAN_POINT('Ctrl Pts',(-8.55163873023419,4.95025746228649,
10.7871121384603));
#109014=CARTESIAN_POINT('Ctrl Pts',(-8.55232280526123,4.95052593235755,
10.7825186465291));
#109015=CARTESIAN_POINT('Ctrl Pts',(-8.5530290781923,4.95079485081986,10.7779279094913));
#109016=CARTESIAN_POINT('Ctrl Pts',(-8.55375750412409,4.95106417108964,
10.7733401740161));
#109017=CARTESIAN_POINT('Ctrl Pts',(-8.56240334503963,4.95426079013659,
10.7188873746995));
#109018=CARTESIAN_POINT('Ctrl Pts',(-8.57417349074655,4.95751339082138,
10.6648527792948));
#109019=CARTESIAN_POINT('Ctrl Pts',(-8.58897377717765,4.96075733947533,
10.6116040649015));
#109020=CARTESIAN_POINT('Ctrl Pts',(-8.60375942891101,4.9639980804746,10.5584080034649));
#109021=CARTESIAN_POINT('Ctrl Pts',(-8.62156890761889,4.96722985270143,
10.5059961179758));
#109022=CARTESIAN_POINT('Ctrl Pts',(-8.64227355478145,4.97040854288448,
10.4547170588198));
#109023=CARTESIAN_POINT('Ctrl Pts',(-8.6629659055008,4.97358534525061,10.4034684541812));
#109024=CARTESIAN_POINT('Ctrl Pts',(-8.686549872134,4.9767089931509,10.3533512631977));
#109025=CARTESIAN_POINT('Ctrl Pts',(-8.71286546266174,4.97975920716823,
10.3046972835109));
#109026=CARTESIAN_POINT('Ctrl Pts',(-8.73917581620004,4.98280881417132,
10.2560529863115));
#109027=CARTESIAN_POINT('Ctrl Pts',(-8.76821672288897,4.98578502014355,
10.2088713554413));
#109028=CARTESIAN_POINT('Ctrl Pts',(-8.79979741045243,4.9886922667281,10.163467982791));
#109029=CARTESIAN_POINT('Ctrl Pts',(-8.83140712435621,4.99160218541182,
10.1180228791383));
#109030=CARTESIAN_POINT('Ctrl Pts',(-8.86556141226627,4.99444314636371,
10.0743594493715));
#109031=CARTESIAN_POINT('Ctrl Pts',(-8.9020369816636,4.99724338856117,10.0327767523536));
#109032=CARTESIAN_POINT('Ctrl Pts',(-8.93852916378889,5.00004490612356,
9.99117511657633));
#109033=CARTESIAN_POINT('Ctrl Pts',(-8.97734495513403,5.00280596129228,
9.95165639069483));
#109034=CARTESIAN_POINT('Ctrl Pts',(-9.01822622710116,5.00557550960801,
9.91449948603069));
#109035=CARTESIAN_POINT('Ctrl Pts',(-9.05918459175291,5.00835028065543,
9.87727251198282));
#109036=CARTESIAN_POINT('Ctrl Pts',(-9.10221650595725,5.01113409695313,
9.84241678604415));
#109037=CARTESIAN_POINT('Ctrl Pts',(-9.14702398921705,5.01399091152725,
9.81018631863586));
#109038=CARTESIAN_POINT('Ctrl Pts',(-9.18119694485144,5.01616969485973,
9.78560537249271));
#109039=CARTESIAN_POINT('Ctrl Pts',(-9.2164018910126,5.01839136576603,9.76255101345989));
#109040=CARTESIAN_POINT('Ctrl Pts',(-9.25249037392882,5.02068651146548,
9.74112206565098));
#109041=CARTESIAN_POINT('Ctrl Pts',(-9.25250628189288,5.02068752317593,
9.74111261967531));
#109042=CARTESIAN_POINT('Ctrl Pts',(-9.25252219002876,5.02068853490066,
9.74110317401505));
#109043=CARTESIAN_POINT('Ctrl Pts',(-9.25253809833646,5.02068954663967,
9.7410937286702));
#109044=CARTESIAN_POINT('Ctrl Pts',(-9.29589163065568,5.02344675127292,
9.71535314888678));
#109045=CARTESIAN_POINT('Ctrl Pts',(-9.34068527737832,5.02631730163087,
9.69186606518692));
#109046=CARTESIAN_POINT('Ctrl Pts',(-9.38664850341049,5.02924103071376,
9.67076279903192));
#109047=CARTESIAN_POINT('Ctrl Pts',(-9.39086904267049,5.02950949997594,
9.66882500721419));
#109048=CARTESIAN_POINT('Ctrl Pts',(-9.39509940753062,5.02977841762489,
9.66690730986158));
#109049=CARTESIAN_POINT('Ctrl Pts',(-9.39933936688573,5.03004773707729,
9.66500980419198));
#109050=CARTESIAN_POINT('Ctrl Pts',(-9.44966448569674,5.03324435579571,
9.64248784342076));
#109051=CARTESIAN_POINT('Ctrl Pts',(-9.50134703697919,5.03649695591628,
9.62281079755896));
#109052=CARTESIAN_POINT('Ctrl Pts',(-9.55402765561808,5.0397409038115,9.60610077255766));
#109053=CARTESIAN_POINT('Ctrl Pts',(-9.60665618291867,5.04298164404532,
9.58940727066462));
#109054=CARTESIAN_POINT('Ctrl Pts',(-9.6602807545277,5.04621341531348,9.57567457046145));
#109055=CARTESIAN_POINT('Ctrl Pts',(-9.7145390850099,5.04939210439157,9.56498549236436));
#109056=CARTESIAN_POINT('Ctrl Pts',(-9.76876519149828,5.05256890564789,
9.55430276250511));
#109057=CARTESIAN_POINT('Ctrl Pts',(-9.82362429815191,5.05569255229287,
9.54665990766906));
#109058=CARTESIAN_POINT('Ctrl Pts',(-9.87875110638128,5.05874276495213,
9.54210429797237));
#109059=CARTESIAN_POINT('Ctrl Pts',(-9.93386694392061,5.06179237059389,
9.53754959487963));
#109060=CARTESIAN_POINT('Ctrl Pts',(-9.98925035416447,5.06476857510239,
9.53608094240158));
#109061=CARTESIAN_POINT('Ctrl Pts',(-10.0445327859616,5.06767582015448,
9.53771107726475));
#109062=CARTESIAN_POINT('Ctrl Pts',(-10.0998660288059,5.07058573730618,
9.5393427104133));
#109063=CARTESIAN_POINT('Ctrl Pts',(-10.1550980526427,5.07342669665712,
9.54407901163698));
#109064=CARTESIAN_POINT('Ctrl Pts',(-10.2098563768151,5.07622693720748,
9.55189644830043));
#109065=CARTESIAN_POINT('Ctrl Pts',(-10.2646396405576,5.07902845312185,
9.55971744539991));
#109066=CARTESIAN_POINT('Ctrl Pts',(-10.3189486537228,5.08178950659631,
9.57062271717316));
#109067=CARTESIAN_POINT('Ctrl Pts',(-10.3724087672457,5.08455905318362,
9.58454854673317));
#109068=CARTESIAN_POINT('Ctrl Pts',(-10.4259696944439,5.08733382250901,
9.59850063725613));
#109069=CARTESIAN_POINT('Ctrl Pts',(-10.478678237989,5.09011763705019,9.61548519505742));
#109070=CARTESIAN_POINT('Ctrl Pts',(-10.5301588194608,5.09297444983745,
9.63539152064834));
#109071=CARTESIAN_POINT('Ctrl Pts',(-10.5694212090269,5.09515323829253,
9.65057335985521));
#109072=CARTESIAN_POINT('Ctrl Pts',(-10.607969260143,5.09737491455902,9.66745379563866));
#109073=CARTESIAN_POINT('Ctrl Pts',(-10.6456390746319,5.09967006612909,
9.68596252398159));
#109074=CARTESIAN_POINT('Ctrl Pts',(-10.6456556796874,5.09967107784415,
9.6859706827279));
#109075=CARTESIAN_POINT('Ctrl Pts',(-10.6456722845726,5.0996720895735,9.6859788417905));
#109076=CARTESIAN_POINT('Ctrl Pts',(-10.6456888892876,5.09967310131713,
9.68598700116936));
#109077=CARTESIAN_POINT('Ctrl Pts',(-10.6909400568651,5.10243030494418,
9.70822293961197));
#109078=CARTESIAN_POINT('Ctrl Pts',(-10.7350912328075,5.10530085442953,
9.73289653818946));
#109079=CARTESIAN_POINT('Ctrl Pts',(-10.7778854184091,5.1082245827779,9.75985247627576));
#109080=CARTESIAN_POINT('Ctrl Pts',(-10.7818149703992,5.10849305248677,
9.76232769010826));
#109081=CARTESIAN_POINT('Ctrl Pts',(-10.7857330652942,5.10876197058531,
9.76482211509285));
#109082=CARTESIAN_POINT('Ctrl Pts',(-10.7896394953668,5.1090312904899,9.76733561083399));
#109083=CARTESIAN_POINT('Ctrl Pts',(-10.83600579177,5.11222790896037,9.79716885663062));
#109084=CARTESIAN_POINT('Ctrl Pts',(-10.8807316418915,5.11548050900234,
9.82969377446877));
#109085=CARTESIAN_POINT('Ctrl Pts',(-10.9235183751133,5.11872445694514,
9.86467616570817));
#109086=CARTESIAN_POINT('Ctrl Pts',(-10.9662628001444,5.12196519722151,
9.89962396581228));
#109087=CARTESIAN_POINT('Ctrl Pts',(-11.0070722105773,5.12519696865785,
9.93702414598331));
#109088=CARTESIAN_POINT('Ctrl Pts',(-11.0456792379536,5.12837565798173,
9.97661858986932));
#109089=CARTESIAN_POINT('Ctrl Pts',(-11.0842633365815,5.13155245947915,
10.0161895185793));
#109090=CARTESIAN_POINT('Ctrl Pts',(-11.1206477753381,5.13467610644268,
10.0579520276114));
#109091=CARTESIAN_POINT('Ctrl Pts',(-11.1545932254964,5.13772631944924,
10.1016261013782));
#109092=CARTESIAN_POINT('Ctrl Pts',(-11.1885319201848,5.14077592543417,
10.1452914835857));
#109093=CARTESIAN_POINT('Ctrl Pts',(-11.2200325561578,5.14375213031462,
10.1908676697158));
#109094=CARTESIAN_POINT('Ctrl Pts',(-11.2488830294713,5.14665937572077,
10.2380529909611));
#109095=CARTESIAN_POINT('Ctrl Pts',(-11.2777600197117,5.1495692932222,10.2852816809822));
#109096=CARTESIAN_POINT('Ctrl Pts',(-11.3039817912036,5.15241025290498,
10.3341225188811));
#109097=CARTESIAN_POINT('Ctrl Pts',(-11.327364464775,5.15521049372753,10.3842507215798));
#109098=CARTESIAN_POINT('Ctrl Pts',(-11.350757787916,5.15801200991149,10.4344017550202));
#109099=CARTESIAN_POINT('Ctrl Pts',(-11.3713090831897,5.16077306359557,
10.4858414077179));
#109100=CARTESIAN_POINT('Ctrl Pts',(-11.3888669371384,5.16354261029997,
10.538221117345));
#109101=CARTESIAN_POINT('Ctrl Pts',(-11.4064579012108,5.16631737974024,
10.5906996032044));
#109102=CARTESIAN_POINT('Ctrl Pts',(-11.4210435465301,5.16910119430287,
10.6441217377681));
#109103=CARTESIAN_POINT('Ctrl Pts',(-11.4325112956144,5.17195800700105,
10.6981125013045));
#109104=CARTESIAN_POINT('Ctrl Pts',(-11.441257340803,5.1741367966458,10.7392893402973));
#109105=CARTESIAN_POINT('Ctrl Pts',(-11.4481905195216,5.17635847408748,
10.7807963793421));
#109106=CARTESIAN_POINT('Ctrl Pts',(-11.4532801239676,5.17865362687244,
10.8224579414613));
#109107=CARTESIAN_POINT('Ctrl Pts',(-11.4532823674888,5.17865463858643,
10.8224763060711));
#109108=CARTESIAN_POINT('Ctrl Pts',(-11.4532846106522,5.1786556503147,10.8224946707113));
#109109=CARTESIAN_POINT('Ctrl Pts',(-11.4532868534577,5.17865666205725,
10.8225130353818));
#109110=CARTESIAN_POINT('Ctrl Pts',(-11.4597488615248,5.1815717113611,10.8754256265488));
#109111=CARTESIAN_POINT('Ctrl Pts',(-11.4632505365527,5.18460896799363,
10.9286963294922));
#109112=CARTESIAN_POINT('Ctrl Pts',(-11.4638019408274,5.18770184618821,
10.9820734860361));
#109113=CARTESIAN_POINT('Ctrl Pts',(-11.4638605279395,5.18803046678456,
10.9877448484085));
#109114=CARTESIAN_POINT('Ctrl Pts',(-11.4638857947485,5.18835971530495,
10.9934173661873));
#109115=CARTESIAN_POINT('Ctrl Pts',(-11.4638777447092,5.18868951188054,
10.999090704177));
#109116=CARTESIAN_POINT('Origin',(-10.,3.5,11.));
#109117=CARTESIAN_POINT('',(-11.4634999578674,5.75937264474327,10.9996488274338));
#109118=CARTESIAN_POINT('',(-11.4634999536212,5.6893446890626,10.9996315564861));
#109119=CARTESIAN_POINT('',(-11.4635,3.5,11.));
#109120=CARTESIAN_POINT('Ctrl Pts',(-11.4634999578674,5.75937264475447,
10.9996488276474));
#109121=CARTESIAN_POINT('Ctrl Pts',(-11.4634751845613,5.75396169207678,
10.8964068375278));
#109122=CARTESIAN_POINT('Ctrl Pts',(-11.4525265696792,5.74891300107215,
10.7934557525576));
#109123=CARTESIAN_POINT('Ctrl Pts',(-11.4259999127222,5.7427693151185,10.6700222404515));
#109124=CARTESIAN_POINT('Ctrl Pts',(-11.4206389907439,5.74165103674276,
10.6476565306573));
#109125=CARTESIAN_POINT('Ctrl Pts',(-11.4091188354672,5.73945225024823,
10.604145228243));
#109126=CARTESIAN_POINT('Ctrl Pts',(-11.403004960128,5.73837244821277,10.5829940732423));
#109127=CARTESIAN_POINT('Ctrl Pts',(-11.3882387752976,5.73592997125282,
10.5359181889912));
#109128=CARTESIAN_POINT('Ctrl Pts',(-11.3793329094427,5.73456239736482,
10.5100822163276));
#109129=CARTESIAN_POINT('Ctrl Pts',(-11.3599257625239,5.73175108511031,
10.4585152748437));
#109130=CARTESIAN_POINT('Ctrl Pts',(-11.3494045105388,5.73030702904237,
10.4328042122368));
#109131=CARTESIAN_POINT('Ctrl Pts',(-11.3354097251332,5.72846081828386,
10.4012018609594));
#109132=CARTESIAN_POINT('Ctrl Pts',(-11.3326175154221,5.72809581569482,
10.3950133064784));
#109133=CARTESIAN_POINT('Ctrl Pts',(-11.3281494377969,5.72751659991553,
10.3852914415388));
#109134=CARTESIAN_POINT('Ctrl Pts',(-11.3265022600051,5.72730407670075,
10.3817449600354));
#109135=CARTESIAN_POINT('Ctrl Pts',(-11.3235442150275,5.72692412715543,
10.3754423361269));
#109136=CARTESIAN_POINT('Ctrl Pts',(-11.3222389178505,5.72675704010261,
10.3726836458046));
#109137=CARTESIAN_POINT('Ctrl Pts',(-11.3191012445146,5.72635676583078,
10.3661056069008));
#109138=CARTESIAN_POINT('Ctrl Pts',(-11.3172609185385,5.72612309845923,
10.3622901392861));
#109139=CARTESIAN_POINT('Ctrl Pts',(-11.3116657873252,5.72541609907429,
10.3508175583392));
#109140=CARTESIAN_POINT('Ctrl Pts',(-11.3078606574134,5.7249398409676,10.3431853579949));
#109141=CARTESIAN_POINT('Ctrl Pts',(-11.2657307358421,5.71971904013604,
10.2605003968687));
#109142=CARTESIAN_POINT('Ctrl Pts',(-11.2210617867717,5.71465341987026,
10.1888653232984));
#109143=CARTESIAN_POINT('Ctrl Pts',(-11.1030396053925,5.7028217672449,10.0316203727491));
#109144=CARTESIAN_POINT('Ctrl Pts',(-11.02546074452,5.69611448254029,9.94981255713691));
#109145=CARTESIAN_POINT('Ctrl Pts',(-10.9256444203635,5.68882098988141,
9.8662758296158));
#109146=CARTESIAN_POINT('Ctrl Pts',(-10.9118086775227,5.68783492589036,
9.85511875640572));
#109147=CARTESIAN_POINT('Ctrl Pts',(-10.8919444391134,5.68645345897277,
9.83968890734707));
#109148=CARTESIAN_POINT('Ctrl Pts',(-10.8860819386882,5.68604985736793,
9.8352058057695));
#109149=CARTESIAN_POINT('Ctrl Pts',(-10.8752669265492,5.68531271865177,
9.82706438268404));
#109150=CARTESIAN_POINT('Ctrl Pts',(-10.8703247838548,5.68497866562314,
9.82339261973629));
#109151=CARTESIAN_POINT('Ctrl Pts',(-10.8602418527226,5.68430272781746,
9.81599979912695));
#109152=CARTESIAN_POINT('Ctrl Pts',(-10.8550997349456,5.68396092499455,
9.81228077144696));
#109153=CARTESIAN_POINT('Ctrl Pts',(-10.8422961207512,5.68311694730654,
9.80314683001247));
#109154=CARTESIAN_POINT('Ctrl Pts',(-10.8346063792301,5.68261628936738,
9.79777187573294));
#109155=CARTESIAN_POINT('Ctrl Pts',(-10.8052700618333,5.68072918415379,
9.77768358987166));
#109156=CARTESIAN_POINT('Ctrl Pts',(-10.7832811845505,5.67936154595055,
9.76347746699176));
#109157=CARTESIAN_POINT('Ctrl Pts',(-10.7266197596804,5.67594343044391,
9.7289891569875));
#109158=CARTESIAN_POINT('Ctrl Pts',(-10.6914711183829,5.67392031772148,
9.70952999718739));
#109159=CARTESIAN_POINT('Ctrl Pts',(-10.5979003951866,5.66872485468788,
9.66264916333116));
#109160=CARTESIAN_POINT('Ctrl Pts',(-10.5383879783768,5.66560704674836,
9.63760110345522));
#109161=CARTESIAN_POINT('Ctrl Pts',(-10.4063970857854,5.65879999027099,
9.59205176891092));
#109162=CARTESIAN_POINT('Ctrl Pts',(-10.3336020572187,5.65511096054384,
9.57305077187021));
#109163=CARTESIAN_POINT('Ctrl Pts',(-10.2478384602662,5.65052616382632,
9.55758774414966));
#109164=CARTESIAN_POINT('Ctrl Pts',(-10.2359719117291,5.64988650988392,
9.55559899725329));
#109165=CARTESIAN_POINT('Ctrl Pts',(-10.2191328204539,5.64896966465492,
9.55298992912052));
#109166=CARTESIAN_POINT('Ctrl Pts',(-10.2141792352614,5.64869883681889,
9.55224843570045));
#109167=CARTESIAN_POINT('Ctrl Pts',(-10.2058081376365,5.64823913171723,
9.55103928341762));
#109168=CARTESIAN_POINT('Ctrl Pts',(-10.2023925485951,5.64805099159888,
9.55055824409221));
#109169=CARTESIAN_POINT('Ctrl Pts',(-10.1953716961818,5.6476630370557,9.54959475288144));
#109170=CARTESIAN_POINT('Ctrl Pts',(-10.191766299478,5.64746315279071,9.54911366181618));
#109171=CARTESIAN_POINT('Ctrl Pts',(-10.1824716902298,5.64694622577664,
9.54790867244031));
#109172=CARTESIAN_POINT('Ctrl Pts',(-10.1767800033127,5.64662810518481,
9.54720477371541));
#109173=CARTESIAN_POINT('Ctrl Pts',(-10.1527148175632,5.6452768330234,9.54437211065711));
#109174=CARTESIAN_POINT('Ctrl Pts',(-10.1343067200596,5.64422792563633,
9.54255840327747));
#109175=CARTESIAN_POINT('Ctrl Pts',(-10.084318370806,5.64134705476572,9.53858819838437));
#109176=CARTESIAN_POINT('Ctrl Pts',(-10.0526952848321,5.6394896638266,9.53710662368729));
#109177=CARTESIAN_POINT('Ctrl Pts',(-9.92296211249676,5.63178824003443,
9.53524035496927));
#109178=CARTESIAN_POINT('Ctrl Pts',(-9.82497810757726,5.62580122030368,
9.54369478198711));
#109179=CARTESIAN_POINT('Ctrl Pts',(-9.70388979024914,5.61854609135911,
9.56654895927752));
#109180=CARTESIAN_POINT('Ctrl Pts',(-9.67933119119105,5.61708083113229,
9.57184218409491));
#109181=CARTESIAN_POINT('Ctrl Pts',(-9.61677945002552,5.61336909554873,
9.5870192468214));
#109182=CARTESIAN_POINT('Ctrl Pts',(-9.57902427984222,5.61114865112057,
9.59780441858418));
#109183=CARTESIAN_POINT('Ctrl Pts',(-9.53106311061488,5.60835377661213,
9.61361730866616));
#109184=CARTESIAN_POINT('Ctrl Pts',(-9.52042126618845,5.60773525419424,
9.61726249019927));
#109185=CARTESIAN_POINT('Ctrl Pts',(-9.50346254046259,5.60675198387285,
9.62329075023911));
#109186=CARTESIAN_POINT('Ctrl Pts',(-9.49711843267061,5.60638469245826,
9.62559542402473));
#109187=CARTESIAN_POINT('Ctrl Pts',(-9.48511146426278,5.60569051149681,
9.63005155629995));
#109188=CARTESIAN_POINT('Ctrl Pts',(-9.47944559020952,5.60536334880239,
9.63219443977061));
#109189=CARTESIAN_POINT('Ctrl Pts',(-9.46658550475148,5.60462163544372,
9.63714971871467));
#109190=CARTESIAN_POINT('Ctrl Pts',(-9.45939989423287,5.60420781903006,
9.63998402888817));
#109191=CARTESIAN_POINT('Ctrl Pts',(-9.43746554908926,5.60294629900765,
9.64883717405807));
#109192=CARTESIAN_POINT('Ctrl Pts',(-9.42279210151057,5.60210471859063,
9.65504012751637));
#109193=CARTESIAN_POINT('Ctrl Pts',(-9.35325211640324,5.59812368510101,
9.68578471831097));
#109194=CARTESIAN_POINT('Ctrl Pts',(-9.29982832664854,5.59509056882238,
9.71345219354998));
#109195=CARTESIAN_POINT('Ctrl Pts',(-9.16108869688416,5.58709484046341,
9.79651303161479));
#109196=CARTESIAN_POINT('Ctrl Pts',(-9.07960050566415,5.58227967614869,
9.8576271266484));
#109197=CARTESIAN_POINT('Ctrl Pts',(-8.97612388070272,5.57519700773471,
9.95354352513776));
#109198=CARTESIAN_POINT('Ctrl Pts',(-8.94824795382478,5.57317087940225,
9.98156463383729));
#109199=CARTESIAN_POINT('Ctrl Pts',(-8.9168971938909,5.57069971731275,10.0157399865872));
#109200=CARTESIAN_POINT('Ctrl Pts',(-8.91228811892609,5.57033123425293,
10.0208359061147));
#109201=CARTESIAN_POINT('Ctrl Pts',(-8.90485573970207,5.56972818882087,
10.0291705825478));
#109202=CARTESIAN_POINT('Ctrl Pts',(-8.90201046193255,5.56949518468129,
10.0323897055122));
#109203=CARTESIAN_POINT('Ctrl Pts',(-8.89695123557325,5.56907692763916,
10.0381647192384));
#109204=CARTESIAN_POINT('Ctrl Pts',(-8.8947319240538,5.56889207194336,10.0407158064448));
#109205=CARTESIAN_POINT('Ctrl Pts',(-8.88990825141467,5.5684872433973,10.0462995550094));
#109206=CARTESIAN_POINT('Ctrl Pts',(-8.88730750298332,5.56826702624702,
10.049335161397));
#109207=CARTESIAN_POINT('Ctrl Pts',(-8.87994370990434,5.56763802831837,
10.058001829791));
#109208=CARTESIAN_POINT('Ctrl Pts',(-8.87521081981659,5.56722717663803,
10.0636582134797));
#109209=CARTESIAN_POINT('Ctrl Pts',(-8.84361926069765,5.56444149849838,
10.1019991614934));
#109210=CARTESIAN_POINT('Ctrl Pts',(-8.81814803464039,5.56198257101558,
10.1357967613737));
#109211=CARTESIAN_POINT('Ctrl Pts',(-8.75528778205999,5.55542204332419,
10.2271911557369));
#109212=CARTESIAN_POINT('Ctrl Pts',(-8.72042312836446,5.55126199252031,
10.2864000872698));
#109213=CARTESIAN_POINT('Ctrl Pts',(-8.64759971134318,5.54146485055223,
10.4326978858288));
#109214=CARTESIAN_POINT('Ctrl Pts',(-8.61369675606955,5.53590411863829,
10.5214744415114));
#109215=CARTESIAN_POINT('Ctrl Pts',(-8.58542759551829,5.52996312122784,
10.6245501201369));
#109216=CARTESIAN_POINT('Ctrl Pts',(-8.58238160814586,5.52929731675091,
10.6362201117934));
#109217=CARTESIAN_POINT('Ctrl Pts',(-8.57764252592889,5.52821730858377,
10.6553410158908));
#109218=CARTESIAN_POINT('Ctrl Pts',(-8.5758629469609,5.52780037672069,10.6627697276098));
#109219=CARTESIAN_POINT('Ctrl Pts',(-8.57277864493263,5.52705662783049,
10.6761048997457));
#109220=CARTESIAN_POINT('Ctrl Pts',(-8.5714522317532,5.5267291302939,10.6820061200553));
#109221=CARTESIAN_POINT('Ctrl Pts',(-8.5687123185696,5.52603588030677,10.6945592275047));
#109222=CARTESIAN_POINT('Ctrl Pts',(-8.56730851784191,5.52567044088332,
10.7012131000287));
#109223=CARTESIAN_POINT('Ctrl Pts',(-8.56365983179548,5.52469201377673,
10.7191246880075));
#109224=CARTESIAN_POINT('Ctrl Pts',(-8.56150091082136,5.52408173412774,
10.7303995547849));
#109225=CARTESIAN_POINT('Ctrl Pts',(-8.55109180550355,5.52096694416077,
10.7884503208215));
#109226=CARTESIAN_POINT('Ctrl Pts',(-8.54498922372527,5.51853011876217,
10.8355845415506));
#109227=CARTESIAN_POINT('Ctrl Pts',(-8.53259470071599,5.51074545742772,
10.9900400917294));
#109228=CARTESIAN_POINT('Ctrl Pts',(-8.53582116955131,5.50565193260519,
11.0977597896024));
#109229=CARTESIAN_POINT('Ctrl Pts',(-8.55462079935962,5.49898023715777,
11.2312092810011));
#109230=CARTESIAN_POINT('Ctrl Pts',(-8.55918896416599,5.49761272712688,
11.258151524485));
#109231=CARTESIAN_POINT('Ctrl Pts',(-8.56991772437733,5.49480118658392,
11.312199953099));
#109232=CARTESIAN_POINT('Ctrl Pts',(-8.57610167191231,5.49335682468041,
11.3392896763584));
#109233=CARTESIAN_POINT('Ctrl Pts',(-8.584751264952,5.49151026392779,11.372759131778));
#109234=CARTESIAN_POINT('Ctrl Pts',(-8.58649586849336,5.49114523381042,
11.3793209973634));
#109235=CARTESIAN_POINT('Ctrl Pts',(-8.58931708511743,5.49056598383598,
11.3896424714518));
#109236=CARTESIAN_POINT('Ctrl Pts',(-8.59036323671866,5.49035345428409,
11.3934103923145));
#109237=CARTESIAN_POINT('Ctrl Pts',(-8.5922527280972,5.48997349937632,11.4001114631985));
#109238=CARTESIAN_POINT('Ctrl Pts',(-8.59309015561774,5.48980641335692,
11.403046217942));
#109239=CARTESIAN_POINT('Ctrl Pts',(-8.59511182572198,5.48940614934375,
11.4100480596921));
#109240=CARTESIAN_POINT('Ctrl Pts',(-8.59630454375795,5.48917249127103,
11.4141126159481));
#109241=CARTESIAN_POINT('Ctrl Pts',(-8.59995143745772,5.48846554736997,
11.4263437447193));
#109242=CARTESIAN_POINT('Ctrl Pts',(-8.60245931730221,5.48798933610691,
11.4344939577332));
#109243=CARTESIAN_POINT('Ctrl Pts',(-8.62994017114206,5.48287744936242,
11.521102342605));
#109244=CARTESIAN_POINT('Ctrl Pts',(-8.6614184597517,5.47793480198223,11.5973345113501));
#109245=CARTESIAN_POINT('Ctrl Pts',(-8.75160458821776,5.46608980884087,
11.7723064487831));
#109246=CARTESIAN_POINT('Ctrl Pts',(-8.81585200155387,5.45924476080286,
11.867611813658));
#109247=CARTESIAN_POINT('Ctrl Pts',(-8.90220574751374,5.45182716053409,
11.9679868464299));
#109248=CARTESIAN_POINT('Ctrl Pts',(-8.91409176617374,5.45083724424171,
11.9813022484115));
#109249=CARTESIAN_POINT('Ctrl Pts',(-8.93165118536552,5.44941837984032,
12.0002634567994));
#109250=CARTESIAN_POINT('Ctrl Pts',(-8.93713167711307,5.44898144814165,
12.0060850383939));
#109251=CARTESIAN_POINT('Ctrl Pts',(-8.94688621259826,5.44821401530213,
12.0162779983136));
#109252=CARTESIAN_POINT('Ctrl Pts',(-8.95114042123761,5.44788268275679,
12.0206680188376));
#109253=CARTESIAN_POINT('Ctrl Pts',(-8.96001183880727,5.44719861235042,
12.029708608236));
#109254=CARTESIAN_POINT('Ctrl Pts',(-8.96463303443362,5.4468460581491,12.0343550849767));
#109255=CARTESIAN_POINT('Ctrl Pts',(-8.97663391877337,5.44594008831225,
12.0462606091984));
#109256=CARTESIAN_POINT('Ctrl Pts',(-8.98405976100066,5.44538870881714,
12.0534727508013));
#109257=CARTESIAN_POINT('Ctrl Pts',(-9.01647678889355,5.44302023808074,
12.0842953054544));
#109258=CARTESIAN_POINT('Ctrl Pts',(-9.04222004650754,5.44123709629285,
12.1071007249004));
#109259=CARTESIAN_POINT('Ctrl Pts',(-9.11485506446146,5.43643698710528,
12.1670148256588));
#109260=CARTESIAN_POINT('Ctrl Pts',(-9.16325495190777,5.43348800578885,
12.2021911517027));
#109261=CARTESIAN_POINT('Ctrl Pts',(-9.29109000396541,5.42608651869492,
12.2836294975852));
#109262=CARTESIAN_POINT('Ctrl Pts',(-9.3729691046201,5.42169686344296,12.3255518478415));
#109263=CARTESIAN_POINT('Ctrl Pts',(-9.4828185889188,5.41565060637893,12.3693269994291));
#109264=CARTESIAN_POINT('Ctrl Pts',(-9.50767029696129,5.41427210959858,
12.3784572311984));
#109265=CARTESIAN_POINT('Ctrl Pts',(-9.53908618184528,5.41250063641447,
12.3890411602327));
#109266=CARTESIAN_POINT('Ctrl Pts',(-9.54543243094899,5.41214132864644,
12.3911309120148));
#109267=CARTESIAN_POINT('Ctrl Pts',(-9.55549153064934,5.41156918822611,
12.3943670852765));
#109268=CARTESIAN_POINT('Ctrl Pts',(-9.55919509641632,5.41135797793863,
12.3955423261554));
#109269=CARTESIAN_POINT('Ctrl Pts',(-9.5658195423956,5.410979123565,12.3976154399182));
#109270=CARTESIAN_POINT('Ctrl Pts',(-9.5687386030014,5.4108118065162,12.3985189289317));
#109271=CARTESIAN_POINT('Ctrl Pts',(-9.57574476515266,5.41040933565046,
12.4006634106976));
#109272=CARTESIAN_POINT('Ctrl Pts',(-9.57983446569008,5.41017368600598,
12.4018956513223));
#109273=CARTESIAN_POINT('Ctrl Pts',(-9.59227516179633,5.40945480484898,
12.4055847472982));
#109274=CARTESIAN_POINT('Ctrl Pts',(-9.60064258559932,5.40896850454128,
12.4079849692451));
#109275=CARTESIAN_POINT('Ctrl Pts',(-9.6201049153665,5.40783173372233,12.4133803584342));
#109276=CARTESIAN_POINT('Ctrl Pts',(-9.63121457885076,5.40717859637654,
12.4163197417373));
#109277=CARTESIAN_POINT('Ctrl Pts',(-9.75031488693492,5.40013989327112,
12.4463348987012));
#109278=CARTESIAN_POINT('Ctrl Pts',(-9.8610203945715,5.39330691625596,12.4611335607252));
#109279=CARTESIAN_POINT('Ctrl Pts',(-10.0530981639029,5.38185587283728,
12.4647657110337));
#109280=CARTESIAN_POINT('Ctrl Pts',(-10.1338624216389,5.37715698106629,
12.4596034144204));
#109281=CARTESIAN_POINT('Ctrl Pts',(-10.225726492517,5.37199539598312,12.4460377567033));
#109282=CARTESIAN_POINT('Ctrl Pts',(-10.2376330578694,5.37132972349012,
12.4441288672457));
#109283=CARTESIAN_POINT('Ctrl Pts',(-10.257041069279,5.37024988534706,12.4407707927581));
#109284=CARTESIAN_POINT('Ctrl Pts',(-10.2645569976898,5.36983299295565,
12.4394096660144));
#109285=CARTESIAN_POINT('Ctrl Pts',(-10.2780048613045,5.36908928759158,
12.4368653828941));
#109286=CARTESIAN_POINT('Ctrl Pts',(-10.283940728777,5.36876179442335,12.4357041810645));
#109287=CARTESIAN_POINT('Ctrl Pts',(-10.2965351810392,5.36806852584463,
12.4331592322019));
#109288=CARTESIAN_POINT('Ctrl Pts',(-10.3031916776256,5.36770306367599,
12.4317658003962));
#109289=CARTESIAN_POINT('Ctrl Pts',(-10.3210591360553,5.36672450877786,
12.4278953380821));
#109290=CARTESIAN_POINT('Ctrl Pts',(-10.3322511861807,5.36611412533469,
12.4253326715511));
#109291=CARTESIAN_POINT('Ctrl Pts',(-10.3896103689285,5.36299776132738,
12.4114866809262));
#109292=CARTESIAN_POINT('Ctrl Pts',(-10.4352403475258,5.3605595508308,12.398090594355));
#109293=CARTESIAN_POINT('Ctrl Pts',(-10.5817832296746,5.35276621454822,
12.3471962836403));
#109294=CARTESIAN_POINT('Ctrl Pts',(-10.6792175310725,5.34766620346676,
12.300796752291));
#109295=CARTESIAN_POINT('Ctrl Pts',(-10.8155966594527,5.33972311825338,
12.2163163638748));
#109296=CARTESIAN_POINT('Ctrl Pts',(-10.8589656600076,5.33705279799055,
12.1860861391736));
#109297=CARTESIAN_POINT('Ctrl Pts',(-10.9063592134991,5.33385381070026,
12.149085979583));
#109298=CARTESIAN_POINT('Ctrl Pts',(-10.912083377669,5.33346251160953,12.144547736108));
#109299=CARTESIAN_POINT('Ctrl Pts',(-10.9211837887232,5.33283206237605,
12.1372211081993));
#109300=CARTESIAN_POINT('Ctrl Pts',(-10.9245819828745,5.3325947579296,12.1344600378519));
#109301=CARTESIAN_POINT('Ctrl Pts',(-10.9305933451481,5.33217150373321,
12.1295307899567));
#109302=CARTESIAN_POINT('Ctrl Pts',(-10.9332114224758,5.33198598579658,
12.127368715312));
#109303=CARTESIAN_POINT('Ctrl Pts',(-10.9358469810233,5.3317980178168,12.1251767324135));
#109304=CARTESIAN_POINT('Ctrl Pts',(-10.935871955471,5.33179623653024,12.1251559598643));
#109305=CARTESIAN_POINT('Ctrl Pts',(-10.9359210161429,5.33179273709403,
12.125115150784));
#109306=CARTESIAN_POINT('Ctrl Pts',(-10.9359451023203,5.33179101895536,
12.12509511439));
#109307=CARTESIAN_POINT('Ctrl Pts',(-10.9359924261973,5.3317876430024,12.1250557448478));
#109308=CARTESIAN_POINT('Ctrl Pts',(-10.9360156639595,5.33178598519068,
12.1250364117379));
#109309=CARTESIAN_POINT('Ctrl Pts',(-10.9360613285538,5.33178272723379,
12.1249984177932));
#109310=CARTESIAN_POINT('Ctrl Pts',(-10.936083755474,5.33178112708882,12.1249797569685));
#109311=CARTESIAN_POINT('Ctrl Pts',(-10.9361278340951,5.33177798193673,
12.124943078127));
#109312=CARTESIAN_POINT('Ctrl Pts',(-10.9361494857658,5.33177643693775,
12.1249250602124));
#109313=CARTESIAN_POINT('Ctrl Pts',(-10.9361920472674,5.33177339971353,
12.1248896396417));
#109314=CARTESIAN_POINT('Ctrl Pts',(-10.9362129571844,5.33177190748768,
12.1248722369852));
#109315=CARTESIAN_POINT('Ctrl Pts',(-10.9362540669237,5.33176897356067,
12.124838020721));
#109316=CARTESIAN_POINT('Ctrl Pts',(-10.936274266782,5.33176753186205,12.1248212071492));
#109317=CARTESIAN_POINT('Ctrl Pts',(-10.9363139866415,5.33176469684657,
12.1247881440808));
#109318=CARTESIAN_POINT('Ctrl Pts',(-10.9363335065546,5.33176330354071,
12.1247718947183));
#109319=CARTESIAN_POINT('Ctrl Pts',(-10.9363718946589,5.33176056331656,
12.1247399368279));
#109320=CARTESIAN_POINT('Ctrl Pts',(-10.9363907629483,5.33175921639562,
12.1247242282746));
#109321=CARTESIAN_POINT('Ctrl Pts',(-10.9364278748516,5.33175656702357,
12.1246933296523));
#109322=CARTESIAN_POINT('Ctrl Pts',(-10.9364461184771,5.33175526457569,
12.124678139626));
#109323=CARTESIAN_POINT('Ctrl Pts',(-10.9364820065062,5.33175270234464,
12.1246482570197));
#109324=CARTESIAN_POINT('Ctrl Pts',(-10.9364996509585,5.33175144256175,
12.1246335644474));
#109325=CARTESIAN_POINT('Ctrl Pts',(-10.9365343649454,5.3317489639366,12.1246046566548));
#109326=CARTESIAN_POINT('Ctrl Pts',(-10.9365514344763,5.33174774509809,
12.1245904414825));
#109327=CARTESIAN_POINT('Ctrl Pts',(-10.9365850215086,5.33174534673773,
12.1245624695622));
#109328=CARTESIAN_POINT('Ctrl Pts',(-10.9366015390759,5.33174416721444,
12.1245487128011));
#109329=CARTESIAN_POINT('Ctrl Pts',(-10.9366340439596,5.33174184593896,
12.124521639689));
#109330=CARTESIAN_POINT('Ctrl Pts',(-10.9366500313338,5.33174070418565,
12.1245083233286));
#109331=CARTESIAN_POINT('Ctrl Pts',(-10.9366814969533,5.33173845695068,
12.1244821135399));
#109332=CARTESIAN_POINT('Ctrl Pts',(-10.936696975063,5.3317373514815,12.1244692202606));
#109333=CARTESIAN_POINT('Ctrl Pts',(-10.9367274412923,5.33173517545619,
12.1244438407989));
#109334=CARTESIAN_POINT('Ctrl Pts',(-10.9367424296135,5.33173410488827,
12.1244313544821));
#109335=CARTESIAN_POINT('Ctrl Pts',(-10.9367719358495,5.33173199727443,
12.1244067727304));
#109336=CARTESIAN_POINT('Ctrl Pts',(-10.9367864535228,5.33173096024819,
12.1243946775279));
#109337=CARTESIAN_POINT('Ctrl Pts',(-10.9368150353102,5.33172891852154,
12.1243708640621));
#109338=CARTESIAN_POINT('Ctrl Pts',(-10.9368290998166,5.33172791379536,
12.1243591455011));
#109339=CARTESIAN_POINT('Ctrl Pts',(-10.9368567931844,5.33172593539581,
12.1243360704784));
#109340=CARTESIAN_POINT('Ctrl Pts',(-10.9368704218646,5.3317249617375,12.1243247141951));
#109341=CARTESIAN_POINT('Ctrl Pts',(-10.9368972593753,5.33172304435154,
12.1243023506472));
#109342=CARTESIAN_POINT('Ctrl Pts',(-10.9369104683585,5.33172210061494,
12.1242913432807));
#109343=CARTESIAN_POINT('Ctrl Pts',(-10.936939951615,5.33171999406892,12.1242667732867));
#109344=CARTESIAN_POINT('Ctrl Pts',(-10.936956225926,5.33171883124094,12.1242532104234));
#109345=CARTESIAN_POINT('Ctrl Pts',(-10.9369886671538,5.33171651316581,
12.1242261730044));
#109346=CARTESIAN_POINT('Ctrl Pts',(-10.9370048339043,5.33171535793116,
12.1242126985953));
#109347=CARTESIAN_POINT('Ctrl Pts',(-10.9370370617322,5.33171305492154,
12.1241858366735));
#109348=CARTESIAN_POINT('Ctrl Pts',(-10.9370531227587,5.3317119071508,12.1241724492111));
#109349=CARTESIAN_POINT('Ctrl Pts',(-10.9401701544016,5.33148914562101,
12.1215741742901));
#109350=CARTESIAN_POINT('Ctrl Pts',(-10.9432603785816,5.33126661211374,
12.1189764988862));
#109351=CARTESIAN_POINT('Ctrl Pts',(-10.9520171785946,5.33063130069911,
12.1115533890752));
#109352=CARTESIAN_POINT('Ctrl Pts',(-10.9576576639757,5.33021642320187,
12.1066975372728));
#109353=CARTESIAN_POINT('Ctrl Pts',(-10.970538068595,5.32925643764137,12.0954366917194));
#109354=CARTESIAN_POINT('Ctrl Pts',(-10.9777520006666,5.32870948082866,
12.0890026188933));
#109355=CARTESIAN_POINT('Ctrl Pts',(-11.0011312587027,5.32690773868589,
12.0677311968709));
#109356=CARTESIAN_POINT('Ctrl Pts',(-11.0170261777752,5.32563647999188,
12.0526021907316));
#109357=CARTESIAN_POINT('Ctrl Pts',(-11.0812036386707,5.3203299720508,11.9887061673248));
#109358=CARTESIAN_POINT('Ctrl Pts',(-11.1263658751875,5.31617932768404,
11.9369314316597));
#109359=CARTESIAN_POINT('Ctrl Pts',(-11.2261998167071,5.30622416108125,
11.8047830664502));
#109360=CARTESIAN_POINT('Ctrl Pts',(-11.2768398944601,5.30048358756676,
11.7217526381657));
#109361=CARTESIAN_POINT('Ctrl Pts',(-11.3269480063776,5.29399935499248,
11.6175649812107));
#109362=CARTESIAN_POINT('Ctrl Pts',(-11.334682150088,5.29296785414346,11.6006672292563));
#109363=CARTESIAN_POINT('Ctrl Pts',(-11.3450408823767,5.29154114339736,
11.5768465399465));
#109364=CARTESIAN_POINT('Ctrl Pts',(-11.3479377299785,5.29113681741341,
11.5700445463398));
#109365=CARTESIAN_POINT('Ctrl Pts',(-11.353153594213,5.29039877158046,11.5575352419882));
#109366=CARTESIAN_POINT('Ctrl Pts',(-11.3554883440904,5.29006453105387,
11.5518347091583));
#109367=CARTESIAN_POINT('Ctrl Pts',(-11.360153480323,5.28938863376775,11.5402360369109));
#109368=CARTESIAN_POINT('Ctrl Pts',(-11.362481661722,5.28904705593197,11.534337149013));
#109369=CARTESIAN_POINT('Ctrl Pts',(-11.3681512763652,5.2882044151365,11.5196940987448));
#109370=CARTESIAN_POINT('Ctrl Pts',(-11.3714473246283,5.28770485840317,
11.5109325909669));
#109371=CARTESIAN_POINT('Ctrl Pts',(-11.383585847489,5.28582704331821,11.4777021494433));
#109372=CARTESIAN_POINT('Ctrl Pts',(-11.3918596346968,5.28446734965808,
11.4530298071265));
#109373=CARTESIAN_POINT('Ctrl Pts',(-11.4111225462403,5.2810736224459,11.3900659779375));
#109374=CARTESIAN_POINT('Ctrl Pts',(-11.4212146428339,5.27906643000164,
11.3515217464882));
#109375=CARTESIAN_POINT('Ctrl Pts',(-11.4522441215614,5.27185225915579,
11.2096092834566));
#109376=CARTESIAN_POINT('Ctrl Pts',(-11.4635668322466,5.26686403610331,
11.1044858904008));
#109377=CARTESIAN_POINT('Ctrl Pts',(-11.4634997032748,5.26158528452068,
10.9990680587078));
#109378=CARTESIAN_POINT('Ctrl Pts',(-11.4634997007504,5.18934561127431,
10.9990641028533));
#109379=CARTESIAN_POINT('Ctrl Pts',(-11.4635344412489,5.1923113975619,11.0533892061211));
#109380=CARTESIAN_POINT('Ctrl Pts',(-11.4605401187862,5.1952771838495,11.107830788412));
#109381=CARTESIAN_POINT('Ctrl Pts',(-11.4545042019612,5.19824297013709,
11.1620178276524));
#109382=CARTESIAN_POINT('Ctrl Pts',(-11.4484754290084,5.20120524623744,
11.2161407332582));
#109383=CARTESIAN_POINT('Ctrl Pts',(-11.4394122436747,5.20416752233779,
11.2700091551932));
#109384=CARTESIAN_POINT('Ctrl Pts',(-11.4273541165932,5.20712979843813,
11.3232529595293));
#109385=CARTESIAN_POINT('Ctrl Pts',(-11.4153051826419,5.21008981609572,
11.3764561707266));
#109386=CARTESIAN_POINT('Ctrl Pts',(-11.4002659467465,5.2130498337533,11.4290351781191));
#109387=CARTESIAN_POINT('Ctrl Pts',(-11.3823272438335,5.21600985141088,
11.4806283813465));
#109388=CARTESIAN_POINT('Ctrl Pts',(-11.3643946646374,5.21896885861022,
11.5322039722542));
#109389=CARTESIAN_POINT('Ctrl Pts',(-11.3435647590433,5.22192786580955,
11.582793912705));
#109390=CARTESIAN_POINT('Ctrl Pts',(-11.319977939129,5.22488687300889,11.6320526008275));
#109391=CARTESIAN_POINT('Ctrl Pts',(-11.2963724811946,5.22784821837996,
11.6813502125701));
#109392=CARTESIAN_POINT('Ctrl Pts',(-11.2700059889758,5.23080956375103,
11.729313977122));
#109393=CARTESIAN_POINT('Ctrl Pts',(-11.2410659713646,5.2337709091221,11.7756207222095));
#109394=CARTESIAN_POINT('Ctrl Pts',(-11.2121150934498,5.23673336579552,
11.8219448448023));
#109395=CARTESIAN_POINT('Ctrl Pts',(-11.1805890795016,5.23969582246895,
11.8666102632355));
#109396=CARTESIAN_POINT('Ctrl Pts',(-11.1467182142998,5.24265827914237,
11.9093236975869));
#109397=CARTESIAN_POINT('Ctrl Pts',(-11.1127842183309,5.2456262574392,11.9521167440727));
#109398=CARTESIAN_POINT('Ctrl Pts',(-11.0764970050056,5.24859423573603,
11.9929501330113));
#109399=CARTESIAN_POINT('Ctrl Pts',(-11.0381255798866,5.25156221403285,
12.0315655725086));
#109400=CARTESIAN_POINT('Ctrl Pts',(-11.0075603484484,5.25392639371253,
12.0623251766064));
#109401=CARTESIAN_POINT('Ctrl Pts',(-10.9756734759043,5.2562905733922,12.0916781261071));
#109402=CARTESIAN_POINT('Ctrl Pts',(-10.9426152373223,5.25865475307187,
12.1195127352415));
#109403=CARTESIAN_POINT('Ctrl Pts',(-10.9005236294952,5.26166495954922,
12.1549533243944));
#109404=CARTESIAN_POINT('Ctrl Pts',(-10.8563421100876,5.26467516602657,
12.1880911796638));
#109405=CARTESIAN_POINT('Ctrl Pts',(-10.8103525819758,5.26768537250392,
12.2186717945719));
#109406=CARTESIAN_POINT('Ctrl Pts',(-10.7644447514548,5.27069023153313,
12.2491980848835));
#109407=CARTESIAN_POINT('Ctrl Pts',(-10.7167357223031,5.27369509056234,
12.2771758599914));
#109408=CARTESIAN_POINT('Ctrl Pts',(-10.667540039108,5.27669994959155,12.3023910880329));
#109409=CARTESIAN_POINT('Ctrl Pts',(-10.6183930013213,5.27970183737237,
12.3275813828896));
#109410=CARTESIAN_POINT('Ctrl Pts',(-10.567762689191,5.28270372515319,12.3500143022685));
#109411=CARTESIAN_POINT('Ctrl Pts',(-10.5159905746625,5.28570561293401,
12.3695203455442));
#109412=CARTESIAN_POINT('Ctrl Pts',(-10.464249207591,5.28870571789379,12.3890148041814));
#109413=CARTESIAN_POINT('Ctrl Pts',(-10.4113678753837,5.29170582285357,
12.40558564628));
#109414=CARTESIAN_POINT('Ctrl Pts',(-10.3577083591411,5.29470592781335,
12.4191113345332));
#109415=CARTESIAN_POINT('Ctrl Pts',(-10.3040595216126,5.29770543572594,
12.4326343310558));
#109416=CARTESIAN_POINT('Ctrl Pts',(-10.2496333193866,5.30070494363854,
12.4431132482567));
#109417=CARTESIAN_POINT('Ctrl Pts',(-10.1948047908919,5.30370445155113,
12.4504769365438));
#109418=CARTESIAN_POINT('Ctrl Pts',(-10.1399258685872,5.30670671636121,
12.457847392919));
#109419=CARTESIAN_POINT('Ctrl Pts',(-10.0846444057419,5.30970898117128,
12.4620968295451));
#109420=CARTESIAN_POINT('Ctrl Pts',(-10.0293421949471,5.31271124598135,
12.4632058247546));
#109421=CARTESIAN_POINT('Ctrl Pts',(-9.97401479689575,5.31571487816558,
12.4643153250532));
#109422=CARTESIAN_POINT('Ctrl Pts',(-9.91866716070167,5.31871851034982,
12.4622815521487));
#109423=CARTESIAN_POINT('Ctrl Pts',(-9.86367939318694,5.32172214253405,
12.4571372420462));
#109424=CARTESIAN_POINT('Ctrl Pts',(-9.80858793123272,5.32473143888633,
12.4519832309434));
#109425=CARTESIAN_POINT('Ctrl Pts',(-9.75385821704293,5.32774073523861,
12.4437070440616));
#109426=CARTESIAN_POINT('Ctrl Pts',(-9.69986239769726,5.33075003159089,
12.4323929871666));
#109427=CARTESIAN_POINT('Ctrl Pts',(-9.65866357676656,5.33304612530791,
12.423760359499));
#109428=CARTESIAN_POINT('Ctrl Pts',(-9.61789185484979,5.33534221902494,
12.4133602535439));
#109429=CARTESIAN_POINT('Ctrl Pts',(-9.57770581235786,5.33763831274196,
12.4012493957478));
#109430=CARTESIAN_POINT('Ctrl Pts',(-9.52502142744368,5.34064851921379,
12.3853719155532));
#109431=CARTESIAN_POINT('Ctrl Pts',(-9.47312310926445,5.34365872568562,
12.3664857125845));
#109432=CARTESIAN_POINT('Ctrl Pts',(-9.42237806430953,5.34666893215746,
12.3446877516395));
#109433=CARTESIAN_POINT('Ctrl Pts',(-9.37172316484394,5.34967379118038,
12.3229285134477));
#109434=CARTESIAN_POINT('Ctrl Pts',(-9.32221795418694,5.3526786502033,12.2982679890259));
#109435=CARTESIAN_POINT('Ctrl Pts',(-9.27421358566678,5.35568350922622,
12.2708525999381));
#109436=CARTESIAN_POINT('Ctrl Pts',(-9.22625668457319,5.35868539700029,
12.2434643195907));
#109437=CARTESIAN_POINT('Ctrl Pts',(-9.17979814208299,5.36168728477436,
12.2133268314117));
#109438=CARTESIAN_POINT('Ctrl Pts',(-9.13516653800798,5.36468917254843,
12.1806334456633));
#109439=CARTESIAN_POINT('Ctrl Pts',(-9.09056144064778,5.367689277501,12.1479594765206));
#109440=CARTESIAN_POINT('Ctrl Pts',(-9.04778155628123,5.37068938245357,
12.1127329299325));
#109441=CARTESIAN_POINT('Ctrl Pts',(-9.0071263998327,5.37368948740614,12.0751903385405));
#109442=CARTESIAN_POINT('Ctrl Pts',(-8.96647933412269,5.37668899531109,
12.0376552184589));
#109443=CARTESIAN_POINT('Ctrl Pts',(-8.92795654433096,5.37968850321604,
11.9978053269995));
#109444=CARTESIAN_POINT('Ctrl Pts',(-8.89182259597033,5.38268801112098,
11.9559158389723));
#109445=CARTESIAN_POINT('Ctrl Pts',(-8.85565543630597,5.38569027592277,
11.9139878496306));
#109446=CARTESIAN_POINT('Ctrl Pts',(-8.82188185029077,5.38869254072455,
11.8700169192059));
#109447=CARTESIAN_POINT('Ctrl Pts',(-8.79072677729523,5.39169480552634,
11.8243121513415));
#109448=CARTESIAN_POINT('Ctrl Pts',(-8.75955751480167,5.39469843770192,
11.7785865673578));
#109449=CARTESIAN_POINT('Ctrl Pts',(-8.73100941535191,5.39770206987751,
11.7311260250927));
#109450=CARTESIAN_POINT('Ctrl Pts',(-8.70526281930563,5.40070570205309,
11.6822667241831));
#109451=CARTESIAN_POINT('Ctrl Pts',(-8.67946767103144,5.40371499839623,
11.6333152857379));
#109452=CARTESIAN_POINT('Ctrl Pts',(-8.65648479953044,5.40672429473936,
11.5829603009542));
#109453=CARTESIAN_POINT('Ctrl Pts',(-8.63644700932875,5.4097335910825,11.5315594902092));
#109454=CARTESIAN_POINT('Ctrl Pts',(-8.62115817096553,5.41202968485902,
11.492340660223));
#109455=CARTESIAN_POINT('Ctrl Pts',(-8.60758288415365,5.41432577863554,
11.4525134434279));
#109456=CARTESIAN_POINT('Ctrl Pts',(-8.59576032018933,5.41662187241205,
11.4122416422988));
#109457=CARTESIAN_POINT('Ctrl Pts',(-8.58026079688599,5.41963207892083,
11.3594448275003));
#109458=CARTESIAN_POINT('Ctrl Pts',(-8.5677104620999,5.4226422854296,11.3056618072144));
#109459=CARTESIAN_POINT('Ctrl Pts',(-8.55822881911808,5.42565249193837,
11.2512530835201));
#109460=CARTESIAN_POINT('Ctrl Pts',(-8.54876401969558,5.42865735099924,
11.1969410135984));
#109461=CARTESIAN_POINT('Ctrl Pts',(-8.54235718375553,5.43166221006011,
11.1420059621385));
#109462=CARTESIAN_POINT('Ctrl Pts',(-8.53907762460567,5.43466706912098,
11.0868220195123));
#109463=CARTESIAN_POINT('Ctrl Pts',(-8.53580130833152,5.43766895693358,
11.0316926435698));
#109464=CARTESIAN_POINT('Ctrl Pts',(-8.53564617431162,5.44067084474618,
10.9763153885533));
#109465=CARTESIAN_POINT('Ctrl Pts',(-8.5386299326001,5.44367273255878,10.921071069261));
#109466=CARTESIAN_POINT('Ctrl Pts',(-8.54161191883472,5.4466728375504,10.8658595595665));
#109467=CARTESIAN_POINT('Ctrl Pts',(-8.5477290739976,5.44967294254202,10.8107813553735));
#109468=CARTESIAN_POINT('Ctrl Pts',(-8.55694702714935,5.45267304753364,
10.7562165560443));
#109469=CARTESIAN_POINT('Ctrl Pts',(-8.56616314584764,5.45567255547808,
10.7016626155883));
#109470=CARTESIAN_POINT('Ctrl Pts',(-8.57847874910111,5.45867206342252,
10.6476223974979));
#109471=CARTESIAN_POINT('Ctrl Pts',(-8.59380800422581,5.46167157136696,
10.5944678545163));
#109472=CARTESIAN_POINT('Ctrl Pts',(-8.60915134872175,5.46467383620863,
10.5412644563175));
#109473=CARTESIAN_POINT('Ctrl Pts',(-8.62751373231333,5.46767610105029,
10.4889488680559));
#109474=CARTESIAN_POINT('Ctrl Pts',(-8.64875925144211,5.47067836589196,
10.4378784033354));
#109475=CARTESIAN_POINT('Ctrl Pts',(-8.67001444678982,5.47368199810769,
10.3867846786986));
#109476=CARTESIAN_POINT('Ctrl Pts',(-8.69415516470174,5.47668563032343,
10.336937684158));
#109477=CARTESIAN_POINT('Ctrl Pts',(-8.72099843466032,5.47968926253916,
10.2886721952161));
#109478=CARTESIAN_POINT('Ctrl Pts',(-8.7478923249234,5.4826985589224,10.2403156885349));
#109479=CARTESIAN_POINT('Ctrl Pts',(-8.77749866489277,5.48570785530564,
10.1935470924382));
#109480=CARTESIAN_POINT('Ctrl Pts',(-8.80959048072246,5.48871715168887,
10.1486731377353));
#109481=CARTESIAN_POINT('Ctrl Pts',(-8.83407653965581,5.49101324515329,
10.1144343054655));
#109482=CARTESIAN_POINT('Ctrl Pts',(-8.86000864186209,5.49330933861771,
10.0812979025415));
#109483=CARTESIAN_POINT('Ctrl Pts',(-8.88727102647093,5.49560543208213,
10.0493862606353));
#109484=CARTESIAN_POINT('Ctrl Pts',(-8.92301234464173,5.49861563857137,
10.007549709538));
#109485=CARTESIAN_POINT('Ctrl Pts',(-8.96119145638884,5.50162584506061,
9.96764382578134));
#109486=CARTESIAN_POINT('Ctrl Pts',(-9.00157178841649,5.50463605154986,
9.92996572189758));
#109487=CARTESIAN_POINT('Ctrl Pts',(-9.04188038724669,5.50764091059083,
9.89235455086778));
#109488=CARTESIAN_POINT('Ctrl Pts',(-9.08438206327088,5.5106457696318,9.85696366333679));
#109489=CARTESIAN_POINT('Ctrl Pts',(-9.12880143194597,5.51365062867278,
9.82405556890616));
#109490=CARTESIAN_POINT('Ctrl Pts',(-9.17317687810099,5.51665251646528,
9.79118001447963));
#109491=CARTESIAN_POINT('Ctrl Pts',(-9.21946583829074,5.51965440425778,
9.76078270267316));
#109492=CARTESIAN_POINT('Ctrl Pts',(-9.26735909218071,5.52265629205027,
9.73308660509499));
#109493=CARTESIAN_POINT('Ctrl Pts',(-9.31522390226739,5.52565639702162,
9.70540695622907));
#109494=CARTESIAN_POINT('Ctrl Pts',(-9.36469066131898,5.52865650199297,
9.68042560568449));
#109495=CARTESIAN_POINT('Ctrl Pts',(-9.41542228234622,5.53165660696432,
9.65832152062325));
#109496=CARTESIAN_POINT('Ctrl Pts',(-9.46614380733411,5.53465611488836,
9.6362218344696));
#109497=CARTESIAN_POINT('Ctrl Pts',(-9.5181292105367,5.5376556228124,9.61699848744594));
#109498=CARTESIAN_POINT('Ctrl Pts',(-9.57102009975651,5.54065513073644,
9.60078289919431));
#109499=CARTESIAN_POINT('Ctrl Pts',(-9.62395960186442,5.54365739555766,
9.58455240692823));
#109500=CARTESIAN_POINT('Ctrl Pts',(-9.6778057467329,5.54665966037887,9.5713353516049));
#109501=CARTESIAN_POINT('Ctrl Pts',(-9.73218503409507,5.54966192520009,
9.5612132214823));
#109502=CARTESIAN_POINT('Ctrl Pts',(-9.78658908836782,5.55266555739531,
9.55108648126082));
#109503=CARTESIAN_POINT('Ctrl Pts',(-9.84152624445177,5.55566918959054,
9.54405754326308));
#109504=CARTESIAN_POINT('Ctrl Pts',(-9.89661615056347,5.55867282178577,
9.54015616257228));
#109505=CARTESIAN_POINT('Ctrl Pts',(-9.95180994371746,5.56168211814866,
9.53624742476419));
#109506=CARTESIAN_POINT('Ctrl Pts',(-10.007156533005,5.56469141451155,9.53547803346949));
#109507=CARTESIAN_POINT('Ctrl Pts',(-10.0622750009097,5.56770071087444,
9.53782556640403));
#109508=CARTESIAN_POINT('Ctrl Pts',(-10.104330401098,5.56999680450037,9.53961673442394));
#109509=CARTESIAN_POINT('Ctrl Pts',(-10.1462529703101,5.5722928981263,9.54322139313254));
#109510=CARTESIAN_POINT('Ctrl Pts',(-10.1878769950017,5.57458899175222,
9.5486094651166));
#109511=CARTESIAN_POINT('Ctrl Pts',(-10.242446594371,5.57759919824257,9.55567329259896));
#109512=CARTESIAN_POINT('Ctrl Pts',(-10.2967318420896,5.58060940473292,
9.5658338050913));
#109513=CARTESIAN_POINT('Ctrl Pts',(-10.3503546283818,5.58361961122327,
9.57905528454784));
#109514=CARTESIAN_POINT('Ctrl Pts',(-10.4038821570629,5.58662447026528,
9.59225327685206));
#109515=CARTESIAN_POINT('Ctrl Pts',(-10.4567490511495,5.58962932930729,
9.60850131970296));
#109516=CARTESIAN_POINT('Ctrl Pts',(-10.5085849649228,5.5926341883493,9.62771228109608));
#109517=CARTESIAN_POINT('Ctrl Pts',(-10.5603696225872,5.59563607614279,
9.64690424640994));
#109518=CARTESIAN_POINT('Ctrl Pts',(-10.6111248266843,5.59863796393629,
9.66905314388547));
#109519=CARTESIAN_POINT('Ctrl Pts',(-10.6604948476701,5.60163985172978,
9.69402189673743));
#109520=CARTESIAN_POINT('Ctrl Pts',(-10.7098355477998,5.60463995670208,
9.7189758206468));
#109521=CARTESIAN_POINT('Ctrl Pts',(-10.757792225087,5.60764006167438,9.74674604267606));
#109522=CARTESIAN_POINT('Ctrl Pts',(-10.8040307689732,5.61064016664668,
9.77714809868718));
#109523=CARTESIAN_POINT('Ctrl Pts',(-10.8502601109811,5.61363967457162,
9.80754410442088));
#109524=CARTESIAN_POINT('Ctrl Pts',(-10.8947715576388,5.61663918249656,
9.84057061400552));
#109525=CARTESIAN_POINT('Ctrl Pts',(-10.9372591706691,5.61963869042149,
9.87599933407643));
#109526=CARTESIAN_POINT('Ctrl Pts',(-10.9797858347639,5.62264095524354,
9.91146061726712));
#109527=CARTESIAN_POINT('Ctrl Pts',(-11.0202845424836,5.62564322006558,
9.94932818312116));
#109528=CARTESIAN_POINT('Ctrl Pts',(-11.0584829112703,5.62864548488763,
9.98933379568286));
#109529=CARTESIAN_POINT('Ctrl Pts',(-11.0966986774081,5.63164911708365,
10.0293576287004));
#109530=CARTESIAN_POINT('Ctrl Pts',(-11.1326116731147,5.63465274927966,
10.0715210468442));
#109531=CARTESIAN_POINT('Ctrl Pts',(-11.1659890931607,5.63765638147568,
10.1155218009299));
#109532=CARTESIAN_POINT('Ctrl Pts',(-11.1994294554341,5.64066567783928,
10.1596055304363));
#109533=CARTESIAN_POINT('Ctrl Pts',(-11.2303243947869,5.64367497420289,
10.2055330780896));
#109534=CARTESIAN_POINT('Ctrl Pts',(-11.258484490896,5.64668427056649,10.2529732025059));
#109535=CARTESIAN_POINT('Ctrl Pts',(-11.2799706488423,5.64898036418509,
10.2891700252103));
#109536=CARTESIAN_POINT('Ctrl Pts',(-11.2998655611633,5.6512764578037,10.3262468080652));
#109537=CARTESIAN_POINT('Ctrl Pts',(-11.3181038415257,5.65357255142231,
10.3640483407089));
#109538=CARTESIAN_POINT('Ctrl Pts',(-11.343785672609,5.6568057448645,10.4172777327763));
#109539=CARTESIAN_POINT('Ctrl Pts',(-11.3662764748868,5.66003893830669,
10.4721417934287));
#109540=CARTESIAN_POINT('Ctrl Pts',(-11.3853830805078,5.66327213174888,
10.5282522175539));
#109541=CARTESIAN_POINT('Ctrl Pts',(-11.4044415639912,5.66649718202937,
10.5842213212585));
#109542=CARTESIAN_POINT('Ctrl Pts',(-11.4201326703982,5.66972223230985,
10.6414301682071));
#109543=CARTESIAN_POINT('Ctrl Pts',(-11.4323106215473,5.67294728259033,
10.6994695799044));
#109544=CARTESIAN_POINT('Ctrl Pts',(-11.4444430750598,5.67616028386819,
10.7572921524944));
#109545=CARTESIAN_POINT('Ctrl Pts',(-11.4530884204079,5.67937328514605,
10.8159387204676));
#109546=CARTESIAN_POINT('Ctrl Pts',(-11.4581508364159,5.68258628642391,
10.8749864476965));
#109547=CARTESIAN_POINT('Ctrl Pts',(-11.4617003573309,5.68483908730347,
10.9163878541492));
#109548=CARTESIAN_POINT('Ctrl Pts',(-11.4634894691637,5.68709188818304,
10.9579860868412));
#109549=CARTESIAN_POINT('Ctrl Pts',(-11.4634999536212,5.6893446890626,10.9996315564861));
#109550=CARTESIAN_POINT('Origin',(-10.,3.5,11.));
#109551=CARTESIAN_POINT('',(-11.4635,6.26064415683876,11.0000000000891));
#109552=CARTESIAN_POINT('',(-11.4635,6.189145110564,10.9999999999277));
#109553=CARTESIAN_POINT('',(-11.4635,3.5,11.));
#109554=CARTESIAN_POINT('Ctrl Pts',(-11.4635,6.26064415683876,11.0000000000891));
#109555=CARTESIAN_POINT('Ctrl Pts',(-11.463500000006,6.25468158645031,10.9008697580982));
#109556=CARTESIAN_POINT('Ctrl Pts',(-11.4534281618735,6.24879590921732,
10.8019773468397));
#109557=CARTESIAN_POINT('Ctrl Pts',(-11.430651981289,6.24244638816578,10.6913631549977));
#109558=CARTESIAN_POINT('Ctrl Pts',(-11.4276852120321,6.24167813351364,
10.6779181051389));
#109559=CARTESIAN_POINT('Ctrl Pts',(-11.4218987475142,6.2402804437222,10.6533476290882));
#109560=CARTESIAN_POINT('Ctrl Pts',(-11.4191370896103,6.23964925057465,
10.6422097740023));
#109561=CARTESIAN_POINT('Ctrl Pts',(-11.4145308461038,6.23865067548806,
10.6245256809034));
#109562=CARTESIAN_POINT('Ctrl Pts',(-11.4127711709199,6.23828060963525,
10.617957987041));
#109563=CARTESIAN_POINT('Ctrl Pts',(-11.4093597359101,6.23758410218281,
10.6055713383786));
#109564=CARTESIAN_POINT('Ctrl Pts',(-11.4077175513289,6.23725736278335,
10.5997499137986));
#109565=CARTESIAN_POINT('Ctrl Pts',(-11.4039194350033,6.23652050575121,
10.5865984466453));
#109566=CARTESIAN_POINT('Ctrl Pts',(-11.4017420881184,6.23611108503517,
10.57927473847));
#109567=CARTESIAN_POINT('Ctrl Pts',(-11.3959785985095,6.2350597932708,10.5604302297379));
#109568=CARTESIAN_POINT('Ctrl Pts',(-11.3923071187277,6.23442067481777,
10.5489360034574));
#109569=CARTESIAN_POINT('Ctrl Pts',(-11.3626723958532,6.22948775571548,
10.4599704120041));
#109570=CARTESIAN_POINT('Ctrl Pts',(-11.3304038902835,6.22541035961006,
10.3847475118716));
#109571=CARTESIAN_POINT('Ctrl Pts',(-11.2877604284509,6.22096502876809,
10.3045953515623));
#109572=CARTESIAN_POINT('Ctrl Pts',(-11.2834251126999,6.22052175378133,
10.2966263243695));
#109573=CARTESIAN_POINT('Ctrl Pts',(-11.2389352487734,6.21605502547736,
10.2166275988383));
#109574=CARTESIAN_POINT('Ctrl Pts',(-11.1928373310914,6.21209729880708,
10.148078462951));
#109575=CARTESIAN_POINT('Ctrl Pts',(-11.1206139507306,6.20625438657933,
10.0581191218579));
#109576=CARTESIAN_POINT('Ctrl Pts',(-11.0991534708841,6.2045534982045,10.0331615667196));
#109577=CARTESIAN_POINT('Ctrl Pts',(-11.072163524223,6.20242633165054,10.0038343672439));
#109578=CARTESIAN_POINT('Ctrl Pts',(-11.06741897992,6.20205282048312,9.99875212456149));
#109579=CARTESIAN_POINT('Ctrl Pts',(-11.0598922158294,6.20146057824844,
9.99080393721421));
#109580=CARTESIAN_POINT('Ctrl Pts',(-11.0571341080158,6.20124361882877,
9.98791518180678));
#109581=CARTESIAN_POINT('Ctrl Pts',(-11.0520189543992,6.20084128168649,
9.9826014518897));
#109582=CARTESIAN_POINT('Ctrl Pts',(-11.0496652999348,6.20065615887383,
9.98017332670547));
#109583=CARTESIAN_POINT('Ctrl Pts',(-11.0442992224879,6.20023412125252,
9.97467571956473));
#109584=CARTESIAN_POINT('Ctrl Pts',(-11.0412816850758,6.19999681772598,
9.97161135872589));
#109585=CARTESIAN_POINT('Ctrl Pts',(-11.0333978981535,6.19937699611587,
9.96367551124866));
#109586=CARTESIAN_POINT('Ctrl Pts',(-11.0285107528044,6.19899293758773,
9.95882504374669));
#109587=CARTESIAN_POINT('Ctrl Pts',(-10.9951073239107,6.19637021401389,
9.92613698475134));
#109588=CARTESIAN_POINT('Ctrl Pts',(-10.9655006423753,6.1940572193856,9.89944180101318));
#109589=CARTESIAN_POINT('Ctrl Pts',(-10.8521258426725,6.18535631354391,
9.8053149155226));
#109590=CARTESIAN_POINT('Ctrl Pts',(-10.762090541751,6.17877269448143,9.74596194987916));
#109591=CARTESIAN_POINT('Ctrl Pts',(-10.6310102219934,6.17012074557002,
9.67892666276233));
#109592=CARTESIAN_POINT('Ctrl Pts',(-10.5949376411045,6.16782328053937,
9.66229366129145));
#109593=CARTESIAN_POINT('Ctrl Pts',(-10.534233528875,6.16410014637168,9.63724517479193));
#109594=CARTESIAN_POINT('Ctrl Pts',(-10.5099759310201,6.16264854528252,
9.62798292757365));
#109595=CARTESIAN_POINT('Ctrl Pts',(-10.4766603218739,6.16070272563627,
9.61626784941353));
#109596=CARTESIAN_POINT('Ctrl Pts',(-10.4678073367868,6.1601901657414,9.61324983204027));
#109597=CARTESIAN_POINT('Ctrl Pts',(-10.4529056764005,6.15933480694297,
9.60832874079627));
#109598=CARTESIAN_POINT('Ctrl Pts',(-10.4468725517433,6.15899052367183,
9.60637976131909));
#109599=CARTESIAN_POINT('Ctrl Pts',(-10.4349518180935,6.15831417285298,
9.60261418122248));
#109600=CARTESIAN_POINT('Ctrl Pts',(-10.4290650293143,6.1579820416617,9.6007954356872));
#109601=CARTESIAN_POINT('Ctrl Pts',(-10.4160851123234,6.1572537500392,9.59687486087051));
#109602=CARTESIAN_POINT('Ctrl Pts',(-10.4089871544659,6.15685812645046,
9.59478952219154));
#109603=CARTESIAN_POINT('Ctrl Pts',(-10.3839773469203,6.15547314938425,
9.58764733777428));
#109604=CARTESIAN_POINT('Ctrl Pts',(-10.3659847389951,6.15449298071503,
9.58287831954562));
#109605=CARTESIAN_POINT('Ctrl Pts',(-10.2558684471843,6.14858425230046,
9.55592874864663));
#109606=CARTESIAN_POINT('Ctrl Pts',(-10.1618595433146,6.14394035810551,
9.54239434931393));
#109607=CARTESIAN_POINT('Ctrl Pts',(-9.97470908243032,6.13482118376619,
9.53379259654499));
#109608=CARTESIAN_POINT('Ctrl Pts',(-9.88203954894,6.13035863826809,9.53832789996629));
#109609=CARTESIAN_POINT('Ctrl Pts',(-9.77616284332801,6.1247583683835,9.55364698991818));
#109610=CARTESIAN_POINT('Ctrl Pts',(-9.76192614438314,6.12399444596427,
9.55592212437193));
#109611=CARTESIAN_POINT('Ctrl Pts',(-9.74257976371953,6.12293870615667,
9.55930767827695));
#109612=CARTESIAN_POINT('Ctrl Pts',(-9.7374385466064,6.12265644299577,9.560235774357));
#109613=CARTESIAN_POINT('Ctrl Pts',(-9.72883492021662,6.122181064772,9.5618365218929));
#109614=CARTESIAN_POINT('Ctrl Pts',(-9.72536972433999,6.12198877831556,
9.56249420816729));
#109615=CARTESIAN_POINT('Ctrl Pts',(-9.71880265285195,6.12162274769433,
9.56376523516815));
#109616=CARTESIAN_POINT('Ctrl Pts',(-9.71570032486233,6.12144914751057,
9.56437611399104));
#109617=CARTESIAN_POINT('Ctrl Pts',(-9.70836612330892,6.12103715891014,
9.5658449954833));
#109618=CARTESIAN_POINT('Ctrl Pts',(-9.70413604307504,6.12079829274913,
9.56671167832684));
#109619=CARTESIAN_POINT('Ctrl Pts',(-9.68937994587993,6.11996082956113,
9.56980309787453));
#109620=CARTESIAN_POINT('Ctrl Pts',(-9.67887493033025,6.11935714154363,
9.57212512005518));
#109621=CARTESIAN_POINT('Ctrl Pts',(-9.566922276486,6.11285036928516,9.59816895866746));
#109622=CARTESIAN_POINT('Ctrl Pts',(-9.46826517280139,6.10649452775306,
9.63254167021684));
#109623=CARTESIAN_POINT('Ctrl Pts',(-9.31539704671918,6.09635222401178,
9.70486739555222));
#109624=CARTESIAN_POINT('Ctrl Pts',(-9.25860345323244,6.09250533866046,
9.73651980365157));
#109625=CARTESIAN_POINT('Ctrl Pts',(-9.17368509345593,6.08669432250208,
9.79155093279611));
#109626=CARTESIAN_POINT('Ctrl Pts',(-9.14401494811772,6.08465063039165,
9.81238247479895));
#109627=CARTESIAN_POINT('Ctrl Pts',(-9.10675271694636,6.08206567258003,
9.84066717386384));
#109628=CARTESIAN_POINT('Ctrl Pts',(-9.09842751197536,6.08148686470424,
9.84712950970302));
#109629=CARTESIAN_POINT('Ctrl Pts',(-9.08500778697391,6.08055160584312,
9.85778067741105));
#109630=CARTESIAN_POINT('Ctrl Pts',(-9.07987060044323,6.08019303202526,
9.86191493251127));
#109631=CARTESIAN_POINT('Ctrl Pts',(-9.07003654436081,6.07950549071964,
9.8699392006974));
#109632=CARTESIAN_POINT('Ctrl Pts',(-9.06533571250799,6.07917633140616,
9.87382412111696));
#109633=CARTESIAN_POINT('Ctrl Pts',(-9.05460067019202,6.0784234117105,9.88280942565999));
#109634=CARTESIAN_POINT('Ctrl Pts',(-9.04858317536251,6.07800045697459,
9.88792954301572));
#109635=CARTESIAN_POINT('Ctrl Pts',(-9.0295064064749,6.07665642146172,9.90442961403695));
#109636=CARTESIAN_POINT('Ctrl Pts',(-9.01660732180629,6.07574283202611,
9.91599300769827));
#109637=CARTESIAN_POINT('Ctrl Pts',(-8.89865904575401,6.06733379481988,
10.0255663205996));
#109638=CARTESIAN_POINT('Ctrl Pts',(-8.80838211625585,6.06058130811177,
10.1383047984967));
#109639=CARTESIAN_POINT('Ctrl Pts',(-8.70810989499425,6.05074622164784,
10.3101386046344));
#109640=CARTESIAN_POINT('Ctrl Pts',(-8.68297629057774,6.04795677449364,
10.3594251658984));
#109641=CARTESIAN_POINT('Ctrl Pts',(-8.65755062505719,6.04459797572021,
10.41714265703));
#109642=CARTESIAN_POINT('Ctrl Pts',(-8.65446542243667,6.04417984271746,
10.4243006845394));
#109643=CARTESIAN_POINT('Ctrl Pts',(-8.64985034858313,6.04353746870808,
10.4352479621997));
#109644=CARTESIAN_POINT('Ctrl Pts',(-8.64827887770282,6.04331563025753,
10.4390196508486));
#109645=CARTESIAN_POINT('Ctrl Pts',(-8.64543769417484,6.04290873903866,
10.4459200324381));
#109646=CARTESIAN_POINT('Ctrl Pts',(-8.64416299569114,6.04272398547366,
10.449046582715));
#109647=CARTESIAN_POINT('Ctrl Pts',(-8.64133047038344,6.04230846503045,
10.4560634957915));
#109648=CARTESIAN_POINT('Ctrl Pts',(-8.63977853956789,6.04207736100753,
10.4599561230735));
#109649=CARTESIAN_POINT('Ctrl Pts',(-8.63529592710011,6.0413997952144,10.4713415333798));
#109650=CARTESIAN_POINT('Ctrl Pts',(-8.63241033577073,6.04095080983986,
10.4788517626643));
#109651=CARTESIAN_POINT('Ctrl Pts',(-8.61000061901428,6.03736224893733,
10.5386447660254));
#109652=CARTESIAN_POINT('Ctrl Pts',(-8.5934214887583,6.03407862599628,10.5919771717417));
#109653=CARTESIAN_POINT('Ctrl Pts',(-8.55994771052658,6.02581151713361,
10.7263027446489));
#109654=CARTESIAN_POINT('Ctrl Pts',(-8.54679227229088,6.02079153274629,
10.8080386513347));
#109655=CARTESIAN_POINT('Ctrl Pts',(-8.53599821490542,6.01226981040269,
10.9518317012995));
#109656=CARTESIAN_POINT('Ctrl Pts',(-8.53526726654161,6.00871318162902,
11.0134498120937));
#109657=CARTESIAN_POINT('Ctrl Pts',(-8.53924543824087,6.00437330895556,
11.0910404204562));
#109658=CARTESIAN_POINT('Ctrl Pts',(-8.54033717277281,6.00348070107881,
11.1071293971752));
#109659=CARTESIAN_POINT('Ctrl Pts',(-8.54234799401081,6.00217056282188,
11.1309317566409));
#109660=CARTESIAN_POINT('Ctrl Pts',(-8.54306290932061,6.00174676488769,
11.1386607821215));
#109661=CARTESIAN_POINT('Ctrl Pts',(-8.54444560600152,6.0009953896149,11.1524152259739));
#109662=CARTESIAN_POINT('Ctrl Pts',(-8.54508939561608,6.0006670770928,11.1584428280959));
#109663=CARTESIAN_POINT('Ctrl Pts',(-8.54652677103316,5.99997678764282,
11.171152260392));
#109664=CARTESIAN_POINT('Ctrl Pts',(-8.54732902675747,5.99961508791348,
11.1778329809677));
#109665=CARTESIAN_POINT('Ctrl Pts',(-8.54958334753883,5.99865765595457,
11.1955713654895));
#109666=CARTESIAN_POINT('Ctrl Pts',(-8.55111579628466,5.99806442932944,
11.2066184843933));
#109667=CARTESIAN_POINT('Ctrl Pts',(-8.55846922427464,5.99545112532016,
11.2555144430481));
#109668=CARTESIAN_POINT('Ctrl Pts',(-8.5656483167018,5.99347343793423,11.2931453164796));
#109669=CARTESIAN_POINT('Ctrl Pts',(-8.60632568254466,5.98433942074173,
11.4686432156434));
#109670=CARTESIAN_POINT('Ctrl Pts',(-8.65827055332199,5.97776955788723,
11.6014231125141));
#109671=CARTESIAN_POINT('Ctrl Pts',(-8.73869416933328,5.9695144334023,11.7425389020239));
#109672=CARTESIAN_POINT('Ctrl Pts',(-8.74926803588948,5.9684535859667,11.7602143792621));
#109673=CARTESIAN_POINT('Ctrl Pts',(-8.76743067278315,5.9666608832001,11.7891702689197));
#109674=CARTESIAN_POINT('Ctrl Pts',(-8.77481014694678,5.96593998170809,
11.8005789515333));
#109675=CARTESIAN_POINT('Ctrl Pts',(-8.78517942399309,5.96493471021708,
11.8161306784213));
#109676=CARTESIAN_POINT('Ctrl Pts',(-8.78803388935176,5.9646587521615,11.8203636152517));
#109677=CARTESIAN_POINT('Ctrl Pts',(-8.79288401360932,5.96419100340557,
11.8274753865341));
#109678=CARTESIAN_POINT('Ctrl Pts',(-8.79486799567978,5.96399998301618,
11.8303621931434));
#109679=CARTESIAN_POINT('Ctrl Pts',(-8.79867515680284,5.96363396998255,
11.8358594435637));
#109680=CARTESIAN_POINT('Ctrl Pts',(-8.800496520631,5.96345910523305,11.8384711031749));
#109681=CARTESIAN_POINT('Ctrl Pts',(-8.80485795815687,5.96304097903037,
11.8446816880644));
#109682=CARTESIAN_POINT('Ctrl Pts',(-8.80740577152801,5.96279720649603,
11.8482751083982));
#109683=CARTESIAN_POINT('Ctrl Pts',(-8.81653132384033,5.96192595345758,
11.861023356524));
#109684=CARTESIAN_POINT('Ctrl Pts',(-8.82319840302699,5.96129284472315,
11.8701133912286));
#109685=CARTESIAN_POINT('Ctrl Pts',(-8.88932645771598,5.95505351759766,
11.9581234177758));
#109686=CARTESIAN_POINT('Ctrl Pts',(-8.95652719445512,5.94904269562805,
12.0309016967563));
#109687=CARTESIAN_POINT('Ctrl Pts',(-9.08164779529878,5.93901307299818,
12.141540878415));
#109688=CARTESIAN_POINT('Ctrl Pts',(-9.13585535488944,5.9349614775753,12.1831068988301));
#109689=CARTESIAN_POINT('Ctrl Pts',(-9.21341639038986,5.92961487194081,
12.2343950599313));
#109690=CARTESIAN_POINT('Ctrl Pts',(-9.23440694465341,5.92820866170775,
12.2475224700076));
#109691=CARTESIAN_POINT('Ctrl Pts',(-9.2714095297554,5.92579973020932,12.2693778632288));
#109692=CARTESIAN_POINT('Ctrl Pts',(-9.28726990844085,5.92478866802482,
12.2783505354414));
#109693=CARTESIAN_POINT('Ctrl Pts',(-9.31046095609257,5.92334051850038,
12.2909045549492));
#109694=CARTESIAN_POINT('Ctrl Pts',(-9.31766006318078,5.92289510484147,
12.2947242476409));
#109695=CARTESIAN_POINT('Ctrl Pts',(-9.33031655222631,5.9221191369893,12.3013046247338));
#109696=CARTESIAN_POINT('Ctrl Pts',(-9.33575998453134,5.92178767369947,
12.3040915803712));
#109697=CARTESIAN_POINT('Ctrl Pts',(-9.34706727987358,5.92110377654723,
12.3097915790624));
#109698=CARTESIAN_POINT('Ctrl Pts',(-9.35293355154243,5.92075152307699,
12.3126995584584));
#109699=CARTESIAN_POINT('Ctrl Pts',(-9.36810030600404,5.91984725550665,
12.3200915221431));
#109700=CARTESIAN_POINT('Ctrl Pts',(-9.37742916571599,5.9192972626419,12.3245166717272));
#109701=CARTESIAN_POINT('Ctrl Pts',(-9.41494620054885,5.9171093455325,12.3418289427692));
#109702=CARTESIAN_POINT('Ctrl Pts',(-9.44349472361689,5.91549831552876,
12.3539183558332));
#109703=CARTESIAN_POINT('Ctrl Pts',(-9.60328906756971,5.90673391503435,
12.4156770729975));
#109704=CARTESIAN_POINT('Ctrl Pts',(-9.7407494839937,5.90020171935599,12.4471716880945));
#109705=CARTESIAN_POINT('Ctrl Pts',(-9.92083274204873,5.89113470822527,
12.4619150778616));
#109706=CARTESIAN_POINT('Ctrl Pts',(-9.96119843300378,5.88906389013771,
12.4635426379631));
#109707=CARTESIAN_POINT('Ctrl Pts',(-10.0088699210632,5.88652104768634,
12.4634912958913));
#109708=CARTESIAN_POINT('Ctrl Pts',(-10.0161633469098,5.88612931754385,
12.4634289154214));
#109709=CARTESIAN_POINT('Ctrl Pts',(-10.0274352523485,5.88551933255902,
12.4632482347966));
#109710=CARTESIAN_POINT('Ctrl Pts',(-10.0314143293995,5.88530312212138,
12.4631682161845));
#109711=CARTESIAN_POINT('Ctrl Pts',(-10.0387750524838,5.88490145469829,
12.4629901538958));
#109712=CARTESIAN_POINT('Ctrl Pts',(-10.0421567257087,5.88471624569875,
12.4628966145593));
#109713=CARTESIAN_POINT('Ctrl Pts',(-10.0498554038322,5.88429307570149,
12.4626569475945));
#109714=CARTESIAN_POINT('Ctrl Pts',(-10.054172088726,5.88405471726738,12.4625034329757));
#109715=CARTESIAN_POINT('Ctrl Pts',(-10.0654304041672,5.88343033789776,
12.4620531408435));
#109716=CARTESIAN_POINT('Ctrl Pts',(-10.0723706325022,5.88304274020497,
12.4617260386823));
#109717=CARTESIAN_POINT('Ctrl Pts',(-10.1205870278084,5.88033243510874,
12.4591093121567));
#109718=CARTESIAN_POINT('Ctrl Pts',(-10.1617491875743,5.87792979837102,
12.4551212468549));
#109719=CARTESIAN_POINT('Ctrl Pts',(-10.2406297538487,5.87322061327362,
12.4440905928907));
#109720=CARTESIAN_POINT('Ctrl Pts',(-10.2783518497674,5.87092160476448,
12.4372962118317));
#109721=CARTESIAN_POINT('Ctrl Pts',(-10.3747225849288,5.86498482981741,
12.416001848089));
#109722=CARTESIAN_POINT('Ctrl Pts',(-10.4328222622625,5.8613463099866,12.3993368872924));
#109723=CARTESIAN_POINT('Ctrl Pts',(-10.5313648372406,5.85517014089614,
12.3643444926323));
#109724=CARTESIAN_POINT('Ctrl Pts',(-10.5723132439562,5.85260135211813,
12.3476804323186));
#109725=CARTESIAN_POINT('Ctrl Pts',(-10.6294833023553,5.84902275284938,
12.321338280286));
#109726=CARTESIAN_POINT('Ctrl Pts',(-10.6463670062081,5.84796675597217,
12.313161763469));
#109727=CARTESIAN_POINT('Ctrl Pts',(-10.6761683010796,5.84610417196677,
12.2980153782613));
#109728=CARTESIAN_POINT('Ctrl Pts',(-10.6891468032443,5.84529347300159,
12.2911716381169));
#109729=CARTESIAN_POINT('Ctrl Pts',(-10.7085798662642,5.8440799448123,12.280547815017));
#109730=CARTESIAN_POINT('Ctrl Pts',(-10.7151117002444,5.84367211290044,
12.2769116619723));
#109731=CARTESIAN_POINT('Ctrl Pts',(-10.7268650342372,5.84293828681873,
12.2702503225802));
#109732=CARTESIAN_POINT('Ctrl Pts',(-10.7320961980485,5.84261168450075,
12.2672426043656));
#109733=CARTESIAN_POINT('Ctrl Pts',(-10.7432766352881,5.8419136009126,12.2607219459371));
#109734=CARTESIAN_POINT('Ctrl Pts',(-10.7492199515903,5.84154248526698,
12.257199048639));
#109735=CARTESIAN_POINT('Ctrl Pts',(-10.7651357047218,5.84054845522319,
12.247612047021));
#109736=CARTESIAN_POINT('Ctrl Pts',(-10.7750610277711,5.83992834111113,
12.2414704507844));
#109737=CARTESIAN_POINT('Ctrl Pts',(-10.8233422285407,5.8369092937055,12.2107902633161));
#109738=CARTESIAN_POINT('Ctrl Pts',(-10.8606137851685,5.83457183224753,
12.1845884995604));
#109739=CARTESIAN_POINT('Ctrl Pts',(-10.9841403881607,5.82671034511541,
12.0888371165977));
#109740=CARTESIAN_POINT('Ctrl Pts',(-11.0636853820692,5.82146967821963,
12.0112718929093));
#109741=CARTESIAN_POINT('Ctrl Pts',(-11.1664350503357,5.81341266616767,
11.8854027033054));
#109742=CARTESIAN_POINT('Ctrl Pts',(-11.1969993297778,5.81079252232597,
11.8436232877529));
#109743=CARTESIAN_POINT('Ctrl Pts',(-11.229495568897,5.80762691933193,11.7938716426076));
#109744=CARTESIAN_POINT('Ctrl Pts',(-11.2336552585333,5.80721377624935,
11.7873920477452));
#109745=CARTESIAN_POINT('Ctrl Pts',(-11.2399331126891,5.80657751500617,
11.7774410972377));
#109746=CARTESIAN_POINT('Ctrl Pts',(-11.2420883239202,5.80635672971682,
11.7739931384626));
#109747=CARTESIAN_POINT('Ctrl Pts',(-11.246007202858,5.80595084731565,11.7676650999878));
#109748=CARTESIAN_POINT('Ctrl Pts',(-11.247775295103,5.80576603995084,11.7647878579543));
#109749=CARTESIAN_POINT('Ctrl Pts',(-11.2517266142452,5.80534922840342,
11.7583076425111));
#109750=CARTESIAN_POINT('Ctrl Pts',(-11.2539042362142,5.80511687664165,
11.7547013733906));
#109751=CARTESIAN_POINT('Ctrl Pts',(-11.2602480636208,5.8044323027948,11.7440923758801));
#109752=CARTESIAN_POINT('Ctrl Pts',(-11.2643713227785,5.80397748014325,
11.7370643104111));
#109753=CARTESIAN_POINT('Ctrl Pts',(-11.3023823204292,5.79969363571814,
11.6710172597385));
#109754=CARTESIAN_POINT('Ctrl Pts',(-11.3321701018699,5.79565151853014,
11.6097416293405));
#109755=CARTESIAN_POINT('Ctrl Pts',(-11.3927064663139,5.78592380186845,
11.4593945914242));
#109756=CARTESIAN_POINT('Ctrl Pts',(-11.4193433606829,5.7802339626094,11.368974493906));
#109757=CARTESIAN_POINT('Ctrl Pts',(-11.4457820611401,5.77211814078187,
11.2316175052003));
#109758=CARTESIAN_POINT('Ctrl Pts',(-11.4523261255213,5.76951522049873,
11.1862307808025));
#109759=CARTESIAN_POINT('Ctrl Pts',(-11.457821008752,5.76634923678101,11.1293025905695));
#109760=CARTESIAN_POINT('Ctrl Pts',(-11.4587806178301,5.7657245705065,11.1179846290805));
#109761=CARTESIAN_POINT('Ctrl Pts',(-11.4601020403181,5.76473387787134,
11.0999007720322));
#109762=CARTESIAN_POINT('Ctrl Pts',(-11.4605487862389,5.76436524029729,
11.093141706839));
#109763=CARTESIAN_POINT('Ctrl Pts',(-11.4613058529663,5.76366994150187,
11.0803373612867));
#109764=CARTESIAN_POINT('Ctrl Pts',(-11.4616256254357,5.76334299511159,
11.07429279989));
#109765=CARTESIAN_POINT('Ctrl Pts',(-11.4622661527338,5.76260369142407,
11.060572041164));
#109766=CARTESIAN_POINT('Ctrl Pts',(-11.4625639829453,5.7621920498984,11.0528949188275));
#109767=CARTESIAN_POINT('Ctrl Pts',(-11.463270694087,5.76097192828551,11.0300316685418));
#109768=CARTESIAN_POINT('Ctrl Pts',(-11.4635036032574,5.76016886599224,
11.0148408779313));
#109769=CARTESIAN_POINT('Ctrl Pts',(-11.4634999578674,5.75937264475447,
10.9996488276474));
#109770=CARTESIAN_POINT('Ctrl Pts',(-11.4634999336402,5.69064613435915,
10.9995592789452));
#109771=CARTESIAN_POINT('Ctrl Pts',(-11.4635018158397,5.69099324829457,
11.0058094882762));
#109772=CARTESIAN_POINT('Ctrl Pts',(-11.4634636586465,5.69133914072625,
11.0120597265349));
#109773=CARTESIAN_POINT('Ctrl Pts',(-11.4633069419806,5.69202989168994,
11.0245852180884));
#109774=CARTESIAN_POINT('Ctrl Pts',(-11.4631880541147,5.69237473197048,
11.0308603209495));
#109775=CARTESIAN_POINT('Ctrl Pts',(-11.4628785535384,5.69304250044161,
11.0430540448561));
#109776=CARTESIAN_POINT('Ctrl Pts',(-11.4626923785698,5.69336555901081,
11.0489726483889));
#109777=CARTESIAN_POINT('Ctrl Pts',(-11.4622520981427,5.69400379743485,
11.060703324342));
#109778=CARTESIAN_POINT('Ctrl Pts',(-11.4619992489765,5.69431901010776,
11.0665153324534));
#109779=CARTESIAN_POINT('Ctrl Pts',(-11.4614260227125,5.69494536437348,
11.078100303415));
#109780=CARTESIAN_POINT('Ctrl Pts',(-11.4611060769315,5.69525651342251,
11.0838731811664));
#109781=CARTESIAN_POINT('Ctrl Pts',(-11.4601549556133,5.69608933733519,
11.099371722434));
#109782=CARTESIAN_POINT('Ctrl Pts',(-11.4594608206098,5.69660906162184,
11.1090933218267));
#109783=CARTESIAN_POINT('Ctrl Pts',(-11.4565053105407,5.69853958675306,
11.1453798823484));
#109784=CARTESIAN_POINT('Ctrl Pts',(-11.453615233189,5.69993101215188,11.1718892054966));
#109785=CARTESIAN_POINT('Ctrl Pts',(-11.4318802298353,5.70818535003896,
11.3308144042948));
#109786=CARTESIAN_POINT('Ctrl Pts',(-11.3956831478777,5.71446881975616,
11.4602022255253));
#109787=CARTESIAN_POINT('Ctrl Pts',(-11.3217986098834,5.72366742386944,
11.6303661184226));
#109788=CARTESIAN_POINT('Ctrl Pts',(-11.2986736785502,5.72628956170694,
11.6767264265003));
#109789=CARTESIAN_POINT('Ctrl Pts',(-11.2693452632507,5.72945751305295,
11.7284601454959));
#109790=CARTESIAN_POINT('Ctrl Pts',(-11.2654937575343,5.72987079994713,
11.7351306859564));
#109791=CARTESIAN_POINT('Ctrl Pts',(-11.2595283040555,5.73050727438153,
11.7452766232226));
#109792=CARTESIAN_POINT('Ctrl Pts',(-11.2574521663534,5.73072812735691,
11.7487742265598));
#109793=CARTESIAN_POINT('Ctrl Pts',(-11.2536250842806,5.73113413010189,
11.7551607841085));
#109794=CARTESIAN_POINT('Ctrl Pts',(-11.2518786940854,5.73131898991543,
11.7580523705641));
#109795=CARTESIAN_POINT('Ctrl Pts',(-11.2479312808657,5.73173591871051,
11.7645374585956));
#109796=CARTESIAN_POINT('Ctrl Pts',(-11.2457247556789,5.73196833545115,
11.7681274891187));
#109797=CARTESIAN_POINT('Ctrl Pts',(-11.2392049449242,5.73265310091989,
11.7786332813967));
#109798=CARTESIAN_POINT('Ctrl Pts',(-11.2348494244724,5.7331080515989,11.7855224854465));
#109799=CARTESIAN_POINT('Ctrl Pts',(-11.1944066929683,5.73730720135154,
11.8483238535662));
#109800=CARTESIAN_POINT('Ctrl Pts',(-11.1546059160706,5.74125525498306,
11.9017450485799));
#109801=CARTESIAN_POINT('Ctrl Pts',(-11.0719281981403,5.74887798584088,
11.9982314972652));
#109802=CARTESIAN_POINT('Ctrl Pts',(-11.029727482961,5.75253796344038,12.0417090925008));
#109803=CARTESIAN_POINT('Ctrl Pts',(-10.929084190016,5.76063360683702,12.1332876912415));
#109804=CARTESIAN_POINT('Ctrl Pts',(-10.8693553018973,5.76502107948247,
12.1797298247095));
#109805=CARTESIAN_POINT('Ctrl Pts',(-10.7978222489062,5.76979424140855,
12.2269535832448));
#109806=CARTESIAN_POINT('Ctrl Pts',(-10.7892867017011,5.77035668701215,
12.2324617422363));
#109807=CARTESIAN_POINT('Ctrl Pts',(-10.7748757565478,5.77129457251933,
12.2415502945528));
#109808=CARTESIAN_POINT('Ctrl Pts',(-10.7690313006929,5.77167175670782,
12.2451788758255));
#109809=CARTESIAN_POINT('Ctrl Pts',(-10.7575594193737,5.77240598825224,
12.2521897137076));
#109810=CARTESIAN_POINT('Ctrl Pts',(-10.7519343963433,5.7727631604787,12.2555755726135));
#109811=CARTESIAN_POINT('Ctrl Pts',(-10.7413107810232,5.77343246209394,
12.2618732252943));
#109812=CARTESIAN_POINT('Ctrl Pts',(-10.7363173543253,5.7737448900131,12.2647934478863));
#109813=CARTESIAN_POINT('Ctrl Pts',(-10.724682700833,5.7744678989753,12.2715052939605));
#109814=CARTESIAN_POINT('Ctrl Pts',(-10.718028774827,5.77487768168256,12.2752746413932));
#109815=CARTESIAN_POINT('Ctrl Pts',(-10.7007842929702,5.77593033981439,
12.2848656222116));
#109816=CARTESIAN_POINT('Ctrl Pts',(-10.6901505147949,5.77657045145195,
12.2906086048096));
#109817=CARTESIAN_POINT('Ctrl Pts',(-10.5968456511078,5.78211203073737,
12.3395167421728));
#109818=CARTESIAN_POINT('Ctrl Pts',(-10.5102926696713,5.78672444256759,
12.3748214091085));
#109819=CARTESIAN_POINT('Ctrl Pts',(-10.3569385672893,5.79453224801308,
12.4208784133698));
#109820=CARTESIAN_POINT('Ctrl Pts',(-10.2916781874053,5.79775525008546,
12.4356962729558));
#109821=CARTESIAN_POINT('Ctrl Pts',(-10.1808056222508,5.8033546033765,12.4529970134473));
#109822=CARTESIAN_POINT('Ctrl Pts',(-10.1356774862987,5.80566845286733,
12.4579032497131));
#109823=CARTESIAN_POINT('Ctrl Pts',(-10.0829175857108,5.80848625382296,
12.4611684044641));
#109824=CARTESIAN_POINT('Ctrl Pts',(-10.0754331290326,5.80888862218868,
12.4615739018387));
#109825=CARTESIAN_POINT('Ctrl Pts',(-10.0639267358958,5.80951170710604,
12.4621086868606));
#109826=CARTESIAN_POINT('Ctrl Pts',(-10.0599067206813,5.80973023837359,
12.4622789144981));
#109827=CARTESIAN_POINT('Ctrl Pts',(-10.0525080964303,5.81013406583393,
12.4625616490958));
#109828=CARTESIAN_POINT('Ctrl Pts',(-10.0491297563374,5.8103190931176,12.4626790297303));
#109829=CARTESIAN_POINT('Ctrl Pts',(-10.0414872913104,5.81073908625171,
12.4629180605544));
#109830=CARTESIAN_POINT('Ctrl Pts',(-10.0372230465051,5.81097442418408,
12.4630327717126));
#109831=CARTESIAN_POINT('Ctrl Pts',(-10.0261921950495,5.81158566939605,
12.4632812524953));
#109832=CARTESIAN_POINT('Ctrl Pts',(-10.0194251275474,5.81196304928457,
12.4633867280592));
#109833=CARTESIAN_POINT('Ctrl Pts',(-9.975121286419,5.81444838972668,12.4637699230797));
#109834=CARTESIAN_POINT('Ctrl Pts',(-9.93758910661046,5.81662239483701,
12.4626502560444));
#109835=CARTESIAN_POINT('Ctrl Pts',(-9.79685753361064,5.824933353312,12.4530256449793));
#109836=CARTESIAN_POINT('Ctrl Pts',(-9.69461059367506,5.83127028825392,
12.4350224212767));
#109837=CARTESIAN_POINT('Ctrl Pts',(-9.55303933856826,5.83996772701815,
12.3942652309968));
#109838=CARTESIAN_POINT('Ctrl Pts',(-9.51152576431471,5.84251227649355,
12.3802690998282));
#109839=CARTESIAN_POINT('Ctrl Pts',(-9.45331720404425,5.84606094950681,
12.3576883967957));
#109840=CARTESIAN_POINT('Ctrl Pts',(-9.43606486065199,5.84711040773884,
12.3506135882876));
#109841=CARTESIAN_POINT('Ctrl Pts',(-9.40554975264926,5.84896264112461,
12.337413317028));
#109842=CARTESIAN_POINT('Ctrl Pts',(-9.39223485454473,5.84976946276726,
12.3314154222908));
#109843=CARTESIAN_POINT('Ctrl Pts',(-9.37225389676864,5.85097846221475,
12.3220524853212));
#109844=CARTESIAN_POINT('Ctrl Pts',(-9.36552042417658,5.85138558545128,
12.318834187759));
#109845=CARTESIAN_POINT('Ctrl Pts',(-9.35343698450079,5.85211571632636,
12.3129448837118));
#109846=CARTESIAN_POINT('Ctrl Pts',(-9.34807824432272,5.85243934712233,
12.3102923439504));
#109847=CARTESIAN_POINT('Ctrl Pts',(-9.33656947070323,5.85313409928735,
12.3045074986618));
#109848=CARTESIAN_POINT('Ctrl Pts',(-9.33042501847381,5.85350483746499,
12.3013643715741));
#109849=CARTESIAN_POINT('Ctrl Pts',(-9.31398288559632,5.85449654487967,
12.2928062988305));
#109850=CARTESIAN_POINT('Ctrl Pts',(-9.30372704551955,5.85511473770878,
12.2873117690531));
#109851=CARTESIAN_POINT('Ctrl Pts',(-9.25396406184489,5.85811382584124,
12.2598827281003));
#109852=CARTESIAN_POINT('Ctrl Pts',(-9.21541998207495,5.86043423088415,
12.2362478748867));
#109853=CARTESIAN_POINT('Ctrl Pts',(-9.08612297010179,5.86829774753281,
12.1484772551841));
#109854=CARTESIAN_POINT('Ctrl Pts',(-9.001623964051,5.87355348532776,12.0758324169943));
#109855=CARTESIAN_POINT('Ctrl Pts',(-8.89095192632912,5.88163018933566,
11.9563103765689));
#109856=CARTESIAN_POINT('Ctrl Pts',(-8.85779427609208,5.88425424699069,
11.9164508822542));
#109857=CARTESIAN_POINT('Ctrl Pts',(-8.82221749491582,5.88742438522831,
11.8687462053216));
#109858=CARTESIAN_POINT('Ctrl Pts',(-8.8176608774552,5.88783773241379,11.8625345168288));
#109859=CARTESIAN_POINT('Ctrl Pts',(-8.81077364781177,5.8884742807303,11.8529885574001));
#109860=CARTESIAN_POINT('Ctrl Pts',(-8.80840747500743,5.88869514645983,
11.8496799687909));
#109861=CARTESIAN_POINT('Ctrl Pts',(-8.80410154027517,5.88910116134296,
11.8436056755123));
#109862=CARTESIAN_POINT('Ctrl Pts',(-8.80215753390207,5.88928602042566,
11.8408430814198));
#109863=CARTESIAN_POINT('Ctrl Pts',(-8.79781013540917,5.88970293323143,
11.8346193950126));
#109864=CARTESIAN_POINT('Ctrl Pts',(-8.79541213362944,5.88993533458507,
11.8311546645128));
#109865=CARTESIAN_POINT('Ctrl Pts',(-8.78842031618624,5.89062001342604,
11.8209587879242));
#109866=CARTESIAN_POINT('Ctrl Pts',(-8.78386779669529,5.89107489190595,
11.814199680439));
#109867=CARTESIAN_POINT('Ctrl Pts',(-8.74136185618165,5.8954061015063,11.7499394113873));
#109868=CARTESIAN_POINT('Ctrl Pts',(-8.70746051135611,5.89950074572649,
11.6898687455693));
#109869=CARTESIAN_POINT('Ctrl Pts',(-8.64271775038151,5.90856366704315,
11.5534927851825));
#109870=CARTESIAN_POINT('Ctrl Pts',(-8.61381439684384,5.91352833716397,
11.4765086927922));
#109871=CARTESIAN_POINT('Ctrl Pts',(-8.57638126639981,5.92159871598075,
11.3438714363327));
#109872=CARTESIAN_POINT('Ctrl Pts',(-8.56431938417028,5.92478572460804,
11.2894134848219));
#109873=CARTESIAN_POINT('Ctrl Pts',(-8.55346989003923,5.92854073272195,
11.2225465528112));
#109874=CARTESIAN_POINT('Ctrl Pts',(-8.55169324807884,5.92920155069513,
11.2106748478936));
#109875=CARTESIAN_POINT('Ctrl Pts',(-8.54912347875291,5.93023592720241,
11.1919307108425));
#109876=CARTESIAN_POINT('Ctrl Pts',(-8.5482327016119,5.930612509227,11.1850723947104));
#109877=CARTESIAN_POINT('Ctrl Pts',(-8.54665565670268,5.93131489230008,
11.1722175784007));
#109878=CARTESIAN_POINT('Ctrl Pts',(-8.5459578065378,5.93164104670507,11.1662226688449));
#109879=CARTESIAN_POINT('Ctrl Pts',(-8.54447915982048,5.93236835797635,
11.1527977277578));
#109880=CARTESIAN_POINT('Ctrl Pts',(-8.5437181283908,5.93276889393007,11.1453656597392));
#109881=CARTESIAN_POINT('Ctrl Pts',(-8.54192986516025,5.93378176512366,
11.126475553821));
#109882=CARTESIAN_POINT('Ctrl Pts',(-8.54098074943659,5.9343916828451,11.1150105222727));
#109883=CARTESIAN_POINT('Ctrl Pts',(-8.53583441652369,5.93822322226448,
11.0424479349112));
#109884=CARTESIAN_POINT('Ctrl Pts',(-8.5353402088393,5.94132829683979,10.9811456480205));
#109885=CARTESIAN_POINT('Ctrl Pts',(-8.54406865517426,5.94924500661307,
10.8217334865408));
#109886=CARTESIAN_POINT('Ctrl Pts',(-8.55934352295727,5.95391822225966,
10.724278014087));
#109887=CARTESIAN_POINT('Ctrl Pts',(-8.59231118522894,5.96039902178524,
10.5984422836911));
#109888=CARTESIAN_POINT('Ctrl Pts',(-8.60133521384235,5.96200145006498,
10.5680590306082));
#109889=CARTESIAN_POINT('Ctrl Pts',(-8.61718181856105,5.96460678829333,
10.5204284825906));
#109890=CARTESIAN_POINT('Ctrl Pts',(-8.62335845861017,5.96558176448198,
10.5029758888031));
#109891=CARTESIAN_POINT('Ctrl Pts',(-8.63188078677515,5.96688244083867,
10.4802741185329));
#109892=CARTESIAN_POINT('Ctrl Pts',(-8.63392893887717,5.96719192650651,
10.4749142667749));
#109893=CARTESIAN_POINT('Ctrl Pts',(-8.63732732554378,5.96770065815684,
10.4661754294132));
#109894=CARTESIAN_POINT('Ctrl Pts',(-8.63865875671988,5.96789881191781,
10.4627891395131));
#109895=CARTESIAN_POINT('Ctrl Pts',(-8.64127722998413,5.96828634130444,
10.4562017027723));
#109896=CARTESIAN_POINT('Ctrl Pts',(-8.64256298332213,5.96847564152219,
10.4530000925222));
#109897=CARTESIAN_POINT('Ctrl Pts',(-8.64574334924329,5.96894142945178,
10.4451610417707));
#109898=CARTESIAN_POINT('Ctrl Pts',(-8.64765046717005,5.96921864803859,
10.4405287449364));
#109899=CARTESIAN_POINT('Ctrl Pts',(-8.654218521303,5.97016612285981,10.4248050722618));
#109900=CARTESIAN_POINT('Ctrl Pts',(-8.65899230585262,5.97084260881341,
10.4137617049339));
#109901=CARTESIAN_POINT('Ctrl Pts',(-8.69459159750092,5.97579512373317,
10.3341192537659));
#109902=CARTESIAN_POINT('Ctrl Pts',(-8.73052596092311,5.98030537611432,
10.2679330302557));
#109903=CARTESIAN_POINT('Ctrl Pts',(-8.80650541858622,5.98871882464578,
10.1505405124206));
#109904=CARTESIAN_POINT('Ctrl Pts',(-8.84518686104693,5.99260982639114,
10.0986575633365));
#109905=CARTESIAN_POINT('Ctrl Pts',(-8.91316235232629,5.99876275002727,
10.019073192881));
#109906=CARTESIAN_POINT('Ctrl Pts',(-8.94038947346599,6.0010790137886,9.98972310901098));
#109907=CARTESIAN_POINT('Ctrl Pts',(-8.98731296814261,6.00482894172307,
9.94312779677988));
#109908=CARTESIAN_POINT('Ctrl Pts',(-9.00632849838731,6.00628901107473,
9.92522981637639));
#109909=CARTESIAN_POINT('Ctrl Pts',(-9.03280939964125,6.00824427520805,
9.90160914350378));
#109910=CARTESIAN_POINT('Ctrl Pts',(-9.03986510669321,6.00875803880145,
9.89543622935417));
#109911=CARTESIAN_POINT('Ctrl Pts',(-9.05179557554975,6.00961490930766,
9.88519917152931));
#109912=CARTESIAN_POINT('Ctrl Pts',(-9.0566382714208,6.00995951102347,9.88109823106945));
#109913=CARTESIAN_POINT('Ctrl Pts',(-9.06623421285141,6.01063611894035,
9.87307868501824));
#109914=CARTESIAN_POINT('Ctrl Pts',(-9.07098582629186,6.0109681915467,9.86915833909039));
#109915=CARTESIAN_POINT('Ctrl Pts',(-9.0814905423681,6.01169591903647,9.86060225949758));
#109916=CARTESIAN_POINT('Ctrl Pts',(-9.08725430213539,6.01209104107755,
9.85597983909939));
#109917=CARTESIAN_POINT('Ctrl Pts',(-9.10760622534809,6.01347191313485,
9.83990972130842));
#109918=CARTESIAN_POINT('Ctrl Pts',(-9.1223770475581,6.01444855376954,9.82869555724841));
#109919=CARTESIAN_POINT('Ctrl Pts',(-9.21790552660439,6.0206128083508,9.75899121276381));
#109920=CARTESIAN_POINT('Ctrl Pts',(-9.30424999006816,6.02548090844909,
9.70860195576097));
#109921=CARTESIAN_POINT('Ctrl Pts',(-9.47528932216425,6.0346211351749,9.63095832930934));
#109922=CARTESIAN_POINT('Ctrl Pts',(-9.5586405582549,6.038886713264,9.60186021444274));
#109923=CARTESIAN_POINT('Ctrl Pts',(-9.65778770622451,6.04424117704663,
9.57700232354516));
#109924=CARTESIAN_POINT('Ctrl Pts',(-9.67153286674872,6.04498973945566,
9.57376686531283));
#109925=CARTESIAN_POINT('Ctrl Pts',(-9.69038436459785,6.04602753189032,
9.56961638844169));
#109926=CARTESIAN_POINT('Ctrl Pts',(-9.69545235965242,6.0463076243835,9.56852878092943));
#109927=CARTESIAN_POINT('Ctrl Pts',(-9.70397079825143,6.04678040793251,
9.56674798192163));
#109928=CARTESIAN_POINT('Ctrl Pts',(-9.70741820900085,6.04697229085019,
9.56604026177898));
#109929=CARTESIAN_POINT('Ctrl Pts',(-9.71397601012079,6.04733839398079,
9.56471864133534));
#109930=CARTESIAN_POINT('Ctrl Pts',(-9.71708590101527,6.04751247577093,
9.56410240145144));
#109931=CARTESIAN_POINT('Ctrl Pts',(-9.72446682569966,6.04792669936896,
9.56266474460264));
#109932=CARTESIAN_POINT('Ctrl Pts',(-9.72873954281502,6.04816733067398,
9.56185225726512));
#109933=CARTESIAN_POINT('Ctrl Pts',(-9.74377070226655,6.04901666308925,
9.5590633436134));
#109934=CARTESIAN_POINT('Ctrl Pts',(-9.75454735747312,6.04963063994186,
9.55718854779365));
#109935=CARTESIAN_POINT('Ctrl Pts',(-9.86708102150152,6.05608732616832,
9.53890849037532));
#109936=CARTESIAN_POINT('Ctrl Pts',(-9.97027283774919,6.06237177883906,
9.53317697744838));
#109937=CARTESIAN_POINT('Ctrl Pts',(-10.1386582383289,6.07248561257343,
9.54161004850172));
#109938=CARTESIAN_POINT('Ctrl Pts',(-10.2038241163778,6.07636962968115,
9.54928138586425));
#109939=CARTESIAN_POINT('Ctrl Pts',(-10.3040906765611,6.08222823466551,
9.56797713593471));
#109940=CARTESIAN_POINT('Ctrl Pts',(-10.3396598823935,6.08428401957572,
9.57599434166768));
#109941=CARTESIAN_POINT('Ctrl Pts',(-10.385103320301,6.08688185296976,9.58803710690994));
#109942=CARTESIAN_POINT('Ctrl Pts',(-10.3952822633051,6.08746190171635,
9.59085283974348));
#109943=CARTESIAN_POINT('Ctrl Pts',(-10.4117717670066,6.08839872628173,
9.59560695580029));
#109944=CARTESIAN_POINT('Ctrl Pts',(-10.4181011360617,6.08875763713726,
9.5974782523236));
#109945=CARTESIAN_POINT('Ctrl Pts',(-10.4302542151432,6.08944553617087,
9.60116092662981));
#109946=CARTESIAN_POINT('Ctrl Pts',(-10.4360796749492,6.08977471857208,
9.6029660127691));
#109947=CARTESIAN_POINT('Ctrl Pts',(-10.4494190677138,6.09052729151737,
9.60719094524674));
#109948=CARTESIAN_POINT('Ctrl Pts',(-10.4569250824447,6.09094988003365,
9.60963528750308));
#109949=CARTESIAN_POINT('Ctrl Pts',(-10.4807938701271,6.09229113394196,
9.61762235466242));
#109950=CARTESIAN_POINT('Ctrl Pts',(-10.4970787556461,6.09320235437092,
9.62339423089913));
#109951=CARTESIAN_POINT('Ctrl Pts',(-10.6474864103047,6.10159206091621,
9.67972061799816));
#109952=CARTESIAN_POINT('Ctrl Pts',(-10.7735907189672,6.10833137986445,
9.74942705050562));
#109953=CARTESIAN_POINT('Ctrl Pts',(-10.9318176043906,6.11816573209087,
9.87011177771781));
#109954=CARTESIAN_POINT('Ctrl Pts',(-10.9741152411387,6.12097342024244,
9.90636857268308));
#109955=CARTESIAN_POINT('Ctrl Pts',(-11.0198680247962,6.12435315626382,
9.95035130128564));
#109956=CARTESIAN_POINT('Ctrl Pts',(-11.0254517645181,6.12477187058527,
9.95580564450794));
#109957=CARTESIAN_POINT('Ctrl Pts',(-11.033893581289,6.12541499353086,9.96418484639018));
#109958=CARTESIAN_POINT('Ctrl Pts',(-11.0367835590472,6.12563699172452,
9.96707753401152));
#109959=CARTESIAN_POINT('Ctrl Pts',(-11.0420383852228,6.12604409212517,
9.97238155879598));
#109960=CARTESIAN_POINT('Ctrl Pts',(-11.044407043167,6.12622889409269,9.97478900482839));
#109961=CARTESIAN_POINT('Ctrl Pts',(-11.0496955546545,6.12664442185702,
9.98020146706591));
#109962=CARTESIAN_POINT('Ctrl Pts',(-11.0526108252374,6.1268754840808,9.98321081096621));
#109963=CARTESIAN_POINT('Ctrl Pts',(-11.0610817406891,6.12755264327352,
9.99203054824887));
#109964=CARTESIAN_POINT('Ctrl Pts',(-11.0666023923804,6.12800125869232,
9.99787415623807));
#109965=CARTESIAN_POINT('Ctrl Pts',(-11.1102798839339,6.13160711449606,
10.0448765420532));
#109966=CARTESIAN_POINT('Ctrl Pts',(-11.1460851233871,6.13491006420475,
10.0881502754917));
#109967=CARTESIAN_POINT('Ctrl Pts',(-11.2180312990137,6.1421668727748,10.1860547029032));
#109968=CARTESIAN_POINT('Ctrl Pts',(-11.2531747000291,6.14612842125434,
10.2412770080597));
#109969=CARTESIAN_POINT('Ctrl Pts',(-11.3113028665365,6.15336603784884,
10.3477398181162));
#109970=CARTESIAN_POINT('Ctrl Pts',(-11.3352649894794,6.15665310519098,
10.3983132786174));
#109971=CARTESIAN_POINT('Ctrl Pts',(-11.3686425860636,6.16173476555258,
10.4806416156491));
#109972=CARTESIAN_POINT('Ctrl Pts',(-11.3799774194024,6.16358618069123,
10.5115553004252));
#109973=CARTESIAN_POINT('Ctrl Pts',(-11.3934463799746,6.16596676404683,
10.5525143211884));
#109974=CARTESIAN_POINT('Ctrl Pts',(-11.3965307380355,6.16652652501124,
10.5622350497297));
#109975=CARTESIAN_POINT('Ctrl Pts',(-11.401420403865,6.16743882689903,10.5782232526967));
#109976=CARTESIAN_POINT('Ctrl Pts',(-11.4032858342451,6.16779329866697,
10.5844718514325));
#109977=CARTESIAN_POINT('Ctrl Pts',(-11.4068233260975,6.16847830398121,
10.5966168829201));
#109978=CARTESIAN_POINT('Ctrl Pts',(-11.4085002324507,6.16880898732581,
10.602511752687));
#109979=CARTESIAN_POINT('Ctrl Pts',(-11.4123025598992,6.16957301203859,
10.6162044179329));
#109980=CARTESIAN_POINT('Ctrl Pts',(-11.4144005256689,6.17000546789695,
10.6240096729527));
#109981=CARTESIAN_POINT('Ctrl Pts',(-11.4210453507104,6.17141217520674,
10.6495739665638));
#109982=CARTESIAN_POINT('Ctrl Pts',(-11.4253233166392,6.17237789432764,
10.6674014793967));
#109983=CARTESIAN_POINT('Ctrl Pts',(-11.4520207565273,6.17885204802569,
10.7886545978085));
#109984=CARTESIAN_POINT('Ctrl Pts',(-11.4634999999948,6.18399426631462,
10.8941661500697));
#109985=CARTESIAN_POINT('Ctrl Pts',(-11.4635,6.189145110564,10.9999999999277));
#109986=CARTESIAN_POINT('Origin',(-10.,3.5,11.));
#109987=CARTESIAN_POINT('',(-11.463499727355,6.76164013593975,10.9991066719022));
#109988=CARTESIAN_POINT('',(-11.4634998124304,6.68841477993962,10.9993388722436));
#109989=CARTESIAN_POINT('',(-11.4635,3.5,11.));
#109990=CARTESIAN_POINT('',(-11.4634994513784,6.26072181654729,11.0012916812098));
#109991=CARTESIAN_POINT('Ctrl Pts',(-11.4634997273561,6.76164013612511,
10.9991066755872));
#109992=CARTESIAN_POINT('Ctrl Pts',(-11.4634766903338,6.75974140573439,
10.9613659897967));
#109993=CARTESIAN_POINT('Ctrl Pts',(-11.4619937755461,6.75780217778772,
10.9236431515581));
#109994=CARTESIAN_POINT('Ctrl Pts',(-11.4585272507504,6.75542963641581,
10.8792671204678));
#109995=CARTESIAN_POINT('Ctrl Pts',(-11.4579526020483,6.75506614139962,
10.8725151927497));
#109996=CARTESIAN_POINT('Ctrl Pts',(-11.4569396555713,6.75446965761194,
10.861517857471));
#109997=CARTESIAN_POINT('Ctrl Pts',(-11.4565296337154,6.75423817156922,
10.8572698737035));
#109998=CARTESIAN_POINT('Ctrl Pts',(-11.4557616291221,6.75382152041032,
10.8496612113574));
#109999=CARTESIAN_POINT('Ctrl Pts',(-11.4554105796174,6.7536367393457,10.8462999134854));
#110000=CARTESIAN_POINT('Ctrl Pts',(-11.4546164770431,6.75323072781694,
10.8389431335412));
#110001=CARTESIAN_POINT('Ctrl Pts',(-11.4541686098306,6.7530092420216,10.8349483023107));
#110002=CARTESIAN_POINT('Ctrl Pts',(-11.4528401893041,6.75237306281412,
10.8235245075761));
#110003=CARTESIAN_POINT('Ctrl Pts',(-11.4519191372956,6.75195622559339,
10.8161004920473));
#110004=CARTESIAN_POINT('Ctrl Pts',(-11.445056196504,6.7490115083928,10.7640519173877));
#110005=CARTESIAN_POINT('Ctrl Pts',(-11.4371154006979,6.74638849443986,
10.7197188648445));
#110006=CARTESIAN_POINT('Ctrl Pts',(-11.412278507717,6.73974205495098,10.6103766182953));
#110007=CARTESIAN_POINT('Ctrl Pts',(-11.3929271760902,6.73567406805343,
10.5460278484075));
#110008=CARTESIAN_POINT('Ctrl Pts',(-11.3362644788532,6.7260581820716,10.3958935241019));
#110009=CARTESIAN_POINT('Ctrl Pts',(-11.2950151259913,6.72058644684051,
10.311895241961));
#110010=CARTESIAN_POINT('Ctrl Pts',(-11.2396961722212,6.71472362894013,
10.2220978425876));
#110011=CARTESIAN_POINT('Ctrl Pts',(-11.2332286693612,6.71405627235717,
10.2118848895927));
#110012=CARTESIAN_POINT('Ctrl Pts',(-11.2224642832084,6.71297426498855,
10.1953436740972));
#110013=CARTESIAN_POINT('Ctrl Pts',(-11.2182431053344,6.71255686917061,
10.1889670377024));
#110014=CARTESIAN_POINT('Ctrl Pts',(-11.2105935739528,6.71181260843058,
10.1776059088211));
#110015=CARTESIAN_POINT('Ctrl Pts',(-11.2071839504809,6.71148505930871,
10.1726090683842));
#110016=CARTESIAN_POINT('Ctrl Pts',(-11.1998786983763,6.71079202658371,
10.162044432933));
#110017=CARTESIAN_POINT('Ctrl Pts',(-11.1959750674047,6.71042685349088,
10.1564823277114));
#110018=CARTESIAN_POINT('Ctrl Pts',(-11.1853866833407,6.70944992244013,
10.1416166960353));
#110019=CARTESIAN_POINT('Ctrl Pts',(-11.178631123743,6.70884085787608,10.1323640339432));
#110020=CARTESIAN_POINT('Ctrl Pts',(-11.1435070314095,6.70574440846674,
10.085424174251));
#110021=CARTESIAN_POINT('Ctrl Pts',(-11.1134357649663,6.70332372090919,
10.04904330392));
#110022=CARTESIAN_POINT('Ctrl Pts',(-11.010429451743,6.69563873161764,9.93602359092591));
#110023=CARTESIAN_POINT('Ctrl Pts',(-10.9309449463051,6.69061964110309,
9.86582439238452));
#110024=CARTESIAN_POINT('Ctrl Pts',(-10.8358594916264,6.6848653261675,9.79863182612754));
#110025=CARTESIAN_POINT('Ctrl Pts',(-10.8270600022895,6.68433468123143,
9.79255711267202));
#110026=CARTESIAN_POINT('Ctrl Pts',(-10.8102001626127,6.68332003863133,
9.78118872614371));
#110027=CARTESIAN_POINT('Ctrl Pts',(-10.8021525054238,6.6828366022932,9.77587722108606));
#110028=CARTESIAN_POINT('Ctrl Pts',(-10.7639092061498,6.68054065376398,
9.75117546598622));
#110029=CARTESIAN_POINT('Ctrl Pts',(-10.7330616269854,6.67869287451012,
9.7328219316908));
#110030=CARTESIAN_POINT('Ctrl Pts',(-10.6957061354172,6.67642332534775,
9.71241702480914));
#110031=CARTESIAN_POINT('Ctrl Pts',(-10.6898171800818,6.67606461998427,
9.70925246481979));
#110032=CARTESIAN_POINT('Ctrl Pts',(-10.6801581267935,6.67547444157025,
9.7041469404916));
#110033=CARTESIAN_POINT('Ctrl Pts',(-10.6764008469551,6.67524441878227,
9.70218178368297));
#110034=CARTESIAN_POINT('Ctrl Pts',(-10.6696348114144,6.67482929967808,
9.69868033056869));
#110035=CARTESIAN_POINT('Ctrl Pts',(-10.6666292206017,6.67464457469725,
9.69713809458523));
#110036=CARTESIAN_POINT('Ctrl Pts',(-10.6600151946942,6.67423735221615,
9.69377316856977));
#110037=CARTESIAN_POINT('Ctrl Pts',(-10.6564045818955,6.67401458833853,
9.69195504036094));
#110038=CARTESIAN_POINT('Ctrl Pts',(-10.6459951871039,6.67337114078406,
9.68676732984023));
#110039=CARTESIAN_POINT('Ctrl Pts',(-10.639177773248,6.67294823832128,9.68343568447771));
#110040=CARTESIAN_POINT('Ctrl Pts',(-10.5889686876092,6.66982443740236,
9.6593805776535));
#110041=CARTESIAN_POINT('Ctrl Pts',(-10.5446085625831,6.66701515702606,
9.64075564474417));
#110042=CARTESIAN_POINT('Ctrl Pts',(-10.4018261915461,6.65799038901365,
9.58891986233803));
#110043=CARTESIAN_POINT('Ctrl Pts',(-10.3007315592184,6.65165006672066,
9.56397256221287));
#110044=CARTESIAN_POINT('Ctrl Pts',(-10.1713997405622,6.64400535460004,
9.54632640320552));
#110045=CARTESIAN_POINT('Ctrl Pts',(-10.1448564578488,6.64245867828334,
9.54344189338611));
#110046=CARTESIAN_POINT('Ctrl Pts',(-10.0862057576738,6.63909347156352,
9.53868748352496));
#110047=CARTESIAN_POINT('Ctrl Pts',(-10.0540850429118,6.63728494193385,
9.53714637172762));
#110048=CARTESIAN_POINT('Ctrl Pts',(-10.011473187987,6.63493050387279,9.53650755110172));
#110049=CARTESIAN_POINT('Ctrl Pts',(-10.0010070445002,6.63435576535727,
9.53646292297054));
#110050=CARTESIAN_POINT('Ctrl Pts',(-9.98396317181616,6.63342542648385,
9.53657308297943));
#110051=CARTESIAN_POINT('Ctrl Pts',(-9.97738550405315,6.63306774475773,
9.53665994797766));
#110052=CARTESIAN_POINT('Ctrl Pts',(-9.96470600657196,6.63238081298814,
9.53691290753786));
#110053=CARTESIAN_POINT('Ctrl Pts',(-9.95860420259536,6.63205137986552,
9.53707283311547));
#110054=CARTESIAN_POINT('Ctrl Pts',(-9.94443361847941,6.63128889570631,
9.53753296819654));
#110055=CARTESIAN_POINT('Ctrl Pts',(-9.93636592447998,6.63085673593114,
9.53786178839829));
#110056=CARTESIAN_POINT('Ctrl Pts',(-9.91052186942392,6.62947830581525,
9.53912944407066));
#110057=CARTESIAN_POINT('Ctrl Pts',(-9.89275940559183,6.62853996961731,
9.5403258555737));
#110058=CARTESIAN_POINT('Ctrl Pts',(-9.80031280902038,6.62369741941265,
9.54824938749413));
#110059=CARTESIAN_POINT('Ctrl Pts',(-9.72620235328725,6.6199632061122,9.56038502841752));
#110060=CARTESIAN_POINT('Ctrl Pts',(-9.57927208519921,6.61255915156996,
9.59620772058036));
#110061=CARTESIAN_POINT('Ctrl Pts',(-9.50672943114754,6.60890157887665,
9.62002605113209));
#110062=CARTESIAN_POINT('Ctrl Pts',(-9.42432347592268,6.60445447073088,
9.65441487566535));
#110063=CARTESIAN_POINT('Ctrl Pts',(-9.41233984663203,6.60380004068105,
9.65960516299982));
#110064=CARTESIAN_POINT('Ctrl Pts',(-9.36893416929882,6.60139610096152,
9.67909877613972));
#110065=CARTESIAN_POINT('Ctrl Pts',(-9.33795340122862,6.59961564764115,
9.69435147188901));
#110066=CARTESIAN_POINT('Ctrl Pts',(-9.30171591329662,6.59742189589772,
9.71381364609854));
#110067=CARTESIAN_POINT('Ctrl Pts',(-9.2959099828604,6.59706692152894,9.7169827564594));
#110068=CARTESIAN_POINT('Ctrl Pts',(-9.28643668965028,6.59648165791445,
9.72223732673075));
#110069=CARTESIAN_POINT('Ctrl Pts',(-9.2827564476262,6.59625277862423,9.72429951291286));
#110070=CARTESIAN_POINT('Ctrl Pts',(-9.27614603032912,6.5958388452928,9.72804123994868));
#110071=CARTESIAN_POINT('Ctrl Pts',(-9.27321269979408,6.59565415262042,
9.72971504120123));
#110072=CARTESIAN_POINT('Ctrl Pts',(-9.26676495754305,6.59524593246318,
9.73342386162479));
#110073=CARTESIAN_POINT('Ctrl Pts',(-9.26325325342763,6.59502212966786,
9.73546333687484));
#110074=CARTESIAN_POINT('Ctrl Pts',(-9.25312893352764,6.59437274808814,
9.7413996772089));
#110075=CARTESIAN_POINT('Ctrl Pts',(-9.24653852850315,6.59394488841513,
9.74533392161576));
#110076=CARTESIAN_POINT('Ctrl Pts',(-9.19648890119403,6.59065796194353,
9.77574836305994));
#110077=CARTESIAN_POINT('Ctrl Pts',(-9.1544102622679,6.58767768782419,9.80442516748937));
#110078=CARTESIAN_POINT('Ctrl Pts',(-9.02723419317661,6.57816578136807,
9.9011730339746));
#110079=CARTESIAN_POINT('Ctrl Pts',(-8.94817448956919,6.57151747219421,
9.97659336176716));
#110080=CARTESIAN_POINT('Ctrl Pts',(-8.84743432461422,6.56239080822099,
10.0968268410983));
#110081=CARTESIAN_POINT('Ctrl Pts',(-8.81847411603009,6.55966201937285,
10.1350568194189));
#110082=CARTESIAN_POINT('Ctrl Pts',(-8.78476405623198,6.556348839506,10.1844180116743));
#110083=CARTESIAN_POINT('Ctrl Pts',(-8.77820682725676,6.55569711042855,
10.1942743436741));
#110084=CARTESIAN_POINT('Ctrl Pts',(-8.76799234867724,6.55466994369967,
10.2100394591696));
#110085=CARTESIAN_POINT('Ctrl Pts',(-8.76425644412322,6.55429162076989,
10.2158964510924));
#110086=CARTESIAN_POINT('Ctrl Pts',(-8.75735557852207,6.55358773206872,
10.2268871626428));
#110087=CARTESIAN_POINT('Ctrl Pts',(-8.75418038399279,6.55326179750983,
10.2320142557398));
#110088=CARTESIAN_POINT('Ctrl Pts',(-8.74716722693097,6.55253717597813,
10.2434965904973));
#110089=CARTESIAN_POINT('Ctrl Pts',(-8.74334573428496,6.55213908969481,
10.2498617293605));
#110090=CARTESIAN_POINT('Ctrl Pts',(-8.73224605268452,6.55097299417077,
10.2686724169392));
#110091=CARTESIAN_POINT('Ctrl Pts',(-8.72510302808039,6.55020980815627,
10.2811969427675));
#110092=CARTESIAN_POINT('Ctrl Pts',(-8.66951087766547,6.54416082360184,
10.3821082529389));
#110093=CARTESIAN_POINT('Ctrl Pts',(-8.63012436627499,6.53921440948321,
10.4751808704421));
#110094=CARTESIAN_POINT('Ctrl Pts',(-8.57227405234132,6.52959503197681,
10.6641389410706));
#110095=CARTESIAN_POINT('Ctrl Pts',(-8.55319228286888,6.52493384855663,
10.7592783469866));
#110096=CARTESIAN_POINT('Ctrl Pts',(-8.54252131499585,6.51923518128711,
10.8668941694635));
#110097=CARTESIAN_POINT('Ctrl Pts',(-8.54153213907268,6.51863061424948,
10.8782101710165));
#110098=CARTESIAN_POINT('Ctrl Pts',(-8.54034125799299,6.51778128682468,
10.8939427699123));
#110099=CARTESIAN_POINT('Ctrl Pts',(-8.54002766683981,6.51754236153391,
10.8983507768655));
#110100=CARTESIAN_POINT('Ctrl Pts',(-8.53952224486626,6.51712921396665,
10.9059407717107));
#110101=CARTESIAN_POINT('Ctrl Pts',(-8.53932083550362,6.51695551426358,
10.9091221166943));
#110102=CARTESIAN_POINT('Ctrl Pts',(-8.53892014000824,6.51658991093408,
10.9157970450796));
#110103=CARTESIAN_POINT('Ctrl Pts',(-8.53872298852783,6.51639788648051,
10.9192907078615));
#110104=CARTESIAN_POINT('Ctrl Pts',(-8.53826995841372,6.51592501326122,
10.9278652859457));
#110105=CARTESIAN_POINT('Ctrl Pts',(-8.53802804143712,6.51564340986202,
10.9329468699114));
#110106=CARTESIAN_POINT('Ctrl Pts',(-8.53724250649838,6.51461157419837,
10.9514814936588));
#110107=CARTESIAN_POINT('Ctrl Pts',(-8.53685806753742,6.51385327151785,
10.9649402015591));
#110108=CARTESIAN_POINT('Ctrl Pts',(-8.53635914556255,6.51192918152371,
10.9987436042074));
#110109=CARTESIAN_POINT('Ctrl Pts',(-8.53648311164518,6.51075342434788,
11.0190886041612));
#110110=CARTESIAN_POINT('Ctrl Pts',(-8.54071338631265,6.50157673869878,
11.1760702021066));
#110111=CARTESIAN_POINT('Ctrl Pts',(-8.56352053996646,6.49312720394605,
11.3115331982211));
#110112=CARTESIAN_POINT('Ctrl Pts',(-8.61777463768181,6.48272372482155,
11.4828366145295));
#110113=CARTESIAN_POINT('Ctrl Pts',(-8.63254496264598,6.48028619518263,
11.5232068418696));
#110114=CARTESIAN_POINT('Ctrl Pts',(-8.65353402259502,6.47726366782131,
11.5735819425154));
#110115=CARTESIAN_POINT('Ctrl Pts',(-8.65812379982414,6.476625293157,11.5842389471223));
#110116=CARTESIAN_POINT('Ctrl Pts',(-8.6656148546357,6.47561804847663,11.6010783184673));
#110117=CARTESIAN_POINT('Ctrl Pts',(-8.66843343461874,6.47524641362629,
11.6072967522178));
#110118=CARTESIAN_POINT('Ctrl Pts',(-8.67357575850673,6.47458132572557,
11.6184339671171));
#110119=CARTESIAN_POINT('Ctrl Pts',(-8.67588359514665,6.47428734034416,
11.6233599181879));
#110120=CARTESIAN_POINT('Ctrl Pts',(-8.68135615977891,6.47360058499883,
11.6348732785525));
#110121=CARTESIAN_POINT('Ctrl Pts',(-8.68454288719673,6.47320857468935,
11.6414501104343));
#110122=CARTESIAN_POINT('Ctrl Pts',(-8.69391246520662,6.47207831580035,
11.6604237283802));
#110123=CARTESIAN_POINT('Ctrl Pts',(-8.7002223221774,6.47134444232889,11.6727571293239));
#110124=CARTESIAN_POINT('Ctrl Pts',(-8.75283245229806,6.46543665597835,
11.7720861843529));
#110125=CARTESIAN_POINT('Ctrl Pts',(-8.80763729227501,6.46058702717733,
11.8542938533409));
#110126=CARTESIAN_POINT('Ctrl Pts',(-8.9340223552646,6.45090540583437,12.00775627458));
#110127=CARTESIAN_POINT('Ctrl Pts',(-9.00552306219934,6.44609346584908,
12.0783745565994));
#110128=CARTESIAN_POINT('Ctrl Pts',(-9.09238560791968,6.44022045134425,
12.1481260493683));
#110129=CARTESIAN_POINT('Ctrl Pts',(-9.1011849735275,6.43962506323052,12.1550276374416));
#110130=CARTESIAN_POINT('Ctrl Pts',(-9.11354717114549,6.43878666981082,
12.1644968449683));
#110131=CARTESIAN_POINT('Ctrl Pts',(-9.11704398933176,6.43854930638491,
12.167150462432));
#110132=CARTESIAN_POINT('Ctrl Pts',(-9.12309454251176,6.43813813124554,
12.1716992710455));
#110133=CARTESIAN_POINT('Ctrl Pts',(-9.12564263440511,6.43796483060316,
12.1736019597695));
#110134=CARTESIAN_POINT('Ctrl Pts',(-9.13101364315418,6.43759919604268,
12.1775853514085));
#110135=CARTESIAN_POINT('Ctrl Pts',(-9.13383785742809,6.43740673566227,
12.179664227753));
#110136=CARTESIAN_POINT('Ctrl Pts',(-9.14080813552137,6.43693129886868,
12.1847564561603));
#110137=CARTESIAN_POINT('Ctrl Pts',(-9.14496258964638,6.43664754967818,
12.1877582016945));
#110138=CARTESIAN_POINT('Ctrl Pts',(-9.16029864175547,6.4355989784113,12.198716906009));
#110139=CARTESIAN_POINT('Ctrl Pts',(-9.17157589690446,6.43482574909199,
12.2065380513964));
#110140=CARTESIAN_POINT('Ctrl Pts',(-9.25141701923626,6.42934578582872,
12.260263428372));
#110141=CARTESIAN_POINT('Ctrl Pts',(-9.32364095183151,6.42436841393295,
12.3004525518307));
#110142=CARTESIAN_POINT('Ctrl Pts',(-9.49556378061459,6.41302193435636,
12.3779064377561));
#110143=CARTESIAN_POINT('Ctrl Pts',(-9.59673243830619,6.40671184978047,
12.410838062045));
#110144=CARTESIAN_POINT('Ctrl Pts',(-9.7167942168775,6.39983462798635,12.4359320842108));
#110145=CARTESIAN_POINT('Ctrl Pts',(-9.73306019329736,6.39891461834012,
12.4390446960002));
#110146=CARTESIAN_POINT('Ctrl Pts',(-9.75815932025603,6.39751257495687,
12.4434073623064));
#110147=CARTESIAN_POINT('Ctrl Pts',(-9.7669565621134,6.39702445482888,12.4448537949936));
#110148=CARTESIAN_POINT('Ctrl Pts',(-9.78132698594896,6.39623235675098,
12.4470818995353));
#110149=CARTESIAN_POINT('Ctrl Pts',(-9.78689234006223,6.39592687492211,
12.4479119577992));
#110150=CARTESIAN_POINT('Ctrl Pts',(-9.79860936751232,6.39528637339991,
12.4495905021196));
#110151=CARTESIAN_POINT('Ctrl Pts',(-9.80476194335179,6.3949515781827,12.4504319748111));
#110152=CARTESIAN_POINT('Ctrl Pts',(-9.81954207845712,6.39415089740001,
12.4523576677396));
#110153=CARTESIAN_POINT('Ctrl Pts',(-9.82817436396092,6.39368619096771,
12.4534042148267));
#110154=CARTESIAN_POINT('Ctrl Pts',(-9.85815242857285,6.39208212867266,
12.4567678293239));
#110155=CARTESIAN_POINT('Ctrl Pts',(-9.87954002367731,6.39095491276024,
12.4586921190527));
#110156=CARTESIAN_POINT('Ctrl Pts',(-9.967364125955,6.38638764105288,12.4646489500817));
#110157=CARTESIAN_POINT('Ctrl Pts',(-10.0339989373755,6.38307052646329,
12.4646183338377));
#110158=CARTESIAN_POINT('Ctrl Pts',(-10.1742840578023,6.37617619102798,
12.4549712470941));
#110159=CARTESIAN_POINT('Ctrl Pts',(-10.2476690867091,6.37262193757632,
12.4442907364485));
#110160=CARTESIAN_POINT('Ctrl Pts',(-10.3703656339709,6.36639019577888,
12.416803842459));
#110161=CARTESIAN_POINT('Ctrl Pts',(-10.4201642585547,6.36377463331692,
12.4028416920848));
#110162=CARTESIAN_POINT('Ctrl Pts',(-10.4760223017506,6.36063704414652,
12.3839393747946));
#110163=CARTESIAN_POINT('Ctrl Pts',(-10.4829119300004,6.36024642016737,
12.3815503930139));
#110164=CARTESIAN_POINT('Ctrl Pts',(-10.4939058042378,6.35961685278395,
12.3776459796838));
#110165=CARTESIAN_POINT('Ctrl Pts',(-10.498021692195,6.35937974692176,12.3761634284863));
#110166=CARTESIAN_POINT('Ctrl Pts',(-10.5053198100759,6.35895671391064,
12.3734976032463));
#110167=CARTESIAN_POINT('Ctrl Pts',(-10.5085046474403,6.35877121690252,
12.3723216823753));
#110168=CARTESIAN_POINT('Ctrl Pts',(-10.5153320479257,6.35837162115853,
12.3697738061966));
#110169=CARTESIAN_POINT('Ctrl Pts',(-10.5189731793357,6.35815733072261,
12.3683984208447));
#110170=CARTESIAN_POINT('Ctrl Pts',(-10.5285795127667,6.35758892916199,
12.3647259099395));
#110171=CARTESIAN_POINT('Ctrl Pts',(-10.5345351592353,6.357233426039,12.3624042245558));
#110172=CARTESIAN_POINT('Ctrl Pts',(-10.5664558270761,6.35531201089413,
12.3497190931489));
#110173=CARTESIAN_POINT('Ctrl Pts',(-10.5921335479654,6.3537093000427,12.3386528643372));
#110174=CARTESIAN_POINT('Ctrl Pts',(-10.6723985087093,6.34855158440738,
12.3013001707151));
#110175=CARTESIAN_POINT('Ctrl Pts',(-10.7256776817075,6.34490808157574,
12.2723572954693));
#110176=CARTESIAN_POINT('Ctrl Pts',(-10.8596083154647,6.33539696344837,
12.1884472580106));
#110177=CARTESIAN_POINT('Ctrl Pts',(-10.93684309052,6.32956591955387,12.1285668055197));
#110178=CARTESIAN_POINT('Ctrl Pts',(-11.0275976349151,6.32245076275521,
12.0424197556812));
#110179=CARTESIAN_POINT('Ctrl Pts',(-11.0470974435837,6.32090215137806,
12.0228308435569));
#110180=CARTESIAN_POINT('Ctrl Pts',(-11.0728068959623,6.31883185757511,
11.9954975630767));
#110181=CARTESIAN_POINT('Ctrl Pts',(-11.07950888307,6.31828938031217,11.9882259924712));
#110182=CARTESIAN_POINT('Ctrl Pts',(-11.0904617852464,6.31739801243513,
11.976097836299));
#110183=CARTESIAN_POINT('Ctrl Pts',(-11.0947551226691,6.31704735862846,
11.9712801420549));
#110184=CARTESIAN_POINT('Ctrl Pts',(-11.1030834874465,6.31636461565882,
11.9618092326366));
#110185=CARTESIAN_POINT('Ctrl Pts',(-11.1071212784697,6.31603241629205,
11.9571586371196));
#110186=CARTESIAN_POINT('Ctrl Pts',(-11.116605011712,6.31524925239579,11.9460952784903));
#110187=CARTESIAN_POINT('Ctrl Pts',(-11.1220252840222,6.31479933437832,
11.9396607335401));
#110188=CARTESIAN_POINT('Ctrl Pts',(-11.139361647786,6.31335242828277,11.9187163857525));
#110189=CARTESIAN_POINT('Ctrl Pts',(-11.1510543444261,6.31236431281994,
11.904023616946));
#110190=CARTESIAN_POINT('Ctrl Pts',(-11.2012248891629,6.30806326651345,
11.8384284049846));
#110191=CARTESIAN_POINT('Ctrl Pts',(-11.2366343255074,6.30486667020402,
11.7852643245582));
#110192=CARTESIAN_POINT('Ctrl Pts',(-11.2960505243368,6.29900710509381,
11.6820150514864));
#110193=CARTESIAN_POINT('Ctrl Pts',(-11.3208982213808,6.29633352547457,
11.6325499390586));
#110194=CARTESIAN_POINT('Ctrl Pts',(-11.3570837304205,6.29188944614951,
11.5490277081228));
#110195=CARTESIAN_POINT('Ctrl Pts',(-11.3700763642429,6.29013560249887,
11.5157501987438));
#110196=CARTESIAN_POINT('Ctrl Pts',(-11.3954917384352,6.28627098578904,
11.4428920920733));
#110197=CARTESIAN_POINT('Ctrl Pts',(-11.4074748804916,6.28414992097693,
11.4031928697614));
#110198=CARTESIAN_POINT('Ctrl Pts',(-11.4194808850742,6.28157176804751,
11.3563068987934));
#110199=CARTESIAN_POINT('Ctrl Pts',(-11.4211575362389,6.2811989962082,11.3495594980313));
#110200=CARTESIAN_POINT('Ctrl Pts',(-11.4237981003146,6.280590313098,11.338599895542));
#110201=CARTESIAN_POINT('Ctrl Pts',(-11.4247915658701,6.28035600849023,
11.3343948453261));
#110202=CARTESIAN_POINT('Ctrl Pts',(-11.4265296658571,6.27993636329822,
11.3268895961812));
#110203=CARTESIAN_POINT('Ctrl Pts',(-11.4272814953309,6.27975143116474,
11.3235911439764));
#110204=CARTESIAN_POINT('Ctrl Pts',(-11.4288926792881,6.27934756017723,
11.3164076366362));
#110205=CARTESIAN_POINT('Ctrl Pts',(-11.4297476173439,6.2791283861473,11.3125217294455));
#110206=CARTESIAN_POINT('Ctrl Pts',(-11.4314814097162,6.27867372956234,
11.3044851784145));
#110207=CARTESIAN_POINT('Ctrl Pts',(-11.4323580818218,6.27843813149116,
11.3003341052601));
#110208=CARTESIAN_POINT('Ctrl Pts',(-11.4345664444169,6.27782977950123,
11.2896478021357));
#110209=CARTESIAN_POINT('Ctrl Pts',(-11.4358715189401,6.27745567019768,
11.2831072421368));
#110210=CARTESIAN_POINT('Ctrl Pts',(-11.4395749326088,6.27635017379599,
11.2638624853237));
#110211=CARTESIAN_POINT('Ctrl Pts',(-11.4418496348152,6.27561304523844,
11.2511354359563));
#110212=CARTESIAN_POINT('Ctrl Pts',(-11.4568941607282,6.27029981905276,
11.1600053367267));
#110213=CARTESIAN_POINT('Ctrl Pts',(-11.4634293422371,6.26549925452231,
11.0807138769344));
#110214=CARTESIAN_POINT('Ctrl Pts',(-11.4634994301469,6.26072184081485,
11.0012914950893));
#110215=CARTESIAN_POINT('Ctrl Pts',(-11.4634994299846,6.26072185188138,
11.0012916790654));
#110216=CARTESIAN_POINT('Ctrl Pts',(-11.4634998099988,6.26069595259754,
11.0008611149732));
#110217=CARTESIAN_POINT('Ctrl Pts',(-11.4635,6.26067005423938,11.000430555273));
#110218=CARTESIAN_POINT('Ctrl Pts',(-11.4635,6.26064415683876,11.0000000000891));
#110219=CARTESIAN_POINT('Ctrl Pts',(-11.4635,6.189145110564,10.9999999999277));
#110220=CARTESIAN_POINT('Ctrl Pts',(-11.4635,6.1891661123127,11.000431520628));
#110221=CARTESIAN_POINT('Ctrl Pts',(-11.463499809146,6.18918711470186,11.0008630466623));
#110222=CARTESIAN_POINT('Ctrl Pts',(-11.4634246718514,6.19332130417299,
11.0858045405408));
#110223=CARTESIAN_POINT('Ctrl Pts',(-11.4560299909816,6.19743501857092,
11.1701401052918));
#110224=CARTESIAN_POINT('Ctrl Pts',(-11.439337749849,6.20250900789312,11.2651064768895));
#110225=CARTESIAN_POINT('Ctrl Pts',(-11.4371287182732,6.20314340504571,
11.2768314133686));
#110226=CARTESIAN_POINT('Ctrl Pts',(-11.4338894976385,6.20402750178027,
11.292939256193));
#110227=CARTESIAN_POINT('Ctrl Pts',(-11.432982012597,6.20427070847752,11.2973466827823));
#110228=CARTESIAN_POINT('Ctrl Pts',(-11.4313924650699,6.20468931615201,
11.304890410363));
#110229=CARTESIAN_POINT('Ctrl Pts',(-11.430720379412,6.20486416293798,11.3080288085857));
#110230=CARTESIAN_POINT('Ctrl Pts',(-11.4292977500027,6.20522990781271,
11.3145668655167));
#110231=CARTESIAN_POINT('Ctrl Pts',(-11.4285453952363,6.20542091206794,
11.3179660735744));
#110232=CARTESIAN_POINT('Ctrl Pts',(-11.4266846000497,6.20588747796026,
11.3262333972047));
#110233=CARTESIAN_POINT('Ctrl Pts',(-11.4255633671261,6.20616374915755,
11.3310985688485));
#110234=CARTESIAN_POINT('Ctrl Pts',(-11.4214720769915,6.20715463933583,
11.3484451039024));
#110235=CARTESIAN_POINT('Ctrl Pts',(-11.4183628973471,6.20787653344378,
11.3608926774896));
#110236=CARTESIAN_POINT('Ctrl Pts',(-11.4102273434133,6.20968941312915,
11.3917328284722));
#110237=CARTESIAN_POINT('Ctrl Pts',(-11.4050045031911,6.21078903755881,
11.4100707918858));
#110238=CARTESIAN_POINT('Ctrl Pts',(-11.381077359834,6.21555559142255,11.4882500874388));
#110239=CARTESIAN_POINT('Ctrl Pts',(-11.3588971493999,6.21933127001888,
11.5469557935838));
#110240=CARTESIAN_POINT('Ctrl Pts',(-11.2883626102926,6.2296151342905,11.702610624167));
#110241=CARTESIAN_POINT('Ctrl Pts',(-11.2329035090032,6.23605972907879,
11.7959245909927));
#110242=CARTESIAN_POINT('Ctrl Pts',(-11.1566563845335,6.24314953014151,
11.896833886094));
#110243=CARTESIAN_POINT('Ctrl Pts',(-11.145387764013,6.24416180167514,11.9111816082512));
#110244=CARTESIAN_POINT('Ctrl Pts',(-11.1287534449904,6.24560657884361,
11.9315647997032));
#110245=CARTESIAN_POINT('Ctrl Pts',(-11.1236017645435,6.24604747802263,
11.937772037316));
#110246=CARTESIAN_POINT('Ctrl Pts',(-11.1144477726761,6.24681959406337,
11.9486179103597));
#110247=CARTESIAN_POINT('Ctrl Pts',(-11.1104671951861,6.24715167334041,
11.9532745605917));
#110248=CARTESIAN_POINT('Ctrl Pts',(-11.1021852624572,6.24783512414195,
11.9628408488933));
#110249=CARTESIAN_POINT('Ctrl Pts',(-11.0978800600493,6.24818632779997,
11.9677469858936));
#110250=CARTESIAN_POINT('Ctrl Pts',(-11.0867459466133,6.24908433764534,
11.9802653069339));
#110251=CARTESIAN_POINT('Ctrl Pts',(-11.0798697503712,6.24962917811855,
11.9878350842966));
#110252=CARTESIAN_POINT('Ctrl Pts',(-11.0503505133671,6.25192805190795,
12.0196552333213));
#110253=CARTESIAN_POINT('Ctrl Pts',(-11.0269648428255,6.25365063691154,
12.0432048805704));
#110254=CARTESIAN_POINT('Ctrl Pts',(-10.9615792014568,6.25823401738371,
12.1047172895536));
#110255=CARTESIAN_POINT('Ctrl Pts',(-10.9181444979434,6.26103473532356,
12.1410723693714));
#110256=CARTESIAN_POINT('Ctrl Pts',(-10.8049950104029,6.26792965623479,
12.2251249544868));
#110257=CARTESIAN_POINT('Ctrl Pts',(-10.7330603779082,6.27196720254323,
12.269475920929));
#110258=CARTESIAN_POINT('Ctrl Pts',(-10.6534326940461,6.27645443154008,
12.309534613145));
#110259=CARTESIAN_POINT('Ctrl Pts',(-10.6491436612378,6.27669620948599,
12.3116659998137));
#110260=CARTESIAN_POINT('Ctrl Pts',(-10.6153194396795,6.27860411246096,
12.3282680316871));
#110261=CARTESIAN_POINT('Ctrl Pts',(-10.5853165066602,6.28030351165344,
12.3417593892835));
#110262=CARTESIAN_POINT('Ctrl Pts',(-10.548265233972,6.28243969939094,12.3569409312405));
#110263=CARTESIAN_POINT('Ctrl Pts',(-10.541623903592,6.28282404815149,12.3596054576904));
#110264=CARTESIAN_POINT('Ctrl Pts',(-10.5312453583326,6.28342731073243,
12.3636812587087));
#110265=CARTESIAN_POINT('Ctrl Pts',(-10.5275213644763,6.28364429634303,
12.3651261536406));
#110266=CARTESIAN_POINT('Ctrl Pts',(-10.520632868438,6.28404671630293,12.3677664674015));
#110267=CARTESIAN_POINT('Ctrl Pts',(-10.5174700982641,6.28423189592542,
12.3689661755446));
#110268=CARTESIAN_POINT('Ctrl Pts',(-10.510274744673,6.28465411166599,12.3716670331593));
#110269=CARTESIAN_POINT('Ctrl Pts',(-10.5062397001636,6.28489153716534,
12.373161363395));
#110270=CARTESIAN_POINT('Ctrl Pts',(-10.49387491415,6.28562095722229,12.3776786062192));
#110271=CARTESIAN_POINT('Ctrl Pts',(-10.4855244116701,6.28611614911237,
12.3806436218913));
#110272=CARTESIAN_POINT('Ctrl Pts',(-10.4080677621062,6.29072979436664,
12.4073565916349));
#110273=CARTESIAN_POINT('Ctrl Pts',(-10.3373068469105,6.29508939958693,
12.425971216637));
#110274=CARTESIAN_POINT('Ctrl Pts',(-10.1426733474741,6.30698568471396,
12.4618707413526));
#110275=CARTESIAN_POINT('Ctrl Pts',(-10.0174679729956,6.31448853329586,
12.4687162676468));
#110276=CARTESIAN_POINT('Ctrl Pts',(-9.87615001354495,6.32241275794081,
12.4583468563332));
#110277=CARTESIAN_POINT('Ctrl Pts',(-9.85942048903276,6.3233433074189,12.4568293676562));
#110278=CARTESIAN_POINT('Ctrl Pts',(-9.8349596064023,6.32469329148715,12.4541852875142));
#110279=CARTESIAN_POINT('Ctrl Pts',(-9.82720565654582,6.3251196651968,12.453284314958));
#110280=CARTESIAN_POINT('Ctrl Pts',(-9.81341995082756,6.32587501861012,
12.4515705877286));
#110281=CARTESIAN_POINT('Ctrl Pts',(-9.80738540188954,6.32620474593271,
12.4507821697445));
#110282=CARTESIAN_POINT('Ctrl Pts',(-9.79477583607914,6.3268918656907,12.4490546581122));
#110283=CARTESIAN_POINT('Ctrl Pts',(-9.7882019301542,6.32724902698332,12.4481084003785));
#110284=CARTESIAN_POINT('Ctrl Pts',(-9.77100491799356,6.32818067126909,
12.4455134263385));
#110285=CARTESIAN_POINT('Ctrl Pts',(-9.76039303226953,6.32875288963202,
12.4437923405117));
#110286=CARTESIAN_POINT('Ctrl Pts',(-9.71191716242938,6.33135557150926,
12.4353811040017));
#110287=CARTESIAN_POINT('Ctrl Pts',(-9.67430544550673,6.33334289558289,
12.4273170697689));
#110288=CARTESIAN_POINT('Ctrl Pts',(-9.52383457807275,6.34122292841183,
12.3887970100353));
#110289=CARTESIAN_POINT('Ctrl Pts',(-9.41450233072162,6.34674913683043,
12.3463588857786));
#110290=CARTESIAN_POINT('Ctrl Pts',(-9.30447220946037,6.35291694712337,
12.2876857789482));
#110291=CARTESIAN_POINT('Ctrl Pts',(-9.2975920995346,6.3533054953928,12.2839457589748));
#110292=CARTESIAN_POINT('Ctrl Pts',(-9.27946745323676,6.35433752114194,
12.2739039390322));
#110293=CARTESIAN_POINT('Ctrl Pts',(-9.26827572561913,6.35498347439784,
12.267508568528));
#110294=CARTESIAN_POINT('Ctrl Pts',(-9.22735266738228,6.35738279077261,
12.2434009701976));
#110295=CARTESIAN_POINT('Ctrl Pts',(-9.19816973426201,6.35916735452538,
12.2247847761987));
#110296=CARTESIAN_POINT('Ctrl Pts',(-9.16422465343283,6.36136579441722,
12.2013973726671));
#110297=CARTESIAN_POINT('Ctrl Pts',(-9.15879874826343,6.36172106447749,
12.1976044955671));
#110298=CARTESIAN_POINT('Ctrl Pts',(-9.14995581642798,6.36230675086501,
12.1913332668282));
#110299=CARTESIAN_POINT('Ctrl Pts',(-9.1465233915624,6.36253575433924,12.1888766734289));
#110300=CARTESIAN_POINT('Ctrl Pts',(-9.14036295824545,6.36294986651786,
12.1844272117324));
#110301=CARTESIAN_POINT('Ctrl Pts',(-9.13763117347545,6.36313461313047,
12.1824397109788));
#110302=CARTESIAN_POINT('Ctrl Pts',(-9.13163048846169,6.36354290077385,
12.1780420770394));
#110303=CARTESIAN_POINT('Ctrl Pts',(-9.12836476777925,6.36376671683052,
12.1756278173726));
#110304=CARTESIAN_POINT('Ctrl Pts',(-9.11895787239892,6.36441599764191,
12.1686128103497));
#110305=CARTESIAN_POINT('Ctrl Pts',(-9.11284287248267,6.36484374152741,
12.163977386823));
#110306=CARTESIAN_POINT('Ctrl Pts',(-9.06654742417541,6.36812376872548,
12.1283067806633));
#110307=CARTESIAN_POINT('Ctrl Pts',(-9.02797339718941,6.3710966889408,12.0952503000835));
#110308=CARTESIAN_POINT('Ctrl Pts',(-8.91232403265526,6.38059833723132,
11.9852138856488));
#110309=CARTESIAN_POINT('Ctrl Pts',(-8.84206017340091,6.38724453507976,
11.9015901411413));
#110310=CARTESIAN_POINT('Ctrl Pts',(-8.75508586776139,6.39637842719503,
11.770929198254));
#110311=CARTESIAN_POINT('Ctrl Pts',(-8.73043522396423,6.39911558255167,
11.729622532684));
#110312=CARTESIAN_POINT('Ctrl Pts',(-8.70229679931413,6.40243736565787,
11.6767119465783));
#110313=CARTESIAN_POINT('Ctrl Pts',(-8.6968602194612,6.40308975022912,11.6661826923902));
#110314=CARTESIAN_POINT('Ctrl Pts',(-8.68843836003114,6.40411777885849,
11.6493740271501));
#110315=CARTESIAN_POINT('Ctrl Pts',(-8.68536899305357,6.4044963152003,11.6431375284242));
#110316=CARTESIAN_POINT('Ctrl Pts',(-8.67971911596831,6.40520050167493,
11.6314483537237));
#110317=CARTESIAN_POINT('Ctrl Pts',(-8.6771276722616,6.40552652169316,11.6260011518868));
#110318=CARTESIAN_POINT('Ctrl Pts',(-8.6714222638398,6.40625120981021,11.6138147597212));
#110319=CARTESIAN_POINT('Ctrl Pts',(-8.66832573701981,6.40664927798001,
11.6070675583003));
#110320=CARTESIAN_POINT('Ctrl Pts',(-8.65937029274392,6.40781493437883,
11.5871557400214));
#110321=CARTESIAN_POINT('Ctrl Pts',(-8.65365421070497,6.40857770642582,
11.5739276174317));
#110322=CARTESIAN_POINT('Ctrl Pts',(-8.60965499604112,6.41460838482074,
11.4678283751579));
#110323=CARTESIAN_POINT('Ctrl Pts',(-8.5808295789151,6.41953944699433,11.3713230142977));
#110324=CARTESIAN_POINT('Ctrl Pts',(-8.54401287212679,6.42916065784511,
11.1771374313188));
#110325=CARTESIAN_POINT('Ctrl Pts',(-8.53546768393207,6.43383817344887,
11.0801042342729));
#110326=CARTESIAN_POINT('Ctrl Pts',(-8.53673142403795,6.43955595299073,
10.971608574267));
#110327=CARTESIAN_POINT('Ctrl Pts',(-8.53699552216339,6.44015987425747,
10.9602648673176));
#110328=CARTESIAN_POINT('Ctrl Pts',(-8.53754566418645,6.44100847472973,
10.9445105094832));
#110329=CARTESIAN_POINT('Ctrl Pts',(-8.53771983316455,6.44124733293883,
10.9400960722164));
#110330=CARTESIAN_POINT('Ctrl Pts',(-8.53805408919055,6.44166042705985,
10.932497651389));
#110331=CARTESIAN_POINT('Ctrl Pts',(-8.53820459831125,6.441834141094,10.9293132515738));
#110332=CARTESIAN_POINT('Ctrl Pts',(-8.53854221978982,6.44219985107157,
10.9226329322084));
#110333=CARTESIAN_POINT('Ctrl Pts',(-8.53873147288181,6.44239196840482,
10.919137169389));
#110334=CARTESIAN_POINT('Ctrl Pts',(-8.53922678545627,6.44286520452323,
10.9105584191917));
#110335=CARTESIAN_POINT('Ctrl Pts',(-8.53954683370768,6.44314707998011,
10.9054763087917));
#110336=CARTESIAN_POINT('Ctrl Pts',(-8.54081157520264,6.44418070538868,
10.8869363069883));
#110337=CARTESIAN_POINT('Ctrl Pts',(-8.54191579521966,6.44494055990392,
10.8734903833549));
#110338=CARTESIAN_POINT('Ctrl Pts',(-8.54515607803518,6.44686934033336,
10.8397580836191));
#110339=CARTESIAN_POINT('Ctrl Pts',(-8.54753064830014,6.44804829259003,
10.8194978700412));
#110340=CARTESIAN_POINT('Ctrl Pts',(-8.56921625361718,6.45728946592261,
10.6628650315527));
#110341=CARTESIAN_POINT('Ctrl Pts',(-8.60726816982389,6.46580451983366,
10.529778137404));
#110342=CARTESIAN_POINT('Ctrl Pts',(-8.68046501034125,6.47619955536067,
10.3656337038305));
#110343=CARTESIAN_POINT('Ctrl Pts',(-8.69919702582557,6.47857868578438,
10.3280585563514));
#110344=CARTESIAN_POINT('Ctrl Pts',(-8.72510674434366,6.48154181482339,
10.2812423438655));
#110345=CARTESIAN_POINT('Ctrl Pts',(-8.73081315283062,6.48217657863567,
10.2712132416078));
#110346=CARTESIAN_POINT('Ctrl Pts',(-8.7400774365639,6.48317953014526,10.2553700118201));
#110347=CARTESIAN_POINT('Ctrl Pts',(-8.74355826775016,6.48355044135184,
10.2495115851688));
#110348=CARTESIAN_POINT('Ctrl Pts',(-8.74989293783888,6.48421498862915,
10.2390176008194));
#110349=CARTESIAN_POINT('Ctrl Pts',(-8.75273194616726,6.48450915024345,
10.2343732752066));
#110350=CARTESIAN_POINT('Ctrl Pts',(-8.75945506014903,6.48519728179882,
10.2235115959183));
#110351=CARTESIAN_POINT('Ctrl Pts',(-8.76336011968737,6.48559048279469,
10.2173073409469));
#110352=CARTESIAN_POINT('Ctrl Pts',(-8.77483460541817,6.48672739955703,
10.1993772493488));
#110353=CARTESIAN_POINT('Ctrl Pts',(-8.78252546186566,6.48746665996089,
10.1877298481481));
#110354=CARTESIAN_POINT('Ctrl Pts',(-8.85104538468401,6.49386328915692,
10.0871200763126));
#110355=CARTESIAN_POINT('Ctrl Pts',(-8.92136186301909,6.49912516150783,
10.0050179513429));
#110356=CARTESIAN_POINT('Ctrl Pts',(-9.0658530029645,6.50875409282547,9.86981435689484));
#110357=CARTESIAN_POINT('Ctrl Pts',(-9.13717931779434,6.51311800831979,
9.81446767233331));
#110358=CARTESIAN_POINT('Ctrl Pts',(-9.22300917556595,6.51847745592388,
9.75973599955377));
#110359=CARTESIAN_POINT('Ctrl Pts',(-9.23296325327591,6.51910067118624,
9.75355539865387));
#110360=CARTESIAN_POINT('Ctrl Pts',(-9.24681765252976,6.51997186850159,
9.74518184476771));
#110361=CARTESIAN_POINT('Ctrl Pts',(-9.25065568571012,6.52021360957955,
9.74288610347632));
#110362=CARTESIAN_POINT('Ctrl Pts',(-9.25725976737182,6.52063035559362,
9.73897682369774));
#110363=CARTESIAN_POINT('Ctrl Pts',(-9.2600207233144,6.52080481728032,9.7373546919234));
#110364=CARTESIAN_POINT('Ctrl Pts',(-9.26579989889062,6.52117053060454,
9.7339847449228));
#110365=CARTESIAN_POINT('Ctrl Pts',(-9.26881905908328,6.52136189346068,
9.73223864810285));
#110366=CARTESIAN_POINT('Ctrl Pts',(-9.27620343452705,6.52183063089651,
9.72800313113295));
#110367=CARTESIAN_POINT('Ctrl Pts',(-9.28057526831405,6.5221087303593,9.72552538019659));
#110368=CARTESIAN_POINT('Ctrl Pts',(-9.29633973795588,6.52311340214833,
9.71669777571772));
#110369=CARTESIAN_POINT('Ctrl Pts',(-9.30780405049165,6.52384751199259,
9.71047795414609));
#110370=CARTESIAN_POINT('Ctrl Pts',(-9.336604391639,6.52569747132265,9.69534739449104));
#110371=CARTESIAN_POINT('Ctrl Pts',(-9.35403790318474,6.52682239192262,
9.68662836203254));
#110372=CARTESIAN_POINT('Ctrl Pts',(-9.43052037306454,6.53176346335816,
9.65026827947765));
#110373=CARTESIAN_POINT('Ctrl Pts',(-9.49120329026381,6.53569551182621,
9.62624312824905));
#110374=CARTESIAN_POINT('Ctrl Pts',(-9.65304267545736,6.54592100760255,
9.57436769384756));
#110375=CARTESIAN_POINT('Ctrl Pts',(-9.75596277995621,6.55214847789187,
9.55319000017357));
#110376=CARTESIAN_POINT('Ctrl Pts',(-9.87676489717327,6.55895291078649,
9.54160369432716));
#110377=CARTESIAN_POINT('Ctrl Pts',(-9.89328111144568,6.55987327941634,
9.54030215960327));
#110378=CARTESIAN_POINT('Ctrl Pts',(-9.9187173547735,6.56127583823559,9.5387317455743));
#110379=CARTESIAN_POINT('Ctrl Pts',(-9.92762332550629,6.56176411968257,
9.53826356626391));
#110380=CARTESIAN_POINT('Ctrl Pts',(-9.94215633180019,6.56255646827424,
9.53763272749554));
#110381=CARTESIAN_POINT('Ctrl Pts',(-9.94778091850796,6.56286204034146,
9.53742107960036));
#110382=CARTESIAN_POINT('Ctrl Pts',(-9.95961490822182,6.56350272319044,
9.53704413052024));
#110383=CARTESIAN_POINT('Ctrl Pts',(-9.96582443519107,6.56383760941523,
9.53688590189154));
#110384=CARTESIAN_POINT('Ctrl Pts',(-9.98073060105931,6.564638494985,9.53660101680788));
#110385=CARTESIAN_POINT('Ctrl Pts',(-9.98942778501862,6.56510331467634,
9.53651234156083));
#110386=CARTESIAN_POINT('Ctrl Pts',(-10.0196004744835,6.56670771840745,
9.53647369268325));
#110387=CARTESIAN_POINT('Ctrl Pts',(-10.0410742440011,6.56783515775781,
9.53691886782261));
#110388=CARTESIAN_POINT('Ctrl Pts',(-10.1291437699085,6.5724088316484,9.54068526796777));
#110389=CARTESIAN_POINT('Ctrl Pts',(-10.1954876020823,6.57573161966994,
9.5480828719828));
#110390=CARTESIAN_POINT('Ctrl Pts',(-10.3174533901714,6.58180865329662,
9.57019731491684));
#110391=CARTESIAN_POINT('Ctrl Pts',(-10.3731579472535,6.58457296050827,
9.58371420542063));
#110392=CARTESIAN_POINT('Ctrl Pts',(-10.4930608471273,6.59071660020756,
9.62037601683172));
#110393=CARTESIAN_POINT('Ctrl Pts',(-10.5567183513361,6.59410600146427,
9.64481220949848));
#110394=CARTESIAN_POINT('Ctrl Pts',(-10.6258040654603,6.59816000944756,
9.67702319678472));
#110395=CARTESIAN_POINT('Ctrl Pts',(-10.6331437805256,6.59859567182318,
9.68052006555455));
#110396=CARTESIAN_POINT('Ctrl Pts',(-10.6442388846093,6.5992623592887,9.68592000625582));
#110397=CARTESIAN_POINT('Ctrl Pts',(-10.6480159439431,6.59949075654161,
9.68777848443906));
#110398=CARTESIAN_POINT('Ctrl Pts',(-10.654809362227,6.59990424409247,9.69115762603904));
#110399=CARTESIAN_POINT('Ctrl Pts',(-10.6578285279339,6.60008897759479,
9.69267246331612));
#110400=CARTESIAN_POINT('Ctrl Pts',(-10.6608562316969,6.60027521475029,
9.6942047284258));
#110401=CARTESIAN_POINT('Ctrl Pts',(-10.6608700002742,6.60027606168986,
9.69421169672277));
#110402=CARTESIAN_POINT('Ctrl Pts',(-10.6608973651576,6.60027774501247,
9.69422554667354));
#110403=CARTESIAN_POINT('Ctrl Pts',(-10.6609109616453,6.60027858140619,
9.69423242841259));
#110404=CARTESIAN_POINT('Ctrl Pts',(-10.6609379853764,6.60028024382181,
9.69424610675938));
#110405=CARTESIAN_POINT('Ctrl Pts',(-10.6609514124614,6.60028106983348,
9.69425290328039));
#110406=CARTESIAN_POINT('Ctrl Pts',(-10.6609780994838,6.60028271161252,
9.69426641223271));
#110407=CARTESIAN_POINT('Ctrl Pts',(-10.6609913595032,6.60028352738446,
9.69427312469913));
#110408=CARTESIAN_POINT('Ctrl Pts',(-10.66101771496,6.60028514884045,9.69428646682185));
#110409=CARTESIAN_POINT('Ctrl Pts',(-10.6610308103756,6.6002859545227,9.69429309646091));
#110410=CARTESIAN_POINT('Ctrl Pts',(-10.6610568389154,6.60028755593885,
9.69430627406986));
#110411=CARTESIAN_POINT('Ctrl Pts',(-10.661069772066,6.60028835167393,9.69431282204704));
#110412=CARTESIAN_POINT('Ctrl Pts',(-10.6610954784154,6.60028993333834,
9.69432583749862));
#110413=CARTESIAN_POINT('Ctrl Pts',(-10.6611082515916,6.60029071926584,
9.69433230495565));
#110414=CARTESIAN_POINT('Ctrl Pts',(-10.6611336406667,6.60029228147833,
9.69434516070334));
#110415=CARTESIAN_POINT('Ctrl Pts',(-10.6611462563701,6.60029305775087,
9.6943515488893));
#110416=CARTESIAN_POINT('Ctrl Pts',(-10.6611713320181,6.6002946007456,9.69436424684657));
#110417=CARTESIAN_POINT('Ctrl Pts',(-10.6611837922187,6.60029536748313,
9.69437055674194));
#110418=CARTESIAN_POINT('Ctrl Pts',(-10.6612085596618,6.60029689157894,
9.6943830995195));
#110419=CARTESIAN_POINT('Ctrl Pts',(-10.6612208667562,6.60029764892769,
9.69438933232128));
#110420=CARTESIAN_POINT('Ctrl Pts',(-10.6612453299952,6.60029915436833,
9.69440172191245));
#110421=CARTESIAN_POINT('Ctrl Pts',(-10.6612574861225,6.60029990245875,
9.69440787868774));
#110422=CARTESIAN_POINT('Ctrl Pts',(-10.6612816496026,6.60030138951539,
9.69442011731182));
#110423=CARTESIAN_POINT('Ctrl Pts',(-10.6612936569411,6.60030212848036,
9.6944261991482));
#110424=CARTESIAN_POINT('Ctrl Pts',(-10.6613175247513,6.60030359740235,
9.69443828884514));
#110425=CARTESIAN_POINT('Ctrl Pts',(-10.66132938531,6.60030432736435,9.69444429674476));
#110426=CARTESIAN_POINT('Ctrl Pts',(-10.6613529619118,6.60030577842402,
9.69445623974416));
#110427=CARTESIAN_POINT('Ctrl Pts',(-10.6613646778394,6.6003064995142,9.6944621747805));
#110428=CARTESIAN_POINT('Ctrl Pts',(-10.6613879672468,6.60030793295638,
9.69447397308615));
#110429=CARTESIAN_POINT('Ctrl Pts',(-10.661399540627,6.6003086453019,9.6944798363002));
#110430=CARTESIAN_POINT('Ctrl Pts',(-10.6614225467408,6.60031006136458,
9.69449149185953));
#110431=CARTESIAN_POINT('Ctrl Pts',(-10.6614339795171,6.60031076508402,
9.69449728422175));
#110432=CARTESIAN_POINT('Ctrl Pts',(-10.6614567065215,6.60031216402264,
9.69450879912654));
#110433=CARTESIAN_POINT('Ctrl Pts',(-10.6614680007405,6.60031285924093,
9.69451452165997));
#110434=CARTESIAN_POINT('Ctrl Pts',(-10.6614904523384,6.60031424128141,
9.69452589775912));
#110435=CARTESIAN_POINT('Ctrl Pts',(-10.6615016098699,6.60031492811267,
9.69453155139775));
#110436=CARTESIAN_POINT('Ctrl Pts',(-10.6615237900186,6.60031629349663,
9.69454279066984));
#110437=CARTESIAN_POINT('Ctrl Pts',(-10.6615348127304,6.60031697205484,
9.69454837634692));
#110438=CARTESIAN_POINT('Ctrl Pts',(-10.6615567254061,6.60031832102514,
9.69455948078091));
#110439=CARTESIAN_POINT('Ctrl Pts',(-10.6615676152757,6.60031899143111,
9.69456499948583));
#110440=CARTESIAN_POINT('Ctrl Pts',(-10.66158926399,6.60032032420204,9.69457597083605));
#110441=CARTESIAN_POINT('Ctrl Pts',(-10.6616000228429,6.60032098656721,
9.69458142348145));
#110442=CARTESIAN_POINT('Ctrl Pts',(-10.661621411343,6.60032230336766,9.69459226362238));
#110443=CARTESIAN_POINT('Ctrl Pts',(-10.6616320410279,6.60032295780496,
9.69459765113308));
#110444=CARTESIAN_POINT('Ctrl Pts',(-10.6616531728078,6.60032425884825,
9.69460836181169));
#110445=CARTESIAN_POINT('Ctrl Pts',(-10.661663675057,6.60032490546345,9.69461368505383));
#110446=CARTESIAN_POINT('Ctrl Pts',(-10.6616845536058,6.60032619096267,
9.6946242680152));
#110447=CARTESIAN_POINT('Ctrl Pts',(-10.6616949300017,6.60032682985235,
9.69462952777942));
#110448=CARTESIAN_POINT('Ctrl Pts',(-10.6617155595835,6.60032810006836,
9.69463998516226));
#110449=CARTESIAN_POINT('Ctrl Pts',(-10.6617258122715,6.60032873136377,
9.69464518252478));
#110450=CARTESIAN_POINT('Ctrl Pts',(-10.6654343566185,6.60055708403641,
9.69652519804279));
#110451=CARTESIAN_POINT('Ctrl Pts',(-10.6691246179307,6.60078577311935,
9.69841570110886));
#110452=CARTESIAN_POINT('Ctrl Pts',(-10.6800603018615,6.60146770675667,
9.70407679641653));
#110453=CARTESIAN_POINT('Ctrl Pts',(-10.6872821259072,6.60192359970746,
9.7078923276443));
#110454=CARTESIAN_POINT('Ctrl Pts',(-10.7039030469933,6.60298505265313,
9.71685248043823));
#110455=CARTESIAN_POINT('Ctrl Pts',(-10.7132782552238,6.60359291536704,
9.72204022965949));
#110456=CARTESIAN_POINT('Ctrl Pts',(-10.7447389593693,6.60566164121148,
9.73990296342047));
#110457=CARTESIAN_POINT('Ctrl Pts',(-10.7665495665393,6.60714440722668,
9.75305080578825));
#110458=CARTESIAN_POINT('Ctrl Pts',(-10.8592216606337,6.61362307637913,
9.81226562251631));
#110459=CARTESIAN_POINT('Ctrl Pts',(-10.9263619093737,6.61876885787463,
9.86385368610624));
#110460=CARTESIAN_POINT('Ctrl Pts',(-11.0502770203702,6.62879998993099,
9.97739008166031));
#110461=CARTESIAN_POINT('Ctrl Pts',(-11.106939806136,6.63366808543925,10.0390105451841));
#110462=CARTESIAN_POINT('Ctrl Pts',(-11.1654265735219,6.63898511210841,
10.1146983048499));
#110463=CARTESIAN_POINT('Ctrl Pts',(-11.1726947627775,6.6396520585584,10.124348702223));
#110464=CARTESIAN_POINT('Ctrl Pts',(-11.1843666526428,6.64073359858019,
10.1402521637163));
#110465=CARTESIAN_POINT('Ctrl Pts',(-11.188842204727,6.64115093218281,10.1464515683117));
#110466=CARTESIAN_POINT('Ctrl Pts',(-11.1967720803589,6.64189520404111,
10.1576191794491));
#110467=CARTESIAN_POINT('Ctrl Pts',(-11.2002445405426,6.64222282544031,
10.1625742399626));
#110468=CARTESIAN_POINT('Ctrl Pts',(-11.2075535311362,6.64291613857872,
10.173142729415));
#110469=CARTESIAN_POINT('Ctrl Pts',(-11.211381882382,6.64328151864185,10.1787616584449));
#110470=CARTESIAN_POINT('Ctrl Pts',(-11.2215621078048,6.64425931265827,
10.1939294154844));
#110471=CARTESIAN_POINT('Ctrl Pts',(-11.2278412002845,6.64486902591594,
10.2035266688422));
#110472=CARTESIAN_POINT('Ctrl Pts',(-11.2594444600442,6.64797371384926,
10.2530926193604));
#110473=CARTESIAN_POINT('Ctrl Pts',(-11.2829335812133,6.65040155593496,
10.2942004656664));
#110474=CARTESIAN_POINT('Ctrl Pts',(-11.3533353981179,6.65820302020536,
10.432579542871));
#110475=CARTESIAN_POINT('Ctrl Pts',(-11.3914843664654,6.66331834433958,
10.5338959229662));
#110476=CARTESIAN_POINT('Ctrl Pts',(-11.4251962124842,6.67007609535568,
10.6661399063797));
#110477=CARTESIAN_POINT('Ctrl Pts',(-11.4314355274829,6.6715056956944,10.6939950921619));
#110478=CARTESIAN_POINT('Ctrl Pts',(-11.4418852528145,6.67431859535422,
10.7480076446833));
#110479=CARTESIAN_POINT('Ctrl Pts',(-11.4462076672111,6.67569726484906,
10.7741317993417));
#110480=CARTESIAN_POINT('Ctrl Pts',(-11.4507306035821,6.67746899546247,
10.8069776493351));
#110481=CARTESIAN_POINT('Ctrl Pts',(-11.4515968819988,6.67782838025732,
10.8136041824377));
#110482=CARTESIAN_POINT('Ctrl Pts',(-11.4528951229609,6.67840065201192,
10.8240934418338));
#110483=CARTESIAN_POINT('Ctrl Pts',(-11.4533571447579,6.67861191597662,
10.827952435071));
#110484=CARTESIAN_POINT('Ctrl Pts',(-11.4541860066022,6.67900557207377,
10.8351171015171));
#110485=CARTESIAN_POINT('Ctrl Pts',(-11.4545569545076,6.67918773591917,
10.8384222250234));
#110486=CARTESIAN_POINT('Ctrl Pts',(-11.4552760619228,6.67955318959257,
10.845032649447));
#110487=CARTESIAN_POINT('Ctrl Pts',(-11.4556242327026,6.67973647327445,
10.8483379122315));
#110488=CARTESIAN_POINT('Ctrl Pts',(-11.456401637062,6.68016077410182,10.8559673496354));
#110489=CARTESIAN_POINT('Ctrl Pts',(-11.4568228741368,6.68040221252141,
10.8602922863916));
#110490=CARTESIAN_POINT('Ctrl Pts',(-11.4578648961559,6.68103060637719,
10.8715084846775));
#110491=CARTESIAN_POINT('Ctrl Pts',(-11.4584560753435,6.68141903918606,
10.878402312484));
#110492=CARTESIAN_POINT('Ctrl Pts',(-11.4619768989559,6.68395562947491,
10.9231876055651));
#110493=CARTESIAN_POINT('Ctrl Pts',(-11.4634782570727,6.68616795268897,
10.9611737192897));
#110494=CARTESIAN_POINT('Ctrl Pts',(-11.4634997655431,6.68841487495421,
10.9991715947004));
#110495=CARTESIAN_POINT('Origin',(-10.,3.5,11.));
#110496=CARTESIAN_POINT('',(-11.46349956662,7.25939591416304,10.9995759468747));
#110497=CARTESIAN_POINT('',(-11.4634999176128,7.19062697240001,10.9995089322141));
#110498=CARTESIAN_POINT('',(-11.4635,3.5,11.));
#110499=CARTESIAN_POINT('Ctrl Pts',(-11.4634999385744,7.25939527076697,
10.9995759803274));
#110500=CARTESIAN_POINT('Ctrl Pts',(-11.4634561086694,7.25150470342572,
10.8482974725707));
#110501=CARTESIAN_POINT('Ctrl Pts',(-11.4399600529956,7.24445648298535,
10.6979562985416));
#110502=CARTESIAN_POINT('Ctrl Pts',(-11.3841873946785,7.23534112134271,
10.5236997451596));
#110503=CARTESIAN_POINT('Ctrl Pts',(-11.3735491355026,7.23373847646734,
10.4938387263501));
#110504=CARTESIAN_POINT('Ctrl Pts',(-11.3551746365144,7.23113287186272,
10.447119638399));
#110505=CARTESIAN_POINT('Ctrl Pts',(-11.3480726623283,7.23015785665119,
10.4300219090754));
#110506=CARTESIAN_POINT('Ctrl Pts',(-11.3383478102608,7.22885718813728,
10.4078088976472));
#110507=CARTESIAN_POINT('Ctrl Pts',(-11.3360161543885,7.22854775148114,
10.4025671619657));
#110508=CARTESIAN_POINT('Ctrl Pts',(-11.3321557556474,7.22803911636505,
10.3940243187581));
#110509=CARTESIAN_POINT('Ctrl Pts',(-11.3306453944295,7.22784100989487,
10.3907149129892));
#110510=CARTESIAN_POINT('Ctrl Pts',(-11.3276790142784,7.22745358865733,
10.3842788120689));
#110511=CARTESIAN_POINT('Ctrl Pts',(-11.3262242586613,7.22726434936961,
10.3811515846654));
#110512=CARTESIAN_POINT('Ctrl Pts',(-11.3226303757709,7.22679873971834,
10.3734968366618));
#110513=CARTESIAN_POINT('Ctrl Pts',(-11.320479048771,7.22652163921353,10.3689751155117));
#110514=CARTESIAN_POINT('Ctrl Pts',(-11.3130836741868,7.22557474941248,
10.3536347329811));
#110515=CARTESIAN_POINT('Ctrl Pts',(-11.3077296724927,7.224898739375,10.3428699682646));
#110516=CARTESIAN_POINT('Ctrl Pts',(-11.2678372935943,7.21993582069678,
10.2650809826297));
#110517=CARTESIAN_POINT('Ctrl Pts',(-11.2283001042013,7.21541344708913,
10.2007538992219));
#110518=CARTESIAN_POINT('Ctrl Pts',(-11.1457918060659,7.20696771984628,
10.0871932804422));
#110519=CARTESIAN_POINT('Ctrl Pts',(-11.1041344827091,7.20305654393707,
10.0372212746924));
#110520=CARTESIAN_POINT('Ctrl Pts',(-11.0319028578451,7.19690479936103,
9.96145083724244));
#110521=CARTESIAN_POINT('Ctrl Pts',(-11.0033548208978,7.19460793576585,
9.93384459040236));
#110522=CARTESIAN_POINT('Ctrl Pts',(-10.9606938758796,7.19136812140267,
9.89582434566826));
#110523=CARTESIAN_POINT('Ctrl Pts',(-10.9474630890683,7.19038810169876,
9.88445066004649));
#110524=CARTESIAN_POINT('Ctrl Pts',(-10.9264594044912,7.18887028638219,
9.86703840822607));
#110525=CARTESIAN_POINT('Ctrl Pts',(-10.9188238958734,7.18832610510823,
9.86083730241024));
#110526=CARTESIAN_POINT('Ctrl Pts',(-10.9045643329139,7.1873236584229,9.8494931858813));
#110527=CARTESIAN_POINT('Ctrl Pts',(-10.8979575111157,7.18686458014011,
9.84432925362347));
#110528=CARTESIAN_POINT('Ctrl Pts',(-10.8864861825065,7.1860766067585,9.83552096007787));
#110529=CARTESIAN_POINT('Ctrl Pts',(-10.8816427316178,7.1857466648648,9.83184963231519));
#110530=CARTESIAN_POINT('Ctrl Pts',(-10.8718309782948,7.18508375479992,
9.82450812569221));
#110531=CARTESIAN_POINT('Ctrl Pts',(-10.8668620287145,7.18475083177108,
9.82083901605691));
#110532=CARTESIAN_POINT('Ctrl Pts',(-10.8558423987814,7.18401857124539,
9.81280934123141));
#110533=CARTESIAN_POINT('Ctrl Pts',(-10.8497812929292,7.18361979284818,
9.80846333301115));
#110534=CARTESIAN_POINT('Ctrl Pts',(-10.8291434521048,7.18227515480108,
9.79390290988805));
#110535=CARTESIAN_POINT('Ctrl Pts',(-10.8144133893468,7.18133751360094,
9.78390793026951));
#110536=CARTESIAN_POINT('Ctrl Pts',(-10.7077425758979,7.17469494872909,
9.71433488179106));
#110537=CARTESIAN_POINT('Ctrl Pts',(-10.6095516740272,7.16938695966699,
9.66497806325042));
#110538=CARTESIAN_POINT('Ctrl Pts',(-10.4488431486929,7.16104624644524,
9.60566000258238));
#110539=CARTESIAN_POINT('Ctrl Pts',(-10.3896304517091,7.15803181718587,
9.58796907139328));
#110540=CARTESIAN_POINT('Ctrl Pts',(-10.3110681493146,7.15391800909917,
9.56981608390005));
#110541=CARTESIAN_POINT('Ctrl Pts',(-10.2925742164616,7.15294134526078,
9.56591851741472));
#110542=CARTESIAN_POINT('Ctrl Pts',(-10.2614910867608,7.15127848920049,
9.55999406322988));
#110543=CARTESIAN_POINT('Ctrl Pts',(-10.2489411941998,7.15060132411581,
9.55777153457303));
#110544=CARTESIAN_POINT('Ctrl Pts',(-10.2314508067843,7.14964759595845,
9.5549091505766));
#110545=CARTESIAN_POINT('Ctrl Pts',(-10.2265333111016,7.14937835771907,
9.55413012461104));
#110546=CARTESIAN_POINT('Ctrl Pts',(-10.2181739900313,7.14891867645609,
9.55284953877119));
#110547=CARTESIAN_POINT('Ctrl Pts',(-10.2147341254406,7.14872894279279,
9.55233512077534));
#110548=CARTESIAN_POINT('Ctrl Pts',(-10.208114586624,7.14836267053087,9.55136930767716));
#110549=CARTESIAN_POINT('Ctrl Pts',(-10.2049352204108,7.14818624150505,
9.55091611045767));
#110550=CARTESIAN_POINT('Ctrl Pts',(-10.1972881264566,7.14776071097816,
9.5498517388271));
#110551=CARTESIAN_POINT('Ctrl Pts',(-10.1928190432518,7.147511057857,9.54925074541061));
#110552=CARTESIAN_POINT('Ctrl Pts',(-10.1764365195446,7.14659253395523,
9.54712469189819));
#110553=CARTESIAN_POINT('Ctrl Pts',(-10.1645075306806,7.14591720873392,
9.5457256930597));
#110554=CARTESIAN_POINT('Ctrl Pts',(-10.0771011463043,7.14092809384779,
9.53656406754474));
#110555=CARTESIAN_POINT('Ctrl Pts',(-10.0011444510717,7.13637582896727,
9.53453553545142));
#110556=CARTESIAN_POINT('Ctrl Pts',(-9.85963515868684,7.12785014603256,
9.54176008105266));
#110557=CARTESIAN_POINT('Ctrl Pts',(-9.79418766767498,7.1238888756256,9.54954898341644));
#110558=CARTESIAN_POINT('Ctrl Pts',(-9.69126761459346,7.1177406879781,9.56890644995313));
#110559=CARTESIAN_POINT('Ctrl Pts',(-9.65335051137601,7.11549252160925,
9.57761505620045));
#110560=CARTESIAN_POINT('Ctrl Pts',(-9.59922353067405,7.11231391154806,
9.59234009616497));
#110561=CARTESIAN_POINT('Ctrl Pts',(-9.58270456515201,7.11134793613943,
9.59714835493381));
#110562=CARTESIAN_POINT('Ctrl Pts',(-9.55318833705484,7.10962911367722,
9.60630731438806));
#110563=CARTESIAN_POINT('Ctrl Pts',(-9.54016033078031,7.10887299860853,
9.61055138254992));
#110564=CARTESIAN_POINT('Ctrl Pts',(-9.52030725867447,7.1077243897284,9.61732864689626));
#110565=CARTESIAN_POINT('Ctrl Pts',(-9.51343853700391,7.1073276639999,9.61973077185539));
#110566=CARTESIAN_POINT('Ctrl Pts',(-9.50097055186475,7.10660867387954,
9.62419570376299));
#110567=CARTESIAN_POINT('Ctrl Pts',(-9.49536547393588,7.10628586832316,
9.62624170677365));
#110568=CARTESIAN_POINT('Ctrl Pts',(-9.48316956817425,7.10558434642002,
9.63077825259796));
#110569=CARTESIAN_POINT('Ctrl Pts',(-9.47658387604776,7.1052060815214,9.63328223382947));
#110570=CARTESIAN_POINT('Ctrl Pts',(-9.45857844210802,7.10417326286533,
9.64027741026515));
#110571=CARTESIAN_POINT('Ctrl Pts',(-9.44719656239041,7.10352190123299,
9.64486487912139));
#110572=CARTESIAN_POINT('Ctrl Pts',(-9.38581513487595,7.10001556471446,
9.67050673599305));
#110573=CARTESIAN_POINT('Ctrl Pts',(-9.33695560333863,7.09724990139249,
9.69418671668403));
#110574=CARTESIAN_POINT('Ctrl Pts',(-9.19811296580911,7.08932858261299,
9.77128480758423));
#110575=CARTESIAN_POINT('Ctrl Pts',(-9.11241339409874,7.08437483904717,
9.83168818786137));
#110576=CARTESIAN_POINT('Ctrl Pts',(-8.99762119814698,7.0767718444092,9.93257339558022));
#110577=CARTESIAN_POINT('Ctrl Pts',(-8.96296141032011,7.07431772668654,
9.96621427529028));
#110578=CARTESIAN_POINT('Ctrl Pts',(-8.92484910683395,7.07134092493417,
10.007054644556));
#110579=CARTESIAN_POINT('Ctrl Pts',(-8.91971123602365,7.07093335276581,
10.0126469205572));
#110580=CARTESIAN_POINT('Ctrl Pts',(-8.91190458021499,7.0703039208405,10.0212778941769));
#110581=CARTESIAN_POINT('Ctrl Pts',(-8.90920440425667,7.07008431725829,
10.0242881724133));
#110582=CARTESIAN_POINT('Ctrl Pts',(-8.90427150190303,7.0696795507079,10.0298336633525));
#110583=CARTESIAN_POINT('Ctrl Pts',(-8.90203504736995,7.06949466681277,
10.0323654488889));
#110584=CARTESIAN_POINT('Ctrl Pts',(-8.89701222562443,7.06907633445715,
10.0380913839395));
#110585=CARTESIAN_POINT('Ctrl Pts',(-8.89423097507864,7.0688425262761,10.041289888092));
#110586=CARTESIAN_POINT('Ctrl Pts',(-8.88710222072903,7.06823773369535,
10.0495604126518));
#110587=CARTESIAN_POINT('Ctrl Pts',(-8.882775526517,7.06786532587704,10.0546501447926));
#110588=CARTESIAN_POINT('Ctrl Pts',(-8.85549418544437,7.06548396301347,
10.0871915841657));
#110589=CARTESIAN_POINT('Ctrl Pts',(-8.8335196466077,7.0634149499355,10.1154459007797));
#110590=CARTESIAN_POINT('Ctrl Pts',(-8.80661239695558,7.06070777093118,
10.1527908515526));
#110591=CARTESIAN_POINT('Ctrl Pts',(-8.80070812818177,7.06010207118817,
10.161169676074));
#110592=CARTESIAN_POINT('Ctrl Pts',(-8.75070097472611,7.05487442462613,
10.2337427761148));
#110593=CARTESIAN_POINT('Ctrl Pts',(-8.71169961706915,7.05014053212184,
10.3013008316306));
#110594=CARTESIAN_POINT('Ctrl Pts',(-8.64614726578373,7.04103579958989,
10.4391891533336));
#110595=CARTESIAN_POINT('Ctrl Pts',(-8.61925720244162,7.03667148529408,
10.5091050196902));
#110596=CARTESIAN_POINT('Ctrl Pts',(-8.59273551887959,7.0314852943699,10.5978122208329));
#110597=CARTESIAN_POINT('Ctrl Pts',(-8.58795347151401,7.03049923058157,
10.6149377065279));
#110598=CARTESIAN_POINT('Ctrl Pts',(-8.58145605961383,7.02908004295298,
10.6399576878742));
#110599=CARTESIAN_POINT('Ctrl Pts',(-8.57949222847651,7.0286390498249,10.6477855028448));
#110600=CARTESIAN_POINT('Ctrl Pts',(-8.57615710186073,7.02786817090244,
10.6615610834613));
#110601=CARTESIAN_POINT('Ctrl Pts',(-8.57475809043128,7.02753741188211,
10.6675018803389));
#110602=CARTESIAN_POINT('Ctrl Pts',(-8.57192813089073,7.02685251183057,
10.6798652156238));
#110603=CARTESIAN_POINT('Ctrl Pts',(-8.57050324911629,7.0264985693548,10.6862890109489));
#110604=CARTESIAN_POINT('Ctrl Pts',(-8.56692270118805,7.02558475392845,
10.702962292976));
#110605=CARTESIAN_POINT('Ctrl Pts',(-8.56483363060761,7.02502698631723,
10.7132257969748));
#110606=CARTESIAN_POINT('Ctrl Pts',(-8.55676932194068,7.02276748046016,
10.755142773298));
#110607=CARTESIAN_POINT('Ctrl Pts',(-8.5517294903422,7.02109497488892,10.786968124971));
#110608=CARTESIAN_POINT('Ctrl Pts',(-8.54446539887284,7.01809587912323,
10.8452309097326));
#110609=CARTESIAN_POINT('Ctrl Pts',(-8.54190162917352,7.01676107180637,
10.8716112413974));
#110610=CARTESIAN_POINT('Ctrl Pts',(-8.53281531177222,7.01025954382913,
11.0017259039225));
#110611=CARTESIAN_POINT('Ctrl Pts',(-8.53663979392552,7.00533426499684,
11.1058745880121));
#110612=CARTESIAN_POINT('Ctrl Pts',(-8.55832350315784,6.99776949338188,
11.2563498356432));
#110613=CARTESIAN_POINT('Ctrl Pts',(-8.56752747361502,6.99532360438646,
11.3035917846686));
#110614=CARTESIAN_POINT('Ctrl Pts',(-8.58085572767398,6.99235614496052,
11.3576581767258));
#110615=CARTESIAN_POINT('Ctrl Pts',(-8.58272931124193,6.99194886756513,
11.3650118175314));
#110616=CARTESIAN_POINT('Ctrl Pts',(-8.58568852138687,6.99131979713757,
11.3762600628425));
#110617=CARTESIAN_POINT('Ctrl Pts',(-8.58673326666128,6.99110025625424,
11.3801654022495));
#110618=CARTESIAN_POINT('Ctrl Pts',(-8.58868072721365,6.99069554841305,
11.3873261842409));
#110619=CARTESIAN_POINT('Ctrl Pts',(-8.5895785447399,6.9905106599599,11.3905828729979));
#110620=CARTESIAN_POINT('Ctrl Pts',(-8.59162865490153,6.99009224469294,
11.397920070209));
#110621=CARTESIAN_POINT('Ctrl Pts',(-8.59278740213968,6.98985835750087,
11.4019986709788));
#110622=CARTESIAN_POINT('Ctrl Pts',(-8.59581868066643,6.98925322639541,
11.4124945581428));
#110623=CARTESIAN_POINT('Ctrl Pts',(-8.59771746681914,6.98888055647306,
11.4189040842209));
#110624=CARTESIAN_POINT('Ctrl Pts',(-8.61008554598533,6.98649380250803,
11.4596271148942));
#110625=CARTESIAN_POINT('Ctrl Pts',(-8.62176893916401,6.98441935680047,
11.493556501585));
#110626=CARTESIAN_POINT('Ctrl Pts',(-8.63825438343233,6.98172661551061,
11.5362642285839));
#110627=CARTESIAN_POINT('Ctrl Pts',(-8.64191661644619,6.98114108217395,
11.5454722402042));
#110628=CARTESIAN_POINT('Ctrl Pts',(-8.64952006408888,6.97995127098647,
11.5640383745218));
#110629=CARTESIAN_POINT('Ctrl Pts',(-8.65346574080428,6.97934691716196,
11.5733941309488));
#110630=CARTESIAN_POINT('Ctrl Pts',(-8.69075804111194,6.97375669615821,
11.6593112677241));
#110631=CARTESIAN_POINT('Ctrl Pts',(-8.73050539330112,6.96868182988944,
11.7329327269284));
#110632=CARTESIAN_POINT('Ctrl Pts',(-8.81017061667026,6.96009761023257,
11.8543698440775));
#110633=CARTESIAN_POINT('Ctrl Pts',(-8.84725980128844,6.95653097920872,
11.9037883067599));
#110634=CARTESIAN_POINT('Ctrl Pts',(-8.89785229536608,6.95218047500992,
11.9629970899625));
#110635=CARTESIAN_POINT('Ctrl Pts',(-8.90854409431341,6.95128662524302,
11.9750984531));
#110636=CARTESIAN_POINT('Ctrl Pts',(-8.92467187259044,6.94997502970096,
11.9927547428533));
#110637=CARTESIAN_POINT('Ctrl Pts',(-8.9299550951268,6.94955099619432,11.9984470270628));
#110638=CARTESIAN_POINT('Ctrl Pts',(-8.93944272463706,6.94879935740589,
12.0085074450352));
#110639=CARTESIAN_POINT('Ctrl Pts',(-8.94362940555503,6.94847101506171,
12.0128919832518));
#110640=CARTESIAN_POINT('Ctrl Pts',(-8.95251853547159,6.94778081797124,
12.0220861381685));
#110641=CARTESIAN_POINT('Ctrl Pts',(-8.95722715115275,6.9474192392453,12.0268896143853));
#110642=CARTESIAN_POINT('Ctrl Pts',(-8.96982290626582,6.94646248640562,
12.0395631508876));
#110643=CARTESIAN_POINT('Ctrl Pts',(-8.9777671699631,6.94586981145631,12.0473759780709));
#110644=CARTESIAN_POINT('Ctrl Pts',(-9.01333924513926,6.94326197701084,
12.0815692148801));
#110645=CARTESIAN_POINT('Ctrl Pts',(-9.04190557041562,6.94128898570957,
12.1069538353413));
#110646=CARTESIAN_POINT('Ctrl Pts',(-9.18116015542493,6.93215331342288,
12.2212641601196));
#110647=CARTESIAN_POINT('Ctrl Pts',(-9.3033910509643,6.92557886826708,12.2948798789891));
#110648=CARTESIAN_POINT('Ctrl Pts',(-9.45329318071163,6.91731816083869,
12.3577069927749));
#110649=CARTESIAN_POINT('Ctrl Pts',(-9.47245752622063,6.91625706703595,
12.3652675531894));
#110650=CARTESIAN_POINT('Ctrl Pts',(-9.5045180395607,6.91446398585834,12.3771399902268));
#110651=CARTESIAN_POINT('Ctrl Pts',(-9.51732652311142,6.91374295824377,
12.3816812998727));
#110652=CARTESIAN_POINT('Ctrl Pts',(-9.53503155485982,6.91273753847133,
12.3876824798256));
#110653=CARTESIAN_POINT('Ctrl Pts',(-9.53987565486393,6.91246156149984,
12.3892961906095));
#110654=CARTESIAN_POINT('Ctrl Pts',(-9.54805713623244,6.91199378993519,
12.3919741981477));
#110655=CARTESIAN_POINT('Ctrl Pts',(-9.55139012510344,6.91180276582628,
12.3930519373962));
#110656=CARTESIAN_POINT('Ctrl Pts',(-9.55775998119547,6.91143675309572,
12.395086432301));
#110657=CARTESIAN_POINT('Ctrl Pts',(-9.56079615112852,6.91126189241858,
12.3960452594954));
#110658=CARTESIAN_POINT('Ctrl Pts',(-9.56803998918668,6.91084378573381,
12.3983069051391));
#110659=CARTESIAN_POINT('Ctrl Pts',(-9.57225043281855,6.91060002875152,
12.3996006425614));
#110660=CARTESIAN_POINT('Ctrl Pts',(-9.58725552499744,6.90972888388539,
12.4041372045183));
#110661=CARTESIAN_POINT('Ctrl Pts',(-9.59808144697446,6.90909586953382,
12.4072742276474));
#110662=CARTESIAN_POINT('Ctrl Pts',(-9.70419116677746,6.90285494222188,
12.4366973671414));
#110663=CARTESIAN_POINT('Ctrl Pts',(-9.80186423727243,6.8968421742921,12.4533898352714));
#110664=CARTESIAN_POINT('Ctrl Pts',(-9.91638197007264,6.88994948645016,
12.4611963458517));
#110665=CARTESIAN_POINT('Ctrl Pts',(-9.93231448413549,6.88899350107593,
12.4620210044104));
#110666=CARTESIAN_POINT('Ctrl Pts',(-10.0052699898543,6.88463431937991,
12.4646019850538));
#110667=CARTESIAN_POINT('Ctrl Pts',(-10.062355610644,6.88127720938945,12.4632838156791));
#110668=CARTESIAN_POINT('Ctrl Pts',(-10.1524638379184,6.87610293892573,
12.4559187366513));
#110669=CARTESIAN_POINT('Ctrl Pts',(-10.1856038309028,6.87422631486022,
12.4520661348605));
#110670=CARTESIAN_POINT('Ctrl Pts',(-10.2287134318626,6.87181886743842,
12.4455543355882));
#110671=CARTESIAN_POINT('Ctrl Pts',(-10.2388254674448,6.87125657780794,
12.4439181329313));
#110672=CARTESIAN_POINT('Ctrl Pts',(-10.2553541109633,6.87034128615449,
12.4410652876855));
#110673=CARTESIAN_POINT('Ctrl Pts',(-10.2617811125795,6.86998632774579,
12.4399116418629));
#110674=CARTESIAN_POINT('Ctrl Pts',(-10.2742190242701,6.86930115751591,
12.4375930095948));
#110675=CARTESIAN_POINT('Ctrl Pts',(-10.2802307584783,6.86897078994783,
12.4364332417742));
#110676=CARTESIAN_POINT('Ctrl Pts',(-10.2941326693982,6.86820861189812,
12.4336607252557));
#110677=CARTESIAN_POINT('Ctrl Pts',(-10.3020172058147,6.86777767454006,
12.4320205002849));
#110678=CARTESIAN_POINT('Ctrl Pts',(-10.3276498940332,6.86638077003142,
12.4264669972027));
#110679=CARTESIAN_POINT('Ctrl Pts',(-10.3453391321258,6.8654231692313,12.4222881104743));
#110680=CARTESIAN_POINT('Ctrl Pts',(-10.469047016273,6.85876269919855,12.3906193616769));
#110681=CARTESIAN_POINT('Ctrl Pts',(-10.5717632578918,6.85345611235032,
12.3516347713466));
#110682=CARTESIAN_POINT('Ctrl Pts',(-10.724107995675,6.84511572138444,12.2733087085237));
#110683=CARTESIAN_POINT('Ctrl Pts',(-10.7771938259892,6.84210007925424,
12.2416183972237));
#110684=CARTESIAN_POINT('Ctrl Pts',(-10.8437015816534,6.83798473529962,
12.1959754356813));
#110685=CARTESIAN_POINT('Ctrl Pts',(-10.8590786120089,6.83700784214176,
12.1849782628524));
#110686=CARTESIAN_POINT('Ctrl Pts',(-10.8844607448046,6.83534463086534,
12.1660720117431));
#110687=CARTESIAN_POINT('Ctrl Pts',(-10.8945835265429,6.83466734487077,
12.1583242369763));
#110688=CARTESIAN_POINT('Ctrl Pts',(-10.9085175908693,6.83371347387333,
12.1473677831018));
#110689=CARTESIAN_POINT('Ctrl Pts',(-10.912415924773,6.83344421660625,12.1442701697531));
#110690=CARTESIAN_POINT('Ctrl Pts',(-10.9190104131131,6.83298451260617,
12.1389750692726));
#110691=CARTESIAN_POINT('Ctrl Pts',(-10.9217147199965,6.83279477540441,
12.1367877209861));
#110692=CARTESIAN_POINT('Ctrl Pts',(-10.9269008966038,6.83242850431745,
12.1325622681523));
#110693=CARTESIAN_POINT('Ctrl Pts',(-10.9293838868846,6.83225208005877,
12.1305256095097));
#110694=CARTESIAN_POINT('Ctrl Pts',(-10.9353369711805,6.83182657188449,
12.1256097599674));
#110695=CARTESIAN_POINT('Ctrl Pts',(-10.9388004799934,6.83157693647195,
12.1227226901884));
#110696=CARTESIAN_POINT('Ctrl Pts',(-10.9514388586231,6.83065856518419,
12.1120883718689));
#110697=CARTESIAN_POINT('Ctrl Pts',(-10.96053137352,6.82998337766097,12.104244497471));
#110698=CARTESIAN_POINT('Ctrl Pts',(-11.0265147817711,6.82498294556569,
12.0458907420029));
#110699=CARTESIAN_POINT('Ctrl Pts',(-11.0794823117569,6.82041795675947,
11.9911286816822));
#110700=CARTESIAN_POINT('Ctrl Pts',(-11.2031723763488,6.80873744319932,
11.841514216691));
#110701=CARTESIAN_POINT('Ctrl Pts',(-11.2671232508944,6.80168190025662,
11.7417398203432));
#110702=CARTESIAN_POINT('Ctrl Pts',(-11.3253539387938,6.79419054166257,
11.6209076177256));
#110703=CARTESIAN_POINT('Ctrl Pts',(-11.3320770638389,6.79330304820856,
11.6063497814011));
#110704=CARTESIAN_POINT('Ctrl Pts',(-11.3416907887255,6.79199891377795,
11.5846007634169));
#110705=CARTESIAN_POINT('Ctrl Pts',(-11.3447655545249,6.79157608802882,
11.5774927113951));
#110706=CARTESIAN_POINT('Ctrl Pts',(-11.3501454195933,6.79082579901812,
11.5647798831403));
#110707=CARTESIAN_POINT('Ctrl Pts',(-11.3524723840587,6.79049760832443,
11.5591846048779));
#110708=CARTESIAN_POINT('Ctrl Pts',(-11.3573133149562,6.78980693153303,
11.5473373901969));
#110709=CARTESIAN_POINT('Ctrl Pts',(-11.3598189957754,6.78944472753037,
11.541082206751));
#110710=CARTESIAN_POINT('Ctrl Pts',(-11.3663729330044,6.78848446538371,
11.5243878497351));
#110711=CARTESIAN_POINT('Ctrl Pts',(-11.3703447892138,6.78788893975489,
11.513919037311));
#110712=CARTESIAN_POINT('Ctrl Pts',(-11.3874997146924,6.78525332632198,
11.4670895245127));
#110713=CARTESIAN_POINT('Ctrl Pts',(-11.399359055975,6.78325653638187,11.430258809936));
#110714=CARTESIAN_POINT('Ctrl Pts',(-11.4139271728694,6.78050716281447,
11.378000840298));
#110715=CARTESIAN_POINT('Ctrl Pts',(-11.4178687848717,6.77972408663825,
11.3629363738974));
#110716=CARTESIAN_POINT('Ctrl Pts',(-11.4494951677349,6.7730742334028,11.233673592005));
#110717=CARTESIAN_POINT('Ctrl Pts',(-11.4635714444221,6.76755111586632,
11.1165980425647));
#110718=CARTESIAN_POINT('Ctrl Pts',(-11.4634997273561,6.7616401361251,10.9991066755872));
#110719=CARTESIAN_POINT('Ctrl Pts',(-11.4634997643993,6.68841475560911,
10.9991695764457));
#110720=CARTESIAN_POINT('Ctrl Pts',(-11.4635596206349,6.69465254772556,
11.1046574160703));
#110721=CARTESIAN_POINT('Ctrl Pts',(-11.4522146970128,6.70110730256879,
11.209849775773));
#110722=CARTESIAN_POINT('Ctrl Pts',(-11.4211342010557,6.70965114077867,
11.351849419943));
#110723=CARTESIAN_POINT('Ctrl Pts',(-11.4110261863502,6.71195754463812,
11.3904176223993));
#110724=CARTESIAN_POINT('Ctrl Pts',(-11.3917335017398,6.71569346635609,
11.4534178352096));
#110725=CARTESIAN_POINT('Ctrl Pts',(-11.3834482721036,6.7171491391733,11.4781013206337));
#110726=CARTESIAN_POINT('Ctrl Pts',(-11.3712930632926,6.71909954638602,
11.5113465275355));
#110727=CARTESIAN_POINT('Ctrl Pts',(-11.3679931312654,6.71961273076903,
11.5201103105693));
#110728=CARTESIAN_POINT('Ctrl Pts',(-11.3623169939192,6.72046890608534,
11.534756859286));
#110729=CARTESIAN_POINT('Ctrl Pts',(-11.3599862720804,6.72081338656028,
11.540656852341));
#110730=CARTESIAN_POINT('Ctrl Pts',(-11.3553161936784,6.72148995799427,
11.5522573952519));
#110731=CARTESIAN_POINT('Ctrl Pts',(-11.3529790527169,6.72182211386263,
11.5579586901893));
#110732=CARTESIAN_POINT('Ctrl Pts',(-11.3477580431241,6.72255026285652,
11.57046926897));
#110733=CARTESIAN_POINT('Ctrl Pts',(-11.3448584222279,6.72294572077665,
11.5772718220309));
#110734=CARTESIAN_POINT('Ctrl Pts',(-11.3344909228821,6.72432906175696,
11.6010919935522));
#110735=CARTESIAN_POINT('Ctrl Pts',(-11.3267504221815,6.72530779114599,
11.6179894545839));
#110736=CARTESIAN_POINT('Ctrl Pts',(-11.2766454447452,6.73132937679715,
11.722084684804));
#110737=CARTESIAN_POINT('Ctrl Pts',(-11.2260258169689,6.73607248076768,
11.8050421951749));
#110738=CARTESIAN_POINT('Ctrl Pts',(-11.1261687554777,6.74413250657181,
11.9371718856615));
#110739=CARTESIAN_POINT('Ctrl Pts',(-11.0809664536226,6.74745833987433,
11.9889679656975));
#110740=CARTESIAN_POINT('Ctrl Pts',(-11.0167360987691,6.75205032575716,
12.0528826982318));
#110741=CARTESIAN_POINT('Ctrl Pts',(-11.0008275543021,6.75317835845129,
12.0680161016339));
#110742=CARTESIAN_POINT('Ctrl Pts',(-10.9774301987005,6.75483448910199,
12.0892915056516));
#110743=CARTESIAN_POINT('Ctrl Pts',(-10.9702108924955,6.75534511029105,
12.0957265136211));
#110744=CARTESIAN_POINT('Ctrl Pts',(-10.9573211899641,6.75625721875792,
12.1069886333773));
#110745=CARTESIAN_POINT('Ctrl Pts',(-10.9516766695869,6.75665677925589,
12.1118449564195));
#110746=CARTESIAN_POINT('Ctrl Pts',(-10.9429141605765,6.75727770326757,
12.1192682628368));
#110747=CARTESIAN_POINT('Ctrl Pts',(-10.9398221121522,6.75749693334687,
12.1218658365089));
#110748=CARTESIAN_POINT('Ctrl Pts',(-10.9367033181617,6.75771822830531,
12.1244639363637));
#110749=CARTESIAN_POINT('Ctrl Pts',(-10.936687245989,6.75771936871561,12.1244773246442));
#110750=CARTESIAN_POINT('Ctrl Pts',(-10.9366549958661,6.75772165705071,
12.124504188148));
#110751=CARTESIAN_POINT('Ctrl Pts',(-10.9366388180197,6.75772280496821,
12.124517663277));
#110752=CARTESIAN_POINT('Ctrl Pts',(-10.936606354723,6.75772510844752,12.1245447019757));
#110753=CARTESIAN_POINT('Ctrl Pts',(-10.9365900693055,6.75772626400706,
12.1245582655103));
#110754=CARTESIAN_POINT('Ctrl Pts',(-10.936560560025,6.75772835789669,12.1245828416359));
#110755=CARTESIAN_POINT('Ctrl Pts',(-10.9365473361729,6.75772929622445,
12.124593854422));
#110756=CARTESIAN_POINT('Ctrl Pts',(-10.9365204687927,6.75773120266519,
12.1246162286965));
#110757=CARTESIAN_POINT('Ctrl Pts',(-10.9365068251932,6.75773217078344,
12.124627590219));
#110758=CARTESIAN_POINT('Ctrl Pts',(-10.9338974646006,6.75791732559571,
12.126800419463));
#110759=CARTESIAN_POINT('Ctrl Pts',(-10.931294353513,6.75810216095389,12.1289528272895));
#110760=CARTESIAN_POINT('Ctrl Pts',(-10.925434312204,6.75851853404814,12.1337641999434));
#110761=CARTESIAN_POINT('Ctrl Pts',(-10.9221733865764,6.75875041506592,
12.1364181323202));
#110762=CARTESIAN_POINT('Ctrl Pts',(-10.9125918148215,6.75943216748588,
12.1441477803177));
#110763=CARTESIAN_POINT('Ctrl Pts',(-10.9062404811443,6.75988460760571,
12.1491849929213));
#110764=CARTESIAN_POINT('Ctrl Pts',(-10.8512860636664,6.76380139628221,
12.1920301981794));
#110765=CARTESIAN_POINT('Ctrl Pts',(-10.800387720404,6.76744073829635,12.2267852145416));
#110766=CARTESIAN_POINT('Ctrl Pts',(-10.6974610577549,6.77460959539087,
12.2879294159088));
#110767=CARTESIAN_POINT('Ctrl Pts',(-10.6457371176473,6.77812759376995,
12.3146246050011));
#110768=CARTESIAN_POINT('Ctrl Pts',(-10.5404023784224,6.78500663497827,
12.361268391505));
#110769=CARTESIAN_POINT('Ctrl Pts',(-10.4869332522373,6.78836355042131,
12.3812977130133));
#110770=CARTESIAN_POINT('Ctrl Pts',(-10.400564024567,6.79353766959075,12.4080103268243));
#110771=CARTESIAN_POINT('Ctrl Pts',(-10.3683718262633,6.79541432398389,
12.4167734710581));
#110772=CARTESIAN_POINT('Ctrl Pts',(-10.325934941767,6.79782190304961,12.426780859836));
#110773=CARTESIAN_POINT('Ctrl Pts',(-10.3159389462908,6.79838429359283,
12.4290275707402));
#110774=CARTESIAN_POINT('Ctrl Pts',(-10.2995331075555,6.79929977277371,
12.4325344057825));
#110775=CARTESIAN_POINT('Ctrl Pts',(-10.2931370762307,6.79965481830326,
12.433856883629));
#110776=CARTESIAN_POINT('Ctrl Pts',(-10.2807267349852,6.8003401739254,12.436336401126));
#110777=CARTESIAN_POINT('Ctrl Pts',(-10.2747136029402,6.80067063971098,
12.4374985895158));
#110778=CARTESIAN_POINT('Ctrl Pts',(-10.2607742176017,6.80143307072447,
12.440102064692));
#110779=CARTESIAN_POINT('Ctrl Pts',(-10.2528429650155,6.80186416204719,
12.441515725838));
#110780=CARTESIAN_POINT('Ctrl Pts',(-10.226973677596,6.80326169070453,12.4459065747587));
#110781=CARTESIAN_POINT('Ctrl Pts',(-10.2089913885507,6.80421975292176,
12.4486150320302));
#110782=CARTESIAN_POINT('Ctrl Pts',(-10.0825181581231,6.81087316484412,
12.465260021753));
#110783=CARTESIAN_POINT('Ctrl Pts',(-9.97281575410425,6.8161734292533,12.4673307946257));
#110784=CARTESIAN_POINT('Ctrl Pts',(-9.80230389895589,6.8245113964672,12.4514046751808));
#110785=CARTESIAN_POINT('Ctrl Pts',(-9.74113952392938,6.82753142975883,
12.4417522538084));
#110786=CARTESIAN_POINT('Ctrl Pts',(-9.66230781691713,6.8316523822422,12.4241328122582));
#110787=CARTESIAN_POINT('Ctrl Pts',(-9.64392431924812,6.83263016155143,
12.4196479599916));
#110788=CARTESIAN_POINT('Ctrl Pts',(-9.61330104291238,6.83429478108754,
12.4115448664109));
#110789=CARTESIAN_POINT('Ctrl Pts',(-9.60101199952237,6.83497257085374,
12.4081205726034));
#110790=CARTESIAN_POINT('Ctrl Pts',(-9.58398886581891,6.8359270814273,12.4031364160519));
#110791=CARTESIAN_POINT('Ctrl Pts',(-9.57921527111767,6.83619646287801,
12.4017122658729));
#110792=CARTESIAN_POINT('Ctrl Pts',(-9.5711201006356,6.83665635430977,12.399252081574));
#110793=CARTESIAN_POINT('Ctrl Pts',(-9.56779472887721,6.83684615392292,
12.398228507537));
#110794=CARTESIAN_POINT('Ctrl Pts',(-9.56140640637077,6.83721252755628,
12.3962371674203));
#110795=CARTESIAN_POINT('Ctrl Pts',(-9.55834295290392,6.83738899176279,
12.3952711637525));
#110796=CARTESIAN_POINT('Ctrl Pts',(-9.55098632490768,6.83781457454818,
12.3929247311359));
#110797=CARTESIAN_POINT('Ctrl Pts',(-9.54669632905109,6.83806424467616,
12.3915345370642));
#110798=CARTESIAN_POINT('Ctrl Pts',(-9.53100804341105,6.83898257141541,
12.3863704261707));
#110799=CARTESIAN_POINT('Ctrl Pts',(-9.51965019969326,6.83965767753596,
12.382476207544));
#110800=CARTESIAN_POINT('Ctrl Pts',(-9.43749790342484,6.84460908323368,
12.3531744196968));
#110801=CARTESIAN_POINT('Ctrl Pts',(-9.36871298539436,6.84911980188319,
12.3224841928642));
#110802=CARTESIAN_POINT('Ctrl Pts',(-9.24580651655688,6.85753112946694,
12.2558651377387));
#110803=CARTESIAN_POINT('Ctrl Pts',(-9.19111270191376,6.86141953108565,
12.221354669168));
#110804=CARTESIAN_POINT('Ctrl Pts',(-9.106487214051,6.86757262508375,12.1597722687065));
#110805=CARTESIAN_POINT('Ctrl Pts',(-9.07507788678621,6.86989140837263,
12.1348816196434));
#110806=CARTESIAN_POINT('Ctrl Pts',(-9.02493341345033,6.87364491368361,
12.0916776329038));
#110807=CARTESIAN_POINT('Ctrl Pts',(-9.00559884993795,6.87510610501388,
12.0740956092025));
#110808=CARTESIAN_POINT('Ctrl Pts',(-8.97997831504608,6.87706260830936,
12.049512240444));
#110809=CARTESIAN_POINT('Ctrl Pts',(-8.97327458908032,6.87757651946804,
12.042954992752));
#110810=CARTESIAN_POINT('Ctrl Pts',(-8.96214034442399,6.87843356710357,
12.0318526348162));
#110811=CARTESIAN_POINT('Ctrl Pts',(-8.95767559755155,6.87877819972474,
12.0273423803525));
#110812=CARTESIAN_POINT('Ctrl Pts',(-8.94893551096392,6.87945481705159,
12.0183975796382));
#110813=CARTESIAN_POINT('Ctrl Pts',(-8.94465855400984,6.87978686854312,
12.0139648042662));
#110814=CARTESIAN_POINT('Ctrl Pts',(-8.93531452630345,6.88051448902606,
12.0041571853324));
#110815=CARTESIAN_POINT('Ctrl Pts',(-8.93025988756787,6.88090952577499,
11.9987706970588));
#110816=CARTESIAN_POINT('Ctrl Pts',(-8.91266695579176,6.88228977137671,
11.9797359713842));
#110817=CARTESIAN_POINT('Ctrl Pts',(-8.90034704673645,6.88326588206761,
11.9658877499353));
#110818=CARTESIAN_POINT('Ctrl Pts',(-8.82312638224702,6.88945519900141,
11.8756944872158));
#110819=CARTESIAN_POINT('Ctrl Pts',(-8.76594740758156,6.89434531659248,
11.7930882446873));
#110820=CARTESIAN_POINT('Ctrl Pts',(-8.6845843936025,6.9025607224419,11.6451533630232));
#110821=CARTESIAN_POINT('Ctrl Pts',(-8.65578693194417,6.90589048998634,
11.5827787862363));
#110822=CARTESIAN_POINT('Ctrl Pts',(-8.62436771221342,6.91040212822098,
11.499870052806));
#110823=CARTESIAN_POINT('Ctrl Pts',(-8.61764887438325,6.91143596060002,
11.4809777128369));
#110824=CARTESIAN_POINT('Ctrl Pts',(-8.60711602913687,6.91318715110918,
11.4493149457309));
#110825=CARTESIAN_POINT('Ctrl Pts',(-8.60308441241113,6.91389419573213,
11.4366193917475));
#110826=CARTESIAN_POINT('Ctrl Pts',(-8.59775927101976,6.91488320898456,
11.4190213136626));
#110827=CARTESIAN_POINT('Ctrl Pts',(-8.59631697546259,6.91515711867852,
11.4141640839236));
#110828=CARTESIAN_POINT('Ctrl Pts',(-8.59392225571318,6.91562243909074,
11.4059431587993));
#110829=CARTESIAN_POINT('Ctrl Pts',(-8.59295659325351,6.91581309847896,
11.4025833111748));
#110830=CARTESIAN_POINT('Ctrl Pts',(-8.59113191896735,6.91617926557934,
11.396147923076));
#110831=CARTESIAN_POINT('Ctrl Pts',(-8.59027092137268,6.91635465099388,
11.3930729845457));
#110832=CARTESIAN_POINT('Ctrl Pts',(-8.58823734789646,6.91677514533323,
11.3857177210569));
#110833=CARTESIAN_POINT('Ctrl Pts',(-8.58707417229547,6.91702077789832,
11.3814348575776));
#110834=CARTESIAN_POINT('Ctrl Pts',(-8.5829733289263,6.91790525209883,11.3660592078926));
#110835=CARTESIAN_POINT('Ctrl Pts',(-8.58014674692846,6.91854994073291,
11.3549375345572));
#110836=CARTESIAN_POINT('Ctrl Pts',(-8.55525738325087,6.92455795344609,
11.2519475240842));
#110837=CARTESIAN_POINT('Ctrl Pts',(-8.54201023192169,6.93029099700035,
11.1581841658445));
#110838=CARTESIAN_POINT('Ctrl Pts',(-8.53479068798238,6.94024356716922,
10.9927497908704));
#110839=CARTESIAN_POINT('Ctrl Pts',(-8.53687350116914,6.94447698571966,
10.9215560388103));
#110840=CARTESIAN_POINT('Ctrl Pts',(-8.54671279346841,6.95003209912957,
10.8255516136567));
#110841=CARTESIAN_POINT('Ctrl Pts',(-8.54995544707844,6.95147470153436,
10.8003832501425));
#110842=CARTESIAN_POINT('Ctrl Pts',(-8.55670221171229,6.95393937509521,
10.7569595892465));
#110843=CARTESIAN_POINT('Ctrl Pts',(-8.55990258801024,6.95497031224033,
10.738663750576));
#110844=CARTESIAN_POINT('Ctrl Pts',(-8.56501931171436,6.95644150215379,
10.7123715498377));
#110845=CARTESIAN_POINT('Ctrl Pts',(-8.56665603741354,6.95689045244903,
10.7043231665356));
#110846=CARTESIAN_POINT('Ctrl Pts',(-8.56963187842073,6.95767058285896,
10.6902955881215));
#110847=CARTESIAN_POINT('Ctrl Pts',(-8.57094094156094,6.95800270038842,
10.6843102867705));
#110848=CARTESIAN_POINT('Ctrl Pts',(-8.57372183266004,6.95868610746447,
10.6719673459886));
#110849=CARTESIAN_POINT('Ctrl Pts',(-8.5751986768565,6.95903723004494,10.6656109688098));
#110850=CARTESIAN_POINT('Ctrl Pts',(-8.57909721034724,6.95993477954982,
10.6493264480112));
#110851=CARTESIAN_POINT('Ctrl Pts',(-8.5815804823815,6.96047924474578,10.639413315821));
#110852=CARTESIAN_POINT('Ctrl Pts',(-8.59179660425233,6.96261678767688,
10.6003704929802));
#110853=CARTESIAN_POINT('Ctrl Pts',(-8.60032488815041,6.96418455636908,
10.5714556132168));
#110854=CARTESIAN_POINT('Ctrl Pts',(-8.64931794281183,6.97221718918085,
10.4224693081286));
#110855=CARTESIAN_POINT('Ctrl Pts',(-8.70435208244871,6.97819022558426,
10.30777233117));
#110856=CARTESIAN_POINT('Ctrl Pts',(-8.80304301882541,6.98714115844825,
10.1561603744093));
#110857=CARTESIAN_POINT('Ctrl Pts',(-8.83511778071097,6.98987959308141,
10.112407985125));
#110858=CARTESIAN_POINT('Ctrl Pts',(-8.87447554567043,6.99318018156136,
10.0645389854067));
#110859=CARTESIAN_POINT('Ctrl Pts',(-8.8794571799808,6.99359696272611,10.0585774644861));
#110860=CARTESIAN_POINT('Ctrl Pts',(-8.88712782911316,6.99423771814737,
10.0495451412914));
#110861=CARTESIAN_POINT('Ctrl Pts',(-8.88978269394219,6.9944593091221,10.046445366176));
#110862=CARTESIAN_POINT('Ctrl Pts',(-8.89465831517188,6.99486601744895,
10.0408006368541));
#110863=CARTESIAN_POINT('Ctrl Pts',(-8.89687494649953,6.99505083821138,
10.0382522293942));
#110864=CARTESIAN_POINT('Ctrl Pts',(-8.90186664747618,6.99546685624546,
10.0325533523104));
#110865=CARTESIAN_POINT('Ctrl Pts',(-8.90464644145621,6.99569839392618,
10.0294071621228));
#110866=CARTESIAN_POINT('Ctrl Pts',(-8.91281440591627,6.9963782185712,10.0202423819891));
#110867=CARTESIAN_POINT('Ctrl Pts',(-8.91823882983352,6.99682905309783,
10.0142564883552));
#110868=CARTESIAN_POINT('Ctrl Pts',(-8.96348025735389,7.00058158956052,
9.96515537879881));
#110869=CARTESIAN_POINT('Ctrl Pts',(-9.00580467843273,7.0040424364072,9.92442996982021));
#110870=CARTESIAN_POINT('Ctrl Pts',(-9.1114479478125,7.01234521357501,9.83435325367631));
#110871=CARTESIAN_POINT('Ctrl Pts',(-9.17661448509601,7.0172096414026,9.78744302364161));
#110872=CARTESIAN_POINT('Ctrl Pts',(-9.28339623073772,7.02457285237012,
9.72317233696785));
#110873=CARTESIAN_POINT('Ctrl Pts',(-9.32252494562857,7.02715903392574,
9.70198693577445));
#110874=CARTESIAN_POINT('Ctrl Pts',(-9.37951920580308,7.03075920786257,
9.67440927619339));
#110875=CARTESIAN_POINT('Ctrl Pts',(-9.39663530535511,7.03181999763212,
9.66653148754627));
#110876=CARTESIAN_POINT('Ctrl Pts',(-9.42738996569851,7.033690238135,9.65308992076048));
#110877=CARTESIAN_POINT('Ctrl Pts',(-9.44096915358737,7.03450384766016,
9.6473974908191));
#110878=CARTESIAN_POINT('Ctrl Pts',(-9.46158021269106,7.03572089436225,
9.63912071040134));
#110879=CARTESIAN_POINT('Ctrl Pts',(-9.46854953560157,7.03612937634007,
9.63638395616053));
#110880=CARTESIAN_POINT('Ctrl Pts',(-9.48117520591405,7.03686398601031,
9.6315375335166));
#110881=CARTESIAN_POINT('Ctrl Pts',(-9.48682415334722,7.03719072644186,
9.62940916351712));
#110882=CARTESIAN_POINT('Ctrl Pts',(-9.49896166157556,7.03788869140184,
9.62492163954777));
#110883=CARTESIAN_POINT('Ctrl Pts',(-9.50545408993207,7.03825955336081,
9.62257331991396));
#110884=CARTESIAN_POINT('Ctrl Pts',(-9.52294108723694,7.03925192986872,
9.61638782823135));
#110885=CARTESIAN_POINT('Ctrl Pts',(-9.53396536051974,7.03987066146595,
9.61263574599982));
#110886=CARTESIAN_POINT('Ctrl Pts',(-9.58811423622361,7.04287760391771,
9.59492460117495));
#110887=CARTESIAN_POINT('Ctrl Pts',(-9.63182852509501,7.04520492408939,
9.58284191736915));
#110888=CARTESIAN_POINT('Ctrl Pts',(-9.78423708315833,7.05306792450703,
9.54824613456444));
#110889=CARTESIAN_POINT('Ctrl Pts',(-9.89487357590158,7.05831780018609,
9.53607028072708));
#110890=CARTESIAN_POINT('Ctrl Pts',(-10.0576063249621,7.06638689262537,
9.53671755362674));
#110891=CARTESIAN_POINT('Ctrl Pts',(-10.1093394153086,7.06900949152846,
9.53967199929593));
#110892=CARTESIAN_POINT('Ctrl Pts',(-10.1684579706689,7.07217796807265,
9.54620720277377));
#110893=CARTESIAN_POINT('Ctrl Pts',(-10.1761072977786,7.07259126945369,
9.54711397566859));
#110894=CARTESIAN_POINT('Ctrl Pts',(-10.1877842264288,7.0732277616402,9.54859176018141));
#110895=CARTESIAN_POINT('Ctrl Pts',(-10.1918173129703,7.07344861767979,
9.54911926336385));
#110896=CARTESIAN_POINT('Ctrl Pts',(-10.1991958458437,7.07385462334052,
9.55011563330863));
#110897=CARTESIAN_POINT('Ctrl Pts',(-10.20254191379,7.074039482978,9.55057927627422));
#110898=CARTESIAN_POINT('Ctrl Pts',(-10.2100583424044,7.07445640792961,
9.55164731519162));
#110899=CARTESIAN_POINT('Ctrl Pts',(-10.2142276849319,7.07468882097198,
9.55225813595572));
#110900=CARTESIAN_POINT('Ctrl Pts',(-10.2264533211291,7.075373565619,9.5541031949715));
#110901=CARTESIAN_POINT('Ctrl Pts',(-10.2345018789549,7.0758284989442,9.55538671609043));
#110902=CARTESIAN_POINT('Ctrl Pts',(-10.3078234901115,7.08000812844363,
9.56770835294022));
#110903=CARTESIAN_POINT('Ctrl Pts',(-10.372282147508,7.08393458619773,9.58309529959434));
#110904=CARTESIAN_POINT('Ctrl Pts',(-10.4875332723914,7.09117586774178,
9.61901580600354));
#110905=CARTESIAN_POINT('Ctrl Pts',(-10.5386490922233,7.09447156149936,
9.63813973876635));
#110906=CARTESIAN_POINT('Ctrl Pts',(-10.6401391103683,7.10108758056456,
9.68272037176556));
#110907=CARTESIAN_POINT('Ctrl Pts',(-10.6903529533229,7.10439947000089,
9.70832764716165));
#110908=CARTESIAN_POINT('Ctrl Pts',(-10.7675153925176,7.10951403615734,
9.753466374741));
#110909=CARTESIAN_POINT('Ctrl Pts',(-10.7954883212648,7.11137446234339,
9.77112875628979));
#110910=CARTESIAN_POINT('Ctrl Pts',(-10.8312877400935,7.11376468940601,
9.79546802277862));
#110911=CARTESIAN_POINT('Ctrl Pts',(-10.8396748426178,7.11432539340569,
9.80129955491489));
#110912=CARTESIAN_POINT('Ctrl Pts',(-10.8533180527149,7.11523883469738,
9.81099910781346));
#110913=CARTESIAN_POINT('Ctrl Pts',(-10.8586104666825,7.11559351216091,
9.81481525105749));
#110914=CARTESIAN_POINT('Ctrl Pts',(-10.8688229835966,7.11627864218418,
9.82228338980021));
#110915=CARTESIAN_POINT('Ctrl Pts',(-10.8737460130215,7.1166092466612,9.82593113614986));
#110916=CARTESIAN_POINT('Ctrl Pts',(-10.8851019019041,7.11737269581499,
9.83445633246428));
#110917=CARTESIAN_POINT('Ctrl Pts',(-10.8915176356738,7.1178046591728,9.83935633095636));
#110918=CARTESIAN_POINT('Ctrl Pts',(-10.9123261435831,7.11920804880857,
9.85552311663579));
#110919=CARTESIAN_POINT('Ctrl Pts',(-10.9265487481129,7.12017099976067,
9.86700671447932));
#110920=CARTESIAN_POINT('Ctrl Pts',(-11.0228812499225,7.12672812389165,
9.94781487178806));
#110921=CARTESIAN_POINT('Ctrl Pts',(-11.0973535634865,7.13194305879504,
10.0257324668975));
#110922=CARTESIAN_POINT('Ctrl Pts',(-11.2010379905446,7.14025260861692,
10.1613467890855));
#110923=CARTESIAN_POINT('Ctrl Pts',(-11.2361488756505,7.14333590560624,
10.2140188271637));
#110924=CARTESIAN_POINT('Ctrl Pts',(-11.2773138678577,7.14753689633787,
10.2853891767278));
#110925=CARTESIAN_POINT('Ctrl Pts',(-11.2865594175158,7.1485265178306,10.3021718318176));
#110926=CARTESIAN_POINT('Ctrl Pts',(-11.3014632376028,7.15020946816211,
10.3305289356323));
#110927=CARTESIAN_POINT('Ctrl Pts',(-11.3073031112047,7.15089348681348,
10.3420056095124));
#110928=CARTESIAN_POINT('Ctrl Pts',(-11.3151991144883,7.15185535313083,
10.358043195592));
#110929=CARTESIAN_POINT('Ctrl Pts',(-11.3173846064278,7.15212571102489,
10.3625401606742));
#110930=CARTESIAN_POINT('Ctrl Pts',(-11.3210532888134,7.15258677019925,
10.3701884500572));
#110931=CARTESIAN_POINT('Ctrl Pts',(-11.3225483744618,7.15277675232312,
10.3733340783712));
#110932=CARTESIAN_POINT('Ctrl Pts',(-11.3253989295665,7.15314306939153,
10.379387223557));
#110933=CARTESIAN_POINT('Ctrl Pts',(-11.3267560862256,7.15331929178104,
10.3822938983339));
#110934=CARTESIAN_POINT('Ctrl Pts',(-11.3299914011575,7.15374373939651,
10.3892829491349));
#110935=CARTESIAN_POINT('Ctrl Pts',(-11.3318603231066,7.15399250992289,
10.3933695342104));
#110936=CARTESIAN_POINT('Ctrl Pts',(-11.3386024419502,7.1549029586282,10.4082931949829));
#110937=CARTESIAN_POINT('Ctrl Pts',(-11.3433622987065,7.15557094237555,
10.4191806159882));
#110938=CARTESIAN_POINT('Ctrl Pts',(-11.3813285017043,7.16110445648099,
10.5089862202344));
#110939=CARTESIAN_POINT('Ctrl Pts',(-11.4076807520629,7.1662729506619,10.5906155383671));
#110940=CARTESIAN_POINT('Ctrl Pts',(-11.4511307273162,7.17801205783973,
10.7808173744109));
#110941=CARTESIAN_POINT('Ctrl Pts',(-11.4634631656624,7.18451521436854,
10.8899792019832));
#110942=CARTESIAN_POINT('Ctrl Pts',(-11.4634999176129,7.19062697242339,
10.9995089326331));
#110943=CARTESIAN_POINT('Origin',(-10.,3.5,11.));
#110944=CARTESIAN_POINT('',(-11.4635,7.76057136598891,11.0000000000874));
#110945=CARTESIAN_POINT('',(-11.4635,7.68921734064608,10.9999999999359));
#110946=CARTESIAN_POINT('',(-11.4635,3.5,11.));
#110947=CARTESIAN_POINT('Ctrl Pts',(-11.4635,7.76057136598891,11.0000000000874));
#110948=CARTESIAN_POINT('Ctrl Pts',(-11.4635000000058,7.75473127865624,
10.9028434297529));
#110949=CARTESIAN_POINT('Ctrl Pts',(-11.4538253005981,7.7489810398877,10.8059141974648));
#110950=CARTESIAN_POINT('Ctrl Pts',(-11.4309379328563,7.74248848403828,
10.6924387728171));
#110951=CARTESIAN_POINT('Ctrl Pts',(-11.4269190101869,7.74145735128413,
10.6743015829138));
#110952=CARTESIAN_POINT('Ctrl Pts',(-11.4208195038144,7.74003105896416,
10.6490600788052));
#110953=CARTESIAN_POINT('Ctrl Pts',(-11.4190288127671,7.73962679038549,
10.6418881151906));
#110954=CARTESIAN_POINT('Ctrl Pts',(-11.4156464487612,7.73888881646997,
10.6287651356866));
#110955=CARTESIAN_POINT('Ctrl Pts',(-11.4140714018754,7.73855459083289,
10.6228100420527));
#110956=CARTESIAN_POINT('Ctrl Pts',(-11.4107985129743,7.73787869048468,
10.6107442669031));
#110957=CARTESIAN_POINT('Ctrl Pts',(-11.4090984531808,7.73753709493676,
10.6046343199833));
#110958=CARTESIAN_POINT('Ctrl Pts',(-11.4047904693904,7.73669434877157,
10.5895324136441));
#110959=CARTESIAN_POINT('Ctrl Pts',(-11.4021358548523,7.73619470522345,
10.5805539935445));
#110960=CARTESIAN_POINT('Ctrl Pts',(-11.3917758517176,7.73431615923099,
10.5467122791798));
#110961=CARTESIAN_POINT('Ctrl Pts',(-11.3834935563223,7.73295584064186,
10.5220298472499));
#110962=CARTESIAN_POINT('Ctrl Pts',(-11.3608759729155,7.72956019734486,
10.4601509757774));
#110963=CARTESIAN_POINT('Ctrl Pts',(-11.3456713366948,7.72755175465078,
10.4232944180265));
#110964=CARTESIAN_POINT('Ctrl Pts',(-11.3018348496926,7.72235356665669,
10.3282412400242));
#110965=CARTESIAN_POINT('Ctrl Pts',(-11.2708081298361,7.71922009721283,
10.2712471344847));
#110966=CARTESIAN_POINT('Ctrl Pts',(-11.1957868279558,7.71238884414837,
10.1528885494575));
#110967=CARTESIAN_POINT('Ctrl Pts',(-11.1506226096604,7.70869154924494,
10.0924928857486));
#110968=CARTESIAN_POINT('Ctrl Pts',(-11.093096540647,7.70409756612352,10.0268007405701));
#110969=CARTESIAN_POINT('Ctrl Pts',(-11.0850636686296,7.70345828583212,
10.0178525251129));
#110970=CARTESIAN_POINT('Ctrl Pts',(-11.0735307420375,7.70254187826395,
10.0053196123172));
#110971=CARTESIAN_POINT('Ctrl Pts',(-11.0701209369918,7.70227110598106,
10.0016521114985));
#110972=CARTESIAN_POINT('Ctrl Pts',(-11.0643309655621,7.7018114672553,9.99548830664228));
#110973=CARTESIAN_POINT('Ctrl Pts',(-11.0619606388141,7.70162333745661,
9.99298274705127));
#110974=CARTESIAN_POINT('Ctrl Pts',(-11.0570722188718,7.70123537533106,
9.98785188487548));
#110975=CARTESIAN_POINT('Ctrl Pts',(-11.0545531702894,7.7010354729684,9.9852275657572));
#110976=CARTESIAN_POINT('Ctrl Pts',(-11.0480364958302,7.70051844687545,
9.97848903024078));
#110977=CARTESIAN_POINT('Ctrl Pts',(-11.0440244552388,7.70020024453759,
9.97438891748906));
#110978=CARTESIAN_POINT('Ctrl Pts',(-11.0269656966991,7.69884816338197,
9.95715950218753));
#110979=CARTESIAN_POINT('Ctrl Pts',(-11.0136951587265,7.69779850588063,
9.94425528355815));
#110980=CARTESIAN_POINT('Ctrl Pts',(-10.9770546748602,7.69491499295608,
9.90995402469883));
#110981=CARTESIAN_POINT('Ctrl Pts',(-10.9532293802638,7.69305565762345,
9.88905913930285));
#110982=CARTESIAN_POINT('Ctrl Pts',(-10.8527542836138,7.68533843619732,
9.8065550171705));
#110983=CARTESIAN_POINT('Ctrl Pts',(-10.7706658411821,7.67933721882721,
9.75197079903355));
#110984=CARTESIAN_POINT('Ctrl Pts',(-10.6295088858711,7.66993941409464,
9.67738517620508));
#110985=CARTESIAN_POINT('Ctrl Pts',(-10.5735482208729,7.66641687429221,
9.65217384858416));
#110986=CARTESIAN_POINT('Ctrl Pts',(-10.5053994519177,7.66237355454415,
9.62648771331742));
#110987=CARTESIAN_POINT('Ctrl Pts',(-10.4945863913979,7.66173899348304,
9.62255710837732));
#110988=CARTESIAN_POINT('Ctrl Pts',(-10.4766777750269,7.6606993095538,9.61628530796765));
#110989=CARTESIAN_POINT('Ctrl Pts',(-10.4696087764442,7.6602917884261,9.61387026216208));
#110990=CARTESIAN_POINT('Ctrl Pts',(-10.4567970850015,7.65955829696784,
9.60960254666077));
#110991=CARTESIAN_POINT('Ctrl Pts',(-10.4510608703118,7.65923172096216,
9.60773107917474));
#110992=CARTESIAN_POINT('Ctrl Pts',(-10.4387281489814,7.65853345144564,
9.60379168874217));
#110993=CARTESIAN_POINT('Ctrl Pts',(-10.4321282165507,7.65816212547454,
9.6017349164676));
#110994=CARTESIAN_POINT('Ctrl Pts',(-10.4140368234832,7.65715055988169,
9.59623732588747));
#110995=CARTESIAN_POINT('Ctrl Pts',(-10.4025171062465,7.65651336123415,
9.59289086175695));
#110996=CARTESIAN_POINT('Ctrl Pts',(-10.3373516056281,7.6529458560142,9.57482613627531));
#110997=CARTESIAN_POINT('Ctrl Pts',(-10.2829394008663,7.65011029165728,
9.56303346596823));
#110998=CARTESIAN_POINT('Ctrl Pts',(-10.1472269861223,7.64326089530265,
9.54163095801759));
#110999=CARTESIAN_POINT('Ctrl Pts',(-10.0655465404924,7.63933599194206,
9.53568451716217));
#111000=CARTESIAN_POINT('Ctrl Pts',(-9.91445236077482,7.63193678802747,
9.53735752369492));
#111001=CARTESIAN_POINT('Ctrl Pts',(-9.84525812767399,7.62849022084844,
9.5430531218684));
#111002=CARTESIAN_POINT('Ctrl Pts',(-9.76868470762343,7.62436971753075,
9.55487306038602));
#111003=CARTESIAN_POINT('Ctrl Pts',(-9.7606430127828,7.62393313132441,9.55618323089514));
#111004=CARTESIAN_POINT('Ctrl Pts',(-9.74846083086693,7.62326534303885,
9.55827254904853));
#111005=CARTESIAN_POINT('Ctrl Pts',(-9.74431194759029,7.62303678260618,
9.55900256232272));
#111006=CARTESIAN_POINT('Ctrl Pts',(-9.73684281684787,7.62262317804185,
9.5603500591529));
#111007=CARTESIAN_POINT('Ctrl Pts',(-9.73352149582339,7.62243849249484,
9.56096113268532));
#111008=CARTESIAN_POINT('Ctrl Pts',(-9.72620570157026,7.62202998574904,
9.56233332560405));
#111009=CARTESIAN_POINT('Ctrl Pts',(-9.72221231999821,7.62180588669955,
9.56309958990127));
#111010=CARTESIAN_POINT('Ctrl Pts',(-9.71066585334278,7.62115480865239,
9.56536509918817));
#111011=CARTESIAN_POINT('Ctrl Pts',(-9.70312145776466,7.62072553086426,
9.56690730482109));
#111012=CARTESIAN_POINT('Ctrl Pts',(-9.64496912776847,7.61738861048399,
9.57927354701719));
#111013=CARTESIAN_POINT('Ctrl Pts',(-9.59495963048441,7.61435568560235,
9.59271471907147));
#111014=CARTESIAN_POINT('Ctrl Pts',(-9.44043382571202,7.60467412627618,
9.64316657271366));
#111015=CARTESIAN_POINT('Ctrl Pts',(-9.33932796696818,7.59791123469256,
9.68941683375412));
#111016=CARTESIAN_POINT('Ctrl Pts',(-9.20548571697756,7.58884003872102,
9.77010362005083));
#111017=CARTESIAN_POINT('Ctrl Pts',(-9.16767248073269,7.58625677601352,
9.79537160226357));
#111018=CARTESIAN_POINT('Ctrl Pts',(-9.12170697210895,7.58309165832408,
9.82928667681572));
#111019=CARTESIAN_POINT('Ctrl Pts',(-9.11240322321058,7.58244959126441,
9.83632465834419));
#111020=CARTESIAN_POINT('Ctrl Pts',(-9.09772583706522,7.58143417998846,
9.84770607149992));
#111021=CARTESIAN_POINT('Ctrl Pts',(-9.09229722245432,7.58105806050645,
9.85197751212453));
#111022=CARTESIAN_POINT('Ctrl Pts',(-9.0821833036215,7.58035620096151,9.86005211806163));
#111023=CARTESIAN_POINT('Ctrl Pts',(-9.0774909023831,7.58003011076133,9.86384612485723));
#111024=CARTESIAN_POINT('Ctrl Pts',(-9.0670366719485,7.57930251167623,9.87240628319394));
#111025=CARTESIAN_POINT('Ctrl Pts',(-9.06128761189233,7.57890162726258,
9.87718780871681));
#111026=CARTESIAN_POINT('Ctrl Pts',(-9.04436071196861,7.57771884778395,
9.89148688787355));
#111027=CARTESIAN_POINT('Ctrl Pts',(-9.03328897720108,7.57694199195277,
9.90112894866623));
#111028=CARTESIAN_POINT('Ctrl Pts',(-9.00839449840216,7.57518642349276,
9.92347634527813));
#111029=CARTESIAN_POINT('Ctrl Pts',(-8.99466728370875,7.57421196672982,
9.93628442767607));
#111030=CARTESIAN_POINT('Ctrl Pts',(-8.94943140007354,7.57097331148404,
9.98014958402837));
#111031=CARTESIAN_POINT('Ctrl Pts',(-8.91908423043094,7.56875510172294,
10.01237115943));
#111032=CARTESIAN_POINT('Ctrl Pts',(-8.85091453899071,7.56358775581954,
10.0916641277628));
#111033=CARTESIAN_POINT('Ctrl Pts',(-8.81445262760388,7.56067227973134,
10.1397971127062));
#111034=CARTESIAN_POINT('Ctrl Pts',(-8.75988673015752,7.55586252034449,
10.2219153468808));
#111035=CARTESIAN_POINT('Ctrl Pts',(-8.7399669734504,7.55398577678086,10.254605322844));
#111036=CARTESIAN_POINT('Ctrl Pts',(-8.70123071358002,7.54999743373747,
10.3241736150263));
#111037=CARTESIAN_POINT('Ctrl Pts',(-8.68265211281551,7.54788087011945,
10.3611440368657));
#111038=CARTESIAN_POINT('Ctrl Pts',(-8.66281111212311,7.5453077950752,10.4051837135376));
#111039=CARTESIAN_POINT('Ctrl Pts',(-8.66000199535045,7.54493522276934,
10.4115393978377));
#111040=CARTESIAN_POINT('Ctrl Pts',(-8.65552020144677,7.5443268018641,10.4218780568315));
#111041=CARTESIAN_POINT('Ctrl Pts',(-8.65381967951906,7.54409255766012,
10.4258489278284));
#111042=CARTESIAN_POINT('Ctrl Pts',(-8.65081876007786,7.54367297718955,
10.4329429685351));
#111043=CARTESIAN_POINT('Ctrl Pts',(-8.64951158323239,7.54348804885193,
10.4360631852956));
#111044=CARTESIAN_POINT('Ctrl Pts',(-8.64669018868265,7.54308413448502,
10.4428638920726));
#111045=CARTESIAN_POINT('Ctrl Pts',(-8.64518018228551,7.54286491286244,
10.4465459830094));
#111046=CARTESIAN_POINT('Ctrl Pts',(-8.64094566635844,7.54224152777444,
10.4569928603596));
#111047=CARTESIAN_POINT('Ctrl Pts',(-8.63825671616897,7.54183534958293,
10.4637718209926));
#111048=CARTESIAN_POINT('Ctrl Pts',(-8.62101672226235,7.53916378229126,
10.5082006350737));
#111049=CARTESIAN_POINT('Ctrl Pts',(-8.60797904506213,7.53682178312963,
10.5464158161719));
#111050=CARTESIAN_POINT('Ctrl Pts',(-8.55685110415499,7.52617313485845,
10.7193710122347));
#111051=CARTESIAN_POINT('Ctrl Pts',(-8.53662520365909,7.51755628813411,
10.8586592934391));
#111052=CARTESIAN_POINT('Ctrl Pts',(-8.53647278092057,7.50777217626109,
11.0299344718732));
#111053=CARTESIAN_POINT('Ctrl Pts',(-8.53744505908784,7.50601619663285,
11.0611657270828));
#111054=CARTESIAN_POINT('Ctrl Pts',(-8.54006961833363,7.50371878521601,
11.1026779118903));
#111055=CARTESIAN_POINT('Ctrl Pts',(-8.54083265787684,7.5031502480287,11.1130050808016));
#111056=CARTESIAN_POINT('Ctrl Pts',(-8.54225752367472,7.50222740574017,
11.1298540576063));
#111057=CARTESIAN_POINT('Ctrl Pts',(-8.54285366321132,7.5018710818799,11.1363809322538));
#111058=CARTESIAN_POINT('Ctrl Pts',(-8.54409051147143,7.5011850479082,11.1489871692392));
#111059=CARTESIAN_POINT('Ctrl Pts',(-8.54472550364562,7.5008551682207,11.1550669442614));
#111060=CARTESIAN_POINT('Ctrl Pts',(-8.54629407886147,7.50008912742966,
11.1692261508662));
#111061=CARTESIAN_POINT('Ctrl Pts',(-8.54725696110659,7.49965388427216,
11.1773021766336));
#111062=CARTESIAN_POINT('Ctrl Pts',(-8.55058328137308,7.49825513371005,
11.2033520519027));
#111063=CARTESIAN_POINT('Ctrl Pts',(-8.55321341158184,7.49729990037004,
11.221290503065));
#111064=CARTESIAN_POINT('Ctrl Pts',(-8.56019498917973,7.49507153921929,
11.2634359015561));
#111065=CARTESIAN_POINT('Ctrl Pts',(-8.56482467844388,7.49380686043093,
11.2875914166956));
#111066=CARTESIAN_POINT('Ctrl Pts',(-8.58442877192753,7.48912855681503,
11.3775493350142));
#111067=CARTESIAN_POINT('Ctrl Pts',(-8.60333958615982,7.48582353326137,
11.4424091854995));
#111068=CARTESIAN_POINT('Ctrl Pts',(-8.66120469948342,7.47766922229001,
11.5995439272189));
#111069=CARTESIAN_POINT('Ctrl Pts',(-8.70526659266771,7.47286938536262,
11.6895550986922));
#111070=CARTESIAN_POINT('Ctrl Pts',(-8.76407532679442,7.46701019427945,
11.7838673002117));
#111071=CARTESIAN_POINT('Ctrl Pts',(-8.77011143161543,7.46641379973005,
11.7933043782688));
#111072=CARTESIAN_POINT('Ctrl Pts',(-8.77866451149831,7.46557420211996,
11.806344326903));
#111073=CARTESIAN_POINT('Ctrl Pts',(-8.78109042656616,7.46533666191741,
11.8100067899694));
#111074=CARTESIAN_POINT('Ctrl Pts',(-8.78530128125618,7.46492526377293,
11.8163022671063));
#111075=CARTESIAN_POINT('Ctrl Pts',(-8.78707839777739,7.46475191820136,
11.8189405076475));
#111076=CARTESIAN_POINT('Ctrl Pts',(-8.79083226780889,7.46438628847645,
11.8244743401019));
#111077=CARTESIAN_POINT('Ctrl Pts',(-8.79281083918449,7.46419387850358,
11.8273686429241));
#111078=CARTESIAN_POINT('Ctrl Pts',(-8.7977049959379,7.46371873683989,11.8344730065873));
#111079=CARTESIAN_POINT('Ctrl Pts',(-8.80063230186567,7.46343523446217,
11.8386749063782));
#111080=CARTESIAN_POINT('Ctrl Pts',(-8.81146804889436,7.46238859951005,
11.8540559515601));
#111081=CARTESIAN_POINT('Ctrl Pts',(-8.81951098854474,7.46161709903128,
11.8651389677207));
#111082=CARTESIAN_POINT('Ctrl Pts',(-8.84016800491446,7.45965226992434,
11.892779488675));
#111083=CARTESIAN_POINT('Ctrl Pts',(-8.85298178075879,7.45844845978603,
11.9091834801123));
#111084=CARTESIAN_POINT('Ctrl Pts',(-8.9126567131123,7.45292851133689,11.9823083240997));
#111085=CARTESIAN_POINT('Ctrl Pts',(-8.96340331046673,7.44847186652789,
12.0357179623672));
#111086=CARTESIAN_POINT('Ctrl Pts',(-9.08749807401176,7.43841781648588,
12.1480295374196));
#111087=CARTESIAN_POINT('Ctrl Pts',(-9.16294733183338,7.43287664782252,
12.2041508024154));
#111088=CARTESIAN_POINT('Ctrl Pts',(-9.25763547307535,7.42667143557581,
12.2613521404095));
#111089=CARTESIAN_POINT('Ctrl Pts',(-9.27215956465722,7.42573807731485,
12.2697884258457));
#111090=CARTESIAN_POINT('Ctrl Pts',(-9.29466538041419,7.42431941830449,
12.2823478143939));
#111091=CARTESIAN_POINT('Ctrl Pts',(-9.30254487553938,7.42382782161387,
12.286650378714));
#111092=CARTESIAN_POINT('Ctrl Pts',(-9.31543643063254,7.42303165242581,
12.2935365300479));
#111093=CARTESIAN_POINT('Ctrl Pts',(-9.32042462953291,7.42272554484162,
12.2961640915257));
#111094=CARTESIAN_POINT('Ctrl Pts',(-9.33092906311407,7.42208497884518,
12.3016200512283));
#111095=CARTESIAN_POINT('Ctrl Pts',(-9.33644834459411,7.42175073673674,
12.3044423630709));
#111096=CARTESIAN_POINT('Ctrl Pts',(-9.3497001709032,7.42095368795321,12.3111128782097));
#111097=CARTESIAN_POINT('Ctrl Pts',(-9.35744922440065,7.42049203277166,
12.3149278885963));
#111098=CARTESIAN_POINT('Ctrl Pts',(-9.38424839036251,7.41891024115927,
12.3278281649582));
#111099=CARTESIAN_POINT('Ctrl Pts',(-9.40346143954344,7.41780178672107,
12.3365700450466));
#111100=CARTESIAN_POINT('Ctrl Pts',(-9.48582338549034,7.41314890729399,
12.3719145346809));
#111101=CARTESIAN_POINT('Ctrl Pts',(-9.55061275836494,7.4097367782104,12.394481774003));
#111102=CARTESIAN_POINT('Ctrl Pts',(-9.69808838671182,7.4022498603411,12.4344981086635));
#111103=CARTESIAN_POINT('Ctrl Pts',(-9.78117776245955,7.39821891189439,
12.4495002537813));
#111104=CARTESIAN_POINT('Ctrl Pts',(-9.90561494572057,7.39195450593427,
12.4610201619974));
#111105=CARTESIAN_POINT('Ctrl Pts',(-9.94627378363094,7.38987039942979,
12.4630794254649));
#111106=CARTESIAN_POINT('Ctrl Pts',(-9.99388300968915,7.38733392454411,
12.4635035827577));
#111107=CARTESIAN_POINT('Ctrl Pts',(-10.0008042463413,7.38696280217191,
12.4635161440193));
#111108=CARTESIAN_POINT('Ctrl Pts',(-10.0120365540918,7.38635628686158,
12.463456852748));
#111109=CARTESIAN_POINT('Ctrl Pts',(-10.016347753843,7.38612248188271,12.4634150431352));
#111110=CARTESIAN_POINT('Ctrl Pts',(-10.0240407722511,7.38570337132344,
12.4633064382759));
#111111=CARTESIAN_POINT('Ctrl Pts',(-10.0274226155955,7.38551846987643,
12.4632469685215));
#111112=CARTESIAN_POINT('Ctrl Pts',(-10.0347893011276,7.38511423689949,
12.4630918774794));
#111113=CARTESIAN_POINT('Ctrl Pts',(-10.0387739130224,7.38489466672256,
12.4629917020665));
#111114=CARTESIAN_POINT('Ctrl Pts',(-10.0500765773374,7.38426931865933,
12.4626613393003));
#111115=CARTESIAN_POINT('Ctrl Pts',(-10.057393276224,7.38386150648101,12.4623925137953));
#111116=CARTESIAN_POINT('Ctrl Pts',(-10.1056936333741,7.38115095313022,
12.4602548612918));
#111117=CARTESIAN_POINT('Ctrl Pts',(-10.1465820904955,7.37876908258855,
12.4567184102257));
#111118=CARTESIAN_POINT('Ctrl Pts',(-10.3362939836918,7.36746837657589,
12.4322423548232));
#111119=CARTESIAN_POINT('Ctrl Pts',(-10.4815189825224,7.35821742802636,
12.3901683126946));
#111120=CARTESIAN_POINT('Ctrl Pts',(-10.6384924191183,7.34843648984094,
12.3170729757888));
#111121=CARTESIAN_POINT('Ctrl Pts',(-10.6589674959353,7.34716232867441,
12.3069490098001));
#111122=CARTESIAN_POINT('Ctrl Pts',(-10.6873235485571,7.34539932304703,
12.2920923869217));
#111123=CARTESIAN_POINT('Ctrl Pts',(-10.6954089299132,7.34489679804423,
12.287758837007));
#111124=CARTESIAN_POINT('Ctrl Pts',(-10.7084279238612,7.34408779933793,
12.2806226261803));
#111125=CARTESIAN_POINT('Ctrl Pts',(-10.7133868341596,7.34377969117181,
12.2778668397354));
#111126=CARTESIAN_POINT('Ctrl Pts',(-10.7235965515742,7.34314537086463,
12.2721150989263));
#111127=CARTESIAN_POINT('Ctrl Pts',(-10.728845077147,7.34281930263742,12.2691153018498));
#111128=CARTESIAN_POINT('Ctrl Pts',(-10.7411776436207,7.34205310138474,
12.261964880065));
#111129=CARTESIAN_POINT('Ctrl Pts',(-10.7482456819274,7.34161395159393,
12.2577869696807));
#111130=CARTESIAN_POINT('Ctrl Pts',(-10.76314667304,7.34068787864448,12.2488089493809));
#111131=CARTESIAN_POINT('Ctrl Pts',(-10.770970361782,7.34020150201364,12.2439941088732));
#111132=CARTESIAN_POINT('Ctrl Pts',(-10.7921259669915,7.33888550379048,
12.2306983182467));
#111133=CARTESIAN_POINT('Ctrl Pts',(-10.8053668889463,7.33806096431955,
12.2220745052581));
#111134=CARTESIAN_POINT('Ctrl Pts',(-10.9155886779984,7.33118189032094,
12.1477174591916));
#111135=CARTESIAN_POINT('Ctrl Pts',(-11.0044901853269,7.32557656359651,
12.0707748816618));
#111136=CARTESIAN_POINT('Ctrl Pts',(-11.1319517305178,7.31630721827846,
11.930461892167));
#111137=CARTESIAN_POINT('Ctrl Pts',(-11.1765842887161,7.31272003209837,
11.8733390272966));
#111138=CARTESIAN_POINT('Ctrl Pts',(-11.2213335166274,7.30843698041421,
11.8063765830779));
#111139=CARTESIAN_POINT('Ctrl Pts',(-11.2258077342041,7.30800001840562,
11.7995587191176));
#111140=CARTESIAN_POINT('Ctrl Pts',(-11.2325072494409,7.30733176731578,
11.7891615103695));
#111141=CARTESIAN_POINT('Ctrl Pts',(-11.2347745211362,7.30710312538032,
11.7856092479263));
#111142=CARTESIAN_POINT('Ctrl Pts',(-11.2388310655877,7.30668943685984,
11.779192688956));
#111143=CARTESIAN_POINT('Ctrl Pts',(-11.2406257987953,7.30650474957136,
11.776331940962));
#111144=CARTESIAN_POINT('Ctrl Pts',(-11.24455896199,7.30609631643565,11.7700141321322));
#111145=CARTESIAN_POINT('Ctrl Pts',(-11.2466928722943,7.30587229338915,
11.7665544044003));
#111146=CARTESIAN_POINT('Ctrl Pts',(-11.2528240753573,7.30522165075082,
11.7565205115662));
#111147=CARTESIAN_POINT('Ctrl Pts',(-11.2567839117989,7.30479273696936,
11.7499237574829));
#111148=CARTESIAN_POINT('Ctrl Pts',(-11.286862325093,7.30146880469705,11.698908298222));
#111149=CARTESIAN_POINT('Ctrl Pts',(-11.3106682918532,7.29844956906858,
11.6531730862665));
#111150=CARTESIAN_POINT('Ctrl Pts',(-11.3858148088539,7.28764733148999,
11.4880752594081));
#111151=CARTESIAN_POINT('Ctrl Pts',(-11.4236543118523,7.27971207713107,
11.3632056139713));
#111152=CARTESIAN_POINT('Ctrl Pts',(-11.4493042064121,7.27060221910975,
11.2055237581379));
#111153=CARTESIAN_POINT('Ctrl Pts',(-11.4531936142035,7.26892673681237,
11.1759295285654));
#111154=CARTESIAN_POINT('Ctrl Pts',(-11.45719232336,7.26671733720045,11.1361114001376));
#111155=CARTESIAN_POINT('Ctrl Pts',(-11.4581034347236,7.26615885443728,
11.1259768290674));
#111156=CARTESIAN_POINT('Ctrl Pts',(-11.4594244295834,7.26524816245517,
11.1093390452742));
#111157=CARTESIAN_POINT('Ctrl Pts',(-11.4598966988704,7.26489403451313,
11.102841251538));
#111158=CARTESIAN_POINT('Ctrl Pts',(-11.4607061936426,7.26422814505174,
11.0905709543574));
#111159=CARTESIAN_POINT('Ctrl Pts',(-11.4610526269498,7.26391610501315,
11.0847992011743));
#111160=CARTESIAN_POINT('Ctrl Pts',(-11.4616865632727,7.2632846707454,11.0730762460578));
#111161=CARTESIAN_POINT('Ctrl Pts',(-11.4619719484179,7.26296534743556,
11.0671250359433));
#111162=CARTESIAN_POINT('Ctrl Pts',(-11.4626126326677,7.26214668737144,
11.0518105282083));
#111163=CARTESIAN_POINT('Ctrl Pts',(-11.4629143706465,7.26164899911573,
11.0424451837417));
#111164=CARTESIAN_POINT('Ctrl Pts',(-11.4633785691653,7.26056397069535,
11.0219121260251));
#111165=CARTESIAN_POINT('Ctrl Pts',(-11.463503176572,7.25997779352992,11.0107441486259));
#111166=CARTESIAN_POINT('Ctrl Pts',(-11.4634999384891,7.25939525541925,
10.9995756860797));
#111167=CARTESIAN_POINT('Ctrl Pts',(-11.4634999176129,7.19062697242339,
10.9995089326331));
#111168=CARTESIAN_POINT('Ctrl Pts',(-11.4635051213571,7.1914923421607,11.0150173531874));
#111169=CARTESIAN_POINT('Ctrl Pts',(-11.4632638158498,7.19235020755999,
11.0305252719007));
#111170=CARTESIAN_POINT('Ctrl Pts',(-11.4625356658954,7.19361955643145,
11.0536665512648));
#111171=CARTESIAN_POINT('Ctrl Pts',(-11.4622354301267,7.19403675453786,
11.0613043449609));
#111172=CARTESIAN_POINT('Ctrl Pts',(-11.461590362189,7.19478087691799,11.0749831270642));
#111173=CARTESIAN_POINT('Ctrl Pts',(-11.4612678792724,7.1951084832571,11.0810249511718));
#111174=CARTESIAN_POINT('Ctrl Pts',(-11.4605033684944,7.19580185987213,
11.0938531158355));
#111175=CARTESIAN_POINT('Ctrl Pts',(-11.4600514863654,7.19616731773661,
11.100638740175));
#111176=CARTESIAN_POINT('Ctrl Pts',(-11.4587100487841,7.19714554879489,
11.1188651341328));
#111177=CARTESIAN_POINT('Ctrl Pts',(-11.4577331972617,7.19775561701456,
11.1302991253625));
#111178=CARTESIAN_POINT('Ctrl Pts',(-11.4520308368187,7.20086566565634,
11.188908667653));
#111179=CARTESIAN_POINT('Ctrl Pts',(-11.4451492228012,7.20329822460771,
11.2358481206412));
#111180=CARTESIAN_POINT('Ctrl Pts',(-11.415358651437,7.21105579417276,11.3873467227317));
#111181=CARTESIAN_POINT('Ctrl Pts',(-11.3832704409702,7.21612901499671,
11.4897342692634));
#111182=CARTESIAN_POINT('Ctrl Pts',(-11.3293779365529,7.22276968588414,
11.6126398979588));
#111183=CARTESIAN_POINT('Ctrl Pts',(-11.3177526773158,7.22413133361263,
11.6372606312539));
#111184=CARTESIAN_POINT('Ctrl Pts',(-11.2926351018324,7.22696396042054,
11.686826188853));
#111185=CARTESIAN_POINT('Ctrl Pts',(-11.2790910658817,7.228436530401,11.7117313832945));
#111186=CARTESIAN_POINT('Ctrl Pts',(-11.2613911837764,7.23031562663727,
11.7421397122222));
#111187=CARTESIAN_POINT('Ctrl Pts',(-11.2579075986177,7.23068343984053,
11.7480291041618));
#111188=CARTESIAN_POINT('Ctrl Pts',(-11.2523619390566,7.2312661822005,11.7572563735347));
#111189=CARTESIAN_POINT('Ctrl Pts',(-11.2503274788332,7.23147938785848,
11.7606108312396));
#111190=CARTESIAN_POINT('Ctrl Pts',(-11.2465261983596,7.23187676404217,
11.766821993147));
#111191=CARTESIAN_POINT('Ctrl Pts',(-11.2447630107207,7.23206070270992,
11.7696808291665));
#111192=CARTESIAN_POINT('Ctrl Pts',(-11.2406751400041,7.23248626784267,
11.7762581258429));
#111193=CARTESIAN_POINT('Ctrl Pts',(-11.2383435793675,7.23272833385409,
11.7799722170576));
#111194=CARTESIAN_POINT('Ctrl Pts',(-11.2310224920121,7.23348623791284,
11.7915188682637));
#111195=CARTESIAN_POINT('Ctrl Pts',(-11.2259751782284,7.23400563614262,
11.7993142986445));
#111196=CARTESIAN_POINT('Ctrl Pts',(-11.2139687620387,7.23523298025802,
11.8174765984065));
#111197=CARTESIAN_POINT('Ctrl Pts',(-11.2069505719273,7.23594418474576,
11.827803383582));
#111198=CARTESIAN_POINT('Ctrl Pts',(-11.1815364561673,7.2384943466751,11.8641882033712));
#111199=CARTESIAN_POINT('Ctrl Pts',(-11.1624225225761,7.24036668439603,
11.8897321535548));
#111200=CARTESIAN_POINT('Ctrl Pts',(-11.0830318516041,7.24790899459085,
11.9889013385968));
#111201=CARTESIAN_POINT('Ctrl Pts',(-11.0164717811869,7.25371189825479,
12.0571993897305));
#111202=CARTESIAN_POINT('Ctrl Pts',(-10.8948564543984,7.26309728359235,
12.1598088156079));
#111203=CARTESIAN_POINT('Ctrl Pts',(-10.8433067629296,7.26677895392274,
12.1978146542371));
#111204=CARTESIAN_POINT('Ctrl Pts',(-10.7796537744778,7.27097672956484,
12.2385907384724));
#111205=CARTESIAN_POINT('Ctrl Pts',(-10.7698039134366,7.27161717065676,
12.2447365067382));
#111206=CARTESIAN_POINT('Ctrl Pts',(-10.7534694187952,7.27266451547499,
12.2546602646565));
#111207=CARTESIAN_POINT('Ctrl Pts',(-10.7470271297079,7.27307387764979,
12.2585066607562));
#111208=CARTESIAN_POINT('Ctrl Pts',(-10.7353478093011,7.2738094381201,12.265358566995));
#111209=CARTESIAN_POINT('Ctrl Pts',(-10.7301212489474,7.27413625615823,
12.2683815147875));
#111210=CARTESIAN_POINT('Ctrl Pts',(-10.7188882121682,7.2748337095986,12.2747860598122));
#111211=CARTESIAN_POINT('Ctrl Pts',(-10.712876236246,7.27520398777064,12.2781577500034));
#111212=CARTESIAN_POINT('Ctrl Pts',(-10.6964228215469,7.27620934072081,
12.2872330995691));
#111213=CARTESIAN_POINT('Ctrl Pts',(-10.6859351727526,7.27684143938897,
12.2928521759372));
#111214=CARTESIAN_POINT('Ctrl Pts',(-10.6275600038426,7.28031353069479,
12.3232181298679));
#111215=CARTESIAN_POINT('Ctrl Pts',(-10.5783997625433,7.28306492826677,
12.3454338708195));
#111216=CARTESIAN_POINT('Ctrl Pts',(-10.4021100008816,7.29250318902173,
12.4136464034992));
#111217=CARTESIAN_POINT('Ctrl Pts',(-10.2699717475884,7.29877546861338,
12.4447130467065));
#111218=CARTESIAN_POINT('Ctrl Pts',(-10.1141191493033,7.30684838720288,
12.4592013822133));
#111219=CARTESIAN_POINT('Ctrl Pts',(-10.0927328581139,7.30797200025533,
12.4607163917823));
#111220=CARTESIAN_POINT('Ctrl Pts',(-10.0650355306731,7.30945627656537,
12.4620677977752));
#111221=CARTESIAN_POINT('Ctrl Pts',(-10.0587471214867,7.30979520417874,
12.4623339695157));
#111222=CARTESIAN_POINT('Ctrl Pts',(-10.0486978123123,7.31034019996122,
12.4626944058978));
#111223=CARTESIAN_POINT('Ctrl Pts',(-10.044937856662,7.31054486303623,12.4628147491592));
#111224=CARTESIAN_POINT('Ctrl Pts',(-10.0377484816496,7.31093770551627,
12.4630171119189));
#111225=CARTESIAN_POINT('Ctrl Pts',(-10.0343191984752,7.31112575117329,
12.4631015717843));
#111226=CARTESIAN_POINT('Ctrl Pts',(-10.0261884361782,7.31157313678651,
12.4632732237992));
#111227=CARTESIAN_POINT('Ctrl Pts',(-10.0214867931346,7.31183305079773,
12.4633498140056));
#111228=CARTESIAN_POINT('Ctrl Pts',(-10.0057474125166,7.31270701761987,
12.4635303413523));
#111229=CARTESIAN_POINT('Ctrl Pts',(-9.99470914775795,7.31332631265321,
12.4635320580216));
#111230=CARTESIAN_POINT('Ctrl Pts',(-9.93184857472069,7.3168853192916,12.4628307018585));
#111231=CARTESIAN_POINT('Ctrl Pts',(-9.88009636637776,7.31993914587323,
12.4595000780852));
#111232=CARTESIAN_POINT('Ctrl Pts',(-9.68767499445089,7.33151238412982,
12.4368128678463));
#111233=CARTESIAN_POINT('Ctrl Pts',(-9.54984485172418,7.34014800453584,
12.3997692678828));
#111234=CARTESIAN_POINT('Ctrl Pts',(-9.40349365373665,7.34907334235398,
12.3365315280307));
#111235=CARTESIAN_POINT('Ctrl Pts',(-9.38761021903613,7.35004016439006,
12.3293288304509));
#111236=CARTESIAN_POINT('Ctrl Pts',(-9.36470247907094,7.35143233656326,
12.3184430544066));
#111237=CARTESIAN_POINT('Ctrl Pts',(-9.35757378633333,7.35186525546715,
12.3149842551331));
#111238=CARTESIAN_POINT('Ctrl Pts',(-9.34500435241188,7.35262812178203,
12.308759030271));
#111239=CARTESIAN_POINT('Ctrl Pts',(-9.33955221116796,7.3529588683287,12.3060161627873));
#111240=CARTESIAN_POINT('Ctrl Pts',(-9.32825179329688,7.3536441285302,12.3002422786112));
#111241=CARTESIAN_POINT('Ctrl Pts',(-9.32240649299769,7.3539984406497,12.2972057190365));
#111242=CARTESIAN_POINT('Ctrl Pts',(-9.30729678370843,7.35491403903563,
12.2892264188123));
#111243=CARTESIAN_POINT('Ctrl Pts',(-9.29806462561568,7.35547320519396,
12.2842232059346));
#111244=CARTESIAN_POINT('Ctrl Pts',(-9.25756965285052,7.35792558053323,
12.2617104771799));
#111245=CARTESIAN_POINT('Ctrl Pts',(-9.22690092271885,7.35978169260165,
12.2431549512157));
#111246=CARTESIAN_POINT('Ctrl Pts',(-9.14362403862164,7.36485099246882,
12.188494876388));
#111247=CARTESIAN_POINT('Ctrl Pts',(-9.09264793688092,7.36798551343019,
12.1500490595042));
#111248=CARTESIAN_POINT('Ctrl Pts',(-8.96402725450231,7.37626442578684,
12.0391525291314));
#111249=CARTESIAN_POINT('Ctrl Pts',(-8.89148842474422,7.38132987985839,
11.9613915807975));
#111250=CARTESIAN_POINT('Ctrl Pts',(-8.82163247437605,7.38748801189372,
11.8679833497076));
#111251=CARTESIAN_POINT('Ctrl Pts',(-8.81536272450085,7.3880542329676,11.8594065588891));
#111252=CARTESIAN_POINT('Ctrl Pts',(-8.8066900144571,7.38885787013781,11.8472673603374));
#111253=CARTESIAN_POINT('Ctrl Pts',(-8.80420837257014,7.38909023766389,
11.8437612721164));
#111254=CARTESIAN_POINT('Ctrl Pts',(-8.79992973353963,7.3894951703912,11.8376595798839));
#111255=CARTESIAN_POINT('Ctrl Pts',(-8.79812561960328,7.38966726117493,
11.8350689729424));
#111256=CARTESIAN_POINT('Ctrl Pts',(-8.79431892367519,7.39003329157356,
11.8295648805122));
#111257=CARTESIAN_POINT('Ctrl Pts',(-8.79231849751489,7.39022737673062,
11.826649948092));
#111258=CARTESIAN_POINT('Ctrl Pts',(-8.78736767205361,7.39071199706625,
11.8193794986493));
#111259=CARTESIAN_POINT('Ctrl Pts',(-8.78443017859925,7.39100336980907,
11.8150152962724));
#111260=CARTESIAN_POINT('Ctrl Pts',(-8.77338894351127,7.39211289821478,
11.798418976431));
#111261=CARTESIAN_POINT('Ctrl Pts',(-8.76544605449303,7.39294074715676,
11.7860814638972));
#111262=CARTESIAN_POINT('Ctrl Pts',(-8.74560453847067,7.39508218757218,
11.7542194634899));
#111263=CARTESIAN_POINT('Ctrl Pts',(-8.73397574702145,7.39640862886415,
11.7345321411261));
#111264=CARTESIAN_POINT('Ctrl Pts',(-8.68191726887963,7.40266527378569,
11.641486926114));
#111265=CARTESIAN_POINT('Ctrl Pts',(-8.64737227816325,7.40776202133643,
11.5650181597829));
#111266=CARTESIAN_POINT('Ctrl Pts',(-8.59022573212598,7.41805473202854,
11.4027034559474));
#111267=CARTESIAN_POINT('Ctrl Pts',(-8.5684923515426,7.42321642601655,11.3168968767975));
#111268=CARTESIAN_POINT('Ctrl Pts',(-8.5527231635129,7.42880351265699,11.2176455083532));
#111269=CARTESIAN_POINT('Ctrl Pts',(-8.55096648108172,7.42947421945445,
11.2056251011709));
#111270=CARTESIAN_POINT('Ctrl Pts',(-8.54834560045252,7.43056060174405,
11.18598527486));
#111271=CARTESIAN_POINT('Ctrl Pts',(-8.54739128465897,7.43097905826682,
11.178378646203));
#111272=CARTESIAN_POINT('Ctrl Pts',(-8.54579053416922,7.43172457065082,
11.1647534936506));
#111273=CARTESIAN_POINT('Ctrl Pts',(-8.54512159088135,7.43205231859116,
11.1587378353822));
#111274=CARTESIAN_POINT('Ctrl Pts',(-8.54378176882612,7.43274511420222,
11.1459683997064));
#111275=CARTESIAN_POINT('Ctrl Pts',(-8.54312051060801,7.43310985624366,
11.1392137422044));
#111276=CARTESIAN_POINT('Ctrl Pts',(-8.54147336645238,7.43408406681422,
11.1210890308898));
#111277=CARTESIAN_POINT('Ctrl Pts',(-8.54057343877856,7.43469086962136,
11.109711514188));
#111278=CARTESIAN_POINT('Ctrl Pts',(-8.53667982779111,7.43775210031699,
11.0518883911406));
#111279=CARTESIAN_POINT('Ctrl Pts',(-8.53576965607636,7.44014171143158,
11.0053272813691));
#111280=CARTESIAN_POINT('Ctrl Pts',(-8.53861279749361,7.44522030222767,
10.9043769718993));
#111281=CARTESIAN_POINT('Ctrl Pts',(-8.54318115389029,7.44788677725391,
10.8500814446646));
#111282=CARTESIAN_POINT('Ctrl Pts',(-8.56501475568105,7.45552339342862,
10.6948477772222));
#111283=CARTESIAN_POINT('Ctrl Pts',(-8.58984866165421,7.46042604266599,
10.5953168345938));
#111284=CARTESIAN_POINT('Ctrl Pts',(-8.6286190311255,7.46640178005219,10.4888564390466));
#111285=CARTESIAN_POINT('Ctrl Pts',(-8.63250359075304,7.46698821861286,
10.4785529191246));
#111286=CARTESIAN_POINT('Ctrl Pts',(-8.6380885556368,7.46781598684039,10.4642309345609));
#111287=CARTESIAN_POINT('Ctrl Pts',(-8.63969131894239,7.46805186037048,
10.4601745050189));
#111288=CARTESIAN_POINT('Ctrl Pts',(-8.6424915269101,7.46846119030437,10.4531791274877));
#111289=CARTESIAN_POINT('Ctrl Pts',(-8.64368045179287,7.46863414676286,
10.4502367747082));
#111290=CARTESIAN_POINT('Ctrl Pts',(-8.6462067249973,7.46899994385732,10.4440428253987));
#111291=CARTESIAN_POINT('Ctrl Pts',(-8.6475462309671,7.46919291675959,10.4407921555278));
#111292=CARTESIAN_POINT('Ctrl Pts',(-8.65088300145523,7.46967115685227,
10.4327767047353));
#111293=CARTESIAN_POINT('Ctrl Pts',(-8.65289379808268,7.46995721617623,
10.4280176387609));
#111294=CARTESIAN_POINT('Ctrl Pts',(-8.66044751025447,7.47102372081813,
10.4104006202979));
#111295=CARTESIAN_POINT('Ctrl Pts',(-8.66614949364902,7.47181294067455,
10.3976121692255));
#111296=CARTESIAN_POINT('Ctrl Pts',(-8.708343072968,7.47753288539119,10.3065174327056));
#111297=CARTESIAN_POINT('Ctrl Pts',(-8.75151952465032,7.48275757688047,
10.2315013602793));
#111298=CARTESIAN_POINT('Ctrl Pts',(-8.85934602088311,7.49406738642449,
10.0774638468247));
#111299=CARTESIAN_POINT('Ctrl Pts',(-8.92616227905056,7.50009912903132,
10.0004786383826));
#111300=CARTESIAN_POINT('Ctrl Pts',(-9.01393904228906,7.50683834941605,
9.91840018342532));
#111301=CARTESIAN_POINT('Ctrl Pts',(-9.02768800544782,7.50786505249159,
9.90602385556067));
#111302=CARTESIAN_POINT('Ctrl Pts',(-9.04724660510811,7.50928637575882,
9.88907799817574));
#111303=CARTESIAN_POINT('Ctrl Pts',(-9.05286141141777,7.5096900194238,9.88428712366565));
#111304=CARTESIAN_POINT('Ctrl Pts',(-9.06322696806261,7.51042727588632,
9.87557727744809));
#111305=CARTESIAN_POINT('Ctrl Pts',(-9.06796664882473,7.51076140441124,
9.87164544301977));
#111306=CARTESIAN_POINT('Ctrl Pts',(-9.07764240649234,7.51143753751119,
9.8637214166346));
#111307=CARTESIAN_POINT('Ctrl Pts',(-9.08257992664108,7.51177945977164,
9.85973118956467));
#111308=CARTESIAN_POINT('Ctrl Pts',(-9.0948820874528,7.51262381397045,9.84992090659537));
#111309=CARTESIAN_POINT('Ctrl Pts',(-9.10227711041635,7.51312472699741,
9.84413929225245));
#111310=CARTESIAN_POINT('Ctrl Pts',(-9.13052008034112,7.51501336155408,
9.82249279267344));
#111311=CARTESIAN_POINT('Ctrl Pts',(-9.15173769788368,7.51638223672181,
9.80711705064996));
#111312=CARTESIAN_POINT('Ctrl Pts',(-9.20653558845931,7.51980400613857,
9.7696085984048));
#111313=CARTESIAN_POINT('Ctrl Pts',(-9.24063673589528,7.52182946067538,
9.74827458882002));
#111314=CARTESIAN_POINT('Ctrl Pts',(-9.3315693783157,7.52702436290864,9.69647182498859));
#111315=CARTESIAN_POINT('Ctrl Pts',(-9.3896108368714,7.53013955325226,9.66830540558073));
#111316=CARTESIAN_POINT('Ctrl Pts',(-9.51889778889712,7.53694241915899,
9.61579896948401));
#111317=CARTESIAN_POINT('Ctrl Pts',(-9.59054064020714,7.54062991985508,
9.59294190404915));
#111318=CARTESIAN_POINT('Ctrl Pts',(-9.6753238596864,7.54521306543516,9.57291819426744));
#111319=CARTESIAN_POINT('Ctrl Pts',(-9.68706933190899,7.5458528440698,9.57029672486));
#111320=CARTESIAN_POINT('Ctrl Pts',(-9.70374826159777,7.54676988319813,
9.56678952758576));
#111321=CARTESIAN_POINT('Ctrl Pts',(-9.70865629456193,7.54704077793354,
9.5657837699402));
#111322=CARTESIAN_POINT('Ctrl Pts',(-9.71695284291605,7.54750060148584,
9.56412797886911));
#111323=CARTESIAN_POINT('Ctrl Pts',(-9.72033872045786,7.54768879282279,
9.56346468101053));
#111324=CARTESIAN_POINT('Ctrl Pts',(-9.72729999083386,7.54807686091922,
9.56212650286891));
#111325=CARTESIAN_POINT('Ctrl Pts',(-9.7308755899008,7.54827680760877,9.56145297607435));
#111326=CARTESIAN_POINT('Ctrl Pts',(-9.74009558932662,7.54879391449836,
9.55975180515244));
#111327=CARTESIAN_POINT('Ctrl Pts',(-9.74574353347414,7.54911215339402,
9.55874401563994));
#111328=CARTESIAN_POINT('Ctrl Pts',(-9.76963450282196,7.55046410257725,
9.55462583707972));
#111329=CARTESIAN_POINT('Ctrl Pts',(-9.78792898935511,7.55151358528922,
9.55182854790981));
#111330=CARTESIAN_POINT('Ctrl Pts',(-9.83766486347408,7.55439632991313,
9.54518636041899));
#111331=CARTESIAN_POINT('Ctrl Pts',(-9.86918523766847,7.55625505240864,
9.54201416261269));
#111332=CARTESIAN_POINT('Ctrl Pts',(-10.0194478175969,7.56519504215065,
9.53180359938533));
#111333=CARTESIAN_POINT('Ctrl Pts',(-10.1386737666099,7.57247589593899,
9.53823591789497));
#111334=CARTESIAN_POINT('Ctrl Pts',(-10.2980315212906,7.58184573626662,
9.56652567958855));
#111335=CARTESIAN_POINT('Ctrl Pts',(-10.3399095523836,7.5842786842282,9.57587450049699));
#111336=CARTESIAN_POINT('Ctrl Pts',(-10.3925169060043,7.58729656209602,
9.59007190331725));
#111337=CARTESIAN_POINT('Ctrl Pts',(-10.4036780259856,7.58793466176356,
9.59322680524494));
#111338=CARTESIAN_POINT('Ctrl Pts',(-10.4213480823094,7.58894163996855,
9.59844919593738));
#111339=CARTESIAN_POINT('Ctrl Pts',(-10.4278819243169,7.58931327970552,
9.60043009325276));
#111340=CARTESIAN_POINT('Ctrl Pts',(-10.4395979623734,7.58997846700903,
9.6040718174313));
#111341=CARTESIAN_POINT('Ctrl Pts',(-10.444785180374,7.59027254634624,9.60571595295905));
#111342=CARTESIAN_POINT('Ctrl Pts',(-10.456921533673,7.59095963784012,9.60963730057673));
#111343=CARTESIAN_POINT('Ctrl Pts',(-10.463863045253,7.59135188883806,9.61193775292204));
#111344=CARTESIAN_POINT('Ctrl Pts',(-10.4839187732104,7.59248323454975,
9.61875157351024));
#111345=CARTESIAN_POINT('Ctrl Pts',(-10.4969866356625,7.59321794224486,
9.62339951472864));
#111346=CARTESIAN_POINT('Ctrl Pts',(-10.526359988934,7.59486498593115,9.63431974902827));
#111347=CARTESIAN_POINT('Ctrl Pts',(-10.5426233248556,7.59577380163185,
9.64069968542083));
#111348=CARTESIAN_POINT('Ctrl Pts',(-10.5955223506516,7.5987238803772,9.66255216731971));
#111349=CARTESIAN_POINT('Ctrl Pts',(-10.6316431353479,7.60072821052824,
9.67922719009759));
#111350=CARTESIAN_POINT('Ctrl Pts',(-10.7625919203625,7.60803493000037,
9.74628167468931));
#111351=CARTESIAN_POINT('Ctrl Pts',(-10.8524619946855,7.61310817153911,
9.8055702820034));
#111352=CARTESIAN_POINT('Ctrl Pts',(-10.9355639916736,7.61852821411153,
9.87458774733009));
#111353=CARTESIAN_POINT('Ctrl Pts',(-10.9360916260817,7.61856266048545,
9.87502658317914));
#111354=CARTESIAN_POINT('Ctrl Pts',(-10.9564345214131,7.61989202797838,
9.89197007952741));
#111355=CARTESIAN_POINT('Ctrl Pts',(-10.9758094935386,7.6212053769002,9.90899449742122));
#111356=CARTESIAN_POINT('Ctrl Pts',(-11.0071288509552,7.62342718757964,
9.93801612348884));
#111357=CARTESIAN_POINT('Ctrl Pts',(-11.0193333456882,7.62431928497335,
9.94972491294196));
#111358=CARTESIAN_POINT('Ctrl Pts',(-11.0354094034414,7.62553460150051,
9.96569218859426));
#111359=CARTESIAN_POINT('Ctrl Pts',(-11.0394631709508,7.62584458533969,
9.96976624229819));
#111360=CARTESIAN_POINT('Ctrl Pts',(-11.0457917121337,7.62633429285329,
9.97620182876728));
#111361=CARTESIAN_POINT('Ctrl Pts',(-11.0480827695288,7.62651278095177,
9.97854735382787));
#111362=CARTESIAN_POINT('Ctrl Pts',(-11.0527583674781,7.62687956404507,
9.9833664012573));
#111363=CARTESIAN_POINT('Ctrl Pts',(-11.0551420830886,7.62706792199881,
9.98584062495737));
#111364=CARTESIAN_POINT('Ctrl Pts',(-11.0607906533447,7.62751748194107,
9.99174513830514));
#111365=CARTESIAN_POINT('Ctrl Pts',(-11.0640475996165,7.62777927342392,
9.99518291175387));
#111366=CARTESIAN_POINT('Ctrl Pts',(-11.0746968835869,7.62864358238071,
10.0065332845908));
#111367=CARTESIAN_POINT('Ctrl Pts',(-11.0820179195412,7.62925107941532,
10.0145119412173));
#111368=CARTESIAN_POINT('Ctrl Pts',(-11.1290963231606,7.63324099374901,
10.0669762339439));
#111369=CARTESIAN_POINT('Ctrl Pts',(-11.1661870582671,7.63677599153351,
10.113772980933));
#111370=CARTESIAN_POINT('Ctrl Pts',(-11.23313686152,7.6437894073516,10.2097488822825));
#111371=CARTESIAN_POINT('Ctrl Pts',(-11.2631642178905,7.64725864854721,
10.2586905477699));
#111372=CARTESIAN_POINT('Ctrl Pts',(-11.3294588923257,7.65564058228828,
10.3825246629181));
#111373=CARTESIAN_POINT('Ctrl Pts',(-11.3623710085283,7.66048071770189,
10.4589958229372));
#111374=CARTESIAN_POINT('Ctrl Pts',(-11.3924306932414,7.66577214313523,
10.5493173140078));
#111375=CARTESIAN_POINT('Ctrl Pts',(-11.3961026238444,7.66643892474545,
10.5608239591491));
#111376=CARTESIAN_POINT('Ctrl Pts',(-11.4018655978654,7.66752025244773,
10.5796863767382));
#111377=CARTESIAN_POINT('Ctrl Pts',(-11.4040421276465,7.66793753677938,
10.58701525057));
#111378=CARTESIAN_POINT('Ctrl Pts',(-11.4078381680992,7.66868175427716,
10.6001743498469));
#111379=CARTESIAN_POINT('Ctrl Pts',(-11.4094791273435,7.66900937019473,
10.605998160946));
#111380=CARTESIAN_POINT('Ctrl Pts',(-11.4128874020312,7.66970270638948,
10.6183880596459));
#111381=CARTESIAN_POINT('Ctrl Pts',(-11.4146451723637,7.67006811472332,
10.6249566394771));
#111382=CARTESIAN_POINT('Ctrl Pts',(-11.4192450801828,7.67104606754592,
10.642638517003));
#111383=CARTESIAN_POINT('Ctrl Pts',(-11.4220024771116,7.67165590978472,
10.6537734958682));
#111384=CARTESIAN_POINT('Ctrl Pts',(-11.4277792051918,7.67298853821813,
10.6783353407623));
#111385=CARTESIAN_POINT('Ctrl Pts',(-11.4307406584607,7.67370949908612,
10.6917747638016));
#111386=CARTESIAN_POINT('Ctrl Pts',(-11.4534527804026,7.67957299637897,
10.8022364208009));
#111387=CARTESIAN_POINT('Ctrl Pts',(-11.4634999999957,7.68439943215103,
10.9009878497116));
#111388=CARTESIAN_POINT('Ctrl Pts',(-11.4635,7.68921734064608,10.9999999999359));
#111389=CARTESIAN_POINT('Origin',(-10.,3.5,11.));
#111390=CARTESIAN_POINT('',(-11.4634998107004,8.26169270208058,10.9993373195887));
#111391=CARTESIAN_POINT('',(-11.4634997901989,8.18835865039335,10.9992163610944));
#111392=CARTESIAN_POINT('',(-11.4635,3.5,11.));
#111393=CARTESIAN_POINT('Ctrl Pts',(-11.4634997595702,8.26169269924574,
10.9991611090195));
#111394=CARTESIAN_POINT('Ctrl Pts',(-11.4634864167997,8.26051570058515,
10.9758837799716));
#111395=CARTESIAN_POINT('Ctrl Pts',(-11.4629177280139,8.25932189804874,
10.9526108535919));
#111396=CARTESIAN_POINT('Ctrl Pts',(-11.4611828866091,8.25744101470029,
10.9167096405711));
#111397=CARTESIAN_POINT('Ctrl Pts',(-11.4604072524839,8.25677105162849,
10.9040659166203));
#111398=CARTESIAN_POINT('Ctrl Pts',(-11.4591292642527,8.25584855081238,
10.8868857032675));
#111399=CARTESIAN_POINT('Ctrl Pts',(-11.4587696514038,8.25560324219304,
10.8823388042376));
#111400=CARTESIAN_POINT('Ctrl Pts',(-11.4581050060773,8.25517317865635,
10.8744070408744));
#111401=CARTESIAN_POINT('Ctrl Pts',(-11.4578094248404,8.25498892673962,
10.8710213951573));
#111402=CARTESIAN_POINT('Ctrl Pts',(-11.4572093906022,8.25462797069292,
10.8644141853886));
#111403=CARTESIAN_POINT('Ctrl Pts',(-11.4569060391381,8.25445132641096,
10.8611925282721));
#111404=CARTESIAN_POINT('Ctrl Pts',(-11.456231264577,8.25407046296591,10.8542722694741));
#111405=CARTESIAN_POINT('Ctrl Pts',(-11.4558564348213,8.25386606099449,
10.8505740720858));
#111406=CARTESIAN_POINT('Ctrl Pts',(-11.4548297689747,8.253324471006,10.840815364646));
#111407=CARTESIAN_POINT('Ctrl Pts',(-11.4541541585032,8.25298600896113,
10.8347574949308));
#111408=CARTESIAN_POINT('Ctrl Pts',(-11.4511332817111,8.25154483503597,
10.8091254382974));
#111409=CARTESIAN_POINT('Ctrl Pts',(-11.4484305683217,8.25042438498102,
10.789596313735));
#111410=CARTESIAN_POINT('Ctrl Pts',(-11.4410627984828,8.24772244227829,
10.7432708553536));
#111411=CARTESIAN_POINT('Ctrl Pts',(-11.4360436130229,8.24612793856456,
10.7165384601872));
#111412=CARTESIAN_POINT('Ctrl Pts',(-11.4082962911959,8.23836764545882,
10.588532800705));
#111413=CARTESIAN_POINT('Ctrl Pts',(-11.3755826569016,8.23202328267557,
10.489727053627));
#111414=CARTESIAN_POINT('Ctrl Pts',(-11.3164263539626,8.22361455592296,
10.3593734032248));
#111415=CARTESIAN_POINT('Ctrl Pts',(-11.2987248283428,8.22133837283691,
10.3242078901882));
#111416=CARTESIAN_POINT('Ctrl Pts',(-11.26710923146,8.21764552567718,10.2672437345054));
#111417=CARTESIAN_POINT('Ctrl Pts',(-11.2539977458552,8.216203463413,10.2450249537688));
#111418=CARTESIAN_POINT('Ctrl Pts',(-11.2353526367903,8.2142681916172,10.2152559866384));
#111419=CARTESIAN_POINT('Ctrl Pts',(-11.2303244844658,8.21375689657923,
10.2073960810805));
#111420=CARTESIAN_POINT('Ctrl Pts',(-11.2217565290376,8.21290305537858,
10.1942808368283));
#111421=CARTESIAN_POINT('Ctrl Pts',(-11.2182571907706,8.21255903630575,
10.1889995036791));
#111422=CARTESIAN_POINT('Ctrl Pts',(-11.2112852296377,8.21188276131197,
10.178624113085));
#111423=CARTESIAN_POINT('Ctrl Pts',(-11.2078144968864,8.2115504450325,10.173528949177));
#111424=CARTESIAN_POINT('Ctrl Pts',(-11.200100255582,8.21082122027339,10.1623565416016));
#111425=CARTESIAN_POINT('Ctrl Pts',(-11.1958425503987,8.21042485386706,
10.1562892769299));
#111426=CARTESIAN_POINT('Ctrl Pts',(-11.1806802429581,8.20903439996681,
10.1350282290229));
#111427=CARTESIAN_POINT('Ctrl Pts',(-11.169530443889,8.20804959612698,10.1200110324375));
#111428=CARTESIAN_POINT('Ctrl Pts',(-11.101400889668,8.20224255907475,10.0318332049646));
#111429=CARTESIAN_POINT('Ctrl Pts',(-11.0378596797326,8.19769125038252,
9.96400753382538));
#111430=CARTESIAN_POINT('Ctrl Pts',(-10.8975922000422,8.18858355248319,
9.84023347611682));
#111431=CARTESIAN_POINT('Ctrl Pts',(-10.8210025518596,8.18404442896131,
9.78481235785662));
#111432=CARTESIAN_POINT('Ctrl Pts',(-10.7311214273068,8.17859299652699,
9.73217082468049));
#111433=CARTESIAN_POINT('Ctrl Pts',(-10.7225682213949,8.17807295909361,
9.72727673269008));
#111434=CARTESIAN_POINT('Ctrl Pts',(-10.7091501056261,8.17725414549164,
9.71977782392446));
#111435=CARTESIAN_POINT('Ctrl Pts',(-10.7043186442631,8.17695871797525,
9.71711343528997));
#111436=CARTESIAN_POINT('Ctrl Pts',(-10.6952567086822,8.17640328338292,
9.71218270252671));
#111437=CARTESIAN_POINT('Ctrl Pts',(-10.6910299132703,8.17614367407504,
9.7099097162209));
#111438=CARTESIAN_POINT('Ctrl Pts',(-10.6837822932254,8.17569748302378,
9.70605809920393));
#111439=CARTESIAN_POINT('Ctrl Pts',(-10.68076695099,8.17551153967774,9.70446913374219));
#111440=CARTESIAN_POINT('Ctrl Pts',(-10.6748998471318,8.17514909528203,
9.7014035426121));
#111441=CARTESIAN_POINT('Ctrl Pts',(-10.6720487441228,8.17497267605955,
9.69992575292316));
#111442=CARTESIAN_POINT('Ctrl Pts',(-10.6651830792277,8.17454719150037,
9.69639574659041));
#111443=CARTESIAN_POINT('Ctrl Pts',(-10.6611638774789,8.17429757479693,
9.69435268758186));
#111444=CARTESIAN_POINT('Ctrl Pts',(-10.6464079546149,8.17337936488766,
9.68693749438024));
#111445=CARTESIAN_POINT('Ctrl Pts',(-10.6356149723367,8.17270432298697,
9.68167910751061));
#111446=CARTESIAN_POINT('Ctrl Pts',(-10.5566507580465,8.1677473100583,9.64440247938146));
#111447=CARTESIAN_POINT('Ctrl Pts',(-10.4861678174006,8.16323029296284,
9.61755880049686));
#111448=CARTESIAN_POINT('Ctrl Pts',(-10.3518027950886,8.1548017513757,9.5779367964271));
#111449=CARTESIAN_POINT('Ctrl Pts',(-10.2885146819234,8.15090242298709,
9.5637586949654));
#111450=CARTESIAN_POINT('Ctrl Pts',(-10.1850806543593,8.14474989359811,
9.5477024561384));
#111451=CARTESIAN_POINT('Ctrl Pts',(-10.1454326595844,8.14244154995233,
9.54319777126721));
#111452=CARTESIAN_POINT('Ctrl Pts',(-10.0796705421542,8.1387029529165,9.53843809657381));
#111453=CARTESIAN_POINT('Ctrl Pts',(-10.0536468584662,8.13724649259769,
9.53725165225554));
#111454=CARTESIAN_POINT('Ctrl Pts',(-10.0182414063516,8.13529530317956,
9.53658372525667));
#111455=CARTESIAN_POINT('Ctrl Pts',(-10.0088770404208,8.13478210175981,
9.53649696073565));
#111456=CARTESIAN_POINT('Ctrl Pts',(-9.99316997170365,8.13392597306222,
9.53650219465627));
#111457=CARTESIAN_POINT('Ctrl Pts',(-9.98682762507647,8.13358155559569,
9.53654553681148));
#111458=CARTESIAN_POINT('Ctrl Pts',(-9.97432683399538,8.13290516498559,
9.53671223718473));
#111459=CARTESIAN_POINT('Ctrl Pts',(-9.96816849439757,8.13257312653889,
9.53683324767879));
#111460=CARTESIAN_POINT('Ctrl Pts',(-9.95462290706325,8.13184530380463,
9.53718497727766));
#111461=CARTESIAN_POINT('Ctrl Pts',(-9.94723624771688,8.13145005373148,
9.53743278431064));
#111462=CARTESIAN_POINT('Ctrl Pts',(-9.92130077953414,8.13006782482262,
9.53849960614553));
#111463=CARTESIAN_POINT('Ctrl Pts',(-9.90276556184566,8.12908998141345,
9.53961564195093));
#111464=CARTESIAN_POINT('Ctrl Pts',(-9.78631631240663,8.12300103694166,
9.54885421329039));
#111465=CARTESIAN_POINT('Ctrl Pts',(-9.68940628282846,8.11819891164212,
9.56646634538527));
#111466=CARTESIAN_POINT('Ctrl Pts',(-9.52759275726565,8.11000461678469,
9.61306742850065));
#111467=CARTESIAN_POINT('Ctrl Pts',(-9.46168759014302,8.10660593824554,
9.63729347777784));
#111468=CARTESIAN_POINT('Ctrl Pts',(-9.37928739195133,8.10200781914097,
9.67449643773879));
#111469=CARTESIAN_POINT('Ctrl Pts',(-9.36097339661832,8.10096221804414,
9.68322789850165));
#111470=CARTESIAN_POINT('Ctrl Pts',(-9.33084201434401,8.09919295082646,
9.69837010837092));
#111471=CARTESIAN_POINT('Ctrl Pts',(-9.31892050305939,8.09847987531609,
9.70456822714081));
#111472=CARTESIAN_POINT('Ctrl Pts',(-9.30260901874348,8.09748380865861,
9.7133361320728));
#111473=CARTESIAN_POINT('Ctrl Pts',(-9.29814423059944,8.09720902944721,
9.71576615556808));
#111474=CARTESIAN_POINT('Ctrl Pts',(-9.2906282312651,8.09674270110176,9.71990774447461));
#111475=CARTESIAN_POINT('Ctrl Pts',(-9.28757028633244,8.09655191150049,
9.7216071058729));
#111476=CARTESIAN_POINT('Ctrl Pts',(-9.28173692445216,8.09618587506674,
9.72487625253952));
#111477=CARTESIAN_POINT('Ctrl Pts',(-9.27896050076673,8.09601075300766,
9.72644416801724));
#111478=CARTESIAN_POINT('Ctrl Pts',(-9.27234557479452,8.09559139644156,
9.73020834573471));
#111479=CARTESIAN_POINT('Ctrl Pts',(-9.26851188310388,8.09534664414556,
9.73241294517049));
#111480=CARTESIAN_POINT('Ctrl Pts',(-9.25484954374753,8.09446843329774,
9.74035221718689));
#111481=CARTESIAN_POINT('Ctrl Pts',(-9.24507811298438,8.09382923192695,
9.74618395784058));
#111482=CARTESIAN_POINT('Ctrl Pts',(-9.15333031157141,8.08772916501643,
9.80240175923716));
#111483=CARTESIAN_POINT('Ctrl Pts',(-9.07644841715503,8.08188458272259,
9.86064001305839));
#111484=CARTESIAN_POINT('Ctrl Pts',(-8.95449610729651,8.071899949597,9.97352569938206));
#111485=CARTESIAN_POINT('Ctrl Pts',(-8.90661936226839,8.06773896364083,
10.024680406677));
#111486=CARTESIAN_POINT('Ctrl Pts',(-8.83871158169893,8.06152979611651,
10.1085514366615));
#111487=CARTESIAN_POINT('Ctrl Pts',(-8.81599421848539,8.05938762165198,
10.1389529572969));
#111488=CARTESIAN_POINT('Ctrl Pts',(-8.78841526071043,8.05669893754897,
10.1790193835894));
#111489=CARTESIAN_POINT('Ctrl Pts',(-8.7824448312407,8.056111063646,10.1879001462068));
#111490=CARTESIAN_POINT('Ctrl Pts',(-8.7729340345619,8.05516484271529,10.2023877405371));
#111491=CARTESIAN_POINT('Ctrl Pts',(-8.7693335010373,8.0548042793897,10.2079544392391));
#111492=CARTESIAN_POINT('Ctrl Pts',(-8.76249985477756,8.05411532660058,
10.2186788803611));
#111493=CARTESIAN_POINT('Ctrl Pts',(-8.75926085884316,8.0537867261296,10.223832694222));
#111494=CARTESIAN_POINT('Ctrl Pts',(-8.7519319743256,8.05303839184356,10.2356573560826));
#111495=CARTESIAN_POINT('Ctrl Pts',(-8.74786322208443,8.05261943014049,
10.2423411277992));
#111496=CARTESIAN_POINT('Ctrl Pts',(-8.73517412397909,8.05130133479323,
10.2635670258701));
#111497=CARTESIAN_POINT('Ctrl Pts',(-8.72675186593977,8.05040928173178,
10.2782263221184));
#111498=CARTESIAN_POINT('Ctrl Pts',(-8.65869889191197,8.04304565585298,
10.4015751488433));
#111499=CARTESIAN_POINT('Ctrl Pts',(-8.61284792867623,8.03710476693989,
10.5172866849481));
#111500=CARTESIAN_POINT('Ctrl Pts',(-8.56384858926869,8.02744365456947,
10.7088880765153));
#111501=CARTESIAN_POINT('Ctrl Pts',(-8.55100129267519,8.02379684512443,
10.7816487034097));
#111502=CARTESIAN_POINT('Ctrl Pts',(-8.54281568212808,8.01940953676066,
10.8638935849525));
#111503=CARTESIAN_POINT('Ctrl Pts',(-8.54201674256544,8.01893435591819,
10.8727368639456));
#111504=CARTESIAN_POINT('Ctrl Pts',(-8.54094996169062,8.01822240791579,
10.8858782453035));
#111505=CARTESIAN_POINT('Ctrl Pts',(-8.54062052708183,8.01798890672005,
10.8901713049565));
#111506=CARTESIAN_POINT('Ctrl Pts',(-8.54006616289705,8.0175701204292,10.8978389526661));
#111507=CARTESIAN_POINT('Ctrl Pts',(-8.53983398059039,8.01738523684094,
10.9012129372323));
#111508=CARTESIAN_POINT('Ctrl Pts',(-8.53935335075794,8.01698078019691,
10.9085694911119));
#111509=CARTESIAN_POINT('Ctrl Pts',(-8.5391094982778,8.01676096636294,10.912552226442));
#111510=CARTESIAN_POINT('Ctrl Pts',(-8.53847474490722,8.0161454128513,10.9236641796471));
#111511=CARTESIAN_POINT('Ctrl Pts',(-8.5381197294417,8.01574778286453,10.9307952378733));
#111512=CARTESIAN_POINT('Ctrl Pts',(-8.53643209474614,8.01351763880237,
10.970549864329));
#111513=CARTESIAN_POINT('Ctrl Pts',(-8.536139441446,8.01163551675328,11.003206213463));
#111514=CARTESIAN_POINT('Ctrl Pts',(-8.53734383931992,8.00875279562614,
11.0523687694782));
#111515=CARTESIAN_POINT('Ctrl Pts',(-8.53802868107255,8.00777582323257,
11.068886639336));
#111516=CARTESIAN_POINT('Ctrl Pts',(-8.54391603292052,8.00177889571196,
11.1696193619885));
#111517=CARTESIAN_POINT('Ctrl Pts',(-8.55611362085474,7.99664436250698,
11.2532668649875));
#111518=CARTESIAN_POINT('Ctrl Pts',(-8.59078684908308,7.9876672006377,11.4005350885795));
#111519=CARTESIAN_POINT('Ctrl Pts',(-8.61057307455072,7.98378514914999,
11.4645478807354));
#111520=CARTESIAN_POINT('Ctrl Pts',(-8.64073056356577,7.97910136331877,
11.5426801680854));
#111521=CARTESIAN_POINT('Ctrl Pts',(-8.6470575091315,7.97816948212285,11.5582667955786));
#111522=CARTESIAN_POINT('Ctrl Pts',(-8.6567465424071,7.97681336645421,11.5810031922856));
#111523=CARTESIAN_POINT('Ctrl Pts',(-8.65989988888751,7.97638221188876,
11.588239964964));
#111524=CARTESIAN_POINT('Ctrl Pts',(-8.66558472747087,7.97562255543015,
11.6010033908312));
#111525=CARTESIAN_POINT('Ctrl Pts',(-8.66809237102331,7.97529325954224,
11.606540406538));
#111526=CARTESIAN_POINT('Ctrl Pts',(-8.67341982918387,7.97460559466635,
11.6181113630333));
#111527=CARTESIAN_POINT('Ctrl Pts',(-8.67624648875098,7.97424746750451,
11.6241420112194));
#111528=CARTESIAN_POINT('Ctrl Pts',(-8.68378182625239,7.97331009368449,
11.6399370902177));
#111529=CARTESIAN_POINT('Ctrl Pts',(-8.6885580433488,7.97273316522437,11.6496689642238));
#111530=CARTESIAN_POINT('Ctrl Pts',(-8.7093997210082,7.97028649146057,11.6909687014452));
#111531=CARTESIAN_POINT('Ctrl Pts',(-8.72650081102523,7.96845261375559,
11.7220020081914));
#111532=CARTESIAN_POINT('Ctrl Pts',(-8.81931062604574,7.95926794952584,
11.8768467921363));
#111533=CARTESIAN_POINT('Ctrl Pts',(-8.91199182485794,7.9525584411088,11.9895042253733));
#111534=CARTESIAN_POINT('Ctrl Pts',(-9.03511869094809,7.94413331061099,
12.1005755604578));
#111535=CARTESIAN_POINT('Ctrl Pts',(-9.05081353369598,7.94306517624342,
12.1141397958369));
#111536=CARTESIAN_POINT('Ctrl Pts',(-9.07731241337673,7.94126128483738,
12.1360750124462));
#111537=CARTESIAN_POINT('Ctrl Pts',(-9.08795522573274,7.9405366574741,12.1446366758369));
#111538=CARTESIAN_POINT('Ctrl Pts',(-9.10274667960778,7.93952700633262,
12.1561984702662));
#111539=CARTESIAN_POINT('Ctrl Pts',(-9.10679386655468,7.93925049056074,
12.1593279196178));
#111540=CARTESIAN_POINT('Ctrl Pts',(-9.11364124719736,7.93878206909761,
12.1645654537245));
#111541=CARTESIAN_POINT('Ctrl Pts',(-9.11643279874338,7.93859093882967,
12.1666848482997));
#111542=CARTESIAN_POINT('Ctrl Pts',(-9.12177314070547,7.93822493378267,
12.1707091690824));
#111543=CARTESIAN_POINT('Ctrl Pts',(-9.12432057269585,7.93805018836196,
12.1726158429585));
#111544=CARTESIAN_POINT('Ctrl Pts',(-9.1304028876468,7.93763263469327,12.1771373943867));
#111545=CARTESIAN_POINT('Ctrl Pts',(-9.13394335590712,7.93738931848249,
12.1797446635967));
#111546=CARTESIAN_POINT('Ctrl Pts',(-9.14656392341383,7.93652121371726,
12.188951266028));
#111547=CARTESIAN_POINT('Ctrl Pts',(-9.15570790812537,7.93589084800901,
12.1954618763893));
#111548=CARTESIAN_POINT('Ctrl Pts',(-9.24673678398372,7.9296091451164,12.2587100720652));
#111549=CARTESIAN_POINT('Ctrl Pts',(-9.33413253089751,7.92354643585885,
12.3070480626427));
#111550=CARTESIAN_POINT('Ctrl Pts',(-9.5168796120167,7.91161790513388,12.385006207289));
#111551=CARTESIAN_POINT('Ctrl Pts',(-9.61173077356932,7.90578647236496,
12.4145318443178));
#111552=CARTESIAN_POINT('Ctrl Pts',(-9.72244061947996,7.89950157636633,
12.4370056787119));
#111553=CARTESIAN_POINT('Ctrl Pts',(-9.7360688009411,7.89873614922377,12.4395710718936));
#111554=CARTESIAN_POINT('Ctrl Pts',(-9.75693490329717,7.89757643514967,
12.4431926612901));
#111555=CARTESIAN_POINT('Ctrl Pts',(-9.76414743979807,7.89717778888479,
12.4443888920172));
#111556=CARTESIAN_POINT('Ctrl Pts',(-9.7767418903623,7.89648546542641,12.4463808832964));
#111557=CARTESIAN_POINT('Ctrl Pts',(-9.78211979648902,7.89619104002323,
12.4472007673798));
#111558=CARTESIAN_POINT('Ctrl Pts',(-9.79425503338721,7.89552932660027,
12.4489816567372));
#111559=CARTESIAN_POINT('Ctrl Pts',(-9.80101479270884,7.89516258232947,
12.4499254195564));
#111560=CARTESIAN_POINT('Ctrl Pts',(-9.81927381426264,7.89417682239226,
12.4523445525943));
#111561=CARTESIAN_POINT('Ctrl Pts',(-9.83078453914054,7.89356058700529,
12.4537306462004));
#111562=CARTESIAN_POINT('Ctrl Pts',(-9.88491769985231,7.89068556752297,
12.4595975438514));
#111563=CARTESIAN_POINT('Ctrl Pts',(-9.92770900113951,7.8884807025409,12.4623417429202));
#111564=CARTESIAN_POINT('Ctrl Pts',(-9.99149861199725,7.88526236244208,
12.4636251231227));
#111565=CARTESIAN_POINT('Ctrl Pts',(-10.01244240482,7.88421649677356,12.4635969386559));
#111566=CARTESIAN_POINT('Ctrl Pts',(-10.1313992827198,7.87831801824072,
12.4608831188763));
#111567=CARTESIAN_POINT('Ctrl Pts',(-10.2289415353001,7.8736609838397,12.4488028516785));
#111568=CARTESIAN_POINT('Ctrl Pts',(-10.3553897213718,7.86719990921243,
12.4200462452602));
#111569=CARTESIAN_POINT('Ctrl Pts',(-10.3860024950595,7.86559991591479,
12.4120322424405));
#111570=CARTESIAN_POINT('Ctrl Pts',(-10.4340567846516,7.86299820623345,
12.3977728264003));
#111571=CARTESIAN_POINT('Ctrl Pts',(-10.4516816977724,7.86202433206106,
12.392177340711));
#111572=CARTESIAN_POINT('Ctrl Pts',(-10.4746268374049,7.86072497745424,
12.3844112465397));
#111573=CARTESIAN_POINT('Ctrl Pts',(-10.4800476882087,7.86041567289538,
12.3825409032618));
#111574=CARTESIAN_POINT('Ctrl Pts',(-10.4888886276334,7.8599072001777,12.3794322706587));
#111575=CARTESIAN_POINT('Ctrl Pts',(-10.4923153907611,7.8597091226726,12.3782129860776));
#111576=CARTESIAN_POINT('Ctrl Pts',(-10.4989830432694,7.85932171112839,
12.3758125130659));
#111577=CARTESIAN_POINT('Ctrl Pts',(-10.5022243519322,7.85913245221642,
12.3746326229606));
#111578=CARTESIAN_POINT('Ctrl Pts',(-10.5101624117455,7.85866672228905,
12.3717112146059));
#111579=CARTESIAN_POINT('Ctrl Pts',(-10.5148544309898,7.85838952028002,
12.369957027072));
#111580=CARTESIAN_POINT('Ctrl Pts',(-10.5307883911688,7.85744183679314,
12.363906439038));
#111581=CARTESIAN_POINT('Ctrl Pts',(-10.5419860102289,7.85676512040187,
12.3594955816079));
#111582=CARTESIAN_POINT('Ctrl Pts',(-10.6226478189352,7.85181895954054,
12.3265671629433));
#111583=CARTESIAN_POINT('Ctrl Pts',(-10.6898751322926,7.84731602813228,
12.2928809571515));
#111584=CARTESIAN_POINT('Ctrl Pts',(-10.8094296251383,7.83892241618557,
12.2209861087014));
#111585=CARTESIAN_POINT('Ctrl Pts',(-10.8623942811609,7.83504394343544,
12.1841707321315));
#111586=CARTESIAN_POINT('Ctrl Pts',(-10.9442002393989,7.82889005692504,
12.1188993280703));
#111587=CARTESIAN_POINT('Ctrl Pts',(-10.9745926470737,7.82656151224971,
12.092528886242));
#111588=CARTESIAN_POINT('Ctrl Pts',(-11.0229284200694,7.82279423510194,
12.0469652572292));
#111589=CARTESIAN_POINT('Ctrl Pts',(-11.0415094834993,7.82132878125215,
12.0284828252419));
#111590=CARTESIAN_POINT('Ctrl Pts',(-11.0660592401253,7.81936765953194,
12.0027153313425));
#111591=CARTESIAN_POINT('Ctrl Pts',(-11.0724679240559,7.81885327574522,
11.9958578697631));
#111592=CARTESIAN_POINT('Ctrl Pts',(-11.0830990247742,7.81799572775894,
11.9842606533324));
#111593=CARTESIAN_POINT('Ctrl Pts',(-11.0873573130261,7.81765106262433,
11.9795542898343));
#111594=CARTESIAN_POINT('Ctrl Pts',(-11.0956854056592,7.81697459635997,
11.9702286531604));
#111595=CARTESIAN_POINT('Ctrl Pts',(-11.0997569427431,7.81664272688003,
11.9656111101594));
#111596=CARTESIAN_POINT('Ctrl Pts',(-11.1086435564058,7.81591576069624,
11.9554036547644));
#111597=CARTESIAN_POINT('Ctrl Pts',(-11.1134457605037,7.81552119340651,
11.9498027267798));
#111598=CARTESIAN_POINT('Ctrl Pts',(-11.1301304938975,7.81414397814236,
11.9300424654383));
#111599=CARTESIAN_POINT('Ctrl Pts',(-11.1417872083514,7.81317037587054,
11.9156942348498));
#111600=CARTESIAN_POINT('Ctrl Pts',(-11.2159952712165,7.80688749904757,
11.8207305818259));
#111601=CARTESIAN_POINT('Ctrl Pts',(-11.2702422955657,7.80191495581177,
11.7339823850138));
#111602=CARTESIAN_POINT('Ctrl Pts',(-11.3445360818144,7.79367758349093,
11.5818727220127));
#111603=CARTESIAN_POINT('Ctrl Pts',(-11.3698442877853,7.79041103265121,
11.5194984311657));
#111604=CARTESIAN_POINT('Ctrl Pts',(-11.3969459205945,7.78597894418571,
11.4367693004369));
#111605=CARTESIAN_POINT('Ctrl Pts',(-11.4027343684134,7.78495622183093,
11.4178056418038));
#111606=CARTESIAN_POINT('Ctrl Pts',(-11.411734266184,7.78322218827329,11.3860221229114));
#111607=CARTESIAN_POINT('Ctrl Pts',(-11.4151606170667,7.78252093447687,
11.3732654839871));
#111608=CARTESIAN_POINT('Ctrl Pts',(-11.419657391117,7.78153878708231,11.355570861964));
#111609=CARTESIAN_POINT('Ctrl Pts',(-11.4208757106502,7.78126580783051,
11.3506707278953));
#111610=CARTESIAN_POINT('Ctrl Pts',(-11.4228935814655,7.78080164423534,
11.3423715788638));
#111611=CARTESIAN_POINT('Ctrl Pts',(-11.423706382874,7.78061120303904,11.3389757768865));
#111612=CARTESIAN_POINT('Ctrl Pts',(-11.4252397904852,7.780245113233,11.3324665429807));
#111613=CARTESIAN_POINT('Ctrl Pts',(-11.4259623624624,7.780069584556,11.3293536139484));
#111614=CARTESIAN_POINT('Ctrl Pts',(-11.4276666341271,7.77964829475175,
11.3219006546947));
#111615=CARTESIAN_POINT('Ctrl Pts',(-11.4286387413593,7.77940200527548,
11.3175584911955));
#111616=CARTESIAN_POINT('Ctrl Pts',(-11.43206486752,7.77851216221731,11.3019206520528));
#111617=CARTESIAN_POINT('Ctrl Pts',(-11.4344047783189,7.77786266848706,
11.2906007226145));
#111618=CARTESIAN_POINT('Ctrl Pts',(-11.4544136213632,7.77191557802975,
11.1876663162052));
#111619=CARTESIAN_POINT('Ctrl Pts',(-11.4634164151182,7.76625774086926,
11.0945920198759));
#111620=CARTESIAN_POINT('Ctrl Pts',(-11.463499806902,7.76062354882082,11.000868104301));
#111621=CARTESIAN_POINT('Ctrl Pts',(-11.4635,7.76059745675011,11.0004340499109));
#111622=CARTESIAN_POINT('Ctrl Pts',(-11.4635,7.76057136598891,11.0000000000874));
#111623=CARTESIAN_POINT('',(-11.4634994441716,7.68928058350007,11.0012989883455));
#111624=CARTESIAN_POINT('Ctrl Pts',(-11.4635,7.68921734064608,10.9999999999359));
#111625=CARTESIAN_POINT('Ctrl Pts',(-11.4635,7.68923840923771,11.0004329775571));
#111626=CARTESIAN_POINT('Ctrl Pts',(-11.4634998078549,7.68925947810631,
11.0008659601426));
#111627=CARTESIAN_POINT('Ctrl Pts',(-11.4634994235514,7.68928054728939,
11.0012989475658));
#111628=CARTESIAN_POINT('Ctrl Pts',(-11.4634994235137,7.68928054935369,
11.0012989899887));
#111629=CARTESIAN_POINT('Ctrl Pts',(-11.4634190836016,7.69368498754126,
11.0918134790247));
#111630=CARTESIAN_POINT('Ctrl Pts',(-11.4549417134562,7.69807278572729,
11.1821153036776));
#111631=CARTESIAN_POINT('Ctrl Pts',(-11.4367852399318,7.70324800997049,
11.2784552169745));
#111632=CARTESIAN_POINT('Ctrl Pts',(-11.4353311770417,7.70364882957371,
11.2858558050101));
#111633=CARTESIAN_POINT('Ctrl Pts',(-11.4328983795781,7.7042988236619,11.297750969576));
#111634=CARTESIAN_POINT('Ctrl Pts',(-11.4319555261105,7.70454615127574,
11.3022528349211));
#111635=CARTESIAN_POINT('Ctrl Pts',(-11.4301047594257,7.70502316788668,
11.3108866745424));
#111636=CARTESIAN_POINT('Ctrl Pts',(-11.4292001191023,7.70525267803507,
11.3150193105026));
#111637=CARTESIAN_POINT('Ctrl Pts',(-11.4276119976659,7.70564951717479,
11.3221266051275));
#111638=CARTESIAN_POINT('Ctrl Pts',(-11.4269371124375,7.70581635994053,
11.3251031260352));
#111639=CARTESIAN_POINT('Ctrl Pts',(-11.4253749339021,7.70619852752224,
11.3318943910655));
#111640=CARTESIAN_POINT('Ctrl Pts',(-11.4244816506068,7.70641418384707,
11.3357076337634));
#111641=CARTESIAN_POINT('Ctrl Pts',(-11.421992473739,7.70700729330801,11.3461445871728));
#111642=CARTESIAN_POINT('Ctrl Pts',(-11.4203656347107,7.70738642764274,
11.3527607272227));
#111643=CARTESIAN_POINT('Ctrl Pts',(-11.4118258237233,7.70933361574373,
11.3864739794682));
#111644=CARTESIAN_POINT('Ctrl Pts',(-11.4041837878065,7.71093797190499,
11.4133787368306));
#111645=CARTESIAN_POINT('Ctrl Pts',(-11.3875659331127,7.71415965687219,
11.4660886731694));
#111646=CARTESIAN_POINT('Ctrl Pts',(-11.3786285912183,7.71577519582412,
11.4918952756727));
#111647=CARTESIAN_POINT('Ctrl Pts',(-11.3595435726369,7.71899418465574,
11.5423883391644));
#111648=CARTESIAN_POINT('Ctrl Pts',(-11.3494318170698,7.72059648400974,
11.5670780942936));
#111649=CARTESIAN_POINT('Ctrl Pts',(-11.3056900203881,7.72710749897456,
11.6660759875016));
#111650=CARTESIAN_POINT('Ctrl Pts',(-11.2665480177364,7.73201515679448,
11.7377952809545));
#111651=CARTESIAN_POINT('Ctrl Pts',(-11.196322377239,7.73941999909446,11.8442496850267));
#111652=CARTESIAN_POINT('Ctrl Pts',(-11.1692181827876,7.74203269372293,
11.8814047014345));
#111653=CARTESIAN_POINT('Ctrl Pts',(-11.1330538131279,7.74522946179679,
11.9263687110538));
#111654=CARTESIAN_POINT('Ctrl Pts',(-11.125589995688,7.74587518075914,11.9354234897006));
#111655=CARTESIAN_POINT('Ctrl Pts',(-11.1135931060359,7.74689135287718,
11.9496260651385));
#111656=CARTESIAN_POINT('Ctrl Pts',(-11.1091314686049,7.74726465410854,
11.9548333137128));
#111657=CARTESIAN_POINT('Ctrl Pts',(-11.1006699922172,7.7479640826584,11.9645695018436));
#111658=CARTESIAN_POINT('Ctrl Pts',(-11.0966783966775,7.74829053523432,
11.9691053871595));
#111659=CARTESIAN_POINT('Ctrl Pts',(-11.0876326404212,7.74902260269109,
11.9792571515646));
#111660=CARTESIAN_POINT('Ctrl Pts',(-11.0825628315591,7.74942755912315,
11.9848588975205));
#111661=CARTESIAN_POINT('Ctrl Pts',(-11.0694773730217,7.7504594016223,11.9990941791225));
#111662=CARTESIAN_POINT('Ctrl Pts',(-11.0614003642233,7.75108370772191,
12.0076707337359));
#111663=CARTESIAN_POINT('Ctrl Pts',(-11.0053360651424,7.75533406773171,
12.0657803912766));
#111664=CARTESIAN_POINT('Ctrl Pts',(-10.9540009474293,7.75880992968169,
12.1119676750545));
#111665=CARTESIAN_POINT('Ctrl Pts',(-10.8194809492821,7.7672197772654,12.2167987811237));
#111666=CARTESIAN_POINT('Ctrl Pts',(-10.7330916586681,7.77203449804421,
12.2707173193917));
#111667=CARTESIAN_POINT('Ctrl Pts',(-10.6093024626622,7.77898255081495,
12.3311243967917));
#111668=CARTESIAN_POINT('Ctrl Pts',(-10.5762072605312,7.78084671267582,
12.3457809797531));
#111669=CARTESIAN_POINT('Ctrl Pts',(-10.5361943283622,7.78314609879579,
12.3617545847397));
#111670=CARTESIAN_POINT('Ctrl Pts',(-10.5297650417542,7.78351694054014,
12.3642686332424));
#111671=CARTESIAN_POINT('Ctrl Pts',(-10.5195734326441,7.78410731782829,
12.3681709609848));
#111672=CARTESIAN_POINT('Ctrl Pts',(-10.5158226975673,7.7843251269959,12.3695894546494));
#111673=CARTESIAN_POINT('Ctrl Pts',(-10.5088985037763,7.78472829262217,
12.3721756436949));
#111674=CARTESIAN_POINT('Ctrl Pts',(-10.5057267882593,7.78491338677897,
12.3733477707008));
#111675=CARTESIAN_POINT('Ctrl Pts',(-10.4985285853816,7.78533439904986,
12.3759795938061));
#111676=CARTESIAN_POINT('Ctrl Pts',(-10.4944997552563,7.78557069721068,
12.3774326060151));
#111677=CARTESIAN_POINT('Ctrl Pts',(-10.4840349262179,7.78618607278444,
12.3811549559348));
#111678=CARTESIAN_POINT('Ctrl Pts',(-10.4775894005346,7.78656665503836,
12.3833969722983));
#111679=CARTESIAN_POINT('Ctrl Pts',(-10.4344952930847,7.78912043756124,
12.3980497983563));
#111680=CARTESIAN_POINT('Ctrl Pts',(-10.3973852673983,7.79136376991451,
12.4090471475469));
#111681=CARTESIAN_POINT('Ctrl Pts',(-10.2607681729708,7.79967713226848,
12.4437066787406));
#111682=CARTESIAN_POINT('Ctrl Pts',(-10.1592865351854,7.80593319436265,
12.4583958448996));
#111683=CARTESIAN_POINT('Ctrl Pts',(-10.0133428077127,7.81455590384069,
12.4640941451296));
#111684=CARTESIAN_POINT('Ctrl Pts',(-9.96953033525498,7.81710068151394,
12.4638380359867));
#111685=CARTESIAN_POINT('Ctrl Pts',(-9.90717085812578,7.82064963712858,
12.460671986689));
#111686=CARTESIAN_POINT('Ctrl Pts',(-9.88856862256505,7.82169915772471,
12.4593707529206));
#111687=CARTESIAN_POINT('Ctrl Pts',(-9.85545048632595,7.82355149027602,
12.456417156809));
#111688=CARTESIAN_POINT('Ctrl Pts',(-9.84092513326514,7.82435834933385,
12.4549023008203));
#111689=CARTESIAN_POINT('Ctrl Pts',(-9.81901420147948,7.82556739315652,
12.4522851258648));
#111690=CARTESIAN_POINT('Ctrl Pts',(-9.81161068268768,7.82597452389837,
12.4513433136478));
#111691=CARTESIAN_POINT('Ctrl Pts',(-9.79828914330987,7.82670466288694,
12.4495450083023));
#111692=CARTESIAN_POINT('Ctrl Pts',(-9.79236859005619,7.82702829435056,
12.4487088043736));
#111693=CARTESIAN_POINT('Ctrl Pts',(-9.779625687343,7.82772304208109,12.4468293065368));
#111694=CARTESIAN_POINT('Ctrl Pts',(-9.77280523956981,7.82809377520274,
12.4457739875189));
#111695=CARTESIAN_POINT('Ctrl Pts',(-9.75450821001206,7.82908545528883,
12.4428102365794));
#111696=CARTESIAN_POINT('Ctrl Pts',(-9.74304636873106,7.82970362611249,
12.4408131174581));
#111697=CARTESIAN_POINT('Ctrl Pts',(-9.68719435328049,7.83270239391885,
12.430393729704));
#111698=CARTESIAN_POINT('Ctrl Pts',(-9.64318467142702,7.83502251694066,
12.4200552520324));
#111699=CARTESIAN_POINT('Ctrl Pts',(-9.49287043064012,7.84288605485962,
12.3773133220856));
#111700=CARTESIAN_POINT('Ctrl Pts',(-9.38983281309044,7.84814203186436,
12.3348660077122));
#111701=CARTESIAN_POINT('Ctrl Pts',(-9.24722868801146,7.85621904635855,
12.2561260472624));
#111702=CARTESIAN_POINT('Ctrl Pts',(-9.20323324608593,7.85884316342265,
12.2286899543104));
#111703=CARTESIAN_POINT('Ctrl Pts',(-9.15447821090923,7.86201336933541,
12.1945645663843));
#111704=CARTESIAN_POINT('Ctrl Pts',(-9.14820190729647,7.86242671838513,
12.1900973083041));
#111705=CARTESIAN_POINT('Ctrl Pts',(-9.13866609243517,7.86306326898607,
12.1831959666657));
#111706=CARTESIAN_POINT('Ctrl Pts',(-9.13538088026638,7.86328413510992,
12.1807974309059));
#111707=CARTESIAN_POINT('Ctrl Pts',(-9.1293857419162,7.8636901503683,12.1763819428009));
#111708=CARTESIAN_POINT('Ctrl Pts',(-9.12667276230554,7.86387500942836,
12.1743692762748));
#111709=CARTESIAN_POINT('Ctrl Pts',(-9.12059137079255,7.86429192173959,
12.1698249731735));
#111710=CARTESIAN_POINT('Ctrl Pts',(-9.11722693457747,7.8645243226174,12.1672881902264));
#111711=CARTESIAN_POINT('Ctrl Pts',(-9.10738786649167,7.86520899877992,
12.1598026729463));
#111712=CARTESIAN_POINT('Ctrl Pts',(-9.10094366504352,7.86566387502757,
12.1548144272894));
#111713=CARTESIAN_POINT('Ctrl Pts',(-9.04034924594162,7.86999968793884,
12.1070956710803));
#111714=CARTESIAN_POINT('Ctrl Pts',(-8.98924704304983,7.87409944965126,
12.0606446003566));
#111715=CARTESIAN_POINT('Ctrl Pts',(-8.88496051018156,7.88316459084927,
11.9514454053834));
#111716=CARTESIAN_POINT('Ctrl Pts',(-8.83338916047024,7.88812616249957,
11.8874583167264));
#111717=CARTESIAN_POINT('Ctrl Pts',(-8.75626213008583,7.89619171918246,
11.7733373097826));
#111718=CARTESIAN_POINT('Ctrl Pts',(-8.72773165158282,7.89937692802259,
11.7254439082916));
#111719=CARTESIAN_POINT('Ctrl Pts',(-8.69645461676477,7.90313014601722,
11.6653914035331));
#111720=CARTESIAN_POINT('Ctrl Pts',(-8.69104178641452,7.90379086791373,
11.6546790764457));
#111721=CARTESIAN_POINT('Ctrl Pts',(-8.68271863939418,7.90482512865225,
11.6376910611875));
#111722=CARTESIAN_POINT('Ctrl Pts',(-8.67972007360504,7.90520168985487,
11.6314594133897));
#111723=CARTESIAN_POINT('Ctrl Pts',(-8.67418747242458,7.90590405388116,
11.6197498016745));
#111724=CARTESIAN_POINT('Ctrl Pts',(-8.671642944657,7.90623020988444,11.6142769814781));
#111725=CARTESIAN_POINT('Ctrl Pts',(-8.66602442064201,7.90695754991232,
11.6019943713698));
#111726=CARTESIAN_POINT('Ctrl Pts',(-8.662968557807,7.90735811279552,11.5951764401221));
#111727=CARTESIAN_POINT('Ctrl Pts',(-8.6553397935828,7.90837109930553,11.5778006159515));
#111728=CARTESIAN_POINT('Ctrl Pts',(-8.65083889311554,7.908981104441,11.5672115479366));
#111729=CARTESIAN_POINT('Ctrl Pts',(-8.62315800396993,7.91281483970639,
11.4998937251341));
#111730=CARTESIAN_POINT('Ctrl Pts',(-8.60343425463699,7.91592185945244,
11.4418063450803));
#111731=CARTESIAN_POINT('Ctrl Pts',(-8.56169064154546,7.92383852963405,
11.2877049284104));
#111732=CARTESIAN_POINT('Ctrl Pts',(-8.5456106443231,7.92851010290634,11.1904158780445));
#111733=CARTESIAN_POINT('Ctrl Pts',(-8.53741334429938,7.93498890228566,
11.0606329410233));
#111734=CARTESIAN_POINT('Ctrl Pts',(-8.53644360842882,7.93659108732605,
11.0289577979744));
#111735=CARTESIAN_POINT('Ctrl Pts',(-8.5365369599794,7.93919606827804,10.978767520455));
#111736=CARTESIAN_POINT('Ctrl Pts',(-8.53692256662853,7.94017093982024,
10.9602602335768));
#111737=CARTESIAN_POINT('Ctrl Pts',(-8.53788735328215,7.94147149567726,
10.9360329839244));
#111738=CARTESIAN_POINT('Ctrl Pts',(-8.53814936931937,7.94178096923293,
10.9303013470084));
#111739=CARTESIAN_POINT('Ctrl Pts',(-8.53863261121367,7.94228968599261,
10.9209377176078));
#111740=CARTESIAN_POINT('Ctrl Pts',(-8.53883369354465,7.94248783709761,
10.9173046930377));
#111741=CARTESIAN_POINT('Ctrl Pts',(-8.53925183810509,7.94287536559478,
10.9102282808228));
#111742=CARTESIAN_POINT('Ctrl Pts',(-8.53946753185463,7.94306466761138,
10.9067848577892));
#111743=CARTESIAN_POINT('Ctrl Pts',(-8.5400262664723,7.94353046656658,10.8983434962636));
#111744=CARTESIAN_POINT('Ctrl Pts',(-8.5403827967072,7.94380769445833,10.8933465157887));
#111745=CARTESIAN_POINT('Ctrl Pts',(-8.54168288047267,7.94475524206195,
10.876354541451));
#111746=CARTESIAN_POINT('Ctrl Pts',(-8.5427486747948,7.94543179279293,10.8643697055457));
#111747=CARTESIAN_POINT('Ctrl Pts',(-8.55154424014717,7.95038284399966,
10.7776037355537));
#111748=CARTESIAN_POINT('Ctrl Pts',(-8.56487788396161,7.95489139453252,
10.7035091596081));
#111749=CARTESIAN_POINT('Ctrl Pts',(-8.60013784970108,7.96330028644251,
10.5682703942036));
#111750=CARTESIAN_POINT('Ctrl Pts',(-8.62055494429744,7.96718843065789,
10.5069110986626));
#111751=CARTESIAN_POINT('Ctrl Pts',(-8.66009499784457,7.97334154157597,
10.4100070084404));
#111752=CARTESIAN_POINT('Ctrl Pts',(-8.67674727870176,7.97566057435793,
10.3735498640916));
#111753=CARTESIAN_POINT('Ctrl Pts',(-8.70669836901665,7.97941443387721,
10.3145177645699));
#111754=CARTESIAN_POINT('Ctrl Pts',(-8.71914345323122,7.98087573627726,
10.2915357221526));
#111755=CARTESIAN_POINT('Ctrl Pts',(-8.73688237588209,7.98283236223632,
10.2607746939086));
#111756=CARTESIAN_POINT('Ctrl Pts',(-8.74164496198704,7.98334628799769,
10.2526963203974));
#111757=CARTESIAN_POINT('Ctrl Pts',(-8.74976036284207,7.98420335316183,
10.2392284344063));
#111758=CARTESIAN_POINT('Ctrl Pts',(-8.75307113977296,7.98454798884169,
10.2338140273876));
#111759=CARTESIAN_POINT('Ctrl Pts',(-8.75966446318483,7.98522460710227,
10.2231873160559));
#111760=CARTESIAN_POINT('Ctrl Pts',(-8.76294490218532,7.98555665650646,
10.2179738646417));
#111761=CARTESIAN_POINT('Ctrl Pts',(-8.77023132832811,7.98628426640856,
10.2065544615098));
#111762=CARTESIAN_POINT('Ctrl Pts',(-8.77425159530096,7.98667929472334,
10.200357792855));
#111763=CARTESIAN_POINT('Ctrl Pts',(-8.78852243768954,7.98805947838855,
10.1787218491865));
#111764=CARTESIAN_POINT('Ctrl Pts',(-8.79901941753807,7.98903553668597,
10.1634467345273));
#111765=CARTESIAN_POINT('Ctrl Pts',(-8.86813830794615,7.99522720688767,
10.0668490635292));
#111766=CARTESIAN_POINT('Ctrl Pts',(-8.93469488988701,8.00011939284524,
9.99153135850552));
#111767=CARTESIAN_POINT('Ctrl Pts',(-9.07289254244124,8.00926245854925,
9.8642250914525));
#111768=CARTESIAN_POINT('Ctrl Pts',(-9.14254727114707,8.0135070055928,9.81076311619941));
#111769=CARTESIAN_POINT('Ctrl Pts',(-9.22845487459194,8.01883527102883,
9.7563164222544));
#111770=CARTESIAN_POINT('Ctrl Pts',(-9.24046212772905,8.01958214496893,
9.74894727778133));
#111771=CARTESIAN_POINT('Ctrl Pts',(-9.25702591541726,8.02061795768229,
9.7391080222834));
#111772=CARTESIAN_POINT('Ctrl Pts',(-9.2614923277946,8.02089780410412,9.73648684759589));
#111773=CARTESIAN_POINT('Ctrl Pts',(-9.26901631995889,8.02137028963123,
9.73212481354041));
#111774=CARTESIAN_POINT('Ctrl Pts',(-9.27206648096569,8.02156212287942,
9.73037114854506));
#111775=CARTESIAN_POINT('Ctrl Pts',(-9.27787782567664,8.0219282241634,9.7270577891966));
#111776=CARTESIAN_POINT('Ctrl Pts',(-9.28063780649281,8.02210235439946,
9.72549604125686));
#111777=CARTESIAN_POINT('Ctrl Pts',(-9.28719799516707,8.02251681393218,
9.72181202571822));
#111778=CARTESIAN_POINT('Ctrl Pts',(-9.2910026162161,8.02275763400676,9.71969772924704));
#111779=CARTESIAN_POINT('Ctrl Pts',(-9.30441883644531,8.02360826755845,
9.71232023414181));
#111780=CARTESIAN_POINT('Ctrl Pts',(-9.31407982772074,8.02422337735138,
9.70714817659425));
#111781=CARTESIAN_POINT('Ctrl Pts',(-9.41502789336033,8.0306700618053,9.65455511111434));
#111782=CARTESIAN_POINT('Ctrl Pts',(-9.51100905065088,8.03694154165222,
9.61677919567156));
#111783=CARTESIAN_POINT('Ctrl Pts',(-9.67343693028765,8.04705111357372,
9.57188938175917));
#111784=CARTESIAN_POINT('Ctrl Pts',(-9.73783377116377,8.05094274476676,
9.55867642030742));
#111785=CARTESIAN_POINT('Ctrl Pts',(-9.83906208740181,8.05681107099318,
9.54491832280981));
#111786=CARTESIAN_POINT('Ctrl Pts',(-9.8753918033547,8.05886930200793,9.54135788304825));
#111787=CARTESIAN_POINT('Ctrl Pts',(-9.92236465972513,8.06146971772881,
9.53852245333272));
#111788=CARTESIAN_POINT('Ctrl Pts',(-9.93291705660242,8.06204999601479,
9.53800008469242));
#111789=CARTESIAN_POINT('Ctrl Pts',(-9.95007040814681,8.06298709811532,
9.53733706603037));
#111790=CARTESIAN_POINT('Ctrl Pts',(-9.95666815610083,8.06334605931964,
9.53712673965328));
#111791=CARTESIAN_POINT('Ctrl Pts',(-9.96936355111284,8.06403399341913,
9.53680799373421));
#111792=CARTESIAN_POINT('Ctrl Pts',(-9.97546088390145,8.06436316102707,
9.53669303544067));
#111793=CARTESIAN_POINT('Ctrl Pts',(-9.98944997867812,8.06511561481059,
9.5365167485406));
#111794=CARTESIAN_POINT('Ctrl Pts',(-9.99734191249357,8.06553809982905,
9.53648113503215));
#111795=CARTESIAN_POINT('Ctrl Pts',(-10.0224985841497,8.06687867824873,
9.53657110237233));
#111796=CARTESIAN_POINT('Ctrl Pts',(-10.0397613144205,8.0677893375019,9.53693834871143));
#111797=CARTESIAN_POINT('Ctrl Pts',(-10.2003233164913,8.07618313636488,
9.54319816184964));
#111798=CARTESIAN_POINT('Ctrl Pts',(-10.3420199857138,8.08292601769029,
9.56981737403164));
#111799=CARTESIAN_POINT('Ctrl Pts',(-10.5301432290091,8.09276186524038,
9.63476296132847));
#111800=CARTESIAN_POINT('Ctrl Pts',(-10.5816210811619,8.09556638536978,
9.65588702263113));
#111801=CARTESIAN_POINT('Ctrl Pts',(-10.6388064169065,8.0989424979864,9.68325419502645));
#111802=CARTESIAN_POINT('Ctrl Pts',(-10.6458186584237,8.0993611262029,9.68667924393484));
#111803=CARTESIAN_POINT('Ctrl Pts',(-10.6564623828216,8.10000414370963,
9.69198390414119));
#111804=CARTESIAN_POINT('Ctrl Pts',(-10.6601140441921,8.10022612378162,
9.69382297718801));
#111805=CARTESIAN_POINT('Ctrl Pts',(-10.6667679916628,8.10063320669391,
9.69720911028051));
#111806=CARTESIAN_POINT('Ctrl Pts',(-10.6697726718672,8.10081800945702,
9.69875128260628));
#111807=CARTESIAN_POINT('Ctrl Pts',(-10.6764932784537,8.10123355885683,
9.70223012341559));
#111808=CARTESIAN_POINT('Ctrl Pts',(-10.68020621072,8.10146464209668,9.70417234233565));
#111809=CARTESIAN_POINT('Ctrl Pts',(-10.691019480823,8.1021419190061,9.7098879967375));
#111810=CARTESIAN_POINT('Ctrl Pts',(-10.6980970093249,8.10259063240782,
9.71370397517261));
#111811=CARTESIAN_POINT('Ctrl Pts',(-10.7544491594172,8.10620469018094,
9.74468932915694));
#111812=CARTESIAN_POINT('Ctrl Pts',(-10.8021466777634,8.10951648582705,
9.77461928193378));
#111813=CARTESIAN_POINT('Ctrl Pts',(-10.9333366754699,8.11913137585377,
9.86788758309227));
#111814=CARTESIAN_POINT('Ctrl Pts',(-11.011928120378,8.12550442276371,9.93754942836499));
#111815=CARTESIAN_POINT('Ctrl Pts',(-11.1140263900329,8.13431599740379,
10.0497454266749));
#111816=CARTESIAN_POINT('Ctrl Pts',(-11.1439513003832,8.13698604171703,
10.0859897902492));
#111817=CARTESIAN_POINT('Ctrl Pts',(-11.1789362401041,8.1402206774688,10.1327788352374));
#111818=CARTESIAN_POINT('Ctrl Pts',(-11.185681419954,8.14085014105599,10.1420240168744));
#111819=CARTESIAN_POINT('Ctrl Pts',(-11.196257080581,8.14184669301241,10.1568823329826));
#111820=CARTESIAN_POINT('Ctrl Pts',(-11.2001580144326,8.14221644543743,
10.1624445416375));
#111821=CARTESIAN_POINT('Ctrl Pts',(-11.2074602329449,8.1429127934953,10.1730123000309));
#111822=CARTESIAN_POINT('Ctrl Pts',(-11.2108694664639,8.14323968340398,
10.1780121614392));
#111823=CARTESIAN_POINT('Ctrl Pts',(-11.2185207157239,8.14397745451822,
10.1893841166433));
#111824=CARTESIAN_POINT('Ctrl Pts',(-11.2227439651303,8.1443876329496,10.1957686627912));
#111825=CARTESIAN_POINT('Ctrl Pts',(-11.2335185598191,8.14544200285631,
10.2123383587657));
#111826=CARTESIAN_POINT('Ctrl Pts',(-11.2399939978019,8.14608341516626,
10.2225723214083));
#111827=CARTESIAN_POINT('Ctrl Pts',(-11.2952233288456,8.15162576423719,
10.3123042197221));
#111828=CARTESIAN_POINT('Ctrl Pts',(-11.3364040862813,8.1562377396036,10.3962154728327));
#111829=CARTESIAN_POINT('Ctrl Pts',(-11.3929522896933,8.16405048275322,
10.5461289331736));
#111830=CARTESIAN_POINT('Ctrl Pts',(-11.4122546636138,8.16727864449445,
10.6103191919022));
#111831=CARTESIAN_POINT('Ctrl Pts',(-11.4371204585222,8.17287715935779,
10.7197091454464));
#111832=CARTESIAN_POINT('Ctrl Pts',(-11.445095468781,8.17518415094482,10.7642532307434));
#111833=CARTESIAN_POINT('Ctrl Pts',(-11.4519718849272,8.17799418340302,
10.816517030565));
#111834=CARTESIAN_POINT('Ctrl Pts',(-11.4528919258658,8.17839627902209,
10.8239505702295));
#111835=CARTESIAN_POINT('Ctrl Pts',(-11.4542182817031,8.17901902922728,
10.8353864523375));
#111836=CARTESIAN_POINT('Ctrl Pts',(-11.4546652366885,8.17923750220132,
10.8393840627548));
#111837=CARTESIAN_POINT('Ctrl Pts',(-11.4554574694855,8.17964127596287,
10.8467445510814));
#111838=CARTESIAN_POINT('Ctrl Pts',(-11.4558075812906,8.17982630837351,
10.8501068255927));
#111839=CARTESIAN_POINT('Ctrl Pts',(-11.4565732840387,8.18024638256619,
10.8577160337075));
#111840=CARTESIAN_POINT('Ctrl Pts',(-11.456981949444,8.18048179706565,10.8619635667941));
#111841=CARTESIAN_POINT('Ctrl Pts',(-11.457991136118,8.18109337132133,10.8729568465031));
#111842=CARTESIAN_POINT('Ctrl Pts',(-11.4585634121716,8.18147100624279,
10.8797050085364));
#111843=CARTESIAN_POINT('Ctrl Pts',(-11.4620084523365,8.18396193030654,
10.9239755428028));
#111844=CARTESIAN_POINT('Ctrl Pts',(-11.4634796431031,8.18614159399153,
10.9615901349345));
#111845=CARTESIAN_POINT('Ctrl Pts',(-11.4634997901997,8.18835865055823,
10.9992163638923));
#111846=CARTESIAN_POINT('Origin',(-10.,3.5,11.));
#111847=CARTESIAN_POINT('',(-11.463499918694,8.75942153140066,10.9995121649462));
#111848=CARTESIAN_POINT('',(-11.4634998917645,8.69060327775791,10.999437145398));
#111849=CARTESIAN_POINT('',(-11.4635,3.5,11.));
#111850=CARTESIAN_POINT('Ctrl Pts',(-11.463499918694,8.75942153142852,10.9995121654828));
#111851=CARTESIAN_POINT('Ctrl Pts',(-11.4634645275482,8.7539097792227,10.8933389916415));
#111852=CARTESIAN_POINT('Ctrl Pts',(-11.4518762295386,8.7487701525544,10.7874851722145));
#111853=CARTESIAN_POINT('Ctrl Pts',(-11.424673565895,8.74263898727559,10.66455019465));
#111854=CARTESIAN_POINT('Ctrl Pts',(-11.420022973337,8.74167703019694,10.6453789583251));
#111855=CARTESIAN_POINT('Ctrl Pts',(-11.397962437214,8.73744051653036,10.5618466969237));
#111856=CARTESIAN_POINT('Ctrl Pts',(-11.376555287381,8.73411808063943,10.4986309937983));
#111857=CARTESIAN_POINT('Ctrl Pts',(-11.3477832177277,8.7301398374855,10.4295799300859));
#111858=CARTESIAN_POINT('Ctrl Pts',(-11.3445861643966,8.72970318007339,
10.4220841768454));
#111859=CARTESIAN_POINT('Ctrl Pts',(-11.339641619479,8.72903530409525,10.4107544397738));
#111860=CARTESIAN_POINT('Ctrl Pts',(-11.3379398437821,8.7288067282174,10.4069005375074));
#111861=CARTESIAN_POINT('Ctrl Pts',(-11.3348439608678,8.72839310774722,
10.3999706211955));
#111862=CARTESIAN_POINT('Ctrl Pts',(-11.3334558227411,8.72820842187445,
10.3968920298181));
#111863=CARTESIAN_POINT('Ctrl Pts',(-11.3303728802607,8.7277999290969,10.3901174031773));
#111864=CARTESIAN_POINT('Ctrl Pts',(-11.3286733437485,8.72757584446508,
10.3864236581859));
#111865=CARTESIAN_POINT('Ctrl Pts',(-11.3237111364668,8.7269248490244,10.3757561730498));
#111866=CARTESIAN_POINT('Ctrl Pts',(-11.3204088482265,8.72649564029826,
10.3688011433907));
#111867=CARTESIAN_POINT('Ctrl Pts',(-11.2945049298553,8.72316119256339,
10.3153371990089));
#111868=CARTESIAN_POINT('Ctrl Pts',(-11.2695094234793,8.7201308743978,10.2700335770897));
#111869=CARTESIAN_POINT('Ctrl Pts',(-11.1836728604298,8.71046264502916,
10.132249657305));
#111870=CARTESIAN_POINT('Ctrl Pts',(-11.1147056682926,8.70371051829409,
10.0452707990669));
#111871=CARTESIAN_POINT('Ctrl Pts',(-11.0043714788515,8.69463654862207,
9.93456407498749));
#111872=CARTESIAN_POINT('Ctrl Pts',(-10.9706525422068,8.69204186986117,
9.90375638993865));
#111873=CARTESIAN_POINT('Ctrl Pts',(-10.92656438772,8.68886508652711,9.86710675957227));
#111874=CARTESIAN_POINT('Ctrl Pts',(-10.9174937233117,8.68822222501483,
9.85974830079362));
#111875=CARTESIAN_POINT('Ctrl Pts',(-10.9029172236286,8.6872058468382,9.84820987376814));
#111876=CARTESIAN_POINT('Ctrl Pts',(-10.8974683164818,8.68682954592883,
9.84395907044817));
#111877=CARTESIAN_POINT('Ctrl Pts',(-10.8872058189293,8.68612752081308,
9.83606937811493));
#111878=CARTESIAN_POINT('Ctrl Pts',(-10.882399453389,8.68580144492677,9.83242136716051));
#111879=CARTESIAN_POINT('Ctrl Pts',(-10.8715902641912,8.68507409828454,
9.82432210803123));
#111880=CARTESIAN_POINT('Ctrl Pts',(-10.8655756075879,8.6846734499943,9.81988688480623));
#111881=CARTESIAN_POINT('Ctrl Pts',(-10.8476633381812,8.68349208299602,
9.80688894942092));
#111882=CARTESIAN_POINT('Ctrl Pts',(-10.8356705749638,8.6827163850512,9.79845856316399));
#111883=CARTESIAN_POINT('Ctrl Pts',(-10.8080647874357,8.68096381244739,
9.7796661959884));
#111884=CARTESIAN_POINT('Ctrl Pts',(-10.792375247735,8.67999117228726,9.76942094941195));
#111885=CARTESIAN_POINT('Ctrl Pts',(-10.7391025221437,8.67676065057149,
9.73607535735618));
#111886=CARTESIAN_POINT('Ctrl Pts',(-10.7006716093015,8.67454848749691,
9.71437264049394));
#111887=CARTESIAN_POINT('Ctrl Pts',(-10.6073761881982,8.66937978291858,
9.66711493531825));
#111888=CARTESIAN_POINT('Ctrl Pts',(-10.5517930079899,8.66645752213874,
9.64316064526222));
#111889=CARTESIAN_POINT('Ctrl Pts',(-10.459204682147,8.66165810865766,9.60989173804095));
#111890=CARTESIAN_POINT('Ctrl Pts',(-10.4230380243323,8.65979872327951,
9.5984620732433));
#111891=CARTESIAN_POINT('Ctrl Pts',(-10.346209889185,8.65581063076442,9.57742721771588));
#111892=CARTESIAN_POINT('Ctrl Pts',(-10.3055000978816,8.65367548108785,
9.56813278545701));
#111893=CARTESIAN_POINT('Ctrl Pts',(-10.2576027004825,8.65108143748451,
9.55933293164266));
#111894=CARTESIAN_POINT('Ctrl Pts',(-10.2507441621798,8.6507080458886,9.55812340524114));
#111895=CARTESIAN_POINT('Ctrl Pts',(-10.2396134709692,8.65009854841575,
9.55624228667367));
#111896=CARTESIAN_POINT('Ctrl Pts',(-10.2353464377018,8.64986405625463,
9.55554058431793));
#111897=CARTESIAN_POINT('Ctrl Pts',(-10.2277354451056,8.64944420995398,
9.55432359620364));
#111898=CARTESIAN_POINT('Ctrl Pts',(-10.2243927366879,8.64925926588518,
9.55380098295991));
#111899=CARTESIAN_POINT('Ctrl Pts',(-10.217117541099,8.6488555289235,9.55268937887835));
#111900=CARTESIAN_POINT('Ctrl Pts',(-10.213184512234,8.64863650214689,9.55210482988563));
#111901=CARTESIAN_POINT('Ctrl Pts',(-10.202047230758,8.64801421336923,9.55049590640659));
#111902=CARTESIAN_POINT('Ctrl Pts',(-10.194837753614,8.64760894753207,9.54950923955838));
#111903=CARTESIAN_POINT('Ctrl Pts',(-10.147950227359,8.64495874586977,9.54344822333674));
#111904=CARTESIAN_POINT('Ctrl Pts',(-10.1080886437577,8.64263856303524,
9.5399490896912));
#111905=CARTESIAN_POINT('Ctrl Pts',(-9.9330302877212,8.63229477533152,9.53178989743308));
#111906=CARTESIAN_POINT('Ctrl Pts',(-9.7976714362682,8.6239721873824,9.54425322988476));
#111907=CARTESIAN_POINT('Ctrl Pts',(-9.63149742474595,8.61417310132988,
9.58321118057635));
#111908=CARTESIAN_POINT('Ctrl Pts',(-9.59734409446262,8.61217691934041,
9.59253659773072));
#111909=CARTESIAN_POINT('Ctrl Pts',(-9.55321637073037,8.6096206352293,9.60632353839052));
#111910=CARTESIAN_POINT('Ctrl Pts',(-9.54290848116356,8.60902512945052,
9.60967016745398));
#111911=CARTESIAN_POINT('Ctrl Pts',(-9.52632782856627,8.60806968051656,
9.61525768772911));
#111912=CARTESIAN_POINT('Ctrl Pts',(-9.52003165884168,8.6077074412124,9.61742740121706));
#111913=CARTESIAN_POINT('Ctrl Pts',(-9.50801729788666,8.60701724778018,
9.62165961443619));
#111914=CARTESIAN_POINT('Ctrl Pts',(-9.50229673064675,8.60668906680138,
9.62371490785453));
#111915=CARTESIAN_POINT('Ctrl Pts',(-9.48917570351211,8.60593729763585,
9.62852155631383));
#111916=CARTESIAN_POINT('Ctrl Pts',(-9.4817843349884,8.60551452008616,9.63129728895752));
#111917=CARTESIAN_POINT('Ctrl Pts',(-9.45871054150167,8.60419670738976,
9.64017606080606));
#111918=CARTESIAN_POINT('Ctrl Pts',(-9.44311039616428,8.60330863688758,
9.64648996193267));
#111919=CARTESIAN_POINT('Ctrl Pts',(-9.36597807694944,8.59892740871482,
9.67926737737361));
#111920=CARTESIAN_POINT('Ctrl Pts',(-9.30620202708779,8.59556799140007,
9.70966511812181));
#111921=CARTESIAN_POINT('Ctrl Pts',(-9.17590928168139,8.58809934648975,
9.78760408510831));
#111922=CARTESIAN_POINT('Ctrl Pts',(-9.10703267099872,8.58404576976513,
9.83740041902271));
#111923=CARTESIAN_POINT('Ctrl Pts',(-9.03133410730086,8.57906632795377,
9.90284424171761));
#111924=CARTESIAN_POINT('Ctrl Pts',(-9.01996519388132,8.57830278931688,
9.91298752133127));
#111925=CARTESIAN_POINT('Ctrl Pts',(-8.98422373513097,8.57584437164307,
9.94589239436067));
#111926=CARTESIAN_POINT('Ctrl Pts',(-8.96047134018448,8.57412224806746,
9.96930891478624));
#111927=CARTESIAN_POINT('Ctrl Pts',(-8.9326027672369,8.57196052948403,9.99872732981579));
#111928=CARTESIAN_POINT('Ctrl Pts',(-8.92770294745746,8.57157487518657,
10.0039764864715));
#111929=CARTESIAN_POINT('Ctrl Pts',(-8.92013457465902,8.57097002987649,
10.0122050270169));
#111930=CARTESIAN_POINT('Ctrl Pts',(-8.91743920539937,8.57075278395131,
10.0151597232456));
#111931=CARTESIAN_POINT('Ctrl Pts',(-8.91248749465034,8.57035018837538,
10.0206327381118));
#111932=CARTESIAN_POINT('Ctrl Pts',(-8.91022774100975,8.57016509627331,
10.0231478587674));
#111933=CARTESIAN_POINT('Ctrl Pts',(-8.90511818447828,8.56974348170336,
10.0288746240597));
#111934=CARTESIAN_POINT('Ctrl Pts',(-8.90227379997858,8.56950657379071,
10.0320909781475));
#111935=CARTESIAN_POINT('Ctrl Pts',(-8.89363111960035,8.56878009373786,
10.041950988129));
#111936=CARTESIAN_POINT('Ctrl Pts',(-8.88787878689673,8.56828735978756,
10.0486344507625));
#111937=CARTESIAN_POINT('Ctrl Pts',(-8.8359803371556,8.56376029228534,10.1100475986001));
#111938=CARTESIAN_POINT('Ctrl Pts',(-8.793851786785,8.5594940833683,10.1680375262622));
#111939=CARTESIAN_POINT('Ctrl Pts',(-8.68933273635898,8.54757483415237,
10.3366305482554));
#111940=CARTESIAN_POINT('Ctrl Pts',(-8.63679972996406,8.53994854839546,
10.4526389604042));
#111941=CARTESIAN_POINT('Ctrl Pts',(-8.59553948283946,8.53202519140167,
10.5882414297746));
#111942=CARTESIAN_POINT('Ctrl Pts',(-8.59141818716706,8.53119879538267,
10.6025685418436));
#111943=CARTESIAN_POINT('Ctrl Pts',(-8.58552204214379,8.52996054929503,
10.6243107414081));
#111944=CARTESIAN_POINT('Ctrl Pts',(-8.58358512804274,8.52954355706952,
10.6316805383285));
#111945=CARTESIAN_POINT('Ctrl Pts',(-8.58031135743822,8.52882034294646,
10.6445448287062));
#111946=CARTESIAN_POINT('Ctrl Pts',(-8.57894863414682,8.52851330264368,
10.6500325194125));
#111947=CARTESIAN_POINT('Ctrl Pts',(-8.57616220270509,8.52787258180239,
10.6615381597554));
#111948=CARTESIAN_POINT('Ctrl Pts',(-8.57474476286851,8.52753910581542,
10.6675575223498));
#111949=CARTESIAN_POINT('Ctrl Pts',(-8.57145747762567,8.52674716933416,
10.6819250156971));
#111950=CARTESIAN_POINT('Ctrl Pts',(-8.5696225824573,8.52628982156482,10.6902809637171));
#111951=CARTESIAN_POINT('Ctrl Pts',(-8.56361987565763,8.52473905068696,
10.7188085418899));
#111952=CARTESIAN_POINT('Ctrl Pts',(-8.55980457331678,8.5236566875341,10.7390523315748));
#111953=CARTESIAN_POINT('Ctrl Pts',(-8.5516406190662,8.52107693928109,10.7880294705139));
#111954=CARTESIAN_POINT('Ctrl Pts',(-8.54771781973208,8.51959226277391,
10.8168252173628));
#111955=CARTESIAN_POINT('Ctrl Pts',(-8.53550746959374,8.51375183287342,
10.9320070792431));
#111956=CARTESIAN_POINT('Ctrl Pts',(-8.5340520787472,8.50957427623218,11.0189397496178));
#111957=CARTESIAN_POINT('Ctrl Pts',(-8.54318437368548,8.50339092607835,
11.1453077892593));
#111958=CARTESIAN_POINT('Ctrl Pts',(-8.5476900963463,8.50143076917602,11.184991427442));
#111959=CARTESIAN_POINT('Ctrl Pts',(-8.55973626669931,8.49748335768654,
11.2626115467538));
#111960=CARTESIAN_POINT('Ctrl Pts',(-8.5671688783992,8.49550048777836,11.3005311169988));
#111961=CARTESIAN_POINT('Ctrl Pts',(-8.57766734553885,8.49307868112752,
11.3447442194711));
#111962=CARTESIAN_POINT('Ctrl Pts',(-8.57928918803116,8.4927129115927,11.3513681004539));
#111963=CARTESIAN_POINT('Ctrl Pts',(-8.58200434492857,8.49211343510491,
11.3621310502496));
#111964=CARTESIAN_POINT('Ctrl Pts',(-8.58306964897397,8.49188125608041,
11.3662771556589));
#111965=CARTESIAN_POINT('Ctrl Pts',(-8.58500871798621,8.49146387387452,
11.3736888400467));
#111966=CARTESIAN_POINT('Ctrl Pts',(-8.5858756235123,8.49127906075411,11.3769561311992));
#111967=CARTESIAN_POINT('Ctrl Pts',(-8.58779552984267,8.49087359821258,
11.3840922551675));
#111968=CARTESIAN_POINT('Ctrl Pts',(-8.58885309810562,8.49065269854811,
11.3879597227804));
#111969=CARTESIAN_POINT('Ctrl Pts',(-8.59191632878156,8.49001984124107,
11.3989835347516));
#111970=CARTESIAN_POINT('Ctrl Pts',(-8.59396060117968,8.48960577365943,
11.4061289085963));
#111971=CARTESIAN_POINT('Ctrl Pts',(-8.60840690439978,8.48673660581106,
11.4552065862102));
#111972=CARTESIAN_POINT('Ctrl Pts',(-8.62262749217222,8.48419169860697,
11.4965769690411));
#111973=CARTESIAN_POINT('Ctrl Pts',(-8.66343975569986,8.47760848871175,
11.5999910366419));
#111974=CARTESIAN_POINT('Ctrl Pts',(-8.69251057751328,8.47352015796154,
11.660949141893));
#111975=CARTESIAN_POINT('Ctrl Pts',(-8.77214635913729,8.46381277417161,
11.8019573239089));
#111976=CARTESIAN_POINT('Ctrl Pts',(-8.82647537672002,8.45827132665699,
11.8795482874018));
#111977=CARTESIAN_POINT('Ctrl Pts',(-8.89574091556883,8.45234895522086,
11.9605149796252));
#111978=CARTESIAN_POINT('Ctrl Pts',(-8.90367877331684,8.451684430649,11.969565331303));
#111979=CARTESIAN_POINT('Ctrl Pts',(-8.91683029716929,8.45060607136661,
11.9841919982478));
#111980=CARTESIAN_POINT('Ctrl Pts',(-8.92197741353878,8.4501895223523,11.9898271569818));
#111981=CARTESIAN_POINT('Ctrl Pts',(-8.93128184269887,8.44944619543235,
11.9998551516512));
#111982=CARTESIAN_POINT('Ctrl Pts',(-8.93542272355338,8.44911874006213,
12.00426293769));
#111983=CARTESIAN_POINT('Ctrl Pts',(-8.94428046264766,8.44842530881467,
12.0135752604602));
#111984=CARTESIAN_POINT('Ctrl Pts',(-8.94900445413408,8.44805964805249,
12.0184728346226));
#111985=CARTESIAN_POINT('Ctrl Pts',(-8.96180266271756,8.44707997746438,
12.031557440636));
#111986=CARTESIAN_POINT('Ctrl Pts',(-8.96993958117814,8.44646868786663,
12.0396826477542));
#111987=CARTESIAN_POINT('Ctrl Pts',(-9.01237064662943,8.4433385336215,12.0810654887214));
#111988=CARTESIAN_POINT('Ctrl Pts',(-9.04818404919093,8.44088818762806,
12.1127269721376));
#111989=CARTESIAN_POINT('Ctrl Pts',(-9.17052104284699,8.43301799221599,
12.2106447059713));
#111990=CARTESIAN_POINT('Ctrl Pts',(-9.26288470198069,8.42786045935254,
12.2689979882786));
#111991=CARTESIAN_POINT('Ctrl Pts',(-9.37312311800238,8.4217848698338,12.3225140059866));
#111992=CARTESIAN_POINT('Ctrl Pts',(-9.38546347127225,8.42110536400519,
12.3282931767602));
#111993=CARTESIAN_POINT('Ctrl Pts',(-9.43297757838394,8.41848519175475,
12.3497408826223));
#111994=CARTESIAN_POINT('Ctrl Pts',(-9.46868151078588,8.4165084090986,12.3641902628457));
#111995=CARTESIAN_POINT('Ctrl Pts',(-9.51132188528475,8.41409350415803,
12.3795188900771));
#111996=CARTESIAN_POINT('Ctrl Pts',(-9.51774915736539,8.41372807801219,
12.3817788495704));
#111997=CARTESIAN_POINT('Ctrl Pts',(-9.52823824234789,8.41312905327127,
12.3853849293675));
#111998=CARTESIAN_POINT('Ctrl Pts',(-9.53229066266431,8.41289697878885,
12.3867582822295));
#111999=CARTESIAN_POINT('Ctrl Pts',(-9.53955518947212,8.41247970708643,
12.3891847440151));
#112000=CARTESIAN_POINT('Ctrl Pts',(-9.54276498582242,8.4122948990213,12.3902445173527));
#112001=CARTESIAN_POINT('Ctrl Pts',(-9.5497916244935,8.41188935463937,12.3925375244892));
#112002=CARTESIAN_POINT('Ctrl Pts',(-9.55360982436096,8.41166836731739,
12.3937661743609));
#112003=CARTESIAN_POINT('Ctrl Pts',(-9.5645240726853,8.41103501365744,12.3972287971112));
#112004=CARTESIAN_POINT('Ctrl Pts',(-9.57163206604343,8.41062053233552,
12.399424347069));
#112005=CARTESIAN_POINT('Ctrl Pts',(-9.62081453727068,8.40774030186502,
12.4142062488135));
#112006=CARTESIAN_POINT('Ctrl Pts',(-9.66341692522347,8.40518397546698,
12.4249463454607));
#112007=CARTESIAN_POINT('Ctrl Pts',(-9.77236999823677,8.39859753151287,
12.4472548923081));
#112008=CARTESIAN_POINT('Ctrl Pts',(-9.83915822434291,8.39451845795667,
12.4561908859409));
#112009=CARTESIAN_POINT('Ctrl Pts',(-10.000582601754,8.38482236978086,12.4665446649694));
#112010=CARTESIAN_POINT('Ctrl Pts',(-10.0952179730144,8.37928314627308,
12.463452167005));
#112011=CARTESIAN_POINT('Ctrl Pts',(-10.2008361147505,8.37336325744281,
12.4497040413589));
#112012=CARTESIAN_POINT('Ctrl Pts',(-10.2127453585057,8.37269919835224,
12.4480042738326));
#112013=CARTESIAN_POINT('Ctrl Pts',(-10.2321714549076,8.3716214388082,12.4449868068446));
#112014=CARTESIAN_POINT('Ctrl Pts',(-10.2397011873949,8.37120502908746,
12.4437568355721));
#112015=CARTESIAN_POINT('Ctrl Pts',(-10.2531815499531,8.3704618556033,12.4414464692778));
#112016=CARTESIAN_POINT('Ctrl Pts',(-10.2591357126286,8.37013441548307,
12.4403879703003));
#112017=CARTESIAN_POINT('Ctrl Pts',(-10.2717766007379,8.36944091783668,
12.4380598216107));
#112018=CARTESIAN_POINT('Ctrl Pts',(-10.2784613898385,8.36907517618777,
12.4367803686507));
#112019=CARTESIAN_POINT('Ctrl Pts',(-10.2964221329984,8.36809505114387,
12.4332126661064));
#112020=CARTESIAN_POINT('Ctrl Pts',(-10.3076805546494,8.36748339243936,
12.4308379759849));
#112021=CARTESIAN_POINT('Ctrl Pts',(-10.3656314240511,8.3643475954843,12.4178990167684));
#112022=CARTESIAN_POINT('Ctrl Pts',(-10.4118152629097,8.36189228354789,
12.405180679042));
#112023=CARTESIAN_POINT('Ctrl Pts',(-10.5612856545771,8.35399017970294,
12.3560142284773));
#112024=CARTESIAN_POINT('Ctrl Pts',(-10.6611032508813,8.34880873799466,
12.3102509300205));
#112025=CARTESIAN_POINT('Ctrl Pts',(-10.7982722729033,8.34086582861755,
12.2276639197434));
#112026=CARTESIAN_POINT('Ctrl Pts',(-10.8402721890174,8.3383000840131,12.199307720493));
#112027=CARTESIAN_POINT('Ctrl Pts',(-10.8865144077847,8.33521910481808,
12.1644643423327));
#112028=CARTESIAN_POINT('Ctrl Pts',(-10.8922822468455,8.3348300159793,12.1600505969529));
#112029=CARTESIAN_POINT('Ctrl Pts',(-10.9014645336381,8.33420245421187,
12.1529150050947));
#112030=CARTESIAN_POINT('Ctrl Pts',(-10.9049001379506,8.33396580034421,
12.1502204370135));
#112031=CARTESIAN_POINT('Ctrl Pts',(-10.9109848700419,8.33354326999398,
12.1454040058389));
#112032=CARTESIAN_POINT('Ctrl Pts',(-10.9136387384782,8.33335781984476,
12.1432882512257));
#112033=CARTESIAN_POINT('Ctrl Pts',(-10.9192634509966,8.33296226109526,
12.1387719462071));
#112034=CARTESIAN_POINT('Ctrl Pts',(-10.9222322176447,8.33275199231582,
12.1363690306685));
#112035=CARTESIAN_POINT('Ctrl Pts',(-10.9301909097327,8.33218436319737,
12.129875547887));
#112036=CARTESIAN_POINT('Ctrl Pts',(-10.9351631871454,8.33182553746506,
12.1257636042037));
#112037=CARTESIAN_POINT('Ctrl Pts',(-10.9463256713037,8.33101079807887,
12.1164075386335));
#112038=CARTESIAN_POINT('Ctrl Pts',(-10.9524997501412,8.33055368163332,
12.1111445849858));
#112039=CARTESIAN_POINT('Ctrl Pts',(-10.9715355772675,8.32912491986422,
12.0946426847807));
#112040=CARTESIAN_POINT('Ctrl Pts',(-10.9842442021166,8.32814319113209,
12.0832300266417));
#112041=CARTESIAN_POINT('Ctrl Pts',(-11.034821319519,8.32413184947629,12.0361855906138));
#112042=CARTESIAN_POINT('Ctrl Pts',(-11.0709767243198,8.32102267512462,
11.9987712485533));
#112043=CARTESIAN_POINT('Ctrl Pts',(-11.1866316464764,8.31041879568386,
11.8655727777863));
#112044=CARTESIAN_POINT('Ctrl Pts',(-11.255904920208,8.30294436957543,11.761593375002));
#112045=CARTESIAN_POINT('Ctrl Pts',(-11.3185780423716,8.29505336459114,
11.6351857395331));
#112046=CARTESIAN_POINT('Ctrl Pts',(-11.3257129526795,8.29413158759976,
11.6201565742105));
#112047=CARTESIAN_POINT('Ctrl Pts',(-11.3358524524978,8.29278540924576,
11.597823338936));
#112048=CARTESIAN_POINT('Ctrl Pts',(-11.3390564961231,8.29235428198561,
11.5906117362635));
#112049=CARTESIAN_POINT('Ctrl Pts',(-11.3446323849648,8.29159355364524,
11.577782978621));
#112050=CARTESIAN_POINT('Ctrl Pts',(-11.3470277310445,8.29126316703562,
11.5721762966359));
#112051=CARTESIAN_POINT('Ctrl Pts',(-11.3519423797732,8.29057766076519,
11.5604708648192));
#112052=CARTESIAN_POINT('Ctrl Pts',(-11.3544556168449,8.29022274987878,
11.5543697073983));
#112053=CARTESIAN_POINT('Ctrl Pts',(-11.360882939792,8.28930347228406,11.5384620292281));
#112054=CARTESIAN_POINT('Ctrl Pts',(-11.3647323538104,8.28874125958458,
11.5286296841599));
#112055=CARTESIAN_POINT('Ctrl Pts',(-11.3813930067757,8.28625373868709,
11.4846790165273));
#112056=CARTESIAN_POINT('Ctrl Pts',(-11.3930341311937,8.28436689972388,
11.4501295124212));
#112057=CARTESIAN_POINT('Ctrl Pts',(-11.4219653224671,8.27918083089114,
11.3523373889305));
#112058=CARTESIAN_POINT('Ctrl Pts',(-11.4363155392342,8.2759652270832,11.2883148596826));
#112059=CARTESIAN_POINT('Ctrl Pts',(-11.457802347785,8.26911157271654,11.1492952597736));
#112060=CARTESIAN_POINT('Ctrl Pts',(-11.4635427146042,8.26549102312458,
11.0742800636214));
#112061=CARTESIAN_POINT('Ctrl Pts',(-11.4634997607281,8.26169280151533,
10.999163131591));
#112062=CARTESIAN_POINT('Ctrl Pts',(-11.4634997901997,8.18835865055823,
10.9992163638923));
#112063=CARTESIAN_POINT('Ctrl Pts',(-11.463562176983,8.19522390914069,11.1157284074538));
#112064=CARTESIAN_POINT('Ctrl Pts',(-11.4497117361902,8.20237636626697,
11.2318341407186));
#112065=CARTESIAN_POINT('Ctrl Pts',(-11.4096862102963,8.21230185552391,
11.39679931889));
#112066=CARTESIAN_POINT('Ctrl Pts',(-11.3943238830279,8.21534323336146,
11.4478021977668));
#112067=CARTESIAN_POINT('Ctrl Pts',(-11.3720654063134,8.21897268514177,
11.5093305192923));
#112068=CARTESIAN_POINT('Ctrl Pts',(-11.3677722757196,8.21964466356928,
11.5207495285298));
#112069=CARTESIAN_POINT('Ctrl Pts',(-11.360780640102,8.22069650232875,11.538662904316));
#112070=CARTESIAN_POINT('Ctrl Pts',(-11.3581773106712,8.22107948369976,
11.5451936079406));
#112071=CARTESIAN_POINT('Ctrl Pts',(-11.3532767418419,8.22178474860526,
11.5572341889608));
#112072=CARTESIAN_POINT('Ctrl Pts',(-11.3509926653047,8.2221074611636,11.562749234654));
#112073=CARTESIAN_POINT('Ctrl Pts',(-11.3458410310021,8.22282224999222,
11.5749760314164));
#112074=CARTESIAN_POINT('Ctrl Pts',(-11.3429568685593,8.22321376091015,
11.5816806419672));
#112075=CARTESIAN_POINT('Ctrl Pts',(-11.3344743946778,8.22434077497162,
11.6009998339117));
#112076=CARTESIAN_POINT('Ctrl Pts',(-11.3287475729203,8.22507194387926,
11.6135573444699));
#112077=CARTESIAN_POINT('Ctrl Pts',(-11.2800791318426,8.23105247205133,
11.7163966898957));
#112078=CARTESIAN_POINT('Ctrl Pts',(-11.228167345611,8.2359669039415,11.8021437964628));
#112079=CARTESIAN_POINT('Ctrl Pts',(-11.1083926811965,8.24564408637833,
11.9607565766766));
#112080=CARTESIAN_POINT('Ctrl Pts',(-11.0410534883211,8.25039133919379,
12.0333394305755));
#112081=CARTESIAN_POINT('Ctrl Pts',(-10.9584658386875,8.25619015764342,
12.1060301294569));
#112082=CARTESIAN_POINT('Ctrl Pts',(-10.9499154741651,8.25679042162266,
12.1133822290202));
#112083=CARTESIAN_POINT('Ctrl Pts',(-10.9379072203726,8.25763467491169,
12.1234686074574));
#112084=CARTESIAN_POINT('Ctrl Pts',(-10.9345204373518,8.25787292059347,
12.1262873599288));
#112085=CARTESIAN_POINT('Ctrl Pts',(-10.9286638060807,8.25828524076763,
12.1311171156803));
#112086=CARTESIAN_POINT('Ctrl Pts',(-10.9262000072615,8.25845879789903,
12.133135446564));
#112087=CARTESIAN_POINT('Ctrl Pts',(-10.9210119189915,8.25882451794363,
12.1373572755665));
#112088=CARTESIAN_POINT('Ctrl Pts',(-10.9182862861381,8.25901680444896,
12.1395590476643));
#112089=CARTESIAN_POINT('Ctrl Pts',(-10.9115685529625,8.25949103760501,
12.1449458961435));
#112090=CARTESIAN_POINT('Ctrl Pts',(-10.9075676555381,8.25977374798341,
12.1481198895938));
#112091=CARTESIAN_POINT('Ctrl Pts',(-10.8928582358072,8.2608138665798,12.1596642430399));
#112092=CARTESIAN_POINT('Ctrl Pts',(-10.8820501864745,8.26157950947296,
12.1679060010974));
#112093=CARTESIAN_POINT('Ctrl Pts',(-10.8545735010986,8.26352613895776,
12.1882596009126));
#112094=CARTESIAN_POINT('Ctrl Pts',(-10.8377612465624,8.26471737506758,
12.2001719740388));
#112095=CARTESIAN_POINT('Ctrl Pts',(-10.7031531968749,8.27422206780122,
12.2913422966162));
#112096=CARTESIAN_POINT('Ctrl Pts',(-10.5746373240541,8.28300562613413,
12.3534369125592));
#112097=CARTESIAN_POINT('Ctrl Pts',(-10.4027751988324,8.29338230351841,
12.4075013684091));
#112098=CARTESIAN_POINT('Ctrl Pts',(-10.3659439172829,8.29553907304429,
12.4175236811612));
#112099=CARTESIAN_POINT('Ctrl Pts',(-10.3179065967355,8.29826669381606,
12.4285978136565));
#112100=CARTESIAN_POINT('Ctrl Pts',(-10.3070243083436,8.29887907489796,
12.4309760309346));
#112101=CARTESIAN_POINT('Ctrl Pts',(-10.2895281082568,8.299854989207,12.4345908732206));
#112102=CARTESIAN_POINT('Ctrl Pts',(-10.2829311226114,8.30022099846868,
12.435906501467));
#112103=CARTESIAN_POINT('Ctrl Pts',(-10.270370021301,8.30091424755945,12.4383216180819));
#112104=CARTESIAN_POINT('Ctrl Pts',(-10.2644077001493,8.30124174817484,
12.4394296075473));
#112105=CARTESIAN_POINT('Ctrl Pts',(-10.2507899146828,8.30198626506028,
12.4418727593506));
#112106=CARTESIAN_POINT('Ctrl Pts',(-10.2431303226611,8.30240252684143,
12.4431840786317));
#112107=CARTESIAN_POINT('Ctrl Pts',(-10.2195064211466,8.30367889658653,
12.4470350648738));
#112108=CARTESIAN_POINT('Ctrl Pts',(-10.2035099122834,8.30453266646097,
12.4493713432527));
#112109=CARTESIAN_POINT('Ctrl Pts',(-10.1261403632141,8.30861562517538,
12.4593648887214));
#112110=CARTESIAN_POINT('Ctrl Pts',(-10.0643596302101,8.31173185163661,
12.4633920100475));
#112111=CARTESIAN_POINT('Ctrl Pts',(-9.918477662454,8.31893520389298,12.4636416443699));
#112112=CARTESIAN_POINT('Ctrl Pts',(-9.83459757347256,8.32295253376796,
12.4565487374624));
#112113=CARTESIAN_POINT('Ctrl Pts',(-9.74122250894853,8.32763874461858,
12.4404795969636));
#112114=CARTESIAN_POINT('Ctrl Pts',(-9.73067407503415,8.32817142762926,
12.4385446811681));
#112115=CARTESIAN_POINT('Ctrl Pts',(-9.71157210276106,8.32914344959219,
12.4348233115218));
#112116=CARTESIAN_POINT('Ctrl Pts',(-9.70301144970894,8.32958177792835,
12.4330758474191));
#112117=CARTESIAN_POINT('Ctrl Pts',(-9.65944023974028,8.33182879178962,
12.4237745915845));
#112118=CARTESIAN_POINT('Ctrl Pts',(-9.62470225268755,8.33367315287845,
12.4150145775189));
#112119=CARTESIAN_POINT('Ctrl Pts',(-9.58390735404576,8.33593891492404,
12.4031193192117));
#112120=CARTESIAN_POINT('Ctrl Pts',(-9.57750444057204,8.33629749863851,
12.4012046291961));
#112121=CARTESIAN_POINT('Ctrl Pts',(-9.56706103386334,8.33688755007849,
12.3980036051969));
#112122=CARTESIAN_POINT('Ctrl Pts',(-9.56301255218311,8.33711756914424,
12.3967434260017));
#112123=CARTESIAN_POINT('Ctrl Pts',(-9.55574757338747,8.33753273440914,
12.3944473637416));
#112124=CARTESIAN_POINT('Ctrl Pts',(-9.55252912755954,8.33771750966202,
12.3934179153244));
#112125=CARTESIAN_POINT('Ctrl Pts',(-9.54546591729748,8.33812491098005,
12.3911316899335));
#112126=CARTESIAN_POINT('Ctrl Pts',(-9.54162283435333,8.33834780413354,
12.3898701321644));
#112127=CARTESIAN_POINT('Ctrl Pts',(-9.53057813562716,8.33899181337655,
12.3861937304018));
#112128=CARTESIAN_POINT('Ctrl Pts',(-9.52339013399067,8.33941515340762,
12.3837387670904));
#112129=CARTESIAN_POINT('Ctrl Pts',(-9.47065945070101,8.34255010725833,
12.3652697246244));
#112130=CARTESIAN_POINT('Ctrl Pts',(-9.42591864636378,8.34537094457319,
12.3470681432332));
#112131=CARTESIAN_POINT('Ctrl Pts',(-9.28743164844201,8.35444848510096,
12.2825751226901));
#112132=CARTESIAN_POINT('Ctrl Pts',(-9.19768719878795,8.36083040119204,
12.2284338519659));
#112133=CARTESIAN_POINT('Ctrl Pts',(-9.07125969917215,8.37012405691028,
12.1323515430637));
#112134=CARTESIAN_POINT('Ctrl Pts',(-9.02990098642693,8.37322814999408,
12.0971269358041));
#112135=CARTESIAN_POINT('Ctrl Pts',(-8.98170315222449,8.37692108965572,
12.0512157060119));
#112136=CARTESIAN_POINT('Ctrl Pts',(-8.97292168402498,8.37759736335255,
12.0426375575669));
#112137=CARTESIAN_POINT('Ctrl Pts',(-8.95926988267405,8.37865441621118,
12.0289619732202));
#112138=CARTESIAN_POINT('Ctrl Pts',(-8.95432681173402,8.37903836753157,
12.0239382330984));
#112139=CARTESIAN_POINT('Ctrl Pts',(-8.94526500986915,8.37974456752219,
12.0145944866072));
#112140=CARTESIAN_POINT('Ctrl Pts',(-8.94113606408313,8.38006725324379,
12.010284632333));
#112141=CARTESIAN_POINT('Ctrl Pts',(-8.93203074039279,8.38078095161214,
12.00066322229));
#112142=CARTESIAN_POINT('Ctrl Pts',(-8.92706737009981,8.38117140788808,
11.9953395391533));
#112143=CARTESIAN_POINT('Ctrl Pts',(-8.91287388596501,8.38229226165493,
11.9798861464303));
#112144=CARTESIAN_POINT('Ctrl Pts',(-8.90374593510384,8.38301839943941,
11.9696633899011));
#112145=CARTESIAN_POINT('Ctrl Pts',(-8.88348400140476,8.38464353665294,
11.9463193630138));
#112146=CARTESIAN_POINT('Ctrl Pts',(-8.87243506350122,8.38553915442498,
11.9331268170073));
#112147=CARTESIAN_POINT('Ctrl Pts',(-8.83717687216577,8.38843257250811,
11.8894872126356));
#112148=CARTESIAN_POINT('Ctrl Pts',(-8.81394755580074,8.39039508931698,
11.8582686077251));
#112149=CARTESIAN_POINT('Ctrl Pts',(-8.75483124242427,8.39560168227607,
11.7718287247594));
#112150=CARTESIAN_POINT('Ctrl Pts',(-8.72138094557179,8.39878394954023,
11.7150513210164));
#112151=CARTESIAN_POINT('Ctrl Pts',(-8.6578475993725,8.40569034572719,11.5884005855447));
#112152=CARTESIAN_POINT('Ctrl Pts',(-8.62915728630368,8.4094131487917,11.5180503153088));
#112153=CARTESIAN_POINT('Ctrl Pts',(-8.60239269459035,8.41403591243409,
11.434361993951));
#112154=CARTESIAN_POINT('Ctrl Pts',(-8.59887497432264,8.41467448943625,
11.4228772470598));
#112155=CARTESIAN_POINT('Ctrl Pts',(-8.59423141433422,8.41556340900609,
11.4070224513203));
#112156=CARTESIAN_POINT('Ctrl Pts',(-8.59298373682327,8.41580716332854,
11.4026882496474));
#112157=CARTESIAN_POINT('Ctrl Pts',(-8.59088176990448,8.41622646720787,
11.3952573625843));
#112158=CARTESIAN_POINT('Ctrl Pts',(-8.59001759751947,8.41640145847003,
11.3921634778409));
#112159=CARTESIAN_POINT('Ctrl Pts',(-8.58823867421885,8.41676721976179,
11.3857127355157));
#112160=CARTESIAN_POINT('Ctrl Pts',(-8.58732570349959,8.41695809409093,
11.3823554451862));
#112161=CARTESIAN_POINT('Ctrl Pts',(-8.58513485538112,8.41742386728659,
11.374184021141));
#112162=CARTESIAN_POINT('Ctrl Pts',(-8.58386957152157,8.4176994701222,11.369366575636));
#112163=CARTESIAN_POINT('Ctrl Pts',(-8.57945234513414,8.41868535991822,
11.352192053796));
#112164=CARTESIAN_POINT('Ctrl Pts',(-8.57643744559754,8.41940282799774,
11.3398006970764));
#112165=CARTESIAN_POINT('Ctrl Pts',(-8.5693542941181,8.42120232351498,11.3089382077662));
#112166=CARTESIAN_POINT('Ctrl Pts',(-8.56548152298121,8.42229283646565,
11.2904249157429));
#112167=CARTESIAN_POINT('Ctrl Pts',(-8.55048718137838,8.42699770160501,
11.2111057325332));
#112168=CARTESIAN_POINT('Ctrl Pts',(-8.5428656041567,8.43071830912486,11.1497053130997));
#112169=CARTESIAN_POINT('Ctrl Pts',(-8.53256757248105,8.44102364854368,
10.9787721750978));
#112170=CARTESIAN_POINT('Ctrl Pts',(-8.53825888193278,8.44754627336864,
10.8691229507904));
#112171=CARTESIAN_POINT('Ctrl Pts',(-8.55909429964202,8.45470107695163,
10.7431858780285));
#112172=CARTESIAN_POINT('Ctrl Pts',(-8.56239558403761,8.4557098040965,10.7253068705239));
#112173=CARTESIAN_POINT('Ctrl Pts',(-8.56763923514614,8.45715048896585,
10.6996006365608));
#112174=CARTESIAN_POINT('Ctrl Pts',(-8.5693143942948,8.45759077448299,10.6917211659979));
#112175=CARTESIAN_POINT('Ctrl Pts',(-8.57237748821839,8.4583621761024,10.6778762358917));
#112176=CARTESIAN_POINT('Ctrl Pts',(-8.57373796234022,8.4586941497333,10.6719049572823));
#112177=CARTESIAN_POINT('Ctrl Pts',(-8.57662675765324,8.45937772342641,
10.6595833100554));
#112178=CARTESIAN_POINT('Ctrl Pts',(-8.57816019122485,8.45972915311864,
10.6532342723218));
#112179=CARTESIAN_POINT('Ctrl Pts',(-8.58220822696148,8.46062844584909,
10.6369521763666));
#112180=CARTESIAN_POINT('Ctrl Pts',(-8.58478475510275,8.461174332051,10.6270347849095));
#112181=CARTESIAN_POINT('Ctrl Pts',(-8.59619338664465,8.46348403823252,
10.5849428900107));
#112182=CARTESIAN_POINT('Ctrl Pts',(-8.60602050944094,8.4652160283151,10.5530471936992));
#112183=CARTESIAN_POINT('Ctrl Pts',(-8.63559091441868,8.46983263671981,
10.4675736158474));
#112184=CARTESIAN_POINT('Ctrl Pts',(-8.65739228966893,8.47265600593214,
10.4147691279232));
#112185=CARTESIAN_POINT('Ctrl Pts',(-8.68810554025373,8.47610873656122,
10.3511949257709));
#112186=CARTESIAN_POINT('Ctrl Pts',(-8.6941562196692,8.47676817976188,10.3391012765721));
#112187=CARTESIAN_POINT('Ctrl Pts',(-8.74704930390492,8.48237143623563,
10.2369456108601));
#112188=CARTESIAN_POINT('Ctrl Pts',(-8.80297191492606,8.48723905629371,
10.1519103500392));
#112189=CARTESIAN_POINT('Ctrl Pts',(-8.87424920774173,8.49317529330558,
10.0647779735337));
#112190=CARTESIAN_POINT('Ctrl Pts',(-8.8813637016999,8.49376546994874,10.0562797540171));
#112191=CARTESIAN_POINT('Ctrl Pts',(-8.89141926482071,8.49459769134213,
10.0445419253335));
#112192=CARTESIAN_POINT('Ctrl Pts',(-8.89427955371946,8.49483420287198,
10.0412332543581));
#112193=CARTESIAN_POINT('Ctrl Pts',(-8.89924277938828,8.49524433590839,
10.0355437377081));
#112194=CARTESIAN_POINT('Ctrl Pts',(-8.90133873271033,8.49541745279741,
10.0331568069406));
#112195=CARTESIAN_POINT('Ctrl Pts',(-8.90576866600101,8.49578322306104,
10.0281448792033));
#112196=CARTESIAN_POINT('Ctrl Pts',(-8.90810434288859,8.49597600634569,
10.0255214413081));
#112197=CARTESIAN_POINT('Ctrl Pts',(-8.91388786799984,8.49645314536408,
10.0190722703125));
#112198=CARTESIAN_POINT('Ctrl Pts',(-8.91734649212379,8.49673828541715,
10.0152563001443));
#112199=CARTESIAN_POINT('Ctrl Pts',(-8.93020617326974,8.49779749216929,
10.0012175897373));
#112200=CARTESIAN_POINT('Ctrl Pts',(-8.93973217576496,8.49858018230051,
9.9911108847064));
#112201=CARTESIAN_POINT('Ctrl Pts',(-9.00842112069237,8.50420047997656,
9.92028200770669));
#112202=CARTESIAN_POINT('Ctrl Pts',(-9.07261441785144,8.50932226641417,
9.86467027633959));
#112203=CARTESIAN_POINT('Ctrl Pts',(-9.22506057525428,8.52064845337834,
9.75420196556883));
#112204=CARTESIAN_POINT('Ctrl Pts',(-9.31508499756035,8.5267964393579,9.70252493029985));
#112205=CARTESIAN_POINT('Ctrl Pts',(-9.42669382011882,8.53363554491536,
9.65334033319139));
#112206=CARTESIAN_POINT('Ctrl Pts',(-9.4437062420526,8.53465896492501,9.64622397259552));
#112207=CARTESIAN_POINT('Ctrl Pts',(-9.46770226104454,8.5360765536621,9.63671510430525));
#112208=CARTESIAN_POINT('Ctrl Pts',(-9.47457585952681,8.53647968316121,
9.63405122163799));
#112209=CARTESIAN_POINT('Ctrl Pts',(-9.48722583358488,8.53721629621282,
9.62925830369983));
#112210=CARTESIAN_POINT('Ctrl Pts',(-9.49299604931491,8.53755029211606,
9.62711357377558));
#112211=CARTESIAN_POINT('Ctrl Pts',(-9.50474689335524,8.538226456425,9.62283009421822));
#112212=CARTESIAN_POINT('Ctrl Pts',(-9.51072825894231,8.53856854035256,
9.62069374170399));
#112213=CARTESIAN_POINT('Ctrl Pts',(-9.52559761667235,8.53941385349291,
9.61549177727954));
#112214=CARTESIAN_POINT('Ctrl Pts',(-9.53450166937893,8.53991555610423,
9.61247272106114));
#112215=CARTESIAN_POINT('Ctrl Pts',(-9.56843106685285,8.54181088182088,
9.6013318082255));
#112216=CARTESIAN_POINT('Ctrl Pts',(-9.59364548291463,8.54318548127028,
9.59379924171949));
#112217=CARTESIAN_POINT('Ctrl Pts',(-9.65810210584721,8.54662486983234,
9.57642212692828));
#112218=CARTESIAN_POINT('Ctrl Pts',(-9.69757511699048,8.54866183660209,
9.56751697269165));
#112219=CARTESIAN_POINT('Ctrl Pts',(-9.80051791310509,8.55385468287236,
9.54873857335101));
#112220=CARTESIAN_POINT('Ctrl Pts',(-9.86435824548773,8.55695764561674,
9.5413861499925));
#112221=CARTESIAN_POINT('Ctrl Pts',(-10.0033391102513,8.56374149225771,
9.53458567073997));
#112222=CARTESIAN_POINT('Ctrl Pts',(-10.0783665272326,8.56742241296831,
9.53667958823188));
#112223=CARTESIAN_POINT('Ctrl Pts',(-10.1648694171721,8.57199828878615,
9.54576641849568));
#112224=CARTESIAN_POINT('Ctrl Pts',(-10.1768281112655,8.57263840930715,
9.5471720559656));
#112225=CARTESIAN_POINT('Ctrl Pts',(-10.1937368810588,8.57355584903683,
9.54937138409314));
#112226=CARTESIAN_POINT('Ctrl Pts',(-10.1987026218256,8.57382679474518,
9.55004323272374));
#112227=CARTESIAN_POINT('Ctrl Pts',(-10.2070815950578,8.57428667920463,
9.55122073163447));
#112228=CARTESIAN_POINT('Ctrl Pts',(-10.2104967199093,8.57447488001396,
9.55171298212554));
#112229=CARTESIAN_POINT('Ctrl Pts',(-10.2175092048529,8.57486294117044,
9.55274907758688));
#112230=CARTESIAN_POINT('Ctrl Pts',(-10.2211063131601,8.57506287126819,
9.55329426478373));
#112231=CARTESIAN_POINT('Ctrl Pts',(-10.2303691701346,8.57557988731915,
9.55473352088277));
#112232=CARTESIAN_POINT('Ctrl Pts',(-10.2360317082139,8.57589805126673,
9.55564748738326));
#112233=CARTESIAN_POINT('Ctrl Pts',(-10.25992914387,8.57724925897089,9.5596489542636));
#112234=CARTESIAN_POINT('Ctrl Pts',(-10.2781092798684,8.5782980541986,9.56304855390563));
#112235=CARTESIAN_POINT('Ctrl Pts',(-10.32720786699,8.58117837771229,9.57319637659068));
#112236=CARTESIAN_POINT('Ctrl Pts',(-10.3579790289336,8.58303531853346,
9.58060422541263));
#112237=CARTESIAN_POINT('Ctrl Pts',(-10.4830038075964,8.59073256139294,
9.61502679418599));
#112238=CARTESIAN_POINT('Ctrl Pts',(-10.5746713296241,8.59671573349496,
9.65048223041181));
#112239=CARTESIAN_POINT('Ctrl Pts',(-10.7170762997039,8.60611768683711,
9.72272450416851));
#112240=CARTESIAN_POINT('Ctrl Pts',(-10.7702310074735,8.60965952272931,
9.7540558534945));
#112241=CARTESIAN_POINT('Ctrl Pts',(-10.8307900159537,8.61372160780584,
9.79511292897453));
#112242=CARTESIAN_POINT('Ctrl Pts',(-10.8402467554536,8.61435689364736,
9.80168856089531));
#112243=CARTESIAN_POINT('Ctrl Pts',(-10.855711434248,8.61539757491591,9.81271483342963));
#112244=CARTESIAN_POINT('Ctrl Pts',(-10.8617645300593,8.61580537552884,
9.81710100892787));
#112245=CARTESIAN_POINT('Ctrl Pts',(-10.8725253356821,8.6165312519021,9.8250249105237));
#112246=CARTESIAN_POINT('Ctrl Pts',(-10.8772457685836,8.61684999087118,
9.82854501358458));
#112247=CARTESIAN_POINT('Ctrl Pts',(-10.8821298712992,8.61718014297625,
9.83223324507816));
#112248=CARTESIAN_POINT('Ctrl Pts',(-10.8823148332192,8.61719264644289,
9.83237298814202));
#112249=CARTESIAN_POINT('Ctrl Pts',(-10.8826547494333,8.61721562585409,
9.83262992969273));
#112250=CARTESIAN_POINT('Ctrl Pts',(-10.8828097136029,8.61722610230432,
9.83274711509683));
#112251=CARTESIAN_POINT('Ctrl Pts',(-10.8830957338018,8.61724543958754,
9.83296349587668));
#112252=CARTESIAN_POINT('Ctrl Pts',(-10.8832267964294,8.61725430075764,
9.83306268245273));
#112253=CARTESIAN_POINT('Ctrl Pts',(-10.8834695682923,8.61727071512074,
9.83324647352652));
#112254=CARTESIAN_POINT('Ctrl Pts',(-10.8835812820982,8.61727826854765,
9.8333310719992));
#112255=CARTESIAN_POINT('Ctrl Pts',(-10.8837888346769,8.61729230239795,
9.83348829403231));
#112256=CARTESIAN_POINT('Ctrl Pts',(-10.8838846766435,8.61729878298445,
9.8335609133546));
#112257=CARTESIAN_POINT('Ctrl Pts',(-10.8840631927785,8.6173108540603,9.83369620941298));
#112258=CARTESIAN_POINT('Ctrl Pts',(-10.8841458691954,8.61731644466389,
9.83375888310001));
#112259=CARTESIAN_POINT('Ctrl Pts',(-10.8843001957146,8.61732688047422,
9.83387589770824));
#112260=CARTESIAN_POINT('Ctrl Pts',(-10.8843718475026,8.61733172576754,
9.83393023646456));
#112261=CARTESIAN_POINT('Ctrl Pts',(-10.8845058427424,8.61734078705367,
9.8340318742442));
#112262=CARTESIAN_POINT('Ctrl Pts',(-10.88456818739,8.61734500310722,9.8340791716495));
#112263=CARTESIAN_POINT('Ctrl Pts',(-10.8846849634896,8.61735290020268,
9.83416777791806));
#112264=CARTESIAN_POINT('Ctrl Pts',(-10.8847393958202,8.61735658128906,
9.83420908557627));
#112265=CARTESIAN_POINT('Ctrl Pts',(-10.8849033399816,8.61736766845881,
9.83433351777107));
#112266=CARTESIAN_POINT('Ctrl Pts',(-10.8850128430213,8.61737507409398,
9.83441665394966));
#112267=CARTESIAN_POINT('Ctrl Pts',(-10.8852290082587,8.61738969362405,
9.83458081752551));
#112268=CARTESIAN_POINT('Ctrl Pts',(-10.8853356710549,8.61739690754953,
9.83466184414135));
#112269=CARTESIAN_POINT('Ctrl Pts',(-10.8855463767032,8.61741115857174,
9.83482195275282));
#112270=CARTESIAN_POINT('Ctrl Pts',(-10.8856504200868,8.61741819569551,
9.83490103404092));
#112271=CARTESIAN_POINT('Ctrl Pts',(-10.8858560900248,8.6174321068266,9.83505740310208));
#112272=CARTESIAN_POINT('Ctrl Pts',(-10.8859577170739,8.61743898085934,
9.83513469025015));
#112273=CARTESIAN_POINT('Ctrl Pts',(-10.8861587416625,8.61745257845554,
9.83528761053412));
#112274=CARTESIAN_POINT('Ctrl Pts',(-10.8862581396372,8.61745930204116,
9.83536324309806));
#112275=CARTESIAN_POINT('Ctrl Pts',(-10.8864548793219,8.61747261044106,
9.83551298337262));
#112276=CARTESIAN_POINT('Ctrl Pts',(-10.8865522214054,8.61747919527402,
9.8355870905523));
#112277=CARTESIAN_POINT('Ctrl Pts',(-10.892319829634,8.61786936193009,9.83997915178782));
#112278=CARTESIAN_POINT('Ctrl Pts',(-10.8979585532419,8.618251337755,9.84433850728786));
#112279=CARTESIAN_POINT('Ctrl Pts',(-10.9099101288337,8.61906221188221,
9.85371868090665));
#112280=CARTESIAN_POINT('Ctrl Pts',(-10.9162137889156,8.61949065258742,
9.85875085914617));
#112281=CARTESIAN_POINT('Ctrl Pts',(-10.9325932443076,8.62060616784555,
9.8720496736586));
#112282=CARTESIAN_POINT('Ctrl Pts',(-10.9426008939329,8.62128999322471,
9.88039932714788));
#112283=CARTESIAN_POINT('Ctrl Pts',(-10.9722931166602,8.62332719461908,
9.90585271096796));
#112284=CARTESIAN_POINT('Ctrl Pts',(-10.9916338788096,8.62466531384855,
9.92335031568456));
#112285=CARTESIAN_POINT('Ctrl Pts',(-11.0996178315456,8.63223052707207,
10.0264232263889));
#112286=CARTESIAN_POINT('Ctrl Pts',(-11.1776333241315,8.63802441659883,
10.1223959681063));
#112287=CARTESIAN_POINT('Ctrl Pts',(-11.2500157820225,8.64484730417465,
10.2387611996853));
#112288=CARTESIAN_POINT('Ctrl Pts',(-11.2571617373649,8.64554118544223,
10.250621378847));
#112289=CARTESIAN_POINT('Ctrl Pts',(-11.281324433762,8.64796527235781,10.2920428561266));
#112290=CARTESIAN_POINT('Ctrl Pts',(-11.2974742549373,8.64972514532873,
10.322094517553));
#112291=CARTESIAN_POINT('Ctrl Pts',(-11.3154748215364,8.651895793797,10.3585939522987));
#112292=CARTESIAN_POINT('Ctrl Pts',(-11.3183511332756,8.65224965719763,
10.3645269397548));
#112293=CARTESIAN_POINT('Ctrl Pts',(-11.322999347385,8.65283348996994,10.3742822322466));
#112294=CARTESIAN_POINT('Ctrl Pts',(-11.3247950392138,8.65306206157142,
10.3780931731842));
#112295=CARTESIAN_POINT('Ctrl Pts',(-11.3280009159035,8.65347572845334,
10.3849737982508));
#112296=CARTESIAN_POINT('Ctrl Pts',(-11.3294169527542,8.65366046541412,
10.3880406657207));
#112297=CARTESIAN_POINT('Ctrl Pts',(-11.3325150243086,8.65406914122047,
10.3948120029844));
#112298=CARTESIAN_POINT('Ctrl Pts',(-11.3341922157194,8.65429335853351,
10.3985185518789));
#112299=CARTESIAN_POINT('Ctrl Pts',(-11.3390019561159,8.65494493713151,
10.4092670538193));
#112300=CARTESIAN_POINT('Ctrl Pts',(-11.3420943112329,8.65537460180141,
10.4163267123689));
#112301=CARTESIAN_POINT('Ctrl Pts',(-11.3655933878837,8.65872240542073,
10.4711478957596));
#112302=CARTESIAN_POINT('Ctrl Pts',(-11.38349848506,8.66176670882384,10.5199367012462));
#112303=CARTESIAN_POINT('Ctrl Pts',(-11.4416195631694,8.67353797512733,
10.7088125266264));
#112304=CARTESIAN_POINT('Ctrl Pts',(-11.4634438448967,8.68243347362415,
10.8537075295653));
#112305=CARTESIAN_POINT('Ctrl Pts',(-11.4634998917645,8.69060327775791,
10.999437145398));
#112306=CARTESIAN_POINT('Origin',(-10.,3.5,11.));
#112307=CARTESIAN_POINT('',(-11.4634994186103,9.26065510840341,11.0013045026646));
#112308=CARTESIAN_POINT('',(-11.4635,9.18928959125266,10.9999999999375));
#112309=CARTESIAN_POINT('',(-11.4635,3.5,11.));
#112310=CARTESIAN_POINT('Ctrl Pts',(-11.4634994144634,9.26057778709026,
11.0013091467826));
#112311=CARTESIAN_POINT('Ctrl Pts',(-11.4635877435601,9.25464699952005,
10.9025657644569));
#112312=CARTESIAN_POINT('Ctrl Pts',(-11.453682574716,9.24882527675797,10.8040494680401));
#112313=CARTESIAN_POINT('Ctrl Pts',(-11.4318075510817,9.24272775562083,
10.6968970697916));
#112314=CARTESIAN_POINT('Ctrl Pts',(-11.4295782608926,9.24214118776937,
10.6865510347163));
#112315=CARTESIAN_POINT('Ctrl Pts',(-11.4256765068438,9.24116956294663,
10.6693514004638));
#112316=CARTESIAN_POINT('Ctrl Pts',(-11.4240663890846,9.24078256357533,
10.6624841922878));
#112317=CARTESIAN_POINT('Ctrl Pts',(-11.4208068992745,9.24002562963409,
10.6490210451381));
#112318=CARTESIAN_POINT('Ctrl Pts',(-11.4191610865205,9.23965559298378,
10.6424244353211));
#112319=CARTESIAN_POINT('Ctrl Pts',(-11.4159642864132,9.23895911046782,
10.6299811154125));
#112320=CARTESIAN_POINT('Ctrl Pts',(-11.4144229074653,9.2386323670594,10.6241321033962));
#112321=CARTESIAN_POINT('Ctrl Pts',(-11.4108523433904,9.2378954610927,10.6109160727615));
#112322=CARTESIAN_POINT('Ctrl Pts',(-11.4088016250538,9.23748599582921,
10.6035550208059));
#112323=CARTESIAN_POINT('Ctrl Pts',(-11.4033635436957,9.23643451146293,
10.5846102280256));
#112324=CARTESIAN_POINT('Ctrl Pts',(-11.3998903431274,9.23579524668041,
10.5730515990501));
#112325=CARTESIAN_POINT('Ctrl Pts',(-11.3716840569564,9.23084261305947,
10.4832293793748));
#112326=CARTESIAN_POINT('Ctrl Pts',(-11.3405488222683,9.226747800436,10.4071256272865));
#112327=CARTESIAN_POINT('Ctrl Pts',(-11.2710077081991,9.21926660010698,
10.2710458664142));
#112328=CARTESIAN_POINT('Ctrl Pts',(-11.234300280176,9.21586728097053,10.2104830391603));
#112329=CARTESIAN_POINT('Ctrl Pts',(-11.1631402345574,9.20977487976479,
10.1102459817806));
#112330=CARTESIAN_POINT('Ctrl Pts',(-11.1306678701584,9.20713275364292,
10.0693300602632));
#112331=CARTESIAN_POINT('Ctrl Pts',(-11.091376028343,9.20397479104373,10.0249199639207));
#112332=CARTESIAN_POINT('Ctrl Pts',(-11.0866303450342,9.20359395804841,
10.0196341492791));
#112333=CARTESIAN_POINT('Ctrl Pts',(-11.0789436800968,9.20297765779986,
10.0111970048797));
#112334=CARTESIAN_POINT('Ctrl Pts',(-11.0760268727035,9.20274391754153,
10.0080236916936));
#112335=CARTESIAN_POINT('Ctrl Pts',(-11.0707962145072,9.20232487611817,
10.0023832612462));
#112336=CARTESIAN_POINT('Ctrl Pts',(-11.0684877808645,9.20213997852701,
9.99991122779515));
#112337=CARTESIAN_POINT('Ctrl Pts',(-11.0634396352549,9.20173569812629,
9.99454274735059));
#112338=CARTESIAN_POINT('Ctrl Pts',(-11.0606966888662,9.20151607621701,
9.99164952611135));
#112339=CARTESIAN_POINT('Ctrl Pts',(-11.0530189145132,9.20090155726755,
9.98361710968607));
#112340=CARTESIAN_POINT('Ctrl Pts',(-11.0480583945807,9.20050477976735,
9.97850275995187));
#112341=CARTESIAN_POINT('Ctrl Pts',(-11.0203384405045,9.19829001114033,
9.95033765101867));
#112342=CARTESIAN_POINT('Ctrl Pts',(-10.9968573509582,9.19642319689324,
9.92801273362056));
#112343=CARTESIAN_POINT('Ctrl Pts',(-10.9049584905991,9.18921556284882,
9.84627063757526));
#112344=CARTESIAN_POINT('Ctrl Pts',(-10.8318159064224,9.18368979199902,
9.79247214079188));
#112345=CARTESIAN_POINT('Ctrl Pts',(-10.7061921957233,9.17494291371066,
9.71693381234001));
#112346=CARTESIAN_POINT('Ctrl Pts',(-10.6565964945217,9.17165161009305,
9.69085972646669));
#112347=CARTESIAN_POINT('Ctrl Pts',(-10.5757232706713,9.16656983228758,
9.65409739632357));
#112348=CARTESIAN_POINT('Ctrl Pts',(-10.5453711172691,9.16472218955835,
9.64151492879573));
#112349=CARTESIAN_POINT('Ctrl Pts',(-10.5050288979023,9.16234257785429,
9.6263613946514));
#112350=CARTESIAN_POINT('Ctrl Pts',(-10.4954006424304,9.16178019335898,
9.62285969605142));
#112351=CARTESIAN_POINT('Ctrl Pts',(-10.4795764453286,9.16086478707162,
9.61729203254613));
#112352=CARTESIAN_POINT('Ctrl Pts',(-10.4734021506136,9.16050980795201,
9.61516596810784));
#112353=CARTESIAN_POINT('Ctrl Pts',(-10.4614118216881,9.15982462492923,
9.61112676480747));
#112354=CARTESIAN_POINT('Ctrl Pts',(-10.4555976142401,9.15949426506742,
9.60920866119674));
#112355=CARTESIAN_POINT('Ctrl Pts',(-10.4421090038998,9.15873214383523,
9.60485243932671));
#112356=CARTESIAN_POINT('Ctrl Pts',(-10.4344261348479,9.15830125517478,
9.60244104802759));
#112357=CARTESIAN_POINT('Ctrl Pts',(-10.4093443373654,9.15690467741667,
9.59479554203964));
#112358=CARTESIAN_POINT('Ctrl Pts',(-10.3918674125743,9.15594734910451,
9.58982188205164));
#112359=CARTESIAN_POINT('Ctrl Pts',(-10.268342237738,9.14928276504524,9.55714243520837));
#112360=CARTESIAN_POINT('Ctrl Pts',(-10.1595694189549,9.1439724906509,9.54110124596277));
#112361=CARTESIAN_POINT('Ctrl Pts',(-9.98834385028947,9.13563078633208,
9.535245947676));
#112362=CARTESIAN_POINT('Ctrl Pts',(-9.92660263098679,9.13261781086763,
9.53703993268307));
#112363=CARTESIAN_POINT('Ctrl Pts',(-9.84635025586176,9.12850584379428,
9.54446539902446));
#112364=CARTESIAN_POINT('Ctrl Pts',(-9.82757321065347,9.12752945492775,
9.54657020661006));
#112365=CARTESIAN_POINT('Ctrl Pts',(-9.79620984333528,9.12586702481034,
9.55070217437578));
#112366=CARTESIAN_POINT('Ctrl Pts',(-9.78359943722578,9.125190004719,9.55253138547809));
#112367=CARTESIAN_POINT('Ctrl Pts',(-9.76609783805104,9.12423644785596,
9.55530390275256));
#112368=CARTESIAN_POINT('Ctrl Pts',(-9.76118480259052,9.1239672324377,9.55610792134571));
#112369=CARTESIAN_POINT('Ctrl Pts',(-9.75284656196811,9.12350757844391,
9.55751619597944));
#112370=CARTESIAN_POINT('Ctrl Pts',(-9.7494191826153,9.12331784902367,9.55810763211673));
#112371=CARTESIAN_POINT('Ctrl Pts',(-9.74283106582253,9.12295157534914,
9.55926869130808));
#112372=CARTESIAN_POINT('Ctrl Pts',(-9.73967005534391,9.12277514060324,
9.55983650787247));
#112373=CARTESIAN_POINT('Ctrl Pts',(-9.73207493810905,9.12234958325666,
9.56122665133343));
#112374=CARTESIAN_POINT('Ctrl Pts',(-9.72764274101372,9.12209990888812,
9.56205907283771));
#112375=CARTESIAN_POINT('Ctrl Pts',(-9.71141777387722,9.12118120205092,
9.56518402770646));
#112376=CARTESIAN_POINT('Ctrl Pts',(-9.69964982875581,9.12050571179411,
9.56760119681718));
#112377=CARTESIAN_POINT('Ctrl Pts',(-9.61393397834814,9.11552515825988,
9.58631016070359));
#112378=CARTESIAN_POINT('Ctrl Pts',(-9.54132530411738,9.11098259187146,
9.60817330256716));
#112379=CARTESIAN_POINT('Ctrl Pts',(-9.40962004770212,9.10248270405019,
9.65926080061698));
#112380=CARTESIAN_POINT('Ctrl Pts',(-9.35015796570116,9.09853753828418,
9.68705052723216));
#112381=CARTESIAN_POINT('Ctrl Pts',(-9.25848438319621,9.09238812134568,
9.7376532271364));
#112382=CARTESIAN_POINT('Ctrl Pts',(-9.22498247231869,9.09012423039904,
9.75794002361032));
#112383=CARTESIAN_POINT('Ctrl Pts',(-9.17090307224934,9.08644889887496,
9.79372853105894));
#112384=CARTESIAN_POINT('Ctrl Pts',(-9.14985021177433,9.08501236587994,
9.80847239787423));
#112385=CARTESIAN_POINT('Ctrl Pts',(-9.12170728193134,9.08308321239783,
9.82930748738281));
#112386=CARTESIAN_POINT('Ctrl Pts',(-9.11427201437805,9.08257265391562,
9.83492274985579));
#112387=CARTESIAN_POINT('Ctrl Pts',(-9.10187404714724,9.08171969621857,
9.84447322638921));
#112388=CARTESIAN_POINT('Ctrl Pts',(-9.09688242159149,9.08137583075347,
9.84837028822827));
#112389=CARTESIAN_POINT('Ctrl Pts',(-9.08707996100995,9.08069959828645,
9.85612619409373));
#112390=CARTESIAN_POINT('Ctrl Pts',(-9.0822679146617,9.08036717284713,9.85998328847165));
#112391=CARTESIAN_POINT('Ctrl Pts',(-9.07171990907488,9.07963739934561,
9.86854810827699));
#112392=CARTESIAN_POINT('Ctrl Pts',(-9.06599506384981,9.07924059643331,
9.87326929017204));
#112393=CARTESIAN_POINT('Ctrl Pts',(-9.04592842082742,9.07784691697698,
9.89007594544118));
#112394=CARTESIAN_POINT('Ctrl Pts',(-9.03178294821479,9.07685938255403,
9.90239361901702));
#112395=CARTESIAN_POINT('Ctrl Pts',(-8.92583626714218,9.06941289107479,
9.99829287749866));
#112396=CARTESIAN_POINT('Ctrl Pts',(-8.84477233680633,9.06347863700027,
10.0929743220037));
#112397=CARTESIAN_POINT('Ctrl Pts',(-8.73766935095357,9.05393429458585,
10.2560963517692));
#112398=CARTESIAN_POINT('Ctrl Pts',(-8.70308158209386,9.05041570019676,
10.3181850210981));
#112399=CARTESIAN_POINT('Ctrl Pts',(-8.6694249938068,9.04618030387344,10.3905085249929));
#112400=CARTESIAN_POINT('Ctrl Pts',(-8.66578392934718,9.04570924407623,
10.3985208444945));
#112401=CARTESIAN_POINT('Ctrl Pts',(-8.66047576666075,9.0450023022064,10.4104870782155));
#112402=CARTESIAN_POINT('Ctrl Pts',(-8.65875336957229,9.04476961959455,
10.4144164175164));
#112403=CARTESIAN_POINT('Ctrl Pts',(-8.6557045564204,9.04435170401406,10.4214557564669));
#112404=CARTESIAN_POINT('Ctrl Pts',(-8.65437161209333,9.0441668654688,10.424562842095));
#112405=CARTESIAN_POINT('Ctrl Pts',(-8.65148435190901,9.04376179236916,
10.4313579215572));
#112406=CARTESIAN_POINT('Ctrl Pts',(-8.64993441379782,9.0435413112134,10.4350476314832));
#112407=CARTESIAN_POINT('Ctrl Pts',(-8.64564136093768,9.04292215597171,
10.4453860290998));
#112408=CARTESIAN_POINT('Ctrl Pts',(-8.64293213405256,9.04252155710716,
10.4520485579467));
#112409=CARTESIAN_POINT('Ctrl Pts',(-8.62786863555786,9.0402384289018,10.489889713662));
#112410=CARTESIAN_POINT('Ctrl Pts',(-8.61654067885616,9.03830354709428,
10.5214637315354));
#112411=CARTESIAN_POINT('Ctrl Pts',(-8.60173242489681,9.03545624272042,
10.56767505946));
#112412=CARTESIAN_POINT('Ctrl Pts',(-8.59737667660224,9.0345700661961,10.5820228963596));
#112413=CARTESIAN_POINT('Ctrl Pts',(-8.58539915775161,9.03198958910947,
10.6237744337858));
#112414=CARTESIAN_POINT('Ctrl Pts',(-8.5783548896762,9.03028405638726,10.6513363596057));
#112415=CARTESIAN_POINT('Ctrl Pts',(-8.567182480993,9.0272207759877,10.7010470224951));
#112416=CARTESIAN_POINT('Ctrl Pts',(-8.56275396330219,9.02586503872493,
10.7231195989814));
#112417=CARTESIAN_POINT('Ctrl Pts',(-8.54039646531599,9.01814187689005,
10.8496173758894));
#112418=CARTESIAN_POINT('Ctrl Pts',(-8.53333767806876,9.01188069924047,
10.9556591124973));
#112419=CARTESIAN_POINT('Ctrl Pts',(-8.53836947750706,9.00522667768161,
11.0752011769721));
#112420=CARTESIAN_POINT('Ctrl Pts',(-8.53913541319428,9.00447254008878,
11.0888463732003));
#112421=CARTESIAN_POINT('Ctrl Pts',(-8.54060138473717,9.00332629101779,
11.1097304510574));
#112422=CARTESIAN_POINT('Ctrl Pts',(-8.54116441710109,9.00292997446441,
11.1169779245923));
#112423=CARTESIAN_POINT('Ctrl Pts',(-8.54224284347945,9.00224020355104,
11.1296374703578));
#112424=CARTESIAN_POINT('Ctrl Pts',(-8.54273443520403,9.00194601887018,
11.1350513823233));
#112425=CARTESIAN_POINT('Ctrl Pts',(-8.54391421717564,9.00128291307834,
11.1472869635453));
#112426=CARTESIAN_POINT('Ctrl Pts',(-8.54462020480608,9.00091455044507,
11.1541068152049));
#112427=CARTESIAN_POINT('Ctrl Pts',(-8.54666444367924,8.99991968705152,
11.1725854037152));
#112428=CARTESIAN_POINT('Ctrl Pts',(-8.54809505411668,8.99929605738093,
11.1842335462639));
#112429=CARTESIAN_POINT('Ctrl Pts',(-8.5556503577789,8.99631616382051,11.2401792389532));
#112430=CARTESIAN_POINT('Ctrl Pts',(-8.56366333813169,8.99401896161288,
11.284199645879));
#112431=CARTESIAN_POINT('Ctrl Pts',(-8.59865740476869,8.98615322456675,
11.4364714875169));
#112432=CARTESIAN_POINT('Ctrl Pts',(-8.6359729848927,8.98087742108433,11.5419387432681));
#112433=CARTESIAN_POINT('Ctrl Pts',(-8.70768111128317,8.97277481424319,
11.6887956499032));
#112434=CARTESIAN_POINT('Ctrl Pts',(-8.73292477266111,8.97014595620894,
11.7341981270518));
#112435=CARTESIAN_POINT('Ctrl Pts',(-8.76462085291051,8.96697042651294,
11.7846846383864));
#112436=CARTESIAN_POINT('Ctrl Pts',(-8.76876912930578,8.96655701013309,
11.7911777023579));
#112437=CARTESIAN_POINT('Ctrl Pts',(-8.77518512542734,8.96592041398787,
11.8010476362268));
#112438=CARTESIAN_POINT('Ctrl Pts',(-8.77741603600157,8.96569957088621,
11.804448408937));
#112439=CARTESIAN_POINT('Ctrl Pts',(-8.781525215121,8.9652936334501,11.8106558170019));
#112440=CARTESIAN_POINT('Ctrl Pts',(-8.78339904760653,8.96510882938309,
11.8134652894205));
#112441=CARTESIAN_POINT('Ctrl Pts',(-8.78763158915703,8.96469209024615,
11.8197638827522));
#112442=CARTESIAN_POINT('Ctrl Pts',(-8.78999562753456,8.96445980817906,
11.8232492968616));
#112443=CARTESIAN_POINT('Ctrl Pts',(-8.79697436286067,8.96377562666277,
11.8334433803736));
#112444=CARTESIAN_POINT('Ctrl Pts',(-8.80162996774863,8.96332113098491,
11.8401236882514));
#112445=CARTESIAN_POINT('Ctrl Pts',(-8.84366256117029,8.95923732544452,
11.8993757902225));
#112446=CARTESIAN_POINT('Ctrl Pts',(-8.88441816822874,8.95541631039829,
11.9494570112974));
#112447=CARTESIAN_POINT('Ctrl Pts',(-8.97528266815056,8.94741767148317,
12.0471571723222));
#112448=CARTESIAN_POINT('Ctrl Pts',(-9.02573605850253,8.94324496191199,
12.0942550594568));
#112449=CARTESIAN_POINT('Ctrl Pts',(-9.13030537370636,8.93527050962021,
12.1788830809087));
#112450=CARTESIAN_POINT('Ctrl Pts',(-9.18400949515908,8.931469310283,12.2166738713741));
#112451=CARTESIAN_POINT('Ctrl Pts',(-9.25430433536874,8.92687059295574,
12.2593837720315));
#112452=CARTESIAN_POINT('Ctrl Pts',(-9.26868163038639,8.92594825581372,
12.2677866475777));
#112453=CARTESIAN_POINT('Ctrl Pts',(-9.2900540357876,8.92460329304843,12.2797932600741));
#112454=CARTESIAN_POINT('Ctrl Pts',(-9.29693945272598,8.92417390865393,
12.2835886922459));
#112455=CARTESIAN_POINT('Ctrl Pts',(-9.30919814896698,8.92341625423245,
12.2902177907251));
#112456=CARTESIAN_POINT('Ctrl Pts',(-9.3145590729222,8.92308720439056,12.2930738114731));
#112457=CARTESIAN_POINT('Ctrl Pts',(-9.32584899316792,8.92239895513897,
12.2989985515554));
#112458=CARTESIAN_POINT('Ctrl Pts',(-9.33178152923678,8.92204000580957,
12.3020602498734));
#112459=CARTESIAN_POINT('Ctrl Pts',(-9.34746576839214,8.92109801361449,
12.3100192365946));
#112460=CARTESIAN_POINT('Ctrl Pts',(-9.35725175215145,8.92051733158653,
12.3148482886332));
#112461=CARTESIAN_POINT('Ctrl Pts',(-9.39963142815733,8.91803183709967,
12.3351750072951));
#112462=CARTESIAN_POINT('Ctrl Pts',(-9.43273947097119,8.9161643654257,12.349574186859));
#112463=CARTESIAN_POINT('Ctrl Pts',(-9.60075544036781,8.90699164084084,
12.4153698474907));
#112464=CARTESIAN_POINT('Ctrl Pts',(-9.74219040319263,8.90031471510722,
12.4478242421376));
#112465=CARTESIAN_POINT('Ctrl Pts',(-9.90671974814241,8.89192922602425,
12.4606710476978));
#112466=CARTESIAN_POINT('Ctrl Pts',(-9.92739700208817,8.89086275113372,
12.4618446728769));
#112467=CARTESIAN_POINT('Ctrl Pts',(-9.96172529594793,8.88906140705812,
12.4630630257577));
#112468=CARTESIAN_POINT('Ctrl Pts',(-9.97536492275711,8.88833762737753,
12.4633562303468));
#112469=CARTESIAN_POINT('Ctrl Pts',(-9.99411964451016,8.88732897251104,
12.4634971201175));
#112470=CARTESIAN_POINT('Ctrl Pts',(-9.99923321598756,8.88705258342828,
12.4635087323438));
#112471=CARTESIAN_POINT('Ctrl Pts',(-10.0078511222671,8.88658431481434,
12.4634831366297));
#112472=CARTESIAN_POINT('Ctrl Pts',(-10.0113555062541,8.88639320954437,
12.4634601407316));
#112473=CARTESIAN_POINT('Ctrl Pts',(-10.0180420390046,8.88602720285449,
12.4633922450245));
#112474=CARTESIAN_POINT('Ctrl Pts',(-10.0212241768802,8.88585243046118,
12.463349552187));
#112475=CARTESIAN_POINT('Ctrl Pts',(-10.0288042782522,8.88543474726858,
12.4632231247295));
#112476=CARTESIAN_POINT('Ctrl Pts',(-10.0332020273367,8.88519132780118,
12.463129940762));
#112477=CARTESIAN_POINT('Ctrl Pts',(-10.0488312490244,8.88432251515276,
12.4627282730109));
#112478=CARTESIAN_POINT('Ctrl Pts',(-10.0600592291526,8.88369153337334,
12.4623102834184));
#112479=CARTESIAN_POINT('Ctrl Pts',(-10.1706133605633,8.87741870649571,
12.4569192584354));
#112480=CARTESIAN_POINT('Ctrl Pts',(-10.2691865864193,8.87136692621747,
12.4419635334144));
#112481=CARTESIAN_POINT('Ctrl Pts',(-10.3803752379357,8.8644726000103,12.4132882683923));
#112482=CARTESIAN_POINT('Ctrl Pts',(-10.3952146324694,8.86355054100444,
12.4092105786047));
#112483=CARTESIAN_POINT('Ctrl Pts',(-10.4647573789175,8.85922464094281,
12.3889161536527));
#112484=CARTESIAN_POINT('Ctrl Pts',(-10.5185498969593,8.85586712182788,
12.3697424968891));
#112485=CARTESIAN_POINT('Ctrl Pts',(-10.6017995354547,8.85069231105968,
12.3344594704143));
#112486=CARTESIAN_POINT('Ctrl Pts',(-10.6320571595934,8.84881554024162,
12.3203971972723));
#112487=CARTESIAN_POINT('Ctrl Pts',(-10.6709457900428,8.84640793599899,
12.30068017723));
#112488=CARTESIAN_POINT('Ctrl Pts',(-10.6800332401621,8.84584563118905,
12.2959521504849));
#112489=CARTESIAN_POINT('Ctrl Pts',(-10.6948310413796,8.84493032119288,
12.2880546223138));
#112490=CARTESIAN_POINT('Ctrl Pts',(-10.700571039241,8.84457535947025,12.2849416745608));
#112491=CARTESIAN_POINT('Ctrl Pts',(-10.7116523436366,8.84389018719403,
12.2788356720092));
#112492=CARTESIAN_POINT('Ctrl Pts',(-10.7169960714237,8.84355982085968,
12.2758473142713));
#112493=CARTESIAN_POINT('Ctrl Pts',(-10.7293247009485,8.84279765190446,
12.268850889797));
#112494=CARTESIAN_POINT('Ctrl Pts',(-10.7362956231097,8.84236672234093,
12.2648185082604));
#112495=CARTESIAN_POINT('Ctrl Pts',(-10.7588882938449,8.84096987013546,
12.2514995301244));
#112496=CARTESIAN_POINT('Ctrl Pts',(-10.7743707408605,8.84001231295309,
12.2419792712989));
#112497=CARTESIAN_POINT('Ctrl Pts',(-10.8818961487801,8.83335104906587,
12.1730686149851));
#112498=CARTESIAN_POINT('Ctrl Pts',(-10.9671931213109,8.8280437578453,12.1037983168661));
#112499=CARTESIAN_POINT('Ctrl Pts',(-11.0872475666993,8.81970312457884,
11.9816001182988));
#112500=CARTESIAN_POINT('Ctrl Pts',(-11.1276931531803,8.81668800129018,
11.934854666268));
#112501=CARTESIAN_POINT('Ctrl Pts',(-11.1765018762316,8.812573314343,11.870650826866));
#112502=CARTESIAN_POINT('Ctrl Pts',(-11.187648040981,8.81159651927403,11.8553838911712));
#112503=CARTESIAN_POINT('Ctrl Pts',(-11.2058101331925,8.80993345993638,
11.8294676865334));
#112504=CARTESIAN_POINT('Ctrl Pts',(-11.2129883876083,8.80925622565848,
11.8189345945206));
#112505=CARTESIAN_POINT('Ctrl Pts',(-11.2227779052904,8.80830241575764,
11.8041587128331));
#112506=CARTESIAN_POINT('Ctrl Pts',(-11.2255066652886,8.80803316662895,
11.7999940330855));
#112507=CARTESIAN_POINT('Ctrl Pts',(-11.230105421393,8.8075734723539,11.792896588397));
#112508=CARTESIAN_POINT('Ctrl Pts',(-11.2319863395222,8.80738373666567,
11.7899708897618));
#112509=CARTESIAN_POINT('Ctrl Pts',(-11.235583870014,8.80701746507647,11.7843309657018));
#112510=CARTESIAN_POINT('Ctrl Pts',(-11.2373019998119,8.80684103877907,
11.7816177610889));
#112511=CARTESIAN_POINT('Ctrl Pts',(-11.2414110225274,8.80641552104535,
11.7750814510423));
#112512=CARTESIAN_POINT('Ctrl Pts',(-11.2437931889061,8.8061658780594,11.7712529317559));
#112513=CARTESIAN_POINT('Ctrl Pts',(-11.2524548919556,8.80524744148726,
11.7571877025385));
#112514=CARTESIAN_POINT('Ctrl Pts',(-11.2586258830092,8.80457219505848,
11.7468850922605));
#112515=CARTESIAN_POINT('Ctrl Pts',(-11.3029040076387,8.79957747836617,
11.6708544507994));
#112516=CARTESIAN_POINT('Ctrl Pts',(-11.3359652213428,8.79501890264714,
11.6023284504375));
#112517=CARTESIAN_POINT('Ctrl Pts',(-11.3875295987129,8.78647654159967,
11.4700539875952));
#112518=CARTESIAN_POINT('Ctrl Pts',(-11.4073169669729,8.78250489947593,
11.4070000285174));
#112519=CARTESIAN_POINT('Ctrl Pts',(-11.431850260053,8.77635755887737,11.3051821911238));
#112520=CARTESIAN_POINT('Ctrl Pts',(-11.4394231093976,8.77411956582275,
11.2671943231907));
#112521=CARTESIAN_POINT('Ctrl Pts',(-11.4494688200691,8.77048119113625,
11.20377007474));
#112522=CARTESIAN_POINT('Ctrl Pts',(-11.4527984197197,8.76905635526781,
11.1784908101196));
#112523=CARTESIAN_POINT('Ctrl Pts',(-11.4564380588712,8.76714015514075,
11.1438982846547));
#112524=CARTESIAN_POINT('Ctrl Pts',(-11.4573220740337,8.7666311630491,11.1346510814868));
#112525=CARTESIAN_POINT('Ctrl Pts',(-11.4586600988221,8.76578008367204,
11.1190923792931));
#112526=CARTESIAN_POINT('Ctrl Pts',(-11.4591613191023,8.76543654427015,
11.1127853061312));
#112527=CARTESIAN_POINT('Ctrl Pts',(-11.4600706334484,8.76476039818953,
11.1003199058104));
#112528=CARTESIAN_POINT('Ctrl Pts',(-11.4604807031084,8.76442773717901,
11.0941618585566));
#112529=CARTESIAN_POINT('Ctrl Pts',(-11.461382260589,8.76362248398171,11.0791957007959));
#112530=CARTESIAN_POINT('Ctrl Pts',(-11.461833089414,8.76315115558401,11.0703853241859));
#112531=CARTESIAN_POINT('Ctrl Pts',(-11.4630747972514,8.76158230661794,
11.0408970541776));
#112532=CARTESIAN_POINT('Ctrl Pts',(-11.4635068166774,8.76049581071048,
11.0202060640286));
#112533=CARTESIAN_POINT('Ctrl Pts',(-11.463499918694,8.75942153142852,10.9995121654828));
#112534=CARTESIAN_POINT('Ctrl Pts',(-11.4634998922174,8.69060334384545,
10.9994383242407));
#112535=CARTESIAN_POINT('Ctrl Pts',(-11.4635041761544,8.69122911239194,
11.010600531755));
#112536=CARTESIAN_POINT('Ctrl Pts',(-11.4633807578742,8.69185105214708,
11.0217626903887));
#112537=CARTESIAN_POINT('Ctrl Pts',(-11.4629135671457,8.69300092039859,
11.0425253298918));
#112538=CARTESIAN_POINT('Ctrl Pts',(-11.4626029579925,8.69352982726182,
11.0521258289666));
#112539=CARTESIAN_POINT('Ctrl Pts',(-11.4619467181113,8.69438189805341,
11.0676720049115));
#112540=CARTESIAN_POINT('Ctrl Pts',(-11.4616592768631,8.6947068458762,11.0736197437169));
#112541=CARTESIAN_POINT('Ctrl Pts',(-11.4610208788094,8.69534542238823,
11.0853448293847));
#112542=CARTESIAN_POINT('Ctrl Pts',(-11.4606719341333,8.6956591072733,11.0911221728518));
#112543=CARTESIAN_POINT('Ctrl Pts',(-11.4598566930235,8.69632419110991,
11.103408240213));
#112544=CARTESIAN_POINT('Ctrl Pts',(-11.4593811192562,8.69667529608018,
11.1099162360673));
#112545=CARTESIAN_POINT('Ctrl Pts',(-11.4580492371702,8.69757274558584,
11.1266059549511));
#112546=CARTESIAN_POINT('Ctrl Pts',(-11.4571297931297,8.69811712925825,
11.1367823777872));
#112547=CARTESIAN_POINT('Ctrl Pts',(-11.4530757017606,8.70025565995408,
11.1769541213546));
#112548=CARTESIAN_POINT('Ctrl Pts',(-11.4491206982659,8.70182445823039,
11.2068601503051));
#112549=CARTESIAN_POINT('Ctrl Pts',(-11.4221473957723,8.71036873031556,
11.3714927638279));
#112550=CARTESIAN_POINT('Ctrl Pts',(-11.3812720274938,8.71675561709629,
11.5025878047017));
#112551=CARTESIAN_POINT('Ctrl Pts',(-11.3098873644176,8.725087116408,11.6534061608572));
#112552=CARTESIAN_POINT('Ctrl Pts',(-11.2961243703384,8.72661787500154,
11.6802984237786));
#112553=CARTESIAN_POINT('Ctrl Pts',(-11.2757276207569,8.72881269286219,
11.7172838753264));
#112554=CARTESIAN_POINT('Ctrl Pts',(-11.2697855386576,8.72944420292249,
11.7277511864386));
#112555=CARTESIAN_POINT('Ctrl Pts',(-11.2591630097293,8.73056169863935,
11.7459371454822));
#112556=CARTESIAN_POINT('Ctrl Pts',(-11.2545389331615,8.73104455530924,
11.7536881100169));
#112557=CARTESIAN_POINT('Ctrl Pts',(-11.2475882844969,8.7317658580685,11.7650977155111));
#112558=CARTESIAN_POINT('Ctrl Pts',(-11.2453165833911,8.7320009129424,11.7687897294129));
#112559=CARTESIAN_POINT('Ctrl Pts',(-11.2412418095311,8.73242141161767,
11.7753466831609));
#112560=CARTESIAN_POINT('Ctrl Pts',(-11.2394451611175,8.73260644082897,
11.7782155235676));
#112561=CARTESIAN_POINT('Ctrl Pts',(-11.2355194045234,8.73300994659747,
11.7844359864338));
#112562=CARTESIAN_POINT('Ctrl Pts',(-11.2333866353785,8.73322865380585,
11.7877851373768));
#112563=CARTESIAN_POINT('Ctrl Pts',(-11.2274290134348,8.73383809164023,
11.7970570720046));
#112564=CARTESIAN_POINT('Ctrl Pts',(-11.2235750007559,8.73423065406589,
11.8029608785832));
#112565=CARTESIAN_POINT('Ctrl Pts',(-11.2023888347466,8.73637856635628,
11.834908389493));
#112566=CARTESIAN_POINT('Ctrl Pts',(-11.1842687470721,8.73817943874383,
11.8604174497835));
#112567=CARTESIAN_POINT('Ctrl Pts',(-11.0883129876362,8.74746320560208,
11.9867233774404));
#112568=CARTESIAN_POINT('Ctrl Pts',(-10.9983733011471,8.75531439409573,
12.0776382947922));
#112569=CARTESIAN_POINT('Ctrl Pts',(-10.8713828452819,8.76468758076267,
12.1762832954717));
#112570=CARTESIAN_POINT('Ctrl Pts',(-10.8442780517665,8.76660879379222,
12.1958868103142));
#112571=CARTESIAN_POINT('Ctrl Pts',(-10.8036559928054,8.76937210551735,
12.2231965162453));
#112572=CARTESIAN_POINT('Ctrl Pts',(-10.790651080159,8.77024018236295,12.2316426296469));
#112573=CARTESIAN_POINT('Ctrl Pts',(-10.7698305707955,8.77160413693417,
12.2446989166562));
#112574=CARTESIAN_POINT('Ctrl Pts',(-10.7621023627579,8.77210490134224,
12.2494456749752));
#112575=CARTESIAN_POINT('Ctrl Pts',(-10.7473660157143,8.77304948632569,
12.2583093175423));
#112576=CARTESIAN_POINT('Ctrl Pts',(-10.7403667581082,8.77349380065015,
12.2624402430465));
#112577=CARTESIAN_POINT('Ctrl Pts',(-10.7281134394506,8.77426423248375,
12.2695351321741));
#112578=CARTESIAN_POINT('Ctrl Pts',(-10.7228748378746,8.77459127994824,
12.2725252857242));
#112579=CARTESIAN_POINT('Ctrl Pts',(-10.711982338249,8.77526654607694,12.2786536716897));
#112580=CARTESIAN_POINT('Ctrl Pts',(-10.7063258196691,8.77561458590073,
12.2817869949436));
#112581=CARTESIAN_POINT('Ctrl Pts',(-10.6919178059187,8.77649455166173,
12.2896437082547));
#112582=CARTESIAN_POINT('Ctrl Pts',(-10.6831385164502,8.77702466606678,
12.2943156177097));
#112583=CARTESIAN_POINT('Ctrl Pts',(-10.649440554567,8.77903700988905,12.3118096388524));
#112584=CARTESIAN_POINT('Ctrl Pts',(-10.6242023050027,8.78049763845742,
12.3240049765261));
#112585=CARTESIAN_POINT('Ctrl Pts',(-10.4673832087891,8.78932434278479,
12.3942996624366));
#112586=CARTESIAN_POINT('Ctrl Pts',(-10.3281996667631,8.7960116787744,12.4334569852349));
#112587=CARTESIAN_POINT('Ctrl Pts',(-10.1452473095871,8.80526438873417,
12.4568411778385));
#112588=CARTESIAN_POINT('Ctrl Pts',(-10.1047519500462,8.807347193197,12.4603114338398));
#112589=CARTESIAN_POINT('Ctrl Pts',(-10.0568694251549,8.80990364845809,
12.4624129015824));
#112590=CARTESIAN_POINT('Ctrl Pts',(-10.0495684008938,8.81029602026976,
12.4626785687462));
#112591=CARTESIAN_POINT('Ctrl Pts',(-10.0382843104793,8.81090683021201,
12.4630045889954));
#112592=CARTESIAN_POINT('Ctrl Pts',(-10.0343023708242,8.81112321583334,
12.463103366971));
#112593=CARTESIAN_POINT('Ctrl Pts',(-10.0269370377758,8.81152509895022,
12.4632559913406));
#112594=CARTESIAN_POINT('Ctrl Pts',(-10.0235538199722,8.81171034726568,
12.4633143603086));
#112595=CARTESIAN_POINT('Ctrl Pts',(-10.0158529560286,8.81213346855527,
12.4634205061721));
#112596=CARTESIAN_POINT('Ctrl Pts',(-10.0115352986583,8.81237173788718,
12.4634609082618));
#112597=CARTESIAN_POINT('Ctrl Pts',(-10.0002769775564,8.81299561878296,
12.463516431904));
#112598=CARTESIAN_POINT('Ctrl Pts',(-9.99333635320748,8.81338280255223,
12.4635012863553));
#112599=CARTESIAN_POINT('Ctrl Pts',(-9.9452654451271,8.81608101168285,12.4630544305883));
#112600=CARTESIAN_POINT('Ctrl Pts',(-9.90417231774244,8.8184711726772,12.4609382696216));
#112601=CARTESIAN_POINT('Ctrl Pts',(-9.78011980128589,8.82583669264184,
12.4492938098128));
#112602=CARTESIAN_POINT('Ctrl Pts',(-9.69783329735729,8.83091788028911,
12.4343972127257));
#112603=CARTESIAN_POINT('Ctrl Pts',(-9.54603557561309,8.84029120069118,
12.3932676088698));
#112604=CARTESIAN_POINT('Ctrl Pts',(-9.47636117999831,8.84459438315749,
12.3686062787301));
#112605=CARTESIAN_POINT('Ctrl Pts',(-9.39267877979302,8.84971746654369,
12.3316550546928));
#112606=CARTESIAN_POINT('Ctrl Pts',(-9.37665048162581,8.85069701962615,
12.3242279506662));
#112607=CARTESIAN_POINT('Ctrl Pts',(-9.35351801073911,8.85210872370557,
12.3129958491874));
#112608=CARTESIAN_POINT('Ctrl Pts',(-9.34630500497379,8.85254862622572,
12.3094196880721));
#112609=CARTESIAN_POINT('Ctrl Pts',(-9.33367766170435,8.8533183282836,12.3030287877865));
#112610=CARTESIAN_POINT('Ctrl Pts',(-9.32825077939944,8.85364899169769,
12.3002393881487));
#112611=CARTESIAN_POINT('Ctrl Pts',(-9.31699845898757,8.85433438584008,
12.2943664804152));
#112612=CARTESIAN_POINT('Ctrl Pts',(-9.31117607915413,8.85468891276253,
12.2912773902836));
#112613=CARTESIAN_POINT('Ctrl Pts',(-9.29611595811837,8.85560572290779,
12.2831563260414));
#112614=CARTESIAN_POINT('Ctrl Pts',(-9.2869111591315,8.85616587523206,12.2780638537231));
#112615=CARTESIAN_POINT('Ctrl Pts',(-9.24942614195055,8.85844701120498,
12.2567945532017));
#112616=CARTESIAN_POINT('Ctrl Pts',(-9.2216339693851,8.86013803850938,12.2397742502176));
#112617=CARTESIAN_POINT('Ctrl Pts',(-9.17288197040072,8.86311941267036,
12.2076316772401));
#112618=CARTESIAN_POINT('Ctrl Pts',(-9.15171134095858,8.86441953494931,
12.1928557889026));
#112619=CARTESIAN_POINT('Ctrl Pts',(-9.04718037307769,8.87089661411987,
12.115708121791));
#112620=CARTESIAN_POINT('Ctrl Pts',(-8.97025856051638,8.87582979390374,
12.0451320758737));
#112621=CARTESIAN_POINT('Ctrl Pts',(-8.86965832404969,8.88340530742882,
11.9308485229977));
#112622=CARTESIAN_POINT('Ctrl Pts',(-8.83964577580599,8.8858536496044,11.8931564812548));
#112623=CARTESIAN_POINT('Ctrl Pts',(-8.80711791617393,8.88882396997827,
11.8478928112567));
#112624=CARTESIAN_POINT('Ctrl Pts',(-8.80273569034753,8.88923141488444,
11.841693562537));
#112625=CARTESIAN_POINT('Ctrl Pts',(-8.79609338116264,8.8898607275815,11.8321402871411));
#112626=CARTESIAN_POINT('Ctrl Pts',(-8.79379857436683,8.89008034123494,
11.8288104272786));
#112627=CARTESIAN_POINT('Ctrl Pts',(-8.78961161023833,8.89048517412593,
11.8226807492016));
#112628=CARTESIAN_POINT('Ctrl Pts',(-8.78771532323919,8.89067011460675,
11.8198838521814));
#112629=CARTESIAN_POINT('Ctrl Pts',(-8.78346090266613,8.89108864016574,
11.8135618363444));
#112630=CARTESIAN_POINT('Ctrl Pts',(-8.78110841061585,8.89132258575099,
11.8100330421049));
#112631=CARTESIAN_POINT('Ctrl Pts',(-8.77508665612442,8.8919278564787,11.8009146379893));
#112632=CARTESIAN_POINT('Ctrl Pts',(-8.77144034181243,8.89230060816078,
11.79531007802));
#112633=CARTESIAN_POINT('Ctrl Pts',(-8.74847242949861,8.89468772120599,
11.7594724196399));
#112634=CARTESIAN_POINT('Ctrl Pts',(-8.7302311108433,8.89676245761913,11.7285644700424));
#112635=CARTESIAN_POINT('Ctrl Pts',(-8.7084402559117,8.8994536989981,11.6883336905298));
#112636=CARTESIAN_POINT('Ctrl Pts',(-8.70382339198042,8.90003742114885,
11.6795999097701));
#112637=CARTESIAN_POINT('Ctrl Pts',(-8.69462145491289,8.90122796725129,
11.6617575692998));
#112638=CARTESIAN_POINT('Ctrl Pts',(-8.69004243253148,8.90183489911153,
11.6526464534744));
#112639=CARTESIAN_POINT('Ctrl Pts',(-8.63897856300995,8.90876657860311,
11.5483392932407));
#112640=CARTESIAN_POINT('Ctrl Pts',(-8.60286173223419,8.91521933920611,
11.4484015389924));
#112641=CARTESIAN_POINT('Ctrl Pts',(-8.56670818222448,8.92411858355313,
11.2995593829959));
#112642=CARTESIAN_POINT('Ctrl Pts',(-8.55779018093599,8.92680278988726,
11.2531655512976));
#112643=CARTESIAN_POINT('Ctrl Pts',(-8.54951362092497,8.93005185553253,
11.1950714409487));
#112644=CARTESIAN_POINT('Ctrl Pts',(-8.54803043389354,8.93068228772016,
11.1837062669191));
#112645=CARTESIAN_POINT('Ctrl Pts',(-8.54588049215706,8.93168000932376,
11.1655744897553));
#112646=CARTESIAN_POINT('Ctrl Pts',(-8.54512713732619,8.9320499736209,11.1588187972773));
#112647=CARTESIAN_POINT('Ctrl Pts',(-8.54379218718497,8.93274650191618,
11.1460399543327));
#112648=CARTESIAN_POINT('Ctrl Pts',(-8.54320082802234,8.93307336205915,
11.1400179859969));
#112649=CARTESIAN_POINT('Ctrl Pts',(-8.54194655786245,8.9338107748212,11.1263760647004));
#112650=CARTESIAN_POINT('Ctrl Pts',(-8.54130599765319,8.93422062743271,
11.1187542015309));
#112651=CARTESIAN_POINT('Ctrl Pts',(-8.53980724165087,8.93527358788995,
11.0990732447401));
#112652=CARTESIAN_POINT('Ctrl Pts',(-8.53903865340875,8.93591392923553,
11.0870077847237));
#112653=CARTESIAN_POINT('Ctrl Pts',(-8.53364145529618,8.94145882479623,
10.9817358816986));
#112654=CARTESIAN_POINT('Ctrl Pts',(-8.53778769339262,8.94607392746065,
10.888291387662));
#112655=CARTESIAN_POINT('Ctrl Pts',(-8.56015387701888,8.95389287733966,
10.7295064786447));
#112656=CARTESIAN_POINT('Ctrl Pts',(-8.57404851758469,8.95712410389077,
10.6638671253848));
#112657=CARTESIAN_POINT('Ctrl Pts',(-8.60474886444194,8.96272212291293,
10.5559900325723));
#112658=CARTESIAN_POINT('Ctrl Pts',(-8.61910838052428,8.96502504122162,
10.5131651215242));
#112659=CARTESIAN_POINT('Ctrl Pts',(-8.63812836538541,8.9678304599192,10.4640951956629));
#112660=CARTESIAN_POINT('Ctrl Pts',(-8.64088779888032,8.96823239288008,
10.4571350734028));
#112661=CARTESIAN_POINT('Ctrl Pts',(-8.64521139180291,8.96885494346698,
10.4464692847369));
#112662=CARTESIAN_POINT('Ctrl Pts',(-8.64673766554276,8.96907338166948,
10.4427482804031));
#112663=CARTESIAN_POINT('Ctrl Pts',(-8.64957503619267,8.96947712342239,
10.4359112698022));
#112664=CARTESIAN_POINT('Ctrl Pts',(-8.65088160793411,8.9696621589135,10.4327934750273));
#112665=CARTESIAN_POINT('Ctrl Pts',(-8.65386219391348,8.97008228155642,
10.4257496427532));
#112666=CARTESIAN_POINT('Ctrl Pts',(-8.65554257793381,8.97031774180539,
10.4218264057545));
#112667=CARTESIAN_POINT('Ctrl Pts',(-8.65993479842792,8.97092951269295,
10.4116944605255));
#112668=CARTESIAN_POINT('Ctrl Pts',(-8.66267260126068,8.97130730002528,
10.4054972016335));
#112669=CARTESIAN_POINT('Ctrl Pts',(-8.68092221578194,8.97380155779059,
10.3649515955078));
#112670=CARTESIAN_POINT('Ctrl Pts',(-8.69771178667431,8.97598460022114,
10.33119686408));
#112671=CARTESIAN_POINT('Ctrl Pts',(-8.76536318953748,8.98429693210015,
10.2074145363756));
#112672=CARTESIAN_POINT('Ctrl Pts',(-8.82441523068524,8.99062442433493,
10.1222062472152));
#112673=CARTESIAN_POINT('Ctrl Pts',(-8.92055331120898,8.99931240625607,
10.0107865307667));
#112674=CARTESIAN_POINT('Ctrl Pts',(-8.95062428422832,9.00185631380975,
9.97894194674716));
#112675=CARTESIAN_POINT('Ctrl Pts',(-8.99547335236816,9.00540419184556,
9.93552549884425));
#112676=CARTESIAN_POINT('Ctrl Pts',(-9.00911384962417,9.00645347463193,
9.92281643604425));
#112677=CARTESIAN_POINT('Ctrl Pts',(-9.03386443242001,9.00830542903683,
9.900624046293));
#112678=CARTESIAN_POINT('Ctrl Pts',(-9.04488049422913,9.00911214541781,
9.89104004859289));
#112679=CARTESIAN_POINT('Ctrl Pts',(-9.06174108829313,9.01032102002174,
9.87680894188968));
#112680=CARTESIAN_POINT('Ctrl Pts',(-9.06748056118138,9.01072812214244,
9.8720392571041));
#112681=CARTESIAN_POINT('Ctrl Pts',(-9.07788395267128,9.01145823019151,
9.8635273889857));
#112682=CARTESIAN_POINT('Ctrl Pts',(-9.08253477084014,9.01178185911014,
9.85976951668824));
#112683=CARTESIAN_POINT('Ctrl Pts',(-9.09260340951733,9.01247662375643,
9.85173552149119));
#112684=CARTESIAN_POINT('Ctrl Pts',(-9.09802872746412,9.01284737616267,
9.84746899791573));
#112685=CARTESIAN_POINT('Ctrl Pts',(-9.11268086756289,9.01383916048615,
9.83611323901252));
#112686=CARTESIAN_POINT('Ctrl Pts',(-9.12196249051524,9.01445741524365,
9.82909531666123));
#112687=CARTESIAN_POINT('Ctrl Pts',(-9.1677059456582,9.01745740504885,9.79535807532475));
#112688=CARTESIAN_POINT('Ctrl Pts',(-9.2053102239292,9.0197786039421,9.77022594637324));
#112689=CARTESIAN_POINT('Ctrl Pts',(-9.3391211136247,9.02764206083292,9.68950121096527));
#112690=CARTESIAN_POINT('Ctrl Pts',(-9.44043796494813,9.03289712536169,
9.64314437965328));
#112691=CARTESIAN_POINT('Ctrl Pts',(-9.59527745331882,9.04097295544686,
9.59262071072323));
#112692=CARTESIAN_POINT('Ctrl Pts',(-9.64534851713804,9.04359684584337,
9.57917696428167));
#112693=CARTESIAN_POINT('Ctrl Pts',(-9.70355718614101,9.0467667935509,9.56681708944067));
#112694=CARTESIAN_POINT('Ctrl Pts',(-9.71110523292502,9.04718013548706,
9.56527654042919));
#112695=CARTESIAN_POINT('Ctrl Pts',(-9.72265669218006,9.0478166773709,9.56301374911531));
#112696=CARTESIAN_POINT('Ctrl Pts',(-9.72665165185683,9.0480375419899,9.56224846535303));
#112697=CARTESIAN_POINT('Ctrl Pts',(-9.73397012071315,9.04844355581598,
9.56087812709937));
#112698=CARTESIAN_POINT('Ctrl Pts',(-9.73729257994235,9.04862841496215,
9.56026791637773));
#112699=CARTESIAN_POINT('Ctrl Pts',(-9.74476413251379,9.04904532915929,
9.55892239723007));
#112700=CARTESIAN_POINT('Ctrl Pts',(-9.74891427580035,9.0492777318521,9.55819350693232));
#112701=CARTESIAN_POINT('Ctrl Pts',(-9.76110006292114,9.04996241823258,
9.55610752354358));
#112702=CARTESIAN_POINT('Ctrl Pts',(-9.76914383108824,9.05041730299622,
9.55479963789781));
#112703=CARTESIAN_POINT('Ctrl Pts',(-9.84509082859884,9.05473706674155,
9.54310116565416));
#112704=CARTESIAN_POINT('Ctrl Pts',(-9.91362943967456,9.05881898805314,
9.53743741322794));
#112705=CARTESIAN_POINT('Ctrl Pts',(-10.0644830973373,9.06787544526682,
9.53561326795602));
#112706=CARTESIAN_POINT('Ctrl Pts',(-10.1466056423097,9.0728468720453,9.54154360736761));
#112707=CARTESIAN_POINT('Ctrl Pts',(-10.2829361158806,9.08092925426571,
9.56302574385637));
#112708=CARTESIAN_POINT('Ctrl Pts',(-10.3375355136485,9.08412158034588,
9.57486184063684));
#112709=CARTESIAN_POINT('Ctrl Pts',(-10.4029015224438,9.0878818765142,9.59300077761915));
#112710=CARTESIAN_POINT('Ctrl Pts',(-10.4144328138846,9.08854297785567,
9.59635406766419));
#112711=CARTESIAN_POINT('Ctrl Pts',(-10.4325392255552,9.08957769580528,
9.60186198420036));
#112712=CARTESIAN_POINT('Ctrl Pts',(-10.4391423997892,9.08995433923746,
9.60392190481373));
#112713=CARTESIAN_POINT('Ctrl Pts',(-10.4514792438239,9.09065677850308,
9.60786668541154));
#112714=CARTESIAN_POINT('Ctrl Pts',(-10.4572163186318,9.09098292821465,
9.60974034343602));
#112715=CARTESIAN_POINT('Ctrl Pts',(-10.4700273770158,9.09171015477695,
9.61401215588393));
#112716=CARTESIAN_POINT('Ctrl Pts',(-10.4770949499233,9.09211061138931,
9.61642909442921));
#112717=CARTESIAN_POINT('Ctrl Pts',(-10.4949950746895,9.0931231428494,9.62270397302916));
#112718=CARTESIAN_POINT('Ctrl Pts',(-10.5058013361027,9.09373280304401,
9.62663570448953));
#112719=CARTESIAN_POINT('Ctrl Pts',(-10.5737487475284,9.09755788824588,
9.65226836083816));
#112720=CARTESIAN_POINT('Ctrl Pts',(-10.6295325247783,9.10065724523289,
9.67740478646118));
#112721=CARTESIAN_POINT('Ctrl Pts',(-10.770686464596,9.10857407175856,9.7519702463093));
#112722=CARTESIAN_POINT('Ctrl Pts',(-10.8529147033749,9.1132521137058,9.8066555115232));
#112723=CARTESIAN_POINT('Ctrl Pts',(-10.9535202924956,9.11973879195422,
9.88930814693232));
#112724=CARTESIAN_POINT('Ctrl Pts',(-10.977355019592,9.12134193643803,9.9102228244174));
#112725=CARTESIAN_POINT('Ctrl Pts',(-11.0140058537742,9.12394832660967,
9.94455350009359));
#112726=CARTESIAN_POINT('Ctrl Pts',(-11.0272791109758,9.12492361087835,
9.95746810547042));
#112727=CARTESIAN_POINT('Ctrl Pts',(-11.0443394244582,9.12622464198219,
9.97470962761396));
#112728=CARTESIAN_POINT('Ctrl Pts',(-11.0483516192572,9.12653416330093,
9.97881242594844));
#112729=CARTESIAN_POINT('Ctrl Pts',(-11.0548683111548,9.12704293878031,
9.98555515819117));
#112730=CARTESIAN_POINT('Ctrl Pts',(-11.0573873129517,9.12724110035875,
9.98818106324872));
#112731=CARTESIAN_POINT('Ctrl Pts',(-11.062275548278,9.1276286323657,9.99331493866138));
#112732=CARTESIAN_POINT('Ctrl Pts',(-11.0646457430461,9.12781792729118,
9.99582193102718));
#112733=CARTESIAN_POINT('Ctrl Pts',(-11.0704353729412,9.12828368277919,
10.0019892519744));
#112734=CARTESIAN_POINT('Ctrl Pts',(-11.0738449083667,9.12856087398673,
10.0056587848762));
#112735=CARTESIAN_POINT('Ctrl Pts',(-11.0853770600799,9.12950813445925,
10.0181988232992));
#112736=CARTESIAN_POINT('Ctrl Pts',(-11.0934089238754,9.1301844296147,10.0271516976484));
#112737=CARTESIAN_POINT('Ctrl Pts',(-11.1509120965089,9.13514147027932,
10.0928604280109));
#112738=CARTESIAN_POINT('Ctrl Pts',(-11.1960448076829,9.13965697341427,
10.1532557705715));
#112739=CARTESIAN_POINT('Ctrl Pts',(-11.2709985495337,9.14808450829513,
10.2715820004104));
#112740=CARTESIAN_POINT('Ctrl Pts',(-11.3019984404251,9.15198435365961,
10.3285604992716));
#112741=CARTESIAN_POINT('Ctrl Pts',(-11.3458115499405,9.1581367030656,10.4236204225296));
#112742=CARTESIAN_POINT('Ctrl Pts',(-11.3610158206485,9.160444404595,10.4605016510532));
#112743=CARTESIAN_POINT('Ctrl Pts',(-11.3836289358003,9.16418217027848,
10.5224213487448));
#112744=CARTESIAN_POINT('Ctrl Pts',(-11.3919080509611,9.16563842225506,
10.547117565857));
#112745=CARTESIAN_POINT('Ctrl Pts',(-11.4022628869522,9.16758946938339,
10.5809788094145));
#112746=CARTESIAN_POINT('Ctrl Pts',(-11.4049156834548,9.16810273015466,
10.58996111116));
#112747=CARTESIAN_POINT('Ctrl Pts',(-11.4092204660547,9.16895899714929,
10.6050694084826));
#112748=CARTESIAN_POINT('Ctrl Pts',(-11.4109191454895,9.16930349360786,
10.6111817124785));
#112749=CARTESIAN_POINT('Ctrl Pts',(-11.4141892089613,9.16998006981207,
10.6232519488273));
#112750=CARTESIAN_POINT('Ctrl Pts',(-11.415762815904,9.17031221466447,10.6292091377886));
#112751=CARTESIAN_POINT('Ctrl Pts',(-11.4191418914766,9.17104030793275,
10.6423364584381));
#112752=CARTESIAN_POINT('Ctrl Pts',(-11.4209307451835,9.17143572145567,
10.6495107174242));
#112753=CARTESIAN_POINT('Ctrl Pts',(-11.4270232309098,9.17281873590946,
10.6747583863271));
#112754=CARTESIAN_POINT('Ctrl Pts',(-11.4310371148213,9.17379718903327,
10.6929003002947));
#112755=CARTESIAN_POINT('Ctrl Pts',(-11.4538534043649,9.17982202874215,
10.8062137438306));
#112756=CARTESIAN_POINT('Ctrl Pts',(-11.4634999999959,9.18456812665941,
10.9029819768369));
#112757=CARTESIAN_POINT('Ctrl Pts',(-11.4635,9.18928959125266,10.9999999999375));
#112758=CARTESIAN_POINT('Origin',(-10.,3.5,11.));
#112759=CARTESIAN_POINT('',(-11.4634998211562,9.76065504584291,10.9992764838212));
#112760=CARTESIAN_POINT('',(-11.4634998339897,9.68830622417397,10.9993269840173));
#112761=CARTESIAN_POINT('',(-11.4635,3.5,11.));
#112762=CARTESIAN_POINT('Ctrl Pts',(-11.4634998211562,9.76065504584291,
10.9992764838212));
#112763=CARTESIAN_POINT('Ctrl Pts',(-11.4634788673927,9.758339008624,10.9568920423594));
#112764=CARTESIAN_POINT('Ctrl Pts',(-11.4616168184814,9.75602297140509,
10.9145549795653));
#112765=CARTESIAN_POINT('Ctrl Pts',(-11.4579250610406,9.75370693418618,
10.8723803839928));
#112766=CARTESIAN_POINT('Ctrl Pts',(-11.4531267995415,9.75069672769344,
10.8175650984766));
#112767=CARTESIAN_POINT('Ctrl Pts',(-11.4452227348698,9.74768652120071,
10.7629056994581));
#112768=CARTESIAN_POINT('Ctrl Pts',(-11.4342328984321,9.74467631470797,
10.708781451389));
#112769=CARTESIAN_POINT('Ctrl Pts',(-11.4232625847686,9.74167145566349,
10.6547533517458));
#112770=CARTESIAN_POINT('Ctrl Pts',(-11.4092174820364,9.738666596619,10.601259029792));
#112771=CARTESIAN_POINT('Ctrl Pts',(-11.3921693129869,9.73566173757451,
10.5486721214265));
#112772=CARTESIAN_POINT('Ctrl Pts',(-11.3751380014157,9.73265984977849,
10.4961372117633));
#112773=CARTESIAN_POINT('Ctrl Pts',(-11.3551096679902,9.72965796198248,
10.444508438124));
#112774=CARTESIAN_POINT('Ctrl Pts',(-11.3322065426073,9.72665607418646,
10.3941469007801));
#112775=CARTESIAN_POINT('Ctrl Pts',(-11.3093170193905,9.72365596921159,
10.3438152731531));
#112776=CARTESIAN_POINT('Ctrl Pts',(-11.2835563064641,9.72065586423672,
10.2947498698395));
#112777=CARTESIAN_POINT('Ctrl Pts',(-11.255094875594,9.71765575926185,10.2472921527859));
#112778=CARTESIAN_POINT('Ctrl Pts',(-11.2266391087995,9.7146562513343,10.1998438802362));
#112779=CARTESIAN_POINT('Ctrl Pts',(-11.1954839629081,9.71165674340675,
10.1540031111753));
#112780=CARTESIAN_POINT('Ctrl Pts',(-11.1618448678258,9.70865723547921,
10.1100849742212));
#112781=CARTESIAN_POINT('Ctrl Pts',(-11.128174854497,9.70565497065451,10.0661264713839));
#112782=CARTESIAN_POINT('Ctrl Pts',(-11.092016652586,9.70265270582982,10.0240945512531));
#112783=CARTESIAN_POINT('Ctrl Pts',(-11.0536269897426,9.69965044100512,
9.98427246936693));
#112784=CARTESIAN_POINT('Ctrl Pts',(-11.0152198424233,9.69664680880643,
9.94443225061321));
#112785=CARTESIAN_POINT('Ctrl Pts',(-10.9745795963937,9.69364317660773,
9.90680423581745));
#112786=CARTESIAN_POINT('Ctrl Pts',(-10.9319986021011,9.69063954440904,
9.87163354548196));
#112787=CARTESIAN_POINT('Ctrl Pts',(-10.889337309732,9.68763024804275,9.83639653121886));
#112788=CARTESIAN_POINT('Ctrl Pts',(-10.8447283847183,9.68462095167646,
9.80362641182894));
#112789=CARTESIAN_POINT('Ctrl Pts',(-10.7984949412382,9.68161165531017,
9.77352616056561));
#112790=CARTESIAN_POINT('Ctrl Pts',(-10.7632188166337,9.67931556171214,
9.75055966414512));
#112791=CARTESIAN_POINT('Ctrl Pts',(-10.7269975994523,9.67701946811412,
9.72914661305899));
#112792=CARTESIAN_POINT('Ctrl Pts',(-10.6899836595581,9.6747233745161,9.70935876420177));
#112793=CARTESIAN_POINT('Ctrl Pts',(-10.6414579364402,9.67171316802338,
9.68341665489134));
#112794=CARTESIAN_POINT('Ctrl Pts',(-10.591365224381,9.66870296153067,9.66016059465073));
#112795=CARTESIAN_POINT('Ctrl Pts',(-10.5400340736877,9.66569275503795,
9.63978110244849));
#112796=CARTESIAN_POINT('Ctrl Pts',(-10.488794109653,9.66268789599348,9.61943781317125));
#112797=CARTESIAN_POINT('Ctrl Pts',(-10.4363205597793,9.65968303694902,
9.6019611442763));
#112798=CARTESIAN_POINT('Ctrl Pts',(-10.3829655137402,9.65667817790455,
9.58749525123428));
#112799=CARTESIAN_POINT('Ctrl Pts',(-10.3296632259492,9.65367629010856,
9.57304366227838));
#112800=CARTESIAN_POINT('Ctrl Pts',(-10.2754816758471,9.65067440231256,
9.5615970891755));
#112801=CARTESIAN_POINT('Ctrl Pts',(-10.220790061141,9.64767251451656,9.55325054038325));
#112802=CARTESIAN_POINT('Ctrl Pts',(-10.1661309277846,9.64467240954171,
9.54490894860629));
#112803=CARTESIAN_POINT('Ctrl Pts',(-10.1109628512463,9.64167230456686,
9.5396638114467));
#112804=CARTESIAN_POINT('Ctrl Pts',(-10.0556649512334,9.63867219959201,
9.53755900522306));
#112805=CARTESIAN_POINT('Ctrl Pts',(-10.0003780559899,9.63567269166448,
9.53545461787439));
#112806=CARTESIAN_POINT('Ctrl Pts',(-9.94496191598655,9.63267318373695,
9.53648934039428));
#112807=CARTESIAN_POINT('Ctrl Pts',(-9.88979817165473,9.62967367580942,
9.54065500753613));
#112808=CARTESIAN_POINT('Ctrl Pts',(-9.83458372541682,9.62667141098474,
9.54482450341128));
#112809=CARTESIAN_POINT('Ctrl Pts',(-9.77962266602956,9.62366914616006,
9.55213065330776));
#112810=CARTESIAN_POINT('Ctrl Pts',(-9.72529251492394,9.62066688133539,
9.5625132878377));
#112811=CARTESIAN_POINT('Ctrl Pts',(-9.67093761928698,9.61766324913671,
9.57290065111255));
#112812=CARTESIAN_POINT('Ctrl Pts',(-9.61721471785987,9.61465961693804,
9.58636716354264));
#112813=CARTESIAN_POINT('Ctrl Pts',(-9.56448886747576,9.61165598473936,
9.60280198130421));
#112814=CARTESIAN_POINT('Ctrl Pts',(-9.51166358812249,9.60864668837309,
9.61926779139641));
#112815=CARTESIAN_POINT('Ctrl Pts',(-9.45983961144264,9.60563739200682,
9.63871290278073));
#112816=CARTESIAN_POINT('Ctrl Pts',(-9.40936351397626,9.60262809564055,
9.66097767330879));
#112817=CARTESIAN_POINT('Ctrl Pts',(-9.37085024371385,9.60033200204236,
9.6779656967044));
#112818=CARTESIAN_POINT('Ctrl Pts',(-9.33312129533429,9.59803590844418,
9.6965942174547));
#112819=CARTESIAN_POINT('Ctrl Pts',(-9.29632003954256,9.59573981484599,
9.71677485870537));
#112820=CARTESIAN_POINT('Ctrl Pts',(-9.2480731478601,9.59272960835328,9.74323192359506));
#112821=CARTESIAN_POINT('Ctrl Pts',(-9.20121912931898,9.58971940186056,
9.77246931550857));
#112822=CARTESIAN_POINT('Ctrl Pts',(-9.15609710226321,9.58670919536784,
9.80431603289521));
#112823=CARTESIAN_POINT('Ctrl Pts',(-9.11105523173663,9.58370433632337,
9.83610617653066));
#112824=CARTESIAN_POINT('Ctrl Pts',(-9.06773967475705,9.58069947727891,
9.87049614477097));
#112825=CARTESIAN_POINT('Ctrl Pts',(-9.02646359002306,9.57769461823444,
9.90726988306847));
#112826=CARTESIAN_POINT('Ctrl Pts',(-8.98522831968392,9.57469273043844,
9.94400725895696));
#112827=CARTESIAN_POINT('Ctrl Pts',(-8.94602891903112,9.57169084264244,
9.98312338601127));
#112828=CARTESIAN_POINT('Ctrl Pts',(-8.90914674100313,9.56868895484644,
10.0243610210042));
#112829=CARTESIAN_POINT('Ctrl Pts',(-8.87228646730048,9.56568884987159,
10.065574164966));
#112830=CARTESIAN_POINT('Ctrl Pts',(-8.83774103984014,9.56268874489674,
10.1089059266928));
#112831=CARTESIAN_POINT('Ctrl Pts',(-8.80575441577487,9.55968863992189,
10.1540628069657));
#112832=CARTESIAN_POINT('Ctrl Pts',(-8.77377415732961,9.55668913199436,
10.1992107006215));
#112833=CARTESIAN_POINT('Ctrl Pts',(-8.74435199604565,9.55368962406683,
10.2461825608034));
#112834=CARTESIAN_POINT('Ctrl Pts',(-8.71768968642659,9.55069011613929,
10.2946543331789));
#112835=CARTESIAN_POINT('Ctrl Pts',(-8.69100287103957,9.54768785131462,
10.3431706567589));
#112836=CARTESIAN_POINT('Ctrl Pts',(-8.66708123020108,9.54468558648994,
10.3931891830754));
#112837=CARTESIAN_POINT('Ctrl Pts',(-8.64608071804832,9.54168332166527,
10.4443608833429));
#112838=CARTESIAN_POINT('Ctrl Pts',(-8.62507064126487,9.53867968946659,
10.4955558896332));
#112839=CARTESIAN_POINT('Ctrl Pts',(-8.60698451801093,9.53567605726792,
10.5479046168425));
#112840=CARTESIAN_POINT('Ctrl Pts',(-8.59192905414153,9.53267242506924,
10.601040777235));
#112841=CARTESIAN_POINT('Ctrl Pts',(-8.57684519908939,9.52966312870297,
10.6542771403482));
#112842=CARTESIAN_POINT('Ctrl Pts',(-8.56480353540812,9.52665383233669,
10.7083033862982));
#112843=CARTESIAN_POINT('Ctrl Pts',(-8.55585980377181,9.52364453597042,
10.7627420314552));
#112844=CARTESIAN_POINT('Ctrl Pts',(-8.54903573513436,9.52134844237225,
10.804278726225));
#112845=CARTESIAN_POINT('Ctrl Pts',(-8.54401412856267,9.51905234877408,
10.8460552602913));
#112846=CARTESIAN_POINT('Ctrl Pts',(-8.54079933768928,9.51675625517591,
10.8879032689506));
#112847=CARTESIAN_POINT('Ctrl Pts',(-8.53658470795139,9.51374604868319,
10.9427665147148));
#112848=CARTESIAN_POINT('Ctrl Pts',(-8.53545966515834,9.51073584219047,
10.9979829834363));
#112849=CARTESIAN_POINT('Ctrl Pts',(-8.53746636104217,9.50772563569775,
11.053175228413));
#112850=CARTESIAN_POINT('Ctrl Pts',(-8.53946949215315,9.50472077665328,
11.1082694277325));
#112851=CARTESIAN_POINT('Ctrl Pts',(-8.54459330239428,9.50171591760881,
11.1633389652341));
#112852=CARTESIAN_POINT('Ctrl Pts',(-8.55282802674087,9.49871105856434,
11.2180035087178));
#112853=CARTESIAN_POINT('Ctrl Pts',(-8.56105460847188,9.49570917076833,
11.2726139991033));
#112854=CARTESIAN_POINT('Ctrl Pts',(-8.57238593237142,9.49270728297233,
11.3268197691464));
#112855=CARTESIAN_POINT('Ctrl Pts',(-8.58676035740054,9.48970539517632,
11.380244608884));
#112856=CARTESIAN_POINT('Ctrl Pts',(-8.6011262454587,9.48670529020147,11.4336377196096));
#112857=CARTESIAN_POINT('Ctrl Pts',(-8.61853151551821,9.48370518522661,
11.4862503103739));
#112858=CARTESIAN_POINT('Ctrl Pts',(-8.63886372590758,9.48070508025175,
11.5377176706691));
#112859=CARTESIAN_POINT('Ctrl Pts',(-8.65919189000795,9.47770557232422,
11.5891747885062));
#112860=CARTESIAN_POINT('Ctrl Pts',(-8.68244564371486,9.47470606439668,
11.6394866376286));
#112861=CARTESIAN_POINT('Ctrl Pts',(-8.70846389145155,9.47170655646915,
11.688307148238));
#112862=CARTESIAN_POINT('Ctrl Pts',(-8.73450605298833,9.46870429164447,
11.7371725305829));
#112863=CARTESIAN_POINT('Ctrl Pts',(-8.76331753600472,9.46570202681979,
11.7845433688876));
#112864=CARTESIAN_POINT('Ctrl Pts',(-8.79469129795319,9.46269976199511,
11.830098297053));
#112865=CARTESIAN_POINT('Ctrl Pts',(-8.82607934900303,9.45969612979643,
11.8756739730964));
#112866=CARTESIAN_POINT('Ctrl Pts',(-8.86003168099162,9.45669249759774,
11.9194316723883));
#112867=CARTESIAN_POINT('Ctrl Pts',(-8.89629988096166,9.45368886539906,
11.9610818369082));
#112868=CARTESIAN_POINT('Ctrl Pts',(-8.93263647451303,9.45067956903279,
12.0028105441711));
#112869=CARTESIAN_POINT('Ctrl Pts',(-8.97129729043019,9.44767027266651,
12.0424233985027));
#112870=CARTESIAN_POINT('Ctrl Pts',(-9.01199668423977,9.44466097630023,
12.0796674015857));
#112871=CARTESIAN_POINT('Ctrl Pts',(-9.04305032808208,9.44236488270209,
12.1080845817632));
#112872=CARTESIAN_POINT('Ctrl Pts',(-9.07528998392297,9.44006878910395,
12.1351234412503));
#112873=CARTESIAN_POINT('Ctrl Pts',(-9.10857704016443,9.43777269550581,
12.160688311597));
#112874=CARTESIAN_POINT('Ctrl Pts',(-9.15221677371128,9.4347624890131,12.194204165988));
#112875=CARTESIAN_POINT('Ctrl Pts',(-9.19784096890391,9.43175228252038,
12.2253258136369));
#112876=CARTESIAN_POINT('Ctrl Pts',(-9.24515658492047,9.42874207602766,
12.2538116559959));
#112877=CARTESIAN_POINT('Ctrl Pts',(-9.29238814763082,9.4257372169832,12.2822468949931));
#112878=CARTESIAN_POINT('Ctrl Pts',(-9.34130471952884,9.42273235793873,
12.308055350696));
#112879=CARTESIAN_POINT('Ctrl Pts',(-9.39158246742835,9.41972749889426,
12.3310373233157));
#112880=CARTESIAN_POINT('Ctrl Pts',(-9.44181049995711,9.41672561109826,
12.3539965710256));
#112881=CARTESIAN_POINT('Ctrl Pts',(-9.49339656428801,9.41372372330227,
12.3741346537078));
#112882=CARTESIAN_POINT('Ctrl Pts',(-9.54599192552215,9.41072183550627,
12.3912975664138));
#112883=CARTESIAN_POINT('Ctrl Pts',(-9.5985560503715,9.40772173053142,12.408450286066));
#112884=CARTESIAN_POINT('Ctrl Pts',(-9.65212778299837,9.40472162555657,
12.4226311744769));
#112885=CARTESIAN_POINT('Ctrl Pts',(-9.70634025235392,9.40172152058171,
12.4337350531435));
#112886=CARTESIAN_POINT('Ctrl Pts',(-9.76054193295044,9.39872201265418,
12.4448367220405));
#112887=CARTESIAN_POINT('Ctrl Pts',(-9.81538357998686,9.39572250472665,
12.4528624914055));
#112888=CARTESIAN_POINT('Ctrl Pts',(-9.87048733978993,9.39272299679912,
12.457758114656));
#112889=CARTESIAN_POINT('Ctrl Pts',(-9.92564174636634,9.38972073197445,
12.4626582375544));
#112890=CARTESIAN_POINT('Ctrl Pts',(-9.98105821987884,9.38671846714977,
12.4644224197221));
#112891=CARTESIAN_POINT('Ctrl Pts',(-10.0363544807912,9.3837162023251,12.4630483935012));
#112892=CARTESIAN_POINT('Ctrl Pts',(-10.0916759262472,9.38071257012642,
12.4616737414834));
#112893=CARTESIAN_POINT('Ctrl Pts',(-10.1468765227223,9.37770893792775,
12.4571580750236));
#112894=CARTESIAN_POINT('Ctrl Pts',(-10.2015780155307,9.37470530572907,
12.4495511559289));
#112895=CARTESIAN_POINT('Ctrl Pts',(-10.2563826629209,9.3716960093628,12.4419298919137));
#112896=CARTESIAN_POINT('Ctrl Pts',(-10.3106858071257,9.36868671299653,
12.4312058327413));
#112897=CARTESIAN_POINT('Ctrl Pts',(-10.3641194595772,9.36567741663025,
12.4174799007948));
#112898=CARTESIAN_POINT('Ctrl Pts',(-10.4048893447556,9.36338132303208,
12.4070070125726));
#112899=CARTESIAN_POINT('Ctrl Pts',(-10.4451532387728,9.36108522943391,
12.3947875948399));
#112900=CARTESIAN_POINT('Ctrl Pts',(-10.4847552668445,9.35878913583574,
12.3808854337948));
#112901=CARTESIAN_POINT('Ctrl Pts',(-10.5366740048791,9.35577892934302,
12.3626595324316));
#112902=CARTESIAN_POINT('Ctrl Pts',(-10.5876724399118,9.3527687228503,12.3414632175733));
#112903=CARTESIAN_POINT('Ctrl Pts',(-10.6373880871114,9.34975851635758,
12.317409836159));
#112904=CARTESIAN_POINT('Ctrl Pts',(-10.6870154174957,9.34675365731311,
12.2933991841099));
#112905=CARTESIAN_POINT('Ctrl Pts',(-10.7353640108114,9.34374879826863,
12.2665417658343));
#112906=CARTESIAN_POINT('Ctrl Pts',(-10.7820896387808,9.34074393922416,
12.2369996147581));
#112907=CARTESIAN_POINT('Ctrl Pts',(-10.8287690637675,9.33774205142816,
12.2074866753919));
#112908=CARTESIAN_POINT('Ctrl Pts',(-10.8738282583114,9.33474016363216,
12.1752945429008));
#112909=CARTESIAN_POINT('Ctrl Pts',(-10.9169476492224,9.33173827583616,
12.1406310790898));
#112910=CARTESIAN_POINT('Ctrl Pts',(-10.9600414315273,9.3287381708613,12.1059882019098));
#112911=CARTESIAN_POINT('Ctrl Pts',(-11.0011972828855,9.32573806588645,
12.068877232753));
#112912=CARTESIAN_POINT('Ctrl Pts',(-11.040126605484,9.32273796091159,12.0295479078529));
#112913=CARTESIAN_POINT('Ctrl Pts',(-11.0790481808044,9.31973845298405,
11.9902264098349));
#112914=CARTESIAN_POINT('Ctrl Pts',(-11.1157437360589,9.31673894505652,
11.948687807931));
#112915=CARTESIAN_POINT('Ctrl Pts',(-11.1499613218517,9.31373943712899,
11.9052188731158));
#112916=CARTESIAN_POINT('Ctrl Pts',(-11.1842103575913,9.31073717230431,
11.8617099852867));
#112917=CARTESIAN_POINT('Ctrl Pts',(-11.2159765463204,9.30773490747963,
11.8162676357775));
#112918=CARTESIAN_POINT('Ctrl Pts',(-11.2450490475493,9.30473264265495,
11.7692107118316));
#112919=CARTESIAN_POINT('Ctrl Pts',(-11.2741347897762,9.30172901045627,
11.7221323559276));
#112920=CARTESIAN_POINT('Ctrl Pts',(-11.3005241468463,9.29872537825759,
11.6734384248046));
#112921=CARTESIAN_POINT('Ctrl Pts',(-11.3240520483837,9.29572174605891,
11.6234728728428));
#112922=CARTESIAN_POINT('Ctrl Pts',(-11.3476243181955,9.29271244969263,
11.5734130972074));
#112923=CARTESIAN_POINT('Ctrl Pts',(-11.368324155093,9.28970315332636,11.5220774013604));
#112924=CARTESIAN_POINT('Ctrl Pts',(-11.386034942466,9.28669385696008,11.4698291053811));
#112925=CARTESIAN_POINT('Ctrl Pts',(-11.3995482760017,9.28439776336194,
11.4299636473769));
#112926=CARTESIAN_POINT('Ctrl Pts',(-11.411322481028,9.2821016697638,11.3895673180003));
#112927=CARTESIAN_POINT('Ctrl Pts',(-11.421325777003,9.27980557616565,11.3488055126096));
#112928=CARTESIAN_POINT('Ctrl Pts',(-11.4384553450834,9.2758737629206,11.2790053065305));
#112929=CARTESIAN_POINT('Ctrl Pts',(-11.4504497976639,9.27194194967556,
11.2078990836009));
#112930=CARTESIAN_POINT('Ctrl Pts',(-11.4571541790753,9.26801013643051,
11.1361394447004));
#112931=CARTESIAN_POINT('Ctrl Pts',(-11.4613346856349,9.26555846042148,
11.0913938339238));
#112932=CARTESIAN_POINT('Ctrl Pts',(-11.4634592272291,9.26310678441244,
11.0463945317134));
#112933=CARTESIAN_POINT('Ctrl Pts',(-11.4634994186103,9.26065510840341,
11.0013045026646));
#112934=CARTESIAN_POINT('Ctrl Pts',(-11.4635,9.18928959125266,10.9999999999375));
#112935=CARTESIAN_POINT('Ctrl Pts',(-11.4635,9.18931070478979,11.0004338470187));
#112936=CARTESIAN_POINT('Ctrl Pts',(-11.4634998070825,9.18933181826334,
11.0008676990741));
#112937=CARTESIAN_POINT('Ctrl Pts',(-11.4634162934266,9.19390164597574,
11.0947723710105));
#112938=CARTESIAN_POINT('Ctrl Pts',(-11.4543786882082,9.19841535153124,
11.1880093984724));
#112939=CARTESIAN_POINT('Ctrl Pts',(-11.4343089561222,9.20394569799821,
11.2910729990247));
#112940=CARTESIAN_POINT('Ctrl Pts',(-11.4319670270922,9.20456026192431,
11.3023840097753));
#112941=CARTESIAN_POINT('Ctrl Pts',(-11.4285379422702,9.20542139636589,
11.3180116245272));
#112942=CARTESIAN_POINT('Ctrl Pts',(-11.427564552336,9.20566191668663,11.3223530575614));
#112943=CARTESIAN_POINT('Ctrl Pts',(-11.4258579286926,9.20607711447965,
11.329805446705));
#112944=CARTESIAN_POINT('Ctrl Pts',(-11.4251342665793,9.20625125777558,
11.3329185896152));
#112945=CARTESIAN_POINT('Ctrl Pts',(-11.4235983581644,9.20661695972425,
11.3394291782735));
#112946=CARTESIAN_POINT('Ctrl Pts',(-11.4227841411512,9.20680863386454,
11.342826106506));
#112947=CARTESIAN_POINT('Ctrl Pts',(-11.420762385351,9.20727923823071,11.3511296450391));
#112948=CARTESIAN_POINT('Ctrl Pts',(-11.419541585996,9.20755890652332,11.3560329582264));
#112949=CARTESIAN_POINT('Ctrl Pts',(-11.4150332432856,9.20857552668693,
11.3737487642164));
#112950=CARTESIAN_POINT('Ctrl Pts',(-11.4115975208428,9.20932024748357,
11.3865224864759));
#112951=CARTESIAN_POINT('Ctrl Pts',(-11.402570587407,9.21120258237549,11.4183569449842));
#112952=CARTESIAN_POINT('Ctrl Pts',(-11.3967636649921,9.21234965395902,
11.4373533841521));
#112953=CARTESIAN_POINT('Ctrl Pts',(-11.3695441099538,9.21744767387213,
11.5203185100442));
#112954=CARTESIAN_POINT('Ctrl Pts',(-11.344110804997,9.22152106032847,11.5828789216155));
#112955=CARTESIAN_POINT('Ctrl Pts',(-11.2697294680659,9.23169700736126,
11.7348247048393));
#112956=CARTESIAN_POINT('Ctrl Pts',(-11.2155934171519,9.23773363401411,
11.8212909808977));
#112957=CARTESIAN_POINT('Ctrl Pts',(-11.1415253723073,9.24447707203091,
11.9160208072718));
#112958=CARTESIAN_POINT('Ctrl Pts',(-11.1298581114288,9.2455036517799,11.9303735737946));
#112959=CARTESIAN_POINT('Ctrl Pts',(-11.1131584311969,9.24692483478562,
11.9501394779548));
#112960=CARTESIAN_POINT('Ctrl Pts',(-11.1083526820278,9.24732845915661,
11.9557411027778));
#112961=CARTESIAN_POINT('Ctrl Pts',(-11.0994597763015,9.24806569146908,
11.9659494663672));
#112962=CARTESIAN_POINT('Ctrl Pts',(-11.0953855429715,9.24839981501118,
11.9705671976394));
#112963=CARTESIAN_POINT('Ctrl Pts',(-11.0870522488457,9.24907594924944,
11.979892830405));
#112964=CARTESIAN_POINT('Ctrl Pts',(-11.0827914562261,9.24941787754999,
11.9845990122182));
#112965=CARTESIAN_POINT('Ctrl Pts',(-11.0721547751027,9.25026226759842,
11.9961950137961));
#112966=CARTESIAN_POINT('Ctrl Pts',(-11.0657429157468,9.25076321014763,
12.0030515491843));
#112967=CARTESIAN_POINT('Ctrl Pts',(-11.0411857703223,9.25265209448541,
12.0288104613804));
#112968=CARTESIAN_POINT('Ctrl Pts',(-11.0225994332753,9.25402118331006,
12.0472866288312));
#112969=CARTESIAN_POINT('Ctrl Pts',(-10.9742545206584,9.25744360974625,
12.0928300974333));
#112970=CARTESIAN_POINT('Ctrl Pts',(-10.9438574363473,9.25946949343498,
12.1191885146192));
#112971=CARTESIAN_POINT('Ctrl Pts',(-10.8620329652188,9.2646643176182,12.1844336850034));
#112972=CARTESIAN_POINT('Ctrl Pts',(-10.8090552544612,9.2677790510141,12.2212345419651));
#112973=CARTESIAN_POINT('Ctrl Pts',(-10.6894606284566,9.27458120824155,
12.2931028859242));
#112974=CARTESIAN_POINT('Ctrl Pts',(-10.6222214494893,9.27826846510201,
12.3267664158778));
#112975=CARTESIAN_POINT('Ctrl Pts',(-10.541561872582,9.28285134077685,12.3596645983925));
#112976=CARTESIAN_POINT('Ctrl Pts',(-10.5303632025621,9.28349113156792,
12.3640718225078));
#112977=CARTESIAN_POINT('Ctrl Pts',(-10.5144274840568,9.28440818493755,
12.3701174091051));
#112978=CARTESIAN_POINT('Ctrl Pts',(-10.5097341265907,9.28467908148262,
12.3718704274806));
#112979=CARTESIAN_POINT('Ctrl Pts',(-10.5017936211981,9.28513890719721,
12.3747899170307));
#112980=CARTESIAN_POINT('Ctrl Pts',(-10.4985511317041,9.28532709887036,
12.3759690850817));
#112981=CARTESIAN_POINT('Ctrl Pts',(-10.491880727274,9.28571516672002,12.3783681797009));
#112982=CARTESIAN_POINT('Ctrl Pts',(-10.4884523992187,9.28591511282023,
12.3795868011033));
#112983=CARTESIAN_POINT('Ctrl Pts',(-10.479606675768,9.2864322164833,12.3826939652239));
#112984=CARTESIAN_POINT('Ctrl Pts',(-10.4741827075524,9.28675045271687,
12.3845634411398));
#112985=CARTESIAN_POINT('Ctrl Pts',(-10.4512170148637,9.28810237555627,
12.3923282382564));
#112986=CARTESIAN_POINT('Ctrl Pts',(-10.4335760114101,9.28915183384186,
12.3979222063333));
#112987=CARTESIAN_POINT('Ctrl Pts',(-10.3854680990713,9.2920344924298,12.4121790612834));
#112988=CARTESIAN_POINT('Ctrl Pts',(-10.3548190891514,9.29389315160753,
12.4201896183692));
#112989=CARTESIAN_POINT('Ctrl Pts',(-10.2281329114532,9.30160436492201,
12.4489440044418));
#112990=CARTESIAN_POINT('Ctrl Pts',(-10.1303818483636,9.30760009445275,
12.4609879686413));
#112991=CARTESIAN_POINT('Ctrl Pts',(-10.0029387493462,9.31510437547275,
12.463788803362));
#112992=CARTESIAN_POINT('Ctrl Pts',(-9.97370791366097,9.3168062485537,12.4635556591013));
#112993=CARTESIAN_POINT('Ctrl Pts',(-9.90883508549313,9.32053474383792,
12.4610938357323));
#112994=CARTESIAN_POINT('Ctrl Pts',(-9.87322733151111,9.32254849869958,
12.458435887098));
#112995=CARTESIAN_POINT('Ctrl Pts',(-9.82694574265264,9.32512362994786,
12.4532730854023));
#112996=CARTESIAN_POINT('Ctrl Pts',(-9.81615495523334,9.32572105737832,
12.4519474663954));
#112997=CARTESIAN_POINT('Ctrl Pts',(-9.79877083918716,9.32667889503289,
12.4496149621946));
#112998=CARTESIAN_POINT('Ctrl Pts',(-9.79216800988718,9.32704162117717,
12.4486830501215));
#112999=CARTESIAN_POINT('Ctrl Pts',(-9.77955896126588,9.32773230034248,
12.4468154494086));
#113000=CARTESIAN_POINT('Ctrl Pts',(-9.7735517648403,9.32806048393344,12.4458874072798));
#113001=CARTESIAN_POINT('Ctrl Pts',(-9.75976705402127,9.32881163979397,
12.4436698136899));
#113002=CARTESIAN_POINT('Ctrl Pts',(-9.75199379129647,9.32923380719507,
12.4423547840332));
#113003=CARTESIAN_POINT('Ctrl Pts',(-9.72773079402021,9.33054736285011,
12.4380481835979));
#113004=CARTESIAN_POINT('Ctrl Pts',(-9.71128126793625,9.33143185376321,
12.4348360961403));
#113005=CARTESIAN_POINT('Ctrl Pts',(-9.62993138743596,9.33578064760873,
12.4174952693153));
#113006=CARTESIAN_POINT('Ctrl Pts',(-9.56598752164667,9.33911357766149,
12.3992419509615));
#113007=CARTESIAN_POINT('Ctrl Pts',(-9.42983710549426,9.34623614843183,
12.3501401484218));
#113008=CARTESIAN_POINT('Ctrl Pts',(-9.35842794888089,9.34998806402997,
12.3177059411876));
#113009=CARTESIAN_POINT('Ctrl Pts',(-9.28291642515852,9.35425842926083,
12.275808858601));
#113010=CARTESIAN_POINT('Ctrl Pts',(-9.27590734334583,9.35465791541158,
12.2718439052434));
#113011=CARTESIAN_POINT('Ctrl Pts',(-9.25760927934127,9.35570986764527,
12.2612926236925));
#113012=CARTESIAN_POINT('Ctrl Pts',(-9.24637531821011,9.35636483054804,
12.2546126459496));
#113013=CARTESIAN_POINT('Ctrl Pts',(-9.20580473223473,9.35876890977939,
12.2297468975157));
#113014=CARTESIAN_POINT('Ctrl Pts',(-9.17702627751852,9.36054894780729,
12.2106764471404));
#113015=CARTESIAN_POINT('Ctrl Pts',(-9.14356918399046,9.36274229331912,
12.1867612523143));
#113016=CARTESIAN_POINT('Ctrl Pts',(-9.13821362696425,9.36309730717949,
12.1828779550769));
#113017=CARTESIAN_POINT('Ctrl Pts',(-9.12948555959472,9.36368265598932,
12.1764585259247));
#113018=CARTESIAN_POINT('Ctrl Pts',(-9.12609730860128,9.36391158083808,
12.1739438399));
#113019=CARTESIAN_POINT('Ctrl Pts',(-9.12001594450787,9.36432561183346,
12.1693894668398));
#113020=CARTESIAN_POINT('Ctrl Pts',(-9.11731897034202,9.36451035657473,
12.1673550713338));
#113021=CARTESIAN_POINT('Ctrl Pts',(-9.11139422199671,9.36491871437721,
12.1628536131513));
#113022=CARTESIAN_POINT('Ctrl Pts',(-9.1081697048281,9.36514260308794,12.1603824706177));
#113023=CARTESIAN_POINT('Ctrl Pts',(-9.09887963399047,9.36579229968712,
12.1532013315938));
#113024=CARTESIAN_POINT('Ctrl Pts',(-9.09284090357253,9.36622039108618,
12.1484570491762));
#113025=CARTESIAN_POINT('Ctrl Pts',(-9.04700269876655,9.36951246213953,
12.1118575224423));
#113026=CARTESIAN_POINT('Ctrl Pts',(-9.00885816539702,9.37249805186184,
12.0779925298275));
#113027=CARTESIAN_POINT('Ctrl Pts',(-8.89503119094708,9.38201322418886,
11.9657789385272));
#113028=CARTESIAN_POINT('Ctrl Pts',(-8.82626172405252,9.38865873790665,
11.8809242442921));
#113029=CARTESIAN_POINT('Ctrl Pts',(-8.74172123076185,9.39777969282462,
11.7489053036056));
#113030=CARTESIAN_POINT('Ctrl Pts',(-8.71789397169585,9.40050555926008,
11.7073397160796));
#113031=CARTESIAN_POINT('Ctrl Pts',(-8.69076981891896,9.40381589248003,
11.6541320055381));
#113032=CARTESIAN_POINT('Ctrl Pts',(-8.68552215720694,9.40446754798275,
11.6435218411537));
#113033=CARTESIAN_POINT('Ctrl Pts',(-8.67739932184916,9.40549468991658,
11.6265843657826));
#113034=CARTESIAN_POINT('Ctrl Pts',(-8.67443957646659,9.40587306025991,
11.6202983855893));
#113035=CARTESIAN_POINT('Ctrl Pts',(-8.6689938842059,9.40657709237264,11.6085157014111));
#113036=CARTESIAN_POINT('Ctrl Pts',(-8.66649695178861,9.40690312262903,
11.6030242624107));
#113037=CARTESIAN_POINT('Ctrl Pts',(-8.66100150152525,9.40762802784437,
11.5907372000281));
#113038=CARTESIAN_POINT('Ctrl Pts',(-8.6580206091867,9.40802630112904,11.5839338454001));
#113039=CARTESIAN_POINT('Ctrl Pts',(-8.64940198222725,9.40919317617536,
11.5638487596563));
#113040=CARTESIAN_POINT('Ctrl Pts',(-8.64390862909211,9.40995694614799,
11.550505806135));
#113041=CARTESIAN_POINT('Ctrl Pts',(-8.60151729682826,9.41602161482387,
11.4430532479255));
#113042=CARTESIAN_POINT('Ctrl Pts',(-8.57426149988435,9.42098098231308,
11.3454310961212));
#113043=CARTESIAN_POINT('Ctrl Pts',(-8.54108168023866,9.43059822153739,
11.1506589601929));
#113044=CARTESIAN_POINT('Ctrl Pts',(-8.53432621167576,9.43524501531815,
11.0541906260235));
#113045=CARTESIAN_POINT('Ctrl Pts',(-8.53743741546067,9.44092691352552,
10.9464066532307));
#113046=CARTESIAN_POINT('Ctrl Pts',(-8.53789797794449,9.44153212453165,
10.9350444613398));
#113047=CARTESIAN_POINT('Ctrl Pts',(-8.53872145120537,9.44238225341211,
10.9192732637801));
#113048=CARTESIAN_POINT('Ctrl Pts',(-8.53897202985836,9.44262132283926,
10.9148585144847));
#113049=CARTESIAN_POINT('Ctrl Pts',(-8.53943775171228,9.44303468400678,
10.9072619890059));
#113050=CARTESIAN_POINT('Ctrl Pts',(-8.53964329634233,9.44320845230994,
10.904079629436));
#113051=CARTESIAN_POINT('Ctrl Pts',(-8.5400962386056,9.44357415971811,10.8974061066962));
#113052=CARTESIAN_POINT('Ctrl Pts',(-8.54034575996971,9.44376621945698,
10.8939151366112));
#113053=CARTESIAN_POINT('Ctrl Pts',(-8.54098868169338,9.44423911521611,
10.8853522689456));
#113054=CARTESIAN_POINT('Ctrl Pts',(-8.54139600815837,9.44452070550036,
10.8802814859852));
#113055=CARTESIAN_POINT('Ctrl Pts',(-8.54297716284364,9.44555212077781,
10.8618052597239));
#113056=CARTESIAN_POINT('Ctrl Pts',(-8.54430939767145,9.44631000629406,
10.8484144521639));
#113057=CARTESIAN_POINT('Ctrl Pts',(-8.54811723558188,9.44823272578966,
10.8148462717941));
#113058=CARTESIAN_POINT('Ctrl Pts',(-8.55082890820206,9.44940751090486,
10.7946989051811));
#113059=CARTESIAN_POINT('Ctrl Pts',(-8.57495946714656,9.45856346935995,
10.6398800551122));
#113060=CARTESIAN_POINT('Ctrl Pts',(-8.61468658402728,9.46699182855886,
10.5087347512731));
#113061=CARTESIAN_POINT('Ctrl Pts',(-8.69019306789367,9.47739765970247,
10.345697823823));
#113062=CARTESIAN_POINT('Ctrl Pts',(-8.71011628315959,9.47985374951358,
10.3072474643031));
#113063=CARTESIAN_POINT('Ctrl Pts',(-8.73751678925365,9.48289522273003,
10.2596598589567));
#113064=CARTESIAN_POINT('Ctrl Pts',(-8.74343724761085,9.48353482422218,
10.2496551179159));
#113065=CARTESIAN_POINT('Ctrl Pts',(-8.75302621417252,9.48454361499292,
10.2338829591029));
#113066=CARTESIAN_POINT('Ctrl Pts',(-8.75661691528472,9.48491558250808,
10.2280690123213));
#113067=CARTESIAN_POINT('Ctrl Pts',(-8.7631394858567,9.48558105935513,10.2176714759101));
#113068=CARTESIAN_POINT('Ctrl Pts',(-8.76605642901196,9.48587510325263,
10.2130787105629));
#113069=CARTESIAN_POINT('Ctrl Pts',(-8.77294942199925,9.48656173445071,
10.2023581722921));
#113070=CARTESIAN_POINT('Ctrl Pts',(-8.77694589167756,9.48695356404656,
10.1962436581768));
#113071=CARTESIAN_POINT('Ctrl Pts',(-8.78864100191446,9.48808244242097,
10.1786396053198));
#113072=CARTESIAN_POINT('Ctrl Pts',(-8.79645705016204,9.48881513428449,
10.1672287797503));
#113073=CARTESIAN_POINT('Ctrl Pts',(-8.81447299691252,9.49045702066079,
10.1417104447309));
#113074=CARTESIAN_POINT('Ctrl Pts',(-8.82476527647107,9.49136272780874,
10.1276705828222));
#113075=CARTESIAN_POINT('Ctrl Pts',(-8.85926040377859,9.49429942271809,
10.0823342515621));
#113076=CARTESIAN_POINT('Ctrl Pts',(-8.88448260680557,9.49629387093512,
10.0518341470824));
#113077=CARTESIAN_POINT('Ctrl Pts',(-8.95441360035844,9.50149456009104,
9.97392859580813));
#113078=CARTESIAN_POINT('Ctrl Pts',(-9.00110352457218,9.50464286327012,
9.92842194881521));
#113079=CARTESIAN_POINT('Ctrl Pts',(-9.10812604573773,9.51149769172588,
9.83720482956861));
#113080=CARTESIAN_POINT('Ctrl Pts',(-9.16928038899626,9.51520348125991,
9.79275757381452));
#113081=CARTESIAN_POINT('Ctrl Pts',(-9.24381078696519,9.51980641726203,
9.74694202233806));
#113082=CARTESIAN_POINT('Ctrl Pts',(-9.25411645731182,9.52044477589274,
9.74078034331006));
#113083=CARTESIAN_POINT('Ctrl Pts',(-9.26839525790908,9.52133344313662,
9.73247994542628));
#113084=CARTESIAN_POINT('Ctrl Pts',(-9.27230447559931,9.52157716849879,
9.73023159194743));
#113085=CARTESIAN_POINT('Ctrl Pts',(-9.27901583539317,9.5219964355525,9.72641278174015));
#113086=CARTESIAN_POINT('Ctrl Pts',(-9.28181289518627,9.52217141916658,
9.72483340296241));
#113087=CARTESIAN_POINT('Ctrl Pts',(-9.28765047246164,9.52253717952849,
9.72156247444341));
#113088=CARTESIAN_POINT('Ctrl Pts',(-9.29069183704921,9.5227280606743,9.71987255116799));
#113089=CARTESIAN_POINT('Ctrl Pts',(-9.29810219848745,9.52319387554117,
9.71578952597999));
#113090=CARTESIAN_POINT('Ctrl Pts',(-9.30247742725874,9.52346951352522,
9.71340786400986));
#113091=CARTESIAN_POINT('Ctrl Pts',(-9.31809998108202,9.52445566578656,
9.70500681470163));
#113092=CARTESIAN_POINT('Ctrl Pts',(-9.32941343204,9.5251733661015,9.69911237297404));
#113093=CARTESIAN_POINT('Ctrl Pts',(-9.35769505325932,9.52697356322383,
9.6848442635865));
#113094=CARTESIAN_POINT('Ctrl Pts',(-9.37475102590782,9.52806455354686,
9.67665049341641));
#113095=CARTESIAN_POINT('Ctrl Pts',(-9.44822723652618,9.53277263575836,
9.64308970759946));
#113096=CARTESIAN_POINT('Ctrl Pts',(-9.50606437777582,9.53649611259197,
9.62098382475941));
#113097=CARTESIAN_POINT('Ctrl Pts',(-9.66955476782688,9.54680031869225,
9.57010477517453));
#113098=CARTESIAN_POINT('Ctrl Pts',(-9.77731701196726,9.55331885509914,
9.54940907622033));
#113099=CARTESIAN_POINT('Ctrl Pts',(-9.90451971688929,9.56047026406354,
9.53950475170611));
#113100=CARTESIAN_POINT('Ctrl Pts',(-9.92267265321241,9.5614791845174,9.53843119292253));
#113101=CARTESIAN_POINT('Ctrl Pts',(-9.94889081625855,9.5629200926222,9.53737051880413));
#113102=CARTESIAN_POINT('Ctrl Pts',(-9.95694281729685,9.56336041164563,
9.53711134033965));
#113103=CARTESIAN_POINT('Ctrl Pts',(-9.97111918697271,9.56413185226006,
9.53677217925446));
#113104=CARTESIAN_POINT('Ctrl Pts',(-9.97724263371884,9.56446383164643,
9.53666413266765));
#113105=CARTESIAN_POINT('Ctrl Pts',(-9.98989743207178,9.56514739856308,
9.53652029572315));
#113106=CARTESIAN_POINT('Ctrl Pts',(-9.99642871485747,9.56549881586043,
9.5364897832541));
#113107=CARTESIAN_POINT('Ctrl Pts',(-10.0132051061119,9.56639803826055,
9.53652371503839));
#113108=CARTESIAN_POINT('Ctrl Pts',(-10.0234498226951,9.5669438671373,9.53665201527382));
#113109=CARTESIAN_POINT('Ctrl Pts',(-10.0670375144166,9.56925297804632,
9.53765575202187));
#113110=CARTESIAN_POINT('Ctrl Pts',(-10.1003479287124,9.57098445121748,
9.53956333932139));
#113111=CARTESIAN_POINT('Ctrl Pts',(-10.1903777585356,9.57559922970326,
9.54781431494368));
#113112=CARTESIAN_POINT('Ctrl Pts',(-10.2468391260356,9.57842135079891,
9.55633867188869));
#113113=CARTESIAN_POINT('Ctrl Pts',(-10.3722729210377,9.58469100852929,
9.5828523652751));
#113114=CARTESIAN_POINT('Ctrl Pts',(-10.4407164520063,9.58811121128971,
9.6026228326214));
#113115=CARTESIAN_POINT('Ctrl Pts',(-10.5533534782184,9.59407825330123,
9.64426129612588));
#113116=CARTESIAN_POINT('Ctrl Pts',(-10.5983744617336,9.59656224368481,
9.66352155691888));
#113117=CARTESIAN_POINT('Ctrl Pts',(-10.6488093458091,9.59954971718296,
9.68815759582505));
#113118=CARTESIAN_POINT('Ctrl Pts',(-10.6552534176226,9.59993539176993,
9.6913644452502));
#113119=CARTESIAN_POINT('Ctrl Pts',(-10.6655516101131,9.60055852464694,
9.69658440675131));
#113120=CARTESIAN_POINT('Ctrl Pts',(-10.6694209489156,9.60079420496739,
9.69856742525034));
#113121=CARTESIAN_POINT('Ctrl Pts',(-10.6762939100976,9.60121570209106,
9.70212854674182));
#113122=CARTESIAN_POINT('Ctrl Pts',(-10.6793009511628,9.60140110108965,
9.70369988831467));
#113123=CARTESIAN_POINT('Ctrl Pts',(-10.6823205747863,9.60158828401621,
9.70529119735832));
#113124=CARTESIAN_POINT('Ctrl Pts',(-10.682338588012,9.60158940067085,9.7053006906141));
#113125=CARTESIAN_POINT('Ctrl Pts',(-10.6823743791361,9.60159161946332,
9.70531955405881));
#113126=CARTESIAN_POINT('Ctrl Pts',(-10.6823921570856,9.60159272160339,
9.70532892426227));
#113127=CARTESIAN_POINT('Ctrl Pts',(-10.6824274812581,9.60159491158719,
9.70534754346307));
#113128=CARTESIAN_POINT('Ctrl Pts',(-10.6824450274407,9.60159599942749,
9.70535679242699));
#113129=CARTESIAN_POINT('Ctrl Pts',(-10.6824798915461,9.60159816102398,
9.70537517094006));
#113130=CARTESIAN_POINT('Ctrl Pts',(-10.682497209407,9.60159923477544,9.70538430044477));
#113131=CARTESIAN_POINT('Ctrl Pts',(-10.6825316202207,9.6016013683994,9.70540244177105));
#113132=CARTESIAN_POINT('Ctrl Pts',(-10.682548713134,9.6016024282686,9.70541145356042));
#113133=CARTESIAN_POINT('Ctrl Pts',(-10.682582677389,9.60160453433238,9.70542936118101));
#113134=CARTESIAN_POINT('Ctrl Pts',(-10.6825995487072,9.60160558052466,
9.7054382569887));
#113135=CARTESIAN_POINT('Ctrl Pts',(-10.6826330728645,9.60160765942387,
9.70545593424326));
#113136=CARTESIAN_POINT('Ctrl Pts',(-10.6826497257856,9.60160869213508,
9.70546471572255));
#113137=CARTESIAN_POINT('Ctrl Pts',(-10.682682816523,9.60161074427897,9.70548216606737));
#113138=CARTESIAN_POINT('Ctrl Pts',(-10.6826992543128,9.60161176370923,
9.70549083490844));
#113139=CARTESIAN_POINT('Ctrl Pts',(-10.6827319179129,9.60161378948269,
9.70550806159347));
#113140=CARTESIAN_POINT('Ctrl Pts',(-10.6827481437337,9.60161479582579,
9.70551661943282));
#113141=CARTESIAN_POINT('Ctrl Pts',(-10.6827803864486,9.60161679561196,
9.70553362569396));
#113142=CARTESIAN_POINT('Ctrl Pts',(-10.68279640338,9.60161778905661,9.70554207412551));
#113143=CARTESIAN_POINT('Ctrl Pts',(-10.6828282314985,9.60161976324108,
9.70555886322003));
#113144=CARTESIAN_POINT('Ctrl Pts',(-10.6828440426436,9.60162074397757,
9.70556720385115));
#113145=CARTESIAN_POINT('Ctrl Pts',(-10.6828754621327,9.60162269292609,
9.70558377886846));
#113146=CARTESIAN_POINT('Ctrl Pts',(-10.6828910704704,9.60162366113703,
9.70559201324188));
#113147=CARTESIAN_POINT('Ctrl Pts',(-10.6829220875001,9.60162558522809,
9.70560837738032));
#113148=CARTESIAN_POINT('Ctrl Pts',(-10.6829374961114,9.60162654110252,
9.7056165070936));
#113149=CARTESIAN_POINT('Ctrl Pts',(-10.6829681161778,9.60162844067294,
9.70563266319781));
#113150=CARTESIAN_POINT('Ctrl Pts',(-10.6829833278201,9.60162938437988,
9.70564068967862));
#113151=CARTESIAN_POINT('Ctrl Pts',(-10.6830135570897,9.60163125980822,
9.70565664094877));
#113152=CARTESIAN_POINT('Ctrl Pts',(-10.6830285746875,9.60163219152713,
9.70566456571385));
#113153=CARTESIAN_POINT('Ctrl Pts',(-10.6830584187838,9.60163404315836,
9.70568031506526));
#113154=CARTESIAN_POINT('Ctrl Pts',(-10.6830732451936,9.60163496306454,
9.70568813959627));
#113155=CARTESIAN_POINT('Ctrl Pts',(-10.68310270972,9.60163679124254,9.7057036899353));
#113156=CARTESIAN_POINT('Ctrl Pts',(-10.6831173477817,9.60163769951032,
9.70571141570603));
#113157=CARTESIAN_POINT('Ctrl Pts',(-10.683146437956,9.60163950455514,9.70572676973713));
#113158=CARTESIAN_POINT('Ctrl Pts',(-10.6831608902278,9.60164040134144,
9.70573439807348));
#113159=CARTESIAN_POINT('Ctrl Pts',(-10.6831896120403,9.60164218362119,
9.70574955891043));
#113160=CARTESIAN_POINT('Ctrl Pts',(-10.6832038814252,9.60164306910437,
9.70575709132099));
#113161=CARTESIAN_POINT('Ctrl Pts',(-10.6832322396096,9.6016448289093,9.70577206141581));
#113162=CARTESIAN_POINT('Ctrl Pts',(-10.683246328575,9.60164570324076,9.70577949918005));
#113163=CARTESIAN_POINT('Ctrl Pts',(-10.6832743288134,9.60164744092008,
9.7057942814869));
#113164=CARTESIAN_POINT('Ctrl Pts',(-10.683288240036,9.60164830426425,9.70580162599546));
#113165=CARTESIAN_POINT('Ctrl Pts',(-10.6833158874056,9.60165002012975,
9.70581622315054));
#113166=CARTESIAN_POINT('Ctrl Pts',(-10.6833296235036,9.60165087264749,
9.70582347576395));
#113167=CARTESIAN_POINT('Ctrl Pts',(-10.6833569228363,9.60165256699583,
9.70583789027534));
#113168=CARTESIAN_POINT('Ctrl Pts',(-10.6833704861922,9.60165340883343,
9.70584505223036));
#113169=CARTESIAN_POINT('Ctrl Pts',(-10.6833974428782,9.60165508199603,
9.70585928690236));
#113170=CARTESIAN_POINT('Ctrl Pts',(-10.6834108360869,9.60165591331299,
9.70586635954843));
#113171=CARTESIAN_POINT('Ctrl Pts',(-10.6834374548406,9.60165756557941,
9.70588041682977));
#113172=CARTESIAN_POINT('Ctrl Pts',(-10.6834506803668,9.60165838652722,
9.70588740144846));
#113173=CARTESIAN_POINT('Ctrl Pts',(-10.68347696589,9.60166001818636,9.70590128378244));
#113174=CARTESIAN_POINT('Ctrl Pts',(-10.6834900260471,9.60166082890715,
9.70590818157588));
#113175=CARTESIAN_POINT('Ctrl Pts',(-10.6835159832055,9.60166244025814,
9.70592189149365));
#113176=CARTESIAN_POINT('Ctrl Pts',(-10.6835288802863,9.60166324089282,
9.70592870365374));
#113177=CARTESIAN_POINT('Ctrl Pts',(-10.6835545141058,9.60166483224487,
9.70594224377232));
#113178=CARTESIAN_POINT('Ctrl Pts',(-10.6835672506391,9.60166562294903,
9.70594897161618));
#113179=CARTESIAN_POINT('Ctrl Pts',(-10.6835925651352,9.60166719454868,
9.70596234401999));
#113180=CARTESIAN_POINT('Ctrl Pts',(-10.6836051432246,9.60166797545158,
9.70596898864081));
#113181=CARTESIAN_POINT('Ctrl Pts',(-10.6836301434222,9.60166952760812,
9.70598219594861));
#113182=CARTESIAN_POINT('Ctrl Pts',(-10.6836425654444,9.601670298856,9.70598875858437));
#113183=CARTESIAN_POINT('Ctrl Pts',(-10.6836672554069,9.60167183181913,
9.70600180290815));
#113184=CARTESIAN_POINT('Ctrl Pts',(-10.6836795234334,9.60167259353931,
9.70600828463608));
#113185=CARTESIAN_POINT('Ctrl Pts',(-10.6837039079859,9.60167410760609,
9.7060211684913));
#113186=CARTESIAN_POINT('Ctrl Pts',(-10.6837160243483,9.60167485994211,
9.70602757052664));
#113187=CARTESIAN_POINT('Ctrl Pts',(-10.6837401074538,9.60167635535615,
9.7060402959743));
#113188=CARTESIAN_POINT('Ctrl Pts',(-10.6837520742491,9.60167709843701,
9.70604661940887));
#113189=CARTESIAN_POINT('Ctrl Pts',(-10.6837758601558,9.6016785754597,9.70605918866168));
#113190=CARTESIAN_POINT('Ctrl Pts',(-10.6837876794018,9.60167930940951,
9.70606543454586));
#113191=CARTESIAN_POINT('Ctrl Pts',(-10.6838111725248,9.6016807683127,9.70607784990575));
#113192=CARTESIAN_POINT('Ctrl Pts',(-10.6838228463518,9.60168149326259,
9.70608401934992));
#113193=CARTESIAN_POINT('Ctrl Pts',(-10.6838460506931,9.60168293429252,
9.70609628290143));
#113194=CARTESIAN_POINT('Ctrl Pts',(-10.6838575811444,9.60168365036827,
9.7061023769705));
#113195=CARTESIAN_POINT('Ctrl Pts',(-10.6838805007578,9.60168507377448,
9.70611449082648));
#113196=CARTESIAN_POINT('Ctrl Pts',(-10.6838918898546,9.60168578110053,
9.70612051057408));
#113197=CARTESIAN_POINT('Ctrl Pts',(-10.6839145287203,9.60168718712807,
9.70613247680945));
#113198=CARTESIAN_POINT('Ctrl Pts',(-10.6839257784642,9.60168788582765,
9.70613842327933));
#113199=CARTESIAN_POINT('Ctrl Pts',(-10.6839481403683,9.60168927470957,
9.70615024386725));
#113200=CARTESIAN_POINT('Ctrl Pts',(-10.6839592526239,9.60168996489747,
9.70615611803117));
#113201=CARTESIAN_POINT('Ctrl Pts',(-10.6839813416535,9.60169133688556,
9.70616779510476));
#113202=CARTESIAN_POINT('Ctrl Pts',(-10.6839923184077,9.60169201868418,
9.70617359799954));
#113203=CARTESIAN_POINT('Ctrl Pts',(-10.6840141381392,9.60169337399861,
9.70618513342284));
#113204=CARTESIAN_POINT('Ctrl Pts',(-10.6840249812056,9.60169404751961,
9.70619086599411));
#113205=CARTESIAN_POINT('Ctrl Pts',(-10.684046535537,9.60169538640055,9.70620226180188));
#113206=CARTESIAN_POINT('Ctrl Pts',(-10.6840572467956,9.60169605175976,
9.70620792503078));
#113207=CARTESIAN_POINT('Ctrl Pts',(-10.6876846865737,9.60192138442477,
9.70812587323267));
#113208=CARTESIAN_POINT('Ctrl Pts',(-10.6912933359568,9.60214699436492,
9.7100532916476));
#113209=CARTESIAN_POINT('Ctrl Pts',(-10.7019458556196,9.60281715643344,
9.71580045453595));
#113210=CARTESIAN_POINT('Ctrl Pts',(-10.7089663747763,9.60326425049677,
9.71966288409624));
#113211=CARTESIAN_POINT('Ctrl Pts',(-10.7250712541704,9.60430180392394,
9.72869626468675));
#113212=CARTESIAN_POINT('Ctrl Pts',(-10.7341325621673,9.60489442810374,
9.73390723858346));
#113213=CARTESIAN_POINT('Ctrl Pts',(-10.7642988113322,9.60689520666466,
9.75168794748396));
#113214=CARTESIAN_POINT('Ctrl Pts',(-10.7851422150384,9.60832381613623,
9.76469143997631));
#113215=CARTESIAN_POINT('Ctrl Pts',(-10.8500329308914,9.61289692380356,
9.80748042237717));
#113216=CARTESIAN_POINT('Ctrl Pts',(-10.8927890585302,9.61609758061416,
9.83914417751405));
#113217=CARTESIAN_POINT('Ctrl Pts',(-11.0175058511338,9.62584439482827,
9.94247850071633));
#113218=CARTESIAN_POINT('Ctrl Pts',(-11.0932968305378,9.63232684168418,
10.0210315914217));
#113219=CARTESIAN_POINT('Ctrl Pts',(-11.1707943135816,9.63944823031381,
10.1217035790922));
#113220=CARTESIAN_POINT('Ctrl Pts',(-11.18163353811,9.64045881947979,10.1363414151755));
#113221=CARTESIAN_POINT('Ctrl Pts',(-11.1968724706293,9.64190165442275,
10.1577449789388));
#113222=CARTESIAN_POINT('Ctrl Pts',(-11.2014935956771,9.64234226250431,
10.164350327813));
#113223=CARTESIAN_POINT('Ctrl Pts',(-11.2095295857406,9.64311403958962,
10.1760412944275));
#113224=CARTESIAN_POINT('Ctrl Pts',(-11.212967509226,9.64344606869018,10.181110758155));
#113225=CARTESIAN_POINT('Ctrl Pts',(-11.2200041662266,9.64412957746605,
10.1916283563145));
#113226=CARTESIAN_POINT('Ctrl Pts',(-11.2235984741443,9.64448088808905,
10.1970792966405));
#113227=CARTESIAN_POINT('Ctrl Pts',(-11.2327335125077,9.64537950511583,
10.211136827257));
#113228=CARTESIAN_POINT('Ctrl Pts',(-11.2382206989335,9.64592484054412,
10.2197778995714));
#113229=CARTESIAN_POINT('Ctrl Pts',(-11.2611537838395,9.64822883442018,
10.2567436589376));
#113230=CARTESIAN_POINT('Ctrl Pts',(-11.2777225527412,9.64995586451404,
10.2856022464121));
#113231=CARTESIAN_POINT('Ctrl Pts',(-11.3198893303148,9.65455493175708,
10.3652142298304));
#113232=CARTESIAN_POINT('Ctrl Pts',(-11.3435388003032,9.65736634004851,
10.4169348788187));
#113233=CARTESIAN_POINT('Ctrl Pts',(-11.3921468751536,9.6639299332138,10.5420199676267));
#113234=CARTESIAN_POINT('Ctrl Pts',(-11.414407470614,9.66764188557768,10.616243322208));
#113235=CARTESIAN_POINT('Ctrl Pts',(-11.4364117936173,9.67286491853837,
10.7184144295653));
#113236=CARTESIAN_POINT('Ctrl Pts',(-11.4413877359852,9.67424030752079,
10.7451068204224));
#113237=CARTESIAN_POINT('Ctrl Pts',(-11.4486330472466,9.67664764207889,
10.7910292703301));
#113238=CARTESIAN_POINT('Ctrl Pts',(-11.4512685332935,9.67766447007054,
10.8101947175152));
#113239=CARTESIAN_POINT('Ctrl Pts',(-11.4542288615562,9.67902503192416,
10.8354177730152));
#113240=CARTESIAN_POINT('Ctrl Pts',(-11.4548971399276,9.67935121356271,
10.8414339226088));
#113241=CARTESIAN_POINT('Ctrl Pts',(-11.4559146112561,9.67988049819796,
10.851142190841));
#113242=CARTESIAN_POINT('Ctrl Pts',(-11.4562871324289,9.68008233526669,
10.8548318564051));
#113243=CARTESIAN_POINT('Ctrl Pts',(-11.4569580544429,9.68046155306436,
10.8617396549847));
#113244=CARTESIAN_POINT('Ctrl Pts',(-11.4572598236306,9.68063874615317,
10.8649574100434));
#113245=CARTESIAN_POINT('Ctrl Pts',(-11.4578576466569,9.68100383610441,
10.871567421347));
#113246=CARTESIAN_POINT('Ctrl Pts',(-11.4581525251255,9.68119179577398,
10.8749597737987));
#113247=CARTESIAN_POINT('Ctrl Pts',(-11.4588160875583,9.68163391969058,
10.8829152824278));
#113248=CARTESIAN_POINT('Ctrl Pts',(-11.4591752024302,9.68188858426316,
10.8874791756721));
#113249=CARTESIAN_POINT('Ctrl Pts',(-11.4604393785231,9.68284592504264,
10.9045703226372));
#113250=CARTESIAN_POINT('Ctrl Pts',(-11.4612045497126,9.68355550289127,
10.9171070285735));
#113251=CARTESIAN_POINT('Ctrl Pts',(-11.4629244220802,9.68559627130138,
10.9528452079629));
#113252=CARTESIAN_POINT('Ctrl Pts',(-11.4634883795329,9.68694349692706,
10.976060848177));
#113253=CARTESIAN_POINT('Ctrl Pts',(-11.4634998222634,9.68830623016798,
10.9992787267827));
#113254=CARTESIAN_POINT('Origin',(-10.,3.5,11.));
#113255=CARTESIAN_POINT('',(-11.4634998963973,10.2594509413108,10.9994493226066));
#113256=CARTESIAN_POINT('',(-11.4634998672782,10.1905769185068,10.9993767206508));
#113257=CARTESIAN_POINT('',(-11.4635,3.5,11.));
#113258=CARTESIAN_POINT('Ctrl Pts',(-11.4634998963974,10.2594509413502,
10.9994493233677));
#113259=CARTESIAN_POINT('Ctrl Pts',(-11.4634862943792,10.2575830488448,
10.9633000642476));
#113260=CARTESIAN_POINT('Ctrl Pts',(-11.462133348461,10.255752951935,10.927162368284));
#113261=CARTESIAN_POINT('Ctrl Pts',(-11.4542405240509,10.2504599843605,
10.8213753825262));
#113262=CARTESIAN_POINT('Ctrl Pts',(-11.4440460393546,10.2470799500598,
10.752101545193));
#113263=CARTESIAN_POINT('Ctrl Pts',(-11.4124588144446,10.2399541673378,
10.6093459547505));
#113264=CARTESIAN_POINT('Ctrl Pts',(-11.3901840202895,10.2362127256549,
10.5362798243507));
#113265=CARTESIAN_POINT('Ctrl Pts',(-11.3579340662727,10.2315686396017,
10.454114030765));
#113266=CARTESIAN_POINT('Ctrl Pts',(-11.3534098793377,10.2309302831277,
10.4429918312827));
#113267=CARTESIAN_POINT('Ctrl Pts',(-11.3469993328789,10.2300416617662,
10.427771569031));
#113268=CARTESIAN_POINT('Ctrl Pts',(-11.3452299929797,10.2297979805115,
10.4236243890496));
#113269=CARTESIAN_POINT('Ctrl Pts',(-11.3421677002724,10.2293788004034,
10.4165375526681));
#113270=CARTESIAN_POINT('Ctrl Pts',(-11.3408841728556,10.2292038594952,
10.4135938287509));
#113271=CARTESIAN_POINT('Ctrl Pts',(-11.3381902921116,10.2288382031425,
10.4074705994657));
#113272=CARTESIAN_POINT('Ctrl Pts',(-11.3367782861009,10.2286473834548,
10.4042918824162));
#113273=CARTESIAN_POINT('Ctrl Pts',(-11.3333173556612,10.2281817472528,
10.3965748816269));
#113274=CARTESIAN_POINT('Ctrl Pts',(-11.3312565827084,10.2279062271955,
10.3920419801395));
#113275=CARTESIAN_POINT('Ctrl Pts',(-11.3238374368099,10.2269206578529,
10.3759413359653));
#113276=CARTESIAN_POINT('Ctrl Pts',(-11.3183512448256,10.2262034320483,
10.3644335219093));
#113277=CARTESIAN_POINT('Ctrl Pts',(-11.3043574104275,10.2244045891495,
10.3360410895325));
#113278=CARTESIAN_POINT('Ctrl Pts',(-11.2956717191823,10.2233144924664,
10.3192471625397));
#113279=CARTESIAN_POINT('Ctrl Pts',(-11.2572250079121,10.2186120366431,
10.2483124170297));
#113280=CARTESIAN_POINT('Ctrl Pts',(-11.2243781907875,10.2148935063949,
10.1959189869045));
#113281=CARTESIAN_POINT('Ctrl Pts',(-11.1244119287705,10.2045868898192,
10.0568572490605));
#113282=CARTESIAN_POINT('Ctrl Pts',(-11.0507174687013,10.1980608497323,
9.97539246817712));
#113283=CARTESIAN_POINT('Ctrl Pts',(-10.9549894127951,10.190903302578,9.89087521219069));
#113284=CARTESIAN_POINT('Ctrl Pts',(-10.9411415869911,10.189894821308,9.87910075015727));
#113285=CARTESIAN_POINT('Ctrl Pts',(-10.9208462259254,10.1884544941744,
9.86248545826009));
#113286=CARTESIAN_POINT('Ctrl Pts',(-10.9145727904991,10.1880143243531,
9.85743546398245));
#113287=CARTESIAN_POINT('Ctrl Pts',(-10.9034571294003,10.1872431300614,
9.84863778500781));
#113288=CARTESIAN_POINT('Ctrl Pts',(-10.898632511624,10.1869112484666,9.84486825625668));
#113289=CARTESIAN_POINT('Ctrl Pts',(-10.8886139335851,10.1862278699084,
9.8371413836111));
#113290=CARTESIAN_POINT('Ctrl Pts',(-10.883416852644,10.1858765431702,9.83318829667214));
#113291=CARTESIAN_POINT('Ctrl Pts',(-10.8699996346552,10.1849775282995,
9.82312371004521));
#113292=CARTESIAN_POINT('Ctrl Pts',(-10.8617414038642,10.1844318156519,
9.81706343106077));
#113293=CARTESIAN_POINT('Ctrl Pts',(-10.8263276494325,10.1821230309942,
9.79164282259333));
#113294=CARTESIAN_POINT('Ctrl Pts',(-10.7985772390656,10.180391760713,9.77312630466797));
#113295=CARTESIAN_POINT('Ctrl Pts',(-10.7217121316134,10.1757774778639,
9.72555194852045));
#113296=CARTESIAN_POINT('Ctrl Pts',(-10.671491497365,10.1729556392773,9.69839098215427));
#113297=CARTESIAN_POINT('Ctrl Pts',(-10.6046300439122,10.1693461943471,
9.66713256544891));
#113298=CARTESIAN_POINT('Ctrl Pts',(-10.5893280728218,10.1685294806238,
9.66029648186219));
#113299=CARTESIAN_POINT('Ctrl Pts',(-10.4837723358048,10.1629431597651,
9.61529847656086));
#113300=CARTESIAN_POINT('Ctrl Pts',(-10.3900122293105,10.1582301446143,
9.58602696272213));
#113301=CARTESIAN_POINT('Ctrl Pts',(-10.2829623046903,10.1524710192988,
9.56407082770563));
#113302=CARTESIAN_POINT('Ctrl Pts',(-10.2718534910464,10.151868810434,9.56192631699846));
#113303=CARTESIAN_POINT('Ctrl Pts',(-10.2563800130152,10.1510222810881,
9.55912491756782));
#113304=CARTESIAN_POINT('Ctrl Pts',(-10.2520352808938,10.1507837456512,
9.55835859853328));
#113305=CARTESIAN_POINT('Ctrl Pts',(-10.244547337332,10.1503710908606,9.55707276715072));
#113306=CARTESIAN_POINT('Ctrl Pts',(-10.2414057464927,10.1501974912041,
9.55654384733852));
#113307=CARTESIAN_POINT('Ctrl Pts',(-10.2348080594086,10.1498318824792,
9.55545519862289));
#113308=CARTESIAN_POINT('Ctrl Pts',(-10.231351658652,10.1496397511864,9.55489761013364));
#113309=CARTESIAN_POINT('Ctrl Pts',(-10.2228587572847,10.1491662472596,
9.55355878057596));
#113310=CARTESIAN_POINT('Ctrl Pts',(-10.2178201357117,10.1488841155311,
9.55279144079065));
#113311=CARTESIAN_POINT('Ctrl Pts',(-10.1993938024115,10.1478481798891,
9.55008367203305));
#113312=CARTESIAN_POINT('Ctrl Pts',(-10.1859837709318,10.1470862237061,
9.54830262902944));
#113313=CARTESIAN_POINT('Ctrl Pts',(-10.1522205497791,10.1451508804495,
9.54429387307351));
#113314=CARTESIAN_POINT('Ctrl Pts',(-10.1318420632849,10.1439673835021,
9.54230695244723));
#113315=CARTESIAN_POINT('Ctrl Pts',(-9.97255185211468,10.1346298881146,
9.53014343409202));
#113316=CARTESIAN_POINT('Ctrl Pts',(-9.83286472504538,10.1260166633179,
9.53941567275816));
#113317=CARTESIAN_POINT('Ctrl Pts',(-9.65686146692039,10.1156266212034,
9.57671633511999));
#113318=CARTESIAN_POINT('Ctrl Pts',(-9.6175107082053,10.1133274195974,9.58678280707845));
#113319=CARTESIAN_POINT('Ctrl Pts',(-9.56773157055176,10.1104498628845,
9.60174906156194));
#113320=CARTESIAN_POINT('Ctrl Pts',(-9.55687487753494,10.1098241412488,
9.60515168638234));
#113321=CARTESIAN_POINT('Ctrl Pts',(-9.53961524541052,10.108832173874,9.61078293053293));
#113322=CARTESIAN_POINT('Ctrl Pts',(-9.53318635401791,10.1084633052205,
9.6129299907974));
#113323=CARTESIAN_POINT('Ctrl Pts',(-9.52161827207353,10.1078006232038,
9.61688292583138));
#113324=CARTESIAN_POINT('Ctrl Pts',(-9.51647383609122,10.1075063012531,
9.61867296834161));
#113325=CARTESIAN_POINT('Ctrl Pts',(-9.50438429093902,10.1068154796893,
9.62295542436544));
#113326=CARTESIAN_POINT('Ctrl Pts',(-9.49744776455892,10.1064197700455,
9.62547173630032));
#113327=CARTESIAN_POINT('Ctrl Pts',(-9.47722316546002,10.1052677542921,
9.63298202820936));
#113328=CARTESIAN_POINT('Ctrl Pts',(-9.46398816403667,10.1045160927794,
9.63811708132038));
#113329=CARTESIAN_POINT('Ctrl Pts',(-9.36378414404764,10.0988379025878,
9.67868236315272));
#113330=CARTESIAN_POINT('Ctrl Pts',(-9.28032948398277,10.094201951275,9.72221758349777));
#113331=CARTESIAN_POINT('Ctrl Pts',(-9.11364814108016,10.0845087558652,
9.83071417379565));
#113332=CARTESIAN_POINT('Ctrl Pts',(-9.03210816717216,10.0794904899148,
9.89726308525945));
#113333=CARTESIAN_POINT('Ctrl Pts',(-8.95085077461707,10.0733851975957,
9.97959148694501));
#113334=CARTESIAN_POINT('Ctrl Pts',(-8.94338986138299,10.0728128427596,
9.98731908660913));
#113335=CARTESIAN_POINT('Ctrl Pts',(-8.93305208019201,10.07200191329,9.99826500199554));
#113336=CARTESIAN_POINT('Ctrl Pts',(-8.93010318396578,10.0717685095511,
10.0014151653953));
#113337=CARTESIAN_POINT('Ctrl Pts',(-8.92501816567224,10.0713623123091,
10.0068956253172));
#113338=CARTESIAN_POINT('Ctrl Pts',(-8.92287556638294,10.0711900009472,
10.0092199046892));
#113339=CARTESIAN_POINT('Ctrl Pts',(-8.91835774106767,10.0708241653642,
10.0141527906046));
#113340=CARTESIAN_POINT('Ctrl Pts',(-8.91598439574228,10.0706304999293,
10.0167630674057));
#113341=CARTESIAN_POINT('Ctrl Pts',(-8.91011713487109,10.0701480970889,
10.0232631222595));
#113342=CARTESIAN_POINT('Ctrl Pts',(-8.9066346044091,10.0698585374223,10.0271630670737));
#113343=CARTESIAN_POINT('Ctrl Pts',(-8.89360817409079,10.0687635040853,
10.0419091366168));
#113344=CARTESIAN_POINT('Ctrl Pts',(-8.8842044636374,10.0679486503046,10.0528773765514));
#113345=CARTESIAN_POINT('Ctrl Pts',(-8.8154564322845,10.0618188517994,10.1355082531234));
#113346=CARTESIAN_POINT('Ctrl Pts',(-8.76290817778324,10.0561683490377,
10.2125412660766));
#113347=CARTESIAN_POINT('Ctrl Pts',(-8.67258339270342,10.0449193983551,
10.3765629510643));
#113348=CARTESIAN_POINT('Ctrl Pts',(-8.63520563135311,10.0393527951374,
10.4632973500904));
#113349=CARTESIAN_POINT('Ctrl Pts',(-8.60073450430408,10.0330218748626,
10.5707735292916));
#113350=CARTESIAN_POINT('Ctrl Pts',(-8.59538408780555,10.031987675413,10.5886200362395));
#113351=CARTESIAN_POINT('Ctrl Pts',(-8.58838619787018,10.0305578976472,
10.6136924917161));
#113352=CARTESIAN_POINT('Ctrl Pts',(-8.58645077902293,10.0301531512991,
10.6208356293082));
#113353=CARTESIAN_POINT('Ctrl Pts',(-8.58300330503894,10.0294145787647,
10.633952754895));
#113354=CARTESIAN_POINT('Ctrl Pts',(-8.58147464678666,10.0290802291361,
10.6399221708042));
#113355=CARTESIAN_POINT('Ctrl Pts',(-8.57844995758247,10.0284043537728,
10.6520518561747));
#113356=CARTESIAN_POINT('Ctrl Pts',(-8.57695615861035,10.0280629052112,
10.6582125498181));
#113357=CARTESIAN_POINT('Ctrl Pts',(-8.57335856940373,10.0272210336467,
10.6734822006574));
#113358=CARTESIAN_POINT('Ctrl Pts',(-8.57130192460902,10.0267221107228,
10.6826020485465));
#113359=CARTESIAN_POINT('Ctrl Pts',(-8.56387157716686,10.0248496232155,
10.7170872014899));
#113360=CARTESIAN_POINT('Ctrl Pts',(-8.55908470370161,10.0234944839752,
10.7425748377645));
#113361=CARTESIAN_POINT('Ctrl Pts',(-8.54869891533128,10.020114708801,10.8073126652342));
#113362=CARTESIAN_POINT('Ctrl Pts',(-8.54401265956118,10.0181166172646,
10.8466885520205));
#113363=CARTESIAN_POINT('Ctrl Pts',(-8.53587294428252,10.0129164816629,
10.9510580080868));
#113364=CARTESIAN_POINT('Ctrl Pts',(-8.53514438064214,10.0097719489477,
11.0161743293147));
#113365=CARTESIAN_POINT('Ctrl Pts',(-8.54293164515807,10.0029236483346,
11.1564443509342));
#113366=CARTESIAN_POINT('Ctrl Pts',(-8.55293028183017,9.99922055924571,
11.2313219634186));
#113367=CARTESIAN_POINT('Ctrl Pts',(-8.57115868811284,9.99462010144775,
11.3168426215016));
#113368=CARTESIAN_POINT('Ctrl Pts',(-8.57380918105517,9.99398104737646,
11.3285673005787));
#113369=CARTESIAN_POINT('Ctrl Pts',(-8.57765241213885,9.99309161963148,
11.3446446504495));
#113370=CARTESIAN_POINT('Ctrl Pts',(-8.57872137691247,9.99284784554781,
11.3490267471933));
#113371=CARTESIAN_POINT('Ctrl Pts',(-8.58058616533332,9.99242854739396,
11.3565205913516));
#113372=CARTESIAN_POINT('Ctrl Pts',(-8.58137201327883,9.99225358196518,
11.3596348161468));
#113373=CARTESIAN_POINT('Ctrl Pts',(-8.58303013768096,9.99188792258592,
11.3661157672652));
#113374=CARTESIAN_POINT('Ctrl Pts',(-8.5839041677126,9.99169712470755,11.3694819869559));
#113375=CARTESIAN_POINT('Ctrl Pts',(-8.58605822908163,9.99123162189138,
11.3776581694534));
#113376=CARTESIAN_POINT('Ctrl Pts',(-8.58735081158651,9.990956214351,11.3824647611288));
#113377=CARTESIAN_POINT('Ctrl Pts',(-8.59203790097204,9.98997148480037,
11.3995462087035));
#113378=CARTESIAN_POINT('Ctrl Pts',(-8.59556798989298,9.98925500199196,
11.4117828939991));
#113379=CARTESIAN_POINT('Ctrl Pts',(-8.60472678743104,9.98745840314594,
11.4420422845281));
#113380=CARTESIAN_POINT('Ctrl Pts',(-8.6105453388387,9.98636983308172,11.4600047874608));
#113381=CARTESIAN_POINT('Ctrl Pts',(-8.63683323579494,9.98167765091917,
11.5361037314702));
#113382=CARTESIAN_POINT('Ctrl Pts',(-8.66061589532994,9.97796828124458,
11.5930264293615));
#113383=CARTESIAN_POINT('Ctrl Pts',(-8.73650629985609,9.96765803100651,
11.7466253520187));
#113384=CARTESIAN_POINT('Ctrl Pts',(-8.79600954596482,9.96111891418536,
11.8392139967933));
#113385=CARTESIAN_POINT('Ctrl Pts',(-8.87678302920461,9.95395052159352,
11.9383740233353));
#113386=CARTESIAN_POINT('Ctrl Pts',(-8.88851607342498,9.95294266699089,
11.9522424552714));
#113387=CARTESIAN_POINT('Ctrl Pts',(-8.90581836444586,9.95150306357661,
11.9719380749385));
#113388=CARTESIAN_POINT('Ctrl Pts',(-8.91118199119699,9.95106300240495,
11.9779429535603));
#113389=CARTESIAN_POINT('Ctrl Pts',(-8.92071087035814,9.95029193455262,
11.9884354837182));
#113390=CARTESIAN_POINT('Ctrl Pts',(-8.92485520611861,9.94996007161204,
11.9929417931585));
#113391=CARTESIAN_POINT('Ctrl Pts',(-8.93347834672682,9.94927667103424,
12.0022008071594));
#113392=CARTESIAN_POINT('Ctrl Pts',(-8.93796093584425,9.94892530406674,
12.0069498114931));
#113393=CARTESIAN_POINT('Ctrl Pts',(-8.94955821806162,9.94802606094409,
12.0190727657173));
#113394=CARTESIAN_POINT('Ctrl Pts',(-8.9567189016098,9.94748016225432,12.0264023557685));
#113395=CARTESIAN_POINT('Ctrl Pts',(-8.98753419436374,9.94516944491471,
12.0572888286523));
#113396=CARTESIAN_POINT('Ctrl Pts',(-9.01191499026243,9.94343649631223,
12.0801087480284));
#113397=CARTESIAN_POINT('Ctrl Pts',(-9.08007794747757,9.93881627062336,
12.1396664304062));
#113398=CARTESIAN_POINT('Ctrl Pts',(-9.12526573037847,9.93599037839805,
12.1747070886251));
#113399=CARTESIAN_POINT('Ctrl Pts',(-9.17977839071617,9.9327582061639,12.2120845864152));
#113400=CARTESIAN_POINT('Ctrl Pts',(-9.18721459082728,9.93232084037367,
12.2170835685018));
#113401=CARTESIAN_POINT('Ctrl Pts',(-9.28010780959744,9.92689662383859,
12.2782999369494));
#113402=CARTESIAN_POINT('Ctrl Pts',(-9.37117488225281,9.92200733388753,
12.3254695675598));
#113403=CARTESIAN_POINT('Ctrl Pts',(-9.47923849118508,9.91592716793035,
12.3677827906596));
#113404=CARTESIAN_POINT('Ctrl Pts',(-9.49214568724392,9.91519641757728,
12.3726275100879));
#113405=CARTESIAN_POINT('Ctrl Pts',(-9.51010225466513,9.91417108554198,
12.3790795803178));
#113406=CARTESIAN_POINT('Ctrl Pts',(-9.51509518492441,9.91388506218078,
12.3808430788164));
#113407=CARTESIAN_POINT('Ctrl Pts',(-9.52311088004403,9.91342423775376,
12.3836253798561));
#113408=CARTESIAN_POINT('Ctrl Pts',(-9.52612764408092,9.91325043250034,
12.3846614800775));
#113409=CARTESIAN_POINT('Ctrl Pts',(-9.53245912566061,9.91288483316092,
12.3868128973142));
#113410=CARTESIAN_POINT('Ctrl Pts',(-9.53577447484118,9.91269291971138,
12.3879262020452));
#113411=CARTESIAN_POINT('Ctrl Pts',(-9.54391295698816,9.91222070352063,
12.3906267081038));
#113412=CARTESIAN_POINT('Ctrl Pts',(-9.54874039953616,9.91193965079142,
12.3922007051873));
#113413=CARTESIAN_POINT('Ctrl Pts',(-9.56633532318243,9.9109120742867,12.3978364370677));
#113414=CARTESIAN_POINT('Ctrl Pts',(-9.57914985334231,9.91015756467046,
12.401747796461));
#113415=CARTESIAN_POINT('Ctrl Pts',(-9.61142430397616,9.90824513808985,
12.4111164407753));
#113416=CARTESIAN_POINT('Ctrl Pts',(-9.63094661017167,9.90707739531486,
12.4163474876122));
#113417=CARTESIAN_POINT('Ctrl Pts',(-9.71818855211159,9.90182874953775,
12.4377980485015));
#113418=CARTESIAN_POINT('Ctrl Pts',(-9.78690466530693,9.89761902283037,
12.449576000437));
#113419=CARTESIAN_POINT('Ctrl Pts',(-9.95459581624042,9.88748715181938,
12.4661336363236));
#113420=CARTESIAN_POINT('Ctrl Pts',(-10.0537414793066,9.88162907834498,
12.4658535856989));
#113421=CARTESIAN_POINT('Ctrl Pts',(-10.1705691530577,9.87504117984222,
12.4536446488069));
#113422=CARTESIAN_POINT('Ctrl Pts',(-10.1889875434898,9.87401107687879,
12.4513649966937));
#113423=CARTESIAN_POINT('Ctrl Pts',(-10.2146727253466,9.87258595522523,
12.4476886644436));
#113424=CARTESIAN_POINT('Ctrl Pts',(-10.2219792960107,9.87218184729995,
12.4465863413923));
#113425=CARTESIAN_POINT('Ctrl Pts',(-10.2353602561993,9.87144407460977,
12.4444638220382));
#113426=CARTESIAN_POINT('Ctrl Pts',(-10.2414371237853,9.87110989060074,
12.4434605295051));
#113427=CARTESIAN_POINT('Ctrl Pts',(-10.2537590579502,9.87043398150606,
12.4413461841859));
#113428=CARTESIAN_POINT('Ctrl Pts',(-10.2600035998408,9.87009233625453,
12.4402328325524));
#113429=CARTESIAN_POINT('Ctrl Pts',(-10.2754514035148,9.86924929458444,
12.4373748688961));
#113430=CARTESIAN_POINT('Ctrl Pts',(-10.2846455989532,9.86874940759867,
12.4355824176591));
#113431=CARTESIAN_POINT('Ctrl Pts',(-10.3193552214165,9.86686881083936,
12.428469045712));
#113432=CARTESIAN_POINT('Ctrl Pts',(-10.3447449176104,9.86550673874607,
12.4225549628151));
#113433=CARTESIAN_POINT('Ctrl Pts',(-10.4085919418975,9.86210571696722,
12.4058729816874));
#113434=CARTESIAN_POINT('Ctrl Pts',(-10.446792107829,9.86009376431832,12.3942034720116));
#113435=CARTESIAN_POINT('Ctrl Pts',(-10.5455648683247,9.85489603500823,
12.3595526119834));
#113436=CARTESIAN_POINT('Ctrl Pts',(-10.6051721444239,9.85176612869738,
12.3340881673152));
#113437=CARTESIAN_POINT('Ctrl Pts',(-10.7300072059253,9.84494011717332,
12.2706643951548));
#113438=CARTESIAN_POINT('Ctrl Pts',(-10.7943798039771,9.84124443254299,
12.2314450292451));
#113439=CARTESIAN_POINT('Ctrl Pts',(-10.8651946002799,9.83665261940266,
12.1804300023848));
#113440=CARTESIAN_POINT('Ctrl Pts',(-10.8748587119894,9.83601368342828,
12.1732855162519));
#113441=CARTESIAN_POINT('Ctrl Pts',(-10.8880269731594,9.83512439223558,
12.1632973343212));
#113442=CARTESIAN_POINT('Ctrl Pts',(-10.8916078498252,9.83488063390505,
12.160555054339));
#113443=CARTESIAN_POINT('Ctrl Pts',(-10.8977168392171,9.83446135578417,
12.1558317534044));
#113444=CARTESIAN_POINT('Ctrl Pts',(-10.900251233902,9.8342863945172,12.1538588653047));
#113445=CARTESIAN_POINT('Ctrl Pts',(-10.9054619442421,9.83392452363076,
12.1497749938534));
#113446=CARTESIAN_POINT('Ctrl Pts',(-10.9081373936128,9.8337375375289,12.1476629916818));
#113447=CARTESIAN_POINT('Ctrl Pts',(-10.9145223683666,9.83328850242657,
12.1425863807602));
#113448=CARTESIAN_POINT('Ctrl Pts',(-10.9182248792449,9.83302584722511,
12.1396130350241));
#113449=CARTESIAN_POINT('Ctrl Pts',(-10.9261735409754,9.83245718425941,
12.1331658832771));
#113450=CARTESIAN_POINT('Ctrl Pts',(-10.9304147494144,9.83215078366186,
12.1296861242071));
#113451=CARTESIAN_POINT('Ctrl Pts',(-10.9421570453954,9.83129440296373,
12.1199410130196));
#113452=CARTESIAN_POINT('Ctrl Pts',(-10.9496149639325,9.8307412323541,12.1136243448397));
#113453=CARTESIAN_POINT('Ctrl Pts',(-10.9738749966481,9.82891277645808,
12.0926558103169));
#113454=CARTESIAN_POINT('Ctrl Pts',(-10.9904050895021,9.8276205057281,12.0776951777825));
#113455=CARTESIAN_POINT('Ctrl Pts',(-11.0644092223474,9.82164344265169,
12.0075764884374));
#113456=CARTESIAN_POINT('Ctrl Pts',(-11.1176612007506,9.8168040787014,11.9481615623249));
#113457=CARTESIAN_POINT('Ctrl Pts',(-11.2223438010768,9.80642700587287,
11.8102177226744));
#113458=CARTESIAN_POINT('Ctrl Pts',(-11.2716120844529,9.80094566884931,
11.73046889136));
#113459=CARTESIAN_POINT('Ctrl Pts',(-11.3182656332789,9.79507576618525,
11.6357306500799));
#113460=CARTESIAN_POINT('Ctrl Pts',(-11.323460518529,9.79440986951528,11.624843986457));
#113461=CARTESIAN_POINT('Ctrl Pts',(-11.3317247335049,9.79332974258818,
11.6069595053183));
#113462=CARTESIAN_POINT('Ctrl Pts',(-11.3348748313196,9.79291278315802,
11.5999998289309));
#113463=CARTESIAN_POINT('Ctrl Pts',(-11.3404211610531,9.79216900387095,
11.5874861223305));
#113464=CARTESIAN_POINT('Ctrl Pts',(-11.3428377104716,9.79184150328524,
11.5819413353436));
#113465=CARTESIAN_POINT('Ctrl Pts',(-11.3478978920332,9.79114826628413,
11.5701313541925));
#113466=CARTESIAN_POINT('Ctrl Pts',(-11.3505323785172,9.79078284274585,
11.5638623813337));
#113467=CARTESIAN_POINT('Ctrl Pts',(-11.3574959711797,9.78980450487223,
11.5469631395508));
#113468=CARTESIAN_POINT('Ctrl Pts',(-11.3617439224967,9.78919429769688,
11.5362998110006));
#113469=CARTESIAN_POINT('Ctrl Pts',(-11.3829166876477,9.78608060602992,
11.4812772567377));
#113470=CARTESIAN_POINT('Ctrl Pts',(-11.3978019122915,9.78364474708211,
11.4361613868698));
#113471=CARTESIAN_POINT('Ctrl Pts',(-11.4457360101786,9.77461698310313,
11.2629805251056));
#113472=CARTESIAN_POINT('Ctrl Pts',(-11.4635701272462,9.76846159256352,
11.1313942033913));
#113473=CARTESIAN_POINT('Ctrl Pts',(-11.4634997927887,9.76174222740085,
10.9992212140726));
#113474=CARTESIAN_POINT('Ctrl Pts',(-11.4634998220212,9.68830620133612,
10.9992782355534));
#113475=CARTESIAN_POINT('Ctrl Pts',(-11.4635429469811,9.69343852619092,
11.0867214055635));
#113476=CARTESIAN_POINT('Ctrl Pts',(-11.4557491548704,9.69876645421532,
11.173991636853));
#113477=CARTESIAN_POINT('Ctrl Pts',(-11.4300728543198,9.70739539864329,
11.316195617827));
#113478=CARTESIAN_POINT('Ctrl Pts',(-11.416658284113,9.71075321983715,11.3717100266276));
#113479=CARTESIAN_POINT('Ctrl Pts',(-11.390318033565,9.7159285351877,11.4582147519796));
#113480=CARTESIAN_POINT('Ctrl Pts',(-11.3795125452969,9.71780551448472,
11.4897860587433));
#113481=CARTESIAN_POINT('Ctrl Pts',(-11.3639897141292,9.72021344075026,
11.5305367850858));
#113482=CARTESIAN_POINT('Ctrl Pts',(-11.3602421131619,9.72077586490582,
11.5400727928912));
#113483=CARTESIAN_POINT('Ctrl Pts',(-11.3539419976944,9.72169138470325,
11.5556221511588));
#113484=CARTESIAN_POINT('Ctrl Pts',(-11.3514488604297,9.72204643757071,
11.5616590491941));
#113485=CARTESIAN_POINT('Ctrl Pts',(-11.346539826344,9.72273179772204,11.5733238633946));
#113486=CARTESIAN_POINT('Ctrl Pts',(-11.3441288548648,9.72306226077398,
11.5789536936174));
#113487=CARTESIAN_POINT('Ctrl Pts',(-11.338464895733,9.7238246716408,11.5919534330316));
#113488=CARTESIAN_POINT('Ctrl Pts',(-11.335186238294,9.72425574569722,11.5993119859952));
#113489=CARTESIAN_POINT('Ctrl Pts',(-11.3243105692131,9.72565315847926,
11.6231888328617));
#113490=CARTESIAN_POINT('Ctrl Pts',(-11.3164663239234,9.7266111240623,11.6395930435499));
#113491=CARTESIAN_POINT('Ctrl Pts',(-11.2592852667694,9.73326631203767,
11.7536607779819));
#113492=CARTESIAN_POINT('Ctrl Pts',(-11.1994388078099,9.73856815202739,
11.8456671707993));
#113493=CARTESIAN_POINT('Ctrl Pts',(-11.0905891970258,9.74690665917458,
11.977891282018));
#113494=CARTESIAN_POINT('Ctrl Pts',(-11.0483033289548,9.74992553095584,
12.0230910591678));
#113495=CARTESIAN_POINT('Ctrl Pts',(-10.9895166896113,9.75404501277318,
12.0784464899131));
#113496=CARTESIAN_POINT('Ctrl Pts',(-10.975494703158,9.75502257273336,12.0911462496094));
#113497=CARTESIAN_POINT('Ctrl Pts',(-10.9546584559813,9.75647462664689,
12.1092950266589));
#113498=CARTESIAN_POINT('Ctrl Pts',(-10.9480349614829,9.75693613029575,
12.1149609539311));
#113499=CARTESIAN_POINT('Ctrl Pts',(-10.9361223498875,9.75776682627462,
12.1249684503344));
#113500=CARTESIAN_POINT('Ctrl Pts',(-10.9308525993667,9.75813452659437,
12.1293327688653));
#113501=CARTESIAN_POINT('Ctrl Pts',(-10.9225259901414,9.75871622076786,
12.1361308521409));
#113502=CARTESIAN_POINT('Ctrl Pts',(-10.9194895916721,9.75892848693532,
12.1385896564424));
#113503=CARTESIAN_POINT('Ctrl Pts',(-10.9139896395615,9.75931330680082,
12.1430070401583));
#113504=CARTESIAN_POINT('Ctrl Pts',(-10.9115295793716,9.75948555673964,
12.1449698600876));
#113505=CARTESIAN_POINT('Ctrl Pts',(-10.9057789791387,9.75988849185047,
12.1495278392403));
#113506=CARTESIAN_POINT('Ctrl Pts',(-10.9024836357942,9.76011960113006,
12.1521167902901));
#113507=CARTESIAN_POINT('Ctrl Pts',(-10.8928314675794,9.76079702390766,
12.1596330922909));
#113508=CARTESIAN_POINT('Ctrl Pts',(-10.8864451905178,9.76124585872733,
12.1645221580183));
#113509=CARTESIAN_POINT('Ctrl Pts',(-10.8362239141879,9.76477816533409,
12.2023169765479));
#113510=CARTESIAN_POINT('Ctrl Pts',(-10.7906156643839,9.7680005774255,12.2327863858057));
#113511=CARTESIAN_POINT('Ctrl Pts',(-10.687479380953,9.77514723503009,12.2936076255848));
#113512=CARTESIAN_POINT('Ctrl Pts',(-10.6294141741077,9.77908159320722,
12.322832774934));
#113513=CARTESIAN_POINT('Ctrl Pts',(-10.5169954982628,9.78636945884805,
12.3703317460775));
#113514=CARTESIAN_POINT('Ctrl Pts',(-10.4631320092967,9.78973020310004,
12.3894614726743));
#113515=CARTESIAN_POINT('Ctrl Pts',(-10.3762331927796,9.79490937830925,
12.4147066087068));
#113516=CARTESIAN_POINT('Ctrl Pts',(-10.3438715931174,9.79678740572847,
12.4229191068024));
#113517=CARTESIAN_POINT('Ctrl Pts',(-10.3012424951101,9.79919645198739,
12.4321976886779));
#113518=CARTESIAN_POINT('Ctrl Pts',(-10.2912066951425,9.79975898453359,
12.4342719158109));
#113519=CARTESIAN_POINT('Ctrl Pts',(-10.2747396865461,9.80067463530868,
12.4374953975996));
#113520=CARTESIAN_POINT('Ctrl Pts',(-10.2683212197175,9.8010297118396,12.4387072803223));
#113521=CARTESIAN_POINT('Ctrl Pts',(-10.2558695753907,9.80171508660512,
12.4409720727719));
#113522=CARTESIAN_POINT('Ctrl Pts',(-10.2498374885065,9.80204554084979,
12.4420301609263));
#113523=CARTESIAN_POINT('Ctrl Pts',(-10.2358568034387,9.80280788678733,
12.4443921542127));
#113524=CARTESIAN_POINT('Ctrl Pts',(-10.2279036872808,9.8032389051946,12.4456683712739));
#113525=CARTESIAN_POINT('Ctrl Pts',(-10.2019716093904,9.80463594455662,
12.4496103113135));
#113526=CARTESIAN_POINT('Ctrl Pts',(-10.1839530810802,9.80559359873114,
12.4520068484133));
#113527=CARTESIAN_POINT('Ctrl Pts',(-10.0570708613357,9.81225447752986,
12.4664827987086));
#113528=CARTESIAN_POINT('Ctrl Pts',(-9.94719826427292,9.8175613665428,12.4666435572833));
#113529=CARTESIAN_POINT('Ctrl Pts',(-9.77694941808122,9.8259016078335,12.4477204837495));
#113530=CARTESIAN_POINT('Ctrl Pts',(-9.71606765643149,9.82891675932577,
12.4370203953792));
#113531=CARTESIAN_POINT('Ctrl Pts',(-9.63767457849472,9.83303153034887,
12.4180655362463));
#113532=CARTESIAN_POINT('Ctrl Pts',(-9.61938948424919,9.83400838726915,
12.4132675453968));
#113533=CARTESIAN_POINT('Ctrl Pts',(-9.58893787359339,9.83567157807621,
12.4046432582679));
#113534=CARTESIAN_POINT('Ctrl Pts',(-9.57671886680961,9.83634888157252,
12.401009570026));
#113535=CARTESIAN_POINT('Ctrl Pts',(-9.55979474875185,9.837302817685,12.3957350709302));
#113536=CARTESIAN_POINT('Ctrl Pts',(-9.55504786047416,9.83757212262337,
12.3942290498799));
#113537=CARTESIAN_POINT('Ctrl Pts',(-9.54699805697024,9.83803192262449,
12.3916298335306));
#113538=CARTESIAN_POINT('Ctrl Pts',(-9.54369113488434,9.83822170800693,
12.3905490186924));
#113539=CARTESIAN_POINT('Ctrl Pts',(-9.53733812669189,9.83858808635694,
12.3884475363546));
#113540=CARTESIAN_POINT('Ctrl Pts',(-9.53429150890127,9.83876456972674,
12.3874286183912));
#113541=CARTESIAN_POINT('Ctrl Pts',(-9.52697502377209,9.83919024236874,
12.384954862183));
#113542=CARTESIAN_POINT('Ctrl Pts',(-9.52270850650006,9.83943998368531,
12.383490306276));
#113543=CARTESIAN_POINT('Ctrl Pts',(-9.50710151365549,9.84035892421729,
12.3780521501353));
#113544=CARTESIAN_POINT('Ctrl Pts',(-9.49580363399297,9.84103458417673,
12.3739587519168));
#113545=CARTESIAN_POINT('Ctrl Pts',(-9.41261059788289,9.84608072569973,
12.3426523637845));
#113546=CARTESIAN_POINT('Ctrl Pts',(-9.34291418490526,9.85069586025734,
12.30995342135));
#113547=CARTESIAN_POINT('Ctrl Pts',(-9.2189234356124,9.85928053045996,12.2393877085059));
#113548=CARTESIAN_POINT('Ctrl Pts',(-9.16398945000605,9.86323843381767,
12.2030169539097));
#113549=CARTESIAN_POINT('Ctrl Pts',(-9.06569624426849,9.87049425980762,
12.1279440729478));
#113550=CARTESIAN_POINT('Ctrl Pts',(-9.02182512190009,9.87380861048452,
12.0901176590184));
#113551=CARTESIAN_POINT('Ctrl Pts',(-8.97161104040798,9.87768991826784,
12.0413430321092));
#113552=CARTESIAN_POINT('Ctrl Pts',(-8.96302173434888,9.87835732588763,
12.0327900327079));
#113553=CARTESIAN_POINT('Ctrl Pts',(-8.94968210782994,9.87939964046026,
12.0191725843584));
#113554=CARTESIAN_POINT('Ctrl Pts',(-8.9448600084295,9.8797776488194,12.0141794869829));
#113555=CARTESIAN_POINT('Ctrl Pts',(-8.93591359088611,9.880481345071,12.0047829416177));
#113556=CARTESIAN_POINT('Ctrl Pts',(-8.93178063984191,9.88080739839743,
12.0003879477035));
#113557=CARTESIAN_POINT('Ctrl Pts',(-8.92261436664782,9.88153278063923,
11.9905189262006));
#113558=CARTESIAN_POINT('Ctrl Pts',(-8.91759533169696,9.88193150405114,
11.9850318182257));
#113559=CARTESIAN_POINT('Ctrl Pts',(-8.90499464957722,9.88293662058158,
11.9710433967644));
#113560=CARTESIAN_POINT('Ctrl Pts',(-8.89746995658573,9.8835406612028,11.9624913032657));
#113561=CARTESIAN_POINT('Ctrl Pts',(-8.85183475573293,9.88722952750027,
11.9093876956457));
#113562=CARTESIAN_POINT('Ctrl Pts',(-8.81632804306537,9.890208133278,11.8626651151827));
#113563=CARTESIAN_POINT('Ctrl Pts',(-8.78168562879809,9.89330338755409,
11.8108980757707));
#113564=CARTESIAN_POINT('Ctrl Pts',(-8.77966521118386,9.89348467383459,
11.8078543183925));
#113565=CARTESIAN_POINT('Ctrl Pts',(-8.72391876214443,9.89850852208393,
11.7231859901556));
#113566=CARTESIAN_POINT('Ctrl Pts',(-8.67849356435907,9.90315067663834,
11.6363966667992));
#113567=CARTESIAN_POINT('Ctrl Pts',(-8.62462901023069,9.91034824039895,
11.5023656581116));
#113568=CARTESIAN_POINT('Ctrl Pts',(-8.60928983286015,9.91272809556236,
11.4581932536058));
#113569=CARTESIAN_POINT('Ctrl Pts',(-8.59396044537834,9.91562070779918,
11.4061304372609));
#113570=CARTESIAN_POINT('Ctrl Pts',(-8.59188567973241,9.91602563134109,
11.3988774466754));
#113571=CARTESIAN_POINT('Ctrl Pts',(-8.58878771090022,9.91665185139239,
11.3877220624297));
#113572=CARTESIAN_POINT('Ctrl Pts',(-8.58772438426416,9.91687092808195,
11.3838308312346));
#113573=CARTESIAN_POINT('Ctrl Pts',(-8.58579974831586,9.91727526022663,
11.3766713703653));
#113574=CARTESIAN_POINT('Ctrl Pts',(-8.58493366099531,9.91746024180222,
11.3734045108452));
#113575=CARTESIAN_POINT('Ctrl Pts',(-8.58300320454476,9.91787948662472,
11.3660197012764));
#113576=CARTESIAN_POINT('Ctrl Pts',(-8.58194547233547,9.91811411606763,
11.3619001183897));
#113577=CARTESIAN_POINT('Ctrl Pts',(-8.57926135294477,9.91872231905239,
11.3512537417045));
#113578=CARTESIAN_POINT('Ctrl Pts',(-8.57766199614514,9.91909734166273,
11.3447203121438));
#113579=CARTESIAN_POINT('Ctrl Pts',(-8.5676318837832,9.92153192026289,11.3024884863029));
#113580=CARTESIAN_POINT('Ctrl Pts',(-8.56050132560197,9.92365455854974,
11.2664973740121));
#113581=CARTESIAN_POINT('Ctrl Pts',(-8.53885626972182,9.93175253910585,
11.1306497032781));
#113582=CARTESIAN_POINT('Ctrl Pts',(-8.53332596227692,9.9379243020373,11.0296452501177));
#113583=CARTESIAN_POINT('Ctrl Pts',(-8.54130347976066,9.94763752349695,
10.8656975168665));
#113584=CARTESIAN_POINT('Ctrl Pts',(-8.54846979039542,9.95129669376925,
10.8027835502904));
#113585=CARTESIAN_POINT('Ctrl Pts',(-8.56258476452079,9.95574547976785,
10.7244332899017));
#113586=CARTESIAN_POINT('Ctrl Pts',(-8.56575310042201,9.95665081479642,
10.708391645769));
#113587=CARTESIAN_POINT('Ctrl Pts',(-8.57083036558007,9.95797594845148,
10.6847741395887));
#113588=CARTESIAN_POINT('Ctrl Pts',(-8.5725321095842,9.95840222216736,10.6771554365603));
#113589=CARTESIAN_POINT('Ctrl Pts',(-8.57566499203983,9.95915644999239,
10.6636387920155));
#113590=CARTESIAN_POINT('Ctrl Pts',(-8.5770720021878,9.9594851584985,10.6577354945192));
#113591=CARTESIAN_POINT('Ctrl Pts',(-8.58011142853446,9.96017474539921,
10.6453259416234));
#113592=CARTESIAN_POINT('Ctrl Pts',(-8.58175194198266,9.96053535807072,
10.6388218015498));
#113593=CARTESIAN_POINT('Ctrl Pts',(-8.58621362830064,9.9614863892437,10.6216318115937));
#113594=CARTESIAN_POINT('Ctrl Pts',(-8.58911125472945,9.96207436368118,
10.6109661349416));
#113595=CARTESIAN_POINT('Ctrl Pts',(-8.60233052175095,9.96463330963514,
10.5643996986256));
#113596=CARTESIAN_POINT('Ctrl Pts',(-8.61390406095152,9.96656408278289,
10.5288673865308));
#113597=CARTESIAN_POINT('Ctrl Pts',(-8.67625315595973,9.97571408849073,
10.3597273146995));
#113598=CARTESIAN_POINT('Ctrl Pts',(-8.74504551395334,9.98232925048296,
10.2336208292813));
#113599=CARTESIAN_POINT('Ctrl Pts',(-8.843431449092,9.99063955110981,10.1030007509666));
#113600=CARTESIAN_POINT('Ctrl Pts',(-8.85619945949582,9.99170285182257,
10.0867756476086));
#113601=CARTESIAN_POINT('Ctrl Pts',(-8.87794811720875,9.99349936051039,
10.0603100982597));
#113602=CARTESIAN_POINT('Ctrl Pts',(-8.88673640826825,9.99422155671268,
10.0499149047499));
#113603=CARTESIAN_POINT('Ctrl Pts',(-8.89902131959352,9.99522839606229,
10.0357882454523));
#113604=CARTESIAN_POINT('Ctrl Pts',(-8.90239466250804,9.99550459446113,
10.0319499579769));
#113605=CARTESIAN_POINT('Ctrl Pts',(-8.90811519392663,9.99597267122059,
10.0255093117909));
#113606=CARTESIAN_POINT('Ctrl Pts',(-8.9104517893094,9.99616377734365,10.0228975348321));
#113607=CARTESIAN_POINT('Ctrl Pts',(-8.91492944366567,9.99652989306577,
10.0179285779094));
#113608=CARTESIAN_POINT('Ctrl Pts',(-8.91706885022544,9.99670477428029,
10.0155699543599));
#113609=CARTESIAN_POINT('Ctrl Pts',(-8.92218539782627,9.99712286147057,
10.0099659960374));
#113610=CARTESIAN_POINT('Ctrl Pts',(-8.92516950622037,9.99736657795279,
10.006727099794));
#113611=CARTESIAN_POINT('Ctrl Pts',(-8.93583702345718,9.99823721170144,
9.99525313592193));
#113612=CARTESIAN_POINT('Ctrl Pts',(-8.94360062944579,9.99886974609392,
9.98709356021656));
#113613=CARTESIAN_POINT('Ctrl Pts',(-9.02052780910603,10.0051194244367,
9.90808927631429));
#113614=CARTESIAN_POINT('Ctrl Pts',(-9.09661340340824,10.0111427820746,
9.84435080480534));
#113615=CARTESIAN_POINT('Ctrl Pts',(-9.23489428455426,10.0211756763731,
9.75056755286459));
#113616=CARTESIAN_POINT('Ctrl Pts',(-9.29384748122678,10.0252189596186,
9.71632622467873));
#113617=CARTESIAN_POINT('Ctrl Pts',(-9.37716974242864,10.0305560874737,
9.67541476174027));
#113618=CARTESIAN_POINT('Ctrl Pts',(-9.39963731902107,10.0319606905992,
9.66508115047922));
#113619=CARTESIAN_POINT('Ctrl Pts',(-9.43908455854085,10.0343672126787,
9.64813552162616));
#113620=CARTESIAN_POINT('Ctrl Pts',(-9.45594533499729,10.0353774484928,
9.6412622535473));
#113621=CARTESIAN_POINT('Ctrl Pts',(-9.48053192370348,10.036824716506,9.63177064775783));
#113622=CARTESIAN_POINT('Ctrl Pts',(-9.48815780350037,10.0372700589915,
9.62889963450686));
#113623=CARTESIAN_POINT('Ctrl Pts',(-9.50154938097836,10.0380460182381,
9.62398523216919));
#113624=CARTESIAN_POINT('Ctrl Pts',(-9.50730460175746,10.0383775429948,
9.62191404222653));
#113625=CARTESIAN_POINT('Ctrl Pts',(-9.51925010262383,10.0390616755179,
9.6176994912034));
#113626=CARTESIAN_POINT('Ctrl Pts',(-9.52544213627317,10.0394141019826,
9.61556148698245));
#113627=CARTESIAN_POINT('Ctrl Pts',(-9.54143913332729,10.0403190439857,
9.61015793066456));
#113628=CARTESIAN_POINT('Ctrl Pts',(-9.5512647964227,10.0408695334523,9.60695449804873));
#113629=CARTESIAN_POINT('Ctrl Pts',(-9.59075090794574,10.043061231024,9.59454209002999));
#113630=CARTESIAN_POINT('Ctrl Pts',(-9.6206682177543,10.0446754280182,9.58617386746621));
#113631=CARTESIAN_POINT('Ctrl Pts',(-9.77282805911964,10.0526907339707,
9.54879123799847));
#113632=CARTESIAN_POINT('Ctrl Pts',(-9.89816789410017,10.0586147550827,
9.53465255419911));
#113633=CARTESIAN_POINT('Ctrl Pts',(-10.0778929076538,10.0675091968103,
9.53757231172584));
#113634=CARTESIAN_POINT('Ctrl Pts',(-10.1319178438482,10.0702435540323,
9.54145326544586));
#113635=CARTESIAN_POINT('Ctrl Pts',(-10.1933019074375,10.0735394864808,
9.54930122177673));
#113636=CARTESIAN_POINT('Ctrl Pts',(-10.2009978286706,10.073956150462,9.55034747605381));
#113637=CARTESIAN_POINT('Ctrl Pts',(-10.2127240431901,10.0745967623492,
9.55203681510023));
#113638=CARTESIAN_POINT('Ctrl Pts',(-10.2167606962006,10.0748183286146,
9.552635601122));
#113639=CARTESIAN_POINT('Ctrl Pts',(-10.2241337399032,10.0752250132131,
9.55376083402037));
#113640=CARTESIAN_POINT('Ctrl Pts',(-10.227470859399,10.0754098351782,9.55428195482394));
#113641=CARTESIAN_POINT('Ctrl Pts',(-10.2349524776899,10.0758258832384,
9.55547682136548));
#113642=CARTESIAN_POINT('Ctrl Pts',(-10.2390958657187,10.0760574499858,
9.55615684837898));
#113643=CARTESIAN_POINT('Ctrl Pts',(-10.2512043440916,10.0767374377372,
9.55819768269092));
#113644=CARTESIAN_POINT('Ctrl Pts',(-10.2591610304336,10.0771884080902,
9.55960661658563));
#113645=CARTESIAN_POINT('Ctrl Pts',(-10.3249658310771,10.0809501261909,
9.57182191523864));
#113646=CARTESIAN_POINT('Ctrl Pts',(-10.3821203951458,10.0844208780651,
9.58604169478641));
#113647=CARTESIAN_POINT('Ctrl Pts',(-10.4532103132402,10.0888772009644,
9.60835411530643));
#113648=CARTESIAN_POINT('Ctrl Pts',(-10.4680864791138,10.0898178078741,
9.61328701753133));
#113649=CARTESIAN_POINT('Ctrl Pts',(-10.5262830611944,10.0935236503403,
9.63362804655819));
#113650=CARTESIAN_POINT('Ctrl Pts',(-10.5689475221038,10.0962969222659,
9.65083543288455));
#113651=CARTESIAN_POINT('Ctrl Pts',(-10.6621165046477,10.1024168949535,
9.69361905306786));
#113652=CARTESIAN_POINT('Ctrl Pts',(-10.7120943129398,10.1057428651567,
9.72017496845359));
#113653=CARTESIAN_POINT('Ctrl Pts',(-10.7887456925683,10.1108760738997,
9.76678792277443));
#113654=CARTESIAN_POINT('Ctrl Pts',(-10.8164853688777,10.1127415912754,
9.78497584981021));
#113655=CARTESIAN_POINT('Ctrl Pts',(-10.8519396333987,10.1151372642407,
9.80998502274923));
#113656=CARTESIAN_POINT('Ctrl Pts',(-10.8602325895159,10.1156984989772,
9.81596592769202));
#113657=CARTESIAN_POINT('Ctrl Pts',(-10.8737156475717,10.1166125815493,
9.82590638584195));
#113658=CARTESIAN_POINT('Ctrl Pts',(-10.8789430466826,10.1169673748126,
9.82981455733642));
#113659=CARTESIAN_POINT('Ctrl Pts',(-10.8890260497643,10.1176525754766,
9.83745861885132));
#113660=CARTESIAN_POINT('Ctrl Pts',(-10.8938846763555,10.1179831359847,
9.8411902800779));
#113661=CARTESIAN_POINT('Ctrl Pts',(-10.9050868590331,10.1187462632,9.84990647754119));
#113662=CARTESIAN_POINT('Ctrl Pts',(-10.911412949548,10.1191779509325,9.85491320341774));
#113663=CARTESIAN_POINT('Ctrl Pts',(-10.9319119848368,10.1205794862349,
9.87141447559486));
#113664=CARTESIAN_POINT('Ctrl Pts',(-10.9459116995941,10.1215408902521,
9.88312206190239));
#113665=CARTESIAN_POINT('Ctrl Pts',(-11.0412972961293,10.1281298732351,
9.96597082458304));
#113666=CARTESIAN_POINT('Ctrl Pts',(-11.1148018409877,10.1333730258618,
10.0456752531836));
#113667=CARTESIAN_POINT('Ctrl Pts',(-11.216066620657,10.141691799218,10.1833263494909));
#113668=CARTESIAN_POINT('Ctrl Pts',(-11.249975355087,10.144754103187,10.2362366285427));
#113669=CARTESIAN_POINT('Ctrl Pts',(-11.2896219527467,10.1489285484622,
10.3078500452822));
#113670=CARTESIAN_POINT('Ctrl Pts',(-11.2985361556874,10.1499142631211,
10.3247221792628));
#113671=CARTESIAN_POINT('Ctrl Pts',(-11.3128914673595,10.1515911684447,
10.3532287540284));
#113672=CARTESIAN_POINT('Ctrl Pts',(-11.3185140424906,10.1522731350291,
10.3647695321754));
#113673=CARTESIAN_POINT('Ctrl Pts',(-11.3261118520167,10.1532325786207,
10.3809002140401));
#113674=CARTESIAN_POINT('Ctrl Pts',(-11.3282166523921,10.1535026155764,
10.3854288390449));
#113675=CARTESIAN_POINT('Ctrl Pts',(-11.3317494841296,10.1539632907507,
10.3931328944634));
#113676=CARTESIAN_POINT('Ctrl Pts',(-11.3331894586537,10.1541532127041,
10.396302857886));
#113677=CARTESIAN_POINT('Ctrl Pts',(-11.3359349899429,10.1545195476271,
10.4024046081798));
#113678=CARTESIAN_POINT('Ctrl Pts',(-11.3372422321661,10.1546958489397,
10.4053355889402));
#113679=CARTESIAN_POINT('Ctrl Pts',(-11.3403588329447,10.1551206673123,
10.4123855948063));
#113680=CARTESIAN_POINT('Ctrl Pts',(-11.3421588480684,10.155369731712,10.4165086841163));
#113681=CARTESIAN_POINT('Ctrl Pts',(-11.3486599108059,10.1562827690098,
10.4315891802221));
#113682=CARTESIAN_POINT('Ctrl Pts',(-11.3532458881252,10.1569530946779,
10.4425953329252));
#113683=CARTESIAN_POINT('Ctrl Pts',(-11.3890690174472,10.1623996076468,
10.5316178874271));
#113684=CARTESIAN_POINT('Ctrl Pts',(-11.4136654823685,10.1674677008347,
10.6121311288679));
#113685=CARTESIAN_POINT('Ctrl Pts',(-11.4526326753921,10.1786934254206,
10.7945677441922));
#113686=CARTESIAN_POINT('Ctrl Pts',(-11.4634561904881,10.1848010301259,
10.8968206735927));
#113687=CARTESIAN_POINT('Ctrl Pts',(-11.4634998672784,10.1905769185562,
10.9993767215278));
#113688=CARTESIAN_POINT('Origin',(-10.,3.5,11.));
#113689=CARTESIAN_POINT('',(-11.4635,10.7604277254418,11.0000000000833));
#113690=CARTESIAN_POINT('',(-11.463499418515,10.6893450235318,11.0013046096532));
#113691=CARTESIAN_POINT('',(-11.4635,3.5,11.));
#113692=CARTESIAN_POINT('Ctrl Pts',(-11.4635,10.7604277254418,11.0000000000833));
#113693=CARTESIAN_POINT('Ctrl Pts',(-11.4635000000053,10.7547997906437,
10.9061827223186));
#113694=CARTESIAN_POINT('Ctrl Pts',(-11.4544789754102,10.749283903319,10.8125691096008));
#113695=CARTESIAN_POINT('Ctrl Pts',(-11.4345115940165,10.743453902123,10.7099604418026));
#113696=CARTESIAN_POINT('Ctrl Pts',(-11.4323553763509,10.7428614340804,
10.6994928570103));
#113697=CARTESIAN_POINT('Ctrl Pts',(-11.428576935905,10.7418815432258,10.6821155188989));
#113698=CARTESIAN_POINT('Ctrl Pts',(-11.4270187869678,10.7414921283556,
10.6751923811775));
#113699=CARTESIAN_POINT('Ctrl Pts',(-11.4238625334524,10.7407311075056,
10.6616298383438));
#113700=CARTESIAN_POINT('Ctrl Pts',(-11.4222681923137,10.740359393331,10.6549897511698));
#113701=CARTESIAN_POINT('Ctrl Pts',(-11.4191752228267,10.7396614638034,
10.6424941034062));
#113702=CARTESIAN_POINT('Ctrl Pts',(-11.4176866857666,10.7393349362192,
10.6366362130144));
#113703=CARTESIAN_POINT('Ctrl Pts',(-11.4142462240952,10.7386007706892,
10.6234398757249));
#113704=CARTESIAN_POINT('Ctrl Pts',(-11.4122733801302,10.7381938087947,
10.6161070301772));
#113705=CARTESIAN_POINT('Ctrl Pts',(-11.4070597360085,10.7371531327239,
10.5973127670552));
#113706=CARTESIAN_POINT('Ctrl Pts',(-11.4037358977619,10.7365220768464,
10.5858748394572));
#113707=CARTESIAN_POINT('Ctrl Pts',(-11.3790129158789,10.7320474974723,
10.5045183856098));
#113708=CARTESIAN_POINT('Ctrl Pts',(-11.3525391369504,10.7283742235854,
10.4362463170501));
#113709=CARTESIAN_POINT('Ctrl Pts',(-11.297519344144,10.7220857438647,10.3208306435393));
#113710=CARTESIAN_POINT('Ctrl Pts',(-11.2712159816375,10.7194398415474,
10.2727879009053));
#113711=CARTESIAN_POINT('Ctrl Pts',(-11.203493963091,10.7131861618418,10.1640462662085));
#113712=CARTESIAN_POINT('Ctrl Pts',(-11.1600786676837,10.7095673986135,
10.104772935813));
#113713=CARTESIAN_POINT('Ctrl Pts',(-11.1057233052021,10.7051458763059,
10.0411913265861));
#113714=CARTESIAN_POINT('Ctrl Pts',(-11.0989558077283,10.704597031036,10.0334420758216));
#113715=CARTESIAN_POINT('Ctrl Pts',(-11.0890178418926,10.703792353166,10.0223017184476));
#113716=CARTESIAN_POINT('Ctrl Pts',(-11.0859119080876,10.7035410446066,
10.0188531626722));
#113717=CARTESIAN_POINT('Ctrl Pts',(-11.0804887171331,10.7031024318616,
10.0128890235853));
#113718=CARTESIAN_POINT('Ctrl Pts',(-11.0781789272478,10.702915679546,10.0103666596512));
#113719=CARTESIAN_POINT('Ctrl Pts',(-11.0732921319586,10.7025206472851,
10.0050675397512));
#113720=CARTESIAN_POINT('Ctrl Pts',(-11.0707131849895,10.7023122270468,
10.0022926903127));
#113721=CARTESIAN_POINT('Ctrl Pts',(-11.0637374129124,10.7017486940809,
9.99484521988085));
#113722=CARTESIAN_POINT('Ctrl Pts',(-11.0593206371623,10.7013921225682,
9.99019150319104));
#113723=CARTESIAN_POINT('Ctrl Pts',(-11.0391466323553,10.6997651433688,
9.96921325798015));
#113724=CARTESIAN_POINT('Ctrl Pts',(-11.0230424470121,10.698471047192,9.95322826347696));
#113725=CARTESIAN_POINT('Ctrl Pts',(-10.9419777833616,10.6920086190878,
9.87642149131234));
#113726=CARTESIAN_POINT('Ctrl Pts',(-10.8719367980879,10.686595600217,9.82123965520631));
#113727=CARTESIAN_POINT('Ctrl Pts',(-10.7429753074925,10.6773729660338,
9.73745492201226));
#113728=CARTESIAN_POINT('Ctrl Pts',(-10.6863399904447,10.6735343819576,
9.70579322690261));
#113729=CARTESIAN_POINT('Ctrl Pts',(-10.6061086226439,10.6684341491352,
9.66769352429766));
#113730=CARTESIAN_POINT('Ctrl Pts',(-10.5841789489759,10.6670721982255,
9.65793321504449));
#113731=CARTESIAN_POINT('Ctrl Pts',(-10.5457162266694,10.6647387806049,
9.64193601883193));
#113732=CARTESIAN_POINT('Ctrl Pts',(-10.5292923931357,10.6637594423995,
9.63545114499648));
#113733=CARTESIAN_POINT('Ctrl Pts',(-10.5051469880933,10.6623438921197,
9.62641900613032));
#113734=CARTESIAN_POINT('Ctrl Pts',(-10.4975155991831,10.6618999752809,
9.623636509283));
#113735=CARTESIAN_POINT('Ctrl Pts',(-10.484102711134,10.6611257335106,9.6188721417314));
#113736=CARTESIAN_POINT('Ctrl Pts',(-10.4783312763615,10.6607945116493,
9.6168627011633));
#113737=CARTESIAN_POINT('Ctrl Pts',(-10.4663405450099,10.66011029016,9.61277191687501));
#113738=CARTESIAN_POINT('Ctrl Pts',(-10.4601194965109,10.6597574769935,
9.61069610618399));
#113739=CARTESIAN_POINT('Ctrl Pts',(-10.4440220735393,10.6588500421336,
9.60544477704503));
#113740=CARTESIAN_POINT('Ctrl Pts',(-10.4341254186934,10.6582974694394,
9.60233229990579));
#113741=CARTESIAN_POINT('Ctrl Pts',(-10.3941506688643,10.6560860361381,
9.59022589019884));
#113742=CARTESIAN_POINT('Ctrl Pts',(-10.3638187791932,10.654454826036,9.58209525359855));
#113743=CARTESIAN_POINT('Ctrl Pts',(-10.210611033843,10.6464094247904,9.54626778635204));
#113744=CARTESIAN_POINT('Ctrl Pts',(-10.0847950563064,10.6404733768689,
9.53354066210397));
#113745=CARTESIAN_POINT('Ctrl Pts',(-9.90550159441945,10.6315925785157,
9.53857726136514));
#113746=CARTESIAN_POINT('Ctrl Pts',(-9.85222588322448,10.6288917342299,
9.54300032109587));
#113747=CARTESIAN_POINT('Ctrl Pts',(-9.79164345380039,10.6256341319354,
9.55138693564193));
#113748=CARTESIAN_POINT('Ctrl Pts',(-9.78397870311705,10.6252185273544,
9.55251008478071));
#113749=CARTESIAN_POINT('Ctrl Pts',(-9.77229532635904,10.6245792502028,
9.55431696245804));
#113750=CARTESIAN_POINT('Ctrl Pts',(-9.76826992439674,10.6243579447619,
9.55495673605292));
#113751=CARTESIAN_POINT('Ctrl Pts',(-9.76091458126963,10.6239515657501,
9.55615727468522));
#113752=CARTESIAN_POINT('Ctrl Pts',(-9.75758386182619,10.623766786603,9.55671275613981));
#113753=CARTESIAN_POINT('Ctrl Pts',(-9.75011299774511,10.6233506200677,
9.55798530150694));
#113754=CARTESIAN_POINT('Ctrl Pts',(-9.74597403330262,10.6231188902979,
9.55870866515151));
#113755=CARTESIAN_POINT('Ctrl Pts',(-9.7338682322749,10.6224378141069,9.5608781517215));
#113756=CARTESIAN_POINT('Ctrl Pts',(-9.72591034288388,10.6219859056689,
9.56237255667462));
#113757=CARTESIAN_POINT('Ctrl Pts',(-9.64613387633493,10.6174162300859,
9.57804015296798));
#113758=CARTESIAN_POINT('Ctrl Pts',(-9.57546875835911,10.6130521952094,
9.59751572274386));
#113759=CARTESIAN_POINT('Ctrl Pts',(-9.43477622288705,10.6040712484098,
9.64790202351978));
#113760=CARTESIAN_POINT('Ctrl Pts',(-9.36510187618191,10.5994671019091,
9.67918487573041));
#113761=CARTESIAN_POINT('Ctrl Pts',(-9.24799583018466,10.5916426884488,
9.74318155588011));
#113762=CARTESIAN_POINT('Ctrl Pts',(-9.19945797605669,10.5883689035972,
9.77352677922071));
#113763=CARTESIAN_POINT('Ctrl Pts',(-9.14296437931245,10.5845278802939,
9.81363236433785));
#113764=CARTESIAN_POINT('Ctrl Pts',(-9.13319939791361,10.5838626515886,
9.82074813948062));
#113765=CARTESIAN_POINT('Ctrl Pts',(-9.11797237170055,10.5828230270341,
9.83213546994633));
#113766=CARTESIAN_POINT('Ctrl Pts',(-9.11245079897331,10.5824455551042,
9.83632619875833));
#113767=CARTESIAN_POINT('Ctrl Pts',(-9.10218044643509,10.581742454745,9.84423675316168));
#113768=CARTESIAN_POINT('Ctrl Pts',(-9.0974245043081,10.5814164647094,9.8479470022687));
#113769=CARTESIAN_POINT('Ctrl Pts',(-9.08685053275288,10.5806907157047,
9.85630173647957));
#113770=CARTESIAN_POINT('Ctrl Pts',(-9.08104470595801,10.5802915664637,
9.86096144146016));
#113771=CARTESIAN_POINT('Ctrl Pts',(-9.06642252352293,10.5792844352352,
9.87288164750657));
#113772=CARTESIAN_POINT('Ctrl Pts',(-9.05765505251029,10.5786788235582,
9.88020149367515));
#113773=CARTESIAN_POINT('Ctrl Pts',(-9.00385929888975,10.5749502684628,
9.92619415363525));
#113774=CARTESIAN_POINT('Ctrl Pts',(-8.96113039516,10.5719363718953,9.96747578191413));
#113775=CARTESIAN_POINT('Ctrl Pts',(-8.85340019644995,10.5640174156504,
10.0850357735143));
#113776=CARTESIAN_POINT('Ctrl Pts',(-8.79352916509664,10.5592671757975,
10.1655676053775));
#113777=CARTESIAN_POINT('Ctrl Pts',(-8.72601741250604,10.5526923763829,
10.2790144626755));
#113778=CARTESIAN_POINT('Ctrl Pts',(-8.71059178427471,10.5510782929004,
10.3069790668705));
#113779=CARTESIAN_POINT('Ctrl Pts',(-8.69042051100301,10.5487732323348,
10.3465553555071));
#113780=CARTESIAN_POINT('Ctrl Pts',(-8.68489007457613,10.548118464817,10.3577584511645));
#113781=CARTESIAN_POINT('Ctrl Pts',(-8.67549826833073,10.5469634886149,
10.3774136740671));
#113782=CARTESIAN_POINT('Ctrl Pts',(-8.67157264501839,10.5464667068261,
10.3858344488774));
#113783=CARTESIAN_POINT('Ctrl Pts',(-8.66591256486667,10.5457285695778,
10.3982839566248));
#113784=CARTESIAN_POINT('Ctrl Pts',(-8.66411554168054,10.5454908392508,
10.4022841858802));
#113785=CARTESIAN_POINT('Ctrl Pts',(-8.66097425502319,10.5450691478249,
10.4093617173169));
#113786=CARTESIAN_POINT('Ctrl Pts',(-8.65962256978433,10.5448856363975,
10.4124356452021));
#113787=CARTESIAN_POINT('Ctrl Pts',(-8.65671542884547,10.544486423175,10.4191091440517));
#113788=CARTESIAN_POINT('Ctrl Pts',(-8.65516388054255,10.5442705023026,
10.4227102662513));
#113789=CARTESIAN_POINT('Ctrl Pts',(-8.65094696472251,10.5436758260625,
10.4326069297103));
#113790=CARTESIAN_POINT('Ctrl Pts',(-8.64831124327319,10.543295374688,10.4389148999977));
#113791=CARTESIAN_POINT('Ctrl Pts',(-8.63499914609308,10.541328980494,10.4714124494827));
#113792=CARTESIAN_POINT('Ctrl Pts',(-8.62504000210766,10.5397058963187,
10.4978875382606));
#113793=CARTESIAN_POINT('Ctrl Pts',(-8.60700287756042,10.536467589061,10.5504069223544));
#113794=CARTESIAN_POINT('Ctrl Pts',(-8.59887299529019,10.5348548222039,
10.5764224727577));
#113795=CARTESIAN_POINT('Ctrl Pts',(-8.56242015342782,10.5268469986105,
10.7056400258164));
#113796=CARTESIAN_POINT('Ctrl Pts',(-8.54474635359602,10.5203248068903,
10.81152067943));
#113797=CARTESIAN_POINT('Ctrl Pts',(-8.53613325584113,10.5113496713486,
10.9657262283736));
#113798=CARTESIAN_POINT('Ctrl Pts',(-8.53579108875596,10.5086535053874,
11.0131722768093));
#113799=CARTESIAN_POINT('Ctrl Pts',(-8.53822806765231,10.5053923791101,
11.0720187922413));
#113800=CARTESIAN_POINT('Ctrl Pts',(-8.53883760063605,10.5047612489473,
11.0834765943436));
#113801=CARTESIAN_POINT('Ctrl Pts',(-8.54002281901201,10.5037627499132,
11.1017108967944));
#113802=CARTESIAN_POINT('Ctrl Pts',(-8.54051109335387,10.5033926978334,
11.1084924378788));
#113803=CARTESIAN_POINT('Ctrl Pts',(-8.54152301812002,10.5026962021431,
11.1213001571628));
#113804=CARTESIAN_POINT('Ctrl Pts',(-8.5420368031537,10.502369460854,11.1273269529748));
#113805=CARTESIAN_POINT('Ctrl Pts',(-8.54328414426527,10.5016325807481,
11.1409593773818));
#113806=CARTESIAN_POINT('Ctrl Pts',(-8.54403993195253,10.5012231390261,
11.1485628273439));
#113807=CARTESIAN_POINT('Ctrl Pts',(-8.54614282808425,10.5001717564433,
11.1681582176433));
#113808=CARTESIAN_POINT('Ctrl Pts',(-8.54757878212707,10.4995325689911,
11.1801401670374));
#113809=CARTESIAN_POINT('Ctrl Pts',(-8.56142465634995,10.493983624911,11.2847095162364));
#113810=CARTESIAN_POINT('Ctrl Pts',(-8.58252471416636,10.4893640179191,
11.3759322176457));
#113811=CARTESIAN_POINT('Ctrl Pts',(-8.63349335585492,10.4815342436606,
11.5282051175993));
#113812=CARTESIAN_POINT('Ctrl Pts',(-8.65916283878904,10.4782967890616,
11.5903355746889));
#113813=CARTESIAN_POINT('Ctrl Pts',(-8.70249735519559,10.4734297386707,
11.6776728785523));
#113814=CARTESIAN_POINT('Ctrl Pts',(-8.7168310180172,10.4718916897755,11.7044365231716));
#113815=CARTESIAN_POINT('Ctrl Pts',(-8.73801513088745,10.4696872486856,
11.7411965099131));
#113816=CARTESIAN_POINT('Ctrl Pts',(-8.74417376612101,10.4690537202878,
11.7515840137387));
#113817=CARTESIAN_POINT('Ctrl Pts',(-8.75517052594085,10.4679329897077,
11.7696191918838));
#113818=CARTESIAN_POINT('Ctrl Pts',(-8.75995242070123,10.4674489422033,
11.7773005293559));
#113819=CARTESIAN_POINT('Ctrl Pts',(-8.76713211262178,10.4667262338022,
11.7885986597269));
#113820=CARTESIAN_POINT('Ctrl Pts',(-8.76947535368254,10.4664909841474,
11.7922500663805));
#113821=CARTESIAN_POINT('Ctrl Pts',(-8.77367535751717,10.4660703233456,
11.7987312290063));
#113822=CARTESIAN_POINT('Ctrl Pts',(-8.77552574034814,10.4658853288083,
11.801565026762));
#113823=CARTESIAN_POINT('Ctrl Pts',(-8.77956574666803,10.4654821230287,
11.8077055226295));
#113824=CARTESIAN_POINT('Ctrl Pts',(-8.7817589544364,10.4652636830626,11.8110096991619));
#113825=CARTESIAN_POINT('Ctrl Pts',(-8.78787844200941,10.464655522755,11.8201481778294));
#113826=CARTESIAN_POINT('Ctrl Pts',(-8.79183333351764,10.4642639819811,
11.8259630784298));
#113827=CARTESIAN_POINT('Ctrl Pts',(-8.81346592532299,10.462131347131,11.8572818010132));
#113828=CARTESIAN_POINT('Ctrl Pts',(-8.83190838480165,10.4603454650886,
11.8822453771999));
#113829=CARTESIAN_POINT('Ctrl Pts',(-8.86304368663352,10.4574046766675,
11.9217008884223));
#113830=CARTESIAN_POINT('Ctrl Pts',(-8.87525467564313,10.456268190878,11.9365629185263));
#113831=CARTESIAN_POINT('Ctrl Pts',(-8.94208266334871,10.450153672356,12.014707070443));
#113832=CARTESIAN_POINT('Ctrl Pts',(-9.00175375946532,10.4450682431004,
12.0734638825186));
#113833=CARTESIAN_POINT('Ctrl Pts',(-9.11756677632043,10.4361436807626,
12.1694482867504));
#113834=CARTESIAN_POINT('Ctrl Pts',(-9.17188182685075,10.4322672649661,
12.2085196839747));
#113835=CARTESIAN_POINT('Ctrl Pts',(-9.24296794176158,10.4275894007463,
12.2526041813151));
#113836=CARTESIAN_POINT('Ctrl Pts',(-9.25740438863672,10.4266581803532,
12.261216303078));
#113837=CARTESIAN_POINT('Ctrl Pts',(-9.27883228470759,10.4253028364607,
12.2735036916358));
#113838=CARTESIAN_POINT('Ctrl Pts',(-9.28570987031505,10.4248718040947,
12.2773739234167));
#113839=CARTESIAN_POINT('Ctrl Pts',(-9.29793935008301,10.4241122860226,
12.2841261759115));
#113840=CARTESIAN_POINT('Ctrl Pts',(-9.30327848434095,10.4237830073013,
12.2870308166398));
#113841=CARTESIAN_POINT('Ctrl Pts',(-9.31450663810641,10.4230953029959,
12.2930489054275));
#113842=CARTESIAN_POINT('Ctrl Pts',(-9.32039914104527,10.4227371198028,
12.2961555830748));
#113843=CARTESIAN_POINT('Ctrl Pts',(-9.33594046880033,10.4217994311675,
12.3042142483516));
#113844=CARTESIAN_POINT('Ctrl Pts',(-9.34562358085017,10.4212222468204,
12.3090994526976));
#113845=CARTESIAN_POINT('Ctrl Pts',(-9.38719995650233,10.4187729317251,
12.329498462767));
#113846=CARTESIAN_POINT('Ctrl Pts',(-9.41959836327716,10.4169367678432,
12.3439584273586));
#113847=CARTESIAN_POINT('Ctrl Pts',(-9.56443809814606,10.4089912704893,
12.402387027644));
#113848=CARTESIAN_POINT('Ctrl Pts',(-9.68153353201755,10.4032927241331,
12.4335207006078));
#113849=CARTESIAN_POINT('Ctrl Pts',(-9.85424200343877,10.3946628512953,
12.4572102741142));
#113850=CARTESIAN_POINT('Ctrl Pts',(-9.90771828257885,10.3919527417577,
12.4615711186602));
#113851=CARTESIAN_POINT('Ctrl Pts',(-9.96905649915228,10.3886845667216,
12.4631933708788));
#113852=CARTESIAN_POINT('Ctrl Pts',(-9.976806955096,10.3882686893503,12.4633367412465));
#113853=CARTESIAN_POINT('Ctrl Pts',(-9.98863483075482,10.3876290780289,
12.4634615489339));
#113854=CARTESIAN_POINT('Ctrl Pts',(-9.99271175871203,10.387407715019,12.4634875308665));
#113855=CARTESIAN_POINT('Ctrl Pts',(-10.0001654646229,10.3870012808454,
12.4635038863192));
#113856=CARTESIAN_POINT('Ctrl Pts',(-10.0035421478281,10.3868165046222,
12.4634996089111));
#113857=CARTESIAN_POINT('Ctrl Pts',(-10.011119285522,10.386400408587,12.4634637870096));
#113858=CARTESIAN_POINT('Ctrl Pts',(-10.0153196039819,10.3861687469633,
12.4634258448017));
#113859=CARTESIAN_POINT('Ctrl Pts',(-10.02761034898,10.3854880534732,12.4632619005959));
#113860=CARTESIAN_POINT('Ctrl Pts',(-10.0356998323165,10.3850364637911,
12.4630868863626));
#113861=CARTESIAN_POINT('Ctrl Pts',(-10.1175056331756,10.3804363962512,
12.4606381974949));
#113862=CARTESIAN_POINT('Ctrl Pts',(-10.1909448198655,10.3760379929665,
12.4528625011414));
#113863=CARTESIAN_POINT('Ctrl Pts',(-10.3094856413223,10.3687950031995,
12.4311668677988));
#113864=CARTESIAN_POINT('Ctrl Pts',(-10.3550651548998,10.3659732394667,
12.420545262272));
#113865=CARTESIAN_POINT('Ctrl Pts',(-10.4544347575514,10.359806687048,12.3923063254228));
#113866=CARTESIAN_POINT('Ctrl Pts',(-10.5078740813945,10.3564815985431,
12.3737149439448));
#113867=CARTESIAN_POINT('Ctrl Pts',(-10.5907360588929,10.3513496616357,
12.3393887524389));
#113868=CARTESIAN_POINT('Ctrl Pts',(-10.6209258391924,10.3494845621877,
12.3256631064033));
#113869=CARTESIAN_POINT('Ctrl Pts',(-10.659781195264,10.347089435138,12.3063787764712));
#113870=CARTESIAN_POINT('Ctrl Pts',(-10.6688895339176,10.3465283414083,
12.3017386573591));
#113871=CARTESIAN_POINT('Ctrl Pts',(-10.6837312892492,10.3456144948202,
12.2939808146894));
#113872=CARTESIAN_POINT('Ctrl Pts',(-10.6894936865504,10.3452597974355,
12.2909195493149));
#113873=CARTESIAN_POINT('Ctrl Pts',(-10.700624712586,10.344574787597,12.2849104134184));
#113874=CARTESIAN_POINT('Ctrl Pts',(-10.7059956805918,10.3442443220705,
12.2819671832572));
#113875=CARTESIAN_POINT('Ctrl Pts',(-10.718396166965,10.3434814239076,12.2750702880158));
#113876=CARTESIAN_POINT('Ctrl Pts',(-10.7254118313522,10.343049869637,12.271092038578));
#113877=CARTESIAN_POINT('Ctrl Pts',(-10.7481869493952,10.3416488211784,
12.2579273730278));
#113878=CARTESIAN_POINT('Ctrl Pts',(-10.763807928455,10.3406877640882,12.2485040945486));
#113879=CARTESIAN_POINT('Ctrl Pts',(-10.8708379990983,10.3340933506595,
12.1811778933719));
#113880=CARTESIAN_POINT('Ctrl Pts',(-10.9557555153073,10.3288453255794,
12.1135860558942));
#113881=CARTESIAN_POINT('Ctrl Pts',(-11.0768961338526,10.3205246851005,
11.9930052524465));
#113882=CARTESIAN_POINT('Ctrl Pts',(-11.1184488281583,10.3174657284237,
11.9459576809373));
#113883=CARTESIAN_POINT('Ctrl Pts',(-11.1685322343153,10.3132955653407,
11.8813218668758));
#113884=CARTESIAN_POINT('Ctrl Pts',(-11.1799148916231,10.3123105324518,
11.8660234444216));
#113885=CARTESIAN_POINT('Ctrl Pts',(-11.1984509536745,10.3106347181775,
11.8400667626018));
#113886=CARTESIAN_POINT('Ctrl Pts',(-11.2057690825715,10.3099531468485,
11.8295286320316));
#113887=CARTESIAN_POINT('Ctrl Pts',(-11.2157406684736,10.3089942145375,
11.8147587348675));
#113888=CARTESIAN_POINT('Ctrl Pts',(-11.2185126380754,10.3087242845307,
11.8106072528732));
#113889=CARTESIAN_POINT('Ctrl Pts',(-11.2231812164023,10.3082637762265,
11.8035372278182));
#113890=CARTESIAN_POINT('Ctrl Pts',(-11.2250887802904,10.3080739135103,
11.8006259081846));
#113891=CARTESIAN_POINT('Ctrl Pts',(-11.2287347902593,10.3077076823169,
11.7950178360897));
#113892=CARTESIAN_POINT('Ctrl Pts',(-11.2304747764753,10.307531425358,11.792322136851));
#113893=CARTESIAN_POINT('Ctrl Pts',(-11.2346327304216,10.3071067022195,
11.7858336356913));
#113894=CARTESIAN_POINT('Ctrl Pts',(-11.2370420894708,10.3068576888654,
11.7820353891011));
#113895=CARTESIAN_POINT('Ctrl Pts',(-11.2457737834779,10.3059447443888,
11.7681289464596));
#113896=CARTESIAN_POINT('Ctrl Pts',(-11.2519898722347,10.305274460854,11.7579549718576));
#113897=CARTESIAN_POINT('Ctrl Pts',(-11.3009618699232,10.2998339891384,
11.6755553593478));
#113898=CARTESIAN_POINT('Ctrl Pts',(-11.3375533695938,10.2947725968978,
11.5998546784398));
#113899=CARTESIAN_POINT('Ctrl Pts',(-11.3953964881368,10.2850034904056,
11.4481645267125));
#113900=CARTESIAN_POINT('Ctrl Pts',(-11.4174063857041,10.2803105400422,
11.3727520379573));
#113901=CARTESIAN_POINT('Ctrl Pts',(-11.4386922612988,10.2742363175254,
11.2696600436006));
#113902=CARTESIAN_POINT('Ctrl Pts',(-11.4433937934071,10.2727078712792,
11.2432415382901));
#113903=CARTESIAN_POINT('Ctrl Pts',(-11.450236806506,10.2701126482664,11.1975377718739));
#113904=CARTESIAN_POINT('Ctrl Pts',(-11.4527259661506,10.269035697827,11.1783123212896));
#113905=CARTESIAN_POINT('Ctrl Pts',(-11.4557401997089,10.2675116182542,
11.150739771814));
#113906=CARTESIAN_POINT('Ctrl Pts',(-11.4565767683192,10.2670549005589,
11.1424293855986));
#113907=CARTESIAN_POINT('Ctrl Pts',(-11.4579055805771,10.2662658104847,
11.1279897257452));
#113908=CARTESIAN_POINT('Ctrl Pts',(-11.4584304183583,10.2659324363664,
11.121863727897));
#113909=CARTESIAN_POINT('Ctrl Pts',(-11.4593673763403,10.2652923167664,
11.1100527023862));
#113910=CARTESIAN_POINT('Ctrl Pts',(-11.4597849193632,10.264985409241,11.1043682273761));
#113911=CARTESIAN_POINT('Ctrl Pts',(-11.4607975261001,10.2641794680605,
11.0893848852245));
#113912=CARTESIAN_POINT('Ctrl Pts',(-11.4613370172568,10.2636821573072,
11.0800824409014));
#113913=CARTESIAN_POINT('Ctrl Pts',(-11.4629378830962,10.2619249084422,
11.0470182948696));
#113914=CARTESIAN_POINT('Ctrl Pts',(-11.4635088466797,10.260680035812,11.0232359460211));
#113915=CARTESIAN_POINT('Ctrl Pts',(-11.4634998963974,10.2594509413502,
10.9994493233677));
#113916=CARTESIAN_POINT('Ctrl Pts',(-11.4634998672784,10.1905769185562,
10.9993767215278));
#113917=CARTESIAN_POINT('Ctrl Pts',(-11.4635087402576,10.1917502954767,
11.0202110747467));
#113918=CARTESIAN_POINT('Ctrl Pts',(-11.4630727178984,10.1929103982478,
11.0410439404734));
#113919=CARTESIAN_POINT('Ctrl Pts',(-11.4618180918408,10.1945436224955,
11.0706991190408));
#113920=CARTESIAN_POINT('Ctrl Pts',(-11.4613640568745,10.1950278809764,
11.0795336226862));
#113921=CARTESIAN_POINT('Ctrl Pts',(-11.4604569612154,10.1958461096992,
11.094529757153));
#113922=CARTESIAN_POINT('Ctrl Pts',(-11.4600449380559,10.1961813381255,
11.1006935500792));
#113923=CARTESIAN_POINT('Ctrl Pts',(-11.4591321939684,10.1968572818914,
11.113161291302));
#113924=CARTESIAN_POINT('Ctrl Pts',(-11.4586296167857,10.1971979323305,
11.119464974271));
#113925=CARTESIAN_POINT('Ctrl Pts',(-11.4572898380598,10.1980346966816,
11.1349979815483));
#113926=CARTESIAN_POINT('Ctrl Pts',(-11.4564057957963,10.1985293522045,
11.14422305779));
#113927=CARTESIAN_POINT('Ctrl Pts',(-11.4527793613769,10.2003657298693,
11.1786212723831));
#113928=CARTESIAN_POINT('Ctrl Pts',(-11.4494713520886,10.2016899589236,
11.2037310262968));
#113929=CARTESIAN_POINT('Ctrl Pts',(-11.4395178835776,10.2049754559772,
11.2666306570856));
#113930=CARTESIAN_POINT('Ctrl Pts',(-11.4320349842601,10.2069121359247,
11.304269147967));
#113931=CARTESIAN_POINT('Ctrl Pts',(-11.4075888170012,10.2121232551803,
11.4061185327691));
#113932=CARTESIAN_POINT('Ctrl Pts',(-11.3877222970212,10.2153327069813,
11.4695376944518));
#113933=CARTESIAN_POINT('Ctrl Pts',(-11.3359554807644,10.2222813590908,
11.6023785995309));
#113934=CARTESIAN_POINT('Ctrl Pts',(-11.302793136757,10.2260187699642,11.6710920949111));
#113935=CARTESIAN_POINT('Ctrl Pts',(-11.2583919615321,10.230658257944,11.7472791459426));
#113936=CARTESIAN_POINT('Ctrl Pts',(-11.2522182138101,10.2312966806352,
11.7575790239711));
#113937=CARTESIAN_POINT('Ctrl Pts',(-11.2435525950672,10.2321854218951,
11.7716408051306));
#113938=CARTESIAN_POINT('Ctrl Pts',(-11.2411688673024,10.2324291557478,
11.7754691680555));
#113939=CARTESIAN_POINT('Ctrl Pts',(-11.2370570634862,10.2328484335978,
11.7820053644841));
#113940=CARTESIAN_POINT('Ctrl Pts',(-11.2353376823465,10.2330234194541,
11.7847186620506));
#113941=CARTESIAN_POINT('Ctrl Pts',(-11.2317373574746,10.2333891800879,
11.7903590564388));
#113942=CARTESIAN_POINT('Ctrl Pts',(-11.2298548992932,10.2335800592346,
11.7932851200699));
#113943=CARTESIAN_POINT('Ctrl Pts',(-11.225252012212,10.2340458618815,11.8003840141447));
#113944=CARTESIAN_POINT('Ctrl Pts',(-11.2225206881745,10.2343214895584,
11.8045497057596));
#113945=CARTESIAN_POINT('Ctrl Pts',(-11.2127196948706,10.2353075648476,
11.8193325925128));
#113946=CARTESIAN_POINT('Ctrl Pts',(-11.2055327481338,10.2360251970548,
11.8298709093419));
#113947=CARTESIAN_POINT('Ctrl Pts',(-11.1873464865875,10.2378251884096,
11.8558028320513));
#113948=CARTESIAN_POINT('Ctrl Pts',(-11.1761848564835,10.2389160387255,
11.8710793824369));
#113949=CARTESIAN_POINT('Ctrl Pts',(-11.1272841915869,10.2436231772408,
11.9353541618816));
#113950=CARTESIAN_POINT('Ctrl Pts',(-11.086757147,10.2473458123594,11.9821482813872));
#113951=CARTESIAN_POINT('Ctrl Pts',(-10.9666762283056,10.2576512976286,
12.1042368700797));
#113952=CARTESIAN_POINT('Ctrl Pts',(-10.8814413221291,10.2641719474604,
12.1734012675663));
#113953=CARTESIAN_POINT('Ctrl Pts',(-10.7739794202707,10.2713245145159,
12.2422231232295));
#113954=CARTESIAN_POINT('Ctrl Pts',(-10.7584959635955,10.2723327750234,
12.2517373309323));
#113955=CARTESIAN_POINT('Ctrl Pts',(-10.73589956152,10.2737729209937,12.2650489912396));
#113956=CARTESIAN_POINT('Ctrl Pts',(-10.7289265713706,10.2742131256107,
12.2690796555173));
#113957=CARTESIAN_POINT('Ctrl Pts',(-10.7165935438463,10.2749844330836,
12.2760734483298));
#113958=CARTESIAN_POINT('Ctrl Pts',(-10.7112475599466,10.2753163928242,
12.2790608518209));
#113959=CARTESIAN_POINT('Ctrl Pts',(-10.7001609224506,10.2759999829107,
12.2851652033948));
#113960=CARTESIAN_POINT('Ctrl Pts',(-10.6944178292519,10.2763514425556,
12.2882774536759));
#113961=CARTESIAN_POINT('Ctrl Pts',(-10.6796107600734,10.277250905233,12.2961737935304));
#113962=CARTESIAN_POINT('Ctrl Pts',(-10.6705169363113,10.2777969299543,
12.3009013542479));
#113963=CARTESIAN_POINT('Ctrl Pts',(-10.6315890813982,10.2801080752409,
12.3206219367596));
#113964=CARTESIAN_POINT('Ctrl Pts',(-10.6012952121128,10.2818413150216,
12.3346877368311));
#113965=CARTESIAN_POINT('Ctrl Pts',(-10.5179247329741,10.2864623492634,
12.3699822511231));
#113966=CARTESIAN_POINT('Ctrl Pts',(-10.4640425903194,10.2892887374912,
12.3891589193271));
#113967=CARTESIAN_POINT('Ctrl Pts',(-10.4020283082121,10.2924472338555,
12.4072174278449));
#113968=CARTESIAN_POINT('Ctrl Pts',(-10.3948662362419,10.2928106623411,
12.4092438773955));
#113969=CARTESIAN_POINT('Ctrl Pts',(-10.2925469536391,10.2979863632561,
12.437353019407));
#113970=CARTESIAN_POINT('Ctrl Pts',(-10.1950157221062,10.3027032357727,
12.453799253202));
#113971=CARTESIAN_POINT('Ctrl Pts',(-10.0788969638044,10.3087485491173,
12.4614792935148));
#113972=CARTESIAN_POINT('Ctrl Pts',(-10.061190717498,10.3096824403585,12.4623276299303));
#113973=CARTESIAN_POINT('Ctrl Pts',(-10.0376230241181,10.3109465687501,
12.4630280328475));
#113974=CARTESIAN_POINT('Ctrl Pts',(-10.0317709270593,10.311262192774,12.4631668130179));
#113975=CARTESIAN_POINT('Ctrl Pts',(-10.0222545753738,10.311778475196,12.4633353718921));
#113976=CARTESIAN_POINT('Ctrl Pts',(-10.0185907066386,10.3119779786252,
12.4633865045774));
#113977=CARTESIAN_POINT('Ctrl Pts',(-10.0114518446186,10.3123681900871,
12.4634593200052));
#113978=CARTESIAN_POINT('Ctrl Pts',(-10.0079769178361,10.3125588224461,
12.463482385946));
#113979=CARTESIAN_POINT('Ctrl Pts',(-9.99954340099898,10.3130231103691,
12.4635083291254));
#113980=CARTESIAN_POINT('Ctrl Pts',(-9.99458483299467,10.3132974594287,
12.4634983814178));
#113981=CARTESIAN_POINT('Ctrl Pts',(-9.9770178232458,10.3142740228842,12.4633738606046));
#113982=CARTESIAN_POINT('Ctrl Pts',(-9.96441126698918,10.314983244761,12.4631215454226));
#113983=CARTESIAN_POINT('Ctrl Pts',(-9.93319129921668,10.3167578755444,
12.4620929790299));
#113984=CARTESIAN_POINT('Ctrl Pts',(-9.9145867634661,10.3178314888808,12.4611241575624));
#113985=CARTESIAN_POINT('Ctrl Pts',(-9.83595563669678,10.3224235074177,
12.4555226258912));
#113986=CARTESIAN_POINT('Ctrl Pts',(-9.77622873261292,10.3260436527171,
12.4475435700484));
#113987=CARTESIAN_POINT('Ctrl Pts',(-9.60754611631345,10.3363898988575,
12.4143178542094));
#113988=CARTESIAN_POINT('Ctrl Pts',(-9.50074091015564,10.3430574924025,
12.3802402714164));
#113989=CARTESIAN_POINT('Ctrl Pts',(-9.38402417628157,10.3502312912186,
12.3276559137121));
#113990=CARTESIAN_POINT('Ctrl Pts',(-9.36931665886675,10.3511339744866,
12.3207327487295));
#113991=CARTESIAN_POINT('Ctrl Pts',(-9.34679748656298,10.3525144765691,
12.3096704847812));
#113992=CARTESIAN_POINT('Ctrl Pts',(-9.33890319326492,10.3529981139995,
12.3057033810059));
#113993=CARTESIAN_POINT('Ctrl Pts',(-9.32555274362245,10.35381560688,12.2988422855884));
#113994=CARTESIAN_POINT('Ctrl Pts',(-9.32007816719641,10.3541507151379,
12.295984832999));
#113995=CARTESIAN_POINT('Ctrl Pts',(-9.30903225092473,10.3548266738485,
12.2901301638649));
#113996=CARTESIAN_POINT('Ctrl Pts',(-9.30346192932136,10.3551674575417,
12.2871313016904));
#113997=CARTESIAN_POINT('Ctrl Pts',(-9.28976911730005,10.3560050211665,
12.2796446592993));
#113998=CARTESIAN_POINT('Ctrl Pts',(-9.28166947103459,10.3565003363637,
12.2751155309557));
#113999=CARTESIAN_POINT('Ctrl Pts',(-9.25155178745401,10.3583421595042,
12.2578963898265));
#114000=CARTESIAN_POINT('Ctrl Pts',(-9.22982174722013,10.3596710359274,
12.2447102531085));
#114001=CARTESIAN_POINT('Ctrl Pts',(-9.17602124379907,10.3629706246461,
12.2101145761539));
#114002=CARTESIAN_POINT('Ctrl Pts',(-9.14443239848515,10.3649164627707,
12.1879910044656));
#114003=CARTESIAN_POINT('Ctrl Pts',(-9.0610844848641,10.370126005813,12.1245666241999));
#114004=CARTESIAN_POINT('Ctrl Pts',(-9.01119467476569,10.3733258543988,
12.0809610257993));
#114005=CARTESIAN_POINT('Ctrl Pts',(-8.9106718461047,10.3802595405064,11.9802978259537));
#114006=CARTESIAN_POINT('Ctrl Pts',(-8.86120083578663,10.3839917521697,
11.9223630849978));
#114007=CARTESIAN_POINT('Ctrl Pts',(-8.80939790475063,10.3886252686737,
11.8511422430614));
#114008=CARTESIAN_POINT('Ctrl Pts',(-8.80245402167343,10.3892637267956,
11.8413442093914));
#114009=CARTESIAN_POINT('Ctrl Pts',(-8.79306947405171,10.3901525089944,
11.8277507445931));
#114010=CARTESIAN_POINT('Ctrl Pts',(-8.7905244279565,10.3903962475449,11.8240275657979));
#114011=CARTESIAN_POINT('Ctrl Pts',(-8.78619619663323,10.3908155313687,
11.8176324941483));
#114012=CARTESIAN_POINT('Ctrl Pts',(-8.78440450906698,10.3909905184656,
11.8149663616191));
#114013=CARTESIAN_POINT('Ctrl Pts',(-8.7806904779767,10.3913562792501,11.8094001762187));
#114014=CARTESIAN_POINT('Ctrl Pts',(-8.77876968961178,10.3915471572909,
11.8064991530652));
#114015=CARTESIAN_POINT('Ctrl Pts',(-8.77412416440732,10.3920129531775,
11.7994282320693));
#114016=CARTESIAN_POINT('Ctrl Pts',(-8.77141034735266,10.3922885751524,
11.7952512348007));
#114017=CARTESIAN_POINT('Ctrl Pts',(-8.76182355985369,10.3932746078615,
11.7803294443974));
#114018=CARTESIAN_POINT('Ctrl Pts',(-8.75506998902289,10.3939922023927,
11.7695090538862));
#114019=CARTESIAN_POINT('Ctrl Pts',(-8.7386531600432,10.3957920799232,11.7424245864894));
#114020=CARTESIAN_POINT('Ctrl Pts',(-8.72916236292778,10.3968828527923,
11.7260590596319));
#114021=CARTESIAN_POINT('Ctrl Pts',(-8.69001256888584,10.4015894693512,
11.6554304425494));
#114022=CARTESIAN_POINT('Ctrl Pts',(-8.66349268225899,10.4053116389298,
11.599502803005));
#114023=CARTESIAN_POINT('Ctrl Pts',(-8.60006938422499,10.4156163611572,
11.4404487695174));
#114024=CARTESIAN_POINT('Ctrl Pts',(-8.57106396768715,10.4221367599141,
11.3345893074705));
#114025=CARTESIAN_POINT('Ctrl Pts',(-8.55131577385237,10.4292897153516,
11.2085109377557));
#114026=CARTESIAN_POINT('Ctrl Pts',(-8.5488371839734,10.4302985478611,11.1904975623334));
#114027=CARTESIAN_POINT('Ctrl Pts',(-8.54574562402567,10.4317393544073,
11.1644425537456));
#114028=CARTESIAN_POINT('Ctrl Pts',(-8.54486249019697,10.4321796581879,
11.156435209291));
#114029=CARTESIAN_POINT('Ctrl Pts',(-8.54342441442566,10.4329510810623,
11.1423282112598));
#114030=CARTESIAN_POINT('Ctrl Pts',(-8.54284156857864,10.4332830578301,
11.1362316539053));
#114031=CARTESIAN_POINT('Ctrl Pts',(-8.54171625039937,10.4339666278286,
11.1236261047494));
#114032=CARTESIAN_POINT('Ctrl Pts',(-8.54117904739401,10.4343180507639,
11.1171167718596));
#114033=CARTESIAN_POINT('Ctrl Pts',(-8.53991112343057,10.4352173051551,
11.1003877194206));
#114034=CARTESIAN_POINT('Ctrl Pts',(-8.53924410535028,10.4357631601072,
11.0901634352357));
#114035=CARTESIAN_POINT('Ctrl Pts',(-8.53686253841685,10.4380725417661,
11.0466241103748));
#114036=CARTESIAN_POINT('Ctrl Pts',(-8.53617986339711,10.4398042500448,
11.0132614341371));
#114037=CARTESIAN_POINT('Ctrl Pts',(-8.53742159065321,10.4444198607817,
10.9228460019067));
#114038=CARTESIAN_POINT('Ctrl Pts',(-8.54154151089922,10.4472425495139,
10.8658813647854));
#114039=CARTESIAN_POINT('Ctrl Pts',(-8.55090612133398,10.4507570759175,
10.7946266489073));
#114040=CARTESIAN_POINT('Ctrl Pts',(-8.55305706585009,10.4514786364106,
10.7799831094522));
#114041=CARTESIAN_POINT('Ctrl Pts',(-8.57147646227741,10.457073659183,10.6665763026729));
#114042=CARTESIAN_POINT('Ctrl Pts',(-8.59761445844416,10.4618789871233,
10.569696980072));
#114043=CARTESIAN_POINT('Ctrl Pts',(-8.63743209187229,10.4677444811539,
10.4658031631833));
#114044=CARTESIAN_POINT('Ctrl Pts',(-8.64155792519702,10.4683404620168,
10.455396769011));
#114045=CARTESIAN_POINT('Ctrl Pts',(-8.64746820164726,10.4691796015083,
10.4409747076588));
#114046=CARTESIAN_POINT('Ctrl Pts',(-8.64915206613876,10.4694171062503,
10.4369179441515));
#114047=CARTESIAN_POINT('Ctrl Pts',(-8.65208698238771,10.4698284912014,
10.4299360841979));
#114048=CARTESIAN_POINT('Ctrl Pts',(-8.65332936700261,10.4700018595023,
10.4270073499827));
#114049=CARTESIAN_POINT('Ctrl Pts',(-8.65596156618187,10.470367597016,10.4208581855653));
#114050=CARTESIAN_POINT('Ctrl Pts',(-8.65735341860562,10.4705600925052,
10.4176386778777));
#114051=CARTESIAN_POINT('Ctrl Pts',(-8.66080752490595,10.4710355519655,
10.4097271539162));
#114052=CARTESIAN_POINT('Ctrl Pts',(-8.66288286874368,10.4713192883491,
10.4050409309285));
#114053=CARTESIAN_POINT('Ctrl Pts',(-8.67060270317975,10.472367432314,10.387853599491));
#114054=CARTESIAN_POINT('Ctrl Pts',(-8.67639807441659,10.4731402368784,
10.375421499448));
#114055=CARTESIAN_POINT('Ctrl Pts',(-8.71822423839432,10.4786128343341,
10.2888942466231));
#114056=CARTESIAN_POINT('Ctrl Pts',(-8.76027875785401,10.4835825371276,
10.2178812410391));
#114057=CARTESIAN_POINT('Ctrl Pts',(-8.86974678993304,10.4949344521506,
10.0642360190502));
#114058=CARTESIAN_POINT('Ctrl Pts',(-8.94066745975049,10.5012573896226,
9.98464396843344));
#114059=CARTESIAN_POINT('Ctrl Pts',(-9.03320343366227,10.5082450353975,
9.90114940024882));
#114060=CARTESIAN_POINT('Ctrl Pts',(-9.04704243294261,10.5092623069535,
9.88912639814773));
#114061=CARTESIAN_POINT('Ctrl Pts',(-9.06730356186042,10.5107128541953,
9.87218134444256));
#114062=CARTESIAN_POINT('Ctrl Pts',(-9.07354594457713,10.5111546165914,
9.86704790375476));
#114063=CARTESIAN_POINT('Ctrl Pts',(-9.08459627017407,10.5119277384135,
9.85811304372277));
#114064=CARTESIAN_POINT('Ctrl Pts',(-9.0893861276056,10.5122599671348,9.85428965856194));
#114065=CARTESIAN_POINT('Ctrl Pts',(-9.09932186413509,10.5129432493903,
9.84646037356761));
#114066=CARTESIAN_POINT('Ctrl Pts',(-9.10447079039932,10.5132941385571,
9.84245854898995));
#114067=CARTESIAN_POINT('Ctrl Pts',(-9.11774025550072,10.5141903622623,
9.83228685079056));
#114068=CARTESIAN_POINT('Ctrl Pts',(-9.12589892344178,10.5147337465359,
9.82616714538261));
#114069=CARTESIAN_POINT('Ctrl Pts',(-9.16066052573272,10.5170176290588,
9.80065635205338));
#114070=CARTESIAN_POINT('Ctrl Pts',(-9.18785073186588,10.518727202849,9.7820797579534));
#114071=CARTESIAN_POINT('Ctrl Pts',(-9.26286072789059,10.5232648462859,
9.73446234385364));
#114072=CARTESIAN_POINT('Ctrl Pts',(-9.31175694967316,10.5260344279026,
9.70721928502519));
#114073=CARTESIAN_POINT('Ctrl Pts',(-9.42756736872976,10.5323314608391,
9.6511318714039));
#114074=CARTESIAN_POINT('Ctrl Pts',(-9.49531067441672,10.5358258931188,
9.62435019068098));
#114075=CARTESIAN_POINT('Ctrl Pts',(-9.58394257400059,10.5404384128553,
9.5967423385813));
#114076=CARTESIAN_POINT('Ctrl Pts',(-9.60324376205152,10.541445604914,9.59116349853737));
#114077=CARTESIAN_POINT('Ctrl Pts',(-9.6520692012048,10.5440134904584,9.57813385293057));
#114078=CARTESIAN_POINT('Ctrl Pts',(-9.68172119537227,10.5455911574977,
9.57120416570205));
#114079=CARTESIAN_POINT('Ctrl Pts',(-9.71842248126392,10.547589436078,9.56382617077153));
#114080=CARTESIAN_POINT('Ctrl Pts',(-9.72528901580081,10.5479652438603,
9.56249694326973));
#114081=CARTESIAN_POINT('Ctrl Pts',(-9.73605562565912,10.5485579113282,
9.56049269492433));
#114082=CARTESIAN_POINT('Ctrl Pts',(-9.73994944954854,10.5487729497922,
9.55978417430872));
#114083=CARTESIAN_POINT('Ctrl Pts',(-9.74718033446681,10.5491736482781,
9.55849872164477));
#114084=CARTESIAN_POINT('Ctrl Pts',(-9.75051656309215,10.549359071667,9.55791757074044));
#114085=CARTESIAN_POINT('Ctrl Pts',(-9.75814559843241,10.5497843195902,
9.55661590504471));
#114086=CARTESIAN_POINT('Ctrl Pts',(-9.76243960950503,10.5500245567199,
9.55590296136369));
#114087=CARTESIAN_POINT('Ctrl Pts',(-9.77573787928642,10.5507711583569,
9.55375593873383));
#114088=CARTESIAN_POINT('Ctrl Pts',(-9.78475223407125,10.5512809367453,
9.55238686996278));
#114089=CARTESIAN_POINT('Ctrl Pts',(-9.80585124718539,10.5524817984529,
9.54938385014964));
#114090=CARTESIAN_POINT('Ctrl Pts',(-9.81794458374595,10.5531759606489,
9.54781655433849));
#114091=CARTESIAN_POINT('Ctrl Pts',(-9.86064193252219,10.5556441655955,
9.54282469042827));
#114092=CARTESIAN_POINT('Ctrl Pts',(-9.89133182094211,10.5574494886226,
9.54021522945709));
#114093=CARTESIAN_POINT('Ctrl Pts',(-10.0298816845532,10.565677567142,9.53282798844815));
#114094=CARTESIAN_POINT('Ctrl Pts',(-10.1380019555013,10.5722797398151,
9.53902589850794));
#114095=CARTESIAN_POINT('Ctrl Pts',(-10.2974345101372,10.5817390468098,
9.56603615990242));
#114096=CARTESIAN_POINT('Ctrl Pts',(-10.3498829700813,10.5848107273916,
9.57792317168964));
#114097=CARTESIAN_POINT('Ctrl Pts',(-10.4133282668786,10.5884707795145,
9.59602647142961));
#114098=CARTESIAN_POINT('Ctrl Pts',(-10.4250505772105,10.5891447511397,
9.59953081267335));
#114099=CARTESIAN_POINT('Ctrl Pts',(-10.443445483883,10.5901990097299,9.60528214637818));
#114100=CARTESIAN_POINT('Ctrl Pts',(-10.450147985461,10.5905824414117,9.60743094175544));
#114101=CARTESIAN_POINT('Ctrl Pts',(-10.4625053676953,10.5912881396837,
9.61149120941357));
#114102=CARTESIAN_POINT('Ctrl Pts',(-10.4681645331558,10.5916108390277,
9.61338907835271));
#114103=CARTESIAN_POINT('Ctrl Pts',(-10.4807084634067,10.592325117948,9.61768138496508));
#114104=CARTESIAN_POINT('Ctrl Pts',(-10.4875872948824,10.5927161363647,
9.62009275212421));
#114105=CARTESIAN_POINT('Ctrl Pts',(-10.5073945686856,10.5938402718558,
9.62720277703443));
#114106=CARTESIAN_POINT('Ctrl Pts',(-10.5202753378402,10.5945690895984,
9.63203251008392));
#114107=CARTESIAN_POINT('Ctrl Pts',(-10.5491868593215,10.596201072058,9.64334052751265));
#114108=CARTESIAN_POINT('Ctrl Pts',(-10.5651748641215,10.5971008121415,
9.64992276708801));
#114109=CARTESIAN_POINT('Ctrl Pts',(-10.6169903147784,10.6000118822921,
9.67233693302531));
#114110=CARTESIAN_POINT('Ctrl Pts',(-10.6523004538226,10.6019874194546,
9.68932434755603));
#114111=CARTESIAN_POINT('Ctrl Pts',(-10.7767544931489,10.6089925087812,
9.75547507805603));
#114112=CARTESIAN_POINT('Ctrl Pts',(-10.8613880590976,10.613818545891,9.8124820050933));
#114113=CARTESIAN_POINT('Ctrl Pts',(-10.948413448068,10.6194743121055,9.88533335293958));
#114114=CARTESIAN_POINT('Ctrl Pts',(-10.957315593808,10.6200620881367,9.89296944599265));
#114115=CARTESIAN_POINT('Ctrl Pts',(-10.9925372238763,10.6224290755521,
9.92392446333581));
#114116=CARTESIAN_POINT('Ctrl Pts',(-11.0181025219248,10.6242411757766,
9.94808004553598));
#114117=CARTESIAN_POINT('Ctrl Pts',(-11.0474368771963,10.6264706148856,
9.97786867090394));
#114118=CARTESIAN_POINT('Ctrl Pts',(-11.0520700761582,10.6268274276144,
9.98263820732939));
#114119=CARTESIAN_POINT('Ctrl Pts',(-11.0595970869691,10.6274151464101,
9.99049311281253));
#114120=CARTESIAN_POINT('Ctrl Pts',(-11.0625103580291,10.6276446230026,
9.99355979801825));
#114121=CARTESIAN_POINT('Ctrl Pts',(-11.0677266801538,10.6280592247461,
9.99909870501392));
#114122=CARTESIAN_POINT('Ctrl Pts',(-11.0700345072656,10.6282439836777,
10.0015663173252));
#114123=CARTESIAN_POINT('Ctrl Pts',(-11.0750923831634,10.6286518538625,
10.007012059954));
#114124=CARTESIAN_POINT('Ctrl Pts',(-11.0778385787115,10.6288752364172,
10.0099935965649));
#114125=CARTESIAN_POINT('Ctrl Pts',(-11.0857227775879,10.6295220387791,
10.0186251368294));
#114126=CARTESIAN_POINT('Ctrl Pts',(-11.0908289105967,10.6299477116908,
10.0243039128229));
#114127=CARTESIAN_POINT('Ctrl Pts',(-11.1286789884811,10.6331524387183,
10.0670672978851));
#114128=CARTESIAN_POINT('Ctrl Pts',(-11.1595653745561,10.6360461089173,
10.1057478429604));
#114129=CARTESIAN_POINT('Ctrl Pts',(-11.2312174537644,10.6433477311361,
10.205449198514));
#114130=CARTESIAN_POINT('Ctrl Pts',(-11.2694694780741,10.647798701241,10.268115548723));
#114131=CARTESIAN_POINT('Ctrl Pts',(-11.3404236409246,10.6570914808106,
10.4067918290544));
#114132=CARTESIAN_POINT('Ctrl Pts',(-11.3717157056356,10.661892724109,10.4832496120246));
#114133=CARTESIAN_POINT('Ctrl Pts',(-11.4000168564154,10.6671485043266,
10.5734665098075));
#114134=CARTESIAN_POINT('Ctrl Pts',(-11.403488030209,10.6678150472914,10.5850308712938));
#114135=CARTESIAN_POINT('Ctrl Pts',(-11.408922509258,10.6688960676021,10.6039847986157));
#114136=CARTESIAN_POINT('Ctrl Pts',(-11.4109716716786,10.6693132805952,
10.6113489719169));
#114137=CARTESIAN_POINT('Ctrl Pts',(-11.41453930508,10.6700574193959,10.6245703649181));
#114138=CARTESIAN_POINT('Ctrl Pts',(-11.4160793145276,10.6703850273874,
10.6304215468959));
#114139=CARTESIAN_POINT('Ctrl Pts',(-11.4192730698448,10.6710783970174,
10.642869144821));
#114140=CARTESIAN_POINT('Ctrl Pts',(-11.4209172168043,10.6714438463253,
10.6494678907394));
#114141=CARTESIAN_POINT('Ctrl Pts',(-11.424173231385,10.6721854758231,10.662935275096));
#114142=CARTESIAN_POINT('Ctrl Pts',(-11.4257815460902,10.6725615359051,
10.669804592818));
#114143=CARTESIAN_POINT('Ctrl Pts',(-11.4296786106541,10.6734979943037,
10.6870089995984));
#114144=CARTESIAN_POINT('Ctrl Pts',(-11.4319050426638,10.67405644641,10.6973578805117));
#114145=CARTESIAN_POINT('Ctrl Pts',(-11.4537097882804,10.6797822166669,
10.8043426556033));
#114146=CARTESIAN_POINT('Ctrl Pts',(-11.4635870590518,10.6846245035735,
10.9026959679584));
#114147=CARTESIAN_POINT('Ctrl Pts',(-11.4634994219804,10.6894249952545,
11.0013007162982));
#114148=CARTESIAN_POINT('Origin',(-10.,3.5,11.));
#114149=CARTESIAN_POINT('',(-11.4634998199575,11.2617878196045,10.9992740621286));
#114150=CARTESIAN_POINT('',(-11.4634998222683,11.1893449541571,10.999278736866));
#114151=CARTESIAN_POINT('',(-11.4635,3.5,11.));
#114152=CARTESIAN_POINT('',(-11.4634993682568,10.7605065214977,11.001312182958));
#114153=CARTESIAN_POINT('Ctrl Pts',(-11.463499819958,11.2617878197064,10.9992740641209));
#114154=CARTESIAN_POINT('Ctrl Pts',(-11.463486688228,11.2604341920573,10.9728002597134));
#114155=CARTESIAN_POINT('Ctrl Pts',(-11.4627552163876,11.2590556290495,
10.946333239001));
#114156=CARTESIAN_POINT('Ctrl Pts',(-11.4609407851069,11.257284080159,10.9132306704544));
#114157=CARTESIAN_POINT('Ctrl Pts',(-11.4605294202421,11.2569247662569,
10.9065617671658));
#114158=CARTESIAN_POINT('Ctrl Pts',(-11.4598066339438,11.2563526182091,
10.8960195233276));
#114159=CARTESIAN_POINT('Ctrl Pts',(-11.4595254219672,11.2561414065003,
10.8921441241544));
#114160=CARTESIAN_POINT('Ctrl Pts',(-11.458995493785,11.2557625509528,10.8852231000926));
#114161=CARTESIAN_POINT('Ctrl Pts',(-11.458752668362,11.2555952341647,10.8821770835459));
#114162=CARTESIAN_POINT('Ctrl Pts',(-11.4581475455987,11.255192765732,10.8748751451752));
#114163=CARTESIAN_POINT('Ctrl Pts',(-11.4577761565212,11.2549571182771,
10.8706200534682));
#114164=CARTESIAN_POINT('Ctrl Pts',(-11.4565913163249,11.2542382503158,
10.8576983509844));
#114165=CARTESIAN_POINT('Ctrl Pts',(-11.4557191796975,11.2537519611746,
10.8490374731997));
#114166=CARTESIAN_POINT('Ctrl Pts',(-11.4535165464869,11.2526152206947,
10.828962125839));
#114167=CARTESIAN_POINT('Ctrl Pts',(-11.4521287737384,11.2519621027094,
10.8175546258698));
#114168=CARTESIAN_POINT('Ctrl Pts',(-11.435861274341,11.2449234509118,10.6958132230162));
#114169=CARTESIAN_POINT('Ctrl Pts',(-11.4085727377921,11.2380905037844,
10.5875083579516));
#114170=CARTESIAN_POINT('Ctrl Pts',(-11.3407520148659,11.2266394173485,
10.4077650713213));
#114171=CARTESIAN_POINT('Ctrl Pts',(-11.3060214706851,11.2219404602744,
10.3346659737906));
#114172=CARTESIAN_POINT('Ctrl Pts',(-11.2593717792556,11.2167788150277,
10.2543725024596));
#114173=CARTESIAN_POINT('Ctrl Pts',(-11.2531856402008,11.2161131419785,
10.2440215566316));
#114174=CARTESIAN_POINT('Ctrl Pts',(-11.2428730993153,11.2150333031189,
10.2272406276176));
#114175=CARTESIAN_POINT('Ctrl Pts',(-11.2388231157101,11.2146164105612,
10.220764554406));
#114176=CARTESIAN_POINT('Ctrl Pts',(-11.2314755565732,11.2138727050138,
10.2092176120861));
#114177=CARTESIAN_POINT('Ctrl Pts',(-11.2281969143172,11.2135452118272,
10.2041349532428));
#114178=CARTESIAN_POINT('Ctrl Pts',(-11.2211650595449,11.212851943327,10.1933808855717));
#114179=CARTESIAN_POINT('Ctrl Pts',(-11.2174036261162,11.2124864812542,
10.1877150058878));
#114180=CARTESIAN_POINT('Ctrl Pts',(-11.2071862182944,11.2115079268949,
10.1725548359386));
#114181=CARTESIAN_POINT('Ctrl Pts',(-11.2006577174758,11.2108975438894,
10.163109851544));
#114182=CARTESIAN_POINT('Ctrl Pts',(-11.166537641028,11.2077811865274,10.1149684690307));
#114183=CARTESIAN_POINT('Ctrl Pts',(-11.1371828998453,11.2053429818794,
10.0775540605704));
#114184=CARTESIAN_POINT('Ctrl Pts',(-11.0355975914252,11.1975496823898,
9.96031396779354));
#114185=CARTESIAN_POINT('Ctrl Pts',(-10.9563891946588,11.192449698844,9.88701832105989));
#114186=CARTESIAN_POINT('Ctrl Pts',(-10.8478650472762,11.1857680377002,
9.80680872110096));
#114187=CARTESIAN_POINT('Ctrl Pts',(-10.8254154028199,11.1843985897977,
9.79117004353052));
#114188=CARTESIAN_POINT('Ctrl Pts',(-10.7794629744942,11.1815939499171,
9.76103616325597));
#114189=CARTESIAN_POINT('Ctrl Pts',(-10.7559622234764,11.1801588411624,
9.74655879875568));
#114190=CARTESIAN_POINT('Ctrl Pts',(-10.7262018665948,11.1783228534056,
9.72936669680408));
#114191=CARTESIAN_POINT('Ctrl Pts',(-10.7203125849238,11.1779586412921,
9.72601887034836));
#114192=CARTESIAN_POINT('Ctrl Pts',(-10.7109905627091,11.177380407447,9.72080496644957));
#114193=CARTESIAN_POINT('Ctrl Pts',(-10.7075731557772,11.1771680662359,
9.71891150086287));
#114194=CARTESIAN_POINT('Ctrl Pts',(-10.7014723129851,11.1767882703901,
9.71556309546341));
#114195=CARTESIAN_POINT('Ctrl Pts',(-10.6987918618229,11.1766211533441,
9.71410284200062));
#114196=CARTESIAN_POINT('Ctrl Pts',(-10.6923764086864,11.1762205830398,
9.7106338208467));
#114197=CARTESIAN_POINT('Ctrl Pts',(-10.6886372509974,11.1759866475075,
9.70863290623313));
#114198=CARTESIAN_POINT('Ctrl Pts',(-10.6773317683744,11.1752780470676,
9.70264613070868));
#114199=CARTESIAN_POINT('Ctrl Pts',(-10.6697392854091,11.174800437032,9.69871038231332));
#114200=CARTESIAN_POINT('Ctrl Pts',(-10.5893245488687,11.1697271998879,
9.65791561526222));
#114201=CARTESIAN_POINT('Ctrl Pts',(-10.5135813304267,11.1648299550675,
9.62714689682599));
#114202=CARTESIAN_POINT('Ctrl Pts',(-10.3256076031161,11.1529822048455,
9.56853033538366));
#114203=CARTESIAN_POINT('Ctrl Pts',(-10.2118479877965,11.1460881788344,
9.54732842820739));
#114204=CARTESIAN_POINT('Ctrl Pts',(-10.079020286721,11.138631551582,9.53852665513824));
#114205=CARTESIAN_POINT('Ctrl Pts',(-10.0612540913168,11.1376451475261,
9.53767427748808));
#114206=CARTESIAN_POINT('Ctrl Pts',(-10.0354956237449,11.1362303488594,
9.53690873264133));
#114207=CARTESIAN_POINT('Ctrl Pts',(-10.0275131285929,11.1357940343046,
9.53673685647315));
#114208=CARTESIAN_POINT('Ctrl Pts',(-10.0134188038962,11.1350273166918,
9.53654875956377));
#114209=CARTESIAN_POINT('Ctrl Pts',(-10.0073075799973,11.1346960871203,
9.5365054840304));
#114210=CARTESIAN_POINT('Ctrl Pts',(-9.99463846173659,11.1340118762913,
9.53649512885722));
#114211=CARTESIAN_POINT('Ctrl Pts',(-9.9880806911095,11.1336590812989,9.53653384530509));
#114212=CARTESIAN_POINT('Ctrl Pts',(-9.97115167042587,11.1327517492285,
9.53674759104382));
#114213=CARTESIAN_POINT('Ctrl Pts',(-9.96078152694503,11.1321992602464,
9.53698880483284));
#114214=CARTESIAN_POINT('Ctrl Pts',(-9.91584923270393,11.1298189020828,
9.53851204623405));
#114215=CARTESIAN_POINT('Ctrl Pts',(-9.88133471590067,11.1280254194898,
9.54090878174838));
#114216=CARTESIAN_POINT('Ctrl Pts',(-9.7869369309863,11.1231877165366,9.55083609028697));
#114217=CARTESIAN_POINT('Ctrl Pts',(-9.72738316798507,11.1202129159283,
9.56085002104142));
#114218=CARTESIAN_POINT('Ctrl Pts',(-9.57780438989927,11.1127159867484,
9.59562279055109));
#114219=CARTESIAN_POINT('Ctrl Pts',(-9.48922683467326,11.1082579249049,
9.62536100537308));
#114220=CARTESIAN_POINT('Ctrl Pts',(-9.381671753301,11.1022174118941,9.67331059672294));
#114221=CARTESIAN_POINT('Ctrl Pts',(-9.35951195405144,11.1009362820014,
9.68386569087924));
#114222=CARTESIAN_POINT('Ctrl Pts',(-9.33175289958555,11.0992718114994,
9.69795488141136));
#114223=CARTESIAN_POINT('Ctrl Pts',(-9.32589681106973,11.0989172385231,
9.70097707277241));
#114224=CARTESIAN_POINT('Ctrl Pts',(-9.31667281868704,11.0983529907968,
9.70581652888809));
#114225=CARTESIAN_POINT('Ctrl Pts',(-9.31329121891552,11.0981449001671,
9.70760766679776));
#114226=CARTESIAN_POINT('Ctrl Pts',(-9.30691021542978,11.0977498304209,
9.71101961847261));
#114227=CARTESIAN_POINT('Ctrl Pts',(-9.30390941756315,11.0975630210812,
9.71263766808647));
#114228=CARTESIAN_POINT('Ctrl Pts',(-9.29690441403648,11.0971245766201,
9.71644646388222));
#114229=CARTESIAN_POINT('Ctrl Pts',(-9.292904776117,11.0968724308582,9.7186454720495));
#114230=CARTESIAN_POINT('Ctrl Pts',(-9.27995131019711,11.096050096812,9.7258464279553));
#114231=CARTESIAN_POINT('Ctrl Pts',(-9.27103995960337,11.0954754543274,
9.73092368695006));
#114232=CARTESIAN_POINT('Ctrl Pts',(-9.22356472910915,11.0923690084629,
9.75863780076442));
#114233=CARTESIAN_POINT('Ctrl Pts',(-9.18600300180205,11.089751104733,9.78293793436466));
#114234=CARTESIAN_POINT('Ctrl Pts',(-9.06307401566891,11.0807723093504,
9.87070415891188));
#114235=CARTESIAN_POINT('Ctrl Pts',(-8.98351406272645,11.0742780520504,
9.94174716314356));
#114236=CARTESIAN_POINT('Ctrl Pts',(-8.90500709897132,11.0674243361306,
10.0289472606158));
#114237=CARTESIAN_POINT('Ctrl Pts',(-8.89775048206228,11.0667856677941,
10.037192187484));
#114238=CARTESIAN_POINT('Ctrl Pts',(-8.86291326084977,11.0636947874948,
10.0776841649977));
#114239=CARTESIAN_POINT('Ctrl Pts',(-8.83664955989742,11.0612883614971,
10.1110404866213));
#114240=CARTESIAN_POINT('Ctrl Pts',(-8.80512367001447,11.0582981947217,
10.1548749576329));
#114241=CARTESIAN_POINT('Ctrl Pts',(-8.79848783667515,11.0576624613002,
10.1643360045507));
#114242=CARTESIAN_POINT('Ctrl Pts',(-8.78811656242673,11.0566584047046,
10.179501825627));
#114243=CARTESIAN_POINT('Ctrl Pts',(-8.7843078245752,11.0562873465705,10.1851556852933));
#114244=CARTESIAN_POINT('Ctrl Pts',(-8.77753033831777,11.0556227662621,
10.1953697858876));
#114245=CARTESIAN_POINT('Ctrl Pts',(-8.77454727205529,11.0553287166808,
10.199920336548));
#114246=CARTESIAN_POINT('Ctrl Pts',(-8.76760944743998,11.0546411425273,
10.2106335501222));
#114247=CARTESIAN_POINT('Ctrl Pts',(-8.76367540416524,11.0542483837425,
10.2168094978812));
#114248=CARTESIAN_POINT('Ctrl Pts',(-8.75239663559079,11.0531137380059,
10.2348124995559));
#114249=CARTESIAN_POINT('Ctrl Pts',(-8.74517400192465,11.0523762798636,
10.2467153275152));
#114250=CARTESIAN_POINT('Ctrl Pts',(-8.68669847874528,11.0463091978923,
10.3462579244345));
#114251=CARTESIAN_POINT('Ctrl Pts',(-8.644521627876,11.0413258428021,10.438910970078));
#114252=CARTESIAN_POINT('Ctrl Pts',(-8.58149710500079,11.0316662114003,
10.6270770134347));
#114253=CARTESIAN_POINT('Ctrl Pts',(-8.5599268650995,11.0270009487026,10.7217791812591));
#114254=CARTESIAN_POINT('Ctrl Pts',(-8.54645992899512,11.0212975155907,
10.829171233828));
#114255=CARTESIAN_POINT('Ctrl Pts',(-8.54517820889322,11.0206931183749,
10.8404545646537));
#114256=CARTESIAN_POINT('Ctrl Pts',(-8.54358036214461,11.0198439921769,
10.8561472523417));
#114257=CARTESIAN_POINT('Ctrl Pts',(-8.54315268042422,11.0196050946766,
10.860545129269));
#114258=CARTESIAN_POINT('Ctrl Pts',(-8.54245076777175,11.0191919822457,
10.8681188170028));
#114259=CARTESIAN_POINT('Ctrl Pts',(-8.54216698201834,11.0190182896834,
10.8712937372095));
#114260=CARTESIAN_POINT('Ctrl Pts',(-8.54159341537822,11.0186526860205,
10.8779560335453));
#114261=CARTESIAN_POINT('Ctrl Pts',(-8.54130576819757,11.0184606539934,
10.8814435445598));
#114262=CARTESIAN_POINT('Ctrl Pts',(-8.54063058711665,11.0179877360115,
10.8900042957124));
#114263=CARTESIAN_POINT('Ctrl Pts',(-8.54025699883146,11.0177060951066,
10.8950785665774));
#114264=CARTESIAN_POINT('Ctrl Pts',(-8.53899101008997,11.016673968829,10.9135917653415));
#114265=CARTESIAN_POINT('Ctrl Pts',(-8.53825770550112,11.0159154072524,
10.9270404920041));
#114266=CARTESIAN_POINT('Ctrl Pts',(-8.53688261837224,11.0139905204385,
10.9608332978521));
#114267=CARTESIAN_POINT('Ctrl Pts',(-8.53647945555567,11.0128142154581,
10.981183866438));
#114268=CARTESIAN_POINT('Ctrl Pts',(-8.53664439499977,11.0036263761541,
11.1384106828293));
#114269=CARTESIAN_POINT('Ctrl Pts',(-8.55598728674533,10.9951654956004,
11.2745952142894));
#114270=CARTESIAN_POINT('Ctrl Pts',(-8.60585611403407,10.984762845462,11.447243828349));
#114271=CARTESIAN_POINT('Ctrl Pts',(-8.6195324964374,10.9823348338308,11.4878260064324));
#114272=CARTESIAN_POINT('Ctrl Pts',(-8.63914739316766,10.9793223389284,
11.538559808752));
#114273=CARTESIAN_POINT('Ctrl Pts',(-8.64345368037679,10.9786849015235,
11.5493164649263));
#114274=CARTESIAN_POINT('Ctrl Pts',(-8.65049843866856,10.9776787880916,
11.5663253015064));
#114275=CARTESIAN_POINT('Ctrl Pts',(-8.65315362717664,10.9773073578466,
11.5726112654904));
#114276=CARTESIAN_POINT('Ctrl Pts',(-8.65800453759039,10.9766424503777,
11.5838750073932));
#114277=CARTESIAN_POINT('Ctrl Pts',(-8.66018422395008,10.9763484425683,
11.588859518675));
#114278=CARTESIAN_POINT('Ctrl Pts',(-8.66535903324808,10.9756613984166,
11.6005157956232));
#114279=CARTESIAN_POINT('Ctrl Pts',(-8.66837648625373,10.9752691238937,
11.6071775285671));
#114280=CARTESIAN_POINT('Ctrl Pts',(-8.67726408030995,10.9741373172945,
11.6264140094053));
#114281=CARTESIAN_POINT('Ctrl Pts',(-8.68326338402909,10.9734021792358,
11.638928420044));
#114282=CARTESIAN_POINT('Ctrl Pts',(-8.73771368267025,10.9669722345414,
11.748485097245));
#114283=CARTESIAN_POINT('Ctrl Pts',(-8.7966351241764,10.9616788967025,11.839948049353));
#114284=CARTESIAN_POINT('Ctrl Pts',(-8.92164338210987,10.9520450975817,
11.9934738906188));
#114285=CARTESIAN_POINT('Ctrl Pts',(-8.98439921637841,10.947707690103,12.0575418234643));
#114286=CARTESIAN_POINT('Ctrl Pts',(-9.06155335046782,10.9423785132384,
12.1230707989617));
#114287=CARTESIAN_POINT('Ctrl Pts',(-9.07059419437932,10.9417539596014,
12.1305640029925));
#114288=CARTESIAN_POINT('Ctrl Pts',(-9.08320336986207,10.9408812575007,
12.1407612428869));
#114289=CARTESIAN_POINT('Ctrl Pts',(-9.08669564218362,10.9406393802955,
12.1435591035216));
#114290=CARTESIAN_POINT('Ctrl Pts',(-9.0927090094764,10.9402224924739,12.1483316435585));
#114291=CARTESIAN_POINT('Ctrl Pts',(-9.09522387665814,10.9400480263199,
12.1503141620051));
#114292=CARTESIAN_POINT('Ctrl Pts',(-9.10048980960202,10.9396824145588,
12.1544374468385));
#114293=CARTESIAN_POINT('Ctrl Pts',(-9.10324203174723,10.9394911585174,
12.1565766497872));
#114294=CARTESIAN_POINT('Ctrl Pts',(-9.10997556710577,10.9390228725697,
12.1617719007692));
#114295=CARTESIAN_POINT('Ctrl Pts',(-9.11396499369372,10.9387451204313,
12.1648173275915));
#114296=CARTESIAN_POINT('Ctrl Pts',(-9.12834970683843,10.9377427734411,
12.1756815951264));
#114297=CARTESIAN_POINT('Ctrl Pts',(-9.13883316314712,10.9370106842262,
12.1833820608782));
#114298=CARTESIAN_POINT('Ctrl Pts',(-9.16522244570663,10.9351667905506,
12.2022295545922));
#114299=CARTESIAN_POINT('Ctrl Pts',(-9.18124989695634,10.934045984839,12.2132014144969));
#114300=CARTESIAN_POINT('Ctrl Pts',(-9.2516714441834,10.9291332178608,12.2593786031975));
#114301=CARTESIAN_POINT('Ctrl Pts',(-9.30814976191267,10.9252265134849,
12.2912678320341));
#114302=CARTESIAN_POINT('Ctrl Pts',(-9.46142865058808,10.9149957445417,
12.3648625864945));
#114303=CARTESIAN_POINT('Ctrl Pts',(-9.56095668223373,10.9087372911465,
12.4000558950807));
#114304=CARTESIAN_POINT('Ctrl Pts',(-9.67955646900472,10.9019039766204,
12.4280838216257));
#114305=CARTESIAN_POINT('Ctrl Pts',(-9.69576530343403,10.9009822691528,
12.4316245105298));
#114306=CARTESIAN_POINT('Ctrl Pts',(-9.72077986417247,10.8995781108575,
12.4366446970227));
#114307=CARTESIAN_POINT('Ctrl Pts',(-9.72954441626644,10.8990895471695,
12.4383204274033));
#114308=CARTESIAN_POINT('Ctrl Pts',(-9.74386139923743,10.8982969299803,
12.4409222546615));
#114309=CARTESIAN_POINT('Ctrl Pts',(-9.74940472577557,10.8979913686292,
12.4418966455825));
#114310=CARTESIAN_POINT('Ctrl Pts',(-9.76107425792123,10.897350860781,12.4438785554664));
#114311=CARTESIAN_POINT('Ctrl Pts',(-9.76720154189295,10.8970161377078,
12.4448791204439));
#114312=CARTESIAN_POINT('Ctrl Pts',(-9.7819178952353,10.8962159280863,12.447186208087));
#114313=CARTESIAN_POINT('Ctrl Pts',(-9.79051264885204,10.8957516170809,
12.448455308037));
#114314=CARTESIAN_POINT('Ctrl Pts',(-9.82033863693388,10.8941504550591,
12.4525883771122));
#114315=CARTESIAN_POINT('Ctrl Pts',(-9.84162161506871,10.8930256838134,
12.4550627297469));
#114316=CARTESIAN_POINT('Ctrl Pts',(-9.98122805657438,10.8857496251962,
12.4681937372834));
#114317=CARTESIAN_POINT('Ctrl Pts',(-10.1004149022225,10.8800618910277,
12.4648766738575));
#114318=CARTESIAN_POINT('Ctrl Pts',(-10.2905829711886,10.8706621499727,
12.4362440704026));
#114319=CARTESIAN_POINT('Ctrl Pts',(-10.3623346248171,10.8670237781975,
12.4198403453594));
#114320=CARTESIAN_POINT('Ctrl Pts',(-10.4402736824534,10.8626843353073,
12.3957280706299));
#114321=CARTESIAN_POINT('Ctrl Pts',(-10.4479859292538,10.8622505778353,
12.3932718198192));
#114322=CARTESIAN_POINT('Ctrl Pts',(-10.4596694780708,10.8615862739666,
12.3894437268116));
#114323=CARTESIAN_POINT('Ctrl Pts',(-10.4636560249375,10.8613583279926,
12.3881185067185));
#114324=CARTESIAN_POINT('Ctrl Pts',(-10.4708365224507,10.8609453545981,
12.3856971609403));
#114325=CARTESIAN_POINT('Ctrl Pts',(-10.4740324410999,10.8607606803902,
12.3846071273428));
#114326=CARTESIAN_POINT('Ctrl Pts',(-10.4810783263755,10.8603516107149,
12.3821767297007));
#114327=CARTESIAN_POINT('Ctrl Pts',(-10.4849264332692,10.860126932439,12.3808313516597));
#114328=CARTESIAN_POINT('Ctrl Pts',(-10.4960733290925,10.8594725318554,
12.3768818236513));
#114329=CARTESIAN_POINT('Ctrl Pts',(-10.5033570048102,10.8590404755058,
12.3742357965485));
#114330=CARTESIAN_POINT('Ctrl Pts',(-10.5524208213832,10.8561015739289,
12.3559694179628));
#114331=CARTESIAN_POINT('Ctrl Pts',(-10.5934856823278,10.8535021285129,
12.3385050893608));
#114332=CARTESIAN_POINT('Ctrl Pts',(-10.7403409264512,10.8438446787764,
12.2679620747211));
#114333=CARTESIAN_POINT('Ctrl Pts',(-10.8404063684241,10.8365963249241,
12.2039746619075));
#114334=CARTESIAN_POINT('Ctrl Pts',(-10.9664515190271,10.8271130626593,
12.0999261247623));
#114335=CARTESIAN_POINT('Ctrl Pts',(-10.9998867756579,10.824550616811,12.069622861117));
#114336=CARTESIAN_POINT('Ctrl Pts',(-11.0401159386909,10.8214075610566,
12.0296243202608));
#114337=CARTESIAN_POINT('Ctrl Pts',(-11.0482623384985,10.8207677107044,
12.0213292747129));
#114338=CARTESIAN_POINT('Ctrl Pts',(-11.0610838036623,10.819754997594,12.0079588281649));
#114339=CARTESIAN_POINT('Ctrl Pts',(-11.0658231988062,10.8193793845616,
12.0029460348501));
#114340=CARTESIAN_POINT('Ctrl Pts',(-11.0746029278732,10.8186811055779,
11.9935273169167));
#114341=CARTESIAN_POINT('Ctrl Pts',(-11.0786520382124,10.8183580718146,
11.9891298013773));
#114342=CARTESIAN_POINT('Ctrl Pts',(-11.0876951689677,10.8176343012436,
11.9791869876923));
#114343=CARTESIAN_POINT('Ctrl Pts',(-11.0926739677109,10.8172342031675,
11.9736280298675));
#114344=CARTESIAN_POINT('Ctrl Pts',(-11.1066701655776,10.8161046484279,
11.9577583258368));
#114345=CARTESIAN_POINT('Ctrl Pts',(-11.1155857627045,10.8153793567944,
11.9473585851255));
#114346=CARTESIAN_POINT('Ctrl Pts',(-11.164933030371,10.8113291240717,11.888133842599));
#114347=CARTESIAN_POINT('Ctrl Pts',(-11.2023069099331,10.8081272035812,
11.8368452430039));
#114348=CARTESIAN_POINT('Ctrl Pts',(-11.2661724462096,10.802227944451,11.7360484391955));
#114349=CARTESIAN_POINT('Ctrl Pts',(-11.2933729088438,10.7995195818688,
11.6871292739145));
#114350=CARTESIAN_POINT('Ctrl Pts',(-11.3295642918049,10.7954671879514,
11.6122366278136));
#114351=CARTESIAN_POINT('Ctrl Pts',(-11.3407336662317,10.7941360479663,
11.5873738865482));
#114352=CARTESIAN_POINT('Ctrl Pts',(-11.3729925052898,10.7899912941477,
11.5098443459131));
#114353=CARTESIAN_POINT('Ctrl Pts',(-11.3917176598579,10.7871356946076,
11.4562568800924));
#114354=CARTESIAN_POINT('Ctrl Pts',(-11.4094933035069,10.783690734242,11.3939868318368));
#114355=CARTESIAN_POINT('Ctrl Pts',(-11.4116381353588,10.7832594743773,
11.3862314918515));
#114356=CARTESIAN_POINT('Ctrl Pts',(-11.4148026004861,10.7825982482181,
11.3744107566704));
#114357=CARTESIAN_POINT('Ctrl Pts',(-11.4158689356968,10.782370846197,11.3703578932564));
#114358=CARTESIAN_POINT('Ctrl Pts',(-11.4177629442364,10.7819584288677,
11.363031520339));
#114359=CARTESIAN_POINT('Ctrl Pts',(-11.418596711397,10.7817737620087,11.3597596708969));
#114360=CARTESIAN_POINT('Ctrl Pts',(-11.4204143973771,10.781364182019,11.3525221746251));
#114361=CARTESIAN_POINT('Ctrl Pts',(-11.4213930240943,10.7811389816206,
11.3485553243097));
#114362=CARTESIAN_POINT('Ctrl Pts',(-11.4241900704397,10.7804815795621,
11.3370098451807));
#114363=CARTESIAN_POINT('Ctrl Pts',(-11.4259645492666,10.7800470117977,
11.3294208422403));
#114364=CARTESIAN_POINT('Ctrl Pts',(-11.4317882136537,10.77856014688,11.3035853885632));
#114365=CARTESIAN_POINT('Ctrl Pts',(-11.4355483030422,10.7774938560526,
11.2852763272408));
#114366=CARTESIAN_POINT('Ctrl Pts',(-11.4552056333645,10.771268744215,11.1792968508592));
#114367=CARTESIAN_POINT('Ctrl Pts',(-11.4634195301979,10.765851273268,11.0903985669709));
#114368=CARTESIAN_POINT('Ctrl Pts',(-11.4634994116541,10.7605064521335,
11.0013122835481));
#114369=CARTESIAN_POINT('Ctrl Pts',(-11.4634994117402,10.7605064463713,
11.0013121875042));
#114370=CARTESIAN_POINT('Ctrl Pts',(-11.4634998039174,10.7604802041083,
11.0008747873294));
#114371=CARTESIAN_POINT('Ctrl Pts',(-11.4635,10.7604539637884,11.0004373914791));
#114372=CARTESIAN_POINT('Ctrl Pts',(-11.4635,10.7604277254418,11.0000000000833));
#114373=CARTESIAN_POINT('Ctrl Pts',(-11.463499418515,10.6893450235318,11.0013046096532));
#114374=CARTESIAN_POINT('Ctrl Pts',(-11.4634349907531,10.6932747544557,
11.0735790956281));
#114375=CARTESIAN_POINT('Ctrl Pts',(-11.4580128964482,10.6972044853797,
11.1456191271162));
#114376=CARTESIAN_POINT('Ctrl Pts',(-11.4473590059667,10.7011342163037,
11.2167582936063));
#114377=CARTESIAN_POINT('Ctrl Pts',(-11.4406841404891,10.7035962676385,
11.2613283375106));
#114378=CARTESIAN_POINT('Ctrl Pts',(-11.4319566126795,10.7060583189733,
11.3055453362204));
#114379=CARTESIAN_POINT('Ctrl Pts',(-11.4212166274608,10.7085203703081,
11.3492499789963));
#114380=CARTESIAN_POINT('Ctrl Pts',(-11.4080854742713,10.7115305768008,
11.4026850953113));
#114381=CARTESIAN_POINT('Ctrl Pts',(-11.3919089668557,10.7145407832936,
11.4554908217744));
#114382=CARTESIAN_POINT('Ctrl Pts',(-11.3727649466491,10.7175509897864,
11.5072954279822));
#114383=CARTESIAN_POINT('Ctrl Pts',(-11.3536549346268,10.7205558488309,
11.5590080064665));
#114384=CARTESIAN_POINT('Ctrl Pts',(-11.3315880529432,10.7235607078754,
11.609722502667));
#114385=CARTESIAN_POINT('Ctrl Pts',(-11.3066923639379,10.72656556692,11.6590806597272));
#114386=CARTESIAN_POINT('Ctrl Pts',(-11.2818212921532,10.729567454716,11.7083900107215));
#114387=CARTESIAN_POINT('Ctrl Pts',(-11.2541271907677,10.732569342512,11.7563452101873));
#114388=CARTESIAN_POINT('Ctrl Pts',(-11.2237861156574,10.7355712303081,
11.8026081192737));
#114389=CARTESIAN_POINT('Ctrl Pts',(-11.1934630601116,10.738571335283,11.8488435528187));
#114390=CARTESIAN_POINT('Ctrl Pts',(-11.1604964357665,10.7415714402579,
11.8933882473642));
#114391=CARTESIAN_POINT('Ctrl Pts',(-11.125106966386,10.7445715452328,11.9359308543849));
#114392=CARTESIAN_POINT('Ctrl Pts',(-11.0897245398217,10.7475710531603,
11.9784649950521));
#114393=CARTESIAN_POINT('Ctrl Pts',(-11.0519205633224,10.7505705610879,
12.0189974337215));
#114394=CARTESIAN_POINT('Ctrl Pts',(-11.011956158834,10.7535700690155,12.0572497257498));
#114395=CARTESIAN_POINT('Ctrl Pts',(-10.9719550224031,10.7565723338402,
12.0955371760898));
#114396=CARTESIAN_POINT('Ctrl Pts',(-10.9297898731728,10.7595745986649,
12.131539926898));
#114397=CARTESIAN_POINT('Ctrl Pts',(-10.8857577661469,10.7625768634896,
12.1650173516778));
#114398=CARTESIAN_POINT('Ctrl Pts',(-10.841705604808,10.7655804956883,12.198510023667));
#114399=CARTESIAN_POINT('Ctrl Pts',(-10.7957852292608,10.768584127887,12.2294747811257));
#114400=CARTESIAN_POINT('Ctrl Pts',(-10.748323061093,10.7715877600857,12.2577141353409));
#114401=CARTESIAN_POINT('Ctrl Pts',(-10.7007713900644,10.774597056452,12.2860067425593));
#114402=CARTESIAN_POINT('Ctrl Pts',(-10.6516725878829,10.7776063528183,
12.3115634352269));
#114403=CARTESIAN_POINT('Ctrl Pts',(-10.6013770268355,10.7806156491846,
12.3342330836831));
#114404=CARTESIAN_POINT('Ctrl Pts',(-10.5630015058961,10.7829117427824,
12.351530028998));
#114405=CARTESIAN_POINT('Ctrl Pts',(-10.5239297800624,10.7852078363802,
12.3671471852995));
#114406=CARTESIAN_POINT('Ctrl Pts',(-10.4843234063868,10.787503929978,12.3810369611368));
#114407=CARTESIAN_POINT('Ctrl Pts',(-10.4323989712049,10.7905141364707,
12.3992466253454));
#114408=CARTESIAN_POINT('Ctrl Pts',(-10.3793371053808,10.7935243429634,
12.414562059867));
#114409=CARTESIAN_POINT('Ctrl Pts',(-10.32549164717,10.7965345494561,12.426845274591));
#114410=CARTESIAN_POINT('Ctrl Pts',(-10.2717418421318,10.7995394085005,
12.4391066689331));
#114411=CARTESIAN_POINT('Ctrl Pts',(-10.217211717851,10.8025442675449,12.4483464166516));
#114412=CARTESIAN_POINT('Ctrl Pts',(-10.1622712787386,10.8055491265894,
12.4544759475827));
#114413=CARTESIAN_POINT('Ctrl Pts',(-10.107385165534,10.8085510143854,12.4605994175441));
#114414=CARTESIAN_POINT('Ctrl Pts',(-10.0520900634723,10.8115529021813,
12.4636187047463));
#114415=CARTESIAN_POINT('Ctrl Pts',(-9.99676536154247,10.8145547899773,
12.4634964253848));
#114416=CARTESIAN_POINT('Ctrl Pts',(-9.94147351695289,10.8175548949522,
12.463374218645));
#114417=CARTESIAN_POINT('Ctrl Pts',(-9.88615263436755,10.820554999927,12.4601141446112));
#114418=CARTESIAN_POINT('Ctrl Pts',(-9.83118408216089,10.8235551049018,
12.453730867762));
#114419=CARTESIAN_POINT('Ctrl Pts',(-9.77622646918038,10.8265546128293,
12.4473488612412));
#114420=CARTESIAN_POINT('Ctrl Pts',(-9.72162157159207,10.8295541207569,
12.4378449471583));
#114421=CARTESIAN_POINT('Ctrl Pts',(-9.66774528388968,10.8325536286844,
12.425285604229));
#114422=CARTESIAN_POINT('Ctrl Pts',(-9.61381947760378,10.835555893509,12.4127147178008));
#114423=CARTESIAN_POINT('Ctrl Pts',(-9.56062413452305,10.8385581583337,
12.3970829120905));
#114424=CARTESIAN_POINT('Ctrl Pts',(-9.50852311948919,10.8415604231584,
12.3785074268655));
#114425=CARTESIAN_POINT('Ctrl Pts',(-9.45639837517843,10.844564055357,12.3599234814823));
#114426=CARTESIAN_POINT('Ctrl Pts',(-9.40536943985125,10.8475676875557,
12.3383933896544));
#114427=CARTESIAN_POINT('Ctrl Pts',(-9.35578010493267,10.8505713197543,
12.3140825608764));
#114428=CARTESIAN_POINT('Ctrl Pts',(-9.30609725580016,10.8535806161206,
12.2897258874011));
#114429=CARTESIAN_POINT('Ctrl Pts',(-9.25785989153677,10.8565899124869,
12.2625782612703));
#114430=CARTESIAN_POINT('Ctrl Pts',(-9.21138607246561,10.8595992088531,
12.2328504870011));
#114431=CARTESIAN_POINT('Ctrl Pts',(-9.17592654124189,10.8618953024515,
12.2101681905818));
#114432=CARTESIAN_POINT('Ctrl Pts',(-9.14149316789575,10.8641913960498,
12.185984763789));
#114433=CARTESIAN_POINT('Ctrl Pts',(-9.10821410804107,10.8664874896482,
12.1604094850108));
#114434=CARTESIAN_POINT('Ctrl Pts',(-9.06458485785984,10.8694976961408,
12.1268799850447));
#114435=CARTESIAN_POINT('Ctrl Pts',(-9.02275759696782,10.8725079026334,
12.0908160919466));
#114436=CARTESIAN_POINT('Ctrl Pts',(-8.98304127681541,10.875518109126,12.0524386943375));
#114437=CARTESIAN_POINT('Ctrl Pts',(-8.94339551028357,10.8785229681704,
12.0141294718347));
#114438=CARTESIAN_POINT('Ctrl Pts',(-8.9058536193491,10.8815278272147,11.9735152647533));
#114439=CARTESIAN_POINT('Ctrl Pts',(-8.8706920063438,10.8845326862591,11.9308575108276));
#114440=CARTESIAN_POINT('Ctrl Pts',(-8.8355651616545,10.887534574055,11.8882419375115));
#114441=CARTESIAN_POINT('Ctrl Pts',(-8.80281426664224,10.8905364618508,
11.8435872257451));
#114442=CARTESIAN_POINT('Ctrl Pts',(-8.77267798871069,10.8935383496467,
11.7971906488443));
#114443=CARTESIAN_POINT('Ctrl Pts',(-8.74255960871446,10.8965384546215,
11.7508216268702));
#114444=CARTESIAN_POINT('Ctrl Pts',(-8.7150530550755,10.8995385595962,11.7027132321823));
#114445=CARTESIAN_POINT('Ctrl Pts',(-8.69035449104467,10.9025386645709,
11.6531928435563));
#114446=CARTESIAN_POINT('Ctrl Pts',(-8.66566084224569,10.9055381724983,
11.6036823099239));
#114447=CARTESIAN_POINT('Ctrl Pts',(-8.64377430882604,10.9085376804257,
11.5527608127128));
#114448=CARTESIAN_POINT('Ctrl Pts',(-8.62484467216533,10.9115371883532,
11.5007794667595));
#114449=CARTESIAN_POINT('Ctrl Pts',(-8.60589763696374,10.9145394531777,
11.4487503438948));
#114450=CARTESIAN_POINT('Ctrl Pts',(-8.58991310925893,10.9175417180023,
11.3956599233924));
#114451=CARTESIAN_POINT('Ctrl Pts',(-8.57699178734229,10.9205439828268,
11.3418769906102));
#114452=CARTESIAN_POINT('Ctrl Pts',(-8.56406458044193,10.9235476150254,
11.2880695625259));
#114453=CARTESIAN_POINT('Ctrl Pts',(-8.55420345460581,10.9265512472239,
11.2335695139773));
#114454=CARTESIAN_POINT('Ctrl Pts',(-8.54745779859224,10.9295548794225,
11.1787551485399));
#114455=CARTESIAN_POINT('Ctrl Pts',(-8.54069942180473,10.9325641757886,
11.1238374156686));
#114456=CARTESIAN_POINT('Ctrl Pts',(-8.53706828588017,10.9355734721548,
11.0686047100736));
#114457=CARTESIAN_POINT('Ctrl Pts',(-8.5365617013168,10.938582768521,11.0134385991544));
#114458=CARTESIAN_POINT('Ctrl Pts',(-8.53617517721555,10.9408788621201,
10.9713468478755));
#114459=CARTESIAN_POINT('Ctrl Pts',(-8.5376065868234,10.9431749557192,10.9292939478672));
#114460=CARTESIAN_POINT('Ctrl Pts',(-8.54083446443999,10.9454710493182,
10.8874469465813));
#114461=CARTESIAN_POINT('Ctrl Pts',(-8.54506625105535,10.9484812558113,
10.832585021512));
#114462=CARTESIAN_POINT('Ctrl Pts',(-8.55240528538672,10.9514914623044,
10.7778468929808));
#114463=CARTESIAN_POINT('Ctrl Pts',(-8.56283545473865,10.9545016687974,
10.7236120121211));
#114464=CARTESIAN_POINT('Ctrl Pts',(-8.57324709553083,10.9575065278422,
10.6694734762196));
#114465=CARTESIAN_POINT('Ctrl Pts',(-8.58673887504706,10.960511386887,10.6158369282496));
#114466=CARTESIAN_POINT('Ctrl Pts',(-8.60324293386438,10.9635162459319,
10.5630767250418));
#114467=CARTESIAN_POINT('Ctrl Pts',(-8.61973067322752,10.9665181337282,
10.5103686918928));
#114468=CARTESIAN_POINT('Ctrl Pts',(-8.63922463455454,10.9695200215245,
10.4585357884465));
#114469=CARTESIAN_POINT('Ctrl Pts',(-8.66160632448387,10.9725219093209,
10.4079403582928));
#114470=CARTESIAN_POINT('Ctrl Pts',(-8.68397472192765,10.9755220142961,
10.3573749767649));
#114471=CARTESIAN_POINT('Ctrl Pts',(-8.70922723546476,10.9785221192713,
10.3080460938113));
#114472=CARTESIAN_POINT('Ctrl Pts',(-8.73719692958272,10.9815222242465,
10.260296914063));
#114473=CARTESIAN_POINT('Ctrl Pts',(-8.76516105748513,10.9845217321743,
10.2125572368222));
#114474=CARTESIAN_POINT('Ctrl Pts',(-8.79584102530502,10.9875212401022,
10.1663970938549));
#114475=CARTESIAN_POINT('Ctrl Pts',(-8.82902466977638,10.9905207480301,
10.1221338222669));
#114476=CARTESIAN_POINT('Ctrl Pts',(-8.86223881388195,10.9935230128551,
10.077829867577));
#114477=CARTESIAN_POINT('Ctrl Pts',(-8.89796091461215,10.9965252776801,
10.0354266908642));
#114478=CARTESIAN_POINT('Ctrl Pts',(-8.93593718392468,10.9995275425051,
9.9952101844436));
#114479=CARTESIAN_POINT('Ctrl Pts',(-8.97393074943399,11.0025311747041,
9.95497536151579));
#114480=CARTESIAN_POINT('Ctrl Pts',(-9.01418014565303,11.0055348069031,
9.91692955754966));
#114481=CARTESIAN_POINT('Ctrl Pts',(-9.05639556972368,11.0085384391021,
9.88132089982743));
#114482=CARTESIAN_POINT('Ctrl Pts',(-9.09869060248836,11.0115477354687,
9.84564509227075));
#114483=CARTESIAN_POINT('Ctrl Pts',(-9.14295864597717,11.0145570318353,
9.8124159297475));
#114484=CARTESIAN_POINT('Ctrl Pts',(-9.18887869987918,11.0175663282019,
9.78183971231602));
#114485=CARTESIAN_POINT('Ctrl Pts',(-9.22391570814423,11.0198624217974,
9.75851005366304));
#114486=CARTESIAN_POINT('Ctrl Pts',(-9.25991380500009,11.0221585153929,
9.73672399505271));
#114487=CARTESIAN_POINT('Ctrl Pts',(-9.29672136993095,11.0244546089884,
9.71655486346778));
#114488=CARTESIAN_POINT('Ctrl Pts',(-9.34497653302352,11.0274648154808,
9.69011288786048));
#114489=CARTESIAN_POINT('Ctrl Pts',(-9.39482634721519,11.0304750219732,
9.66634063167969));
#114490=CARTESIAN_POINT('Ctrl Pts',(-9.44594424770867,11.0334852284657,
9.64543199751622));
#114491=CARTESIAN_POINT('Ctrl Pts',(-9.49697134036953,11.0364900875099,
9.62456050626616));
#114492=CARTESIAN_POINT('Ctrl Pts',(-9.54926156404086,11.039494946554,9.60654274003543));
#114493=CARTESIAN_POINT('Ctrl Pts',(-9.60246433689903,11.0424998055982,
9.59152648354225));
#114494=CARTESIAN_POINT('Ctrl Pts',(-9.65561450207914,11.045501693394,9.57652507534258));
#114495=CARTESIAN_POINT('Ctrl Pts',(-9.70967492321259,11.0485035811897,
9.56451944026266));
#114496=CARTESIAN_POINT('Ctrl Pts',(-9.76427740368708,11.0515054689854,
9.55560839534858));
#114497=CARTESIAN_POINT('Ctrl Pts',(-9.81884745574875,11.05450557396,9.54670264270402));
#114498=CARTESIAN_POINT('Ctrl Pts',(-9.87395840891588,11.0575056789346,
9.54088792230632));
#114499=CARTESIAN_POINT('Ctrl Pts',(-9.92923161693159,11.0605057839091,
9.53821202428058));
#114500=CARTESIAN_POINT('Ctrl Pts',(-9.984493825092,11.0635052918364,9.53553665878212));
#114501=CARTESIAN_POINT('Ctrl Pts',(-10.0399176968041,11.0665047997637,
9.53599890063128));
#114502=CARTESIAN_POINT('Ctrl Pts',(-10.0951215276541,11.0695043076909,
9.53959452720255));
#114503=CARTESIAN_POINT('Ctrl Pts',(-10.1503760972545,11.0725065725153,
9.54319345857343));
#114504=CARTESIAN_POINT('Ctrl Pts',(-10.2054096938424,11.0755088373398,
9.54993149399967));
#114505=CARTESIAN_POINT('Ctrl Pts',(-10.2598441946035,11.0785111021642,
9.55975236694141));
#114506=CARTESIAN_POINT('Ctrl Pts',(-10.3143034874218,11.0815147343626,
9.56957771277516));
#114507=CARTESIAN_POINT('Ctrl Pts',(-10.3681626260665,11.084518366561,9.58248857172123));
#114508=CARTESIAN_POINT('Ctrl Pts',(-10.4210554282106,11.0875219987594,
9.59837787675339));
#114509=CARTESIAN_POINT('Ctrl Pts',(-10.4740479741572,11.0905312951255,
9.61429714540322));
#114510=CARTESIAN_POINT('Ctrl Pts',(-10.5260700457833,11.0935405914915,
9.63320589943068));
#114511=CARTESIAN_POINT('Ctrl Pts',(-10.576773436003,11.0965498878575,9.65494808519475));
#114512=CARTESIAN_POINT('Ctrl Pts',(-10.6154601307107,11.0988459814578,
9.67153737635038));
#114513=CARTESIAN_POINT('Ctrl Pts',(-10.6533794910279,11.1011420750581,
9.6897751790565));
#114514=CARTESIAN_POINT('Ctrl Pts',(-10.6903872410026,11.1034381686584,
9.70957460213277));
#114515=CARTESIAN_POINT('Ctrl Pts',(-10.7389048490023,11.1064483751505,
9.73553188535293));
#114516=CARTESIAN_POINT('Ctrl Pts',(-10.7860583777846,11.1094585816426,
9.76428373505595));
#114517=CARTESIAN_POINT('Ctrl Pts',(-10.8315069607238,11.1124687881346,
9.79566266176466));
#114518=CARTESIAN_POINT('Ctrl Pts',(-10.8768748070272,11.1154736471784,
9.82698584572369));
#114519=CARTESIAN_POINT('Ctrl Pts',(-10.9205432869829,11.1184785062222,
9.86092654767628));
#114520=CARTESIAN_POINT('Ctrl Pts',(-10.9621970268473,11.121483365266,9.8972719593997));
#114521=CARTESIAN_POINT('Ctrl Pts',(-11.0038095788859,11.1244852530614,
9.93358143224962));
#114522=CARTESIAN_POINT('Ctrl Pts',(-11.0434109413571,11.1274871408567,
9.97229055903382));
#114523=CARTESIAN_POINT('Ctrl Pts',(-11.0807171191185,11.1304890286521,
10.0131450165074));
#114524=CARTESIAN_POINT('Ctrl Pts',(-11.1180011407411,11.1334891336262,
10.0539752105188));
#114525=CARTESIAN_POINT('Ctrl Pts',(-11.1529923240554,11.1364892386004,
10.0969478206531));
#114526=CARTESIAN_POINT('Ctrl Pts',(-11.1854436932004,11.1394893435746,
10.1417718833251));
#114527=CARTESIAN_POINT('Ctrl Pts',(-11.2178886042371,11.1424888515015,
10.1865870256137));
#114528=CARTESIAN_POINT('Ctrl Pts',(-11.2477943954007,11.1454883594283,
10.2332524611863));
#114529=CARTESIAN_POINT('Ctrl Pts',(-11.2749559756063,11.1484878673552,
10.2814462370387));
#114530=CARTESIAN_POINT('Ctrl Pts',(-11.3021425204678,11.1514901321792,
10.3296843085845));
#114531=CARTESIAN_POINT('Ctrl Pts',(-11.326579555432,11.1544923970032,10.3794530658141));
#114532=CARTESIAN_POINT('Ctrl Pts',(-11.3481075293614,11.1574946618272,
10.4304051095039));
#114533=CARTESIAN_POINT('Ctrl Pts',(-11.3696453081526,11.1604982940252,
10.4813803591746));
#114534=CARTESIAN_POINT('Ctrl Pts',(-11.3882712068658,11.1635019262232,
10.5335394714238));
#114535=CARTESIAN_POINT('Ctrl Pts',(-11.4038747417405,11.1665055584212,
10.5865172802847));
#114536=CARTESIAN_POINT('Ctrl Pts',(-11.4195077013352,11.1695148547868,
10.6395949932514));
#114537=CARTESIAN_POINT('Ctrl Pts',(-11.4321067910242,11.1725241511524,
10.6934939714734));
#114538=CARTESIAN_POINT('Ctrl Pts',(-11.4416123738597,11.175533447518,10.7478373272378));
#114539=CARTESIAN_POINT('Ctrl Pts',(-11.4488651350685,11.1778295411215,
10.7893013162918));
#114540=CARTESIAN_POINT('Ctrl Pts',(-11.4543180078065,11.180125634725,10.8310237505242));
#114541=CARTESIAN_POINT('Ctrl Pts',(-11.4579648995368,11.1824217283285,
10.8728363191844));
#114542=CARTESIAN_POINT('Ctrl Pts',(-11.4616302923563,11.1847294702714,
10.9148610076761));
#114543=CARTESIAN_POINT('Ctrl Pts',(-11.4634790087263,11.1870372122142,
10.9570464174956));
#114544=CARTESIAN_POINT('Ctrl Pts',(-11.4634998222683,11.1893449541571,
10.999278736866));
#114545=CARTESIAN_POINT('Origin',(-10.,3.5,11.));
#114546=CARTESIAN_POINT('',(-11.4634998686003,11.759483043376,10.9993798331215));
#114547=CARTESIAN_POINT('',(-11.4634998405534,11.6905473354117,10.9993168449445));
#114548=CARTESIAN_POINT('',(-11.4635,3.5,11.));
#114549=CARTESIAN_POINT('Ctrl Pts',(-11.4634998686003,11.759483043376,10.9993798331215));
#114550=CARTESIAN_POINT('Ctrl Pts',(-11.4634424942562,11.7525188724877,
10.863985074265));
#114551=CARTESIAN_POINT('Ctrl Pts',(-11.4445984465822,11.7461686400878,
10.7292564909312));
#114552=CARTESIAN_POINT('Ctrl Pts',(-11.3938575632165,11.7369685184196,
10.5511426273315));
#114553=CARTESIAN_POINT('Ctrl Pts',(-11.3777805713092,11.7344413008791,
10.5039842588742));
#114554=CARTESIAN_POINT('Ctrl Pts',(-11.3565020214225,11.7313814454091,
10.4506431739692));
#114555=CARTESIAN_POINT('Ctrl Pts',(-11.3536148451146,11.7309713329516,
10.443567162624));
#114556=CARTESIAN_POINT('Ctrl Pts',(-11.3491115253287,11.730338786047,10.4327727284323));
#114557=CARTESIAN_POINT('Ctrl Pts',(-11.3475350862997,11.7301186425966,
10.4290377632698));
#114558=CARTESIAN_POINT('Ctrl Pts',(-11.3446168045301,11.7297133682378,
10.4222030565607));
#114559=CARTESIAN_POINT('Ctrl Pts',(-11.3432797318978,11.7295285212857,
10.4191013684297));
#114560=CARTESIAN_POINT('Ctrl Pts',(-11.3402453023586,11.729110892674,10.4121287177449));
#114561=CARTESIAN_POINT('Ctrl Pts',(-11.3385419179345,11.7288777568964,
10.4082604897329));
#114562=CARTESIAN_POINT('Ctrl Pts',(-11.334119134539,11.7282758431147,10.398333574308));
#114563=CARTESIAN_POINT('Ctrl Pts',(-11.3313752384149,11.727905663636,10.3922859849185));
#114564=CARTESIAN_POINT('Ctrl Pts',(-11.3139025398083,11.7255694592676,
10.354462215987));
#114565=CARTESIAN_POINT('Ctrl Pts',(-11.2980791811996,11.7235458891817,
10.3232068399372));
#114566=CARTESIAN_POINT('Ctrl Pts',(-11.2752789935019,11.7207739495255,
10.2819169122308));
#114567=CARTESIAN_POINT('Ctrl Pts',(-11.2692744583298,11.7200559390253,
10.2713559364059));
#114568=CARTESIAN_POINT('Ctrl Pts',(-11.2006257645169,11.711987347571,10.1540382899813));
#114569=CARTESIAN_POINT('Ctrl Pts',(-11.1247988889472,11.7044068157916,
10.0555488463371));
#114570=CARTESIAN_POINT('Ctrl Pts',(-11.0190471673143,11.6957650675023,
9.94925841761822));
#114571=CARTESIAN_POINT('Ctrl Pts',(-11.0001243080575,11.6942777935473,
9.93123132143435));
#114572=CARTESIAN_POINT('Ctrl Pts',(-10.9710413142432,11.6920787460667,
9.90497427782668));
#114573=CARTESIAN_POINT('Ctrl Pts',(-10.9612378316976,11.6913515348915,
9.89635856708299));
#114574=CARTESIAN_POINT('Ctrl Pts',(-10.945185979161,11.6901831422179,9.88262769097901));
#114575=CARTESIAN_POINT('Ctrl Pts',(-10.9390083765175,11.6897386948096,
9.87743121161688));
#114576=CARTESIAN_POINT('Ctrl Pts',(-10.9272282591607,11.6889008938301,
9.86768729378933));
#114577=CARTESIAN_POINT('Ctrl Pts',(-10.9216345112152,11.6885071384502,
9.86312967337223));
#114578=CARTESIAN_POINT('Ctrl Pts',(-10.9159158980214,11.6881086647101,
9.85854026288203));
#114579=CARTESIAN_POINT('Ctrl Pts',(-10.9158245712297,11.6881023020954,
9.85846698758125));
#114580=CARTESIAN_POINT('Ctrl Pts',(-10.9156395850463,11.6880894164798,
9.85831860192528));
#114581=CARTESIAN_POINT('Ctrl Pts',(-10.9155459251939,11.6880828935006,
9.8582434921252));
#114582=CARTESIAN_POINT('Ctrl Pts',(-10.91535610056,11.6880696753179,9.85809130209254));
#114583=CARTESIAN_POINT('Ctrl Pts',(-10.9152599352929,11.6880629801397,
9.85801422248929));
#114584=CARTESIAN_POINT('Ctrl Pts',(-10.9150649131779,11.6880494047442,
9.85785794635015));
#114585=CARTESIAN_POINT('Ctrl Pts',(-10.9149660557833,11.6880425245542,
9.85777875050008));
#114586=CARTESIAN_POINT('Ctrl Pts',(-10.9103385841818,11.6877205232028,
9.85407261347046));
#114587=CARTESIAN_POINT('Ctrl Pts',(-10.9057884079304,11.687406471117,9.85047258647511));
#114588=CARTESIAN_POINT('Ctrl Pts',(-10.895814345535,11.686723589641,9.84267725991775));
#114589=CARTESIAN_POINT('Ctrl Pts',(-10.8903821247848,11.6863551896471,
9.83849281516649));
#114590=CARTESIAN_POINT('Ctrl Pts',(-10.8755712654802,11.6853601156105,
9.82724896207685));
#114591=CARTESIAN_POINT('Ctrl Pts',(-10.8661366720745,11.6847363147741,
9.82026387959406));
#114592=CARTESIAN_POINT('Ctrl Pts',(-10.8204839211805,11.6817642436415,
9.78730688070494));
#114593=CARTESIAN_POINT('Ctrl Pts',(-10.7831744819301,11.6794745936183,
9.76288372335997));
#114594=CARTESIAN_POINT('Ctrl Pts',(-10.648064197173,11.6715717947472,9.68300522338928));
#114595=CARTESIAN_POINT('Ctrl Pts',(-10.5450626399567,11.666257996532,9.63714713233808));
#114596=CARTESIAN_POINT('Ctrl Pts',(-10.3931199970811,11.6583583565572,
9.58950913556167));
#114597=CARTESIAN_POINT('Ctrl Pts',(-10.3477653502953,11.6559880039351,
9.57764760496075));
#114598=CARTESIAN_POINT('Ctrl Pts',(-10.2916510011308,11.6529573775868,
9.56581654810985));
#114599=CARTESIAN_POINT('Ctrl Pts',(-10.2813550799387,11.652397319608,9.56376123619725));
#114600=CARTESIAN_POINT('Ctrl Pts',(-10.2665102913943,11.6515829486251,
9.56096360539452));
#114601=CARTESIAN_POINT('Ctrl Pts',(-10.2619784080785,11.6513334156389,
9.56013167513231));
#114602=CARTESIAN_POINT('Ctrl Pts',(-10.2540806978368,11.6508968408326,
9.55872039034368));
#114603=CARTESIAN_POINT('Ctrl Pts',(-10.2507166054712,11.6507103356166,
9.55813138676255));
#114604=CARTESIAN_POINT('Ctrl Pts',(-10.2436006556844,11.6503146401129,
9.55691114442579));
#114605=CARTESIAN_POINT('Ctrl Pts',(-10.239848397897,11.6501053008798,9.55628275971959));
#114606=CARTESIAN_POINT('Ctrl Pts',(-10.2296891584629,11.6495367342492,
9.55462210628225));
#114607=CARTESIAN_POINT('Ctrl Pts',(-10.2232777677505,11.649176004278,9.55361782353091));
#114608=CARTESIAN_POINT('Ctrl Pts',(-10.1936538664019,11.6475010936978,
9.54917918195676));
#114609=CARTESIAN_POINT('Ctrl Pts',(-10.1703687125812,11.646161532245,9.54626094421371));
#114610=CARTESIAN_POINT('Ctrl Pts',(-10.0534673905235,11.6393543889882,
9.53445718900411));
#114611=CARTESIAN_POINT('Ctrl Pts',(-9.95922065802072,11.6336199679331,
9.53404955545915));
#114612=CARTESIAN_POINT('Ctrl Pts',(-9.80520023455023,11.6243634832209,
9.54825513208688));
#114613=CARTESIAN_POINT('Ctrl Pts',(-9.74521144150929,11.6207837092217,
9.55757354901897));
#114614=CARTESIAN_POINT('Ctrl Pts',(-9.65207574211328,11.6153174881503,
9.57803474818691));
#114615=CARTESIAN_POINT('Ctrl Pts',(-9.61845600041192,11.6133628021498,
9.58668442067806));
#114616=CARTESIAN_POINT('Ctrl Pts',(-9.57521487396315,11.6108721633427,
9.59946521493751));
#114617=CARTESIAN_POINT('Ctrl Pts',(-9.56528772308476,11.6103019693183,
9.60251463995475));
#114618=CARTESIAN_POINT('Ctrl Pts',(-9.54914339413789,11.6093771243343,
9.60766253759527));
#114619=CARTESIAN_POINT('Ctrl Pts',(-9.5429065039128,11.6090204379554,9.60969757748716));
#114620=CARTESIAN_POINT('Ctrl Pts',(-9.53088745208363,11.6083341680599,
9.61370890405043));
#114621=CARTESIAN_POINT('Ctrl Pts',(-9.52510357960061,11.6080044113381,
9.61567959750339));
#114622=CARTESIAN_POINT('Ctrl Pts',(-9.51179683587907,11.6072468187616,
9.62030671261641));
#114623=CARTESIAN_POINT('Ctrl Pts',(-9.50428296762525,11.6068198226367,
9.62298855345223));
#114624=CARTESIAN_POINT('Ctrl Pts',(-9.48012368217048,11.6054491929746,
9.6318348339827));
#114625=CARTESIAN_POINT('Ctrl Pts',(-9.46356803220921,11.6045134845507,
9.63824081169274));
#114626=CARTESIAN_POINT('Ctrl Pts',(-9.33997749788962,11.5975463788458,
9.68866626711206));
#114627=CARTESIAN_POINT('Ctrl Pts',(-9.23838775952141,11.591965677738,9.74494023042731));
#114628=CARTESIAN_POINT('Ctrl Pts',(-9.07848775998065,11.5823594252192,
9.86014756995489));
#114629=CARTESIAN_POINT('Ctrl Pts',(-9.01657999458253,11.5783670579818,
9.91310982224851));
#114630=CARTESIAN_POINT('Ctrl Pts',(-8.9534226984433,11.5735939322803,9.97697485353089));
#114631=CARTESIAN_POINT('Ctrl Pts',(-8.94749884260123,11.5731386873473,
9.98307040296981));
#114632=CARTESIAN_POINT('Ctrl Pts',(-8.93870673871934,11.5724509858833,
9.99227644642512));
#114633=CARTESIAN_POINT('Ctrl Pts',(-8.93579823325915,11.5722214795905,
9.99534844566566));
#114634=CARTESIAN_POINT('Ctrl Pts',(-8.93081485720318,11.5718246858552,
10.0006578706696));
#114635=CARTESIAN_POINT('Ctrl Pts',(-8.92873360968667,11.5716578848684,
10.0028892329251));
#114636=CARTESIAN_POINT('Ctrl Pts',(-8.92399828930383,11.5712758709605,
10.0079980384012));
#114637=CARTESIAN_POINT('Ctrl Pts',(-8.92134881802128,11.571060327158,10.0108795825991));
#114638=CARTESIAN_POINT('Ctrl Pts',(-8.91412361622041,11.5704676618925,
10.018801208185));
#114639=CARTESIAN_POINT('Ctrl Pts',(-8.9095714985369,11.570088862648,10.0238625765528));
#114640=CARTESIAN_POINT('Ctrl Pts',(-8.88654011679276,11.5681454355156,
10.0498326483015));
#114641=CARTESIAN_POINT('Ctrl Pts',(-8.86862732873863,11.5665446624375,
10.0712338376494));
#114642=CARTESIAN_POINT('Ctrl Pts',(-8.83441132044706,11.5633261337647,
10.1145727068805));
#114643=CARTESIAN_POINT('Ctrl Pts',(-8.81808847498346,11.5617100395966,
10.1364819094037));
#114644=CARTESIAN_POINT('Ctrl Pts',(-8.7629388345888,11.5559882812125,10.2150012825382));
#114645=CARTESIAN_POINT('Ctrl Pts',(-8.72748877255023,11.5518262476291,
10.2738741785106));
#114646=CARTESIAN_POINT('Ctrl Pts',(-8.66194377399587,11.5432199472893,
10.4023753854391));
#114647=CARTESIAN_POINT('Ctrl Pts',(-8.63285497269362,11.5388050167115,
10.4723005416013));
#114648=CARTESIAN_POINT('Ctrl Pts',(-8.60373125867463,11.5335665810548,
10.5611545243207));
#114649=CARTESIAN_POINT('Ctrl Pts',(-8.59847542299494,11.5325750906874,
10.5782410058611));
#114650=CARTESIAN_POINT('Ctrl Pts',(-8.59129799792309,11.5311496087261,
10.603192330531));
#114651=CARTESIAN_POINT('Ctrl Pts',(-8.5891266756742,11.5307076496595,10.6109831320211));
#114652=CARTESIAN_POINT('Ctrl Pts',(-8.5854295984133,11.5299356609608,10.6246866515785));
#114653=CARTESIAN_POINT('Ctrl Pts',(-8.58387607265188,11.5296047502809,
10.6305916155493));
#114654=CARTESIAN_POINT('Ctrl Pts',(-8.58072709578384,11.5289200809813,
10.6428727519618));
#114655=CARTESIAN_POINT('Ctrl Pts',(-8.57913754992648,11.5285665168862,
10.6492503060187));
#114656=CARTESIAN_POINT('Ctrl Pts',(-8.57513442405915,11.5276548381275,
10.6657854906743));
#114657=CARTESIAN_POINT('Ctrl Pts',(-8.57278645417067,11.5270988098742,
10.6759587219705));
#114658=CARTESIAN_POINT('Ctrl Pts',(-8.56369899359542,11.5248555106611,
10.7173490598808));
#114659=CARTESIAN_POINT('Ctrl Pts',(-8.5578730292936,11.523196933513,10.7487588251569));
#114660=CARTESIAN_POINT('Ctrl Pts',(-8.53218269435429,11.5144510085156,
10.917980104887));
#114661=CARTESIAN_POINT('Ctrl Pts',(-8.53103444530728,11.5079672197986,
11.0578857983742));
#114662=CARTESIAN_POINT('Ctrl Pts',(-8.55505583806701,11.4989583218038,
11.2357818294622));
#114663=CARTESIAN_POINT('Ctrl Pts',(-8.56209649598592,11.4968914165499,
11.2754808220132));
#114664=CARTESIAN_POINT('Ctrl Pts',(-8.57233387995621,11.4943529938332,
11.3219547280457));
#114665=CARTESIAN_POINT('Ctrl Pts',(-8.57395532951994,11.4939614496551,
11.3290622899376));
#114666=CARTESIAN_POINT('Ctrl Pts',(-8.57654376880891,11.4933516931382,
11.340030059812));
#114667=CARTESIAN_POINT('Ctrl Pts',(-8.57747353757602,11.4931355227729,
11.3438990355231));
#114668=CARTESIAN_POINT('Ctrl Pts',(-8.57922297926627,11.4927338909099,
11.3510503567288));
#114669=CARTESIAN_POINT('Ctrl Pts',(-8.58003826458599,11.4925486770264,
11.354333691432));
#114670=CARTESIAN_POINT('Ctrl Pts',(-8.58192065730371,11.4921254452299,
11.3618036681155));
#114671=CARTESIAN_POINT('Ctrl Pts',(-8.58299492022926,11.4918870294069,
11.3659884142591));
#114672=CARTESIAN_POINT('Ctrl Pts',(-8.58584592001532,11.4912624017895,
11.3768936318395));
#114673=CARTESIAN_POINT('Ctrl Pts',(-8.58765201643302,11.4908746112489,
11.3836062318812));
#114674=CARTESIAN_POINT('Ctrl Pts',(-8.60055284734017,11.4881594522332,
11.4302275151662));
#114675=CARTESIAN_POINT('Ctrl Pts',(-8.6132889125125,11.4857518383235,11.4696592716363));
#114676=CARTESIAN_POINT('Ctrl Pts',(-8.64096512073443,11.481041905672,11.5443516599621));
#114677=CARTESIAN_POINT('Ctrl Pts',(-8.65565148326296,11.4787474078218,
11.5796735577058));
#114678=CARTESIAN_POINT('Ctrl Pts',(-8.69706546661657,11.4728132613263,
11.6692112389772));
#114679=CARTESIAN_POINT('Ctrl Pts',(-8.72579928695462,11.4691728498757,
11.7224231519741));
#114680=CARTESIAN_POINT('Ctrl Pts',(-8.7810844752932,11.4629966844251,11.8111885712552));
#114681=CARTESIAN_POINT('Ctrl Pts',(-8.80611374901831,11.4604296359684,
11.8475954727107));
#114682=CARTESIAN_POINT('Ctrl Pts',(-8.84406263891625,11.4568531892661,
11.8977709006743));
#114683=CARTESIAN_POINT('Ctrl Pts',(-8.85565908674962,11.4557976658339,
11.9125062695176));
#114684=CARTESIAN_POINT('Ctrl Pts',(-8.87682574403533,11.453935834131,11.9383639680648));
#114685=CARTESIAN_POINT('Ctrl Pts',(-8.88628591673415,11.4531254187194,
11.9495726978218));
#114686=CARTESIAN_POINT('Ctrl Pts',(-8.90081947171254,11.4519122266862,
11.9662765051693));
#114687=CARTESIAN_POINT('Ctrl Pts',(-8.90576890541274,11.4515044515295,
11.9718777869328));
#114688=CARTESIAN_POINT('Ctrl Pts',(-8.91479107840204,11.4507706865977,
11.9819318996718));
#114689=CARTESIAN_POINT('Ctrl Pts',(-8.91884883412423,11.4504440891259,
11.9863979000073));
#114690=CARTESIAN_POINT('Ctrl Pts',(-8.92761212326882,11.449745971754,11.995923809079));
#114691=CARTESIAN_POINT('Ctrl Pts',(-8.93232611606177,11.4493748178274,
12.0009757596638));
#114692=CARTESIAN_POINT('Ctrl Pts',(-8.94510061040143,11.44838058073,12.014473173132));
#114693=CARTESIAN_POINT('Ctrl Pts',(-8.9532267699252,11.4477602998774,12.0228559802902));
#114694=CARTESIAN_POINT('Ctrl Pts',(-8.99356461553095,11.4447387857988,
12.0634835714805));
#114695=CARTESIAN_POINT('Ctrl Pts',(-9.02717160273462,11.4423991512414,
12.0943102458646));
#114696=CARTESIAN_POINT('Ctrl Pts',(-9.07591485195291,11.4392055914501,
12.1349976569982));
#114697=CARTESIAN_POINT('Ctrl Pts',(-9.08987453997787,11.4383121002684,
12.1462219298007));
#114698=CARTESIAN_POINT('Ctrl Pts',(-9.18149871929675,11.432568204177,12.2171627984452));
#114699=CARTESIAN_POINT('Ctrl Pts',(-9.26478235065502,11.4279148031777,
12.2692057770446));
#114700=CARTESIAN_POINT('Ctrl Pts',(-9.38100134151841,11.421458148884,12.3265267261546));
#114701=CARTESIAN_POINT('Ctrl Pts',(-9.40981020434452,11.4198586877313,
12.3395925824074));
#114702=CARTESIAN_POINT('Ctrl Pts',(-9.45609249157997,11.4172577598147,
12.3588004355484));
#114703=CARTESIAN_POINT('Ctrl Pts',(-9.47329892573647,11.4162841147581,
12.3655621250389));
#114704=CARTESIAN_POINT('Ctrl Pts',(-9.49600347830573,11.4149850240082,
12.3739914973173));
#114705=CARTESIAN_POINT('Ctrl Pts',(-9.50139054316824,11.4146757460125,
12.3759555719406));
#114706=CARTESIAN_POINT('Ctrl Pts',(-9.51021329099656,11.4141673059653,
12.3791136495742));
#114707=CARTESIAN_POINT('Ctrl Pts',(-9.51364218039606,11.413969234299,12.3803266097115));
#114708=CARTESIAN_POINT('Ctrl Pts',(-9.52033180486485,11.4135818247282,
12.3826650250974));
#114709=CARTESIAN_POINT('Ctrl Pts',(-9.52359204767646,11.4133925618799,
12.3837917513907));
#114710=CARTESIAN_POINT('Ctrl Pts',(-9.53159678254224,11.4129268077977,
12.3865265133184));
#114711=CARTESIAN_POINT('Ctrl Pts',(-9.53634558633175,11.412649585399,12.3881217271715));
#114712=CARTESIAN_POINT('Ctrl Pts',(-9.55253278709311,11.4117017429061,
12.3934669868706));
#114713=CARTESIAN_POINT('Ctrl Pts',(-9.56400892420642,11.4110248850594,
12.3971001800116));
#114714=CARTESIAN_POINT('Ctrl Pts',(-9.64733843275038,11.406081637634,12.422354533796));
#114715=CARTESIAN_POINT('Ctrl Pts',(-9.72071029128511,11.4015821084823,
12.4385610814297));
#114716=CARTESIAN_POINT('Ctrl Pts',(-9.85869333012996,11.3931975413301,
12.4580821391088));
#114717=CARTESIAN_POINT('Ctrl Pts',(-9.92292114403549,11.3893247174424,
12.4628843995483));
#114718=CARTESIAN_POINT('Ctrl Pts',(-10.0275671328543,11.3831704423263,
12.4637954694185));
#114719=CARTESIAN_POINT('Ctrl Pts',(-10.0678748107872,11.3808364026854,
12.4624809510527));
#114720=CARTESIAN_POINT('Ctrl Pts',(-10.1256605894001,11.3775499753839,
12.4582017898254));
#114721=CARTESIAN_POINT('Ctrl Pts',(-10.1432173253624,11.3765593255652,
12.4565822594953));
#114722=CARTESIAN_POINT('Ctrl Pts',(-10.1746259480028,11.3748009529641,
12.4531115485322));
#114723=CARTESIAN_POINT('Ctrl Pts',(-10.1884884755116,11.374029740693,12.4513784853414));
#114724=CARTESIAN_POINT('Ctrl Pts',(-10.2095861661059,11.3728631336376,
12.4484335157498));
#114725=CARTESIAN_POINT('Ctrl Pts',(-10.2168402905223,11.3724632995181,
12.4473652965648));
#114726=CARTESIAN_POINT('Ctrl Pts',(-10.2300407460209,11.3717379805044,
12.4453199691868));
#114727=CARTESIAN_POINT('Ctrl Pts',(-10.2359896230982,11.3714119512394,
12.444360570442));
#114728=CARTESIAN_POINT('Ctrl Pts',(-10.2488558160518,11.3707085760832,
12.442203977344));
#114729=CARTESIAN_POINT('Ctrl Pts',(-10.2557708053247,11.3703316480437,
12.4409936942706));
#114730=CARTESIAN_POINT('Ctrl Pts',(-10.2746377429737,11.3693061056603,
12.4375514543835));
#114731=CARTESIAN_POINT('Ctrl Pts',(-10.2865711526202,11.3686606082065,
12.4352202131067));
#114732=CARTESIAN_POINT('Ctrl Pts',(-10.3500158759908,11.3652438766463,
12.4220031483192));
#114733=CARTESIAN_POINT('Ctrl Pts',(-10.4009431512887,11.3625564372787,
12.408491892493));
#114734=CARTESIAN_POINT('Ctrl Pts',(-10.5517992938335,11.3546352794877,
12.3596208081135));
#114735=CARTESIAN_POINT('Ctrl Pts',(-10.6487158848414,11.3496190955654,
12.3161373578487));
#114736=CARTESIAN_POINT('Ctrl Pts',(-10.7821001760998,11.3419303981839,
12.2379511348052));
#114737=CARTESIAN_POINT('Ctrl Pts',(-10.8228529943803,11.3394559791379,
12.211245545055));
#114738=CARTESIAN_POINT('Ctrl Pts',(-10.8683425189849,11.3364561228357,
12.1780795385852));
#114739=CARTESIAN_POINT('Ctrl Pts',(-10.8744547735832,11.3360478311921,
12.1735497320214));
#114740=CARTESIAN_POINT('Ctrl Pts',(-10.8837636605859,11.3354175169901,
12.1665377913031));
#114741=CARTESIAN_POINT('Ctrl Pts',(-10.8869858677704,11.3351977604464,
12.1640896425475));
#114742=CARTESIAN_POINT('Ctrl Pts',(-10.8928791169897,11.3347928504524,
12.1595734317947));
#114743=CARTESIAN_POINT('Ctrl Pts',(-10.8955531883116,11.3346079774608,
12.1575094589641));
#114744=CARTESIAN_POINT('Ctrl Pts',(-10.9015638265741,11.3341898464147,
12.1528368721524));
#114745=CARTESIAN_POINT('Ctrl Pts',(-10.9048962080823,11.333956230238,12.1502230387444));
#114746=CARTESIAN_POINT('Ctrl Pts',(-10.9134466631671,11.3333522600879,
12.1434561294621));
#114747=CARTESIAN_POINT('Ctrl Pts',(-10.9186477226205,11.3329804889804,
12.1392818285136));
#114748=CARTESIAN_POINT('Ctrl Pts',(-10.9514035971639,11.3306121508043,
12.1126222637292));
#114749=CARTESIAN_POINT('Ctrl Pts',(-10.9781576964593,11.3285562560528,
12.0891759450938));
#114750=CARTESIAN_POINT('Ctrl Pts',(-11.0119533995221,11.3258248614941,
12.0573084661654));
#114751=CARTESIAN_POINT('Ctrl Pts',(-11.0197938353524,11.3251811905767,
12.0497482562144));
#114752=CARTESIAN_POINT('Ctrl Pts',(-11.1160937526781,11.3171570681968,
11.9547931104636));
#114753=CARTESIAN_POINT('Ctrl Pts',(-11.1931654580102,11.3095387455601,
11.856538667084));
#114754=CARTESIAN_POINT('Ctrl Pts',(-11.270294152291,11.3008603254226,11.7272348183555));
#114755=CARTESIAN_POINT('Ctrl Pts',(-11.2831010585926,11.2993699947618,
11.7043930054864));
#114756=CARTESIAN_POINT('Ctrl Pts',(-11.3041442646358,11.2968326329587,
11.6643808577152));
#114757=CARTESIAN_POINT('Ctrl Pts',(-11.3126708161345,11.2957760194702,
11.6473712715336));
#114758=CARTESIAN_POINT('Ctrl Pts',(-11.3244335666525,11.2942753146663,
11.622717199005));
#114759=CARTESIAN_POINT('Ctrl Pts',(-11.3279399550492,11.2938220332981,
11.6152044067964));
#114760=CARTESIAN_POINT('Ctrl Pts',(-11.3339309244136,11.2930369474052,
11.6020782454489));
#114761=CARTESIAN_POINT('Ctrl Pts',(-11.3364443555855,11.2927041694526,
11.5964783405632));
#114762=CARTESIAN_POINT('Ctrl Pts',(-11.3412298601791,11.2920638432507,
11.5856341638999));
#114763=CARTESIAN_POINT('Ctrl Pts',(-11.343506586619,11.2917561425349,11.5803920784616));
#114764=CARTESIAN_POINT('Ctrl Pts',(-11.3488420787001,11.2910276090775,
11.5679076522584));
#114765=CARTESIAN_POINT('Ctrl Pts',(-11.351873326542,11.2906077021265,11.560653696133));
#114766=CARTESIAN_POINT('Ctrl Pts',(-11.3608518716564,11.2893451986867,
11.5386712546625));
#114767=CARTESIAN_POINT('Ctrl Pts',(-11.3666180901469,11.2885085790709,
11.5238697914193));
#114768=CARTESIAN_POINT('Ctrl Pts',(-11.4128432419754,11.2815697369377,
11.399252198799));
#114769=CARTESIAN_POINT('Ctrl Pts',(-11.440236324836,11.275931943562,11.28504386706));
#114770=CARTESIAN_POINT('Ctrl Pts',(-11.4602677332692,11.2674633686444,
11.112514165549));
#114771=CARTESIAN_POINT('Ctrl Pts',(-11.4635279155575,11.2646839331958,
11.0559152993318));
#114772=CARTESIAN_POINT('Ctrl Pts',(-11.463499819958,11.2617878197064,10.9992740641209));
#114773=CARTESIAN_POINT('Ctrl Pts',(-11.4634998522255,11.1882569054959,
10.99934232525));
#114774=CARTESIAN_POINT('Ctrl Pts',(-11.4635338577437,11.1926793304679,
11.0750135760492));
#114775=CARTESIAN_POINT('Ctrl Pts',(-11.4576989133034,11.1972663920743,
11.1505728907243));
#114776=CARTESIAN_POINT('Ctrl Pts',(-11.4355453177886,11.2059062555568,
11.2927357097168));
#114777=CARTESIAN_POINT('Ctrl Pts',(-11.4203436720628,11.2099570437846,
11.3593187447778));
#114778=CARTESIAN_POINT('Ctrl Pts',(-11.3897135834784,11.2160275233218,
11.4603518144949));
#114779=CARTESIAN_POINT('Ctrl Pts',(-11.3775105646457,11.2181359984491,
11.4956739190319));
#114780=CARTESIAN_POINT('Ctrl Pts',(-11.3601086820031,11.2207893666858,
11.5404165078517));
#114781=CARTESIAN_POINT('Ctrl Pts',(-11.3561407329977,11.2213742944607,
11.5502980551487));
#114782=CARTESIAN_POINT('Ctrl Pts',(-11.3495318268785,11.2223170183909,
11.5662507495036));
#114783=CARTESIAN_POINT('Ctrl Pts',(-11.3469569498686,11.2226769998052,
11.5723487051358));
#114784=CARTESIAN_POINT('Ctrl Pts',(-11.3419328037563,11.2233656542342,
11.5840254429781));
#114785=CARTESIAN_POINT('Ctrl Pts',(-11.3394898997157,11.223694531822,11.5896067994388));
#114786=CARTESIAN_POINT('Ctrl Pts',(-11.3338187661337,11.2244446177062,
11.6023465865331));
#114787=CARTESIAN_POINT('Ctrl Pts',(-11.3305676181248,11.2248650421615,
11.6094946497238));
#114788=CARTESIAN_POINT('Ctrl Pts',(-11.3203355243064,11.226159339565,11.6315191068243));
#114789=CARTESIAN_POINT('Ctrl Pts',(-11.3131613173344,11.2270266441307,
11.646304620224));
#114790=CARTESIAN_POINT('Ctrl Pts',(-11.2487837638936,11.2344807689899,
11.7734824723576));
#114791=CARTESIAN_POINT('Ctrl Pts',(-11.177527444974,11.2405144428455,11.8781611834126));
#114792=CARTESIAN_POINT('Ctrl Pts',(-11.0598518892127,11.2491721620616,
12.0105175878392));
#114793=CARTESIAN_POINT('Ctrl Pts',(-11.0240084805301,11.2516885334046,
12.046822719719));
#114794=CARTESIAN_POINT('Ctrl Pts',(-10.9738768593859,11.2551675984063,
12.0925571003518));
#114795=CARTESIAN_POINT('Ctrl Pts',(-10.9612117502599,11.2560434589762,
12.1037160341963));
#114796=CARTESIAN_POINT('Ctrl Pts',(-10.9422286974817,11.2573565504918,
12.119866988916));
#114797=CARTESIAN_POINT('Ctrl Pts',(-10.9360576667886,11.2577834597663,
12.1250302352685));
#114798=CARTESIAN_POINT('Ctrl Pts',(-10.9248992325891,11.2585561192119,
12.1342110343685));
#114799=CARTESIAN_POINT('Ctrl Pts',(-10.9199273977997,11.258900644706,12.1382472669462));
#114800=CARTESIAN_POINT('Ctrl Pts',(-10.9119542999476,11.2594538329858,
12.1446336243853));
#114801=CARTESIAN_POINT('Ctrl Pts',(-10.9089700115832,11.2596610406498,
12.1470049244167));
#114802=CARTESIAN_POINT('Ctrl Pts',(-10.9033089076799,11.2600544659016,
12.1514672400781));
#114803=CARTESIAN_POINT('Ctrl Pts',(-10.900634052081,11.2602405154443,12.1535606144061));
#114804=CARTESIAN_POINT('Ctrl Pts',(-10.8944920312796,11.2606680618265,
12.1583330499074));
#114805=CARTESIAN_POINT('Ctrl Pts',(-10.8910201047251,11.2609099821988,
12.1610058658297));
#114806=CARTESIAN_POINT('Ctrl Pts',(-10.8817212241847,11.2615584358344,
12.1680982058668));
#114807=CARTESIAN_POINT('Ctrl Pts',(-10.8758731302221,11.2619667878203,
12.172489654982));
#114808=CARTESIAN_POINT('Ctrl Pts',(-10.8264733175058,11.265418962106,12.2090091273422));
#114809=CARTESIAN_POINT('Ctrl Pts',(-10.781206944492,11.2685988583441,12.2387396063636));
#114810=CARTESIAN_POINT('Ctrl Pts',(-10.6422796541326,11.2781817087353,
12.3193378189134));
#114811=CARTESIAN_POINT('Ctrl Pts',(-10.5445850578446,11.2846710858472,
12.3625734969083));
#114812=CARTESIAN_POINT('Ctrl Pts',(-10.3979600770254,11.2936104666671,
12.4091484437394));
#114813=CARTESIAN_POINT('Ctrl Pts',(-10.3521880454408,11.2963010748327,
12.4212796503466));
#114814=CARTESIAN_POINT('Ctrl Pts',(-10.2946893415239,11.2995566599851,
12.4335696611234));
#114815=CARTESIAN_POINT('Ctrl Pts',(-10.2834459614915,11.3001875278057,
12.4358350109554));
#114816=CARTESIAN_POINT('Ctrl Pts',(-10.2654963904741,11.3011857754426,
12.4392324845373));
#114817=CARTESIAN_POINT('Ctrl Pts',(-10.2588070893192,11.3015558350145,
12.4404504054594));
#114818=CARTESIAN_POINT('Ctrl Pts',(-10.2461493823004,11.3022524445173,
12.4426639735371));
#114819=CARTESIAN_POINT('Ctrl Pts',(-10.2401828341048,11.3025792914326,
12.4436693065458));
#114820=CARTESIAN_POINT('Ctrl Pts',(-10.2266629668339,11.3033165438201,
12.4458611989896));
#114821=CARTESIAN_POINT('Ctrl Pts',(-10.2191062065598,11.3037262505235,
12.4470256322978));
#114822=CARTESIAN_POINT('Ctrl Pts',(-10.1995874378448,11.3047785799762,
12.4498769019648));
#114823=CARTESIAN_POINT('Ctrl Pts',(-10.1876129218288,11.3054184418868,
12.4514749667877));
#114824=CARTESIAN_POINT('Ctrl Pts',(-10.0829394314003,11.3109647745834,
12.4641271939158));
#114825=CARTESIAN_POINT('Ctrl Pts',(-9.98939683332163,11.3155815356956,
12.4664370591649));
#114826=CARTESIAN_POINT('Ctrl Pts',(-9.82937065051905,11.3234042208506,
12.4550652823896));
#114827=CARTESIAN_POINT('Ctrl Pts',(-9.76288738159231,11.3266374998875,
12.4457199905939));
#114828=CARTESIAN_POINT('Ctrl Pts',(-9.65316561131281,11.3322351874399,
12.4225229040288));
#114829=CARTESIAN_POINT('Ctrl Pts',(-9.60950750941634,11.3345353776697,
12.4111627843756));
#114830=CARTESIAN_POINT('Ctrl Pts',(-9.55929835679746,11.3373377064522,
12.3955896026911));
#114831=CARTESIAN_POINT('Ctrl Pts',(-9.55216646471291,11.3377395301958,
12.3933174072764));
#114832=CARTESIAN_POINT('Ctrl Pts',(-9.54123025632845,11.3383619467455,
12.3897405313191));
#114833=CARTESIAN_POINT('Ctrl Pts',(-9.53741326040538,11.338580361597,12.3884746773582));
#114834=CARTESIAN_POINT('Ctrl Pts',(-9.53039721874848,11.3389840818613,
12.3861157622858));
#114835=CARTESIAN_POINT('Ctrl Pts',(-9.52719670209757,11.3391691194281,
12.3850273352827));
#114836=CARTESIAN_POINT('Ctrl Pts',(-9.51996352002133,11.3395892746415,
12.382539492501));
#114837=CARTESIAN_POINT('Ctrl Pts',(-9.51593321050209,11.3398247656405,
12.3811335246087));
#114838=CARTESIAN_POINT('Ctrl Pts',(-9.5055202373898,11.3404366687097,12.3774497962112));
#114839=CARTESIAN_POINT('Ctrl Pts',(-9.49914721181735,11.3408145585016,
12.3751453224019));
#114840=CARTESIAN_POINT('Ctrl Pts',(-9.45740217733963,11.3433110638844,
12.3597217160524));
#114841=CARTESIAN_POINT('Ctrl Pts',(-9.42253529966939,11.3454963847404,
12.3452842113327));
#114842=CARTESIAN_POINT('Ctrl Pts',(-9.29438587855687,11.3538090634982,
12.2863206353601));
#114843=CARTESIAN_POINT('Ctrl Pts',(-9.2053421834017,11.3601341771834,12.2333015328602));
#114844=CARTESIAN_POINT('Ctrl Pts',(-9.08758944111155,11.3688197762693,
12.1451005107877));
#114845=CARTESIAN_POINT('Ctrl Pts',(-9.05374878703321,11.3713635216003,
12.1172991313714));
#114846=CARTESIAN_POINT('Ctrl Pts',(-9.00734496610683,11.3749111987279,
12.0755536735094));
#114847=CARTESIAN_POINT('Ctrl Pts',(-8.99372590804323,11.375960437172,12.0628227588898));
#114848=CARTESIAN_POINT('Ctrl Pts',(-8.96988012686894,11.3778123210649,
12.0396626643827));
#114849=CARTESIAN_POINT('Ctrl Pts',(-8.95955946815754,11.37861901084,12.0293342168726));
#114850=CARTESIAN_POINT('Ctrl Pts',(-8.94419970191335,11.3798278538856,
12.0134957659249));
#114851=CARTESIAN_POINT('Ctrl Pts',(-8.93904556594582,11.3802349506662,
12.0080990173196));
#114852=CARTESIAN_POINT('Ctrl Pts',(-8.92983647158431,11.3809650529399,
11.9983075791992));
#114853=CARTESIAN_POINT('Ctrl Pts',(-8.92576676618197,11.3812886813808,
11.9939270401103));
#114854=CARTESIAN_POINT('Ctrl Pts',(-8.91705738379454,11.3819834491744,
11.9844364763555));
#114855=CARTESIAN_POINT('Ctrl Pts',(-8.91242676692383,11.3823542051727,
11.9793183092796));
#114856=CARTESIAN_POINT('Ctrl Pts',(-8.90008718501891,11.3833460089234,
11.9654840452408));
#114857=CARTESIAN_POINT('Ctrl Pts',(-8.89244558790739,11.3839642793259,
11.9567083551246));
#114858=CARTESIAN_POINT('Ctrl Pts',(-8.85563077471804,11.3869644970278,
11.9133975051337));
#114859=CARTESIAN_POINT('Ctrl Pts',(-8.82796245483918,11.3892858965692,
11.8776129115956));
#114860=CARTESIAN_POINT('Ctrl Pts',(-8.73820138827559,11.397149338335,11.7496875480694));
#114861=CARTESIAN_POINT('Ctrl Pts',(-8.68496898238816,11.40240423267,11.6518124315955));
#114862=CARTESIAN_POINT('Ctrl Pts',(-8.62388760927176,11.4104798418267,
11.5008307100602));
#114863=CARTESIAN_POINT('Ctrl Pts',(-8.60702257077679,11.4131036899311,
11.4518069977571));
#114864=CARTESIAN_POINT('Ctrl Pts',(-8.5906774498911,11.4162735894621,11.3945903526116));
#114865=CARTESIAN_POINT('Ctrl Pts',(-8.58861995127858,11.4166869300703,
11.3871665656652));
#114866=CARTESIAN_POINT('Ctrl Pts',(-8.58556579661784,11.4173234703266,
11.3757987225679));
#114867=CARTESIAN_POINT('Ctrl Pts',(-8.58452678498911,11.4175443346645,
11.3718660677663));
#114868=CARTESIAN_POINT('Ctrl Pts',(-8.58265492112876,11.4179503482263,
11.3646595523714));
#114869=CARTESIAN_POINT('Ctrl Pts',(-8.58181699741172,11.418135207392,11.3613870948667));
#114870=CARTESIAN_POINT('Ctrl Pts',(-8.5799593317833,11.4185521219528,11.354026137339));
#114871=CARTESIAN_POINT('Ctrl Pts',(-8.57894592034459,11.4187845249927,
11.3499361471693));
#114872=CARTESIAN_POINT('Ctrl Pts',(-8.57602438381154,11.4194692133065,
11.3379232286568));
#114873=CARTESIAN_POINT('Ctrl Pts',(-8.57416478900355,11.4199240996775,
11.3299888011569));
#114874=CARTESIAN_POINT('Ctrl Pts',(-8.55726624375546,11.4242411825554,
11.2550761046984));
#114875=CARTESIAN_POINT('Ctrl Pts',(-8.54689245103548,11.4283201241921,
11.1871392351558));
#114876=CARTESIAN_POINT('Ctrl Pts',(-8.5346551527919,11.4373747604101,11.0368000541727));
#114877=CARTESIAN_POINT('Ctrl Pts',(-8.53490063362485,11.4423474610716,
10.9544444929529));
#114878=CARTESIAN_POINT('Ctrl Pts',(-8.54692419697573,11.4504326588445,
10.8169114196226));
#114879=CARTESIAN_POINT('Ctrl Pts',(-8.55496806311521,11.4536265045182,
10.7616000036699));
#114880=CARTESIAN_POINT('Ctrl Pts',(-8.56856024749333,11.4573883116653,
10.6951119579994));
#114881=CARTESIAN_POINT('Ctrl Pts',(-8.57111044210045,11.4580494938647,
10.6833754169989));
#114882=CARTESIAN_POINT('Ctrl Pts',(-8.5753567021834,11.4590843092491,10.6649304979668));
#114883=CARTESIAN_POINT('Ctrl Pts',(-8.57695632193355,11.4594609702094,
10.6582006585649));
#114884=CARTESIAN_POINT('Ctrl Pts',(-8.58004081992036,11.4601634255311,
10.6456208249245));
#114885=CARTESIAN_POINT('Ctrl Pts',(-8.58151428331777,11.4604895739194,
10.6397682053318));
#114886=CARTESIAN_POINT('Ctrl Pts',(-8.58489214075479,11.4612167763679,
10.6266934511137));
#114887=CARTESIAN_POINT('Ctrl Pts',(-8.5868157103419,11.4616172103819,10.6194764146541));
#114888=CARTESIAN_POINT('Ctrl Pts',(-8.59184044717048,11.4626296450614,
10.601187874811));
#114889=CARTESIAN_POINT('Ctrl Pts',(-8.59501701784213,11.46323923189,10.5901375021112));
#114890=CARTESIAN_POINT('Ctrl Pts',(-8.6158914852719,11.4670624821144,10.5206173732966));
#114891=CARTESIAN_POINT('Ctrl Pts',(-8.63710635422932,11.4701602134969,
10.4632634777758));
#114892=CARTESIAN_POINT('Ctrl Pts',(-8.70174583024231,11.4780770733069,
10.3173009905806));
#114893=CARTESIAN_POINT('Ctrl Pts',(-8.75064043438508,11.4827564871018,
10.2314681731663));
#114894=CARTESIAN_POINT('Ctrl Pts',(-8.82617550680336,11.4892448366329,
10.1253722688021));
#114895=CARTESIAN_POINT('Ctrl Pts',(-8.84539872465434,11.4908481850891,
10.1001481844332));
#114896=CARTESIAN_POINT('Ctrl Pts',(-8.87712323574395,11.4934548748436,
10.0612119401588));
#114897=CARTESIAN_POINT('Ctrl Pts',(-8.88909263149134,11.4944302468442,
10.0470781748281));
#114898=CARTESIAN_POINT('Ctrl Pts',(-8.90511759946581,11.495731378972,10.0288678193027));
#114899=CARTESIAN_POINT('Ctrl Pts',(-8.90893401068924,11.4960409104457,
10.0245820443698));
#114900=CARTESIAN_POINT('Ctrl Pts',(-8.91521134998595,11.4965496984126,
10.0176156169505));
#114901=CARTESIAN_POINT('Ctrl Pts',(-8.91765728071185,11.4967478622209,
10.0149214606584));
#114902=CARTESIAN_POINT('Ctrl Pts',(-8.92244177286516,11.4971353949788,
10.0096907451988));
#114903=CARTESIAN_POINT('Ctrl Pts',(-8.9247792919548,11.4973246883982,10.007153294208));
#114904=CARTESIAN_POINT('Ctrl Pts',(-8.93053247137639,11.4977904346543,
10.000952180998));
#114905=CARTESIAN_POINT('Ctrl Pts',(-8.93395799604242,11.4980676180705,
9.99729775918687));
#114906=CARTESIAN_POINT('Ctrl Pts',(-8.94567198399762,11.499014817498,9.98492890645159));
#114907=CARTESIAN_POINT('Ctrl Pts',(-8.95404886379648,11.4996910583094,
9.97629931520783));
#114908=CARTESIAN_POINT('Ctrl Pts',(-9.01565166136431,11.5046494570885,
9.91438359564765));
#114909=CARTESIAN_POINT('Ctrl Pts',(-9.07281033988419,11.5091665324305,
9.86517751281857));
#114910=CARTESIAN_POINT('Ctrl Pts',(-9.18574523258869,11.5175982913541,
9.7822048250766));
#114911=CARTESIAN_POINT('Ctrl Pts',(-9.24049110956728,11.521500790821,9.74732964846882));
#114912=CARTESIAN_POINT('Ctrl Pts',(-9.33231177819378,11.5276529684802,
9.69707590664529));
#114913=CARTESIAN_POINT('Ctrl Pts',(-9.36802000449302,11.5299581016063,
9.67938634490512));
#114914=CARTESIAN_POINT('Ctrl Pts',(-9.42038182505174,11.5332083615117,
9.65605772394456));
#114915=CARTESIAN_POINT('Ctrl Pts',(-9.43648259885476,11.5341908190591,
9.64922753758803));
#114916=CARTESIAN_POINT('Ctrl Pts',(-9.46557641200887,11.5359361131764,
9.63749628791977));
#114917=CARTESIAN_POINT('Ctrl Pts',(-9.47852390074208,11.5367023642279,
9.6324885253499));
#114918=CARTESIAN_POINT('Ctrl Pts',(-9.49840045758861,11.5378631279315,
9.62512412911922));
#114919=CARTESIAN_POINT('Ctrl Pts',(-9.50527895969779,11.5382620106919,
9.62263408773687));
#114920=CARTESIAN_POINT('Ctrl Pts',(-9.51730642667266,11.5389546655555,
9.61838182685496));
#114921=CARTESIAN_POINT('Ctrl Pts',(-9.52244704619107,11.5392491872347,
9.61659657384115));
#114922=CARTESIAN_POINT('Ctrl Pts',(-9.53405769521518,11.5399110166898,
9.6126368153354));
#114923=CARTESIAN_POINT('Ctrl Pts',(-9.54053324506639,11.5402777811637,
9.61047880879388));
#114924=CARTESIAN_POINT('Ctrl Pts',(-9.55804397950657,11.5412633547282,
9.60477907161012));
#114925=CARTESIAN_POINT('Ctrl Pts',(-9.5691066486116,11.5418793865342,9.60132294899019));
#114926=CARTESIAN_POINT('Ctrl Pts',(-9.6212384049464,11.5447527602802,9.58571353580589));
#114927=CARTESIAN_POINT('Ctrl Pts',(-9.66278887903261,11.5469562561097,
9.57523488124948));
#114928=CARTESIAN_POINT('Ctrl Pts',(-9.81567343986054,11.5548302545749,
9.54374318844541));
#114929=CARTESIAN_POINT('Ctrl Pts',(-9.92887569317197,11.5601862287449,
9.53384843766438));
#114930=CARTESIAN_POINT('Ctrl Pts',(-10.0943802268656,11.5683921616117,
9.53860965573711));
#114931=CARTESIAN_POINT('Ctrl Pts',(-10.1465529279434,11.5710401837991,
9.54291711010381));
#114932=CARTESIAN_POINT('Ctrl Pts',(-10.2060242161885,11.5742376277456,
9.55105354171047));
#114933=CARTESIAN_POINT('Ctrl Pts',(-10.213662366315,11.574651720035,9.55216015916214));
#114934=CARTESIAN_POINT('Ctrl Pts',(-10.2253150581689,11.5752891813678,
9.55394262059777));
#114935=CARTESIAN_POINT('Ctrl Pts',(-10.2293362415998,11.575510204658,9.55457490424558));
#114936=CARTESIAN_POINT('Ctrl Pts',(-10.2366894778973,11.5759163696421,
9.55576257076315));
#114937=CARTESIAN_POINT('Ctrl Pts',(-10.2400222918119,11.5761012198466,
9.55631272090408));
#114938=CARTESIAN_POINT('Ctrl Pts',(-10.2475048866822,11.5765179358098,
9.55757450529623));
#114939=CARTESIAN_POINT('Ctrl Pts',(-10.2516534879026,11.5767501476157,
9.55829250614975));
#114940=CARTESIAN_POINT('Ctrl Pts',(-10.2622826857882,11.5773480023673,
9.56017938365066));
#114941=CARTESIAN_POINT('Ctrl Pts',(-10.2687585278728,11.5777150155759,
9.56137410528359));
#114942=CARTESIAN_POINT('Ctrl Pts',(-10.3085748111801,11.5799877157225,
9.56899798864811));
#114943=CARTESIAN_POINT('Ctrl Pts',(-10.3416889610966,11.5819474996295,
9.5765417177384));
#114944=CARTESIAN_POINT('Ctrl Pts',(-10.3882638754592,11.5847757388921,
9.58887070363993));
#114945=CARTESIAN_POINT('Ctrl Pts',(-10.401965451617,11.5856167567329,9.59271236512463));
#114946=CARTESIAN_POINT('Ctrl Pts',(-10.4227529164756,11.586904490152,9.5988691206094));
#114947=CARTESIAN_POINT('Ctrl Pts',(-10.4298809735023,11.587348186084,9.6010396301536));
#114948=CARTESIAN_POINT('Ctrl Pts',(-10.5385004210813,11.5941392658103,
9.63502304186722));
#114949=CARTESIAN_POINT('Ctrl Pts',(-10.6362569208829,11.6006193198647,
9.6777572439905));
#114950=CARTESIAN_POINT('Ctrl Pts',(-10.769536815379,11.609548489495,9.75425442627853));
#114951=CARTESIAN_POINT('Ctrl Pts',(-10.8093919713453,11.6122374739243,
9.77977285531112));
#114952=CARTESIAN_POINT('Ctrl Pts',(-10.8572905478218,11.6154914056674,
9.81382267231472));
#114953=CARTESIAN_POINT('Ctrl Pts',(-10.8665582505874,11.6161221631041,
9.82057618096684));
#114954=CARTESIAN_POINT('Ctrl Pts',(-10.8811929403732,11.6171202774378,
9.83150632270964));
#114955=CARTESIAN_POINT('Ctrl Pts',(-10.8866117158469,11.6174903128553,
9.83561254750769));
#114956=CARTESIAN_POINT('Ctrl Pts',(-10.8967985845378,11.6181869017374,
9.84344426914289));
#114957=CARTESIAN_POINT('Ctrl Pts',(-10.9015725559512,11.6185137519738,
9.84716185538678));
#114958=CARTESIAN_POINT('Ctrl Pts',(-10.9123271126009,11.6192510448913,
9.85564430457269));
#114959=CARTESIAN_POINT('Ctrl Pts',(-10.91829371158,11.6196607884903,9.86042666742356));
#114960=CARTESIAN_POINT('Ctrl Pts',(-10.9335908280592,11.6207132775376,
9.87288580951611));
#114961=CARTESIAN_POINT('Ctrl Pts',(-10.9428643493104,11.6213532607155,
9.88063184658284));
#114962=CARTESIAN_POINT('Ctrl Pts',(-11.022830065191,11.6268918776169,9.94912496147416));
#114963=CARTESIAN_POINT('Ctrl Pts',(-11.0876675785056,11.631501820198,10.0163834043436));
#114964=CARTESIAN_POINT('Ctrl Pts',(-11.1953770397652,11.6399426892902,
10.1518922052661));
#114965=CARTESIAN_POINT('Ctrl Pts',(-11.2398750237063,11.6437824786447,
10.2183853352463));
#114966=CARTESIAN_POINT('Ctrl Pts',(-11.2949577015895,11.6495171981335,
10.3173354497481));
#114967=CARTESIAN_POINT('Ctrl Pts',(-11.3101887256513,11.6512424445273,
10.3470440138117));
#114968=CARTESIAN_POINT('Ctrl Pts',(-11.3273431482387,11.6533953435391,
10.3835256803938));
#114969=CARTESIAN_POINT('Ctrl Pts',(-11.3302517077373,11.653768429802,10.3898272292362));
#114970=CARTESIAN_POINT('Ctrl Pts',(-11.3347261776431,11.6543555201815,
10.3997054694105));
#114971=CARTESIAN_POINT('Ctrl Pts',(-11.3363228208845,11.6545677174694,
10.4032682257474));
#114972=CARTESIAN_POINT('Ctrl Pts',(-11.339280855516,11.6549660212945,10.4099402058511));
#114973=CARTESIAN_POINT('Ctrl Pts',(-11.3406457019655,11.6551519181444,
10.4130478114445));
#114974=CARTESIAN_POINT('Ctrl Pts',(-11.34373882174,11.6555780695504,10.4201575790975));
#114975=CARTESIAN_POINT('Ctrl Pts',(-11.345460031113,11.6558187375606,10.4241627332253));
#114976=CARTESIAN_POINT('Ctrl Pts',(-11.3499910108855,11.6564616516842,
10.4348372833239));
#114977=CARTESIAN_POINT('Ctrl Pts',(-11.3527692127832,11.6568656693083,
10.4415198495659));
#114978=CARTESIAN_POINT('Ctrl Pts',(-11.3743479126688,11.6600811132635,
10.4945301359121));
#114979=CARTESIAN_POINT('Ctrl Pts',(-11.3908111221768,11.663008888266,10.5417691952744));
#114980=CARTESIAN_POINT('Ctrl Pts',(-11.4131984756936,11.6677619763251,
10.6184310231344));
#114981=CARTESIAN_POINT('Ctrl Pts',(-11.4206929841681,11.669556070806,10.6473582611478));
#114982=CARTESIAN_POINT('Ctrl Pts',(-11.4432326409644,11.6756901368494,
10.7468024114972));
#114983=CARTESIAN_POINT('Ctrl Pts',(-11.453952661775,11.6800311954178,10.81819682255));
#114984=CARTESIAN_POINT('Ctrl Pts',(-11.4621041968615,11.6863840911647,
10.9264352976285));
#114985=CARTESIAN_POINT('Ctrl Pts',(-11.4634828265411,11.6884853094528,
10.9628682430287));
#114986=CARTESIAN_POINT('Ctrl Pts',(-11.4634998405537,11.690547335478,10.9993168461169));
#114987=CARTESIAN_POINT('Origin',(-10.,3.5,11.));
#114988=CARTESIAN_POINT('',(-11.4635,12.2603577583743,11.0000000000809));
#114989=CARTESIAN_POINT('',(-11.4634994198187,12.1893450843268,11.0013031462968));
#114990=CARTESIAN_POINT('',(-11.4635,3.5,11.));
#114991=CARTESIAN_POINT('Ctrl Pts',(-11.4635,12.2603577583743,11.0000000000809));
#114992=CARTESIAN_POINT('Ctrl Pts',(-11.4635000000051,12.2548059746649,
10.9073254685672));
#114993=CARTESIAN_POINT('Ctrl Pts',(-11.4546974320718,12.2493769166143,
10.8148476026833));
#114994=CARTESIAN_POINT('Ctrl Pts',(-11.4349328125928,12.2435558897438,
10.711998698516));
#114995=CARTESIAN_POINT('Ctrl Pts',(-11.4325173017963,12.2428918921651,
10.7002148795474));
#114996=CARTESIAN_POINT('Ctrl Pts',(-11.4283326869135,12.2418141969465,
10.6810075377871));
#114997=CARTESIAN_POINT('Ctrl Pts',(-11.4266503480007,12.2413977910046,
10.6735658671736));
#114998=CARTESIAN_POINT('Ctrl Pts',(-11.4235302230986,12.2406546022506,
10.6602493131919));
#114999=CARTESIAN_POINT('Ctrl Pts',(-11.4221140747212,12.240327143294,10.6543695828532));
#115000=CARTESIAN_POINT('Ctrl Pts',(-11.4190266597989,12.239633582581,10.6418911880217));
#115001=CARTESIAN_POINT('Ctrl Pts',(-11.4173457178811,12.2392677969016,
10.6352950499755));
#115002=CARTESIAN_POINT('Ctrl Pts',(-11.4126992279587,12.2382874969709,
10.6175793218541));
#115003=CARTESIAN_POINT('Ctrl Pts',(-11.4096484108479,12.2376757086318,
10.6064824634673));
#115004=CARTESIAN_POINT('Ctrl Pts',(-11.3932251538891,12.2345382837069,
10.5493889029438));
#115005=CARTESIAN_POINT('Ctrl Pts',(-11.3777306688271,12.2320815545049,
10.5040307602516));
#115006=CARTESIAN_POINT('Ctrl Pts',(-11.3195491799641,12.224170028088,10.3576280633855));
#115007=CARTESIAN_POINT('Ctrl Pts',(-11.2677430341436,12.2189814486879,
10.2606231323323));
#115008=CARTESIAN_POINT('Ctrl Pts',(-11.1769872196089,12.2110382755514,
10.128748398086));
#115009=CARTESIAN_POINT('Ctrl Pts',(-11.1462536186344,12.2084814995651,
10.0886932687176));
#115010=CARTESIAN_POINT('Ctrl Pts',(-11.1088113422629,12.2054110500189,
10.0447920471613));
#115011=CARTESIAN_POINT('Ctrl Pts',(-11.1040652484266,12.2050225902678,
10.039310274393));
#115012=CARTESIAN_POINT('Ctrl Pts',(-11.0963984611413,12.2043958392435,
10.0305869300754));
#115013=CARTESIAN_POINT('Ctrl Pts',(-11.0935036073444,12.204159359192,10.0273226920158));
#115014=CARTESIAN_POINT('Ctrl Pts',(-11.0883310000833,12.2037370111398,
10.0215423345221));
#115015=CARTESIAN_POINT('Ctrl Pts',(-11.0860590368975,12.2035515679007,
10.0190211332302));
#115016=CARTESIAN_POINT('Ctrl Pts',(-11.0811572689418,12.2031515810018,
10.0136195350622));
#115017=CARTESIAN_POINT('Ctrl Pts',(-11.0785247560787,12.2029368416973,
10.010741787198));
#115018=CARTESIAN_POINT('Ctrl Pts',(-11.0711861694832,12.2023385143601,
10.0027836755638));
#115019=CARTESIAN_POINT('Ctrl Pts',(-11.0664555535178,12.2019531539081,
9.9977262070975));
#115020=CARTESIAN_POINT('Ctrl Pts',(-11.038882781628,12.1997099873192,9.96866456397212));
#115021=CARTESIAN_POINT('Ctrl Pts',(-11.0152680514787,12.1978005197452,
9.9454097122866));
#115022=CARTESIAN_POINT('Ctrl Pts',(-10.932943887834,12.1912433901656,9.86966947375594));
#115023=CARTESIAN_POINT('Ctrl Pts',(-10.8707955870396,12.1864618595326,
9.82112513581298));
#115024=CARTESIAN_POINT('Ctrl Pts',(-10.7259178908006,12.1760619507911,
9.72569494404273));
#115025=CARTESIAN_POINT('Ctrl Pts',(-10.6419046781459,12.1705043963497,
9.68137431195839));
#115026=CARTESIAN_POINT('Ctrl Pts',(-10.5430705873411,12.164569381805,9.64093754359289));
#115027=CARTESIAN_POINT('Ctrl Pts',(-10.5319017711133,12.1639065613599,
9.63652761628501));
#115028=CARTESIAN_POINT('Ctrl Pts',(-10.5135558057522,12.1628303988043,
9.62954358365076));
#115029=CARTESIAN_POINT('Ctrl Pts',(-10.5064107323465,12.1624143607992,
9.62688728504845));
#115030=CARTESIAN_POINT('Ctrl Pts',(-10.4935611252204,12.161671597705,9.62222417336057));
#115031=CARTESIAN_POINT('Ctrl Pts',(-10.4878643279251,12.1613441992047,
9.62019667638689));
#115032=CARTESIAN_POINT('Ctrl Pts',(-10.4757251913483,12.1606505269177,
9.6159609220166));
#115033=CARTESIAN_POINT('Ctrl Pts',(-10.4692796600842,12.1602845710383,
9.61376220299878));
#115034=CARTESIAN_POINT('Ctrl Pts',(-10.4518860353491,12.1593032379807,
9.60796405518009));
#115035=CARTESIAN_POINT('Ctrl Pts',(-10.4409102653362,12.1586905974093,
9.60444877965924));
#115036=CARTESIAN_POINT('Ctrl Pts',(-10.383876467884,12.1555397068102,9.58692226507335));
#115037=CARTESIAN_POINT('Ctrl Pts',(-10.3371869458659,12.1530711108834,
9.57505951298429));
#115038=CARTESIAN_POINT('Ctrl Pts',(-10.181226427311,12.145082463203,9.54353058818045));
#115039=CARTESIAN_POINT('Ctrl Pts',(-10.070317629146,12.1398361262459,9.5339849224058));
#115040=CARTESIAN_POINT('Ctrl Pts',(-9.93941505871758,12.1333293657368,
9.53761791554359));
#115041=CARTESIAN_POINT('Ctrl Pts',(-9.91944561469846,12.1323271295369,
9.53858190722312));
#115042=CARTESIAN_POINT('Ctrl Pts',(-9.8690636967917,12.1297611654952,9.54204977377601));
#115043=CARTESIAN_POINT('Ctrl Pts',(-9.83869956372696,12.1281802200906,
9.54509618940577));
#115044=CARTESIAN_POINT('Ctrl Pts',(-9.80151793989404,12.1261782967226,
9.55000479907706));
#115045=CARTESIAN_POINT('Ctrl Pts',(-9.79458771849976,12.1258023228816,
9.55097032410739));
#115046=CARTESIAN_POINT('Ctrl Pts',(-9.78374890645254,12.1252094877737,
9.55255971498088));
#115047=CARTESIAN_POINT('Ctrl Pts',(-9.77983537985621,12.1249944501264,
9.55314981651763));
#115048=CARTESIAN_POINT('Ctrl Pts',(-9.77257887999176,12.1245938178299,
9.55427411140282));
#115049=CARTESIAN_POINT('Ctrl Pts',(-9.76923532733898,12.1244084602799,
9.55480403545743));
#115050=CARTESIAN_POINT('Ctrl Pts',(-9.76159997108689,12.1239834531014,
9.55604134547359));
#115051=CARTESIAN_POINT('Ctrl Pts',(-9.75730947576301,12.1237433919598,
9.55675626513817));
#115052=CARTESIAN_POINT('Ctrl Pts',(-9.74404741984771,12.1229976556589,
9.55902691344309));
#115053=CARTESIAN_POINT('Ctrl Pts',(-9.73508731533925,12.1224885767231,
9.56064722167714));
#115054=CARTESIAN_POINT('Ctrl Pts',(-9.71418407045161,12.1212895864138,
9.56462906759807));
#115055=CARTESIAN_POINT('Ctrl Pts',(-9.70225423868412,12.1205966079204,
9.56705621084313));
#115056=CARTESIAN_POINT('Ctrl Pts',(-9.66033000443401,12.1181338657539,
9.57613189438323));
#115057=CARTESIAN_POINT('Ctrl Pts',(-9.63051722765552,12.1163329555175,
9.58357549943435));
#115058=CARTESIAN_POINT('Ctrl Pts',(-9.53674198267762,12.1105532686362,
9.61015116941723));
#115059=CARTESIAN_POINT('Ctrl Pts',(-9.47384269054574,12.1065077713021,
9.63272309724021));
#115060=CARTESIAN_POINT('Ctrl Pts',(-9.32735953324229,12.0969250660342,
9.69690027953282));
#115061=CARTESIAN_POINT('Ctrl Pts',(-9.24576967904837,12.091464213834,9.74236109430823));
#115062=CARTESIAN_POINT('Ctrl Pts',(-9.15908229161052,12.0856101219716,
9.8021535144291));
#115063=CARTESIAN_POINT('Ctrl Pts',(-9.1492027114298,12.0849417668494,9.80915039515757));
#115064=CARTESIAN_POINT('Ctrl Pts',(-9.13322143189497,12.0838584770434,
9.82076901274582));
#115065=CARTESIAN_POINT('Ctrl Pts',(-9.12706730216103,12.0834407863807,
9.82531735538098));
#115066=CARTESIAN_POINT('Ctrl Pts',(-9.1161122930673,12.0826962046614,9.83354752794579));
#115067=CARTESIAN_POINT('Ctrl Pts',(-9.11129806775944,12.0823686270161,
9.83721122933819));
#115068=CARTESIAN_POINT('Ctrl Pts',(-9.1011276182116,12.0816757453845,9.84505116206975));
#115069=CARTESIAN_POINT('Ctrl Pts',(-9.09577745751848,12.0813107502746,
9.84923504886328));
#115070=CARTESIAN_POINT('Ctrl Pts',(-9.08149370477378,12.0803348016928,
9.86056622723117));
#115071=CARTESIAN_POINT('Ctrl Pts',(-9.07261437602079,12.0797265321294,
9.86778135893339));
#115072=CARTESIAN_POINT('Ctrl Pts',(-9.02772556506568,12.0766419107304,
9.90513933710712));
#115073=CARTESIAN_POINT('Ctrl Pts',(-8.99309559981289,12.074231625155,9.93690003354028));
#115074=CARTESIAN_POINT('Ctrl Pts',(-8.88640550605975,12.0666095479148,
10.0446493225219));
#115075=CARTESIAN_POINT('Ctrl Pts',(-8.82095494826308,12.0616373535182,
10.1267074767315));
#115076=CARTESIAN_POINT('Ctrl Pts',(-8.73459889633989,12.0536880857346,
10.2625947504823));
#115077=CARTESIAN_POINT('Ctrl Pts',(-8.7071545206653,12.0508506118036,10.3118461270923));
#115078=CARTESIAN_POINT('Ctrl Pts',(-8.67911761104667,12.0474262492691,
10.3697884399054));
#115079=CARTESIAN_POINT('Ctrl Pts',(-8.67567533345731,12.0469953178371,
10.3770545226679));
#115080=CARTESIAN_POINT('Ctrl Pts',(-8.67053080171456,12.046334498301,10.3881491584753));
#115081=CARTESIAN_POINT('Ctrl Pts',(-8.66878477456983,12.0461071697904,
10.391957382938));
#115082=CARTESIAN_POINT('Ctrl Pts',(-8.66566112536145,12.0456948283028,
10.3988482570086));
#115083=CARTESIAN_POINT('Ctrl Pts',(-8.66427779567627,12.0455101631393,
10.401928229283));
#115084=CARTESIAN_POINT('Ctrl Pts',(-8.6612435286354,12.0451005162417,10.4087470386492));
#115085=CARTESIAN_POINT('Ctrl Pts',(-8.65959760765169,12.0448752466374,
10.4124879748611));
#115086=CARTESIAN_POINT('Ctrl Pts',(-8.65485628996998,12.0442174497102,
10.423387927128));
#115087=CARTESIAN_POINT('Ctrl Pts',(-8.65180247527174,12.0437825520738,
10.4305647428377));
#115088=CARTESIAN_POINT('Ctrl Pts',(-8.62749121198827,12.0402296517615,
10.4889909422773));
#115089=CARTESIAN_POINT('Ctrl Pts',(-8.60910842535902,12.0369679878286,
10.5413824395642));
#115090=CARTESIAN_POINT('Ctrl Pts',(-8.55399259994106,12.0250888368134,
10.7326087439801));
#115091=CARTESIAN_POINT('Ctrl Pts',(-8.53473776357802,12.0163479269612,
10.8756691694954));
#115092=CARTESIAN_POINT('Ctrl Pts',(-8.53685348325511,12.0073464281386,
11.0364960509889));
#115093=CARTESIAN_POINT('Ctrl Pts',(-8.53738516658651,12.0063904543788,
11.0537361687143));
#115094=CARTESIAN_POINT('Ctrl Pts',(-8.53860391863576,12.0050109499559,
11.0788413030466));
#115095=CARTESIAN_POINT('Ctrl Pts',(-8.53905004193811,12.0045800409144,
11.0867160949721));
#115096=CARTESIAN_POINT('Ctrl Pts',(-8.53995381605657,12.0038195608795,
11.1006705281967));
#115097=CARTESIAN_POINT('Ctrl Pts',(-8.54038583399948,12.0034892061035,
11.1067515923067));
#115098=CARTESIAN_POINT('Ctrl Pts',(-8.54136469399968,12.0028036323156,
11.1194104580995));
#115099=CARTESIAN_POINT('Ctrl Pts',(-8.54191806356541,12.0024486230723,
11.1259876263951));
#115100=CARTESIAN_POINT('Ctrl Pts',(-8.54347304899,12.0015288021931,11.1430844211263));
#115101=CARTESIAN_POINT('Ctrl Pts',(-8.54454414567865,12.0009661493641,
11.1535974430187));
#115102=CARTESIAN_POINT('Ctrl Pts',(-8.54982498712061,11.9984736826175,
11.2003973328238));
#115103=CARTESIAN_POINT('Ctrl Pts',(-8.55527874288746,11.9965825318892,
11.2365320918327));
#115104=CARTESIAN_POINT('Ctrl Pts',(-8.57432477963348,11.9913799573634,
11.3370606429539));
#115105=CARTESIAN_POINT('Ctrl Pts',(-8.59091464485725,11.9881528734285,
11.4007978902761));
#115106=CARTESIAN_POINT('Ctrl Pts',(-8.64423644301081,11.9799453178317,
11.5606075965663));
#115107=CARTESIAN_POINT('Ctrl Pts',(-8.68689202115462,11.9750266073954,
11.6543071253193));
#115108=CARTESIAN_POINT('Ctrl Pts',(-8.74456251159488,11.9690328458795,
11.7522163493403));
#115109=CARTESIAN_POINT('Ctrl Pts',(-8.75023915335709,11.9684482528034,
11.7616104881095));
#115110=CARTESIAN_POINT('Ctrl Pts',(-8.758314866178,11.967622719986,11.7746413650166));
#115111=CARTESIAN_POINT('Ctrl Pts',(-8.76062546216422,11.9673871987733,
11.7783328143804));
#115112=CARTESIAN_POINT('Ctrl Pts',(-8.76464702000663,11.9669783423139,
11.7846944129708));
#115113=CARTESIAN_POINT('Ctrl Pts',(-8.76635026159977,11.966805504622,11.7873694364642));
#115114=CARTESIAN_POINT('Ctrl Pts',(-8.76996041578092,11.9664397960954,
11.7929988879357));
#115115=CARTESIAN_POINT('Ctrl Pts',(-8.77186929701796,11.966246792018,11.7959520027421));
#115116=CARTESIAN_POINT('Ctrl Pts',(-8.77661225173234,11.9657681937331,
11.8032318596183));
#115117=CARTESIAN_POINT('Ctrl Pts',(-8.77945864011871,11.9654818043323,
11.8075504876417));
#115118=CARTESIAN_POINT('Ctrl Pts',(-8.79012115710668,11.9644123341662,
11.8235428365423));
#115119=CARTESIAN_POINT('Ctrl Pts',(-8.79808211699375,11.9636204154628,
11.8351185490441));
#115120=CARTESIAN_POINT('Ctrl Pts',(-8.85658456097778,11.95785762137,11.9176151265116));
#115121=CARTESIAN_POINT('Ctrl Pts',(-8.9131975903255,11.952588506484,11.9840095898735));
#115122=CARTESIAN_POINT('Ctrl Pts',(-9.04738992528469,11.9412851037012,
12.1155893772728));
#115123=CARTESIAN_POINT('Ctrl Pts',(-9.12652587627735,11.9353026248179,
12.1785815153733));
#115124=CARTESIAN_POINT('Ctrl Pts',(-9.22712181784205,11.9286061533182,
12.2429136713676));
#115125=CARTESIAN_POINT('Ctrl Pts',(-9.24290884947954,11.9275783753904,
12.2525925565333));
#115126=CARTESIAN_POINT('Ctrl Pts',(-9.26524176343757,11.9261558976793,
12.2657081360948));
#115127=CARTESIAN_POINT('Ctrl Pts',(-9.2716359759257,11.9257521532284,12.2693985202424));
#115128=CARTESIAN_POINT('Ctrl Pts',(-9.28341395702334,11.9250148360302,
12.2760778212882));
#115129=CARTESIAN_POINT('Ctrl Pts',(-9.28878916259913,11.924680746424,12.2790814318645));
#115130=CARTESIAN_POINT('Ctrl Pts',(-9.29974159867636,11.9240048179416,
12.2851111551536));
#115131=CARTESIAN_POINT('Ctrl Pts',(-9.30531987602035,11.9236630604178,
12.2881351003707));
#115132=CARTESIAN_POINT('Ctrl Pts',(-9.31919064809662,11.9228193499423,
12.2955380400237));
#115133=CARTESIAN_POINT('Ctrl Pts',(-9.32750596275297,11.9223189117851,
12.2998738254677));
#115134=CARTESIAN_POINT('Ctrl Pts',(-9.35915766562077,11.920433661042,12.3159926872941));
#115135=CARTESIAN_POINT('Ctrl Pts',(-9.38276733800983,11.9190676086697,
12.3272300482196));
#115136=CARTESIAN_POINT('Ctrl Pts',(-9.44331449664166,11.9156543676327,
12.3540829978543));
#115137=CARTESIAN_POINT('Ctrl Pts',(-9.4806165080502,11.9136344385394,12.3688245319763));
#115138=CARTESIAN_POINT('Ctrl Pts',(-9.57945121937701,11.9084383659812,
12.4032604703767));
#115139=CARTESIAN_POINT('Ctrl Pts',(-9.64176408505081,11.9053171411273,
12.4204465781561));
#115140=CARTESIAN_POINT('Ctrl Pts',(-9.7786354195135,11.8985047848275,12.4486133100641));
#115141=CARTESIAN_POINT('Ctrl Pts',(-9.85331323675533,11.8948139309531,
12.4580683829241));
#115142=CARTESIAN_POINT('Ctrl Pts',(-9.94039336046036,11.8902271089276,
12.4623351281179));
#115143=CARTESIAN_POINT('Ctrl Pts',(-9.95241568093956,11.889587541225,12.4627756809019));
#115144=CARTESIAN_POINT('Ctrl Pts',(-9.96944876114729,11.8886707976507,
12.4631896519195));
#115145=CARTESIAN_POINT('Ctrl Pts',(-9.97445636122614,11.8883999833124,
12.4632856374339));
#115146=CARTESIAN_POINT('Ctrl Pts',(-9.98291319048334,11.8879402948549,
12.4634043146915));
#115147=CARTESIAN_POINT('Ctrl Pts',(-9.98636223924958,11.8877521577671,
12.4634405210253));
#115148=CARTESIAN_POINT('Ctrl Pts',(-9.99344872588289,11.8873642028206,
12.4634898570841));
#115149=CARTESIAN_POINT('Ctrl Pts',(-9.99708612032296,11.8871643150776,
12.4635016192993));
#115150=CARTESIAN_POINT('Ctrl Pts',(-10.0064588771287,11.8866473675899,
12.4634969858861));
#115151=CARTESIAN_POINT('Ctrl Pts',(-10.0121941120456,11.8863292298372,
12.4634604354747));
#115152=CARTESIAN_POINT('Ctrl Pts',(-10.0364267107871,11.8849777835674,
12.4631635471214));
#115153=CARTESIAN_POINT('Ctrl Pts',(-10.0549177208273,11.883928714258,12.4625862196702));
#115154=CARTESIAN_POINT('Ctrl Pts',(-10.1050100814931,11.8810472718436,
12.4600710127188));
#115155=CARTESIAN_POINT('Ctrl Pts',(-10.1365667759029,11.8791894598557,
12.4574579846259));
#115156=CARTESIAN_POINT('Ctrl Pts',(-10.2655120137174,11.8714846040999,
12.442556350046));
#115157=CARTESIAN_POINT('Ctrl Pts',(-10.3616331145905,11.865494497724,12.4215093552516));
#115158=CARTESIAN_POINT('Ctrl Pts',(-10.5133055760395,11.8560994955007,
12.3719045139553));
#115159=CARTESIAN_POINT('Ctrl Pts',(-10.5704274783732,11.8525701630846,
12.3491547706635));
#115160=CARTESIAN_POINT('Ctrl Pts',(-10.6364068692296,11.8485172306536,
12.3179348270918));
#115161=CARTESIAN_POINT('Ctrl Pts',(-10.64679846414,11.84787949189,12.3128662038372));
#115162=CARTESIAN_POINT('Ctrl Pts',(-10.6638191353195,11.8468357002052,
12.3043130237419));
#115163=CARTESIAN_POINT('Ctrl Pts',(-10.6704833373149,11.8464272162831,
12.3008998445705));
#115164=CARTESIAN_POINT('Ctrl Pts',(-10.682349601798,11.8457001434379,12.2947069372998));
#115165=CARTESIAN_POINT('Ctrl Pts',(-10.6875615727535,11.8453808890408,
12.2919466388532));
#115166=CARTESIAN_POINT('Ctrl Pts',(-10.6986504977495,11.8447017924644,
12.2859877521747));
#115167=CARTESIAN_POINT('Ctrl Pts',(-10.704522503127,11.8443422730469,12.2827802077367));
#115168=CARTESIAN_POINT('Ctrl Pts',(-10.7165546524216,11.8436056795521,
12.2761001846483));
#115169=CARTESIAN_POINT('Ctrl Pts',(-10.7227120459811,11.8432287788758,
12.272623098998));
#115170=CARTESIAN_POINT('Ctrl Pts',(-10.7380589061946,11.8422893440294,
12.2638094081906));
#115171=CARTESIAN_POINT('Ctrl Pts',(-10.7472159814269,11.8417287759056,
12.2584170429673));
#115172=CARTESIAN_POINT('Ctrl Pts',(-10.7730028698787,11.84014939064,12.242851090319));
#115173=CARTESIAN_POINT('Ctrl Pts',(-10.7894895581006,11.8391387027473,
12.2324441370172));
#115174=CARTESIAN_POINT('Ctrl Pts',(-10.8448405796337,11.8357359084201,
12.1959380648638));
#115175=CARTESIAN_POINT('Ctrl Pts',(-10.8826599310488,11.8333954347197,
12.1683044681025));
#115176=CARTESIAN_POINT('Ctrl Pts',(-10.9755601415778,11.8275113879887,
12.0933343409568));
#115177=CARTESIAN_POINT('Ctrl Pts',(-11.0285603759722,11.8240255258427,
12.0436287391181));
#115178=CARTESIAN_POINT('Ctrl Pts',(-11.1199840400863,11.8173834963673,
11.9441302713563));
#115179=CARTESIAN_POINT('Ctrl Pts',(-11.1593112561158,11.8142528259374,
11.8954004525021));
#115180=CARTESIAN_POINT('Ctrl Pts',(-11.2000847119548,11.8104939784547,
11.8376723589042));
#115181=CARTESIAN_POINT('Ctrl Pts',(-11.2047177453511,11.8100584889564,
11.8309954541469));
#115182=CARTESIAN_POINT('Ctrl Pts',(-11.2116649693189,11.8093920516097,
11.8208032412061));
#115183=CARTESIAN_POINT('Ctrl Pts',(-11.2140200761227,11.8091637293957,
11.8173158584814));
#115184=CARTESIAN_POINT('Ctrl Pts',(-11.2182379568744,11.8087503699657,
11.811011673547));
#115185=CARTESIAN_POINT('Ctrl Pts',(-11.2201060554532,11.8085656892533,
11.8081985320733));
#115186=CARTESIAN_POINT('Ctrl Pts',(-11.2242043130961,11.8081569661181,
11.8019804340152));
#115187=CARTESIAN_POINT('Ctrl Pts',(-11.2264299852938,11.8079326439324,
11.7985726686392));
#115188=CARTESIAN_POINT('Ctrl Pts',(-11.2328354766852,11.8072802874163,
11.7886751708793));
#115189=CARTESIAN_POINT('Ctrl Pts',(-11.2369781376446,11.8068499407652,
11.7821616964879));
#115190=CARTESIAN_POINT('Ctrl Pts',(-11.2688508272659,11.8034742444762,
11.7311619600476));
#115191=CARTESIAN_POINT('Ctrl Pts',(-11.2942216581094,11.8004004055587,
11.6852514067206));
#115192=CARTESIAN_POINT('Ctrl Pts',(-11.369044800095,11.7901749755661,11.5308085307833));
#115193=CARTESIAN_POINT('Ctrl Pts',(-11.407723773277,11.7828982666145,11.4175664497123));
#115194=CARTESIAN_POINT('Ctrl Pts',(-11.4399883204299,11.7738639909726,
11.2639840358877));
#115195=CARTESIAN_POINT('Ctrl Pts',(-11.4463117504704,11.7717332821447,
11.2267964202192));
#115196=CARTESIAN_POINT('Ctrl Pts',(-11.4526286991968,11.7690328257708,
11.1783965519156));
#115197=CARTESIAN_POINT('Ctrl Pts',(-11.4539400364801,11.7684225837634,
11.1673733768493));
#115198=CARTESIAN_POINT('Ctrl Pts',(-11.4558434087634,11.7674493197095,
11.1496574067769));
#115199=CARTESIAN_POINT('Ctrl Pts',(-11.4565149777432,11.7670838442857,
11.1429737456393));
#115200=CARTESIAN_POINT('Ctrl Pts',(-11.4576884218097,11.7664009218756,
11.1304274997349));
#115201=CARTESIAN_POINT('Ctrl Pts',(-11.4582010022206,11.7660831495338,
11.1245660719387));
#115202=CARTESIAN_POINT('Ctrl Pts',(-11.459153545937,11.7654510448967,11.1128606344265));
#115203=CARTESIAN_POINT('Ctrl Pts',(-11.4595937819835,11.7651367098116,
11.1070167574441));
#115204=CARTESIAN_POINT('Ctrl Pts',(-11.4605169322783,11.7644228827377,
11.0936946861254));
#115205=CARTESIAN_POINT('Ctrl Pts',(-11.4609775380424,11.7640240816738,
11.0862150786803));
#115206=CARTESIAN_POINT('Ctrl Pts',(-11.4628044140944,11.7622246781202,
11.0523056692109));
#115207=CARTESIAN_POINT('Ctrl Pts',(-11.4635111105567,11.7608442923582,
11.025844731747));
#115208=CARTESIAN_POINT('Ctrl Pts',(-11.4634998679599,11.7594829657366,
10.9993783236864));
#115209=CARTESIAN_POINT('Ctrl Pts',(-11.4634998405537,11.690547335478,10.9993168461169));
#115210=CARTESIAN_POINT('Ctrl Pts',(-11.4635110117752,11.6919012400444,
11.023248614949));
#115211=CARTESIAN_POINT('Ctrl Pts',(-11.4629351707176,11.693237851355,11.0471779657481));
#115212=CARTESIAN_POINT('Ctrl Pts',(-11.4613190077038,11.6950711538873,
11.0804130227707));
#115213=CARTESIAN_POINT('Ctrl Pts',(-11.4607760139058,11.6955830245042,
11.0897381711136));
#115214=CARTESIAN_POINT('Ctrl Pts',(-11.4597576234224,11.6964030878732,
11.1047495986055));
#115215=CARTESIAN_POINT('Ctrl Pts',(-11.4593381917171,11.6967130012465,
11.1104393092238));
#115216=CARTESIAN_POINT('Ctrl Pts',(-11.4583977047227,11.6973547198214,
11.1222545545916));
#115217=CARTESIAN_POINT('Ctrl Pts',(-11.457871301458,11.6976863529116,11.1283795592229));
#115218=CARTESIAN_POINT('Ctrl Pts',(-11.4565399129737,11.6984650497468,
11.1428050205016));
#115219=CARTESIAN_POINT('Ctrl Pts',(-11.4557025398489,11.6989111016444,
11.151102320701));
#115220=CARTESIAN_POINT('Ctrl Pts',(-11.4526923246627,11.7003823114869,
11.1785769763488));
#115221=CARTESIAN_POINT('Ctrl Pts',(-11.4502110205741,11.70139792342,11.1977189114103));
#115222=CARTESIAN_POINT('Ctrl Pts',(-11.4434001245814,11.7037915102701,
11.243186872661));
#115223=CARTESIAN_POINT('Ctrl Pts',(-11.4387278955424,11.7051591633226,
11.2694548588893));
#115224=CARTESIAN_POINT('Ctrl Pts',(-11.4176628825599,11.7104392807719,
11.3716037768903));
#115225=CARTESIAN_POINT('Ctrl Pts',(-11.3959617091636,11.7142074138894,
11.4462613099121));
#115226=CARTESIAN_POINT('Ctrl Pts',(-11.3382945830485,11.7221239245019,
11.5983565033105));
#115227=CARTESIAN_POINT('Ctrl Pts',(-11.3012792295772,11.7262611852359,
11.6750792636379));
#115228=CARTESIAN_POINT('Ctrl Pts',(-11.2517321146167,11.7313617765336,
11.7583803635228));
#115229=CARTESIAN_POINT('Ctrl Pts',(-11.2455199461069,11.7319949932516,
11.7685402452513));
#115230=CARTESIAN_POINT('Ctrl Pts',(-11.2367921393787,11.7328777297301,
11.782430621376));
#115231=CARTESIAN_POINT('Ctrl Pts',(-11.2343820864251,11.7331207834384,
11.7862272807159));
#115232=CARTESIAN_POINT('Ctrl Pts',(-11.2302224556582,11.7335391966889,
11.7927138550937));
#115233=CARTESIAN_POINT('Ctrl Pts',(-11.2284814442481,11.7337140031849,
11.795409257675));
#115234=CARTESIAN_POINT('Ctrl Pts',(-11.2248326494808,11.7340797439245,
11.8010177003377));
#115235=CARTESIAN_POINT('Ctrl Pts',(-11.2229233244739,11.7342707848579,
11.803929671737));
#115236=CARTESIAN_POINT('Ctrl Pts',(-11.2182492911315,11.7347375739999,
11.8110030058457));
#115237=CARTESIAN_POINT('Ctrl Pts',(-11.2154736412383,11.7350140333436,
11.8151570626571));
#115238=CARTESIAN_POINT('Ctrl Pts',(-11.2054821914291,11.7360063349114,
11.8299458426191));
#115239=CARTESIAN_POINT('Ctrl Pts',(-11.1981478517334,11.736729478913,11.8404993265583));
#115240=CARTESIAN_POINT('Ctrl Pts',(-11.1795644907716,11.7385461431458,
11.866501607227));
#115241=CARTESIAN_POINT('Ctrl Pts',(-11.1681502456499,11.739648345848,11.8818289889599));
#115242=CARTESIAN_POINT('Ctrl Pts',(-11.1178625270516,11.7444324664026,
11.9466666622002));
#115243=CARTESIAN_POINT('Ctrl Pts',(-11.0761184031524,11.7482238468011,
11.9938625965223));
#115244=CARTESIAN_POINT('Ctrl Pts',(-10.9549528328743,11.7585020099576,
12.1142399248257));
#115245=CARTESIAN_POINT('Ctrl Pts',(-10.8702564604242,11.7649248297365,
12.1815778704343));
#115246=CARTESIAN_POINT('Ctrl Pts',(-10.7634618307599,11.7719962085118,
12.2487159501406));
#115247=CARTESIAN_POINT('Ctrl Pts',(-10.7478263365112,11.7730092245914,
12.2581420045889));
#115248=CARTESIAN_POINT('Ctrl Pts',(-10.7250312781815,11.7744548611267,
12.2713091671595));
#115249=CARTESIAN_POINT('Ctrl Pts',(-10.7180111394805,11.7748958889714,
12.2752871676856));
#115250=CARTESIAN_POINT('Ctrl Pts',(-10.7056034514141,11.7756681548096,
12.2821831194939));
#115251=CARTESIAN_POINT('Ctrl Pts',(-10.7002298511229,11.7760002562438,
12.285125651342));
#115252=CARTESIAN_POINT('Ctrl Pts',(-10.6890941349368,11.7766836814334,
12.2911328802317));
#115253=CARTESIAN_POINT('Ctrl Pts',(-10.6833296715704,11.7770348378461,
12.2941929543368));
#115254=CARTESIAN_POINT('Ctrl Pts',(-10.6684843208565,11.7779325796945,
12.3019467929988));
#115255=CARTESIAN_POINT('Ctrl Pts',(-10.6593742949861,11.7784772017356,
12.3065842051738));
#115256=CARTESIAN_POINT('Ctrl Pts',(-10.6205278844389,11.7807738206129,
12.3258489980042));
#115257=CARTESIAN_POINT('Ctrl Pts',(-10.5903467332848,11.7824944482346,
12.3395601405463));
#115258=CARTESIAN_POINT('Ctrl Pts',(-10.5075283757096,11.7870709311126,
12.3738407552375));
#115259=CARTESIAN_POINT('Ctrl Pts',(-10.4541228284109,11.7898669502416,
12.3924067467507));
#115260=CARTESIAN_POINT('Ctrl Pts',(-10.3532740435257,11.7949954785566,
12.4210441280469));
#115261=CARTESIAN_POINT('Ctrl Pts',(-10.3061475759296,11.7973340620579,
12.4319366592589));
#115262=CARTESIAN_POINT('Ctrl Pts',(-10.1875682578389,11.8032257602593,
12.4532219024205));
#115263=CARTESIAN_POINT('Ctrl Pts',(-10.1157303474011,11.8068007674967,
12.4606984117221));
#115264=CARTESIAN_POINT('Ctrl Pts',(-10.0354923283458,11.8110697324395,
12.4630922897331));
#115265=CARTESIAN_POINT('Ctrl Pts',(-10.0273392723034,11.8115066978225,
12.4632673411975));
#115266=CARTESIAN_POINT('Ctrl Pts',(-10.0149708413075,11.8121749900491,
12.4634294957998));
#115267=CARTESIAN_POINT('Ctrl Pts',(-10.0107561514835,11.8124036700102,
12.4634665420066));
#115268=CARTESIAN_POINT('Ctrl Pts',(-10.0031632908043,11.8128174483842,
12.4635004801965));
#115269=CARTESIAN_POINT('Ctrl Pts',(-9.99978523063362,11.8130021875297,
12.4635038829548));
#115270=CARTESIAN_POINT('Ctrl Pts',(-9.99234057179896,11.8134107649638,
12.4634856064393));
#115271=CARTESIAN_POINT('Ctrl Pts',(-9.98827411070654,11.8136348808513,
12.4634586737577));
#115272=CARTESIAN_POINT('Ctrl Pts',(-9.97650959394823,11.8142858787328,
12.4633317194362));
#115273=CARTESIAN_POINT('Ctrl Pts',(-9.96881226615034,11.8147150579741,
12.4631879032821));
#115274=CARTESIAN_POINT('Ctrl Pts',(-9.90949647449959,11.8180454556237,
12.4616113990794));
#115275=CARTESIAN_POINT('Ctrl Pts',(-9.8579897214329,11.8210714072089,12.4575084372319));
#115276=CARTESIAN_POINT('Ctrl Pts',(-9.69745368511258,11.8307165385426,
12.4361300436332));
#115277=CARTESIAN_POINT('Ctrl Pts',(-9.59007704654421,11.8374498201066,
12.4092449579377));
#115278=CARTESIAN_POINT('Ctrl Pts',(-9.44368260530488,11.8465281658592,
12.3544213684133));
#115279=CARTESIAN_POINT('Ctrl Pts',(-9.40140523225442,11.8491423945864,
12.3362751351717));
#115280=CARTESIAN_POINT('Ctrl Pts',(-9.34952205362358,11.852339245398,12.3110483235708));
#115281=CARTESIAN_POINT('Ctrl Pts',(-9.33905667484916,11.8529835608785,
12.3058036596419));
#115282=CARTESIAN_POINT('Ctrl Pts',(-9.32250811324443,11.8540017730185,
12.2972605171938));
#115283=CARTESIAN_POINT('Ctrl Pts',(-9.31638360595431,11.85437846987,12.2940435596092));
#115284=CARTESIAN_POINT('Ctrl Pts',(-9.30495923376991,11.8550809579258,
12.2879390534127));
#115285=CARTESIAN_POINT('Ctrl Pts',(-9.29965399339151,11.8554071034629,
12.2850619224599));
#115286=CARTESIAN_POINT('Ctrl Pts',(-9.2878241277172,11.8561342560457,12.2785513467937));
#115287=CARTESIAN_POINT('Ctrl Pts',(-9.2813091850471,11.8565346434405,12.2749005979892));
#115288=CARTESIAN_POINT('Ctrl Pts',(-9.26211710165048,11.8577141160207,
12.2639521491568));
#115289=CARTESIAN_POINT('Ctrl Pts',(-9.24952090630249,11.8584882066064,
12.2565139701634));
#115290=CARTESIAN_POINT('Ctrl Pts',(-9.22109322533103,11.8602365578425,
12.2391471293402));
#115291=CARTESIAN_POINT('Ctrl Pts',(-9.20533601634961,11.8612066149366,
12.2291015269812));
#115292=CARTESIAN_POINT('Ctrl Pts',(-9.15319414696045,11.8644253707161,
12.1944378029605));
#115293=CARTESIAN_POINT('Ctrl Pts',(-9.11772514137229,11.8666287442568,
12.1684833157643));
#115294=CARTESIAN_POINT('Ctrl Pts',(-9.00118954138337,11.8740177459268,
12.0748721009633));
#115295=CARTESIAN_POINT('Ctrl Pts',(-8.92630165542791,11.8790098265681,
12.000070782526));
#115296=CARTESIAN_POINT('Ctrl Pts',(-8.83784661744725,11.8861259268869,
11.8902203176989));
#115297=CARTESIAN_POINT('Ctrl Pts',(-8.81659530711786,11.8879548142065,
11.8617689111651));
#115298=CARTESIAN_POINT('Ctrl Pts',(-8.79260815497748,11.8902031535213,
11.8270922756725));
#115299=CARTESIAN_POINT('Ctrl Pts',(-8.78885288290314,11.8905608928085,
11.821583445141));
#115300=CARTESIAN_POINT('Ctrl Pts',(-8.78277387753446,11.8911498321082,
11.8125335402636));
#115301=CARTESIAN_POINT('Ctrl Pts',(-8.78042760477626,11.891379592623,11.8090076385069));
#115302=CARTESIAN_POINT('Ctrl Pts',(-8.77623701002282,11.8917944891896,
11.8026504916372));
#115303=CARTESIAN_POINT('Ctrl Pts',(-8.77438715379534,11.891979256549,11.7998229917981));
#115304=CARTESIAN_POINT('Ctrl Pts',(-8.77034207789726,11.8923868807085,
11.7935931193736));
#115305=CARTESIAN_POINT('Ctrl Pts',(-8.76815120649359,11.8926100066002,
11.7901880748501));
#115306=CARTESIAN_POINT('Ctrl Pts',(-8.76188057642953,11.8932553422944,
11.7803528273381));
#115307=CARTESIAN_POINT('Ctrl Pts',(-8.75783690187051,11.8936797898567,
11.7738999126079));
#115308=CARTESIAN_POINT('Ctrl Pts',(-8.72821205601396,11.8968499672761,
11.7257940750527));
#115309=CARTESIAN_POINT('Ctrl Pts',(-8.70468385022007,11.8997076390147,
11.6829178607607));
#115310=CARTESIAN_POINT('Ctrl Pts',(-8.63690324694497,11.9089365988993,
11.5432455677334));
#115311=CARTESIAN_POINT('Ctrl Pts',(-8.60102786700979,11.9154334416971,
11.4427514169575));
#115312=CARTESIAN_POINT('Ctrl Pts',(-8.56429942952245,11.9246877905211,
11.2886261628154));
#115313=CARTESIAN_POINT('Ctrl Pts',(-8.55494276765743,11.9276595985992,
11.2373851542438));
#115314=CARTESIAN_POINT('Ctrl Pts',(-8.54679724379622,11.9312189752489,
11.1737265765467));
#115315=CARTESIAN_POINT('Ctrl Pts',(-8.54540819747792,11.9318866101137,
11.1616844904096));
#115316=CARTESIAN_POINT('Ctrl Pts',(-8.54345191824111,11.9329331744484,
11.1426503191556));
#115317=CARTESIAN_POINT('Ctrl Pts',(-8.54278508989747,11.9333151736115,
11.1356692160593));
#115318=CARTESIAN_POINT('Ctrl Pts',(-8.54163843878561,11.9340226275517,
11.1226790183282));
#115319=CARTESIAN_POINT('Ctrl Pts',(-8.54114551634454,11.9343484811728,
11.1166712551616));
#115320=CARTESIAN_POINT('Ctrl Pts',(-8.54013430989423,11.9350688685808,
11.1033362057976));
#115321=CARTESIAN_POINT('Ctrl Pts',(-8.53963404223708,11.9354628373827,
11.0960076905857));
#115322=CARTESIAN_POINT('Ctrl Pts',(-8.53833902149591,11.9366042640014,
11.0746739752814));
#115323=CARTESIAN_POINT('Ctrl Pts',(-8.5376904099062,11.9373472107645,11.0606605250857));
#115324=CARTESIAN_POINT('Ctrl Pts',(-8.53440327311705,11.9427667660186,
10.9575661032025));
#115325=CARTESIAN_POINT('Ctrl Pts',(-8.53970464130877,11.9471841584076,
10.8684161277608));
#115326=CARTESIAN_POINT('Ctrl Pts',(-8.56729326171334,11.9561533492868,
10.6867263682943));
#115327=CARTESIAN_POINT('Ctrl Pts',(-8.59054211638132,11.9606784445313,
10.5947663909453));
#115328=CARTESIAN_POINT('Ctrl Pts',(-8.63015593426963,11.966714379885,10.4843711040327));
#115329=CARTESIAN_POINT('Ctrl Pts',(-8.63830491782483,11.9679003322964,
10.4632204211187));
#115330=CARTESIAN_POINT('Ctrl Pts',(-8.64938591504725,11.9694559988522,
10.4363378724926));
#115331=CARTESIAN_POINT('Ctrl Pts',(-8.65186950456898,11.969801313743,10.4304233460472));
#115332=CARTESIAN_POINT('Ctrl Pts',(-8.65588162559528,11.9703541846037,
10.4210419707561));
#115333=CARTESIAN_POINT('Ctrl Pts',(-8.65738490388514,11.9705602635697,
10.4175643322563));
#115334=CARTESIAN_POINT('Ctrl Pts',(-8.66027140765136,11.9709540112089,
10.410957340259));
#115335=CARTESIAN_POINT('Ctrl Pts',(-8.6616521185089,11.9711415312223,10.4078269650013));
#115336=CARTESIAN_POINT('Ctrl Pts',(-8.66493276309844,11.9715851317555,
10.4004591013694));
#115337=CARTESIAN_POINT('Ctrl Pts',(-8.66684190464219,11.9718417593491,
10.396225780811));
#115338=CARTESIAN_POINT('Ctrl Pts',(-8.67321675718063,11.9726935184268,
10.38226786777));
#115339=CARTESIAN_POINT('Ctrl Pts',(-8.67776887452713,11.9732935446977,
10.3725833936841));
#115340=CARTESIAN_POINT('Ctrl Pts',(-8.703613764076,11.9766522729277,10.319129915983));
#115341=CARTESIAN_POINT('Ctrl Pts',(-8.72697208711382,11.9795122390927,
10.2763975687509));
#115342=CARTESIAN_POINT('Ctrl Pts',(-8.81414457006448,11.9894527788356,
10.134250193169));
#115343=CARTESIAN_POINT('Ctrl Pts',(-8.88784297415349,11.9966575825876,
10.0414130238849));
#115344=CARTESIAN_POINT('Ctrl Pts',(-8.99889684461246,12.005642625901,9.93179422090867));
#115345=CARTESIAN_POINT('Ctrl Pts',(-9.02692023781159,12.0077865030222,
9.90620511124144));
#115346=CARTESIAN_POINT('Ctrl Pts',(-9.06440059964213,12.0105003703335,
9.87456251383102));
#115347=CARTESIAN_POINT('Ctrl Pts',(-9.07297449345965,12.011111382399,9.8674897382469));
#115348=CARTESIAN_POINT('Ctrl Pts',(-9.086861565038,12.0120856416605,9.85629740520999));
#115349=CARTESIAN_POINT('Ctrl Pts',(-9.09212388939959,12.0124513500671,
9.85211568673977));
#115350=CARTESIAN_POINT('Ctrl Pts',(-9.10218945284373,12.0131443567595,
9.84422958122118));
#115351=CARTESIAN_POINT('Ctrl Pts',(-9.10698726549476,12.0134719131042,
9.8405185223371));
#115352=CARTESIAN_POINT('Ctrl Pts',(-9.11799197360889,12.0142170056589,
9.83211531826694));
#115353=CARTESIAN_POINT('Ctrl Pts',(-9.12421352317552,12.0146337829848,
9.82744260753788));
#115354=CARTESIAN_POINT('Ctrl Pts',(-9.14351570151897,12.0159133755062,
9.81318499402276));
#115355=CARTESIAN_POINT('Ctrl Pts',(-9.15671883024058,12.0167698050895,
9.8037675359362));
#115356=CARTESIAN_POINT('Ctrl Pts',(-9.22133618280742,12.0208753706536,
9.7592792301931));
#115357=CARTESIAN_POINT('Ctrl Pts',(-9.2747976756298,12.0240100410187,9.72729106218812));
#115358=CARTESIAN_POINT('Ctrl Pts',(-9.40549959371762,12.0312666224709,
9.66000520675954));
#115359=CARTESIAN_POINT('Ctrl Pts',(-9.48408635047773,12.0353175094535,
9.62783045858136));
#115360=CARTESIAN_POINT('Ctrl Pts',(-9.59111449114856,12.0408670959175,
9.59451355427368));
#115361=CARTESIAN_POINT('Ctrl Pts',(-9.61743670002312,12.042235405722,9.58712183294962));
#115362=CARTESIAN_POINT('Ctrl Pts',(-9.6708217851838,12.0450440104625,9.57373161329404));
#115363=CARTESIAN_POINT('Ctrl Pts',(-9.69787854910073,12.0464844624224,
9.56775621982086));
#115364=CARTESIAN_POINT('Ctrl Pts',(-9.73175046183815,12.0483266121899,
9.56127818404375));
#115365=CARTESIAN_POINT('Ctrl Pts',(-9.73842276732701,12.0486913548658,
9.56005013065172));
#115366=CARTESIAN_POINT('Ctrl Pts',(-9.74895336939738,12.0492702831473,
9.5581875550232));
#115367=CARTESIAN_POINT('Ctrl Pts',(-9.75280616579475,12.04948278216,9.55752201235764));
#115368=CARTESIAN_POINT('Ctrl Pts',(-9.75967211349373,12.0498627679538,
9.55636428478791));
#115369=CARTESIAN_POINT('Ctrl Pts',(-9.76268418901474,12.050029916045,9.55586608079199));
#115370=CARTESIAN_POINT('Ctrl Pts',(-9.7698827128681,12.0504304439857,9.55469855796119));
#115371=CARTESIAN_POINT('Ctrl Pts',(-9.77407050209983,12.0506643052666,
9.55403800698251));
#115372=CARTESIAN_POINT('Ctrl Pts',(-9.78670444021941,12.051372272506,9.55210144690249));
#115373=CARTESIAN_POINT('Ctrl Pts',(-9.7951587990506,12.0518493152875,9.55088120183108));
#115374=CARTESIAN_POINT('Ctrl Pts',(-9.87893733775948,12.0566058053555,
9.53953695334387));
#115375=CARTESIAN_POINT('Ctrl Pts',(-9.95492454414636,12.0611478408244,
9.53522204687687));
#115376=CARTESIAN_POINT('Ctrl Pts',(-10.1527822744948,12.0730483290963,
9.53939974891064));
#115377=CARTESIAN_POINT('Ctrl Pts',(-10.2738946133895,12.0803633111809,
9.55719462233386));
#115378=CARTESIAN_POINT('Ctrl Pts',(-10.4062784178916,12.0880508868389,
9.59393874717616));
#115379=CARTESIAN_POINT('Ctrl Pts',(-10.4210825261054,12.0889070065552,
9.5983010554303));
#115380=CARTESIAN_POINT('Ctrl Pts',(-10.4432153798648,12.0901819076362,
9.60520522394749));
#115381=CARTESIAN_POINT('Ctrl Pts',(-10.4505971221414,12.0906062649102,
9.60757241588731));
#115382=CARTESIAN_POINT('Ctrl Pts',(-10.4633623027606,12.0913387099574,
9.61177812237349));
#115383=CARTESIAN_POINT('Ctrl Pts',(-10.468754425429,12.0916476678799,9.61358956472201));
#115384=CARTESIAN_POINT('Ctrl Pts',(-10.4799632069949,12.0922890517359,
9.61742793695909));
#115385=CARTESIAN_POINT('Ctrl Pts',(-10.4857779141201,12.0926212947834,
9.61946024710825));
#115386=CARTESIAN_POINT('Ctrl Pts',(-10.4995008098727,12.0934043316828,
9.62435400099146));
#115387=CARTESIAN_POINT('Ctrl Pts',(-10.5073975531057,12.0938540810313,
9.62724703579641));
#115388=CARTESIAN_POINT('Ctrl Pts',(-10.5333239737599,12.0953282281213,
9.63699967116124));
#115389=CARTESIAN_POINT('Ctrl Pts',(-10.5512433803618,12.0963431317486,
9.6441478183767));
#115390=CARTESIAN_POINT('Ctrl Pts',(-10.5937894559204,12.0987468943643,
9.66210265399243));
#115391=CARTESIAN_POINT('Ctrl Pts',(-10.6182701063352,12.1001250851949,
9.67323799873459));
#115392=CARTESIAN_POINT('Ctrl Pts',(-10.7131794117581,12.1054706786855,
9.71960653548191));
#115393=CARTESIAN_POINT('Ctrl Pts',(-10.7810256427484,12.1092894833434,
9.75982579066119));
#115394=CARTESIAN_POINT('Ctrl Pts',(-10.9134749785787,12.1171872009357,
9.85354074408562));
#115395=CARTESIAN_POINT('Ctrl Pts',(-10.9773818633263,12.1212558609013,
9.90751341006546));
#115396=CARTESIAN_POINT('Ctrl Pts',(-11.0447525946586,12.1262768103044,
9.97507731370438));
#115397=CARTESIAN_POINT('Ctrl Pts',(-11.0530701673999,12.1269109773163,
9.98362521599326));
#115398=CARTESIAN_POINT('Ctrl Pts',(-11.0643802149046,12.1277948092838,
9.99553633595286));
#115399=CARTESIAN_POINT('Ctrl Pts',(-11.0674632507447,12.1280379866086,
9.99881335330881));
#115400=CARTESIAN_POINT('Ctrl Pts',(-11.0727194557177,12.1284565571468,
10.004452150928));
#115401=CARTESIAN_POINT('Ctrl Pts',(-11.0749000758861,12.1286313963913,
10.0068069790213));
#115402=CARTESIAN_POINT('Ctrl Pts',(-11.0794301196352,12.1289971432191,
10.0117313173801));
#115403=CARTESIAN_POINT('Ctrl Pts',(-11.0817781313781,12.1291881570838,
10.014302051414));
#115404=CARTESIAN_POINT('Ctrl Pts',(-11.0874713173949,12.1296547731608,
10.0205801111985));
#115405=CARTESIAN_POINT('Ctrl Pts',(-11.0908067207928,12.1299310852558,
10.0242962124069));
#115406=CARTESIAN_POINT('Ctrl Pts',(-11.1023704176418,12.130899128477,10.0373131747386));
#115407=CARTESIAN_POINT('Ctrl Pts',(-11.110499071855,12.1315975932638,10.0467013836924));
#115408=CARTESIAN_POINT('Ctrl Pts',(-11.1628290466101,12.1362067855806,
10.1087176158682));
#115409=CARTESIAN_POINT('Ctrl Pts',(-11.2033924431876,12.1403119039653,
10.1642962803177));
#115410=CARTESIAN_POINT('Ctrl Pts',(-11.2693042751074,12.1477707613005,
10.2694092109433));
#115411=CARTESIAN_POINT('Ctrl Pts',(-11.2960274746703,12.1511101693563,
10.3179374132596));
#115412=CARTESIAN_POINT('Ctrl Pts',(-11.3519386845608,12.1587972464062,
10.4346833094707));
#115413=CARTESIAN_POINT('Ctrl Pts',(-11.3788226890236,12.1630888458333,
10.5038430529542));
#115414=CARTESIAN_POINT('Ctrl Pts',(-11.4038246835025,12.1678703798191,
10.5861750699359));
#115415=CARTESIAN_POINT('Ctrl Pts',(-11.4071542316012,12.1685294214914,
10.597642205175));
#115416=CARTESIAN_POINT('Ctrl Pts',(-11.412373780027,12.169600777187,10.616476377842));
#115417=CARTESIAN_POINT('Ctrl Pts',(-11.4143473087481,12.17001574586,10.6238195160066));
#115418=CARTESIAN_POINT('Ctrl Pts',(-11.4177873350232,12.1707574183349,
10.6370290890842));
#115419=CARTESIAN_POINT('Ctrl Pts',(-11.419274862089,12.1710847864414,10.6428898252919));
#115420=CARTESIAN_POINT('Ctrl Pts',(-11.4223641899192,12.1717792495184,
10.6553857950484));
#115421=CARTESIAN_POINT('Ctrl Pts',(-11.4239559820754,12.1721460197657,
10.6620233702162));
#115422=CARTESIAN_POINT('Ctrl Pts',(-11.4271066675951,12.1728908485569,
10.6755788353909));
#115423=CARTESIAN_POINT('Ctrl Pts',(-11.4286618355269,12.1732687816688,
10.6824974097555));
#115424=CARTESIAN_POINT('Ctrl Pts',(-11.4324315420034,12.1742116504702,
10.6998566465726));
#115425=CARTESIAN_POINT('Ctrl Pts',(-11.4345822904332,12.1747745984343,
10.7103108305581));
#115426=CARTESIAN_POINT('Ctrl Pts',(-11.454580405202,12.1802701420819,10.8132062665199));
#115427=CARTESIAN_POINT('Ctrl Pts',(-11.4635827899384,12.1849093905218,
10.9071414041028));
#115428=CARTESIAN_POINT('Ctrl Pts',(-11.463499426367,12.1894964612477,11.001295771428));
#115429=CARTESIAN_POINT('Origin',(-10.,3.5,11.));
#115430=CARTESIAN_POINT('',(-11.4634998767682,12.7606556498649,10.9993994174008));
#115431=CARTESIAN_POINT('',(-11.4634998508852,12.6893449541571,10.9993393494607));
#115432=CARTESIAN_POINT('',(-11.4635,3.5,11.));
#115433=CARTESIAN_POINT('Ctrl Pts',(-11.4634998503757,12.7618466610292,
10.9993382219031));
#115434=CARTESIAN_POINT('Ctrl Pts',(-11.4634894474406,12.7606645999763,
10.9763324830867));
#115435=CARTESIAN_POINT('Ctrl Pts',(-11.4629365817839,12.7594623465774,
10.9533312021013));
#115436=CARTESIAN_POINT('Ctrl Pts',(-11.4616132755002,12.7579758532266,
10.9255556921769));
#115437=CARTESIAN_POINT('Ctrl Pts',(-11.4613610733915,12.7577178906591,
10.9207590131217));
#115438=CARTESIAN_POINT('Ctrl Pts',(-11.4608857152345,12.757271125723,10.9124942628439));
#115439=CARTESIAN_POINT('Ctrl Pts',(-11.4606738092072,12.757082922709,10.9090255552098));
#115440=CARTESIAN_POINT('Ctrl Pts',(-11.4602450317801,12.7567217780512,
10.902394971115));
#115441=CARTESIAN_POINT('Ctrl Pts',(-11.4600302388922,12.756548950413,10.8992329621475));
#115442=CARTESIAN_POINT('Ctrl Pts',(-11.4595810867635,12.7562028765707,
10.8929240507426));
#115443=CARTESIAN_POINT('Ctrl Pts',(-11.4593468195799,12.7560296424497,
10.8897771913828));
#115444=CARTESIAN_POINT('Ctrl Pts',(-11.4587699610399,12.7556195211129,
10.8823527918867));
#115445=CARTESIAN_POINT('Ctrl Pts',(-11.4584187314394,12.755382166558,10.8780759759065));
#115446=CARTESIAN_POINT('Ctrl Pts',(-11.4571332909366,12.7545542514349,
10.8632245728841));
#115447=CARTESIAN_POINT('Ctrl Pts',(-11.4561028579416,12.7539587445218,
10.8526589028469));
#115448=CARTESIAN_POINT('Ctrl Pts',(-11.4521366632352,12.7518784527108,
10.8161113837737));
#115449=CARTESIAN_POINT('Ctrl Pts',(-11.4486197544557,12.7503678034206,
10.7901987488577));
#115450=CARTESIAN_POINT('Ctrl Pts',(-11.4369981628361,12.7461397984288,
10.7189506482705));
#115451=CARTESIAN_POINT('Ctrl Pts',(-11.4274450953092,12.7433821114147,
10.6738825386551));
#115452=CARTESIAN_POINT('Ctrl Pts',(-11.3861242123945,12.7335717682075,
10.5160512474317));
#115453=CARTESIAN_POINT('Ctrl Pts',(-11.342967712621,12.726537121834,10.4067099920741));
#115454=CARTESIAN_POINT('Ctrl Pts',(-11.2773261207098,12.7187728284586,
10.285364739421));
#115455=CARTESIAN_POINT('Ctrl Pts',(-11.2670319210252,12.7176145680666,
10.2672682976527));
#115456=CARTESIAN_POINT('Ctrl Pts',(-11.2519420209439,12.7159967905618,
10.2420109155834));
#115457=CARTESIAN_POINT('Ctrl Pts',(-11.2474641589254,12.7155260452772,
10.2346638304005));
#115458=CARTESIAN_POINT('Ctrl Pts',(-11.2396457870149,12.7147198237232,
10.2220867172594));
#115459=CARTESIAN_POINT('Ctrl Pts',(-11.2363363595623,12.7143832363241,
10.2168377177181));
#115460=CARTESIAN_POINT('Ctrl Pts',(-11.2299423810909,12.7137417304175,
10.2068379291625));
#115461=CARTESIAN_POINT('Ctrl Pts',(-11.2268634435443,12.713436615467,10.2020836989107));
#115462=CARTESIAN_POINT('Ctrl Pts',(-11.21878564542,12.7126458333635,10.1897679575433));
#115463=CARTESIAN_POINT('Ctrl Pts',(-11.2137439564345,12.7121617502312,
10.1822347370623));
#115464=CARTESIAN_POINT('Ctrl Pts',(-11.1961475355776,12.7105039412831,
10.1564636691253));
#115465=CARTESIAN_POINT('Ctrl Pts',(-11.1832488168193,12.7093430103865,
10.1384637133702));
#115466=CARTESIAN_POINT('Ctrl Pts',(-11.0981661263326,12.7020059036102,
10.0252494880466));
#115467=CARTESIAN_POINT('Ctrl Pts',(-11.0149634294888,12.696293138055,9.93888835959894));
#115468=CARTESIAN_POINT('Ctrl Pts',(-10.8841763938904,12.688043338562,9.83275525115613));
#115469=CARTESIAN_POINT('Ctrl Pts',(-10.8446469023027,12.6856209014528,
9.8038398008398));
#115470=CARTESIAN_POINT('Ctrl Pts',(-10.7899819016892,12.682262862902,9.76791554141985));
#115471=CARTESIAN_POINT('Ctrl Pts',(-10.7760666022131,12.6814073190726,
9.75910350629386));
#115472=CARTESIAN_POINT('Ctrl Pts',(-10.7552474950749,12.6801217779288,
9.74640670919831));
#115473=CARTESIAN_POINT('Ctrl Pts',(-10.7484557280079,12.6797015431931,
9.74233989661829));
#115474=CARTESIAN_POINT('Ctrl Pts',(-10.736090433911,12.6789342959174,9.73507137175173));
#115475=CARTESIAN_POINT('Ctrl Pts',(-10.7305281296132,12.6785883830516,
9.73185087222255));
#115476=CARTESIAN_POINT('Ctrl Pts',(-10.7216779502969,12.6780364812003,
9.72680428474577));
#115477=CARTESIAN_POINT('Ctrl Pts',(-10.7184038749353,12.6778319810264,
9.72495401450765));
#115478=CARTESIAN_POINT('Ctrl Pts',(-10.7122749455627,12.6774484878162,
9.7215214880068));
#115479=CARTESIAN_POINT('Ctrl Pts',(-10.7094219021865,12.677269691098,9.71993614701244));
#115480=CARTESIAN_POINT('Ctrl Pts',(-10.7027261341567,12.6768494397151,
9.71624479276612));
#115481=CARTESIAN_POINT('Ctrl Pts',(-10.6988792468815,12.6766075123453,
9.71414649007319));
#115482=CARTESIAN_POINT('Ctrl Pts',(-10.6885931111383,12.6759594623919,
9.70859566313385));
#115483=CARTESIAN_POINT('Ctrl Pts',(-10.6821374144762,12.6755515287889,
9.70517407450599));
#115484=CARTESIAN_POINT('Ctrl Pts',(-10.6289116304516,12.6721799959832,
9.67747235213827));
#115485=CARTESIAN_POINT('Ctrl Pts',(-10.5808909738258,12.6690875270071,
9.65568833507584));
#115486=CARTESIAN_POINT('Ctrl Pts',(-10.4315706989491,12.6595337911352,
9.5974471540304));
#115487=CARTESIAN_POINT('Ctrl Pts',(-10.3273171616091,12.6529748856029,
9.56951921617888));
#115488=CARTESIAN_POINT('Ctrl Pts',(-10.1739743702117,12.64396001741,9.54610089912031));
#115489=CARTESIAN_POINT('Ctrl Pts',(-10.1266819238536,12.6412582005032,
9.54121897489193));
#115490=CARTESIAN_POINT('Ctrl Pts',(-10.0677655455937,12.6379911061445,
9.53802464425919));
#115491=CARTESIAN_POINT('Ctrl Pts',(-10.0562922184129,12.6373594264461,
9.53753792985515));
#115492=CARTESIAN_POINT('Ctrl Pts',(-10.0380144679226,12.636360158785,9.53697798073755));
#115493=CARTESIAN_POINT('Ctrl Pts',(-10.0312133715262,12.635989883757,9.53681708039404));
#115494=CARTESIAN_POINT('Ctrl Pts',(-10.0183612385959,12.6352930276925,
9.53660267576345));
#115495=CARTESIAN_POINT('Ctrl Pts',(-10.0123105288893,12.6349661483493,
9.5365392673338));
#115496=CARTESIAN_POINT('Ctrl Pts',(-9.99861733198425,12.6342290348967,
9.53648069961854));
#115497=CARTESIAN_POINT('Ctrl Pts',(-9.99097489329851,12.63381949751,9.53650787333637));
#115498=CARTESIAN_POINT('Ctrl Pts',(-9.97126718221537,12.632768026784,9.53673232932138));
#115499=CARTESIAN_POINT('Ctrl Pts',(-9.95920338141168,12.6321288451747,
9.53701896861355));
#115500=CARTESIAN_POINT('Ctrl Pts',(-9.8525615147297,12.6265150488621,9.54087295853045));
#115501=CARTESIAN_POINT('Ctrl Pts',(-9.75853035651112,12.6218390501067,
9.55345757397152));
#115502=CARTESIAN_POINT('Ctrl Pts',(-9.60040233431529,12.6139231810561,
9.5904811444635));
#115503=CARTESIAN_POINT('Ctrl Pts',(-9.53559549225147,12.6106565924612,
9.6104859046516));
#115504=CARTESIAN_POINT('Ctrl Pts',(-9.43183973579149,12.6050948505191,
9.65058605550645));
#115505=CARTESIAN_POINT('Ctrl Pts',(-9.39199174492293,12.6028721921051,
9.6680655461373));
#115506=CARTESIAN_POINT('Ctrl Pts',(-9.34632746337796,12.6001577132666,
9.69057281520895));
#115507=CARTESIAN_POINT('Ctrl Pts',(-9.33969530501415,12.5997592076041,
9.69390465792816));
#115508=CARTESIAN_POINT('Ctrl Pts',(-9.32952239983745,12.599140932343,9.69911257542349));
#115509=CARTESIAN_POINT('Ctrl Pts',(-9.32596343965669,12.59892329728,9.70095303461193));
#115510=CARTESIAN_POINT('Ctrl Pts',(-9.31941764462149,12.5985204696344,
9.7043722289648));
#115511=CARTESIAN_POINT('Ctrl Pts',(-9.3164286813142,12.5983355391674,9.705946710845));
#115512=CARTESIAN_POINT('Ctrl Pts',(-9.30966652207587,12.5979149149971,
9.70953874662261));
#115513=CARTESIAN_POINT('Ctrl Pts',(-9.30589672703332,12.5976788420207,
9.71156249561004));
#115514=CARTESIAN_POINT('Ctrl Pts',(-9.29614207424592,12.5970639804193,
9.71685434595702));
#115515=CARTESIAN_POINT('Ctrl Pts',(-9.29017115375962,12.5966836876554,
9.72014776065694));
#115516=CARTESIAN_POINT('Ctrl Pts',(-9.25047931193279,12.594130476364,9.74240400788577));
#115517=CARTESIAN_POINT('Ctrl Pts',(-9.21750117099134,12.5918873798663,
9.7626544379481));
#115518=CARTESIAN_POINT('Ctrl Pts',(-9.1002739033882,12.5835638481817,9.84120032584352));
#115519=CARTESIAN_POINT('Ctrl Pts',(-9.02140065611844,12.5772965219298,
9.90699098461165));
#115520=CARTESIAN_POINT('Ctrl Pts',(-8.91959327582179,12.5686689592212,
10.0118381553829));
#115521=CARTESIAN_POINT('Ctrl Pts',(-8.8905640827925,12.5661290833656,10.0445446299181));
#115522=CARTESIAN_POINT('Ctrl Pts',(-8.85131847704376,12.5625865686471,
10.0929665998304));
#115523=CARTESIAN_POINT('Ctrl Pts',(-8.83987313394618,12.5615387070698,
10.1076522377533));
#115524=CARTESIAN_POINT('Ctrl Pts',(-8.81996814810889,12.5596892169058,
10.1342230612114));
#115525=CARTESIAN_POINT('Ctrl Pts',(-8.81140026193073,12.5588835504876,
10.1460236751454));
#115526=CARTESIAN_POINT('Ctrl Pts',(-8.79872161626993,12.5576762323239,
10.1640466250147));
#115527=CARTESIAN_POINT('Ctrl Pts',(-8.79447986189196,12.5572696445021,
10.1701753198133));
#115528=CARTESIAN_POINT('Ctrl Pts',(-8.78689292171742,12.5565374457522,
10.1813182585474));
#115529=CARTESIAN_POINT('Ctrl Pts',(-8.78353156238559,12.5562112339537,
10.1863212433915));
#115530=CARTESIAN_POINT('Ctrl Pts',(-8.77638134830163,12.5555133290493,
10.1971068339415));
#115531=CARTESIAN_POINT('Ctrl Pts',(-8.7726023567602,12.5551420064076,10.202895823314));
#115532=CARTESIAN_POINT('Ctrl Pts',(-8.7625344735466,12.5541458768174,10.2185600566457));
#115533=CARTESIAN_POINT('Ctrl Pts',(-8.75632275529827,12.553523897762,10.22848445526));
#115534=CARTESIAN_POINT('Ctrl Pts',(-8.7262263060429,12.5504716945306,10.2778774371942));
#115535=CARTESIAN_POINT('Ctrl Pts',(-8.70409682043416,12.5481047547185,
10.3183872794507));
#115536=CARTESIAN_POINT('Ctrl Pts',(-8.63567188281134,12.5402414485446,
10.4590681049536));
#115537=CARTESIAN_POINT('Ctrl Pts',(-8.59879772192441,12.5350227405036,
10.563388555284));
#115538=CARTESIAN_POINT('Ctrl Pts',(-8.56238393094561,12.5269941816567,
10.7211516090788));
#115539=CARTESIAN_POINT('Ctrl Pts',(-8.55344548046709,12.5243799337738,
10.7720188881128));
#115540=CARTESIAN_POINT('Ctrl Pts',(-8.54628397301305,12.5212211485216,
10.8308813538659));
#115541=CARTESIAN_POINT('Ctrl Pts',(-8.54541529928664,12.5208084789294,
10.83852323097));
#115542=CARTESIAN_POINT('Ctrl Pts',(-8.54417998218654,12.520172931339,10.8502107348267));
#115543=CARTESIAN_POINT('Ctrl Pts',(-8.54376986916777,12.5199523834001,
10.8542517462381));
#115544=CARTESIAN_POINT('Ctrl Pts',(-8.54304971716165,12.5195468125867,
10.8616543470988));
#115545=CARTESIAN_POINT('Ctrl Pts',(-8.54273448214689,12.5193620780995,
10.8650153482225));
#115546=CARTESIAN_POINT('Ctrl Pts',(-8.54205195033577,12.5189453153129,
10.8725736055849));
#115547=CARTESIAN_POINT('Ctrl Pts',(-8.54169115060968,12.5187129382252,
10.8767713491267));
#115548=CARTESIAN_POINT('Ctrl Pts',(-8.54068571062748,12.5180283043031,
10.8890925553855));
#115549=CARTESIAN_POINT('Ctrl Pts',(-8.54009079846664,12.5175734468549,
10.8972197803135));
#115550=CARTESIAN_POINT('Ctrl Pts',(-8.53514020494721,12.5132702662394,
10.9736078385341));
#115551=CARTESIAN_POINT('Ctrl Pts',(-8.53550765054672,12.5092067474882,
11.0420840663074));
#115552=CARTESIAN_POINT('Ctrl Pts',(-8.54686534541231,12.5001591530132,
11.1923866470026));
#115553=CARTESIAN_POINT('Ctrl Pts',(-8.55998964699262,12.4951774396486,
11.2738335673536));
#115554=CARTESIAN_POINT('Ctrl Pts',(-8.59342405360091,12.4870759654508,
11.4080548044198));
#115555=CARTESIAN_POINT('Ctrl Pts',(-8.61005727511625,12.4838747839393,
11.4615462969679));
#115556=CARTESIAN_POINT('Ctrl Pts',(-8.63393632541507,12.4801055819105,
11.5252111173232));
#115557=CARTESIAN_POINT('Ctrl Pts',(-8.63829536729621,12.4794439402727,
11.5364113963155));
#115558=CARTESIAN_POINT('Ctrl Pts',(-8.6453808793314,12.4784085342946,11.553973978279));
#115559=CARTESIAN_POINT('Ctrl Pts',(-8.64801529640762,12.4780317382863,
11.5603726387224));
#115560=CARTESIAN_POINT('Ctrl Pts',(-8.65303247927755,12.4773291037495,
11.5723173771531));
#115561=CARTESIAN_POINT('Ctrl Pts',(-8.65540435905859,12.477002910593,11.5778678446976));
#115562=CARTESIAN_POINT('Ctrl Pts',(-8.66078755461343,12.476275699633,11.5902525285417));
#115563=CARTESIAN_POINT('Ctrl Pts',(-8.66381699185834,12.4758753009355,
11.5970787158168));
#115564=CARTESIAN_POINT('Ctrl Pts',(-8.67164090223024,12.4748631210593,
11.6143504254785));
#115565=CARTESIAN_POINT('Ctrl Pts',(-8.67650645863034,12.4742537497267,
11.6247633101871));
#115566=CARTESIAN_POINT('Ctrl Pts',(-8.7079573950299,12.4704364011011,11.6900554921859));
#115567=CARTESIAN_POINT('Ctrl Pts',(-8.73782954314724,12.4673438478479,
11.7432883074414));
#115568=CARTESIAN_POINT('Ctrl Pts',(-8.82443354765386,12.4594310890618,
11.8772603134091));
#115569=CARTESIAN_POINT('Ctrl Pts',(-8.88614621896858,12.4547509232849,
11.9543953930471));
#115570=CARTESIAN_POINT('Ctrl Pts',(-8.97734030901839,12.4482619717324,
12.0473799742652));
#115571=CARTESIAN_POINT('Ctrl Pts',(-9.00027101729209,12.4466585003391,
12.0692892038057));
#115572=CARTESIAN_POINT('Ctrl Pts',(-9.03769365315214,12.4440516466825,
12.1027881828501));
#115573=CARTESIAN_POINT('Ctrl Pts',(-9.05172612389743,12.443076210292,12.1148775155358));
#115574=CARTESIAN_POINT('Ctrl Pts',(-9.07040271748093,12.4417749476347,
12.130360160247));
#115575=CARTESIAN_POINT('Ctrl Pts',(-9.07484331153129,12.4414653391721,
12.1339974863874));
#115576=CARTESIAN_POINT('Ctrl Pts',(-9.08213461224409,12.4409564086106,
12.1398985174307));
#115577=CARTESIAN_POINT('Ctrl Pts',(-9.08497261234077,12.4407581788672,
12.1421779105389));
#115578=CARTESIAN_POINT('Ctrl Pts',(-9.09051694479987,12.4403705834913,
12.1465970194147));
#115579=CARTESIAN_POINT('Ctrl Pts',(-9.09322237997149,12.4401812937438,
12.1487377854108));
#115580=CARTESIAN_POINT('Ctrl Pts',(-9.09987445609668,12.439715537668,12.1539633214591));
#115581=CARTESIAN_POINT('Ctrl Pts',(-9.10382939755445,12.4394383407508,
12.1570374202562));
#115582=CARTESIAN_POINT('Ctrl Pts',(-9.11733608042784,12.43849093561,12.1674251067066));
#115583=CARTESIAN_POINT('Ctrl Pts',(-9.12696193790596,12.4378144993517,
12.1746410080914));
#115584=CARTESIAN_POINT('Ctrl Pts',(-9.19739370495686,12.4328627054967,
12.2260953269246));
#115585=CARTESIAN_POINT('Ctrl Pts',(-9.26143560336475,12.4283532231816,
12.2657042967515));
#115586=CARTESIAN_POINT('Ctrl Pts',(-9.38564438867118,12.4199416182248,
12.3298780920897));
#115587=CARTESIAN_POINT('Ctrl Pts',(-9.44496327842079,12.4160516903926,
12.3557077969249));
#115588=CARTESIAN_POINT('Ctrl Pts',(-9.54346986221302,12.4098992913092,
12.3910479297677));
#115589=CARTESIAN_POINT('Ctrl Pts',(-9.58168270016009,12.4075825624172,
12.4030128785986));
#115590=CARTESIAN_POINT('Ctrl Pts',(-9.64555658158733,12.4038320693768,
12.420170357843));
#115591=CARTESIAN_POINT('Ctrl Pts',(-9.67095048204999,12.402371887615,12.4262680390445));
#115592=CARTESIAN_POINT('Ctrl Pts',(-9.70566461537061,12.4004165812916,
12.4336271444188));
#115593=CARTESIAN_POINT('Ctrl Pts',(-9.71485269869166,12.3999028847763,
12.4354828909204));
#115594=CARTESIAN_POINT('Ctrl Pts',(-9.73028859109409,12.3990461576815,
12.438446472925));
#115595=CARTESIAN_POINT('Ctrl Pts',(-9.73652683209026,12.3987016324888,
12.4396021641803));
#115596=CARTESIAN_POINT('Ctrl Pts',(-9.74883472305933,12.3980251995637,
12.4417996310882));
#115597=CARTESIAN_POINT('Ctrl Pts',(-9.75490381939485,12.3976932252714,
12.4428437324908));
#115598=CARTESIAN_POINT('Ctrl Pts',(-9.76826556625888,12.3969657440448,
12.4450556893994));
#115599=CARTESIAN_POINT('Ctrl Pts',(-9.77556085621405,12.3965707693593,
12.4462067164402));
#115600=CARTESIAN_POINT('Ctrl Pts',(-9.80119233926919,12.3951905920487,
12.4500521470978));
#115601=CARTESIAN_POINT('Ctrl Pts',(-9.81957111800628,12.3942144881424,
12.4524535015816));
#115602=CARTESIAN_POINT('Ctrl Pts',(-9.93764592036376,12.3880214722084,
12.4656051680104));
#115603=CARTESIAN_POINT('Ctrl Pts',(-10.0381788947011,12.3831281873992,
12.4664349054896));
#115604=CARTESIAN_POINT('Ctrl Pts',(-10.2252821373829,12.3739832539474,
12.4487111778383));
#115605=CARTESIAN_POINT('Ctrl Pts',(-10.3116207670601,12.3697379345213,
12.4326218204824));
#115606=CARTESIAN_POINT('Ctrl Pts',(-10.4095526973019,12.3644087044578,
12.4050969027435));
#115607=CARTESIAN_POINT('Ctrl Pts',(-10.4230588217514,12.3636618362922,
12.4010895483128));
#115608=CARTESIAN_POINT('Ctrl Pts',(-10.4414464326001,12.3626260908841,
12.3953437227848));
#115609=CARTESIAN_POINT('Ctrl Pts',(-10.4463800691739,12.3623463074613,
12.3937732562323));
#115610=CARTESIAN_POINT('Ctrl Pts',(-10.4546509782038,12.3618739488042,
12.3910920561473));
#115611=CARTESIAN_POINT('Ctrl Pts',(-10.4579928174043,12.3616821792871,
12.3899953955018));
#115612=CARTESIAN_POINT('Ctrl Pts',(-10.464338771086,12.361316224399,12.3878875324804));
#115613=CARTESIAN_POINT('Ctrl Pts',(-10.4673436099646,12.3611421768721,
12.3868785985005));
#115614=CARTESIAN_POINT('Ctrl Pts',(-10.4744643986938,12.3607279445525,
12.3844618836772));
#115615=CARTESIAN_POINT('Ctrl Pts',(-10.4785773726445,12.3604872696361,
12.3830455055393));
#115616=CARTESIAN_POINT('Ctrl Pts',(-10.4930201096844,12.3596373119801,
12.3779997453773));
#115617=CARTESIAN_POINT('Ctrl Pts',(-10.5033151468152,12.3590227416419,
12.3742728897));
#115618=CARTESIAN_POINT('Ctrl Pts',(-10.6099780062433,12.3525716476919,
12.3343011334252));
#115619=CARTESIAN_POINT('Ctrl Pts',(-10.7023008517762,12.346294341507,12.2881008595586));
#115620=CARTESIAN_POINT('Ctrl Pts',(-10.8442670702993,12.3361822497266,
12.197226169405));
#115621=CARTESIAN_POINT('Ctrl Pts',(-10.8970913734018,12.3322934495163,
12.1581735055416));
#115622=CARTESIAN_POINT('Ctrl Pts',(-10.9749238674062,12.3264289135999,
12.0921015598315));
#115623=CARTESIAN_POINT('Ctrl Pts',(-11.0018369888671,12.3243717478676,
12.0674667866193));
#115624=CARTESIAN_POINT('Ctrl Pts',(-11.0353211642512,12.3217726116964,
12.034434076519));
#115625=CARTESIAN_POINT('Ctrl Pts',(-11.0427586341738,12.3211925811825,
12.0269363226797));
#115626=CARTESIAN_POINT('Ctrl Pts',(-11.0547102547638,12.3202558739916,
12.0146241005199));
#115627=CARTESIAN_POINT('Ctrl Pts',(-11.0592740526431,12.3198970614614,
12.0098585397155));
#115628=CARTESIAN_POINT('Ctrl Pts',(-11.0679918317583,12.3192094107241,
12.0006312288865));
#115629=CARTESIAN_POINT('Ctrl Pts',(-11.072150463228,12.3188803779409,11.9961740784972));
#115630=CARTESIAN_POINT('Ctrl Pts',(-11.0816265808518,12.3181282324177,
11.9858896585889));
#115631=CARTESIAN_POINT('Ctrl Pts',(-11.0869250681915,12.3177059202737,
11.9800450901591));
#115632=CARTESIAN_POINT('Ctrl Pts',(-11.1036633086237,12.316365904541,11.9612790291556));
#115633=CARTESIAN_POINT('Ctrl Pts',(-11.1149221035705,12.3154556296693,
11.9481976621597));
#115634=CARTESIAN_POINT('Ctrl Pts',(-11.2031459955531,12.3082413439645,
11.8419474352726));
#115635=CARTESIAN_POINT('Ctrl Pts',(-11.2685312522559,12.302436673178,11.7397745812336));
#115636=CARTESIAN_POINT('Ctrl Pts',(-11.3439797821411,12.2938926012885,
11.5817987233216));
#115637=CARTESIAN_POINT('Ctrl Pts',(-11.3646064053514,12.2912260598091,
11.5316201918534));
#115638=CARTESIAN_POINT('Ctrl Pts',(-11.3881502599117,12.2875547587559,
11.4638726897905));
#115639=CARTESIAN_POINT('Ctrl Pts',(-11.393602080732,12.286647117436,11.4472272474252));
#115640=CARTESIAN_POINT('Ctrl Pts',(-11.4022942662534,12.285091580831,11.4189843958975));
#115641=CARTESIAN_POINT('Ctrl Pts',(-11.4056927008977,12.2844512781024,
11.4074372900909));
#115642=CARTESIAN_POINT('Ctrl Pts',(-11.4102646239921,12.2835412116344,
11.3911644503277));
#115643=CARTESIAN_POINT('Ctrl Pts',(-11.4115576362297,12.2832779154584,
11.3864724765427));
#115644=CARTESIAN_POINT('Ctrl Pts',(-11.4137290623644,12.2828253138687,
11.3784367060661));
#115645=CARTESIAN_POINT('Ctrl Pts',(-11.4146190875962,12.2826366650252,
11.3750960398911));
#115646=CARTESIAN_POINT('Ctrl Pts',(-11.4163201272103,12.2822699103311,
11.3686191001326));
#115647=CARTESIAN_POINT('Ctrl Pts',(-11.4171325735832,12.2820918967471,
11.3654832584311));
#115648=CARTESIAN_POINT('Ctrl Pts',(-11.4193088770208,12.2816072816868,
11.3569669056941));
#115649=CARTESIAN_POINT('Ctrl Pts',(-11.420652531175,12.2812995633183,11.3515813473378));
#115650=CARTESIAN_POINT('Ctrl Pts',(-11.4256318040382,12.2801265452896,
11.331129030298));
#115651=CARTESIAN_POINT('Ctrl Pts',(-11.4290585075076,12.2792505144565,
11.3160130035892));
#115652=CARTESIAN_POINT('Ctrl Pts',(-11.452936642639,12.2726092505123,11.2023358419851));
#115653=CARTESIAN_POINT('Ctrl Pts',(-11.4634095186046,12.2664666592914,
11.1019588962303));
#115654=CARTESIAN_POINT('Ctrl Pts',(-11.4634998054292,12.26040996372,11.0008714174426));
#115655=CARTESIAN_POINT('Ctrl Pts',(-11.4635,12.2603838599167,11.0004357065747));
#115656=CARTESIAN_POINT('Ctrl Pts',(-11.4635,12.2603577583743,11.0000000000809));
#115657=CARTESIAN_POINT('Ctrl Pts',(-11.4634994198187,12.1893450843268,
11.0013031462968));
#115658=CARTESIAN_POINT('Ctrl Pts',(-11.4634359485494,12.1932196543108,
11.0725846026601));
#115659=CARTESIAN_POINT('Ctrl Pts',(-11.4581608845053,12.1970942242948,
11.1436375246629));
#115660=CARTESIAN_POINT('Ctrl Pts',(-11.447796367688,12.2009687942788,11.2138175102968));
#115661=CARTESIAN_POINT('Ctrl Pts',(-11.4404497091357,12.2037151975325,
11.2635630412024));
#115662=CARTESIAN_POINT('Ctrl Pts',(-11.4305469451326,12.2064616007861,
11.3128705823204));
#115663=CARTESIAN_POINT('Ctrl Pts',(-11.4181457399084,12.2092080040398,
11.3615175104743));
#115664=CARTESIAN_POINT('Ctrl Pts',(-11.4045533990745,12.2122181992923,
11.414836975481));
#115665=CARTESIAN_POINT('Ctrl Pts',(-11.3879212767731,12.2152283945447,
11.4675007691464));
#115666=CARTESIAN_POINT('Ctrl Pts',(-11.3683304217789,12.2182385897972,
11.5191378495491));
#115667=CARTESIAN_POINT('Ctrl Pts',(-11.3487743686918,12.2212434376294,
11.5706831999645));
#115668=CARTESIAN_POINT('Ctrl Pts',(-11.3262701993104,12.2242482854616,
11.6212049668901));
#115669=CARTESIAN_POINT('Ctrl Pts',(-11.3009490650713,12.2272531332938,
11.6703460151967));
#115670=CARTESIAN_POINT('Ctrl Pts',(-11.275652968618,12.2302550099029,11.7194384723529));
#115671=CARTESIAN_POINT('Ctrl Pts',(-11.2475456658493,12.2332568865121,
11.767152448301));
#115672=CARTESIAN_POINT('Ctrl Pts',(-11.2168061261672,12.2362587631213,
11.8131513397406));
#115673=CARTESIAN_POINT('Ctrl Pts',(-11.1860848423066,12.2392588569541,
11.8591229130239));
#115674=CARTESIAN_POINT('Ctrl Pts',(-11.1527347128426,12.2422589507869,
11.9033809824768));
#115675=CARTESIAN_POINT('Ctrl Pts',(-11.1169791419518,12.2452590446198,
11.9456161200215));
#115676=CARTESIAN_POINT('Ctrl Pts',(-11.0812306859958,12.2482585414695,
11.9878428532745));
#115677=CARTESIAN_POINT('Ctrl Pts',(-11.0430780802319,12.2512580383192,
12.0280470512292));
#115678=CARTESIAN_POINT('Ctrl Pts',(-11.0027848412112,12.2542575351689,
12.0659525375161));
#115679=CARTESIAN_POINT('Ctrl Pts',(-10.9624545653709,12.2572597891021,
12.1038928658433));
#115680=CARTESIAN_POINT('Ctrl Pts',(-10.9199801106826,12.2602620430353,
12.1395298985348));
#115681=CARTESIAN_POINT('Ctrl Pts',(-10.8756605986392,12.2632642969685,
12.1726255864473));
#115682=CARTESIAN_POINT('Ctrl Pts',(-10.8313209000313,12.2662679183625,
12.2057363487189));
#115683=CARTESIAN_POINT('Ctrl Pts',(-10.7851349099702,12.2692715397564,
12.2363031668105));
#115684=CARTESIAN_POINT('Ctrl Pts',(-10.737430742612,12.2722751611503,12.2641313815623));
#115685=CARTESIAN_POINT('Ctrl Pts',(-10.6896366113356,12.2752844469876,
12.2920120767446));
#115686=CARTESIAN_POINT('Ctrl Pts',(-10.6403190549909,12.2782937328248,
12.3171436110791));
#115687=CARTESIAN_POINT('Ctrl Pts',(-10.5898297368758,12.281303018662,12.3393778897298));
#115688=CARTESIAN_POINT('Ctrl Pts',(-10.551304766603,12.2835992003446,12.3563433579919));
#115689=CARTESIAN_POINT('Ctrl Pts',(-10.5120980785672,12.2858953820271,
12.3716229555613));
#115690=CARTESIAN_POINT('Ctrl Pts',(-10.4723716545434,12.2881915637097,
12.3851704840863));
#115691=CARTESIAN_POINT('Ctrl Pts',(-10.4202917244482,12.2912017762937,
12.4029308125298));
#115692=CARTESIAN_POINT('Ctrl Pts',(-10.3670994124745,12.2942119888777,
12.4177871813881));
#115693=CARTESIAN_POINT('Ctrl Pts',(-10.3131497370528,12.2972222014618,
12.4296046628994));
#115694=CARTESIAN_POINT('Ctrl Pts',(-10.2592959026268,12.3002270664367,
12.4414011507869));
#115695=CARTESIAN_POINT('Ctrl Pts',(-10.2046878864915,12.3032319314117,
12.4501693527271));
#115696=CARTESIAN_POINT('Ctrl Pts',(-10.149696445571,12.3062367963867,12.455823898754));
#115697=CARTESIAN_POINT('Ctrl Pts',(-10.0947593827573,12.3092386900108,
12.4614728533016));
#115698=CARTESIAN_POINT('Ctrl Pts',(-10.0394401689671,12.3122405836349,
12.4640141974152));
#115699=CARTESIAN_POINT('Ctrl Pts',(-9.98411850308232,12.315242477259,12.4634138266586));
#115700=CARTESIAN_POINT('Ctrl Pts',(-9.92882969472483,12.3182425879505,
12.4628138124839));
#115701=CARTESIAN_POINT('Ctrl Pts',(-9.87353896415618,12.3212426986419,
12.4590757876622));
#115702=CARTESIAN_POINT('Ctrl Pts',(-9.81862753988087,12.3242428093334,
12.4522177111957));
#115703=CARTESIAN_POINT('Ctrl Pts',(-9.7637270456489,12.327242322857,12.4453609998198));
#115704=CARTESIAN_POINT('Ctrl Pts',(-9.70920623148442,12.3302418363806,
12.4353855355812));
#115705=CARTESIAN_POINT('Ctrl Pts',(-9.65544040457701,12.3332413499042,
12.4223610424931));
#115706=CARTESIAN_POINT('Ctrl Pts',(-9.60162516479915,12.3362436200965,
12.409324579393));
#115707=CARTESIAN_POINT('Ctrl Pts',(-9.54856681285668,12.3392458902888,
12.3932336136817));
#115708=CARTESIAN_POINT('Ctrl Pts',(-9.49662818818895,12.3422481604811,
12.3742085245966));
#115709=CARTESIAN_POINT('Ctrl Pts',(-9.44466591029834,12.3452517979288,
12.3551747713493));
#115710=CARTESIAN_POINT('Ctrl Pts',(-9.39382486179272,12.3482554353765,
12.3332044409116));
#115711=CARTESIAN_POINT('Ctrl Pts',(-9.34444739335229,12.3512590728242,
12.308465907052));
#115712=CARTESIAN_POINT('Ctrl Pts',(-9.294976814621,12.3542683741823,12.2836807241406));
#115713=CARTESIAN_POINT('Ctrl Pts',(-9.24697578822731,12.3572776755404,
12.2561171737835));
#115714=CARTESIAN_POINT('Ctrl Pts',(-9.20076054257025,12.3602869768985,
12.2259888008002));
#115715=CARTESIAN_POINT('Ctrl Pts',(-9.16549904896773,12.3625830257256,
12.2030013338701));
#115716=CARTESIAN_POINT('Ctrl Pts',(-9.13127660587293,12.3648790745528,
12.1785217172341));
#115717=CARTESIAN_POINT('Ctrl Pts',(-9.09822041264864,12.3671751233799,
12.152660325437));
#115718=CARTESIAN_POINT('Ctrl Pts',(-9.05488208539472,12.3701853585509,
12.11875474371));
#115719=CARTESIAN_POINT('Ctrl Pts',(-9.01336762957972,12.3731955937218,
12.0823303949769));
#115720=CARTESIAN_POINT('Ctrl Pts',(-8.97398407865333,12.3762058288928,
12.0436108370188));
#115721=CARTESIAN_POINT('Ctrl Pts',(-8.93467048646908,12.3792107168499,
12.0049600583228));
#115722=CARTESIAN_POINT('Ctrl Pts',(-8.89748066087892,12.3822156048071,
11.9640225286445));
#115723=CARTESIAN_POINT('Ctrl Pts',(-8.86268873646129,12.3852204927643,
11.9210620716477));
#115724=CARTESIAN_POINT('Ctrl Pts',(-8.82793121307218,12.3882224095942,
11.8781440924366));
#115725=CARTESIAN_POINT('Ctrl Pts',(-8.79556722479157,12.391224326424,11.8332075565802));
#115726=CARTESIAN_POINT('Ctrl Pts',(-8.7658328626038,12.3942262432539,11.786551795479));
#115727=CARTESIAN_POINT('Ctrl Pts',(-8.73611615880286,12.3972263773313,
11.7399237418992));
#115728=CARTESIAN_POINT('Ctrl Pts',(-8.70902626901255,12.4002265114086,
11.6915789312041));
#115729=CARTESIAN_POINT('Ctrl Pts',(-8.68475652125001,12.403226645486,11.6418464314816));
#115730=CARTESIAN_POINT('Ctrl Pts',(-8.66049160320257,12.4062261825323,
11.5921238285988));
#115731=CARTESIAN_POINT('Ctrl Pts',(-8.63904594409448,12.4092257195786,
11.5410145594304));
#115732=CARTESIAN_POINT('Ctrl Pts',(-8.62056628656747,12.412225256625,11.4888710261876));
#115733=CARTESIAN_POINT('Ctrl Pts',(-8.6020696455284,12.4152275503606,11.4366795710434));
#115734=CARTESIAN_POINT('Ctrl Pts',(-8.58654462875385,12.4182298440961,
11.3834524516073));
#115735=CARTESIAN_POINT('Ctrl Pts',(-8.57408874487946,12.4212321378317,
11.3295593156331));
#115736=CARTESIAN_POINT('Ctrl Pts',(-8.56162718835348,12.4242357988702,
11.2756416356774));
#115737=CARTESIAN_POINT('Ctrl Pts',(-8.55223764071012,12.4272394599088,
11.2210578558749));
#115738=CARTESIAN_POINT('Ctrl Pts',(-8.5459662207352,12.4302431209473,11.1661866984958));
#115739=CARTESIAN_POINT('Ctrl Pts',(-8.5396829753973,12.4332524456763,11.1112120762943));
#115740=CARTESIAN_POINT('Ctrl Pts',(-8.53652963311143,12.4362617704054,
11.0559495225351));
#115741=CARTESIAN_POINT('Ctrl Pts',(-8.53650020816352,12.4392710951345,
11.0007805732336));
#115742=CARTESIAN_POINT('Ctrl Pts',(-8.53647775939356,12.4415669577729,
10.9586912871281));
#115743=CARTESIAN_POINT('Ctrl Pts',(-8.53827247435514,12.4438628204114,
10.9166565551187));
#115744=CARTESIAN_POINT('Ctrl Pts',(-8.54186145355085,12.4461586830499,
10.8748431809322));
#115745=CARTESIAN_POINT('Ctrl Pts',(-8.54656699279778,12.4491688068656,
10.8200213325592));
#115746=CARTESIAN_POINT('Ctrl Pts',(-8.55437843174097,12.4521789306813,
10.7653500779782));
#115747=CARTESIAN_POINT('Ctrl Pts',(-8.56527639107325,12.4551890544969,
10.7112086982124));
#115748=CARTESIAN_POINT('Ctrl Pts',(-8.57615499067921,12.4581938309653,
10.6571634981315));
#115749=CARTESIAN_POINT('Ctrl Pts',(-8.59010912612933,12.4611986074337,
10.603646818399));
#115750=CARTESIAN_POINT('Ctrl Pts',(-8.60706771717639,12.4642033839021,
10.5510324004254));
#115751=CARTESIAN_POINT('Ctrl Pts',(-8.62400953955768,12.4672051892456,
10.4984700076222));
#115752=CARTESIAN_POINT('Ctrl Pts',(-8.64394977128636,12.4702069945891,
10.4468086094374));
#115753=CARTESIAN_POINT('Ctrl Pts',(-8.6667668035885,12.4732087999326,10.396409498098));
#115754=CARTESIAN_POINT('Ctrl Pts',(-8.68957028651218,12.4762088227218,
10.3460403151306));
#115755=CARTESIAN_POINT('Ctrl Pts',(-8.7152469666204,12.4792088455111,10.2969324134366));
#115756=CARTESIAN_POINT('Ctrl Pts',(-8.74362695988841,12.4822088683004,
10.2494275290948));
#115757=CARTESIAN_POINT('Ctrl Pts',(-8.772001309016,12.4852082944528,10.2019320924028));
#115758=CARTESIAN_POINT('Ctrl Pts',(-8.80307763289055,12.4882077206053,
10.1560394930444));
#115759=CARTESIAN_POINT('Ctrl Pts',(-8.83664104477877,12.4912071467577,
10.112065209992));
#115760=CARTESIAN_POINT('Ctrl Pts',(-8.87023532050129,12.494209331086,10.0680504896029));
#115761=CARTESIAN_POINT('Ctrl Pts',(-8.90632093232706,12.4972115154142,
10.0259580304943));
#115762=CARTESIAN_POINT('Ctrl Pts',(-8.94464164190699,12.5002136997425,
9.986071508437));
#115763=CARTESIAN_POINT('Ctrl Pts',(-8.98297981251082,12.5032172520312,
9.9461668118855));
#115764=CARTESIAN_POINT('Ctrl Pts',(-9.02355472345282,12.5062208043198,
9.90847041614168));
#115765=CARTESIAN_POINT('Ctrl Pts',(-9.06607444964933,12.5092243566085,
9.87322792171522));
#115766=CARTESIAN_POINT('Ctrl Pts',(-9.10867438812128,12.5122335750146,
9.83791894330773));
#115767=CARTESIAN_POINT('Ctrl Pts',(-9.15322604477021,12.5152427934207,
9.80507342790123));
#115768=CARTESIAN_POINT('Ctrl Pts',(-9.19940666010578,12.5182520118268,
9.77489488038086));
#115769=CARTESIAN_POINT('Ctrl Pts',(-9.23465336534182,12.5205487554579,
9.75186152837433));
#115770=CARTESIAN_POINT('Ctrl Pts',(-9.27084833277887,12.522845499089,9.73038089439293));
#115771=CARTESIAN_POINT('Ctrl Pts',(-9.30783917747576,12.5251422427201,
9.71052505035477));
#115772=CARTESIAN_POINT('Ctrl Pts',(-9.3563219892478,12.5281525170208,9.68450057978738));
#115773=CARTESIAN_POINT('Ctrl Pts',(-9.40637636703392,12.5311627913216,
9.6611596215563));
#115774=CARTESIAN_POINT('Ctrl Pts',(-9.45767406955702,12.5341730656223,
9.64069325199602));
#115775=CARTESIAN_POINT('Ctrl Pts',(-9.50888062854282,12.537177991398,9.62026324619524));
#115776=CARTESIAN_POINT('Ctrl Pts',(-9.56132564180244,12.5401829171737,
9.60269788736832));
#115777=CARTESIAN_POINT('Ctrl Pts',(-9.61465725107809,12.5431878429494,
9.58814192786481));
#115778=CARTESIAN_POINT('Ctrl Pts',(-9.66793611391122,12.54618979677,9.57360036460944));
#115779=CARTESIAN_POINT('Ctrl Pts',(-9.7220993287952,12.5491917505907,9.56206244293968));
#115780=CARTESIAN_POINT('Ctrl Pts',(-9.77677784667349,12.5521937044113,
9.55362379711768));
#115781=CARTESIAN_POINT('Ctrl Pts',(-9.83142387686649,12.5551938745967,
9.5451901651856));
#115782=CARTESIAN_POINT('Ctrl Pts',(-9.88658408235999,12.5581940447822,
9.53985223956952));
#115783=CARTESIAN_POINT('Ctrl Pts',(-9.94187940564944,12.5611942149676,
9.53765453927181));
#115784=CARTESIAN_POINT('Ctrl Pts',(-9.99716370792009,12.5641937871832,
9.53545727700204));
#115785=CARTESIAN_POINT('Ctrl Pts',(-10.0525825471576,12.5671933593989,
9.53639901802073));
#115786=CARTESIAN_POINT('Ctrl Pts',(-10.107754256804,12.5701929316145,9.5404722441349));
#115787=CARTESIAN_POINT('Ctrl Pts',(-10.1629766392909,12.5731952588081,
9.54454921133193));
#115788=CARTESIAN_POINT('Ctrl Pts',(-10.2179509109613,12.5761975860017,
9.55176337078766));
#115789=CARTESIAN_POINT('Ctrl Pts',(-10.2722994359728,12.5791999131953,
9.56205519328144));
#115790=CARTESIAN_POINT('Ctrl Pts',(-10.3266726958133,12.5822036067931,
9.57235169973801));
#115791=CARTESIAN_POINT('Ctrl Pts',(-10.3804191279725,12.5852073003908,
9.58572853366859));
#115792=CARTESIAN_POINT('Ctrl Pts',(-10.4331734744544,12.5882109939886,
9.6020754701955));
#115793=CARTESIAN_POINT('Ctrl Pts',(-10.4860272605871,12.5912203494182,
9.61845321998747));
#115794=CARTESIAN_POINT('Ctrl Pts',(-10.5378847294422,12.5942297048479,
9.63781207111598));
#115795=CARTESIAN_POINT('Ctrl Pts',(-10.5883990198768,12.5972390602776,
9.65999296889605));
#115796=CARTESIAN_POINT('Ctrl Pts',(-10.626932065613,12.5995346409818,9.67691288485005));
#115797=CARTESIAN_POINT('Ctrl Pts',(-10.66468390458,12.601830221686,9.69547388902272));
#115798=CARTESIAN_POINT('Ctrl Pts',(-10.7015111127347,12.6041258023902,
9.71558791320317));
#115799=CARTESIAN_POINT('Ctrl Pts',(-10.7498054253778,12.6071361715651,
9.74196495944039));
#115800=CARTESIAN_POINT('Ctrl Pts',(-10.7967113092331,12.61014654074,9.77112495197029));
#115801=CARTESIAN_POINT('Ctrl Pts',(-10.8418893385065,12.6131569099149,
9.80289741805095));
#115802=CARTESIAN_POINT('Ctrl Pts',(-10.8869871444668,12.6161619335315,
9.83461346528072));
#115803=CARTESIAN_POINT('Ctrl Pts',(-10.9303627562825,12.6191669571481,
9.86893247856823));
#115804=CARTESIAN_POINT('Ctrl Pts',(-10.9717026357077,12.6221719807647,
9.90563889060391));
#115805=CARTESIAN_POINT('Ctrl Pts',(-11.0130016540376,12.6251740341608,
9.94230902134847));
#115806=CARTESIAN_POINT('Ctrl Pts',(-11.0522685330941,12.6281760875569,
9.98136152739303));
#115807=CARTESIAN_POINT('Ctrl Pts',(-11.0892214739027,12.631178140953,10.0225396014215));
#115808=CARTESIAN_POINT('Ctrl Pts',(-11.1261524784831,12.6341784122521,
10.0636932310727));
#115809=CARTESIAN_POINT('Ctrl Pts',(-11.1607719154766,12.6371786835511,
10.106969535533));
#115810=CARTESIAN_POINT('Ctrl Pts',(-11.1928353225168,12.6401789548502,
10.1520753905233));
#115811=CARTESIAN_POINT('Ctrl Pts',(-11.2248923535146,12.6431786295234,
10.1971722758853));
#115812=CARTESIAN_POINT('Ctrl Pts',(-11.254394058255,12.6461783041966,10.2440975591149));
#115813=CARTESIAN_POINT('Ctrl Pts',(-11.281138126595,12.6491779788698,10.2925274912871));
#115814=CARTESIAN_POINT('Ctrl Pts',(-11.3079067683252,12.6521804097495,
10.3410019225834));
#115815=CARTESIAN_POINT('Ctrl Pts',(-11.3319124556534,12.6551828406292,
10.3909833017));
#115816=CARTESIAN_POINT('Ctrl Pts',(-11.3529986372382,12.658185271509,10.4421228292612));
#115817=CARTESIAN_POINT('Ctrl Pts',(-11.3740944210341,12.6611890696337,
10.4932856447059));
#115818=CARTESIAN_POINT('Ctrl Pts',(-11.3922678752924,12.6641928677583,
10.5456071602774));
#115819=CARTESIAN_POINT('Ctrl Pts',(-11.4074116677767,12.667196665883,10.5987212347931));
#115820=CARTESIAN_POINT('Ctrl Pts',(-11.4225840048725,12.6702061258821,
10.6519354242983));
#115821=CARTESIAN_POINT('Ctrl Pts',(-11.4347151563662,12.6732155858811,
10.7059446405957));
#115822=CARTESIAN_POINT('Ctrl Pts',(-11.4437487361425,12.6762250458801,
10.7603714606171));
#115823=CARTESIAN_POINT('Ctrl Pts',(-11.4506370172559,12.6785198179401,
10.8018729744899));
#115824=CARTESIAN_POINT('Ctrl Pts',(-11.4557253172557,12.6808145900002,
10.8436170499894));
#115825=CARTESIAN_POINT('Ctrl Pts',(-11.4590089977681,12.6831093620602,
10.8854356319284));
#115826=CARTESIAN_POINT('Ctrl Pts',(-11.4619832499258,12.6851878927591,
10.9233135579597));
#115827=CARTESIAN_POINT('Ctrl Pts',(-11.463482683238,12.6872664234581,10.9613088817886));
#115828=CARTESIAN_POINT('Ctrl Pts',(-11.4634998508852,12.6893449541571,
10.9993393494607));
#115829=CARTESIAN_POINT('Origin',(-10.,2.67563288526385,11.));
#115830=CARTESIAN_POINT('',(-9.81114928992193,3.88681266808998,9.83748958206689));
#115831=CARTESIAN_POINT('',(-9.81122626339384,3.78734488014006,9.83776771472429));
#115832=CARTESIAN_POINT('',(-9.81114930150157,2.67563288526385,9.83748958018577));
#115833=CARTESIAN_POINT('',(-10.6734112416282,3.60000000000002,11.9662361834193));
#115834=CARTESIAN_POINT('Ctrl Pts',(-10.6734112416282,3.60000000000002,
11.9662361834193));
#115835=CARTESIAN_POINT('Ctrl Pts',(-10.6076401063727,3.60576385847941,
12.0120748951295));
#115836=CARTESIAN_POINT('Ctrl Pts',(-10.5373609849263,3.61172496704385,
12.0510783909628));
#115837=CARTESIAN_POINT('Ctrl Pts',(-10.4144644721966,3.62142732589243,
12.1037113510594));
#115838=CARTESIAN_POINT('Ctrl Pts',(-10.3638812952038,3.62524111380476,
12.1214059755054));
#115839=CARTESIAN_POINT('Ctrl Pts',(-10.2979722282098,3.62997290147053,
12.1395294144316));
#115840=CARTESIAN_POINT('Ctrl Pts',(-10.2836078761959,3.63099050025991,
12.1431891103141));
#115841=CARTESIAN_POINT('Ctrl Pts',(-10.2618160673463,3.63251449315885,
12.1483050943822));
#115842=CARTESIAN_POINT('Ctrl Pts',(-10.2544378270285,3.63302709607077,
12.1499624513958));
#115843=CARTESIAN_POINT('Ctrl Pts',(-10.2410446760205,3.63395163506925,
12.152835710273));
#115844=CARTESIAN_POINT('Ctrl Pts',(-10.2350353052688,3.63436430889171,
12.154075872025));
#115845=CARTESIAN_POINT('Ctrl Pts',(-10.2220687292935,3.63525023891689,
12.1566463198814));
#115846=CARTESIAN_POINT('Ctrl Pts',(-10.2151086336705,3.63572299786806,
12.1579609273009));
#115847=CARTESIAN_POINT('Ctrl Pts',(-10.1961522398362,3.63700333997121,
12.1613645533158));
#115848=CARTESIAN_POINT('Ctrl Pts',(-10.1841345160798,3.63780715382542,
12.1633304880455));
#115849=CARTESIAN_POINT('Ctrl Pts',(-10.1016688057958,3.64327371775184,
12.1755107717892));
#115850=CARTESIAN_POINT('Ctrl Pts',(-10.0304479196749,3.64773776334513,
12.1795070403536));
#115851=CARTESIAN_POINT('Ctrl Pts',(-9.90282463635051,3.65568177613116,
12.1750934705548));
#115852=CARTESIAN_POINT('Ctrl Pts',(-9.84657183949155,3.65916801272263,
12.1690794671231));
#115853=CARTESIAN_POINT('Ctrl Pts',(-9.77156556559751,3.66402317316801,
12.1555525135955));
#115854=CARTESIAN_POINT('Ctrl Pts',(-9.75225159375018,3.66529260520351,
12.151566126792));
#115855=CARTESIAN_POINT('Ctrl Pts',(-9.72436350978812,3.66716537113145,
12.1450760196958));
#115856=CARTESIAN_POINT('Ctrl Pts',(-9.71570263460018,3.66775261388313,
12.1429565010709));
#115857=CARTESIAN_POINT('Ctrl Pts',(-9.7020545940468,3.66868814781368,12.1394517883324));
#115858=CARTESIAN_POINT('Ctrl Pts',(-9.69705088779674,3.66903330562306,
12.1381316602287));
#115859=CARTESIAN_POINT('Ctrl Pts',(-9.68777942932785,3.66967716405612,
12.1356200994521));
#115860=CARTESIAN_POINT('Ctrl Pts',(-9.68350936349092,3.66997540477882,
12.134437468749));
#115861=CARTESIAN_POINT('Ctrl Pts',(-9.67921189070997,3.67027737596578,
12.1332210961266));
#115862=CARTESIAN_POINT('Ctrl Pts',(-9.67917762583091,3.67027978377793,
12.1332113959896));
#115863=CARTESIAN_POINT('Ctrl Pts',(-9.67910884701939,3.67028461713749,
12.1331919218409));
#115864=CARTESIAN_POINT('Ctrl Pts',(-9.67907433308936,3.67028704268642,
12.1331821478053));
#115865=CARTESIAN_POINT('Ctrl Pts',(-9.6790050452971,3.67029191228932,12.1331625227043));
#115866=CARTESIAN_POINT('Ctrl Pts',(-9.67897027143043,3.6702943563454,12.1331526716117));
#115867=CARTESIAN_POINT('Ctrl Pts',(-9.67890045257057,3.67029926375491,
12.1331328891473));
#115868=CARTESIAN_POINT('Ctrl Pts',(-9.67886540753536,3.67030172711319,
12.1331229577364));
#115869=CARTESIAN_POINT('Ctrl Pts',(-9.67879503473358,3.67030667394865,
12.1331030112644));
#115870=CARTESIAN_POINT('Ctrl Pts',(-9.67875970701393,3.67030915742452,
12.1330929961881));
#115871=CARTESIAN_POINT('Ctrl Pts',(-9.67868875696434,3.67031414533633,
12.1330728789314));
#115872=CARTESIAN_POINT('Ctrl Pts',(-9.67865313458732,3.67031664977768,
12.1330627767077));
#115873=CARTESIAN_POINT('Ctrl Pts',(-9.67533879979775,3.67054967678575,
12.1321226887629));
#115874=CARTESIAN_POINT('Ctrl Pts',(-9.67206417250361,3.67078098341316,
12.131178487239));
#115875=CARTESIAN_POINT('Ctrl Pts',(-9.66500751402686,3.67128183960506,
12.1291105628655));
#115876=CARTESIAN_POINT('Ctrl Pts',(-9.66122698629646,3.67155165318916,
12.127982035709));
#115877=CARTESIAN_POINT('Ctrl Pts',(-9.65089094831939,3.67229326949472,
12.1248399716574));
#115878=CARTESIAN_POINT('Ctrl Pts',(-9.6443473648619,3.67276712969324,12.1227881765384));
#115879=CARTESIAN_POINT('Ctrl Pts',(-9.60966774251945,3.67530036434515,
12.1115805227044));
#115880=CARTESIAN_POINT('Ctrl Pts',(-9.58186858945627,3.67740763778038,
12.101424682371));
#115881=CARTESIAN_POINT('Ctrl Pts',(-9.48585192388128,3.68489282322666,
12.0621881909969));
#115882=CARTESIAN_POINT('Ctrl Pts',(-9.42002167801562,3.69038873977898,
12.0277244434366));
#115883=CARTESIAN_POINT('Ctrl Pts',(-9.30942826949605,3.69995604767478,
11.9557952805702));
#115884=CARTESIAN_POINT('Ctrl Pts',(-9.26336755970211,3.70406427996755,
11.920765111295));
#115885=CARTESIAN_POINT('Ctrl Pts',(-9.21119894917348,3.70885796744483,
11.8746586659127));
#115886=CARTESIAN_POINT('Ctrl Pts',(-9.20245705446857,3.70966668642815,
11.8666949562687));
#115887=CARTESIAN_POINT('Ctrl Pts',(-9.18881576452309,3.7109377915769,11.8538867754581));
#115888=CARTESIAN_POINT('Ctrl Pts',(-9.18383658816349,3.71140374365305,
11.8491288346453));
#115889=CARTESIAN_POINT('Ctrl Pts',(-9.1745441962993,3.71227723601005,11.8400920687556));
#115890=CARTESIAN_POINT('Ctrl Pts',(-9.17022182017962,3.71268517283036,
11.8358230329989));
#115891=CARTESIAN_POINT('Ctrl Pts',(-9.16054712051434,3.71360208702088,
11.8261187023165));
#115892=CARTESIAN_POINT('Ctrl Pts',(-9.15521414646362,3.71411021796876,
11.8206644341121));
#115893=CARTESIAN_POINT('Ctrl Pts',(-9.13925602307237,3.71563937748437,
11.8040229477714));
#115894=CARTESIAN_POINT('Ctrl Pts',(-9.12879707964987,3.71665339554492,
11.7926781198217));
#115895=CARTESIAN_POINT('Ctrl Pts',(-9.0578900204787,3.72362113782536,11.7126658185357));
#115896=CARTESIAN_POINT('Ctrl Pts',(-9.0053987836687,3.72923080061634,11.6373651020107));
#115897=CARTESIAN_POINT('Ctrl Pts',(-8.93275267329638,3.73875081443016,
11.5019415588118));
#115898=CARTESIAN_POINT('Ctrl Pts',(-8.90774650272783,3.74262477020322,
11.4449071565028));
#115899=CARTESIAN_POINT('Ctrl Pts',(-8.88439159573,3.74732510517342,11.3776175326174));
#115900=CARTESIAN_POINT('Ctrl Pts',(-8.88152043194352,3.74792760526034,
11.3690264979567));
#115901=CARTESIAN_POINT('Ctrl Pts',(-8.8774224206772,3.74882644413533,11.3562771769473));
#115902=CARTESIAN_POINT('Ctrl Pts',(-8.87611890386585,3.74911859101242,
11.3521436193897));
#115903=CARTESIAN_POINT('Ctrl Pts',(-8.8738385102668,3.74964113752494,11.3447706619282));
#115904=CARTESIAN_POINT('Ctrl Pts',(-8.87285273439543,3.74987102315994,
11.3415341147376));
#115905=CARTESIAN_POINT('Ctrl Pts',(-8.87072507411335,3.75037612411805,
11.3344389276494));
#115906=CARTESIAN_POINT('Ctrl Pts',(-8.86958903364209,3.75065165084314,
11.3305787356789));
#115907=CARTESIAN_POINT('Ctrl Pts',(-8.86642545266812,3.75143559383312,
11.3196220878707));
#115908=CARTESIAN_POINT('Ctrl Pts',(-8.86444484894353,3.75194653329984,
11.3125124403464));
#115909=CARTESIAN_POINT('Ctrl Pts',(-8.85114196219382,3.75552080516272,
11.2629631047359));
#115910=CARTESIAN_POINT('Ctrl Pts',(-8.84213599307941,3.7586909773219,11.219941944433));
#115911=CARTESIAN_POINT('Ctrl Pts',(-8.83269062674888,3.76329180259075,
11.157635236095));
#115912=CARTESIAN_POINT('Ctrl Pts',(-8.83028727043316,3.76469292037048,
11.138680028719));
#115913=CARTESIAN_POINT('Ctrl Pts',(-8.82326021856566,3.76976943944122,
11.069883123102));
#115914=CARTESIAN_POINT('Ctrl Pts',(-8.82135327896773,3.77344464776853,
11.0198147518067));
#115915=CARTESIAN_POINT('Ctrl Pts',(-8.82389602710666,3.78059003794093,
10.9207673506824));
#115916=CARTESIAN_POINT('Ctrl Pts',(-8.8282128638355,3.78405605637047,10.8718811716616));
#115917=CARTESIAN_POINT('Ctrl Pts',(-8.83726035092925,3.78820585674591,
10.8122253443826));
#115918=CARTESIAN_POINT('Ctrl Pts',(-8.8391159757393,3.78897817884333,10.8010751132491));
#115919=CARTESIAN_POINT('Ctrl Pts',(-8.84233083340901,3.79020181309389,
10.7833381515133));
#115920=CARTESIAN_POINT('Ctrl Pts',(-8.84358641775555,3.79065635510335,
10.7767335987616));
#115921=CARTESIAN_POINT('Ctrl Pts',(-8.84607237866616,3.7915141810694,10.7642410483639));
#115922=CARTESIAN_POINT('Ctrl Pts',(-8.84729144022765,3.7919178078913,10.7583510457577));
#115923=CARTESIAN_POINT('Ctrl Pts',(-8.85016665662888,3.79283260600555,
10.7449762663465));
#115924=CARTESIAN_POINT('Ctrl Pts',(-8.85185088265918,3.79334286975461,
10.7374977499553));
#115925=CARTESIAN_POINT('Ctrl Pts',(-8.85725501843316,3.7949052449084,10.7145492858512));
#115926=CARTESIAN_POINT('Ctrl Pts',(-8.86121557739403,3.79594969632241,
10.6991374377218));
#115927=CARTESIAN_POINT('Ctrl Pts',(-8.88754244673397,3.80233108621313,
10.6046747375139));
#115928=CARTESIAN_POINT('Ctrl Pts',(-8.91781685175525,3.80739776949927,
10.5280619652498));
#115929=CARTESIAN_POINT('Ctrl Pts',(-8.98741992908515,3.81669623702062,
10.3946547690604));
#115930=CARTESIAN_POINT('Ctrl Pts',(-9.02422218429668,3.82091459929457,
10.3369642818983));
#115931=CARTESIAN_POINT('Ctrl Pts',(-9.07217578343922,3.82608973118099,
10.2745025110137));
#115932=CARTESIAN_POINT('Ctrl Pts',(-9.07865276245423,3.82678305175988,
10.2662945873173));
#115933=CARTESIAN_POINT('Ctrl Pts',(-9.08782917457149,3.82775929311212,
10.2549789445394));
#115934=CARTESIAN_POINT('Ctrl Pts',(-9.09043714978407,3.82803608529447,
10.2517972146001));
#115935=CARTESIAN_POINT('Ctrl Pts',(-9.09523664994044,3.82854441061294,
10.2460040017464));
#115936=CARTESIAN_POINT('Ctrl Pts',(-9.09742291734095,3.82877557089012,
10.2433882801904));
#115937=CARTESIAN_POINT('Ctrl Pts',(-9.10201802268148,3.82926067464093,
10.2379388065023));
#115938=CARTESIAN_POINT('Ctrl Pts',(-9.10442889576257,3.82951475253467,
10.2351070071509));
#115939=CARTESIAN_POINT('Ctrl Pts',(-9.11084169307029,3.83018932816418,
10.2276464483381));
#115940=CARTESIAN_POINT('Ctrl Pts',(-9.11486628289574,3.83061140235356,
10.2230374511281));
#115941=CARTESIAN_POINT('Ctrl Pts',(-9.13404041202692,3.8326154227512,10.2014213848871));
#115942=CARTESIAN_POINT('Ctrl Pts',(-9.14964425372815,3.83422631343528,
10.1848259370066));
#115943=CARTESIAN_POINT('Ctrl Pts',(-9.19827334595643,3.83916155418949,
10.1360227224417));
#115944=CARTESIAN_POINT('Ctrl Pts',(-9.23271799356437,3.84254378481007,
10.1052932245412));
#115945=CARTESIAN_POINT('Ctrl Pts',(-9.33839851980891,3.85243650913369,
10.0216120200536));
#115946=CARTESIAN_POINT('Ctrl Pts',(-9.41393231624312,3.85889814558944,
9.97457820044386));
#115947=CARTESIAN_POINT('Ctrl Pts',(-9.50810387707239,3.86612829135702,
9.92977771915933));
#115948=CARTESIAN_POINT('Ctrl Pts',(-9.52229686477993,3.86719855499594,
9.92336762037548));
#115949=CARTESIAN_POINT('Ctrl Pts',(-9.54364122342731,3.86878015125677,
9.91423291359118));
#115950=CARTESIAN_POINT('Ctrl Pts',(-9.55069829669737,3.86929860288262,
9.91129366537752));
#115951=CARTESIAN_POINT('Ctrl Pts',(-9.56340361954665,3.87022419007852,
9.90614652218766));
#115952=CARTESIAN_POINT('Ctrl Pts',(-9.56904119254915,3.87063215832115,
9.90391316996486));
#115953=CARTESIAN_POINT('Ctrl Pts',(-9.58108157594356,3.87149779551212,
9.89925056941802));
#115954=CARTESIAN_POINT('Ctrl Pts',(-9.58748885398772,3.87195505375524,
9.8968334157158));
#115955=CARTESIAN_POINT('Ctrl Pts',(-9.60489169103266,3.87318812541816,
9.8904409965152));
#115956=CARTESIAN_POINT('Ctrl Pts',(-9.61592614221113,3.87396042085412,
9.88657328678001));
#115957=CARTESIAN_POINT('Ctrl Pts',(-9.6793667675919,3.87834952424524,9.86539195299809));
#115958=CARTESIAN_POINT('Ctrl Pts',(-9.73288428558844,3.88184977177665,
9.85161355363714));
#115959=CARTESIAN_POINT('Ctrl Pts',(-9.79515509970242,3.88580319363651,
9.84017267140372));
#115960=CARTESIAN_POINT('Ctrl Pts',(-9.8031463758426,3.88630842190814,9.83878966160478));
#115961=CARTESIAN_POINT('Ctrl Pts',(-9.81114928987733,3.88681266881678,
9.83748958207414));
#115962=CARTESIAN_POINT('',(-9.31533557546055,3.6,11.9582951989184));
#115963=CARTESIAN_POINT('Origin',(-10.,3.6,11.));
#115964=CARTESIAN_POINT('Ctrl Pts',(-9.31533557546055,3.59999999999999,
11.9582951989184));
#115965=CARTESIAN_POINT('Ctrl Pts',(-9.27952779879854,3.60297350162211,
11.9327119435395));
#115966=CARTESIAN_POINT('Ctrl Pts',(-9.24515221848037,3.60586801722685,
11.9050602062982));
#115967=CARTESIAN_POINT('Ctrl Pts',(-9.21243262399748,3.60872903762957,
11.8755410579236));
#115968=CARTESIAN_POINT('Ctrl Pts',(-9.20893916100851,3.60903450806848,
11.872389305772));
#115969=CARTESIAN_POINT('Ctrl Pts',(-9.20546458751275,3.60933959666946,
11.8692163130887));
#115970=CARTESIAN_POINT('Ctrl Pts',(-9.202009183194,3.60964435880173,11.8660223588113));
#115971=CARTESIAN_POINT('Ctrl Pts',(-9.16664002443302,3.61276387224969,
11.8333293754465));
#115972=CARTESIAN_POINT('Ctrl Pts',(-9.13327747291354,3.6158499463446,11.7984348992447));
#115973=CARTESIAN_POINT('Ctrl Pts',(-9.10216851218451,3.61895386478193,
11.7616324235534));
#115974=CARTESIAN_POINT('Ctrl Pts',(-9.0710664844534,3.62205709147451,11.7248381497268));
#115975=CARTESIAN_POINT('Ctrl Pts',(-9.04221668982256,3.6251786225143,11.686137155056));
#115976=CARTESIAN_POINT('Ctrl Pts',(-9.01582547133837,3.62835240830818,
11.6458410771479));
#115977=CARTESIAN_POINT('Ctrl Pts',(-8.98943097752029,3.63152658799097,
11.6055399982161));
#115978=CARTESIAN_POINT('Ctrl Pts',(-8.96549540996297,3.63475327603208,
11.5636436378072));
#115979=CARTESIAN_POINT('Ctrl Pts',(-8.94418935979433,3.63804388640053,
11.5204775031662));
#115980=CARTESIAN_POINT('Ctrl Pts',(-8.92240571076791,3.64140825946741,
11.4763437515133));
#115981=CARTESIAN_POINT('Ctrl Pts',(-8.90337077504814,3.64483962474168,
11.430882655337));
#115982=CARTESIAN_POINT('Ctrl Pts',(-8.88723137466389,3.64832333332596,
11.3844550831564));
#115983=CARTESIAN_POINT('Ctrl Pts',(-8.87141311202751,3.65173772394908,
11.3389513151826));
#115984=CARTESIAN_POINT('Ctrl Pts',(-8.85837622789009,3.65520220875543,
11.2925190888577));
#115985=CARTESIAN_POINT('Ctrl Pts',(-8.8482262988994,3.65867789490675,11.2455108681042));
#115986=CARTESIAN_POINT('Ctrl Pts',(-8.83776727856803,3.66225942460567,
11.1970711265992));
#115987=CARTESIAN_POINT('Ctrl Pts',(-8.83037424426111,3.66585260042745,
11.1480194597946));
#115988=CARTESIAN_POINT('Ctrl Pts',(-8.82612410542532,3.66939078883076,
11.0987582105073));
#115989=CARTESIAN_POINT('Ctrl Pts',(-8.82236414574358,3.67252090910609,
11.0551783844478));
#115990=CARTESIAN_POINT('Ctrl Pts',(-8.8210638569035,3.67560737985468,11.0114334068894));
#115991=CARTESIAN_POINT('Ctrl Pts',(-8.82224547606375,3.67859306807471,
10.9678187462665));
#115992=CARTESIAN_POINT('Ctrl Pts',(-8.82239952161993,3.67898230685646,
10.9621327817196));
#115993=CARTESIAN_POINT('Ctrl Pts',(-8.82259570631382,3.67936983275185,
10.9564489734659));
#115994=CARTESIAN_POINT('Ctrl Pts',(-8.82283404223744,3.67975551917013,
10.9507679222468));
#115995=CARTESIAN_POINT('Ctrl Pts',(-8.82283477330836,3.67975670222352,
10.9507504962069));
#115996=CARTESIAN_POINT('Ctrl Pts',(-8.82283550477624,3.67975788526099,
10.9507330701661));
#115997=CARTESIAN_POINT('Ctrl Pts',(-8.82283623664109,3.67975906828253,
10.9507156441244));
#115998=CARTESIAN_POINT('Ctrl Pts',(-8.82459438669725,3.68260102659963,
10.9088532754429));
#115999=CARTESIAN_POINT('Ctrl Pts',(-8.82864619469332,3.68535111233409,
10.8669822558701));
#116000=CARTESIAN_POINT('Ctrl Pts',(-8.83496693962794,3.68805751581524,
10.8253750683343));
#116001=CARTESIAN_POINT('Ctrl Pts',(-8.83593848320487,3.68847350933275,
10.8189797468615));
#116002=CARTESIAN_POINT('Ctrl Pts',(-8.83696356715889,3.68888847081849,
10.8125907347874));
#116003=CARTESIAN_POINT('Ctrl Pts',(-8.83804202823939,3.68930257527402,
10.806209101972));
#116004=CARTESIAN_POINT('Ctrl Pts',(-8.84576787862284,3.69226912559685,
10.7604925330335));
#116005=CARTESIAN_POINT('Ctrl Pts',(-8.85623641748609,3.69519241554704,
10.7151495884285));
#116006=CARTESIAN_POINT('Ctrl Pts',(-8.86936170545022,3.69812844777868,
10.6705287431991));
#116007=CARTESIAN_POINT('Ctrl Pts',(-8.88247207956862,3.70106114389061,
10.6259585992117));
#116008=CARTESIAN_POINT('Ctrl Pts',(-8.89823266840009,3.70400699377354,
10.5821089164399));
#116009=CARTESIAN_POINT('Ctrl Pts',(-8.91651908517567,3.70700480847988,
10.5393068715871));
#116010=CARTESIAN_POINT('Ctrl Pts',(-8.93479319105893,3.71000060497923,
10.4965336421863));
#116011=CARTESIAN_POINT('Ctrl Pts',(-8.95558942741747,3.71304852454467,
10.4548066158049));
#116012=CARTESIAN_POINT('Ctrl Pts',(-8.9787508638237,3.71616537582486,10.4144324703729));
#116013=CARTESIAN_POINT('Ctrl Pts',(-9.00190743045923,3.71928157177648,
10.3740668137421));
#116014=CARTESIAN_POINT('Ctrl Pts',(-9.02742805929849,3.72246674823824,
10.3350534679578));
#116015=CARTESIAN_POINT('Ctrl Pts',(-9.05512640331091,3.72571352430631,
10.2976792920264));
#116016=CARTESIAN_POINT('Ctrl Pts',(-9.08285120233328,3.72896340140791,
10.2602694195857));
#116017=CARTESIAN_POINT('Ctrl Pts',(-9.11275789086444,3.73227494106182,
10.2245018907523));
#116018=CARTESIAN_POINT('Ctrl Pts',(-9.14463101029142,3.73561632063236,
10.1906444400298));
#116019=CARTESIAN_POINT('Ctrl Pts',(-9.17652206051582,3.73895957995615,
10.1567679421887));
#116020=CARTESIAN_POINT('Ctrl Pts',(-9.2103819497421,3.74233247733741,10.1248038032949));
#116021=CARTESIAN_POINT('Ctrl Pts',(-9.24596474086576,3.74568081267078,
10.0949990455823));
#116022=CARTESIAN_POINT('Ctrl Pts',(-9.27977331508401,3.74886219445818,
10.0666804024584));
#116023=CARTESIAN_POINT('Ctrl Pts',(-9.31513781804173,3.75202094745203,
10.0403110594085));
#116024=CARTESIAN_POINT('Ctrl Pts',(-9.35181713097022,3.755096123696,10.0160830257501));
#116025=CARTESIAN_POINT('Ctrl Pts',(-9.35381316437787,3.75526347019263,
10.0147645723571));
#116026=CARTESIAN_POINT('Ctrl Pts',(-9.35581309691475,3.75543056918726,
10.0134524485644));
#116027=CARTESIAN_POINT('Ctrl Pts',(-9.35781689172642,3.75559741085792,
10.0121466813497));
#116028=CARTESIAN_POINT('Ctrl Pts',(-9.37108236899922,3.75670193232758,
10.0035022706501));
#116029=CARTESIAN_POINT('Ctrl Pts',(-9.38451652038935,3.75779506837919,
9.99513677164828));
#116030=CARTESIAN_POINT('Ctrl Pts',(-9.39810704177623,3.75887372113637,
9.9870582776767));
#116031=CARTESIAN_POINT('Ctrl Pts',(-9.39812479668914,3.75887513030863,
9.98704772378014));
#116032=CARTESIAN_POINT('Ctrl Pts',(-9.39814255190346,3.75887653945831,
9.98703717035145));
#116033=CARTESIAN_POINT('Ctrl Pts',(-9.39816030741919,3.7588779485854,9.98702661739068));
#116034=CARTESIAN_POINT('Ctrl Pts',(-9.43429528423232,3.76174572080231,
9.96554985497536));
#116035=CARTESIAN_POINT('Ctrl Pts',(-9.47168294468352,3.76451995721889,
9.94601165757724));
#116036=CARTESIAN_POINT('Ctrl Pts',(-9.51007961331314,3.76724699079868,
9.92853655434178));
#116037=CARTESIAN_POINT('Ctrl Pts',(-9.51444171242871,3.76755679868544,
9.9265512744962));
#116038=CARTESIAN_POINT('Ctrl Pts',(-9.51881677961752,3.76786599735512,
9.92459261243027));
#116039=CARTESIAN_POINT('Ctrl Pts',(-9.52320441600076,3.76817465474311,
9.92266074246035));
#116040=CARTESIAN_POINT('Ctrl Pts',(-9.56617000891803,3.77119715855265,
9.90374305388122));
#116041=CARTESIAN_POINT('Ctrl Pts',(-9.61034674190773,3.77416854800187,
9.88739513018952));
#116042=CARTESIAN_POINT('Ctrl Pts',(-9.65538534121425,3.77714573714556,
9.87373501287088));
#116043=CARTESIAN_POINT('Ctrl Pts',(-9.70037163513504,3.7801194687433,9.86009075967138));
#116044=CARTESIAN_POINT('Ctrl Pts',(-9.74621750840829,3.78309947129679,
9.8491276013752));
#116045=CARTESIAN_POINT('Ctrl Pts',(-9.79257172567752,3.78612610132558,
9.84091846578863));
#116046=CARTESIAN_POINT('Ctrl Pts',(-9.79878106658418,3.78653153105245,
9.83981881780817));
#116047=CARTESIAN_POINT('Ctrl Pts',(-9.80499952754965,3.78693776780986,
9.83876852723399));
#116048=CARTESIAN_POINT('Ctrl Pts',(-9.81122626339384,3.78734488014006,
9.83776771472429));
#116049=CARTESIAN_POINT('Origin',(-10.,2.67563288526385,11.));
#116050=CARTESIAN_POINT('',(-9.811149300339,4.38555086460676,9.83748958037463));
#116051=CARTESIAN_POINT('',(-9.8111493102158,4.28736676513878,9.83748957877014));
#116052=CARTESIAN_POINT('',(-9.81114930150157,2.67563288526385,9.83748958018577));
#116053=CARTESIAN_POINT('',(-11.1777499567556,4.02542774070688,10.9996808414991));
#116054=CARTESIAN_POINT('Ctrl Pts',(-9.81114929917643,4.38555086460676,
9.83748958056349));
#116055=CARTESIAN_POINT('Ctrl Pts',(-9.80545487101009,4.38514543956214,
9.8384146447453));
#116056=CARTESIAN_POINT('Ctrl Pts',(-9.79976679208289,4.38474175459961,
9.83938162194824));
#116057=CARTESIAN_POINT('Ctrl Pts',(-9.78692347298589,4.38383350864485,
9.84166223899126));
#116058=CARTESIAN_POINT('Ctrl Pts',(-9.77977312848684,4.38333014153298,
9.84300038606684));
#116059=CARTESIAN_POINT('Ctrl Pts',(-9.76869675801355,4.38255441403126,
9.84517967357046));
#116060=CARTESIAN_POINT('Ctrl Pts',(-9.76476200914118,4.38227963686756,
9.84597475549734));
#116061=CARTESIAN_POINT('Ctrl Pts',(-9.75750962082406,4.38177473314452,
9.84747885622845));
#116062=CARTESIAN_POINT('Ctrl Pts',(-9.75419096752231,4.38154430541003,
9.84818209299985));
#116063=CARTESIAN_POINT('Ctrl Pts',(-9.74659749587188,4.38101842603738,
9.84982549592669));
#116064=CARTESIAN_POINT('Ctrl Pts',(-9.74232483650834,4.38072350940182,
9.85077516100225));
#116065=CARTESIAN_POINT('Ctrl Pts',(-9.72899561395014,4.37980626065909,
9.85381586289115));
#116066=CARTESIAN_POINT('Ctrl Pts',(-9.71995818396933,4.37918838283575,
9.85599036371886));
#116067=CARTESIAN_POINT('Ctrl Pts',(-9.69868464022037,4.37774142853516,
9.86137621560176));
#116068=CARTESIAN_POINT('Ctrl Pts',(-9.68647245263797,4.37691668853803,
9.86467820721197));
#116069=CARTESIAN_POINT('Ctrl Pts',(-9.64185725491757,4.37391737300405,
9.87751632716325));
#116070=CARTESIAN_POINT('Ctrl Pts',(-9.60981355997273,4.37178974534407,
9.88824881754348));
#116071=CARTESIAN_POINT('Ctrl Pts',(-9.50655670984423,4.36489229626578,
9.92784863789512));
#116072=CARTESIAN_POINT('Ctrl Pts',(-9.43770457338135,4.3602144759889,9.96230129870551));
#116073=CARTESIAN_POINT('Ctrl Pts',(-9.34145779412713,4.3530147533512,10.0228717509436));
#116074=CARTESIAN_POINT('Ctrl Pts',(-9.31116277054166,4.35064182712439,
10.0439872861446));
#116075=CARTESIAN_POINT('Ctrl Pts',(-9.27332396900916,4.34750361023579,
10.0730941906534));
#116076=CARTESIAN_POINT('Ctrl Pts',(-9.26482866026045,4.34678708015665,
10.0798176692303));
#116077=CARTESIAN_POINT('Ctrl Pts',(-9.25126943767698,4.34562322085544,
10.0908565306512));
#116078=CARTESIAN_POINT('Ctrl Pts',(-9.24614709463581,4.34517876993035,
10.0950993994765));
#116079=CARTESIAN_POINT('Ctrl Pts',(-9.23640694013003,4.34432427716778,
10.1033073302091));
#116080=CARTESIAN_POINT('Ctrl Pts',(-9.2317833758583,4.34391453200491,10.1072652571192));
#116081=CARTESIAN_POINT('Ctrl Pts',(-9.22119089377006,4.34296610936018,
10.116476001195));
#116082=CARTESIAN_POINT('Ctrl Pts',(-9.2152441345657,4.34242642093464,10.1217537323093));
#116083=CARTESIAN_POINT('Ctrl Pts',(-9.19654528371765,4.34070596379446,
10.1386904612228));
#116084=CARTESIAN_POINT('Ctrl Pts',(-9.1839966013592,4.33951608066461,10.1505696018073));
#116085=CARTESIAN_POINT('Ctrl Pts',(-9.15505466941829,4.3366854442535,10.1792006289783));
#116086=CARTESIAN_POINT('Ctrl Pts',(-9.13889165452325,4.33503570117327,
10.1961738314522));
#116087=CARTESIAN_POINT('Ctrl Pts',(-9.07776075066569,4.32851922481694,
10.2643298355626));
#116088=CARTESIAN_POINT('Ctrl Pts',(-9.03676492301814,4.32352042396874,
10.3188890034304));
#116089=CARTESIAN_POINT('Ctrl Pts',(-8.99207626874832,4.31732634394048,
10.3905318506115));
#116090=CARTESIAN_POINT('Ctrl Pts',(-8.9837235148132,4.31612992847146,10.4045641994645));
#116091=CARTESIAN_POINT('Ctrl Pts',(-8.95377825338545,4.31170091294788,
10.4573380693342));
#116092=CARTESIAN_POINT('Ctrl Pts',(-8.93408497720491,4.30849945875291,
10.4971203310144));
#116093=CARTESIAN_POINT('Ctrl Pts',(-8.91402582913007,4.30493808588415,
10.5441480858898));
#116094=CARTESIAN_POINT('Ctrl Pts',(-8.91142413810173,4.30446933473366,
10.5503963238662));
#116095=CARTESIAN_POINT('Ctrl Pts',(-8.90727387630822,4.3037105996848,10.5606108732897));
#116096=CARTESIAN_POINT('Ctrl Pts',(-8.90569273757954,4.30341882011965,
10.5645636637711));
#116097=CARTESIAN_POINT('Ctrl Pts',(-8.90289280166687,4.30289728397698,
10.5716749851558));
#116098=CARTESIAN_POINT('Ctrl Pts',(-8.90166615926598,4.30266707995038,
10.5748302713845));
#116099=CARTESIAN_POINT('Ctrl Pts',(-8.898980423482,4.30215919416052,10.5818279705535));
#116100=CARTESIAN_POINT('Ctrl Pts',(-8.89752782578054,4.30188189220269,
10.5856727616492));
#116101=CARTESIAN_POINT('Ctrl Pts',(-8.89332630991856,4.30107184093554,
10.5969720480115));
#116102=CARTESIAN_POINT('Ctrl Pts',(-8.89063259554763,4.30054218547111,
10.6044470240463));
#116103=CARTESIAN_POINT('Ctrl Pts',(-8.88461317093232,4.2993329879493,10.6216960735602));
#116104=CARTESIAN_POINT('Ctrl Pts',(-8.88133987583456,4.29865608503598,
10.6314878811016));
#116105=CARTESIAN_POINT('Ctrl Pts',(-8.87066887760985,4.29637706817461,
10.6648625695285));
#116106=CARTESIAN_POINT('Ctrl Pts',(-8.86388448180307,4.29480097051105,
10.6886359566033));
#116107=CARTESIAN_POINT('Ctrl Pts',(-8.8450058056344,4.28992395321358,10.7636628412607));
#116108=CARTESIAN_POINT('Ctrl Pts',(-8.83559617110343,4.2866900431747,10.8155250020107));
#116109=CARTESIAN_POINT('Ctrl Pts',(-8.82164376118859,4.27898657352759,
10.9390815398083));
#116110=CARTESIAN_POINT('Ctrl Pts',(-8.82012126194865,4.27450245348635,
11.0108945094171));
#116111=CARTESIAN_POINT('Ctrl Pts',(-8.82599352158789,4.26900289545835,
11.094626634492));
#116112=CARTESIAN_POINT('Ctrl Pts',(-8.82704228193272,4.26819402903912,
11.106843739188));
#116113=CARTESIAN_POINT('Ctrl Pts',(-8.82899219180597,4.2669121276084,11.1260365252301));
#116114=CARTESIAN_POINT('Ctrl Pts',(-8.82976542441508,4.266443053136,11.1330245355063));
#116115=CARTESIAN_POINT('Ctrl Pts',(-8.83131765988417,4.2655682196711,11.1459896534167));
#116116=CARTESIAN_POINT('Ctrl Pts',(-8.83208007518994,4.26516298945407,
11.1519685425486));
#116117=CARTESIAN_POINT('Ctrl Pts',(-8.83387341000413,4.26426069749989,
11.1652204469248));
#116118=CARTESIAN_POINT('Ctrl Pts',(-8.83492654140633,4.26376295861869,
11.1724901499563));
#116119=CARTESIAN_POINT('Ctrl Pts',(-8.83820269195217,4.26230213088745,
11.1937045942322));
#116120=CARTESIAN_POINT('Ctrl Pts',(-8.84060851107346,4.26133339870239,
11.2076193637501));
#116121=CARTESIAN_POINT('Ctrl Pts',(-8.84665416823165,4.25911022360444,
11.2391933614422));
#116122=CARTESIAN_POINT('Ctrl Pts',(-8.85045044268305,4.2578511961013,11.2568186655625));
#116123=CARTESIAN_POINT('Ctrl Pts',(-8.8647368499826,4.25352847649837,11.3164614420512));
#116124=CARTESIAN_POINT('Ctrl Pts',(-8.87713804190924,4.25041151022462,
11.3579813186815));
#116125=CARTESIAN_POINT('Ctrl Pts',(-8.9124700471894,4.24280782000833,11.4561831086075));
#116126=CARTESIAN_POINT('Ctrl Pts',(-8.93758193569904,4.23829222730713,
11.5119493863169));
#116127=CARTESIAN_POINT('Ctrl Pts',(-8.98382977446494,4.23130202306741,
11.5964357433773));
#116128=CARTESIAN_POINT('Ctrl Pts',(-9.00213631804458,4.22877654873722,
11.6265828788589));
#116129=CARTESIAN_POINT('Ctrl Pts',(-9.02574390185242,4.22582601752877,
11.6617938132694));
#116130=CARTESIAN_POINT('Ctrl Pts',(-9.02977215507508,4.22533230680293,
11.667685503268));
#116131=CARTESIAN_POINT('Ctrl Pts',(-9.03613171866395,4.22456830015571,
11.6768078484734));
#116132=CARTESIAN_POINT('Ctrl Pts',(-9.03842620214576,4.22429569710059,
11.6800637911102));
#116133=CARTESIAN_POINT('Ctrl Pts',(-9.04270708433118,4.223792787301,11.6860735121716));
#116134=CARTESIAN_POINT('Ctrl Pts',(-9.04468887530698,4.223562198274,11.6888303463048));
#116135=CARTESIAN_POINT('Ctrl Pts',(-9.04927712089132,4.22303338986309,
11.6951550845806));
#116136=CARTESIAN_POINT('Ctrl Pts',(-9.05189175856961,4.22273572961909,
11.6987169302257));
#116137=CARTESIAN_POINT('Ctrl Pts',(-9.06020220530425,4.22180087442736,
11.7099054678455));
#116138=CARTESIAN_POINT('Ctrl Pts',(-9.06597063062168,4.22116838288076,
11.7174780968593));
#116139=CARTESIAN_POINT('Ctrl Pts',(-9.10954760207446,4.21650342491617,
11.7732683308702));
#116140=CARTESIAN_POINT('Ctrl Pts',(-9.15098082921299,4.21268562450963,
11.8185461674166));
#116141=CARTESIAN_POINT('Ctrl Pts',(-9.26208594594291,4.20326369313489,
11.922400098976));
#116142=CARTESIAN_POINT('Ctrl Pts',(-9.33535583512995,4.19769536342337,
11.9765168674888));
#116143=CARTESIAN_POINT('Ctrl Pts',(-9.42743602667551,4.19077868071714,
12.0293208992469));
#116144=CARTESIAN_POINT('Ctrl Pts',(-9.44090898253159,4.1897693726546,12.0367006395394));
#116145=CARTESIAN_POINT('Ctrl Pts',(-9.46125050617425,4.18824747642119,
12.0473307419839));
#116146=CARTESIAN_POINT('Ctrl Pts',(-9.46801279460902,4.18774186355949,
12.0507817608767));
#116147=CARTESIAN_POINT('Ctrl Pts',(-9.48021841034802,4.18682959034212,
12.0568626693673));
#116148=CARTESIAN_POINT('Ctrl Pts',(-9.48564956039587,4.18642377273221,
12.0595165056753));
#116149=CARTESIAN_POINT('Ctrl Pts',(-9.49727887281609,4.18555495197049,
12.0650884758553));
#116150=CARTESIAN_POINT('Ctrl Pts',(-9.50348252534367,4.18509155510865,
12.0679945632145));
#116151=CARTESIAN_POINT('Ctrl Pts',(-9.52039978944569,4.18382788817665,
12.0757401633843));
#116152=CARTESIAN_POINT('Ctrl Pts',(-9.53116083572198,4.18302407449006,
12.0804735451495));
#116153=CARTESIAN_POINT('Ctrl Pts',(-9.59442734495721,4.17829676033138,
12.1071790349394));
#116154=CARTESIAN_POINT('Ctrl Pts',(-9.64839152900485,4.17425298666236,
12.1254795977402));
#116155=CARTESIAN_POINT('Ctrl Pts',(-9.78379292482323,4.16410761979585,
12.1607065868919));
#116156=CARTESIAN_POINT('Ctrl Pts',(-9.86610696898521,4.15793029281035,
12.173054781595));
#116157=CARTESIAN_POINT('Ctrl Pts',(-9.97235361452773,4.15030313677893,
12.1776568101523));
#116158=CARTESIAN_POINT('Ctrl Pts',(-9.9956999893063,4.14864995150201,12.1779735010678));
#116159=CARTESIAN_POINT('Ctrl Pts',(-10.0254424184894,4.1465848903847,12.1774925564826));
#116160=CARTESIAN_POINT('Ctrl Pts',(-10.0318419636709,4.14614298796184,
12.1773368809239));
#116161=CARTESIAN_POINT('Ctrl Pts',(-10.0420187736987,4.14544444745924,
12.1770062780671));
#116162=CARTESIAN_POINT('Ctrl Pts',(-10.0457969030579,4.14518603422506,
12.1768653281657));
#116163=CARTESIAN_POINT('Ctrl Pts',(-10.0530171172669,4.14469403190513,
12.1765611422393));
#116164=CARTESIAN_POINT('Ctrl Pts',(-10.0564592244019,4.14446028826536,
12.1764009913397));
#116165=CARTESIAN_POINT('Ctrl Pts',(-10.0646877867724,4.14390336015333,
12.1759819425084));
#116166=CARTESIAN_POINT('Ctrl Pts',(-10.0694735201485,4.14358094320803,
12.17570892267));
#116167=CARTESIAN_POINT('Ctrl Pts',(-10.0858958259647,4.14247928069505,
12.1746714261922));
#116168=CARTESIAN_POINT('Ctrl Pts',(-10.0975230741869,4.14170741814325,
12.1737633183833));
#116169=CARTESIAN_POINT('Ctrl Pts',(-10.1261493788268,4.13982292967059,
12.1710992177458));
#116170=CARTESIAN_POINT('Ctrl Pts',(-10.1431277476888,4.13871903408671,
12.1691456508466));
#116171=CARTESIAN_POINT('Ctrl Pts',(-10.2159797890412,4.13401900242998,
12.1591522045225));
#116172=CARTESIAN_POINT('Ctrl Pts',(-10.2712814298878,4.13054169511843,
12.1474704403719));
#116173=CARTESIAN_POINT('Ctrl Pts',(-10.396640386337,4.12247084615861,12.1114160443687));
#116174=CARTESIAN_POINT('Ctrl Pts',(-10.4656517385879,4.11787670504938,
12.0843135719998));
#116175=CARTESIAN_POINT('Ctrl Pts',(-10.5457948020873,4.11203220953603,
12.0437691246371));
#116176=CARTESIAN_POINT('Ctrl Pts',(-10.5597822849108,4.11099267488013,
12.0363347463778));
#116177=CARTESIAN_POINT('Ctrl Pts',(-10.5804132724414,4.10942774182562,
12.0248297825597));
#116178=CARTESIAN_POINT('Ctrl Pts',(-10.5871735819314,4.10890977013106,
12.0209715127674));
#116179=CARTESIAN_POINT('Ctrl Pts',(-10.5989121811411,4.10800101296404,
12.0141168655572));
#116180=CARTESIAN_POINT('Ctrl Pts',(-10.6039075189443,4.10761129297839,
12.0111500997529));
#116181=CARTESIAN_POINT('Ctrl Pts',(-10.6143983584433,4.1067863644352,12.0048140477297));
#116182=CARTESIAN_POINT('Ctrl Pts',(-10.6198885422211,4.10635086242538,
12.0014363712938));
#116183=CARTESIAN_POINT('Ctrl Pts',(-10.6310395584621,4.10545841849413,
11.994449198718));
#116184=CARTESIAN_POINT('Ctrl Pts',(-10.6366977994507,4.10500135396665,
11.9908360319024));
#116185=CARTESIAN_POINT('Ctrl Pts',(-10.6606897373317,4.10304498470337,
11.9752252038765));
#116186=CARTESIAN_POINT('Ctrl Pts',(-10.678716563024,4.10152885166098,11.962766245634));
#116187=CARTESIAN_POINT('Ctrl Pts',(-10.7224338747785,4.09773325429489,
11.9307135440793));
#116188=CARTESIAN_POINT('Ctrl Pts',(-10.7476844619221,4.09543416873777,
11.9105526019979));
#116189=CARTESIAN_POINT('Ctrl Pts',(-10.8100300577425,4.08948330359305,
11.856430301704));
#116190=CARTESIAN_POINT('Ctrl Pts',(-10.845836857643,4.08579465355212,11.8210852615673));
#116191=CARTESIAN_POINT('Ctrl Pts',(-10.892426778849,4.0806563535634,11.7688044794737));
#116192=CARTESIAN_POINT('Ctrl Pts',(-10.9052058306496,4.07920711827698,
11.7537163328523));
#116193=CARTESIAN_POINT('Ctrl Pts',(-10.944762803722,4.07460365869485,11.7045536827577));
#116194=CARTESIAN_POINT('Ctrl Pts',(-10.9700457849697,4.07147820234942,
11.6693165612151));
#116195=CARTESIAN_POINT('Ctrl Pts',(-10.9969598285936,4.06798891737618,
11.6270660075567));
#116196=CARTESIAN_POINT('Ctrl Pts',(-11.0005394935001,4.06752115665813,
11.6213383980434));
#116197=CARTESIAN_POINT('Ctrl Pts',(-11.0062928316159,4.06676368168116,
11.6119541561829));
#116198=CARTESIAN_POINT('Ctrl Pts',(-11.008496258779,4.06647218167176,11.6083160771185));
#116199=CARTESIAN_POINT('Ctrl Pts',(-11.0124173277992,4.06595102056128,
11.6017621358257));
#116200=CARTESIAN_POINT('Ctrl Pts',(-11.0141421545963,4.06572091325328,
11.5988507367367));
#116201=CARTESIAN_POINT('Ctrl Pts',(-11.0179340359284,4.06521313529474,
11.5923869106844));
#116202=CARTESIAN_POINT('Ctrl Pts',(-11.0199950612416,4.06493584523101,
11.5888310706609));
#116203=CARTESIAN_POINT('Ctrl Pts',(-11.0259907951662,4.06412512457036,
11.5783608212627));
#116204=CARTESIAN_POINT('Ctrl Pts',(-11.0298742034711,4.06359480158102,
11.5714170848397));
#116205=CARTESIAN_POINT('Ctrl Pts',(-11.0386439438995,4.06238370640867,
11.555356460268));
#116206=CARTESIAN_POINT('Ctrl Pts',(-11.0434811955834,4.06170558964388,
11.546213374679));
#116207=CARTESIAN_POINT('Ctrl Pts',(-11.0595015775335,4.05942054711805,
11.5149428099191));
#116208=CARTESIAN_POINT('Ctrl Pts',(-11.0701068433932,4.0578398256393,11.492525321489));
#116209=CARTESIAN_POINT('Ctrl Pts',(-11.1201943011912,4.04992573185198,
11.3773791993501));
#116210=CARTESIAN_POINT('Ctrl Pts',(-11.1483650778436,4.04386800583311,
11.2801948813759));
#116211=CARTESIAN_POINT('Ctrl Pts',(-11.1681788572242,4.03561089019528,
11.1525166453065));
#116212=CARTESIAN_POINT('Ctrl Pts',(-11.171519394874,4.03376973216029,11.1242790148007));
#116213=CARTESIAN_POINT('Ctrl Pts',(-11.1746240567457,4.03125916748005,
11.0862970819995));
#116214=CARTESIAN_POINT('Ctrl Pts',(-11.1752939629511,4.030617621944,11.0766351909747));
#116215=CARTESIAN_POINT('Ctrl Pts',(-11.1762130665869,4.02954069067114,
11.0604968952244));
#116216=CARTESIAN_POINT('Ctrl Pts',(-11.1765281092073,4.02910735124556,
11.0540246031525));
#116217=CARTESIAN_POINT('Ctrl Pts',(-11.1770223572,4.02828553752146,11.0417927600797));
#116218=CARTESIAN_POINT('Ctrl Pts',(-11.1772127357043,4.02789742129255,
11.0360338314944));
#116219=CARTESIAN_POINT('Ctrl Pts',(-11.1774846441397,4.02718247833615,
11.0254592063782));
#116220=CARTESIAN_POINT('Ctrl Pts',(-11.1775789082012,4.02685605452467,
11.0206439371467));
#116221=CARTESIAN_POINT('Ctrl Pts',(-11.1777160192758,4.02616263411095,
11.0104427075363));
#116222=CARTESIAN_POINT('Ctrl Pts',(-11.1777514162835,4.02579609702368,
11.005066751442));
#116223=CARTESIAN_POINT('Ctrl Pts',(-11.1777499567556,4.02542774070688,
10.9996808414991));
#116224=CARTESIAN_POINT('Ctrl Pts',(-9.81114928987733,3.88681266881678,
9.83748958207414));
#116225=CARTESIAN_POINT('Ctrl Pts',(-9.88349677129376,3.89137113260811,
9.82573667815999));
#116226=CARTESIAN_POINT('Ctrl Pts',(-9.95679594885871,3.89583947364135,
9.82076101815262));
#116227=CARTESIAN_POINT('Ctrl Pts',(-10.0557717545651,3.90216350620044,
9.82329087899932));
#116228=CARTESIAN_POINT('Ctrl Pts',(-10.0814191107826,3.90382968482452,
9.82478701936196));
#116229=CARTESIAN_POINT('Ctrl Pts',(-10.1135968970998,3.90597745380489,
9.82772240575238));
#116230=CARTESIAN_POINT('Ctrl Pts',(-10.1201936102639,3.90642081265862,
9.82838039276763));
#116231=CARTESIAN_POINT('Ctrl Pts',(-10.1306026787047,3.90712571284111,
9.8295074736127));
#116232=CARTESIAN_POINT('Ctrl Pts',(-10.1344190160324,3.9073852855184,9.82993959938407));
#116233=CARTESIAN_POINT('Ctrl Pts',(-10.1416463850623,3.90787912410904,
9.83079378323193));
#116234=CARTESIAN_POINT('Ctrl Pts',(-10.1450577569216,3.90811318665105,
9.8312121143408));
#116235=CARTESIAN_POINT('Ctrl Pts',(-10.1531336324011,3.90866954160889,
9.83223834608793));
#116236=CARTESIAN_POINT('Ctrl Pts',(-10.1577963712204,3.90899253410569,
9.83285926596049));
#116237=CARTESIAN_POINT('Ctrl Pts',(-10.1734576679684,3.9100830910275,9.8350403857033));
#116238=CARTESIAN_POINT('Ctrl Pts',(-10.184437452998,3.91085709087615,9.83672820493649));
#116239=CARTESIAN_POINT('Ctrl Pts',(-10.2111738021389,3.91276231090104,
9.84122615332461));
#116240=CARTESIAN_POINT('Ctrl Pts',(-10.2268998435754,3.91390039852764,
9.84420260811822));
#116241=CARTESIAN_POINT('Ctrl Pts',(-10.2915134748616,3.91863642102911,
9.85780141887378));
#116242=CARTESIAN_POINT('Ctrl Pts',(-10.3397587807551,3.92231293604581,
9.87121251672868));
#116243=CARTESIAN_POINT('Ctrl Pts',(-10.4650451089811,3.93204512346644,
9.91480141214939));
#116244=CARTESIAN_POINT('Ctrl Pts',(-10.5400267401995,3.93804672012161,
9.95009587472389));
#116245=CARTESIAN_POINT('Ctrl Pts',(-10.6240429857011,3.94486345101177,
10.001046171468));
#116246=CARTESIAN_POINT('Ctrl Pts',(-10.6372197382432,3.94593633977283,
10.0093994523147));
#116247=CARTESIAN_POINT('Ctrl Pts',(-10.656745890261,3.94753269362524,10.0223287759564));
#116248=CARTESIAN_POINT('Ctrl Pts',(-10.6632215581862,3.94806321378293,
10.0267100347006));
#116249=CARTESIAN_POINT('Ctrl Pts',(-10.6745214962456,3.94899108805173,
10.0345204115596));
#116250=CARTESIAN_POINT('Ctrl Pts',(-10.6793643800589,3.94938945100427,
10.0379219751546));
#116251=CARTESIAN_POINT('Ctrl Pts',(-10.6851221326266,3.9498639694129,10.0420312837205));
#116252=CARTESIAN_POINT('Ctrl Pts',(-10.6860617836726,3.94994143856181,
10.0427040024187));
#116253=CARTESIAN_POINT('Ctrl Pts',(-10.6872928275471,3.95004296998422,
10.0435880797069));
#116254=CARTESIAN_POINT('Ctrl Pts',(-10.6875851131722,3.95006707934939,
10.0437981885497));
#116255=CARTESIAN_POINT('Ctrl Pts',(-10.6880907464622,3.95010879179155,
10.0441620135825));
#116256=CARTESIAN_POINT('Ctrl Pts',(-10.6883041389346,3.95012639722791,
10.0443156671937));
#116257=CARTESIAN_POINT('Ctrl Pts',(-10.6886801993407,3.95015742590001,
10.0445866414159));
#116258=CARTESIAN_POINT('Ctrl Pts',(-10.6888428887337,3.95017085026404,
10.0447039320891));
#116259=CARTESIAN_POINT('Ctrl Pts',(-10.6891333126216,3.95019481627762,
10.0449134255197));
#116260=CARTESIAN_POINT('Ctrl Pts',(-10.6892610585642,3.95020535852866,
10.0450056123388));
#116261=CARTESIAN_POINT('Ctrl Pts',(-10.6894912719451,3.95022435791724,
10.0451718142046));
#116262=CARTESIAN_POINT('Ctrl Pts',(-10.689593745944,3.95023281539887,10.045245820102));
#116263=CARTESIAN_POINT('Ctrl Pts',(-10.6897797545735,3.95024816788882,
10.0453801996064));
#116264=CARTESIAN_POINT('Ctrl Pts',(-10.6898632931567,3.9502550631036,10.0454405676555));
#116265=CARTESIAN_POINT('Ctrl Pts',(-10.6901667489168,3.95028011098889,
10.0456599165769));
#116266=CARTESIAN_POINT('Ctrl Pts',(-10.6903866192063,3.95029826120068,
10.0458189625864));
#116267=CARTESIAN_POINT('Ctrl Pts',(-10.6908199238057,3.95033403359993,
10.0461326272305));
#116268=CARTESIAN_POINT('Ctrl Pts',(-10.6910333612235,3.95035165595002,
10.0462872415463));
#116269=CARTESIAN_POINT('Ctrl Pts',(-10.6914553316493,3.95038649882012,
10.0465931334396));
#116270=CARTESIAN_POINT('Ctrl Pts',(-10.6916638669528,3.9504037194599,10.0467444078197));
#116271=CARTESIAN_POINT('Ctrl Pts',(-10.6920773636549,3.95043786859194,
10.0470445711401));
#116272=CARTESIAN_POINT('Ctrl Pts',(-10.6922823266804,3.95045479716884,
10.0471934578084));
#116273=CARTESIAN_POINT('Ctrl Pts',(-10.6926898585311,3.95048845947975,
10.0474896928989));
#116274=CARTESIAN_POINT('Ctrl Pts',(-10.6928924283992,3.95050519326737,
10.0476370398252));
#116275=CARTESIAN_POINT('Ctrl Pts',(-10.6932962410866,3.95053855407357,
10.0479309654342));
#116276=CARTESIAN_POINT('Ctrl Pts',(-10.6934974844736,3.95055518112166,
10.0480775433299));
#116277=CARTESIAN_POINT('Ctrl Pts',(-10.6938996286883,3.95058840975273,
10.048370644822));
#116278=CARTESIAN_POINT('Ctrl Pts',(-10.6941005296231,3.95060501134102,
10.048517168254));
#116279=CARTESIAN_POINT('Ctrl Pts',(-10.7007537293004,3.95115485020022,
10.0533727866245));
#116280=CARTESIAN_POINT('Ctrl Pts',(-10.7071581274307,3.95168559241107,
10.0581474328468));
#116281=CARTESIAN_POINT('Ctrl Pts',(-10.7209565705541,3.95283265037311,
10.0686546256902));
#116282=CARTESIAN_POINT('Ctrl Pts',(-10.7283319256506,3.95344802524244,
10.074410891923));
#116283=CARTESIAN_POINT('Ctrl Pts',(-10.7960459972145,3.9591219023593,10.1285704971005));
#116284=CARTESIAN_POINT('Ctrl Pts',(-10.8515500481824,3.96393471929509,
10.182722035206));
#116285=CARTESIAN_POINT('Ctrl Pts',(-10.9515581345386,3.97354827509237,
10.3016323791841));
#116286=CARTESIAN_POINT('Ctrl Pts',(-10.9957055578151,3.97832990072858,
10.3661647284829));
#116287=CARTESIAN_POINT('Ctrl Pts',(-11.0374477373467,3.98405328936284,
10.4424360415357));
#116288=CARTESIAN_POINT('Ctrl Pts',(-11.0416601558663,3.98464777027854,
10.4503460328993));
#116289=CARTESIAN_POINT('Ctrl Pts',(-11.0478039464498,3.98554170978516,
10.46220702612));
#116290=CARTESIAN_POINT('Ctrl Pts',(-11.0498042306579,3.98583719558249,
10.4661222342895));
#116291=CARTESIAN_POINT('Ctrl Pts',(-11.0532130063567,3.98634863627746,
10.4728875523748));
#116292=CARTESIAN_POINT('Ctrl Pts',(-11.0546319832116,3.98656395539278,
10.4757323693199));
#116293=CARTESIAN_POINT('Ctrl Pts',(-11.0576048632744,3.98702029580721,
10.4817534188943));
#116294=CARTESIAN_POINT('Ctrl Pts',(-11.0591560020607,3.98726148842192,
10.4849309484457));
#116295=CARTESIAN_POINT('Ctrl Pts',(-11.0629922828051,3.98786570642831,
10.4928802300873));
#116296=CARTESIAN_POINT('Ctrl Pts',(-11.0652596017972,3.98822978142213,
10.4976604410803));
#116297=CARTESIAN_POINT('Ctrl Pts',(-11.0738711780948,3.98963936841443,
10.5161368061777));
#116298=CARTESIAN_POINT('Ctrl Pts',(-11.0799838123693,3.99069730366133,
10.5299385045099));
#116299=CARTESIAN_POINT('Ctrl Pts',(-11.0952951204919,3.99349717016018,
10.566386109816));
#116300=CARTESIAN_POINT('Ctrl Pts',(-11.1040567912271,3.99525618840401,
10.5892070366145));
#116301=CARTESIAN_POINT('Ctrl Pts',(-11.1515590930124,4.00573336330964,
10.7254592861947));
#116302=CARTESIAN_POINT('Ctrl Pts',(-11.1735195827319,4.01465078658567,
10.8440340662471));
#116303=CARTESIAN_POINT('Ctrl Pts',(-11.1775622213838,4.02379012574538,
10.9758185091774));
#116304=CARTESIAN_POINT('Ctrl Pts',(-11.1777467220233,4.02461135750004,
10.9877441209098));
#116305=CARTESIAN_POINT('Ctrl Pts',(-11.1777499567556,4.0254277407069,10.9996808414993));
#116306=CARTESIAN_POINT('Ctrl Pts',(-9.8111909408254,3.78717977191134,9.83748281661147));
#116307=CARTESIAN_POINT('Ctrl Pts',(-9.83186521214867,3.7885115074803,9.834125025627));
#116308=CARTESIAN_POINT('Ctrl Pts',(-9.85262448211808,3.78985562457532,
9.83131948339227));
#116309=CARTESIAN_POINT('Ctrl Pts',(-9.88706949073275,3.79210489619596,
9.82759669487098));
#116310=CARTESIAN_POINT('Ctrl Pts',(-9.90071644216444,3.79300093351796,
9.82636225320016));
#116311=CARTESIAN_POINT('Ctrl Pts',(-9.92174634108278,3.79439080007871,
9.82482939198034));
#116312=CARTESIAN_POINT('Ctrl Pts',(-9.9291160318592,3.7948795703048,9.82436185323403));
#116313=CARTESIAN_POINT('Ctrl Pts',(-9.94236646803447,3.79576166591126,
9.82364627853993));
#116314=CARTESIAN_POINT('Ctrl Pts',(-9.94824564369183,3.79615421610068,
9.82337296201398));
#116315=CARTESIAN_POINT('Ctrl Pts',(-9.96023251616122,3.79695707231853,
9.82290571771047));
#116316=CARTESIAN_POINT('Ctrl Pts',(-9.96634015948064,3.79736747038934,
9.82271523625787));
#116317=CARTESIAN_POINT('Ctrl Pts',(-9.97952660612457,3.79825649510429,
9.82240668148574));
#116318=CARTESIAN_POINT('Ctrl Pts',(-9.98660551401167,3.7987356005114,9.82230489187658));
#116319=CARTESIAN_POINT('Ctrl Pts',(-10.0058511252984,3.80004337939542,
9.82220169339636));
#116320=CARTESIAN_POINT('Ctrl Pts',(-10.0180173466603,3.80087578069572,
9.82232498409029));
#116321=CARTESIAN_POINT('Ctrl Pts',(-10.0741072111654,3.80474078510826,
9.82376272344821));
#116322=CARTESIAN_POINT('Ctrl Pts',(-10.117932753502,3.80784007236256,9.82734614125115));
#116323=CARTESIAN_POINT('Ctrl Pts',(-10.2113651647645,3.81461086318063,
9.84027635675216));
#116324=CARTESIAN_POINT('Ctrl Pts',(-10.2607815333187,3.81829339099118,
9.85037980365581));
#116325=CARTESIAN_POINT('Ctrl Pts',(-10.3613839702597,3.82591219044261,
9.87777016555957));
#116326=CARTESIAN_POINT('Ctrl Pts',(-10.4123440190162,3.82983964485881,
9.89547676947773));
#116327=CARTESIAN_POINT('Ctrl Pts',(-10.4733288341233,3.83450474199927,
9.92147841532427));
#116328=CARTESIAN_POINT('Ctrl Pts',(-10.4846646379504,3.83537017676505,
9.92652470365892));
#116329=CARTESIAN_POINT('Ctrl Pts',(-10.5004474527437,3.8365706688864,9.93385163564893));
#116330=CARTESIAN_POINT('Ctrl Pts',(-10.5049624889999,3.83691357885045,
9.9359826718283));
#116331=CARTESIAN_POINT('Ctrl Pts',(-10.5126639505387,3.83749743631072,
9.93967772180947));
#116332=CARTESIAN_POINT('Ctrl Pts',(-10.5158570621624,3.83773919705357,
9.94122752583201));
#116333=CARTESIAN_POINT('Ctrl Pts',(-10.522458568816,3.8382382946786,9.94446857791479));
#116334=CARTESIAN_POINT('Ctrl Pts',(-10.5258658785043,3.83849549664795,
9.94616195839164));
#116335=CARTESIAN_POINT('Ctrl Pts',(-10.5349834121951,3.83918281232974,
9.95074846363894));
#116336=CARTESIAN_POINT('Ctrl Pts',(-10.5406784547341,3.83961114925493,
9.95367172887309));
#116337=CARTESIAN_POINT('Ctrl Pts',(-10.5665603782186,3.84155459203336,
9.96722466872166));
#116338=CARTESIAN_POINT('Ctrl Pts',(-10.5864610197276,3.84304000166565,
9.97839382371818));
#116339=CARTESIAN_POINT('Ctrl Pts',(-10.6783304987106,3.84991411205333,
10.0335252472169));
#116340=CARTESIAN_POINT('Ctrl Pts',(-10.7457712080805,3.85502528071217,
10.0845583553547));
#116341=CARTESIAN_POINT('Ctrl Pts',(-10.8340688279533,3.86259828256421,
10.1676617182122));
#116342=CARTESIAN_POINT('Ctrl Pts',(-10.8597446359299,3.8649268438506,10.1942105265188));
#116343=CARTESIAN_POINT('Ctrl Pts',(-10.8948844204761,3.86834897734536,
10.2341397514795));
#116344=CARTESIAN_POINT('Ctrl Pts',(-10.9053837716029,3.86940476758947,
10.2465809705057));
#116345=CARTESIAN_POINT('Ctrl Pts',(-10.9237564351787,3.87131702108456,
10.269290486496));
#116346=CARTESIAN_POINT('Ctrl Pts',(-10.931724872412,3.87216973914192,10.2794786016404));
#116347=CARTESIAN_POINT('Ctrl Pts',(-10.9427397837941,3.8733832540482,10.2940501381976));
#116348=CARTESIAN_POINT('Ctrl Pts',(-10.9459269194831,3.87373865916736,
10.2983264514276));
#116349=CARTESIAN_POINT('Ctrl Pts',(-10.952649409716,3.87449758863686,10.307475340365));
#116350=CARTESIAN_POINT('Ctrl Pts',(-10.9561766589285,3.87490140514236,
10.3123536543578));
#116351=CARTESIAN_POINT('Ctrl Pts',(-10.9634925728257,3.87575097777854,
10.3226369581759));
#116352=CARTESIAN_POINT('Ctrl Pts',(-10.9672734983907,3.87619700656133,
10.3280471708622));
#116353=CARTESIAN_POINT('Ctrl Pts',(-10.9769538047166,3.87735740709784,
10.3421499515712));
#116354=CARTESIAN_POINT('Ctrl Pts',(-10.9827826040734,3.87807436143261,
10.3508900219928));
#116355=CARTESIAN_POINT('Ctrl Pts',(-11.0066657026378,3.88109069429384,
10.3877610734617));
#116356=CARTESIAN_POINT('Ctrl Pts',(-11.0236336006712,3.88342865802187,
10.4165737312155));
#116357=CARTESIAN_POINT('Ctrl Pts',(-11.0771850887938,3.8915228856007,10.5170530409613));
#116358=CARTESIAN_POINT('Ctrl Pts',(-11.107642603271,3.89745749333156,10.5917225107488));
#116359=CARTESIAN_POINT('Ctrl Pts',(-11.1433600988057,3.90675989727036,
10.7136488065752));
#116360=CARTESIAN_POINT('Ctrl Pts',(-11.153801180218,3.91014559080387,10.7591410248119));
#116361=CARTESIAN_POINT('Ctrl Pts',(-11.1632088270509,3.91413436228698,
10.815216993787));
#116362=CARTESIAN_POINT('Ctrl Pts',(-11.1647687354342,3.91484568831707,
10.8253193047656));
#116363=CARTESIAN_POINT('Ctrl Pts',(-11.166832552659,3.91586385921513,10.8399451733449));
#116364=CARTESIAN_POINT('Ctrl Pts',(-11.1674420302284,3.91617607419578,
10.844453025549));
#116365=CARTESIAN_POINT('Ctrl Pts',(-11.1684620266461,3.9167194859728,10.8523411103658));
#116366=CARTESIAN_POINT('Ctrl Pts',(-11.1688840285047,3.91695130494591,
10.8557197707956));
#116367=CARTESIAN_POINT('Ctrl Pts',(-11.1697552092392,3.91744530509341,
10.8629494835501));
#116368=CARTESIAN_POINT('Ctrl Pts',(-11.1702000314669,3.91770724526915,
10.8668009720451));
#116369=CARTESIAN_POINT('Ctrl Pts',(-11.1713649764337,3.91842110390037,
10.8773441786168));
#116370=CARTESIAN_POINT('Ctrl Pts',(-11.1720467854851,3.9188709643508,10.8840401084514));
#116371=CARTESIAN_POINT('Ctrl Pts',(-11.1753451866422,3.92123264997068,
10.9194419065752));
#116372=CARTESIAN_POINT('Ctrl Pts',(-11.1769649244369,3.92309530461378,
10.9482333235354));
#116373=CARTESIAN_POINT('Ctrl Pts',(-11.1776763809832,3.92541691352806,
10.9847492214321));
#116374=CARTESIAN_POINT('Ctrl Pts',(-11.177750876702,3.92590372022819,10.992442162376));
#116375=CARTESIAN_POINT('Ctrl Pts',(-11.1777430102078,3.93021726774146,
11.0608648101056));
#116376=CARTESIAN_POINT('Ctrl Pts',(-11.1730389131068,3.93393105739488,
11.1215049712384));
#116377=CARTESIAN_POINT('Ctrl Pts',(-11.1570204480465,3.94038268400652,
11.2241987308866));
#116378=CARTESIAN_POINT('Ctrl Pts',(-11.1480193233025,3.94308672030422,
11.2664818720717));
#116379=CARTESIAN_POINT('Ctrl Pts',(-11.1320140660241,3.94700495076092,
11.3255183492424));
#116380=CARTESIAN_POINT('Ctrl Pts',(-11.1269153687118,3.94816629037035,
11.3427531794665));
#116381=CARTESIAN_POINT('Ctrl Pts',(-11.1171263907553,3.95025805637157,
11.3732580411187));
#116382=CARTESIAN_POINT('Ctrl Pts',(-11.1125887803687,3.95118365892871,
11.3865735589111));
#116383=CARTESIAN_POINT('Ctrl Pts',(-11.105334780562,3.95260161186483,11.4066736046932));
#116384=CARTESIAN_POINT('Ctrl Pts',(-11.1027918428489,3.95308826751543,
11.4135197034856));
#116385=CARTESIAN_POINT('Ctrl Pts',(-11.0980496638493,3.95397754490102,
11.4259316954146));
#116386=CARTESIAN_POINT('Ctrl Pts',(-11.0958713410895,3.95437946012569,
11.4315053591154));
#116387=CARTESIAN_POINT('Ctrl Pts',(-11.0910640770182,3.95525260093537,
11.443534468164));
#116388=CARTESIAN_POINT('Ctrl Pts',(-11.0884201273098,3.95572431708372,
11.4499836301975));
#116389=CARTESIAN_POINT('Ctrl Pts',(-11.08101985291,3.95702204152894,11.4675876270796));
#116390=CARTESIAN_POINT('Ctrl Pts',(-11.0761483594504,3.95785189837919,
11.4786928040614));
#116391=CARTESIAN_POINT('Ctrl Pts',(-11.0401596144436,3.96381649619392,
11.5574066444271));
#116392=CARTESIAN_POINT('Ctrl Pts',(-11.0028724648894,3.96916563896348,
11.6219945973047));
#116393=CARTESIAN_POINT('Ctrl Pts',(-10.9258839014303,3.97888923270412,
11.7302384326686));
#116394=CARTESIAN_POINT('Ctrl Pts',(-10.8885208976615,3.98320876028655,
11.7752677248567));
#116395=CARTESIAN_POINT('Ctrl Pts',(-10.8341149077159,3.98887156766593,
11.8317126598989));
#116396=CARTESIAN_POINT('Ctrl Pts',(-10.8198960780281,3.99030071147375,
11.8457329023861));
#116397=CARTESIAN_POINT('Ctrl Pts',(-10.7958032856493,3.99263095797866,
11.8683101630334));
#116398=CARTESIAN_POINT('Ctrl Pts',(-10.7861314861791,3.99354336405576,
11.8770762399197));
#116399=CARTESIAN_POINT('Ctrl Pts',(-10.7725682825127,3.99478913154316,
11.888964645294));
#116400=CARTESIAN_POINT('Ctrl Pts',(-10.7688002029142,3.99513171897993,
11.8922253874352));
#116401=CARTESIAN_POINT('Ctrl Pts',(-10.7623799425228,3.99570936039403,
11.8977103457199));
#116402=CARTESIAN_POINT('Ctrl Pts',(-10.7597384802511,3.99594529330754,
11.8999469342664));
#116403=CARTESIAN_POINT('Ctrl Pts',(-10.7546082460949,3.99640015180379,
11.9042521382106));
#116404=CARTESIAN_POINT('Ctrl Pts',(-10.7521207870267,3.99661918853367,
11.9063221595514));
#116405=CARTESIAN_POINT('Ctrl Pts',(-10.7453469787629,3.99721168901267,
11.9119121150621));
#116406=CARTESIAN_POINT('Ctrl Pts',(-10.7410441795162,3.99758376244596,
11.9154121210513));
#116407=CARTESIAN_POINT('Ctrl Pts',(-10.7244881757141,3.99899978997435,
11.928685956909));
#116408=CARTESIAN_POINT('Ctrl Pts',(-10.7120644240592,4.00002999623509,
11.9382457230221));
#116409=CARTESIAN_POINT('Ctrl Pts',(-10.6045503425333,4.00870883020965,
12.017608941363));
#116410=CARTESIAN_POINT('Ctrl Pts',(-10.4996539969478,4.01569141676283,
12.0730154839968));
#116411=CARTESIAN_POINT('Ctrl Pts',(-10.3665711596204,4.02464398416576,
12.1194858060677));
#116412=CARTESIAN_POINT('Ctrl Pts',(-10.3446652118292,4.02611776764204,
12.1264229571339));
#116413=CARTESIAN_POINT('Ctrl Pts',(-10.3061921711463,4.028717265921,12.1373792034351));
#116414=CARTESIAN_POINT('Ctrl Pts',(-10.2897144266052,4.02983405907228,
12.1416876111871));
#116415=CARTESIAN_POINT('Ctrl Pts',(-10.2654488487225,4.03148651947439,
12.1474731568581));
#116416=CARTESIAN_POINT('Ctrl Pts',(-10.2577298298946,4.03201331974995,
12.1492315113542));
#116417=CARTESIAN_POINT('Ctrl Pts',(-10.2440393658826,4.03294994497636,
12.1522052676661));
#116418=CARTESIAN_POINT('Ctrl Pts',(-10.2380750565669,4.03335875468874,
12.1534524073436));
#116419=CARTESIAN_POINT('Ctrl Pts',(-10.2255402103787,4.03421965523097,
12.1559720866541));
#116420=CARTESIAN_POINT('Ctrl Pts',(-10.2189679853552,4.03467203196904,
12.1572350106314));
#116421=CARTESIAN_POINT('Ctrl Pts',(-10.2015867673294,4.03587120292094,
12.1604216342817));
#116422=CARTESIAN_POINT('Ctrl Pts',(-10.1907612396291,4.03662092966357,
12.1622502869132));
#116423=CARTESIAN_POINT('Ctrl Pts',(-10.1426754265992,4.03996470536645,
12.1696830679689));
#116424=CARTESIAN_POINT('Ctrl Pts',(-10.1051879882529,4.0426084945087,12.1736480340791));
#116425=CARTESIAN_POINT('Ctrl Pts',(-9.99097281550542,4.050776290538,12.1802124228883));
#116426=CARTESIAN_POINT('Ctrl Pts',(-9.91412559701792,4.05643861130657,
12.1771177991398));
#116427=CARTESIAN_POINT('Ctrl Pts',(-9.80579576437694,4.06442957565171,
12.1620868177153));
#116428=CARTESIAN_POINT('Ctrl Pts',(-9.77365439540717,4.06679896948399,
12.1562564600043));
#116429=CARTESIAN_POINT('Ctrl Pts',(-9.7297091024715,4.07000503987318,12.1463818460743));
#116430=CARTESIAN_POINT('Ctrl Pts',(-9.71766628242738,4.07088005807052,
12.1434754936989));
#116431=CARTESIAN_POINT('Ctrl Pts',(-9.69680930490211,4.07238680119161,
12.1380923630375));
#116432=CARTESIAN_POINT('Ctrl Pts',(-9.68797417263657,4.07302232170028,
12.1357018623852));
#116433=CARTESIAN_POINT('Ctrl Pts',(-9.67497246707904,4.07395260489652,
12.1320208363953));
#116434=CARTESIAN_POINT('Ctrl Pts',(-9.67078400202692,4.07425153067137,
12.1308098422755));
#116435=CARTESIAN_POINT('Ctrl Pts',(-9.66334157587681,4.07478121149281,
12.128613187214));
#116436=CARTESIAN_POINT('Ctrl Pts',(-9.66008504401674,4.07501246863267,
12.1276366633906));
#116437=CARTESIAN_POINT('Ctrl Pts',(-9.65296184841235,4.07551717080174,
12.1254669951038));
#116438=CARTESIAN_POINT('Ctrl Pts',(-9.64909707120239,4.07579028052519,
12.1242680158706));
#116439=CARTESIAN_POINT('Ctrl Pts',(-9.63817484753469,4.0765602686588,12.1208177797033));
#116440=CARTESIAN_POINT('Ctrl Pts',(-9.63113220391451,4.07705456810155,
12.1185197772727));
#116441=CARTESIAN_POINT('Ctrl Pts',(-9.58300193994254,4.08042063832355,
12.1023109115636));
#116442=CARTESIAN_POINT('Ctrl Pts',(-9.5426835731107,4.08318052324722,12.0862040809514));
#116443=CARTESIAN_POINT('Ctrl Pts',(-9.48553598709015,4.08712810544038,
12.059626095717));
#116444=CARTESIAN_POINT('Ctrl Pts',(-9.46793974515926,4.08834867210622,
12.0509008516992));
#116445=CARTESIAN_POINT('Ctrl Pts',(-9.40619190187101,4.09267595367205,
12.0183340320949));
#116446=CARTESIAN_POINT('Ctrl Pts',(-9.36335623170701,4.09576219207596,
11.9921173430956));
#116447=CARTESIAN_POINT('Ctrl Pts',(-9.28244953479867,4.10196450703922,
11.93519691149));
#116448=CARTESIAN_POINT('Ctrl Pts',(-9.24436034925133,4.10507126687519,
11.9046987321219));
#116449=CARTESIAN_POINT('Ctrl Pts',(-9.1998798969313,4.10901668761309,11.8643097891163));
#116450=CARTESIAN_POINT('Ctrl Pts',(-9.19159740646188,4.10976590095353,
11.8565680492916));
#116451=CARTESIAN_POINT('Ctrl Pts',(-9.17855632430423,4.11096992415317,
11.8440207680903));
#116452=CARTESIAN_POINT('Ctrl Pts',(-9.17372499289209,4.11142147914149,
11.8392915933849));
#116453=CARTESIAN_POINT('Ctrl Pts',(-9.16464028349946,4.11228126111537,
11.8302445053379));
#116454=CARTESIAN_POINT('Ctrl Pts',(-9.1603789837844,4.1126891217111,11.8259348287685));
#116455=CARTESIAN_POINT('Ctrl Pts',(-9.15075050317312,4.11362130269754,
11.8160455204478));
#116456=CARTESIAN_POINT('Ctrl Pts',(-9.14540474231337,4.11414651776933,
11.8104455193861));
#116457=CARTESIAN_POINT('Ctrl Pts',(-9.12908422750585,4.11577417600533,
11.7930077868126));
#116458=CARTESIAN_POINT('Ctrl Pts',(-9.11829773088535,4.11688439372328,
11.7809972449681));
#116459=CARTESIAN_POINT('Ctrl Pts',(-9.06268070530291,4.12279777635008,
11.7164478060619));
#116460=CARTESIAN_POINT('Ctrl Pts',(-9.02229632605453,4.1277739389759,11.6602708617861));
#116461=CARTESIAN_POINT('Ctrl Pts',(-8.95614417321754,4.13726303012911,
11.5487570417756));
#116462=CARTESIAN_POINT('Ctrl Pts',(-8.92928831565067,4.1417416169295,11.4943138304972));
#116463=CARTESIAN_POINT('Ctrl Pts',(-8.90014676754216,4.14737927673124,
11.4215831948789));
#116464=CARTESIAN_POINT('Ctrl Pts',(-8.89392350837116,4.14864410014872,
11.4049745500135));
#116465=CARTESIAN_POINT('Ctrl Pts',(-8.88412702597324,4.15073657759108,
11.3769166802849));
#116466=CARTESIAN_POINT('Ctrl Pts',(-8.88034938154421,4.1515728740737,11.3655423344774));
#116467=CARTESIAN_POINT('Ctrl Pts',(-8.87529005113792,4.15273424403023,
11.3494939725525));
#116468=CARTESIAN_POINT('Ctrl Pts',(-8.87386272242192,4.15306692375363,
11.3448671338819));
#116469=CARTESIAN_POINT('Ctrl Pts',(-8.8714671421849,4.15363392655669,11.3369281190602));
#116470=CARTESIAN_POINT('Ctrl Pts',(-8.87048484797974,4.15386903624528,
11.3336202799735));
#116471=CARTESIAN_POINT('Ctrl Pts',(-8.8684647211989,4.15435803064825,11.3267063742156));
#116472=CARTESIAN_POINT('Ctrl Pts',(-8.86742956766783,4.15461176432302,
11.3230996114546));
#116473=CARTESIAN_POINT('Ctrl Pts',(-8.86470632751593,4.15528803399112,
11.3134371694362));
#116474=CARTESIAN_POINT('Ctrl Pts',(-8.86304942971062,4.15570883886035,
11.3073727167613));
#116475=CARTESIAN_POINT('Ctrl Pts',(-8.8557865665455,4.15759804924544,11.279927210067));
#116476=CARTESIAN_POINT('Ctrl Pts',(-8.85073422503047,4.15903819357584,
11.2584026929605));
#116477=CARTESIAN_POINT('Ctrl Pts',(-8.82924317984186,4.16590219087264,
11.153673125334));
#116478=CARTESIAN_POINT('Ctrl Pts',(-8.82121702098378,4.17103463526259,
11.0689943703428));
#116479=CARTESIAN_POINT('Ctrl Pts',(-8.82311674496046,4.17985462864931,
10.9275625937719));
#116480=CARTESIAN_POINT('Ctrl Pts',(-8.8279592582305,4.18344006776357,10.8710789015476));
#116481=CARTESIAN_POINT('Ctrl Pts',(-8.83868552693927,4.18792415483805,
10.8035784070306));
#116482=CARTESIAN_POINT('Ctrl Pts',(-8.84070004444882,4.18869904614588,
10.7920184036299));
#116483=CARTESIAN_POINT('Ctrl Pts',(-8.8441618316719,4.18993421222923,10.7737700630447));
#116484=CARTESIAN_POINT('Ctrl Pts',(-8.84549528090512,4.19039091276263,
10.767060724652));
#116485=CARTESIAN_POINT('Ctrl Pts',(-8.84811551936153,4.19125418005944,
10.7544523330769));
#116486=CARTESIAN_POINT('Ctrl Pts',(-8.84938937571386,4.19166032623932,
10.7485507955461));
#116487=CARTESIAN_POINT('Ctrl Pts',(-8.85236574208077,4.19257995449355,
10.7352582464699));
#116488=CARTESIAN_POINT('Ctrl Pts',(-8.8540943726802,4.1930942490326,10.7278734216752));
#116489=CARTESIAN_POINT('Ctrl Pts',(-8.85953713761521,4.19465640059544,
10.7055935227753));
#116490=CARTESIAN_POINT('Ctrl Pts',(-8.86347115095915,4.195711170969,10.6907543839071));
#116491=CARTESIAN_POINT('Ctrl Pts',(-8.89269759213039,4.20307420709794,
10.5886155976283));
#116492=CARTESIAN_POINT('Ctrl Pts',(-8.92772778630018,4.20970237084639,
10.5044376979018));
#116493=CARTESIAN_POINT('Ctrl Pts',(-9.00318625361909,4.22104808273707,
10.3695078240405));
#116494=CARTESIAN_POINT('Ctrl Pts',(-9.03876700534044,4.22571692897838,
10.3164863170655));
#116495=CARTESIAN_POINT('Ctrl Pts',(-9.0834080683673,4.23071661314367,10.2603938750841));
#116496=CARTESIAN_POINT('Ctrl Pts',(-9.0884105668474,4.23126620307071,10.2542368317976));
#116497=CARTESIAN_POINT('Ctrl Pts',(-9.09609534446169,4.23209388294506,
10.2449713362918));
#116498=CARTESIAN_POINT('Ctrl Pts',(-9.09873217570549,4.23237498809018,
10.2418257327626));
#116499=CARTESIAN_POINT('Ctrl Pts',(-9.10357236764456,4.23288564434076,
10.2361125682141));
#116500=CARTESIAN_POINT('Ctrl Pts',(-9.10577036706129,4.23311555310008,
10.2335406907896));
#116501=CARTESIAN_POINT('Ctrl Pts',(-9.11075890513035,4.23363291053683,
10.2277542771242));
#116502=CARTESIAN_POINT('Ctrl Pts',(-9.11355581204901,4.23391989205777,
10.2245453692401));
#116503=CARTESIAN_POINT('Ctrl Pts',(-9.12084420734665,4.23466001074259,
10.2162743136332));
#116504=CARTESIAN_POINT('Ctrl Pts',(-9.12536211132016,4.23511130555952,
10.2112355052733));
#116505=CARTESIAN_POINT('Ctrl Pts',(-9.15799282231843,4.23832014852505,
10.1754676793928));
#116506=CARTESIAN_POINT('Ctrl Pts',(-9.18767800847342,4.24097418281745,
10.1462064534804));
#116507=CARTESIAN_POINT('Ctrl Pts',(-9.23336477374673,4.24480256946397,
10.1057173807133));
#116508=CARTESIAN_POINT('Ctrl Pts',(-9.24819064370382,4.24600877827611,
10.0932179434441));
#116509=CARTESIAN_POINT('Ctrl Pts',(-9.30011884296329,4.2501363652677,10.0515876036319));
#116510=CARTESIAN_POINT('Ctrl Pts',(-9.33865747017137,4.25303712323874,
10.024322957885));
#116511=CARTESIAN_POINT('Ctrl Pts',(-9.42011566560855,4.25902874891225,
9.97374334336126));
#116512=CARTESIAN_POINT('Ctrl Pts',(-9.46305497035722,4.26211723545089,
9.95063933483388));
#116513=CARTESIAN_POINT('Ctrl Pts',(-9.52026460450015,4.26622949527544,
9.9242896267536));
#116514=CARTESIAN_POINT('Ctrl Pts',(-9.53333806667504,4.26716883333011,
9.91855399199684));
#116515=CARTESIAN_POINT('Ctrl Pts',(-9.55332131269216,4.26860570687354,
9.9102166964114));
#116516=CARTESIAN_POINT('Ctrl Pts',(-9.56015692971892,4.26909739586418,
9.90743990194864));
#116517=CARTESIAN_POINT('Ctrl Pts',(-9.57262613945093,4.26999486240817,
9.90251058710886));
#116518=CARTESIAN_POINT('Ctrl Pts',(-9.57825107500133,4.27039991631639,
9.90033674698008));
#116519=CARTESIAN_POINT('Ctrl Pts',(-9.59044803797316,4.27127878257451,
9.89573039547568));
#116520=CARTESIAN_POINT('Ctrl Pts',(-9.59702554792629,4.27175308049506,
9.89331316245796));
#116521=CARTESIAN_POINT('Ctrl Pts',(-9.61506887717908,4.27305532179186,
9.88686442559264));
#116522=CARTESIAN_POINT('Ctrl Pts',(-9.62657588009894,4.27388709042424,
9.88295157497811));
#116523=CARTESIAN_POINT('Ctrl Pts',(-9.69469245384951,4.27881992435266,
9.86095926410189));
#116524=CARTESIAN_POINT('Ctrl Pts',(-9.75252715560894,4.28305149012379,
9.84701279130022));
#116525=CARTESIAN_POINT('Ctrl Pts',(-9.81114931893004,4.28736676513878,
9.8374895773545));
#116526=CARTESIAN_POINT('Origin',(-10.,2.67563288526385,11.));
#116527=CARTESIAN_POINT('',(-9.81114928033716,4.88742944471338,9.83748958362395));
#116528=CARTESIAN_POINT('',(-9.81114930150159,4.7888800033368,9.83748958018577));
#116529=CARTESIAN_POINT('',(-9.81114930150157,2.67563288526385,9.83748958018577));
#116530=CARTESIAN_POINT('Ctrl Pts',(-9.81114928023156,4.88742944622416,
9.8374895836411));
#116531=CARTESIAN_POINT('Ctrl Pts',(-9.78935088328749,4.88586560561609,
9.84103075015003));
#116532=CARTESIAN_POINT('Ctrl Pts',(-9.76765219414491,4.884285230485,9.84518501267445));
#116533=CARTESIAN_POINT('Ctrl Pts',(-9.69802535573987,4.87914157996404,
9.86055799325162));
#116534=CARTESIAN_POINT('Ctrl Pts',(-9.65068647776341,4.87552991262804,
9.87416860760851));
#116535=CARTESIAN_POINT('Ctrl Pts',(-9.58516738225473,4.8704258024824,9.89753760209531));
#116536=CARTESIAN_POINT('Ctrl Pts',(-9.56617441987963,4.86893359467803,
9.90487223059995));
#116537=CARTESIAN_POINT('Ctrl Pts',(-9.5080573735057,4.86434257286067,9.92906498398443));
#116538=CARTESIAN_POINT('Ctrl Pts',(-9.46964630448459,4.86127168932063,
9.94755754742094));
#116539=CARTESIAN_POINT('Ctrl Pts',(-9.42636526504175,4.85783046383883,
9.97136769745121));
#116540=CARTESIAN_POINT('Ctrl Pts',(-9.42044071952102,4.85735986507994,
9.97469406089045));
#116541=CARTESIAN_POINT('Ctrl Pts',(-9.41084442113239,4.85659875478454,
9.98019170604868));
#116542=CARTESIAN_POINT('Ctrl Pts',(-9.40715519065467,4.85630642943153,
9.98233193722733));
#116543=CARTESIAN_POINT('Ctrl Pts',(-9.40055824947098,4.85578431568561,
9.98620706573903));
#116544=CARTESIAN_POINT('Ctrl Pts',(-9.3976463228998,4.85555407540329,9.98793450094272));
#116545=CARTESIAN_POINT('Ctrl Pts',(-9.39122158146995,4.8550465792897,9.99178338708724));
#116546=CARTESIAN_POINT('Ctrl Pts',(-9.38771237679128,4.85476969933343,
9.99391065547778));
#116547=CARTESIAN_POINT('Ctrl Pts',(-9.37746957216578,4.85396223780954,
10.0001932512222));
#116548=CARTESIAN_POINT('Ctrl Pts',(-9.3707664842563,4.85343471935769,10.0043982425234));
#116549=CARTESIAN_POINT('Ctrl Pts',(-9.31069721575149,4.84871072062784,
10.0429300201396));
#116550=CARTESIAN_POINT('Ctrl Pts',(-9.2601363207659,4.8447552483553,10.0814547848116));
#116551=CARTESIAN_POINT('Ctrl Pts',(-9.14509364953285,4.83517350826218,
10.1848046140644));
#116552=CARTESIAN_POINT('Ctrl Pts',(-9.08457940318283,4.8295833148745,10.2534000512102));
#116553=CARTESIAN_POINT('Ctrl Pts',(-9.02384554462224,4.82264392370784,
10.3408700554137));
#116554=CARTESIAN_POINT('Ctrl Pts',(-9.0153539897059,4.82163716406329,10.3536239454152));
#116555=CARTESIAN_POINT('Ctrl Pts',(-9.00303472580952,4.82011836423999,
10.3729331575823));
#116556=CARTESIAN_POINT('Ctrl Pts',(-8.99901744316373,4.81961325655743,
10.3793660505472));
#116557=CARTESIAN_POINT('Ctrl Pts',(-8.99191082418715,4.81870153798718,
10.3909944111676));
#116558=CARTESIAN_POINT('Ctrl Pts',(-8.98879879813591,4.81829576559348,
10.396175753513));
#116559=CARTESIAN_POINT('Ctrl Pts',(-8.98224236697227,4.81742665264136,
10.4072846712908));
#116560=CARTESIAN_POINT('Ctrl Pts',(-8.97880957413239,4.81696291536751,
10.4132188046981));
#116561=CARTESIAN_POINT('Ctrl Pts',(-8.9696199967512,4.81569732194231,10.4294293618923));
#116562=CARTESIAN_POINT('Ctrl Pts',(-8.96396538661737,4.81489190359518,
10.4397624909176));
#116563=CARTESIAN_POINT('Ctrl Pts',(-8.93164803050363,4.81012625115241,
10.5009816121629));
#116564=CARTESIAN_POINT('Ctrl Pts',(-8.90858624262785,4.80604335559248,
10.5536710924557));
#116565=CARTESIAN_POINT('Ctrl Pts',(-8.86310113160392,4.79613458815596,
10.682473260286));
#116566=CARTESIAN_POINT('Ctrl Pts',(-8.84433450764669,4.79025083081842,
10.7595855403343));
#116567=CARTESIAN_POINT('Ctrl Pts',(-8.8298473150328,4.78267198524842,10.8639046067092));
#116568=CARTESIAN_POINT('Ctrl Pts',(-8.82711309537822,4.78081387093843,
10.889928172748));
#116569=CARTESIAN_POINT('Ctrl Pts',(-8.824773532442,4.7785341610091,10.9226563835733));
#116570=CARTESIAN_POINT('Ctrl Pts',(-8.82435554332993,4.7780747864903,10.929293552698));
#116571=CARTESIAN_POINT('Ctrl Pts',(-8.82378517736112,4.77735515174573,
10.9397633015969));
#116572=CARTESIAN_POINT('Ctrl Pts',(-8.82359527169342,4.77709293381873,
10.9435935721269));
#116573=CARTESIAN_POINT('Ctrl Pts',(-8.82327115050244,4.77659844650349,
10.9508470485647));
#116574=CARTESIAN_POINT('Ctrl Pts',(-8.82313316132455,4.77636599007145,
10.9542698982325));
#116575=CARTESIAN_POINT('Ctrl Pts',(-8.82284229358829,4.77581845532227,
10.9623619829776));
#116576=CARTESIAN_POINT('Ctrl Pts',(-8.8227022584358,4.77550408052008,10.9670315963024));
#116577=CARTESIAN_POINT('Ctrl Pts',(-8.82232716560084,4.7744583097091,10.9826382937824));
#116578=CARTESIAN_POINT('Ctrl Pts',(-8.82221669438312,4.77373333411558,
10.9935781829952));
#116579=CARTESIAN_POINT('Ctrl Pts',(-8.82231884241623,4.77198515462371,
11.0202029591469));
#116580=CARTESIAN_POINT('Ctrl Pts',(-8.82269232899375,4.77096913520445,
11.0358854486177));
#116581=CARTESIAN_POINT('Ctrl Pts',(-8.82549279781047,4.76686750495758,
11.0997975997953));
#116582=CARTESIAN_POINT('Ctrl Pts',(-8.83057156803924,4.7638720742231,11.1478667205664));
#116583=CARTESIAN_POINT('Ctrl Pts',(-8.85275230224345,4.75560163230495,
11.2796422688943));
#116584=CARTESIAN_POINT('Ctrl Pts',(-8.87601823205132,4.75034725401852,
11.3619945436492));
#116585=CARTESIAN_POINT('Ctrl Pts',(-8.91387476661186,4.74376539921164,
11.4557139596163));
#116586=CARTESIAN_POINT('Ctrl Pts',(-8.920067223747,4.742730800921,11.4702003789319));
#116587=CARTESIAN_POINT('Ctrl Pts',(-8.92970272987694,4.74117826885783,
11.491546137922));
#116588=CARTESIAN_POINT('Ctrl Pts',(-8.93292542414599,4.74066774071938,
11.4985034574213));
#116589=CARTESIAN_POINT('Ctrl Pts',(-8.9388129675024,4.73975009953142,11.5108950689445));
#116590=CARTESIAN_POINT('Ctrl Pts',(-8.94145223039851,4.73934387104034,
11.5163412694653));
#116591=CARTESIAN_POINT('Ctrl Pts',(-8.94714711068771,4.73847792874671,
11.5278656408669));
#116592=CARTESIAN_POINT('Ctrl Pts',(-8.95021364080381,4.73801785015515,
11.5339381406458));
#116593=CARTESIAN_POINT('Ctrl Pts',(-8.95862112944483,4.73677270649401,
11.5502346434823));
#116594=CARTESIAN_POINT('Ctrl Pts',(-8.96405984860207,4.73598427211538,
11.5604070852986));
#116595=CARTESIAN_POINT('Ctrl Pts',(-8.99498602149185,4.73159128775035,
11.6162616085485));
#116596=CARTESIAN_POINT('Ctrl Pts',(-9.02334221066041,4.72788606487821,
11.6602799770764));
#116597=CARTESIAN_POINT('Ctrl Pts',(-9.10149720517369,4.71841208696263,
11.7655019380811));
#116598=CARTESIAN_POINT('Ctrl Pts',(-9.15469117032413,4.71256210582804,
11.8238643759852));
#116599=CARTESIAN_POINT('Ctrl Pts',(-9.23674938252155,4.7045849875174,11.8975163123333));
#116600=CARTESIAN_POINT('Ctrl Pts',(-9.26102516843012,4.70233613450133,
11.9176075507893));
#116601=CARTESIAN_POINT('Ctrl Pts',(-9.29158494747188,4.69966357540991,
11.9408990874632));
#116602=CARTESIAN_POINT('Ctrl Pts',(-9.29712745726284,4.69918495391991,
11.9450466516835));
#116603=CARTESIAN_POINT('Ctrl Pts',(-9.30587757506763,4.69843923848597,
11.9514749633381));
#116604=CARTESIAN_POINT('Ctrl Pts',(-9.30906048701106,4.69817000551934,
11.9537888325944));
#116605=CARTESIAN_POINT('Ctrl Pts',(-9.3147403149997,4.69769324130179,11.9578745218285));
#116606=CARTESIAN_POINT('Ctrl Pts',(-9.31723255137716,4.69748529779839,
11.9596525657217));
#116607=CARTESIAN_POINT('Ctrl Pts',(-9.32324123861699,4.69698692789213,
11.9639041050822));
#116608=CARTESIAN_POINT('Ctrl Pts',(-9.32676433278709,4.69669714003421,
11.9663680886446));
#116609=CARTESIAN_POINT('Ctrl Pts',(-9.33761411837906,4.69581184523313,
11.9738680842505));
#116610=CARTESIAN_POINT('Ctrl Pts',(-9.34498460395086,4.69522036158093,
11.9788406122913));
#116611=CARTESIAN_POINT('Ctrl Pts',(-9.39678491442307,4.69112669804982,
12.0129407560385));
#116612=CARTESIAN_POINT('Ctrl Pts',(-9.44309045240427,4.68778757293291,
12.0391201096924));
#116613=CARTESIAN_POINT('Ctrl Pts',(-9.57402772706918,4.67876200021067,
12.1018698957587));
#116614=CARTESIAN_POINT('Ctrl Pts',(-9.66141521300852,4.67315520043928,
12.1317812601404));
#116615=CARTESIAN_POINT('Ctrl Pts',(-9.77116144926607,4.66590046667336,
12.1554812977025));
#116616=CARTESIAN_POINT('Ctrl Pts',(-9.79103636417713,4.66457991090727,
12.1592403688672));
#116617=CARTESIAN_POINT('Ctrl Pts',(-9.81872901891244,4.66272586824122,
12.1637427780793));
#116618=CARTESIAN_POINT('Ctrl Pts',(-9.82647292350091,4.66220590662008,
12.1649226459023));
#116619=CARTESIAN_POINT('Ctrl Pts',(-9.83987605973425,4.66130309556185,
12.1668281506324));
#116620=CARTESIAN_POINT('Ctrl Pts',(-9.84552992403799,4.66092138466888,
12.1675900834829));
#116621=CARTESIAN_POINT('Ctrl Pts',(-9.85729087800224,4.6601254346971,12.1690881086357));
#116622=CARTESIAN_POINT('Ctrl Pts',(-9.86339863178913,4.6597109997397,12.1698174913179));
#116623=CARTESIAN_POINT('Ctrl Pts',(-9.877836390027,4.65872866243836,12.1714270255873));
#116624=CARTESIAN_POINT('Ctrl Pts',(-9.88617053079292,4.65815950906774,
12.172266211038));
#116625=CARTESIAN_POINT('Ctrl Pts',(-9.91418311736064,4.65623903703907,
12.1747853328779));
#116626=CARTESIAN_POINT('Ctrl Pts',(-9.93389378768376,4.65487534432103,
12.1760590984233));
#116627=CARTESIAN_POINT('Ctrl Pts',(-9.98162049705699,4.65154151061157,
12.1779397927006));
#116628=CARTESIAN_POINT('Ctrl Pts',(-10.0096432324052,4.64955741754914,
12.178043615419));
#116629=CARTESIAN_POINT('Ctrl Pts',(-10.1435302956369,4.63995600755402,
12.173762359381));
#116630=CARTESIAN_POINT('Ctrl Pts',(-10.2484650167861,4.63201013804697,
12.1561059782564));
#116631=CARTESIAN_POINT('Ctrl Pts',(-10.3666773423264,4.62319865589227,
12.1193578129637));
#116632=CARTESIAN_POINT('Ctrl Pts',(-10.383614430605,4.62194127412702,12.1136670235969));
#116633=CARTESIAN_POINT('Ctrl Pts',(-10.4058999067678,4.62029935988162,
12.1056103857407));
#116634=CARTESIAN_POINT('Ctrl Pts',(-10.4113686094444,4.61989746161655,
12.1035873006045));
#116635=CARTESIAN_POINT('Ctrl Pts',(-10.4202402173155,4.61924739372102,
12.1002302386096));
#116636=CARTESIAN_POINT('Ctrl Pts',(-10.4236522536035,4.61899783945435,
12.0989209194205));
#116637=CARTESIAN_POINT('Ctrl Pts',(-10.4303270736903,4.61851063261477,
12.0963238460185));
#116638=CARTESIAN_POINT('Ctrl Pts',(-10.4335902764236,4.61827291578774,
12.0950373684737));
#116639=CARTESIAN_POINT('Ctrl Pts',(-10.4416216244056,4.61768890065987,
12.0918295788202));
#116640=CARTESIAN_POINT('Ctrl Pts',(-10.4463831047845,4.61734357547912,
12.0898915608987));
#116641=CARTESIAN_POINT('Ctrl Pts',(-10.4640367009841,4.6160661161042,12.0825710942364));
#116642=CARTESIAN_POINT('Ctrl Pts',(-10.4768460109367,4.61514490297321,
12.0769903238631));
#116643=CARTESIAN_POINT('Ctrl Pts',(-10.5094744755595,4.61280552977485,
12.062078409285));
#116644=CARTESIAN_POINT('Ctrl Pts',(-10.5291386823864,4.61140256083007,
12.0524196690198));
#116645=CARTESIAN_POINT('Ctrl Pts',(-10.5908233230821,4.60698853854376,
12.0199548002418));
#116646=CARTESIAN_POINT('Ctrl Pts',(-10.6317310498277,4.60404009413044,
11.9951363422169));
#116647=CARTESIAN_POINT('Ctrl Pts',(-10.7325804761389,4.5964484446862,11.9252201048143));
#116648=CARTESIAN_POINT('Ctrl Pts',(-10.7899226762571,4.59180006704116,
11.8767706475621));
#116649=CARTESIAN_POINT('Ctrl Pts',(-10.8535185562632,4.58587867745126,
11.8117019056287));
#116650=CARTESIAN_POINT('Ctrl Pts',(-10.8645266226401,4.58482250137414,
11.7999672417249));
#116651=CARTESIAN_POINT('Ctrl Pts',(-10.8804632275538,4.5832438646828,11.782265516363));
#116652=CARTESIAN_POINT('Ctrl Pts',(-10.8855791931164,4.58272918665431,
11.776469137266));
#116653=CARTESIAN_POINT('Ctrl Pts',(-10.8946020246303,4.58180695869125,
11.7660411147553));
#116654=CARTESIAN_POINT('Ctrl Pts',(-10.898530948527,4.58140032856354,11.7614288569319));
#116655=CARTESIAN_POINT('Ctrl Pts',(-10.9067712702278,4.58053656742262,
11.7516027516027));
#116656=CARTESIAN_POINT('Ctrl Pts',(-10.9110736653269,4.58007909479101,
11.746381675673));
#116657=CARTESIAN_POINT('Ctrl Pts',(-10.922480061762,4.57884850040848,11.7322941184548));
#116658=CARTESIAN_POINT('Ctrl Pts',(-10.9295009946528,4.5780721439498,11.7233616146462));
#116659=CARTESIAN_POINT('Ctrl Pts',(-10.966214025614,4.57390872849835,11.6752356718678));
#116660=CARTESIAN_POINT('Ctrl Pts',(-10.9935552030944,4.57043330897733,
11.6343182600281));
#116661=CARTESIAN_POINT('Ctrl Pts',(-11.0433495994662,4.56328808529452,
11.548643987611));
#116662=CARTESIAN_POINT('Ctrl Pts',(-11.0656696076276,4.55962319867447,
11.5039209839741));
#116663=CARTESIAN_POINT('Ctrl Pts',(-11.0934021420118,4.55438963568818,
11.4382061677087));
#116664=CARTESIAN_POINT('Ctrl Pts',(-11.1011828247663,4.5528212810994,11.4182694194178));
#116665=CARTESIAN_POINT('Ctrl Pts',(-11.122444905285,4.54823706237586,11.3590748175927));
#116666=CARTESIAN_POINT('Ctrl Pts',(-11.1344011184732,4.54524778835645,
11.319299463151));
#116667=CARTESIAN_POINT('Ctrl Pts',(-11.1458345967664,4.54188555681425,
11.2724038241856));
#116668=CARTESIAN_POINT('Ctrl Pts',(-11.1473794057222,4.54141733013264,
11.2658218786926));
#116669=CARTESIAN_POINT('Ctrl Pts',(-11.1498040121204,4.54065927430008,
11.2550762636829));
#116670=CARTESIAN_POINT('Ctrl Pts',(-11.1507180472539,4.54036765454002,
11.2509205924777));
#116671=CARTESIAN_POINT('Ctrl Pts',(-11.1523188590524,4.53984627495291,
11.2434497287522));
#116672=CARTESIAN_POINT('Ctrl Pts',(-11.1530138804904,4.53961606914807,
11.240136452052));
#116673=CARTESIAN_POINT('Ctrl Pts',(-11.1545215403728,4.53910801973409,
11.2327917240606));
#116674=CARTESIAN_POINT('Ctrl Pts',(-11.1553273576541,4.53883055728417,
11.2287589821495));
#116675=CARTESIAN_POINT('Ctrl Pts',(-11.1576300130813,4.53801964959261,
11.216912668126));
#116676=CARTESIAN_POINT('Ctrl Pts',(-11.1590688609997,4.53748930737678,
11.2090878684105));
#116677=CARTESIAN_POINT('Ctrl Pts',(-11.1621953530721,4.53627830984126,
11.1910600862751));
#116678=CARTESIAN_POINT('Ctrl Pts',(-11.1638281512367,4.53560030423341,
11.1808481287856));
#116679=CARTESIAN_POINT('Ctrl Pts',(-11.1689154539555,4.53331630767468,
11.1461012056031));
#116680=CARTESIAN_POINT('Ctrl Pts',(-11.1717304074329,4.53173645267795,
11.1214780264382));
#116681=CARTESIAN_POINT('Ctrl Pts',(-11.1780890175756,4.52685905695322,
11.0443618685767));
#116682=CARTESIAN_POINT('Ctrl Pts',(-11.1788949953248,4.52362810332556,
10.9917081161661));
#116683=CARTESIAN_POINT('Ctrl Pts',(-11.1724719151175,4.51592269433473,
10.8675043427265));
#116684=CARTESIAN_POINT('Ctrl Pts',(-11.1622232749476,4.51143343985635,
10.7963321732177));
#116685=CARTESIAN_POINT('Ctrl Pts',(-11.1427326533986,4.50593269969573,
10.7146830681849));
#116686=CARTESIAN_POINT('Ctrl Pts',(-11.1397183487971,4.50512844291463,
10.7028708426992));
#116687=CARTESIAN_POINT('Ctrl Pts',(-11.1346814391405,4.50385221604343,
10.68433830365));
#116688=CARTESIAN_POINT('Ctrl Pts',(-11.1327811409424,4.50338414667368,
10.6775854252382));
#116689=CARTESIAN_POINT('Ctrl Pts',(-11.1291357535778,4.5025102018442,10.6650614089987));
#116690=CARTESIAN_POINT('Ctrl Pts',(-11.1274064489855,4.50210484581669,
10.6592858878423));
#116691=CARTESIAN_POINT('Ctrl Pts',(-11.1234659104343,4.50120101618447,
10.6464838475428));
#116692=CARTESIAN_POINT('Ctrl Pts',(-11.1212329599107,4.50070185444174,
10.6394643328258));
#116693=CARTESIAN_POINT('Ctrl Pts',(-11.1144968471133,4.49923276753994,
10.6189566371282));
#116694=CARTESIAN_POINT('Ctrl Pts',(-11.1098152129217,4.49825710258634,
10.605528924841));
#116695=CARTESIAN_POINT('Ctrl Pts',(-11.0800532894808,4.49231199834423,
10.5248941063271));
#116696=CARTESIAN_POINT('Ctrl Pts',(-11.0491229812589,4.48715011053184,
10.4600199533741));
#116697=CARTESIAN_POINT('Ctrl Pts',(-10.9705335679791,4.47589317269532,
10.3277604434209));
#116698=CARTESIAN_POINT('Ctrl Pts',(-10.921302147259,4.46980001440404,10.2617279248));
#116699=CARTESIAN_POINT('Ctrl Pts',(-10.8591420552707,4.46338118288953,
10.1943570294853));
#116700=CARTESIAN_POINT('Ctrl Pts',(-10.8526025098898,4.46271967824316,
10.1874394535999));
#116701=CARTESIAN_POINT('Ctrl Pts',(-10.8429380636886,4.46176291679154,
10.1774614935414));
#116702=CARTESIAN_POINT('Ctrl Pts',(-10.8398790454551,4.4614630543714,10.1743382264131));
#116703=CARTESIAN_POINT('Ctrl Pts',(-10.8344114948334,4.46093246847359,
10.1688176695815));
#116704=CARTESIAN_POINT('Ctrl Pts',(-10.8320098903734,4.46070123296669,
10.1664136802313));
#116705=CARTESIAN_POINT('Ctrl Pts',(-10.8267832916401,4.46020195052738,
10.161226983148));
#116706=CARTESIAN_POINT('Ctrl Pts',(-10.8239546257036,4.45993419493283,
10.1584481233624));
#116707=CARTESIAN_POINT('Ctrl Pts',(-10.8159123295414,4.45917965934843,
10.1506268552643));
#116708=CARTESIAN_POINT('Ctrl Pts',(-10.8106659702057,4.45869536207058,
10.1456181417232));
#116709=CARTESIAN_POINT('Ctrl Pts',(-10.7738073029846,4.45534469761582,
10.1110742739515));
#116710=CARTESIAN_POINT('Ctrl Pts',(-10.7406310742971,4.45259057852758,
10.0832485641292));
#116711=CARTESIAN_POINT('Ctrl Pts',(-10.6320453469658,4.44409095950227,
10.0019271374568));
#116712=CARTESIAN_POINT('Ctrl Pts',(-10.5518388566261,4.43850384445114,
9.95544033677818));
#116713=CARTESIAN_POINT('Ctrl Pts',(-10.4399497825646,4.43072433830512,
9.90710981141323));
#116714=CARTESIAN_POINT('Ctrl Pts',(-10.4124488876198,4.42881605951598,
9.89643737578552));
#116715=CARTESIAN_POINT('Ctrl Pts',(-10.3751064692611,4.42621405895943,
9.88353655708448));
#116716=CARTESIAN_POINT('Ctrl Pts',(-10.3655936596621,4.42555033062063,
9.88038544646553));
#116717=CARTESIAN_POINT('Ctrl Pts',(-10.349869075622,4.42445119030145,9.87539845698945));
#116718=CARTESIAN_POINT('Ctrl Pts',(-10.3436801819509,4.42401808484502,
9.87349170872139));
#116719=CARTESIAN_POINT('Ctrl Pts',(-10.3315806777661,4.42317021511648,
9.86987293631155));
#116720=CARTESIAN_POINT('Ctrl Pts',(-10.3256717452688,4.4227556247994,9.86815600111354));
#116721=CARTESIAN_POINT('Ctrl Pts',(-10.3116756534665,4.42177224390696,
9.86420788540265));
#116722=CARTESIAN_POINT('Ctrl Pts',(-10.3035776641246,4.42120219489107,
9.86201668022578));
#116723=CARTESIAN_POINT('Ctrl Pts',(-10.2762625421271,4.4192753790898,9.85493788520672));
#116724=CARTESIAN_POINT('Ctrl Pts',(-10.2569464649077,4.41790612635147,
9.85044936139298));
#116725=CARTESIAN_POINT('Ctrl Pts',(-10.1294256696776,4.40881756920577,
9.82419156072048));
#116726=CARTESIAN_POINT('Ctrl Pts',(-10.0187439281125,4.40062467277096,
9.81724218644562));
#116727=CARTESIAN_POINT('Ctrl Pts',(-9.87606656163429,4.39021398731939,
9.82833022979994));
#116728=CARTESIAN_POINT('Ctrl Pts',(-9.84350542182004,4.38785451689339,
9.83223330385834));
#116729=CARTESIAN_POINT('Ctrl Pts',(-9.81114929917643,4.38555086460676,
9.83748958056349));
#116730=CARTESIAN_POINT('Ctrl Pts',(-9.81114931893004,4.28736676513878,
9.8374895773545));
#116731=CARTESIAN_POINT('Ctrl Pts',(-9.8176029126927,4.28784182491725,9.83644118625737));
#116732=CARTESIAN_POINT('Ctrl Pts',(-9.82406605585664,4.28831781899759,
9.83544640201666));
#116733=CARTESIAN_POINT('Ctrl Pts',(-9.91549711542973,4.29505360548248,
9.82215240518902));
#116734=CARTESIAN_POINT('Ctrl Pts',(-10.0015534061697,4.30144350458995,
9.8191256241258));
#116735=CARTESIAN_POINT('Ctrl Pts',(-10.1003602461953,4.3084360922676,9.82645934817442));
#116736=CARTESIAN_POINT('Ctrl Pts',(-10.1135276330211,4.3093603270354,9.82765988147998));
#116737=CARTESIAN_POINT('Ctrl Pts',(-10.1316771713635,4.31062127344421,
9.82962334134962));
#116738=CARTESIAN_POINT('Ctrl Pts',(-10.1366782575393,4.31096735884294,
9.83019682989313));
#116739=CARTESIAN_POINT('Ctrl Pts',(-10.1451378796171,4.31155029517138,
9.83122191087831));
#116740=CARTESIAN_POINT('Ctrl Pts',(-10.1485983319158,4.31178804162246,
9.83165683008288));
#116741=CARTESIAN_POINT('Ctrl Pts',(-10.1557141877214,4.31227541003412,
9.83258329772278));
#116742=CARTESIAN_POINT('Ctrl Pts',(-10.1593692848611,4.3125249319178,9.8330766533318));
#116743=CARTESIAN_POINT('Ctrl Pts',(-10.1689490584446,4.3131769099589,9.83441555707696));
#116744=CARTESIAN_POINT('Ctrl Pts',(-10.1748698047786,4.31357785099239,
9.83528912039918));
#116745=CARTESIAN_POINT('Ctrl Pts',(-10.1997328823759,4.3152540384694,9.83915135747098));
#116746=CARTESIAN_POINT('Ctrl Pts',(-10.2186085711031,4.31650827410858,
9.84255747940336));
#116747=CARTESIAN_POINT('Ctrl Pts',(-10.2632354874528,4.31944797778381,
9.85174122760832));
#116748=CARTESIAN_POINT('Ctrl Pts',(-10.2888926705017,4.32111764828848,
9.85792630662254));
#116749=CARTESIAN_POINT('Ctrl Pts',(-10.3686225275086,4.32630117029982,
9.88000572296107));
#116750=CARTESIAN_POINT('Ctrl Pts',(-10.4217751150709,4.32975253131279,
9.89892061542318));
#116751=CARTESIAN_POINT('Ctrl Pts',(-10.5263460200968,4.33685486313371,
9.94482132151407));
#116752=CARTESIAN_POINT('Ctrl Pts',(-10.5775299905111,4.34049992035176,
9.97194353755557));
#116753=CARTESIAN_POINT('Ctrl Pts',(-10.6385455950005,4.34520488486823,
10.0102744882102));
#116754=CARTESIAN_POINT('Ctrl Pts',(-10.6504422952424,4.3461401581382,10.0180520085386));
#116755=CARTESIAN_POINT('Ctrl Pts',(-10.6682843493942,4.34757195813149,
10.0301828455577));
#116756=CARTESIAN_POINT('Ctrl Pts',(-10.6743346805138,4.34806269815868,
10.0343799819663));
#116757=CARTESIAN_POINT('Ctrl Pts',(-10.6852650846769,4.34895901403887,
10.0421152706204));
#116758=CARTESIAN_POINT('Ctrl Pts',(-10.6901581461131,4.34936387296301,
10.0456347019598));
#116759=CARTESIAN_POINT('Ctrl Pts',(-10.7006862924606,4.35024298085217,
10.0533305873043));
#116760=CARTESIAN_POINT('Ctrl Pts',(-10.7063114877112,4.35071772050998,
10.0575201137276));
#116761=CARTESIAN_POINT('Ctrl Pts',(-10.7216094924051,4.35202287284885,
10.0691276196982));
#116762=CARTESIAN_POINT('Ctrl Pts',(-10.731204858794,4.35285714296539,10.0766457434577));
#116763=CARTESIAN_POINT('Ctrl Pts',(-10.796502445049,4.35864544050587,10.1294635944975));
#116764=CARTESIAN_POINT('Ctrl Pts',(-10.8480677882746,4.36379630652066,
10.1796174884723));
#116765=CARTESIAN_POINT('Ctrl Pts',(-10.9289553239716,4.37288806274017,
10.2741173188097));
#116766=CARTESIAN_POINT('Ctrl Pts',(-10.9604536172668,4.37677112949434,
10.3163388500359));
#116767=CARTESIAN_POINT('Ctrl Pts',(-11.0024737972854,4.38239215705284,
10.3813280165174));
#116768=CARTESIAN_POINT('Ctrl Pts',(-11.0152655193393,4.38417591325399,
10.4025514105242));
#116769=CARTESIAN_POINT('Ctrl Pts',(-11.0324341194424,4.38666339097465,
10.4331827905196));
#116770=CARTESIAN_POINT('Ctrl Pts',(-11.0373704309133,4.38739068759862,
10.4422683751598));
#116771=CARTESIAN_POINT('Ctrl Pts',(-11.0458915231141,4.38866659912175,
10.4584566031053));
#116772=CARTESIAN_POINT('Ctrl Pts',(-11.0495251377214,4.38921768947345,
10.4655326738455));
#116773=CARTESIAN_POINT('Ctrl Pts',(-11.0549277393483,4.39004731762736,
10.4763212540827));
#116774=CARTESIAN_POINT('Ctrl Pts',(-11.0567493481242,4.39032888585328,
10.4800069416803));
#116775=CARTESIAN_POINT('Ctrl Pts',(-11.0600351382682,4.39084006462629,
10.4867437093701));
#116776=CARTESIAN_POINT('Ctrl Pts',(-11.0615054867223,4.39107003641809,
10.4897915949931));
#116777=CARTESIAN_POINT('Ctrl Pts',(-11.064793933245,4.39158718435804,10.4966839698019));
#116778=CARTESIAN_POINT('Ctrl Pts',(-11.066604362527,4.3918738963073,10.5005320012464));
#116779=CARTESIAN_POINT('Ctrl Pts',(-11.071236799887,4.39261297413039,10.510518212821));
#116780=CARTESIAN_POINT('Ctrl Pts',(-11.0740269543595,4.39306350502977,
10.516671118258));
#116781=CARTESIAN_POINT('Ctrl Pts',(-11.09423202715,4.39636897974889,10.5622668418));
#116782=CARTESIAN_POINT('Ctrl Pts',(-11.109524309971,4.39911267563124,10.6026201661121));
#116783=CARTESIAN_POINT('Ctrl Pts',(-11.1285947471217,4.40306160565966,
10.6627084393003));
#116784=CARTESIAN_POINT('Ctrl Pts',(-11.1341370122423,4.40429934542467,
10.6818412803923));
#116785=CARTESIAN_POINT('Ctrl Pts',(-11.1519202813151,4.40864222409862,
10.7496196157493));
#116786=CARTESIAN_POINT('Ctrl Pts',(-11.1615367472825,4.41172692598226,
10.7988957762677));
#116787=CARTESIAN_POINT('Ctrl Pts',(-11.1742623401533,4.41793383306148,
10.8970901689433));
#116788=CARTESIAN_POINT('Ctrl Pts',(-11.1775199086907,4.42104699064732,
10.9458845685595));
#116789=CARTESIAN_POINT('Ctrl Pts',(-11.1777889193395,4.42499948822347,
11.006076527421));
#116790=CARTESIAN_POINT('Ctrl Pts',(-11.1776758112269,4.42574887434394,
11.0174164216368));
#116791=CARTESIAN_POINT('Ctrl Pts',(-11.1772339670548,4.4269529486864,11.0355096328468));
#116792=CARTESIAN_POINT('Ctrl Pts',(-11.1770107960306,4.42740437628947,
11.0422649976929));
#116793=CARTESIAN_POINT('Ctrl Pts',(-11.1764774030606,4.42826376538773,
11.055069679104));
#116794=CARTESIAN_POINT('Ctrl Pts',(-11.1761786350201,4.42867135941875,
11.061119273904));
#116795=CARTESIAN_POINT('Ctrl Pts',(-11.1753921587998,4.42960271725558,
11.0748875810885));
#116796=CARTESIAN_POINT('Ctrl Pts',(-11.1748750601296,4.43012737315115,
11.0826042669487));
#116797=CARTESIAN_POINT('Ctrl Pts',(-11.1730463342591,4.43175248122253,
11.1063814520022));
#116798=CARTESIAN_POINT('Ctrl Pts',(-11.1714811221476,4.43286067986431,
11.1224199804469));
#116799=CARTESIAN_POINT('Ctrl Pts',(-11.1614619840533,4.43877660475674,
11.2070768209603));
#116800=CARTESIAN_POINT('Ctrl Pts',(-11.1473084651564,4.44375780042572,
11.2748730517339));
#116801=CARTESIAN_POINT('Ctrl Pts',(-11.109792181109,4.45323928603169,11.3988865593206));
#116802=CARTESIAN_POINT('Ctrl Pts',(-11.0878597431626,4.45770488081936,
11.4553139009629));
#116803=CARTESIAN_POINT('Ctrl Pts',(-11.0540281136573,4.46332795361206,
11.5257691978859));
#116804=CARTESIAN_POINT('Ctrl Pts',(-11.0460050614667,4.46459062953133,
11.54155516174));
#116805=CARTESIAN_POINT('Ctrl Pts',(-11.03196640375,4.4666799275982,11.567700333859));
#116806=CARTESIAN_POINT('Ctrl Pts',(-11.0261433973429,4.46751515649371,
11.5781592195697));
#116807=CARTESIAN_POINT('Ctrl Pts',(-11.0177431716448,4.4686753351643,11.5927202741614));
#116808=CARTESIAN_POINT('Ctrl Pts',(-11.0152987908928,4.46900786758517,
11.5968976914875));
#116809=CARTESIAN_POINT('Ctrl Pts',(-11.011067432765,4.46957475519306,11.6040278295014));
#116810=CARTESIAN_POINT('Ctrl Pts',(-11.0092931185738,4.46980989486945,
11.6069879525041));
#116811=CARTESIAN_POINT('Ctrl Pts',(-11.0055599974178,4.47029924075484,
11.6131543607253));
#116812=CARTESIAN_POINT('Ctrl Pts',(-11.0035988323984,4.4705532939128,11.6163591186031));
#116813=CARTESIAN_POINT('Ctrl Pts',(-10.9983089297511,4.47123069022618,
11.6249112067222));
#116814=CARTESIAN_POINT('Ctrl Pts',(-10.9949525197387,4.4716522963643,11.6302414008273));
#116815=CARTESIAN_POINT('Ctrl Pts',(-10.9795762377741,4.47354835843217,
11.65423091468));
#116816=CARTESIAN_POINT('Ctrl Pts',(-10.9670722889544,4.47499434479083,
11.6725764148484));
#116817=CARTESIAN_POINT('Ctrl Pts',(-10.9412457556231,4.47782196265575,
11.7082576133397));
#116818=CARTESIAN_POINT('Ctrl Pts',(-10.927944522357,4.47920368773306,11.7255973219149));
#116819=CARTESIAN_POINT('Ctrl Pts',(-10.9021277648146,4.48177108055849,
11.7573805126361));
#116820=CARTESIAN_POINT('Ctrl Pts',(-10.8897285386905,4.48295910905912,
11.7719086110447));
#116821=CARTESIAN_POINT('Ctrl Pts',(-10.8454961928222,4.4870688672886,11.8212528486644));
#116822=CARTESIAN_POINT('Ctrl Pts',(-10.8119299571669,4.48996980502761,
11.8544528796232));
#116823=CARTESIAN_POINT('Ctrl Pts',(-10.7363094414386,4.4962542550023,11.9207580610405));
#116824=CARTESIAN_POINT('Ctrl Pts',(-10.6938119541341,4.49964460115605,
11.9531898578906));
#116825=CARTESIAN_POINT('Ctrl Pts',(-10.6395952408456,4.5039094313344,11.9890132974028));
#116826=CARTESIAN_POINT('Ctrl Pts',(-10.6298325274351,4.50467497751764,
11.9952589343325));
#116827=CARTESIAN_POINT('Ctrl Pts',(-10.61418628108,4.50589895765639,12.0049461186358));
#116828=CARTESIAN_POINT('Ctrl Pts',(-10.6083621375354,4.5063539377153,12.0084825211948));
#116829=CARTESIAN_POINT('Ctrl Pts',(-10.5973104458913,4.50721627887771,
12.0150625008954));
#116830=CARTESIAN_POINT('Ctrl Pts',(-10.5920894779881,4.50762323948006,
12.0181167404638));
#116831=CARTESIAN_POINT('Ctrl Pts',(-10.5802163198807,4.50854789850906,
12.0249402624885));
#116832=CARTESIAN_POINT('Ctrl Pts',(-10.5735505412796,4.50906643973288,
12.0286852246221));
#116833=CARTESIAN_POINT('Ctrl Pts',(-10.5531350602009,4.51065312716357,
12.0398949166697));
#116834=CARTESIAN_POINT('Ctrl Pts',(-10.5392731379948,4.51172849594223,
12.0471505500359));
#116835=CARTESIAN_POINT('Ctrl Pts',(-10.4472749848917,4.51885592383234,
12.0929931918995));
#116836=CARTESIAN_POINT('Ctrl Pts',(-10.3652196553214,4.52519829330641,
12.1230753603032));
#116837=CARTESIAN_POINT('Ctrl Pts',(-10.2153874672716,4.53652013414761,
12.1598336646745));
#116838=CARTESIAN_POINT('Ctrl Pts',(-10.1489025225625,4.54144974552421,
12.1702289855845));
#116839=CARTESIAN_POINT('Ctrl Pts',(-10.0741109404351,4.546676416282,12.1754417917166));
#116840=CARTESIAN_POINT('Ctrl Pts',(-10.0663285411522,4.54721636035049,
12.175906616167));
#116841=CARTESIAN_POINT('Ctrl Pts',(-10.0544679034948,4.54803272961443,
12.1764968967643));
#116842=CARTESIAN_POINT('Ctrl Pts',(-10.0503928586997,4.54831204362456,
12.1766784869538));
#116843=CARTESIAN_POINT('Ctrl Pts',(-10.0429333270717,4.54882109589726,
12.1769720719134));
#116844=CARTESIAN_POINT('Ctrl Pts',(-10.0395492715957,4.54905117556684,
12.1770906440683));
#116845=CARTESIAN_POINT('Ctrl Pts',(-10.0318750593658,4.54957103068973,
12.1773264036419));
#116846=CARTESIAN_POINT('Ctrl Pts',(-10.0275847348621,4.54986031971243,
12.1774347387318));
#116847=CARTESIAN_POINT('Ctrl Pts',(-10.0164101449972,4.55061053710988,
12.177655795767));
#116848=CARTESIAN_POINT('Ctrl Pts',(-10.009525198518,4.55106953834802,12.1777316087501));
#116849=CARTESIAN_POINT('Ctrl Pts',(-9.94811945672836,4.55513767886441,
12.1778692426881));
#116850=CARTESIAN_POINT('Ctrl Pts',(-9.89364873682566,4.55856777628396,
12.1742054967705));
#116851=CARTESIAN_POINT('Ctrl Pts',(-9.7699361677852,4.56633257232132,12.1572007205283));
#116852=CARTESIAN_POINT('Ctrl Pts',(-9.70125141872055,4.57063149165816,
12.141399093971));
#116853=CARTESIAN_POINT('Ctrl Pts',(-9.59787919830339,4.57751020548022,
12.107641160083));
#116854=CARTESIAN_POINT('Ctrl Pts',(-9.56197906516847,4.57997808144023,
12.0939411662865));
#116855=CARTESIAN_POINT('Ctrl Pts',(-9.51711045968681,4.58320071565414,
12.0742555816289));
#116856=CARTESIAN_POINT('Ctrl Pts',(-9.50746436613115,4.58390188078179,
12.0698672815768));
#116857=CARTESIAN_POINT('Ctrl Pts',(-9.49191018522385,4.58504678566279,
12.0625362790872));
#116858=CARTESIAN_POINT('Ctrl Pts',(-9.48596517053034,4.58548781757339,
12.0596729662286));
#116859=CARTESIAN_POINT('Ctrl Pts',(-9.47457148731538,4.58633985404428,
12.0540669560271));
#116860=CARTESIAN_POINT('Ctrl Pts',(-9.46911943692768,4.58675059584803,
12.0513315818908));
#116861=CARTESIAN_POINT('Ctrl Pts',(-9.4566358206962,4.5876981952847,12.0449465020946));
#116862=CARTESIAN_POINT('Ctrl Pts',(-9.44961940590022,4.58823603959938,
12.0412679866012));
#116863=CARTESIAN_POINT('Ctrl Pts',(-9.42712927411358,4.58997734158236,
12.0291862013365));
#116864=CARTESIAN_POINT('Ctrl Pts',(-9.41180735817389,4.59119037708787,
12.0205069641094));
#116865=CARTESIAN_POINT('Ctrl Pts',(-9.31483805942347,4.59904510937552,
11.9626685151572));
#116866=CARTESIAN_POINT('Ctrl Pts',(-9.23923100081285,4.6060341372894,11.9041026106128));
#116867=CARTESIAN_POINT('Ctrl Pts',(-9.14387898807866,4.61586835512337,
11.8097309595252));
#116868=CARTESIAN_POINT('Ctrl Pts',(-9.11760870544614,4.6187063855589,11.7810207417496));
#116869=CARTESIAN_POINT('Ctrl Pts',(-9.07970508688606,4.62295157698888,
11.7352376234035));
#116870=CARTESIAN_POINT('Ctrl Pts',(-9.06701971101092,4.6244012196619,11.7190723152465));
#116871=CARTESIAN_POINT('Ctrl Pts',(-9.05123709173938,4.62623486180655,
11.697838762465));
#116872=CARTESIAN_POINT('Ctrl Pts',(-9.04774697102238,4.62664234330034,
11.693068659624));
#116873=CARTESIAN_POINT('Ctrl Pts',(-9.04214729130931,4.627299126527,11.6852931707056));
#116874=CARTESIAN_POINT('Ctrl Pts',(-9.04001566983577,4.62754986567732,
11.6823039118573));
#116875=CARTESIAN_POINT('Ctrl Pts',(-9.03590562890243,4.62803465793218,
11.6764828442253));
#116876=CARTESIAN_POINT('Ctrl Pts',(-9.03392564509386,4.62826880932367,
11.6736522367678));
#116877=CARTESIAN_POINT('Ctrl Pts',(-9.02908276793474,4.62884312928643,
11.666663540382));
#116878=CARTESIAN_POINT('Ctrl Pts',(-9.02623405658253,4.62918236300633,
11.6624956130718));
#116879=CARTESIAN_POINT('Ctrl Pts',(-9.01804466287896,4.63016209846142,
11.6503468237788));
#116880=CARTESIAN_POINT('Ctrl Pts',(-9.01277453485048,4.63079827246414,
11.642318589494));
#116881=CARTESIAN_POINT('Ctrl Pts',(-8.97418231570867,4.6355072288593,11.5819319555626));
#116882=CARTESIAN_POINT('Ctrl Pts',(-8.94494293651263,4.63936527579464,
11.5270704846781));
#116883=CARTESIAN_POINT('Ctrl Pts',(-8.90398648983254,4.64571778886585,
11.4330026332319));
#116884=CARTESIAN_POINT('Ctrl Pts',(-8.88973941422442,4.64821553204775,
11.3950420761122));
#116885=CARTESIAN_POINT('Ctrl Pts',(-8.86111387621251,4.65412349941017,
11.3048886236862));
#116886=CARTESIAN_POINT('Ctrl Pts',(-8.84832068443017,4.65755435814954,
11.2522941351092));
#116887=CARTESIAN_POINT('Ctrl Pts',(-8.83722201608939,4.66186476759799,
11.1875566237165));
#116888=CARTESIAN_POINT('Ctrl Pts',(-8.83542793955184,4.66263241353258,
11.1760739256517));
#116889=CARTESIAN_POINT('Ctrl Pts',(-8.83285112336307,4.663858949278,11.1578134328437));
#116890=CARTESIAN_POINT('Ctrl Pts',(-8.83195681426822,4.66431435915672,
11.151051953945));
#116891=CARTESIAN_POINT('Ctrl Pts',(-8.8303804856278,4.66517701346931,11.1382816737736));
#116892=CARTESIAN_POINT('Ctrl Pts',(-8.82968591751854,4.66558385303865,
11.1322746223257));
#116893=CARTESIAN_POINT('Ctrl Pts',(-8.82821929078819,4.66650755023159,
11.1186730893941));
#116894=CARTESIAN_POINT('Ctrl Pts',(-8.82747475292135,4.66702524419319,
11.1110759778041));
#116895=CARTESIAN_POINT('Ctrl Pts',(-8.82543504329498,4.66860682553322,
11.0879492231059));
#116896=CARTESIAN_POINT('Ctrl Pts',(-8.82437423709542,4.6696778688018,11.0724011650262));
#116897=CARTESIAN_POINT('Ctrl Pts',(-8.81937287241452,4.67686336695797,
10.9688864273935));
#116898=CARTESIAN_POINT('Ctrl Pts',(-8.82500092438609,4.68327508990191,
10.8807518817124));
#116899=CARTESIAN_POINT('Ctrl Pts',(-8.84851253836293,4.69314412886784,
10.7483459189598));
#116900=CARTESIAN_POINT('Ctrl Pts',(-8.85933421271973,4.69655186893781,
10.7031242896483));
#116901=CARTESIAN_POINT('Ctrl Pts',(-8.87724568163762,4.70097950021217,
10.643975934462));
#116902=CARTESIAN_POINT('Ctrl Pts',(-8.8819784226795,4.70206934674861,10.6293813357934));
#116903=CARTESIAN_POINT('Ctrl Pts',(-8.89051312628796,4.703902207842,10.6047156935149));
#116904=CARTESIAN_POINT('Ctrl Pts',(-8.89417036398552,4.7046514808301,10.5945969383928));
#116905=CARTESIAN_POINT('Ctrl Pts',(-8.89960267635627,4.70571328342289,
10.5801877556245));
#116906=CARTESIAN_POINT('Ctrl Pts',(-8.90126512471728,4.70603182370425,
10.5758558428181));
#116907=CARTESIAN_POINT('Ctrl Pts',(-8.90419747552359,4.70658259929692,
10.568347838692));
#116908=CARTESIAN_POINT('Ctrl Pts',(-8.90545567738848,4.70681550383555,
10.5651672872587));
#116909=CARTESIAN_POINT('Ctrl Pts',(-8.90815927000994,4.70730873398822,
10.5584190914935));
#116910=CARTESIAN_POINT('Ctrl Pts',(-8.90960830924958,4.70756884278562,
10.5548530127831));
#116911=CARTESIAN_POINT('Ctrl Pts',(-8.91363440652476,4.70828019546412,
10.5450824301981));
#116912=CARTESIAN_POINT('Ctrl Pts',(-8.91624715859867,4.70872938789392,
10.5388926567701));
#116913=CARTESIAN_POINT('Ctrl Pts',(-8.92966213313801,4.71097603291763,
10.5078557521369));
#116914=CARTESIAN_POINT('Ctrl Pts',(-8.94126738929449,4.71273057957525,
10.4833621890808));
#116915=CARTESIAN_POINT('Ctrl Pts',(-8.9894891493147,4.71942446501789,10.3900517051512));
#116916=CARTESIAN_POINT('Ctrl Pts',(-9.0320561594786,4.72415706839001,10.3245331244351));
#116917=CARTESIAN_POINT('Ctrl Pts',(-9.11679481297087,4.73260498514031,
10.2187439545342));
#116918=CARTESIAN_POINT('Ctrl Pts',(-9.15604728247543,4.73624939421226,
10.1764983601737));
#116919=CARTESIAN_POINT('Ctrl Pts',(-9.2068599499617,4.74080021401076,10.1292745729884));
#116920=CARTESIAN_POINT('Ctrl Pts',(-9.2156108547363,4.74157833374439,10.1213831547994));
#116921=CARTESIAN_POINT('Ctrl Pts',(-9.22963773862795,4.74281774122112,
10.1091105321957));
#116922=CARTESIAN_POINT('Ctrl Pts',(-9.2348362589808,4.74327542031232,10.1046416897827));
#116923=CARTESIAN_POINT('Ctrl Pts',(-9.24468955974819,4.7441399884822,10.0963199074066));
#116924=CARTESIAN_POINT('Ctrl Pts',(-9.24933557250957,4.74454645161698,
10.0924568958592));
#116925=CARTESIAN_POINT('Ctrl Pts',(-9.25987627873562,4.74546606624515,
10.083828951764));
#116926=CARTESIAN_POINT('Ctrl Pts',(-9.26578761294311,4.74598002429814,
10.0790848690289));
#116927=CARTESIAN_POINT('Ctrl Pts',(-9.28337823068622,4.74750451204133,
10.0652447163958));
#116928=CARTESIAN_POINT('Ctrl Pts',(-9.29518331334793,4.7485213098117,10.0563117018003));
#116929=CARTESIAN_POINT('Ctrl Pts',(-9.3834523900869,4.75608169018832,9.9920979262408));
#116930=CARTESIAN_POINT('Ctrl Pts',(-9.4661318174951,4.76297386497827,9.94597173662926));
#116931=CARTESIAN_POINT('Ctrl Pts',(-9.6101393026443,4.77439150988871,9.88695777810674));
#116932=CARTESIAN_POINT('Ctrl Pts',(-9.66860898375979,4.7788729784233,9.86817136444711));
#116933=CARTESIAN_POINT('Ctrl Pts',(-9.73569462249501,4.78367708283696,
9.85226493786488));
#116934=CARTESIAN_POINT('Ctrl Pts',(-9.74312480958272,4.78420455164554,
9.85057916776584));
#116935=CARTESIAN_POINT('Ctrl Pts',(-9.75452125070296,4.78500600213383,
9.84810956128453));
#116936=CARTESIAN_POINT('Ctrl Pts',(-9.75847588529832,4.78528271894022,
9.84727388230923));
#116937=CARTESIAN_POINT('Ctrl Pts',(-9.76575371767529,4.78578931728173,
9.84577505485302));
#116938=CARTESIAN_POINT('Ctrl Pts',(-9.76907549402655,4.78601951768966,
9.84510588456476));
#116939=CARTESIAN_POINT('Ctrl Pts',(-9.77665547041992,4.78654251660726,
9.84361291387361));
#116940=CARTESIAN_POINT('Ctrl Pts',(-9.7809153732916,4.78683480244171,9.84279828911069));
#116941=CARTESIAN_POINT('Ctrl Pts',(-9.79381884848504,4.78771547281951,
9.84040455437087));
#116942=CARTESIAN_POINT('Ctrl Pts',(-9.80247590263699,4.78829998253793,
9.8388985804029));
#116943=CARTESIAN_POINT('Ctrl Pts',(-9.81114930150162,4.7888800033368,9.83748958018576));
#116944=CARTESIAN_POINT('Origin',(-10.,2.67563288526385,11.));
#116945=CARTESIAN_POINT('',(-9.81114929911337,5.38686993568377,9.83748958057373));
#116946=CARTESIAN_POINT('',(-9.81114934765212,5.28707251297004,9.83748957268858));
#116947=CARTESIAN_POINT('',(-9.81114930150157,2.67563288526385,9.83748958018577));
#116948=CARTESIAN_POINT('Ctrl Pts',(-9.81114929672518,5.38686993568377,
9.8374895809617));
#116949=CARTESIAN_POINT('Ctrl Pts',(-9.77383957756958,5.38451728128952,
9.84355057326433));
#116950=CARTESIAN_POINT('Ctrl Pts',(-9.73684185792727,5.38214351580701,
9.85140438837419));
#116951=CARTESIAN_POINT('Ctrl Pts',(-9.68265892178359,5.37855494172641,
9.86566237149448));
#116952=CARTESIAN_POINT('Ctrl Pts',(-9.66514465425574,5.37737732064956,
9.87070860271603));
#116953=CARTESIAN_POINT('Ctrl Pts',(-9.63416603170385,5.37525765284383,
9.88041821359246));
#116954=CARTESIAN_POINT('Ctrl Pts',(-9.62065574617396,5.37432056159209,
9.88492342077664));
#116955=CARTESIAN_POINT('Ctrl Pts',(-9.60028242012395,5.37288646857356,
9.89213031350666));
#116956=CARTESIAN_POINT('Ctrl Pts',(-9.5933572742663,5.37239528108828,9.89465341390828));
#116957=CARTESIAN_POINT('Ctrl Pts',(-9.58081112709059,5.37149839681785,
9.8993583225349));
#116958=CARTESIAN_POINT('Ctrl Pts',(-9.57518228935085,5.37109342009036,
9.90151862839889));
#116959=CARTESIAN_POINT('Ctrl Pts',(-9.56304360255536,5.37021434086383,
9.90628461888746));
#116960=CARTESIAN_POINT('Ctrl Pts',(-9.55653997020156,5.36973974969493,
9.9089053998624));
#116961=CARTESIAN_POINT('Ctrl Pts',(-9.53880849051417,5.36843573250735,
9.91623540783355));
#116962=CARTESIAN_POINT('Ctrl Pts',(-9.52762991922011,5.3676024614754,9.92106080469345));
#116963=CARTESIAN_POINT('Ctrl Pts',(-9.4507630739026,5.36179286740916,9.95566504243812));
#116964=CARTESIAN_POINT('Ctrl Pts',(-9.38786793819306,5.35661775705928,
9.99124449867526));
#116965=CARTESIAN_POINT('Ctrl Pts',(-9.28519044294973,5.34748274547146,
10.0624831964507));
#116966=CARTESIAN_POINT('Ctrl Pts',(-9.24382927970387,5.34358089192591,
10.095513198855));
#116967=CARTESIAN_POINT('Ctrl Pts',(-9.17813003333663,5.33711477866057,
10.155645442417));
#116968=CARTESIAN_POINT('Ctrl Pts',(-9.15257050671636,5.33452115345847,
10.1813006265899));
#116969=CARTESIAN_POINT('Ctrl Pts',(-9.12353971114573,5.33151833365936,
10.213259190026));
#116970=CARTESIAN_POINT('Ctrl Pts',(-9.118894346754,5.33103599336783,10.2184652447055));
#116971=CARTESIAN_POINT('Ctrl Pts',(-9.11172086145086,5.33028866210104,
10.2266498264172));
#116972=CARTESIAN_POINT('Ctrl Pts',(-9.10916092177233,5.33002146333288,
10.2296000669919));
#116973=CARTESIAN_POINT('Ctrl Pts',(-9.10439473139028,5.32952312032252,
10.2351484573874));
#116974=CARTESIAN_POINT('Ctrl Pts',(-9.1021850863348,5.32929174278562,10.2377434417703));
#116975=CARTESIAN_POINT('Ctrl Pts',(-9.09710806630722,5.32875926311865,
10.2437585464309));
#116976=CARTESIAN_POINT('Ctrl Pts',(-9.09424883040803,5.32845874102173,
10.2471854143134));
#116977=CARTESIAN_POINT('Ctrl Pts',(-9.08503193542932,5.32748757334217,
10.25836062885));
#116978=CARTESIAN_POINT('Ctrl Pts',(-9.07875348478723,5.3268222393217,10.2661741414961));
#116979=CARTESIAN_POINT('Ctrl Pts',(-9.02563801185253,5.32115109750923,
10.3340324882525));
#116980=CARTESIAN_POINT('Ctrl Pts',(-8.98462028609136,5.31647442145438,
10.3984176284241));
#116981=CARTESIAN_POINT('Ctrl Pts',(-8.91877512769588,5.30748431055952,
10.5279535045634));
#116982=CARTESIAN_POINT('Ctrl Pts',(-8.89293734698695,5.30319302654339,
10.5922181935774));
#116983=CARTESIAN_POINT('Ctrl Pts',(-8.86727296043656,5.29746484354759,
10.6768917709104));
#116984=CARTESIAN_POINT('Ctrl Pts',(-8.8621177354506,5.29619937239654,10.695544162278));
#116985=CARTESIAN_POINT('Ctrl Pts',(-8.85540876014022,5.29436959629865,
10.7223761298572));
#116986=CARTESIAN_POINT('Ctrl Pts',(-8.85347842193886,5.29381720877396,
10.7304589367145));
#116987=CARTESIAN_POINT('Ctrl Pts',(-8.85027082141928,5.2928519470735,10.744548282752));
#116988=CARTESIAN_POINT('Ctrl Pts',(-8.84895468459916,5.29244031800254,
10.7505457088158));
#116989=CARTESIAN_POINT('Ctrl Pts',(-8.8463412736594,5.29158964127037,10.7629158425951));
#116990=CARTESIAN_POINT('Ctrl Pts',(-8.84504976925513,5.29115042726968,
10.7692895404749));
#116991=CARTESIAN_POINT('Ctrl Pts',(-8.84187814143452,5.29002149604888,
10.7856362527082));
#116992=CARTESIAN_POINT('Ctrl Pts',(-8.84007405125164,5.28932942257549,
10.7956232946519));
#116993=CARTESIAN_POINT('Ctrl Pts',(-8.83335786323388,5.28653782764351,
10.8357612510318));
#116994=CARTESIAN_POINT('Ctrl Pts',(-8.82949097789187,5.2844063735152,10.866072490169));
#116995=CARTESIAN_POINT('Ctrl Pts',(-8.81876839943437,5.27576234468517,
10.9876121294635));
#116996=CARTESIAN_POINT('Ctrl Pts',(-8.82137296420124,5.26898842046517,
11.0793454637697));
#116997=CARTESIAN_POINT('Ctrl Pts',(-8.84023647551718,5.25944943377978,
11.2087901399952));
#116998=CARTESIAN_POINT('Ctrl Pts',(-8.84786332197083,5.25660940960404,
11.2474397824672));
#116999=CARTESIAN_POINT('Ctrl Pts',(-8.85969799244893,5.25319324378736,
11.2947798968669));
#117000=CARTESIAN_POINT('Ctrl Pts',(-8.86209306935238,5.25253849845545,
11.3038942038931));
#117001=CARTESIAN_POINT('Ctrl Pts',(-8.86576683691049,5.25158640962711,
11.3172216270186));
#117002=CARTESIAN_POINT('Ctrl Pts',(-8.86696009361955,5.25128459030296,
11.3214576193168));
#117003=CARTESIAN_POINT('Ctrl Pts',(-8.86911565861918,5.25075237509649,
11.3289486107772));
#117004=CARTESIAN_POINT('Ctrl Pts',(-8.87006832596017,5.2505214481757,11.3322062539182));
#117005=CARTESIAN_POINT('Ctrl Pts',(-8.87217340130492,5.25002039625304,
11.3392907263693));
#117006=CARTESIAN_POINT('Ctrl Pts',(-8.87333121314125,5.24975058201332,
11.3431158399504));
#117007=CARTESIAN_POINT('Ctrl Pts',(-8.87662789171236,5.24899802102508,
11.3538105900437));
#117008=CARTESIAN_POINT('Ctrl Pts',(-8.87881031257755,5.24851768048171,
11.3606667692848));
#117009=CARTESIAN_POINT('Ctrl Pts',(-8.89247986271362,5.24561223097657,
11.4022867816741));
#117010=CARTESIAN_POINT('Ctrl Pts',(-8.90552126588685,5.24326647971728,
11.4365230637684));
#117011=CARTESIAN_POINT('Ctrl Pts',(-8.96477539437933,5.23391228628043,
11.5726352900586));
#117012=CARTESIAN_POINT('Ctrl Pts',(-9.02378587616673,5.22721385814172,
11.6682876468));
#117013=CARTESIAN_POINT('Ctrl Pts',(-9.10837370719953,5.21867353291113,
11.7697454049295));
#117014=CARTESIAN_POINT('Ctrl Pts',(-9.12174453154593,5.21734998302817,
11.7849666796344));
#117015=CARTESIAN_POINT('Ctrl Pts',(-9.14124519040035,5.21545113474133,
11.8060439142007));
#117016=CARTESIAN_POINT('Ctrl Pts',(-9.14705637021043,5.21488905655065,
11.8121907244224));
#117017=CARTESIAN_POINT('Ctrl Pts',(-9.15721663689287,5.21391243778539,
11.8227085000909));
#117018=CARTESIAN_POINT('Ctrl Pts',(-9.16153482086476,5.21349922796665,
11.827108949397));
#117019=CARTESIAN_POINT('Ctrl Pts',(-9.16990125761127,5.21270206108784,
11.8355019250035));
#117020=CARTESIAN_POINT('Ctrl Pts',(-9.17394427235542,5.21231833910881,
11.8394994470958));
#117021=CARTESIAN_POINT('Ctrl Pts',(-9.18357072410076,5.21140811831416,
11.8488807088324));
#117022=CARTESIAN_POINT('Ctrl Pts',(-9.18917865489282,5.21088054100748,
11.8542388200649));
#117023=CARTESIAN_POINT('Ctrl Pts',(-9.20923034713505,5.20900320872296,
11.8730219148817));
#117024=CARTESIAN_POINT('Ctrl Pts',(-9.22395720347804,5.20764074116543,
11.8861384794655));
#117025=CARTESIAN_POINT('Ctrl Pts',(-9.32431559389986,5.19845718146427,
11.9711023166934));
#117026=CARTESIAN_POINT('Ctrl Pts',(-9.41946460329918,5.19014945770986,
12.0308047578809));
#117027=CARTESIAN_POINT('Ctrl Pts',(-9.55520952467588,5.17935550942639,
12.0911517606643));
#117028=CARTESIAN_POINT('Ctrl Pts',(-9.58954065153449,5.17671391924322,
12.1045245228352));
#117029=CARTESIAN_POINT('Ctrl Pts',(-9.63127260505924,5.17364879671387,
12.1185647318539));
#117030=CARTESIAN_POINT('Ctrl Pts',(-9.63812108617193,5.17315040410591,
12.1207990940866));
#117031=CARTESIAN_POINT('Ctrl Pts',(-9.64880220310638,5.17238070331368,
12.1241757676518));
#117032=CARTESIAN_POINT('Ctrl Pts',(-9.65262074405741,5.17210703527531,
12.125361587602));
#117033=CARTESIAN_POINT('Ctrl Pts',(-9.6596916007007,5.17160314818303,12.1275179707317));
#117034=CARTESIAN_POINT('Ctrl Pts',(-9.66294208077079,5.17137263762025,
12.1284939257797));
#117035=CARTESIAN_POINT('Ctrl Pts',(-9.6704145529168,5.17084526247733,12.1307023650096));
#117036=CARTESIAN_POINT('Ctrl Pts',(-9.67463927349406,5.17054894518587,
12.1319252644798));
#117037=CARTESIAN_POINT('Ctrl Pts',(-9.68792298917391,5.16962273422924,
12.1356898892993));
#117038=CARTESIAN_POINT('Ctrl Pts',(-9.6970059153899,5.16899742081043,12.1381468199288));
#117039=CARTESIAN_POINT('Ctrl Pts',(-9.74411778931241,5.16579055321982,
12.1502865935834));
#117040=CARTESIAN_POINT('Ctrl Pts',(-9.78258770476654,5.16329412667142,
12.1581742065285));
#117041=CARTESIAN_POINT('Ctrl Pts',(-9.91148474980412,5.15512027463574,
12.1779513966106));
#117042=CARTESIAN_POINT('Ctrl Pts',(-10.0028838238839,5.14960684017788,
12.1812690027037));
#117043=CARTESIAN_POINT('Ctrl Pts',(-10.1245626232589,5.14182845144815,
12.1715521982986));
#117044=CARTESIAN_POINT('Ctrl Pts',(-10.1552619548405,5.13983099362933,
12.1678800750543));
#117045=CARTESIAN_POINT('Ctrl Pts',(-10.1958429888563,5.13712553053322,
12.1613976258602));
#117046=CARTESIAN_POINT('Ctrl Pts',(-10.2058849732749,5.13645074394458,
12.1596595572523));
#117047=CARTESIAN_POINT('Ctrl Pts',(-10.2223048843288,5.13533807897131,
12.1565976014719));
#117048=CARTESIAN_POINT('Ctrl Pts',(-10.2286967597792,5.13490262297411,
12.1553507097474));
#117049=CARTESIAN_POINT('Ctrl Pts',(-10.2410903698406,5.13405361896181,
12.152826156166));
#117050=CARTESIAN_POINT('Ctrl Pts',(-10.2470931181834,5.13364027185536,
12.1515544716907));
#117051=CARTESIAN_POINT('Ctrl Pts',(-10.2611766109388,5.13266532025565,
12.1484556912962));
#117052=CARTESIAN_POINT('Ctrl Pts',(-10.2692484687094,5.13210251703561,
12.14659014168));
#117053=CARTESIAN_POINT('Ctrl Pts',(-10.295957548229,5.13022652122012,12.1401196140459));
#117054=CARTESIAN_POINT('Ctrl Pts',(-10.3145009823067,5.12890172417182,
12.1351443353065));
#117055=CARTESIAN_POINT('Ctrl Pts',(-10.3975680186762,5.12286231762431,
12.1106655352585));
#117056=CARTESIAN_POINT('Ctrl Pts',(-10.4604578121652,5.11799110665826,
12.0861005208796));
#117057=CARTESIAN_POINT('Ctrl Pts',(-10.5911172768324,5.1073212803377,12.0216682488829));
#117058=CARTESIAN_POINT('Ctrl Pts',(-10.6577175852677,5.10152431010428,
11.9801199295008));
#117059=CARTESIAN_POINT('Ctrl Pts',(-10.7274423234572,5.09535074712509,
11.9262927586026));
#117060=CARTESIAN_POINT('Ctrl Pts',(-10.7351053454085,5.0946709144487,11.920223209443));
#117061=CARTESIAN_POINT('Ctrl Pts',(-10.74617443561,5.09368800044318,11.9112293374319));
#117062=CARTESIAN_POINT('Ctrl Pts',(-10.7496405323456,5.09338008553982,
11.9083800238188));
#117063=CARTESIAN_POINT('Ctrl Pts',(-10.7557130946631,5.09284051450154,
11.9033296286212));
#117064=CARTESIAN_POINT('Ctrl Pts',(-10.7583264006519,5.09260828128118,
11.9011369322361));
#117065=CARTESIAN_POINT('Ctrl Pts',(-10.7639005616079,5.09211289672363,
11.8964185066615));
#117066=CARTESIAN_POINT('Ctrl Pts',(-10.7668584546817,5.09184998963851,
11.893889433146));
#117067=CARTESIAN_POINT('Ctrl Pts',(-10.7750339078488,5.09112305548,11.8868287663237));
#117068=CARTESIAN_POINT('Ctrl Pts',(-10.7802243031159,5.09066123072138,
11.8822657545132));
#117069=CARTESIAN_POINT('Ctrl Pts',(-10.8113039855021,5.0878918012946,11.8544539996888));
#117070=CARTESIAN_POINT('Ctrl Pts',(-10.8361953765718,5.08565643491603,
11.8301105920734));
#117071=CARTESIAN_POINT('Ctrl Pts',(-10.9163563298724,5.07824582340873,
11.7444432170743));
#117072=CARTESIAN_POINT('Ctrl Pts',(-10.966250790811,5.07324847894144,11.6784284628813));
#117073=CARTESIAN_POINT('Ctrl Pts',(-11.0323191741656,5.06520506690983,
11.5687558494935));
#117074=CARTESIAN_POINT('Ctrl Pts',(-11.0535207903303,5.06229974692301,
11.5284499246184));
#117075=CARTESIAN_POINT('Ctrl Pts',(-11.0770875526717,5.05855865942498,
11.476560057148));
#117076=CARTESIAN_POINT('Ctrl Pts',(-11.0816854199365,5.05779954922199,
11.4660297429387));
#117077=CARTESIAN_POINT('Ctrl Pts',(-11.0887552740787,5.05658341400903,
11.4491694147342));
#117078=CARTESIAN_POINT('Ctrl Pts',(-11.0913278928781,5.05612976466467,
11.4428821930669));
#117079=CARTESIAN_POINT('Ctrl Pts',(-11.0958654931348,5.05530899895008,
11.4315131125838));
#117080=CARTESIAN_POINT('Ctrl Pts',(-11.0978498886201,5.05494254094094,
11.4264391700164));
#117081=CARTESIAN_POINT('Ctrl Pts',(-11.1024407955994,5.0540766205341,11.4144561291335));
#117082=CARTESIAN_POINT('Ctrl Pts',(-11.1050176481486,5.0535761955108,11.4075359907606));
#117083=CARTESIAN_POINT('Ctrl Pts',(-11.1123965078601,5.05209963592151,
11.3871354378024));
#117084=CARTESIAN_POINT('Ctrl Pts',(-11.1170179558219,5.05111767257959,
11.3735916126547));
#117085=CARTESIAN_POINT('Ctrl Pts',(-11.1368686147346,5.04662464344426,
11.3117516970751));
#117086=CARTESIAN_POINT('Ctrl Pts',(-11.1492181346826,5.04302380785564,
11.2625944156849));
#117087=CARTESIAN_POINT('Ctrl Pts',(-11.1724229198635,5.0337217525597,11.1362808312511));
#117088=CARTESIAN_POINT('Ctrl Pts',(-11.1788629978936,5.02794353485431,
11.058560484151));
#117089=CARTESIAN_POINT('Ctrl Pts',(-11.1771109855138,5.02019302164646,
10.95124557561));
#117090=CARTESIAN_POINT('Ctrl Pts',(-11.1755183098171,5.0180881803883,10.9217421322267));
#117091=CARTESIAN_POINT('Ctrl Pts',(-11.1721959031427,5.01556141155346,
10.8855530531357));
#117092=CARTESIAN_POINT('Ctrl Pts',(-11.1715152869319,5.01509119052823,
10.8787841720338));
#117093=CARTESIAN_POINT('Ctrl Pts',(-11.1703513971733,5.01435568545808,
10.8681366580499));
#117094=CARTESIAN_POINT('Ctrl Pts',(-11.1699074157735,5.0140883535152,10.8642540112942));
#117095=CARTESIAN_POINT('Ctrl Pts',(-11.1690806298808,5.01361320484443,
10.8573292483185));
#117096=CARTESIAN_POINT('Ctrl Pts',(-11.1687052719952,5.0134049926363,10.8542864108302));
#117097=CARTESIAN_POINT('Ctrl Pts',(-11.167770037172,5.01290372551258,10.8469411018433));
#117098=CARTESIAN_POINT('Ctrl Pts',(-11.1671982631466,5.01261133081293,
10.842640214722));
#117099=CARTESIAN_POINT('Ctrl Pts',(-11.1653543158997,5.01170983696046,
10.8293333536938));
#117100=CARTESIAN_POINT('Ctrl Pts',(-11.1640015424532,5.01110497722067,
10.8203386314895));
#117101=CARTESIAN_POINT('Ctrl Pts',(-11.1514904161216,5.00595181152115,
10.7432353949822));
#117102=CARTESIAN_POINT('Ctrl Pts',(-11.1344677578868,5.00168011800253,
10.6762039996229));
#117103=CARTESIAN_POINT('Ctrl Pts',(-11.0843042130208,4.99228203334683,
10.5328331340842));
#117104=CARTESIAN_POINT('Ctrl Pts',(-11.0487669327679,4.98717073271439,
10.4577395044924));
#117105=CARTESIAN_POINT('Ctrl Pts',(-10.9973871434363,4.98074389667977,
10.3734492959406));
#117106=CARTESIAN_POINT('Ctrl Pts',(-10.9888547086039,4.97970184073197,
10.3600677964907));
#117107=CARTESIAN_POINT('Ctrl Pts',(-10.9757905009485,4.97814028266468,
10.3404644894427));
#117108=CARTESIAN_POINT('Ctrl Pts',(-10.9714636917894,4.97762831546317,
10.3341077547538));
#117109=CARTESIAN_POINT('Ctrl Pts',(-10.9636195088911,4.97670908900929,
10.3228226530725));
#117110=CARTESIAN_POINT('Ctrl Pts',(-10.9601257621239,4.97630272654266,
10.3178781372223));
#117111=CARTESIAN_POINT('Ctrl Pts',(-10.952633409262,4.97543756494151,10.3074462126003));
#117112=CARTESIAN_POINT('Ctrl Pts',(-10.9486251765066,4.97497840917501,
10.3019660237129));
#117113=CARTESIAN_POINT('Ctrl Pts',(-10.9377167239613,4.9737384173116,10.2873191132736));
#117114=CARTESIAN_POINT('Ctrl Pts',(-10.9307297150587,4.97295425980651,
10.2782182587006));
#117115=CARTESIAN_POINT('Ctrl Pts',(-10.8918682053794,4.96864537509792,
10.2291022733612));
#117116=CARTESIAN_POINT('Ctrl Pts',(-10.8575496183533,4.96502459233316,
10.1910997863715));
#117117=CARTESIAN_POINT('Ctrl Pts',(-10.7708038815786,4.95628839840166,
10.1067856336749));
#117118=CARTESIAN_POINT('Ctrl Pts',(-10.7165060587857,4.95112187008965,
10.0626693950568));
#117119=CARTESIAN_POINT('Ctrl Pts',(-10.643428359353,4.94469951640419,10.0133738950112));
#117120=CARTESIAN_POINT('Ctrl Pts',(-10.6279929546477,4.94337093645498,
10.0034780364284));
#117121=CARTESIAN_POINT('Ctrl Pts',(-10.5915767333335,4.94030984370705,
9.98131338874795));
#117122=CARTESIAN_POINT('Ctrl Pts',(-10.5704334501427,4.93858717391493,
9.96932482500798));
#117123=CARTESIAN_POINT('Ctrl Pts',(-10.5431961669236,4.93644936836165,
9.95497606352385));
#117124=CARTESIAN_POINT('Ctrl Pts',(-10.5374345746495,4.93600165472439,
9.95200134240666));
#117125=CARTESIAN_POINT('Ctrl Pts',(-10.528259102095,4.93529611153656,9.94735959986447));
#117126=CARTESIAN_POINT('Ctrl Pts',(-10.5248613204555,4.93503644661463,
9.94566130381987));
#117127=CARTESIAN_POINT('Ctrl Pts',(-10.5183733769119,4.93454376041603,
9.94245760416173));
#117128=CARTESIAN_POINT('Ctrl Pts',(-10.5152848539088,4.93431057640804,
9.94094929464511));
#117129=CARTESIAN_POINT('Ctrl Pts',(-10.5079140699309,4.93375721855073,
9.93738958005762));
#117130=CARTESIAN_POINT('Ctrl Pts',(-10.5036259356046,4.93343779209456,
9.93535051499438));
#117131=CARTESIAN_POINT('Ctrl Pts',(-10.4890041787416,4.93235669773757,
9.92850578643829));
#117132=CARTESIAN_POINT('Ctrl Pts',(-10.4786128071935,4.93160205575712,
9.92382401955124));
#117133=CARTESIAN_POINT('Ctrl Pts',(-10.4529516563136,4.92976788168413,
9.91270778364184));
#117134=CARTESIAN_POINT('Ctrl Pts',(-10.4376105871074,4.9286964957058,9.90644314390221));
#117135=CARTESIAN_POINT('Ctrl Pts',(-10.3723904892332,4.92422629048837,
9.8814024700492));
#117136=CARTESIAN_POINT('Ctrl Pts',(-10.3213964288365,4.92093495731556,
9.86569832859299));
#117137=CARTESIAN_POINT('Ctrl Pts',(-10.1932275076868,4.91279051138116,
9.83556928329505));
#117138=CARTESIAN_POINT('Ctrl Pts',(-10.1153543503117,4.90794033421488,
9.82529695337106));
#117139=CARTESIAN_POINT('Ctrl Pts',(-10.021025004204,4.901797638359,9.82232864202871));
#117140=CARTESIAN_POINT('Ctrl Pts',(-10.0049995052522,4.90074553332221,
9.82215160432838));
#117141=CARTESIAN_POINT('Ctrl Pts',(-9.98125717062269,4.89917182107703,
9.8223738478858));
#117142=CARTESIAN_POINT('Ctrl Pts',(-9.97353941221862,4.89865792473856,
9.82252198306959));
#117143=CARTESIAN_POINT('Ctrl Pts',(-9.95976890387531,4.8977365666231,9.82292174674305));
#117144=CARTESIAN_POINT('Ctrl Pts',(-9.95371553428081,4.89733001803941,
9.8231442308925));
#117145=CARTESIAN_POINT('Ctrl Pts',(-9.9408987645737,4.89646586980267,9.82371433369115));
#117146=CARTESIAN_POINT('Ctrl Pts',(-9.9341361301628,4.89600792426916,9.82407361108874));
#117147=CARTESIAN_POINT('Ctrl Pts',(-9.91600589500242,4.89477468058692,
9.82519369663301));
#117148=CARTESIAN_POINT('Ctrl Pts',(-9.90464585239356,4.89399612332243,
9.82606114689032));
#117149=CARTESIAN_POINT('Ctrl Pts',(-9.86579458385425,4.8913126402476,9.82959545185898));
#117150=CARTESIAN_POINT('Ctrl Pts',(-9.8383940495945,4.88938401548889,9.8330636497039));
#117151=CARTESIAN_POINT('Ctrl Pts',(-9.81114928023156,4.88742944622416,
9.8374895836411));
#117152=CARTESIAN_POINT('Ctrl Pts',(-9.81114930150162,4.7888800033368,9.83748958018576));
#117153=CARTESIAN_POINT('Ctrl Pts',(-9.81144932862408,4.78890006720957,
9.8374408405524));
#117154=CARTESIAN_POINT('Ctrl Pts',(-9.81174937530434,4.78892012571072,
9.83739221695604));
#117155=CARTESIAN_POINT('Ctrl Pts',(-9.87979352543049,4.79346745574619,
9.82639246051551));
#117156=CARTESIAN_POINT('Ctrl Pts',(-9.94837521288134,4.79771647491303,
9.82138140135665));
#117157=CARTESIAN_POINT('Ctrl Pts',(-10.1002918206641,4.80711738079732,
9.82357586222741));
#117158=CARTESIAN_POINT('Ctrl Pts',(-10.1832000021336,4.81225366063202,
9.83360899739349));
#117159=CARTESIAN_POINT('Ctrl Pts',(-10.2797977998483,4.81870752550248,
9.85585863549241));
#117160=CARTESIAN_POINT('Ctrl Pts',(-10.2951689211226,4.81974830798736,
9.85972742728444));
#117161=CARTESIAN_POINT('Ctrl Pts',(-10.3178694174919,4.82130824038348,
9.86593071323048));
#117162=CARTESIAN_POINT('Ctrl Pts',(-10.3252619589583,4.82181987677813,
9.86802881346254));
#117163=CARTESIAN_POINT('Ctrl Pts',(-10.3384391827347,4.82273863779968,
9.87190842024684));
#117164=CARTESIAN_POINT('Ctrl Pts',(-10.3442317128404,4.82314486774321,
9.87366247586994));
#117165=CARTESIAN_POINT('Ctrl Pts',(-10.356492972385,4.82400988232411,9.87747876710599));
#117166=CARTESIAN_POINT('Ctrl Pts',(-10.362957881295,4.82446902443469,9.87955244177456));
#117167=CARTESIAN_POINT('Ctrl Pts',(-10.380303027397,4.82570931001288,9.88528191426843));
#117168=CARTESIAN_POINT('Ctrl Pts',(-10.3911481127463,4.82649377901595,
9.88904098138364));
#117169=CARTESIAN_POINT('Ctrl Pts',(-10.4501353397126,4.83081124885458,
9.91045760202083));
#117170=CARTESIAN_POINT('Ctrl Pts',(-10.4971333857008,4.8344407822134,9.93108393590812));
#117171=CARTESIAN_POINT('Ctrl Pts',(-10.6055015085322,4.84325937306923,
9.98733985229364));
#117172=CARTESIAN_POINT('Ctrl Pts',(-10.6652961909556,4.84850285222669,
10.0255808468813));
#117173=CARTESIAN_POINT('Ctrl Pts',(-10.7527856428889,4.85656082267927,
10.0933598301527));
#117174=CARTESIAN_POINT('Ctrl Pts',(-10.7830284947511,4.85942679321481,
10.1193470126605));
#117175=CARTESIAN_POINT('Ctrl Pts',(-10.8172064231,4.8627123686331,10.1518712285529));
#117176=CARTESIAN_POINT('Ctrl Pts',(-10.8224673008177,4.86321947546268,
10.1569719478138));
#117177=CARTESIAN_POINT('Ctrl Pts',(-10.8305440844558,4.86399967934948,
10.1649504270405));
#117178=CARTESIAN_POINT('Ctrl Pts',(-10.8333933065157,4.86427523681034,
10.1677939777956));
#117179=CARTESIAN_POINT('Ctrl Pts',(-10.83861509026,4.86478076286787,10.1730590802628));
#117180=CARTESIAN_POINT('Ctrl Pts',(-10.8409917872438,4.86501104019017,
10.1754762776879));
#117181=CARTESIAN_POINT('Ctrl Pts',(-10.8464003797232,4.86553554323703,
10.1810247528577));
#117182=CARTESIAN_POINT('Ctrl Pts',(-10.8494253608081,4.86582924395821,
10.1841626288553));
#117183=CARTESIAN_POINT('Ctrl Pts',(-10.8587831138173,4.86673918113316,
10.1939780913136));
#117184=CARTESIAN_POINT('Ctrl Pts',(-10.8650552679232,4.86735106214369,
10.2007133492027));
#117185=CARTESIAN_POINT('Ctrl Pts',(-10.8796505764579,4.86878163612467,
10.2167593836701));
#117186=CARTESIAN_POINT('Ctrl Pts',(-10.8879060028588,4.86959612322724,
10.2261305300146));
#117187=CARTESIAN_POINT('Ctrl Pts',(-10.9174926071089,4.87254258411477,
10.2608126646368));
#117188=CARTESIAN_POINT('Ctrl Pts',(-10.9379045773303,4.87462933624073,
10.2868899677504));
#117189=CARTESIAN_POINT('Ctrl Pts',(-11.0020586212681,4.88150099022316,
10.3763787963712));
#117190=CARTESIAN_POINT('Ctrl Pts',(-11.0406780308878,4.88618878943377,
10.443210898045));
#117191=CARTESIAN_POINT('Ctrl Pts',(-11.0879880207593,4.89343246841507,
10.547471116482));
#117192=CARTESIAN_POINT('Ctrl Pts',(-11.1018381841972,4.89584096618305,
10.5823248770731));
#117193=CARTESIAN_POINT('Ctrl Pts',(-11.1175547335366,4.8990236667496,10.6281313287243));
#117194=CARTESIAN_POINT('Ctrl Pts',(-11.1209626835328,4.89974751920242,
10.638534178552));
#117195=CARTESIAN_POINT('Ctrl Pts',(-11.1262142547077,4.90092026852565,
10.6553537157111));
#117196=CARTESIAN_POINT('Ctrl Pts',(-11.1281492390682,4.90136620292018,
10.6617413710231));
#117197=CARTESIAN_POINT('Ctrl Pts',(-11.1317421650146,4.9022215415435,10.6739759722585));
#117198=CARTESIAN_POINT('Ctrl Pts',(-11.1334093513402,4.90263063272673,
10.679819996474));
#117199=CARTESIAN_POINT('Ctrl Pts',(-11.1371385024988,4.90357461764932,
10.6932860716369));
#117200=CARTESIAN_POINT('Ctrl Pts',(-11.1391691742857,4.90411049264994,
10.7009164083062));
#117201=CARTESIAN_POINT('Ctrl Pts',(-11.1453255622494,4.90580682045551,
10.7250220575759));
#117202=CARTESIAN_POINT('Ctrl Pts',(-11.1491715564009,4.90697603268181,
10.7415658801416));
#117203=CARTESIAN_POINT('Ctrl Pts',(-11.157362473948,4.90974853018851,10.7806097042691));
#117204=CARTESIAN_POINT('Ctrl Pts',(-11.1614110106253,4.91136031355026,
10.8031641725468));
#117205=CARTESIAN_POINT('Ctrl Pts',(-11.1821491163321,4.92133230655422,
10.9418476099529));
#117206=CARTESIAN_POINT('Ctrl Pts',(-11.1820646756277,4.93016371082831,
11.0597933233473));
#117207=CARTESIAN_POINT('Ctrl Pts',(-11.1621508531987,4.93963510711482,
11.1917316485292));
#117208=CARTESIAN_POINT('Ctrl Pts',(-11.1594137199758,4.94076881184951,
11.2076427701734));
#117209=CARTESIAN_POINT('Ctrl Pts',(-11.1552858047043,4.9422748055171,11.2290005059576));
#117210=CARTESIAN_POINT('Ctrl Pts',(-11.154182089105,4.94266116510058,11.2344999586727));
#117211=CARTESIAN_POINT('Ctrl Pts',(-11.1523773693867,4.94326785470465,
11.2431707358121));
#117212=CARTESIAN_POINT('Ctrl Pts',(-11.1517024823791,4.94348959354747,
11.2463473177439));
#117213=CARTESIAN_POINT('Ctrl Pts',(-11.1502780647939,4.9439471109822,11.252918005051));
#117214=CARTESIAN_POINT('Ctrl Pts',(-11.1495266383952,4.94418276733786,
11.256311629842));
#117215=CARTESIAN_POINT('Ctrl Pts',(-11.147662502225,4.94475389923947,11.2645574120348));
#117216=CARTESIAN_POINT('Ctrl Pts',(-11.1465340150007,4.94508849824611,
11.2694060094633));
#117217=CARTESIAN_POINT('Ctrl Pts',(-11.1423803664345,4.94628169261917,
11.2867534269149));
#117218=CARTESIAN_POINT('Ctrl Pts',(-11.1391811643632,4.94713114765455,
11.2992101893408));
#117219=CARTESIAN_POINT('Ctrl Pts',(-11.1306122721246,4.94924815403828,
11.3304424333679));
#117220=CARTESIAN_POINT('Ctrl Pts',(-11.1249783667895,4.95050391164761,
11.3491419091925));
#117221=CARTESIAN_POINT('Ctrl Pts',(-11.0957182786318,4.9564643460093,11.4381795583914));
#117222=CARTESIAN_POINT('Ctrl Pts',(-11.0659448820378,4.9609782572752,11.5063227975903));
#117223=CARTESIAN_POINT('Ctrl Pts',(-11.0014069483683,4.96926347345763,
11.6226909354701));
#117224=CARTESIAN_POINT('Ctrl Pts',(-10.969043038991,4.97298203542559,11.6719480227077));
#117225=CARTESIAN_POINT('Ctrl Pts',(-10.9257990598139,4.97762813165029,
11.7281042364935));
#117226=CARTESIAN_POINT('Ctrl Pts',(-10.918316634404,4.97842171905366,11.7375189624746));
#117227=CARTESIAN_POINT('Ctrl Pts',(-10.9062673894164,4.97968466313244,
11.7522121779879));
#117228=CARTESIAN_POINT('Ctrl Pts',(-10.9017954313233,4.98015025380448,
11.7575676460588));
#117229=CARTESIAN_POINT('Ctrl Pts',(-10.8933705461015,4.98102179760876,
11.7674767010294));
#117230=CARTESIAN_POINT('Ctrl Pts',(-10.8894297029852,4.98142725264809,
11.772040297134));
#117231=CARTESIAN_POINT('Ctrl Pts',(-10.8805684279968,4.98233416891385,
11.7821439811619));
#117232=CARTESIAN_POINT('Ctrl Pts',(-10.8756304418856,4.9828363429974,11.7876682604741));
#117233=CARTESIAN_POINT('Ctrl Pts',(-10.8609150918387,4.98432372865178,
11.8038213924484));
#117234=CARTESIAN_POINT('Ctrl Pts',(-10.8509942814216,4.98531490113986,
11.8143170925434));
#117235=CARTESIAN_POINT('Ctrl Pts',(-10.8047467521311,4.9898853766641,11.8614763078938));
#117236=CARTESIAN_POINT('Ctrl Pts',(-10.766232001747,4.99355809055028,11.8959051280465));
#117237=CARTESIAN_POINT('Ctrl Pts',(-10.6581227140113,5.00350656235326,
11.9804619640586));
#117238=CARTESIAN_POINT('Ctrl Pts',(-10.5851050780729,5.0098866441019,12.0257108633622));
#117239=CARTESIAN_POINT('Ctrl Pts',(-10.4883149290882,5.01756422992387,
12.0719660855871));
#117240=CARTESIAN_POINT('Ctrl Pts',(-10.4685476512781,5.01909325947478,
12.0807525149932));
#117241=CARTESIAN_POINT('Ctrl Pts',(-10.4427425821387,5.02102995744698,
12.0913814602302));
#117242=CARTESIAN_POINT('Ctrl Pts',(-10.4369177896574,5.02146327774358,
12.0937263529831));
#117243=CARTESIAN_POINT('Ctrl Pts',(-10.4275820842982,5.02215136190298,
12.097398153048));
#117244=CARTESIAN_POINT('Ctrl Pts',(-10.42408319784,5.02240781473686,12.0987550170217));
#117245=CARTESIAN_POINT('Ctrl Pts',(-10.4173522155762,5.02289834180884,
12.1013283415712));
#117246=CARTESIAN_POINT('Ctrl Pts',(-10.4141211971399,5.0231325529114,12.1025473333035));
#117247=CARTESIAN_POINT('Ctrl Pts',(-10.4063383799733,5.02369379941877,
12.1054445793754));
#117248=CARTESIAN_POINT('Ctrl Pts',(-10.4017814220648,5.0240200323881,12.1071089774942));
#117249=CARTESIAN_POINT('Ctrl Pts',(-10.3858808034036,5.02515050371265,
12.1128054636253));
#117250=CARTESIAN_POINT('Ctrl Pts',(-10.3744852661921,5.02594682005417,
12.1166919034619));
#117251=CARTESIAN_POINT('Ctrl Pts',(-10.3460569593042,5.02790384169957,
12.125903207728));
#117252=CARTESIAN_POINT('Ctrl Pts',(-10.3289585779317,5.02905490768233,
12.1310171418321));
#117253=CARTESIAN_POINT('Ctrl Pts',(-10.2525568352456,5.0341105212969,12.1519886697963));
#117254=CARTESIAN_POINT('Ctrl Pts',(-10.1921802164538,5.03787731623307,
12.163585268697));
#117255=CARTESIAN_POINT('Ctrl Pts',(-10.0573999606523,5.04627537022066,
12.1786903139196));
#117256=CARTESIAN_POINT('Ctrl Pts',(-9.98302252080802,5.05091028382481,
12.1799641068196));
#117257=CARTESIAN_POINT('Ctrl Pts',(-9.89689790122508,5.05657119578408,
12.1732915131266));
#117258=CARTESIAN_POINT('Ctrl Pts',(-9.88478623426478,5.05737372187899,
12.1721641471339));
#117259=CARTESIAN_POINT('Ctrl Pts',(-9.86572757957192,5.05864773187734,
12.1700919161389));
#117260=CARTESIAN_POINT('Ctrl Pts',(-9.85876763198313,5.05911533660402,
12.1692722479207));
#117261=CARTESIAN_POINT('Ctrl Pts',(-9.84583586902019,5.05998873285216,
12.1676321401961));
#117262=CARTESIAN_POINT('Ctrl Pts',(-9.83986220692685,5.06039400826612,
12.166827870347));
#117263=CARTESIAN_POINT('Ctrl Pts',(-9.82659820482548,5.06129806405785,
12.1649382837008));
#117264=CARTESIAN_POINT('Ctrl Pts',(-9.81931140046457,5.06179753574432,
12.1638303197332));
#117265=CARTESIAN_POINT('Ctrl Pts',(-9.79797055448183,5.06326884926167,
12.1603801799919));
#117266=CARTESIAN_POINT('Ctrl Pts',(-9.78394847409247,5.06424645893532,
12.1578513576034));
#117267=CARTESIAN_POINT('Ctrl Pts',(-9.75209015237582,5.06649340875057,
12.1515069990639));
#117268=CARTESIAN_POINT('Ctrl Pts',(-9.73429010466333,5.06776747537856,
12.1475303267562));
#117269=CARTESIAN_POINT('Ctrl Pts',(-9.67377854526126,5.07216343541959,
12.1325282040226));
#117270=CARTESIAN_POINT('Ctrl Pts',(-9.63160095718511,5.0753406116986,12.1195186564465));
#117271=CARTESIAN_POINT('Ctrl Pts',(-9.53081786635906,5.0831771684397,12.0821194726807));
#117272=CARTESIAN_POINT('Ctrl Pts',(-9.47325869471765,5.08786790493696,
12.0552999620151));
#117273=CARTESIAN_POINT('Ctrl Pts',(-9.39029099118561,5.09477489144795,
12.0081546628066));
#117274=CARTESIAN_POINT('Ctrl Pts',(-9.36309832723165,5.09706291933443,
11.9912000598176));
#117275=CARTESIAN_POINT('Ctrl Pts',(-9.33088577087955,5.09977472546562,
11.969241720141));
#117276=CARTESIAN_POINT('Ctrl Pts',(-9.32517776176575,5.10025529421663,
11.9652762901257));
#117277=CARTESIAN_POINT('Ctrl Pts',(-9.31628875887191,5.10100333012165,
11.958983591966));
#117278=CARTESIAN_POINT('Ctrl Pts',(-9.31308388507036,5.10127295797896,
11.9566905681032));
#117279=CARTESIAN_POINT('Ctrl Pts',(-9.3074111418512,5.1017499945713,11.9525886298054));
#117280=CARTESIAN_POINT('Ctrl Pts',(-9.30493880180195,5.10195781946971,
11.9507861774204));
#117281=CARTESIAN_POINT('Ctrl Pts',(-9.29901806473303,5.10245535453567,
11.946434244425));
#117282=CARTESIAN_POINT('Ctrl Pts',(-9.2955765354794,5.10274443175343,11.9438755408784));
#117283=CARTESIAN_POINT('Ctrl Pts',(-9.28508481208236,5.10362558463302,
11.9359858219779));
#117284=CARTESIAN_POINT('Ctrl Pts',(-9.27808039726865,5.10421369035769,
11.9305940487124));
#117285=CARTESIAN_POINT('Ctrl Pts',(-9.26183025330577,5.10557945297592,
11.9177912995013));
#117286=CARTESIAN_POINT('Ctrl Pts',(-9.25263420333359,5.10635340479528,
11.91031853412));
#117287=CARTESIAN_POINT('Ctrl Pts',(-9.22018359223284,5.1090947154251,11.8831256909381));
#117288=CARTESIAN_POINT('Ctrl Pts',(-9.19758258635908,5.1110233009323,11.8626419706338));
#117289=CARTESIAN_POINT('Ctrl Pts',(-9.12323633130206,5.11753581749449,
11.7898071545867));
#117290=CARTESIAN_POINT('Ctrl Pts',(-9.07561409503207,5.12201543991753,
11.7334990380201));
#117291=CARTESIAN_POINT('Ctrl Pts',(-9.02700070388263,5.12736615091861,
11.663701011924));
#117292=CARTESIAN_POINT('Ctrl Pts',(-9.02058231813385,5.12809084004091,
11.6541923708683));
#117293=CARTESIAN_POINT('Ctrl Pts',(-8.99567284534512,5.13098094313283,
11.6161013286426));
#117294=CARTESIAN_POINT('Ctrl Pts',(-8.9782872071473,5.13317482428793,11.5868189808562));
#117295=CARTESIAN_POINT('Ctrl Pts',(-8.95721371552045,5.13610686600386,
11.5475425459004));
#117296=CARTESIAN_POINT('Ctrl Pts',(-8.95235725327569,5.13680407222857,
11.5381921015038));
#117297=CARTESIAN_POINT('Ctrl Pts',(-8.94467032610381,5.13794412294475,
11.5228935935638));
#117298=CARTESIAN_POINT('Ctrl Pts',(-8.94176309013027,5.13838430311074,
11.5169845939778));
#117299=CARTESIAN_POINT('Ctrl Pts',(-8.93625680252158,5.13923581030615,
11.5055519116172));
#117300=CARTESIAN_POINT('Ctrl Pts',(-8.9336508349475,5.13964688358976,11.5000317802965));
#117301=CARTESIAN_POINT('Ctrl Pts',(-8.92769111895437,5.14060621311621,
11.4871490323272));
#117302=CARTESIAN_POINT('Ctrl Pts',(-8.92437012322664,5.14115555906681,
11.4797716942523));
#117303=CARTESIAN_POINT('Ctrl Pts',(-8.91387745058903,5.14294040364245,
11.4558063794001));
#117304=CARTESIAN_POINT('Ctrl Pts',(-8.90701178677612,5.14418601258378,
11.4390880903001));
#117305=CARTESIAN_POINT('Ctrl Pts',(-8.87110137843636,5.15115965402037,
11.3455767637822));
#117306=CARTESIAN_POINT('Ctrl Pts',(-8.84976835999797,5.15713527881844,
11.2660793067991));
#117307=CARTESIAN_POINT('Ctrl Pts',(-8.82678129329819,5.16787317661145,
11.1215757976017));
#117308=CARTESIAN_POINT('Ctrl Pts',(-8.82189578655519,5.17259252077701,
11.0574005079799));
#117309=CARTESIAN_POINT('Ctrl Pts',(-8.82232554485016,5.17777320283397,
10.9835975661307));
#117310=CARTESIAN_POINT('Ctrl Pts',(-8.82249714680485,5.17843827158686,
10.9740537669406));
#117311=CARTESIAN_POINT('Ctrl Pts',(-8.8229364202516,5.17944526863039,10.9594817912362));
#117312=CARTESIAN_POINT('Ctrl Pts',(-8.82312033123578,5.17979132833694,
10.9544517446419));
#117313=CARTESIAN_POINT('Ctrl Pts',(-8.82348470875356,5.18037177385699,
10.9459745902367));
#117314=CARTESIAN_POINT('Ctrl Pts',(-8.82364809094381,5.18060707268519,
10.9425268525269));
#117315=CARTESIAN_POINT('Ctrl Pts',(-8.82401679341926,5.18109122779144,
10.9354083933392));
#117316=CARTESIAN_POINT('Ctrl Pts',(-8.82422414685637,5.1813399720985,10.9317378442333));
#117317=CARTESIAN_POINT('Ctrl Pts',(-8.82481102559976,5.18198771539791,
10.9221467220803));
#117318=CARTESIAN_POINT('Ctrl Pts',(-8.8252181100707,5.18238523434374,10.9162278495741));
#117319=CARTESIAN_POINT('Ctrl Pts',(-8.82725177669946,5.18416463307864,
10.889599984298));
#117320=CARTESIAN_POINT('Ctrl Pts',(-8.82938144580318,5.18552137481392,
10.8689317514374));
#117321=CARTESIAN_POINT('Ctrl Pts',(-8.8371554648429,5.18940799569405,10.8090678054501));
#117322=CARTESIAN_POINT('Ctrl Pts',(-8.84423087633856,5.19188537719516,
10.7700854209061));
#117323=CARTESIAN_POINT('Ctrl Pts',(-8.87590496229846,5.20051440441316,
10.6347922245004));
#117324=CARTESIAN_POINT('Ctrl Pts',(-8.91069929638746,5.20657054187645,
10.5413187964714));
#117325=CARTESIAN_POINT('Ctrl Pts',(-8.96281734149196,5.21390000260526,
10.4418650936321));
#117326=CARTESIAN_POINT('Ctrl Pts',(-8.96901073523546,5.21475052102616,
10.4305058774916));
#117327=CARTESIAN_POINT('Ctrl Pts',(-8.97923281250113,5.21612380050177,
10.4124711486786));
#117328=CARTESIAN_POINT('Ctrl Pts',(-8.98314294825022,5.21664239868115,
10.4057294104122));
#117329=CARTESIAN_POINT('Ctrl Pts',(-8.99022267288183,5.21756990677087,
10.3937972347492));
#117330=CARTESIAN_POINT('Ctrl Pts',(-8.99336612518701,5.21797786979149,
10.3885915582233));
#117331=CARTESIAN_POINT('Ctrl Pts',(-9.0000362285879,5.21883567669276,10.3777364955041));
#117332=CARTESIAN_POINT('Ctrl Pts',(-9.00357075584341,5.21928579594137,
10.372092226985));
#117333=CARTESIAN_POINT('Ctrl Pts',(-9.01300475067712,5.22047585719046,
10.3573073901725));
#117334=CARTESIAN_POINT('Ctrl Pts',(-9.01898321181328,5.22121867242826,
10.3482182417021));
#117335=CARTESIAN_POINT('Ctrl Pts',(-9.04861812060305,5.22484792513734,
10.3044953904511));
#117336=CARTESIAN_POINT('Ctrl Pts',(-9.07398462415618,5.22779756156051,
10.2710631509616));
#117337=CARTESIAN_POINT('Ctrl Pts',(-9.16772397305489,5.23819362648886,
10.160326160456));
#117338=CARTESIAN_POINT('Ctrl Pts',(-9.24441595009571,5.24591863098025,
10.0907007179582));
#117339=CARTESIAN_POINT('Ctrl Pts',(-9.34598384071172,5.25474751622672,
10.0203187121912));
#117340=CARTESIAN_POINT('Ctrl Pts',(-9.36307972343717,5.2561900881126,10.009118955144));
#117341=CARTESIAN_POINT('Ctrl Pts',(-9.38566597550263,5.25803207900457,
9.99514864482541));
#117342=CARTESIAN_POINT('Ctrl Pts',(-9.39089755161546,5.25845439114048,
9.99196887395632));
#117343=CARTESIAN_POINT('Ctrl Pts',(-9.3993460043569,5.25912914486498,9.98692366329682));
#117344=CARTESIAN_POINT('Ctrl Pts',(-9.40254725038583,5.259383166397,9.98503246386043));
#117345=CARTESIAN_POINT('Ctrl Pts',(-9.40875267389584,5.25987230637961,
9.98140601949193));
#117346=CARTESIAN_POINT('Ctrl Pts',(-9.41175562072408,5.26010753721595,
9.97966885359074));
#117347=CARTESIAN_POINT('Ctrl Pts',(-9.41905472784858,5.26067583073346,
9.97548934876312));
#117348=CARTESIAN_POINT('Ctrl Pts',(-9.42335873151174,5.26100803818526,
9.97306069635257));
#117349=CARTESIAN_POINT('Ctrl Pts',(-9.43870822479607,5.26218301792305,
9.9645262513405));
#117350=CARTESIAN_POINT('Ctrl Pts',(-9.44983687399048,5.26301701316344,
9.95857073820351));
#117351=CARTESIAN_POINT('Ctrl Pts',(-9.47797980568794,5.2650870679309,9.94408707815932));
#117352=CARTESIAN_POINT('Ctrl Pts',(-9.49510949288136,5.26631199103282,
9.93579004002828));
#117353=CARTESIAN_POINT('Ctrl Pts',(-9.57624201158654,5.27198575680174,
9.8988924522562));
#117354=CARTESIAN_POINT('Ctrl Pts',(-9.64251748923933,5.27626141068937,
9.87562630167969));
#117355=CARTESIAN_POINT('Ctrl Pts',(-9.74372672579125,5.28274817852381,
9.84995824108618));
#117356=CARTESIAN_POINT('Ctrl Pts',(-9.77731781255851,5.28489307668369,
9.84298552981361));
#117357=CARTESIAN_POINT('Ctrl Pts',(-9.81114934783795,5.28707251000898,
9.83748957265839));
#117358=CARTESIAN_POINT('Origin',(-10.,2.67563288526385,11.));
#117359=CARTESIAN_POINT('',(-9.81114930150122,5.88552497076973,9.83748958018583));
#117360=CARTESIAN_POINT('',(-9.81114942708287,5.7873151623385,9.837489559785));
#117361=CARTESIAN_POINT('',(-9.81114930150157,2.67563288526385,9.83748958018577));
#117362=CARTESIAN_POINT('Ctrl Pts',(-9.81114930150087,5.88552497076973,
9.83748958018588));
#117363=CARTESIAN_POINT('Ctrl Pts',(-9.81114406242107,5.88552459974339,
9.83749043127837));
#117364=CARTESIAN_POINT('Ctrl Pts',(-9.81113882334679,5.88552422871864,
9.8374912824063));
#117365=CARTESIAN_POINT('Ctrl Pts',(-9.8024360018317,5.88490790764762,9.83890518312361));
#117366=CARTESIAN_POINT('Ctrl Pts',(-9.79375422478925,5.88429634821271,
9.8404158508858));
#117367=CARTESIAN_POINT('Ctrl Pts',(-9.78087802284497,5.88339498956459,
9.84280555972011));
#117368=CARTESIAN_POINT('Ctrl Pts',(-9.77667035322581,5.88310134728357,
9.84361023706996));
#117369=CARTESIAN_POINT('Ctrl Pts',(-9.76946483245139,5.88260014890704,
9.84502902114163));
#117370=CARTESIAN_POINT('Ctrl Pts',(-9.76646488435682,5.88239197812917,
9.84563187154425));
#117371=CARTESIAN_POINT('Ctrl Pts',(-9.7596016137902,5.8819168798276,9.84703892117514));
#117372=CARTESIAN_POINT('Ctrl Pts',(-9.75573995403913,5.8816503887072,9.84785084973122));
#117373=CARTESIAN_POINT('Ctrl Pts',(-9.74506802685902,5.88091602711178,
9.85015073006728));
#117374=CARTESIAN_POINT('Ctrl Pts',(-9.73826664506999,5.88045038129041,
9.85167978716491));
#117375=CARTESIAN_POINT('Ctrl Pts',(-9.6999348315331,5.87783741387306,9.8606556473168));
#117376=CARTESIAN_POINT('Ctrl Pts',(-9.66870560956317,5.87575201213268,
9.86934129665199));
#117377=CARTESIAN_POINT('Ctrl Pts',(-9.5637075312571,5.86876674638351,9.90326916325355));
#117378=CARTESIAN_POINT('Ctrl Pts',(-9.49210290870555,5.86403657435735,
9.93453700007007));
#117379=CARTESIAN_POINT('Ctrl Pts',(-9.3786102531275,5.85589983708813,9.99815642822322));
#117380=CARTESIAN_POINT('Ctrl Pts',(-9.33486077963731,5.85258517254869,
10.0266529047521));
#117381=CARTESIAN_POINT('Ctrl Pts',(-9.28392688182018,5.84840546082868,
10.0648704771497));
#117382=CARTESIAN_POINT('Ctrl Pts',(-9.27480908290593,5.84764395340013,
10.0719234656966));
#117383=CARTESIAN_POINT('Ctrl Pts',(-9.26047863966877,5.84642487351907,
10.0833487707033));
#117384=CARTESIAN_POINT('Ctrl Pts',(-9.25519767027068,5.84597070568024,
10.0876345003682));
#117385=CARTESIAN_POINT('Ctrl Pts',(-9.24528793210228,5.84510892310494,
10.0958200469238));
#117386=CARTESIAN_POINT('Ctrl Pts',(-9.24065151237843,5.84470170048504,
10.0997102883073));
#117387=CARTESIAN_POINT('Ctrl Pts',(-9.23020768045122,5.84377509530863,
10.1086113755649));
#117388=CARTESIAN_POINT('Ctrl Pts',(-9.22441887064966,5.84325485693479,
10.1136435243144));
#117389=CARTESIAN_POINT('Ctrl Pts',(-9.20688101688818,5.84165799172213,
10.1291923433159));
#117390=CARTESIAN_POINT('Ctrl Pts',(-9.19529407838422,5.8405740070527,10.139888359381));
#117391=CARTESIAN_POINT('Ctrl Pts',(-9.12259871485794,5.83358134324374,
10.2097490987593));
#117392=CARTESIAN_POINT('Ctrl Pts',(-9.06784708086802,5.82739781719684,
10.2751445530646));
#117393=CARTESIAN_POINT('Ctrl Pts',(-8.99369033251992,5.81759994807685,
10.3861702362804));
#117394=CARTESIAN_POINT('Ctrl Pts',(-8.96927336903892,5.81403881829452,
10.4281178212426));
#117395=CARTESIAN_POINT('Ctrl Pts',(-8.94045560497558,5.80943498656051,
10.4855022893029));
#117396=CARTESIAN_POINT('Ctrl Pts',(-8.93368192941249,5.80831736531687,
10.4996920530868));
#117397=CARTESIAN_POINT('Ctrl Pts',(-8.92267213861576,5.80644289014544,
10.5239959750511));
#117398=CARTESIAN_POINT('Ctrl Pts',(-8.91828953693916,5.80567942425871,
10.5340411517773));
#117399=CARTESIAN_POINT('Ctrl Pts',(-8.91223818135282,5.80460122856949,
10.5484569318351));
#117400=CARTESIAN_POINT('Ctrl Pts',(-8.91045440928401,5.8042802408036,10.552778215949));
#117401=CARTESIAN_POINT('Ctrl Pts',(-8.90740801032695,5.80372662015021,
10.5602847005243));
#117402=CARTESIAN_POINT('Ctrl Pts',(-8.90613348055591,5.80349329830521,
10.563464962039));
#117403=CARTESIAN_POINT('Ctrl Pts',(-8.90346236441944,5.80300070632083,
10.570215204812));
#117404=CARTESIAN_POINT('Ctrl Pts',(-8.90206931225173,5.80274164166202,
10.5737864826511));
#117405=CARTESIAN_POINT('Ctrl Pts',(-8.89830999552497,5.80203636423725,
10.5835647459076));
#117406=CARTESIAN_POINT('Ctrl Pts',(-8.89597872324454,5.80159214434732,
10.5897851631884));
#117407=CARTESIAN_POINT('Ctrl Pts',(-8.88476098448996,5.79941854582555,
10.6205053498393));
#117408=CARTESIAN_POINT('Ctrl Pts',(-8.87663605874554,5.79772878289715,
10.6452776583816));
#117409=CARTESIAN_POINT('Ctrl Pts',(-8.84714296391513,5.79100481729385,
10.7464205376861));
#117410=CARTESIAN_POINT('Ctrl Pts',(-8.83268873918605,5.78619299971891,
10.8245914967287));
#117411=CARTESIAN_POINT('Ctrl Pts',(-8.82150063333779,5.77767052953856,
10.9608594532464));
#117412=CARTESIAN_POINT('Ctrl Pts',(-8.82099420148175,5.77403646468365,
11.0183522329159));
#117413=CARTESIAN_POINT('Ctrl Pts',(-8.82543849920718,5.76949716008584,
11.0874017388211));
#117414=CARTESIAN_POINT('Ctrl Pts',(-8.8263712559981,5.76871938450978,11.0991430180399));
#117415=CARTESIAN_POINT('Ctrl Pts',(-8.82812524258723,5.76748032267523,
11.1176928660274));
#117416=CARTESIAN_POINT('Ctrl Pts',(-8.82883013409321,5.76702264022554,
11.124511845306));
#117417=CARTESIAN_POINT('Ctrl Pts',(-8.8302684478575,5.76615793937679,11.1373305855902));
#117418=CARTESIAN_POINT('Ctrl Pts',(-8.83098860812364,5.76575134604358,
11.1433316334499));
#117419=CARTESIAN_POINT('Ctrl Pts',(-8.83271655231483,5.76483126450219,
11.1568500548333));
#117420=CARTESIAN_POINT('Ctrl Pts',(-8.83375081870324,5.76431696771949,
11.1643637107505));
#117421=CARTESIAN_POINT('Ctrl Pts',(-8.83709358290215,5.76275674420453,
11.1870254383559));
#117422=CARTESIAN_POINT('Ctrl Pts',(-8.83962512001978,5.76170394410675,
11.2021384405338));
#117423=CARTESIAN_POINT('Ctrl Pts',(-8.85926430824147,5.75432361253402,
11.3068052293917));
#117424=CARTESIAN_POINT('Ctrl Pts',(-8.88642319868119,5.74767420660396,
11.3941420762905));
#117425=CARTESIAN_POINT('Ctrl Pts',(-8.94909745041793,5.73632949069466,
11.5354682693347));
#117426=CARTESIAN_POINT('Ctrl Pts',(-8.97947433378415,5.73168246798129,
11.5913134392622));
#117427=CARTESIAN_POINT('Ctrl Pts',(-9.01853842902365,5.72670382108187,
11.6510690493442));
#117428=CARTESIAN_POINT('Ctrl Pts',(-9.02293664404694,5.72615542599091,
11.6576510695236));
#117429=CARTESIAN_POINT('Ctrl Pts',(-9.02971559722468,5.72532894656235,
11.6675777743943));
#117430=CARTESIAN_POINT('Ctrl Pts',(-9.03204790532599,5.72504786695366,
11.6709550289205));
#117431=CARTESIAN_POINT('Ctrl Pts',(-9.03633637052463,5.72453706611834,
11.6770959570043));
#117432=CARTESIAN_POINT('Ctrl Pts',(-9.03828680974816,5.72430698861169,
11.6798634172351));
#117433=CARTESIAN_POINT('Ctrl Pts',(-9.0427207451727,5.72378895972093,11.686097423051));
#117434=CARTESIAN_POINT('Ctrl Pts',(-9.04521115462734,5.72350147859463,
11.6895589226553));
#117435=CARTESIAN_POINT('Ctrl Pts',(-9.05171656195851,5.72275926243928,
11.6984981800828));
#117436=CARTESIAN_POINT('Ctrl Pts',(-9.05576030387578,5.72230638705161,
11.7039549616198));
#117437=CARTESIAN_POINT('Ctrl Pts',(-9.08540933040225,5.71904418403597,
11.743249319572));
#117438=CARTESIAN_POINT('Ctrl Pts',(-9.11278257776186,5.71634235973109,
11.7757201378216));
#117439=CARTESIAN_POINT('Ctrl Pts',(-9.15587792623229,5.71239901438189,
11.8215670137983));
#117440=CARTESIAN_POINT('Ctrl Pts',(-9.17029087370016,5.71112615640171,
11.8361203478293));
#117441=CARTESIAN_POINT('Ctrl Pts',(-9.22052008000168,5.70681409874214,
11.884260319799));
#117442=CARTESIAN_POINT('Ctrl Pts',(-9.25805239757169,5.70379426690557,
11.9159797393901));
#117443=CARTESIAN_POINT('Ctrl Pts',(-9.33747171227837,5.69759586544388,
11.9750063295858));
#117444=CARTESIAN_POINT('Ctrl Pts',(-9.37933312926429,5.69442158664187,
12.0021740393106));
#117445=CARTESIAN_POINT('Ctrl Pts',(-9.4327244065501,5.69040002346307,12.0321935128412));
#117446=CARTESIAN_POINT('Ctrl Pts',(-9.44274265852867,5.68964668518327,
12.0376363946056));
#117447=CARTESIAN_POINT('Ctrl Pts',(-9.45883660155914,5.68843764028238,
12.0460798846348));
#117448=CARTESIAN_POINT('Ctrl Pts',(-9.46486206456467,5.68798524005714,
12.0491750738924));
#117449=CARTESIAN_POINT('Ctrl Pts',(-9.4763253168761,5.68712487681217,12.0549391345705));
#117450=CARTESIAN_POINT('Ctrl Pts',(-9.48175766784359,5.68671728908274,
12.0576183783416));
#117451=CARTESIAN_POINT('Ctrl Pts',(-9.49415668642269,5.68578716624395,
12.0636151290799));
#117452=CARTESIAN_POINT('Ctrl Pts',(-9.50113571530714,5.68526375002682,
12.0669062851322));
#117453=CARTESIAN_POINT('Ctrl Pts',(-9.52269288726857,5.68364707536877,
12.0768144141167));
#117454=CARTESIAN_POINT('Ctrl Pts',(-9.537373491662,5.68254619025874,12.0832026737725));
#117455=CARTESIAN_POINT('Ctrl Pts',(-9.62519938446605,5.67595754357751,
12.1193090241073));
#117456=CARTESIAN_POINT('Ctrl Pts',(-9.70104056978686,5.67023716878254,
12.1419051472132));
#117457=CARTESIAN_POINT('Ctrl Pts',(-9.83047798117983,5.66057127619783,
12.1666841498741));
#117458=CARTESIAN_POINT('Ctrl Pts',(-9.88301121043996,5.65667956352694,
12.1731171029779));
#117459=CARTESIAN_POINT('Ctrl Pts',(-9.95227149067951,5.65169952400828,
12.1768981018724));
#117460=CARTESIAN_POINT('Ctrl Pts',(-9.96876008011703,5.65052537016828,
12.1774511781401));
#117461=CARTESIAN_POINT('Ctrl Pts',(-9.9966136112175,5.64856671112462,12.1777999057641));
#117462=CARTESIAN_POINT('Ctrl Pts',(-10.0079735508587,5.64777484537909,
12.1777777939335));
#117463=CARTESIAN_POINT('Ctrl Pts',(-10.0240731894887,5.64666406673858,
12.1775134945803));
#117464=CARTESIAN_POINT('Ctrl Pts',(-10.0288140672277,5.64633838616956,
12.1774070238633));
#117465=CARTESIAN_POINT('Ctrl Pts',(-10.0369890303224,5.64577937746597,
12.1771740233588));
#117466=CARTESIAN_POINT('Ctrl Pts',(-10.0404234054626,5.64554532178425,
12.1770610940759));
#117467=CARTESIAN_POINT('Ctrl Pts',(-10.047656018266,5.64505412198855,12.1767915772513));
#117468=CARTESIAN_POINT('Ctrl Pts',(-10.0514540396017,5.64479716141633,
12.1766316310561));
#117469=CARTESIAN_POINT('Ctrl Pts',(-10.061740876167,5.6441036859817,12.1761485171375));
#117470=CARTESIAN_POINT('Ctrl Pts',(-10.0682280147675,5.64366905365487,
12.1757900377627));
#117471=CARTESIAN_POINT('Ctrl Pts',(-10.0991106491538,5.6416113511472,12.1738270056852));
#117472=CARTESIAN_POINT('Ctrl Pts',(-10.1234570948852,5.64002304374319,
12.1715166672989));
#117473=CARTESIAN_POINT('Ctrl Pts',(-10.2285514178665,5.63324627137455,
12.1582306034192));
#117474=CARTESIAN_POINT('Ctrl Pts',(-10.3081138554265,5.62830661856359,
12.1396498766632));
#117475=CARTESIAN_POINT('Ctrl Pts',(-10.4391284790065,5.61966370903022,
12.0943156428758));
#117476=CARTESIAN_POINT('Ctrl Pts',(-10.4916931303341,5.61604662169256,
12.0717262544816));
#117477=CARTESIAN_POINT('Ctrl Pts',(-10.5528506709881,5.61152642924802,
12.0399950157005));
#117478=CARTESIAN_POINT('Ctrl Pts',(-10.5632123365653,5.61074944104743,
12.0344202940601));
#117479=CARTESIAN_POINT('Ctrl Pts',(-10.5794738502178,5.60951134623697,
12.0253546112582));
#117480=CARTESIAN_POINT('Ctrl Pts',(-10.5854299065914,5.60905383368398,
12.0219656760583));
#117481=CARTESIAN_POINT('Ctrl Pts',(-10.5965832380452,5.60818927667283,
12.0154900483042));
#117482=CARTESIAN_POINT('Ctrl Pts',(-10.6017870040175,5.607782655702,12.0124149335053));
#117483=CARTESIAN_POINT('Ctrl Pts',(-10.6134699051194,5.60686227232976,
12.0053891400716));
#117484=CARTESIAN_POINT('Ctrl Pts',(-10.6199349394416,5.60634769915679,
12.0014156547904));
#117485=CARTESIAN_POINT('Ctrl Pts',(-10.6393545172723,5.60478578231564,
11.989220036783));
#117486=CARTESIAN_POINT('Ctrl Pts',(-10.6521867798943,5.60373154325811,
11.980807241826));
#117487=CARTESIAN_POINT('Ctrl Pts',(-10.7399264649682,5.59636461716038,
11.9208021129442));
#117488=CARTESIAN_POINT('Ctrl Pts',(-10.8087887160381,5.58973181859896,
11.8609427742068));
#117489=CARTESIAN_POINT('Ctrl Pts',(-10.9001104349996,5.57978878465653,
11.7608438176995));
#117490=CARTESIAN_POINT('Ctrl Pts',(-10.9282617293026,5.57652272338885,
11.7262318700659));
#117491=CARTESIAN_POINT('Ctrl Pts',(-10.967461607773,5.5717331635018,11.6720202319838));
#117492=CARTESIAN_POINT('Ctrl Pts',(-10.9800232298039,5.57015517411939,
11.6535654361874));
#117493=CARTESIAN_POINT('Ctrl Pts',(-10.9953288582824,5.56818582382703,
11.6296447048368));
#117494=CARTESIAN_POINT('Ctrl Pts',(-10.9985644707956,5.56776666929828,
11.6245005941458));
#117495=CARTESIAN_POINT('Ctrl Pts',(-11.003710509252,5.56709569547738,11.616176947964));
#117496=CARTESIAN_POINT('Ctrl Pts',(-11.0056459330865,5.56684232732312,
11.613013112269));
#117497=CARTESIAN_POINT('Ctrl Pts',(-11.009345482797,5.56635612360757,11.6069007857162));
#117498=CARTESIAN_POINT('Ctrl Pts',(-11.0111116878844,5.56612316335686,
11.6039536590662));
#117499=CARTESIAN_POINT('Ctrl Pts',(-11.014992189835,5.5656093665597,11.5974138382281));
#117500=CARTESIAN_POINT('Ctrl Pts',(-11.0171003815897,5.56532891452956,
11.5938175263586));
#117501=CARTESIAN_POINT('Ctrl Pts',(-11.0245405850407,5.56433413180136,
11.5809695965326));
#117502=CARTESIAN_POINT('Ctrl Pts',(-11.0297660127139,5.56362614902656,
11.571656418801));
#117503=CARTESIAN_POINT('Ctrl Pts',(-11.063216956933,5.55902263083453,11.5100899144462));
#117504=CARTESIAN_POINT('Ctrl Pts',(-11.0875857488051,5.5553219452896,11.4558300495267));
#117505=CARTESIAN_POINT('Ctrl Pts',(-11.1257961811559,5.54835085356728,
11.3499988564461));
#117506=CARTESIAN_POINT('Ctrl Pts',(-11.1404329096589,5.54508402266163,
11.2988792322528));
#117507=CARTESIAN_POINT('Ctrl Pts',(-11.157832931308,5.53986631643473,11.2177390931551));
#117508=CARTESIAN_POINT('Ctrl Pts',(-11.1629825626586,5.53796778550377,
11.1883050083109));
#117509=CARTESIAN_POINT('Ctrl Pts',(-11.1697973235746,5.53470031998053,
11.1381950382607));
#117510=CARTESIAN_POINT('Ctrl Pts',(-11.1720455713564,5.53334835728354,
11.1176126781708));
#117511=CARTESIAN_POINT('Ctrl Pts',(-11.174452548057,5.53141580923354,11.0884818251458));
#117512=CARTESIAN_POINT('Ctrl Pts',(-11.1750625578011,5.53084910635873,
11.0799737452216));
#117513=CARTESIAN_POINT('Ctrl Pts',(-11.1759549176895,5.52986703646142,
11.0652936315042));
#117514=CARTESIAN_POINT('Ctrl Pts',(-11.1762812219478,5.52945304144557,
11.0591245395319));
#117515=CARTESIAN_POINT('Ctrl Pts',(-11.1768139011635,5.52865617850915,
11.0472890367062));
#117516=CARTESIAN_POINT('Ctrl Pts',(-11.1770279198747,5.52827355866869,
11.0416231289635));
#117517=CARTESIAN_POINT('Ctrl Pts',(-11.177435879426,5.52736878559432,11.028266508282));
#117518=CARTESIAN_POINT('Ctrl Pts',(-11.1775953918063,5.52684558491964,
11.0205750815706));
#117519=CARTESIAN_POINT('Ctrl Pts',(-11.1778910658077,5.52499898106644,
10.9935460788147));
#117520=CARTESIAN_POINT('Ctrl Pts',(-11.1776263072097,5.52366340042991,
10.974208137152));
#117521=CARTESIAN_POINT('Ctrl Pts',(-11.1724407701324,5.51421429580306,
10.8389321317401));
#117522=CARTESIAN_POINT('Ctrl Pts',(-11.1508821866952,5.50556835244807,
10.7242826832966));
#117523=CARTESIAN_POINT('Ctrl Pts',(-11.1018482266343,5.49470750186665,
10.5826593882331));
#117524=CARTESIAN_POINT('Ctrl Pts',(-11.0893874093102,5.49228474974297,
10.5511367259678));
#117525=CARTESIAN_POINT('Ctrl Pts',(-11.0727868559334,5.48945172931495,
10.51392331266));
#117526=CARTESIAN_POINT('Ctrl Pts',(-11.0699354526548,5.48897728695651,
10.5076786445618));
#117527=CARTESIAN_POINT('Ctrl Pts',(-11.0653864428832,5.48823947147091,
10.4979423770558));
#117528=CARTESIAN_POINT('Ctrl Pts',(-11.0637259519631,5.48797397793081,
10.49443375345));
#117529=CARTESIAN_POINT('Ctrl Pts',(-11.0605726301511,5.48747700080756,
10.48785508753));
#117530=CARTESIAN_POINT('Ctrl Pts',(-11.0590838042314,5.48724529960491,
10.4847833357211));
#117531=CARTESIAN_POINT('Ctrl Pts',(-11.0555996030202,5.48670976856614,
10.4776736407389));
#117532=CARTESIAN_POINT('Ctrl Pts',(-11.0535943950282,5.48640654164237,
10.4736406171644));
#117533=CARTESIAN_POINT('Ctrl Pts',(-11.0469480797857,5.48541729057034,
10.4604632201044));
#117534=CARTESIAN_POINT('Ctrl Pts',(-11.0422105248734,5.48473685629135,
10.4513676477389));
#117535=CARTESIAN_POINT('Ctrl Pts',(-11.0031303788792,5.47930845945104,
10.3786717647131));
#117536=CARTESIAN_POINT('Ctrl Pts',(-10.9631133308537,5.47485492961544,
10.3182852947561));
#117537=CARTESIAN_POINT('Ctrl Pts',(-10.8824209095297,5.46688975445587,
10.2179407046006));
#117538=CARTESIAN_POINT('Ctrl Pts',(-10.8439189247069,5.4633963659952,10.1765416553175));
#117539=CARTESIAN_POINT('Ctrl Pts',(-10.7871115117689,5.45845171046103,
10.1236448470087));
#117540=CARTESIAN_POINT('Ctrl Pts',(-10.7712391376717,5.45709064810652,
10.1096444533341));
#117541=CARTESIAN_POINT('Ctrl Pts',(-10.7427307503486,5.45467283327899,
10.0858328362572));
#117542=CARTESIAN_POINT('Ctrl Pts',(-10.7302557564939,5.45362335693133,
10.0758371024373));
#117543=CARTESIAN_POINT('Ctrl Pts',(-10.7114668705541,5.45205282311485,
10.0614002873347));
#117544=CARTESIAN_POINT('Ctrl Pts',(-10.7053061978194,5.45153943029495,
10.0567621237956));
#117545=CARTESIAN_POINT('Ctrl Pts',(-10.6942263617664,5.45061862925353,
10.0485897289282));
#117546=CARTESIAN_POINT('Ctrl Pts',(-10.6893246009638,5.45021212994072,
10.0450322846075));
#117547=CARTESIAN_POINT('Ctrl Pts',(-10.678880643486,5.44934772076676,10.037574908011));
#117548=CARTESIAN_POINT('Ctrl Pts',(-10.6733318073897,5.44888946223864,
10.0336846996783));
#117549=CARTESIAN_POINT('Ctrl Pts',(-10.6583479255175,5.44765447422548,
10.0233714403328));
#117550=CARTESIAN_POINT('Ctrl Pts',(-10.6488527702463,5.44687446957186,
10.0170374364967));
#117551=CARTESIAN_POINT('Ctrl Pts',(-10.602305862934,5.44306204074122,9.98695535019707));
#117552=CARTESIAN_POINT('Ctrl Pts',(-10.5640391137128,5.439960129923,9.9651614370261));
#117553=CARTESIAN_POINT('Ctrl Pts',(-10.4588046511441,5.43151692831929,
9.91280093839774));
#117554=CARTESIAN_POINT('Ctrl Pts',(-10.3900416424152,5.42607936855843,
9.88628122184891));
#117555=CARTESIAN_POINT('Ctrl Pts',(-10.2900044000344,5.41849327848107,
9.85810837965382));
#117556=CARTESIAN_POINT('Ctrl Pts',(-10.2604357582787,5.41629123771702,
9.85100370638562));
#117557=CARTESIAN_POINT('Ctrl Pts',(-10.219026518867,5.4132886761397,9.84273499111006));
#117558=CARTESIAN_POINT('Ctrl Pts',(-10.2073947470695,5.41245408513059,
9.84059396276645));
#117559=CARTESIAN_POINT('Ctrl Pts',(-10.187028629238,5.4110103215799,9.83716155093464));
#117560=CARTESIAN_POINT('Ctrl Pts',(-10.1783084910422,5.4103977231405,9.83579251832996));
#117561=CARTESIAN_POINT('Ctrl Pts',(-10.1653314596302,5.40949513956807,
9.83390440077596));
#117562=CARTESIAN_POINT('Ctrl Pts',(-10.1610860284991,5.40920129664895,
9.83331035362914));
#117563=CARTESIAN_POINT('Ctrl Pts',(-10.1538044284708,5.40869987692085,
9.83233197138127));
#117564=CARTESIAN_POINT('Ctrl Pts',(-10.1507699039277,5.40849168383517,
9.83193627566852));
#117565=CARTESIAN_POINT('Ctrl Pts',(-10.1438209931884,5.40801670140396,
9.83105768366957));
#117566=CARTESIAN_POINT('Ctrl Pts',(-10.1399056940824,5.40775034718834,
9.83058261732952));
#117567=CARTESIAN_POINT('Ctrl Pts',(-10.1290729601648,5.4070167324915,9.82932340182948));
#117568=CARTESIAN_POINT('Ctrl Pts',(-10.1221507121503,5.40655168935038,
9.82858088804931));
#117569=CARTESIAN_POINT('Ctrl Pts',(-10.0831521311226,5.40395073157816,
9.82474717346643));
#117570=CARTESIAN_POINT('Ctrl Pts',(-10.0509630330365,5.40187606457298,
9.82291178587159));
#117571=CARTESIAN_POINT('Ctrl Pts',(-9.95549252278619,5.39583034815833,
9.82139280444906));
#117572=CARTESIAN_POINT('Ctrl Pts',(-9.89226756188441,5.39196179669756,
9.82548291059762));
#117573=CARTESIAN_POINT('Ctrl Pts',(-9.82349116475283,5.38764709326431,
9.83553499775459));
#117574=CARTESIAN_POINT('Ctrl Pts',(-9.8173159697757,5.38725879013721,9.83648780022633));
#117575=CARTESIAN_POINT('Ctrl Pts',(-9.81114929672518,5.38686993568377,
9.8374895809617));
#117576=CARTESIAN_POINT('Ctrl Pts',(-9.81114934783795,5.28707251000898,
9.83748957265839));
#117577=CARTESIAN_POINT('Ctrl Pts',(-9.84003655603766,5.28893342893285,
9.83279682498117));
#117578=CARTESIAN_POINT('Ctrl Pts',(-9.8690990738413,5.29081941320123,9.82918072532109));
#117579=CARTESIAN_POINT('Ctrl Pts',(-9.91035600248275,5.29353346110809,
9.82560398103576));
#117580=CARTESIAN_POINT('Ctrl Pts',(-9.92244983736818,5.29433342294489,
9.82474342793177));
#117581=CARTESIAN_POINT('Ctrl Pts',(-9.94154279040337,5.29560425869866,
9.82368082334977));
#117582=CARTESIAN_POINT('Ctrl Pts',(-9.94853433172485,5.29607128605353,
9.8233542027683));
#117583=CARTESIAN_POINT('Ctrl Pts',(-9.96155207023144,5.29694414827467,
9.82286230308912));
#117584=CARTESIAN_POINT('Ctrl Pts',(-9.96757745713924,5.29734947218436,
9.82268093653636));
#117585=CARTESIAN_POINT('Ctrl Pts',(-9.98098357699742,5.29825433367354,
9.82238039863986));
#117586=CARTESIAN_POINT('Ctrl Pts',(-9.98836452071871,5.29875456865255,
9.82228434620873));
#117587=CARTESIAN_POINT('Ctrl Pts',(-10.0100480122875,5.300230412983,9.82220602068969));
#117588=CARTESIAN_POINT('Ctrl Pts',(-10.0243494687764,5.30121184429461,
9.82241488951198));
#117589=CARTESIAN_POINT('Ctrl Pts',(-10.1064466018248,5.30689422286634,
9.82511002214406));
#117590=CARTESIAN_POINT('Ctrl Pts',(-10.173919772126,5.31176545401268,9.8331896124798));
#117591=CARTESIAN_POINT('Ctrl Pts',(-10.3115809662342,5.32204088859045,
9.86188217036142));
#117592=CARTESIAN_POINT('Ctrl Pts',(-10.3813200809907,5.32743634491947,
9.88331267003869));
#117593=CARTESIAN_POINT('Ctrl Pts',(-10.4662599648282,5.33398713876658,
9.91830686357245));
#117594=CARTESIAN_POINT('Ctrl Pts',(-10.4837065430341,5.33533073191038,
9.92599512252269));
#117595=CARTESIAN_POINT('Ctrl Pts',(-10.50636381614,5.33706620373662,9.93664380355342));
#117596=CARTESIAN_POINT('Ctrl Pts',(-10.5117484463958,5.33747793486259,
9.93922469570708));
#117597=CARTESIAN_POINT('Ctrl Pts',(-10.5204239482764,5.3381398701793,9.9434643621364));
#117598=CARTESIAN_POINT('Ctrl Pts',(-10.5237269876681,5.33839155208412,
9.94509778493546));
#117599=CARTESIAN_POINT('Ctrl Pts',(-10.5301407993323,5.33887952871056,
9.94830710050897));
#117600=CARTESIAN_POINT('Ctrl Pts',(-10.5332523059126,5.33911591144904,
9.94988133976267));
#117601=CARTESIAN_POINT('Ctrl Pts',(-10.5408422871726,5.33969177948089,
9.9537638569598));
#117602=CARTESIAN_POINT('Ctrl Pts',(-10.5453130984274,5.3400303525816,9.95608713315175));
#117603=CARTESIAN_POINT('Ctrl Pts',(-10.5614997382277,5.34125434447246,
9.964630956192));
#117604=CARTESIAN_POINT('Ctrl Pts',(-10.573125677455,5.3421299908398,9.97102089090047));
#117605=CARTESIAN_POINT('Ctrl Pts',(-10.6598725121756,5.34865619797864,
10.0206258696862));
#117606=CARTESIAN_POINT('Ctrl Pts',(-10.7301349744772,5.35391471485805,
10.0718231339762));
#117607=CARTESIAN_POINT('Ctrl Pts',(-10.8422957840801,5.36334458069843,
10.1742374655474));
#117608=CARTESIAN_POINT('Ctrl Pts',(-10.8867028622079,5.3674436026676,10.2221167540769));
#117609=CARTESIAN_POINT('Ctrl Pts',(-10.9344091126706,5.37251143922848,
10.2829768972989));
#117610=CARTESIAN_POINT('Ctrl Pts',(-10.9417520274596,5.37331263907679,
10.2926488703571));
#117611=CARTESIAN_POINT('Ctrl Pts',(-10.9530919253782,5.37458500742185,
10.308075226238));
#117612=CARTESIAN_POINT('Ctrl Pts',(-10.9571894931464,5.37505231362611,
10.3137548678383));
#117613=CARTESIAN_POINT('Ctrl Pts',(-10.9647191132482,5.37592543355481,
10.3243903271433));
#117614=CARTESIAN_POINT('Ctrl Pts',(-10.9681642600872,5.37633073383439,
10.3293366263896));
#117615=CARTESIAN_POINT('Ctrl Pts',(-10.9757404392779,5.37723520509736,
10.3403940067513));
#117616=CARTESIAN_POINT('Ctrl Pts',(-10.9798523066338,5.37773507053128,
10.3465178471625));
#117617=CARTESIAN_POINT('Ctrl Pts',(-10.991752671097,5.37920872015507,10.3646060257387));
#117618=CARTESIAN_POINT('Ctrl Pts',(-10.9993812377255,5.38018830005791,
10.3766734613125));
#117619=CARTESIAN_POINT('Ctrl Pts',(-11.0537990668637,5.38744288416676,
10.4663234262583));
#117620=CARTESIAN_POINT('Ctrl Pts',(-11.0917078444396,5.39403838982277,
10.5489223726652));
#117621=CARTESIAN_POINT('Ctrl Pts',(-11.1388464897861,5.40520174648392,
10.693549104112));
#117622=CARTESIAN_POINT('Ctrl Pts',(-11.1533052169353,5.40971560106077,
10.7534802030505));
#117623=CARTESIAN_POINT('Ctrl Pts',(-11.164689748759,5.41478374034189,10.824769137523));
#117624=CARTESIAN_POINT('Ctrl Pts',(-11.1662239967187,5.41552393345971,
10.835289116389));
#117625=CARTESIAN_POINT('Ctrl Pts',(-11.1681602729992,5.41654374003203,
10.8499535127358));
#117626=CARTESIAN_POINT('Ctrl Pts',(-11.1686830383015,5.41682946634,10.8540810874074));
#117627=CARTESIAN_POINT('Ctrl Pts',(-11.169597240414,5.41734880062795,10.8616195678858));
#117628=CARTESIAN_POINT('Ctrl Pts',(-11.169995656157,5.41758278371806,10.8650295789037));
#117629=CARTESIAN_POINT('Ctrl Pts',(-11.1707937052025,5.41806793129367,
10.8721292277762));
#117630=CARTESIAN_POINT('Ctrl Pts',(-11.1711908184042,5.41831895740958,
10.8758190740244));
#117631=CARTESIAN_POINT('Ctrl Pts',(-11.1721935440615,5.41897946267186,
10.8855690249623));
#117632=CARTESIAN_POINT('Ctrl Pts',(-11.1727696135399,5.41938735304755,
10.8916321528842));
#117633=CARTESIAN_POINT('Ctrl Pts',(-11.1752513204197,5.42128995084117,
10.9200952317838));
#117634=CARTESIAN_POINT('Ctrl Pts',(-11.1765625327089,5.42275506185808,
10.9425439132997));
#117635=CARTESIAN_POINT('Ctrl Pts',(-11.178570873109,5.42709631502357,11.0101296033905));
#117636=CARTESIAN_POINT('Ctrl Pts',(-11.1773173543358,5.42990436419411,
11.0552844313765));
#117637=CARTESIAN_POINT('Ctrl Pts',(-11.1658069306276,5.43827995951092,
11.1900076949119));
#117638=CARTESIAN_POINT('Ctrl Pts',(-11.1478699386521,5.44380701521126,
11.2785700845506));
#117639=CARTESIAN_POINT('Ctrl Pts',(-11.1152485044215,5.45067991826223,
11.3788847325628));
#117640=CARTESIAN_POINT('Ctrl Pts',(-11.1101922042834,5.45169309687747,
11.3934540646525));
#117641=CARTESIAN_POINT('Ctrl Pts',(-11.102218422932,5.45321959649493,11.4150510869215));
#117642=CARTESIAN_POINT('Ctrl Pts',(-11.0995164126636,5.45372587649981,
11.4221569736007));
#117643=CARTESIAN_POINT('Ctrl Pts',(-11.0945430116122,5.45463876729614,
11.4348645659652));
#117644=CARTESIAN_POINT('Ctrl Pts',(-11.0922969126987,5.45504452891149,
11.4404759325852));
#117645=CARTESIAN_POINT('Ctrl Pts',(-11.0874169737869,5.45591259223395,
11.4524004627123));
#117646=CARTESIAN_POINT('Ctrl Pts',(-11.0847711348596,5.45637528250779,
11.4587084423802));
#117647=CARTESIAN_POINT('Ctrl Pts',(-11.077445555866,5.45763538786231,11.4757555697594));
#117648=CARTESIAN_POINT('Ctrl Pts',(-11.0726604020385,5.45843631435026,
11.4864482837258));
#117649=CARTESIAN_POINT('Ctrl Pts',(-11.0440676953305,5.46309958184428,
11.5478663191076));
#117650=CARTESIAN_POINT('Ctrl Pts',(-11.0168272362663,5.4670783035356,11.5969049761292));
#117651=CARTESIAN_POINT('Ctrl Pts',(-10.9394109995266,5.47734176831897,
11.7154925765967));
#117652=CARTESIAN_POINT('Ctrl Pts',(-10.8849445616635,5.48371795124326,
11.7818537567358));
#117653=CARTESIAN_POINT('Ctrl Pts',(-10.8080703047851,5.49141902045241,
11.8570880304801));
#117654=CARTESIAN_POINT('Ctrl Pts',(-10.7919444462839,5.49297240465356,
11.8720101211003));
#117655=CARTESIAN_POINT('Ctrl Pts',(-10.7706858767621,5.4949323528122,11.8906052580174));
#117656=CARTESIAN_POINT('Ctrl Pts',(-10.7659292176721,5.49536545225431,
11.8946993260946));
#117657=CARTESIAN_POINT('Ctrl Pts',(-10.7582767463356,5.49605326875225,
11.9011800684941));
#117658=CARTESIAN_POINT('Ctrl Pts',(-10.7554019404259,5.49630967257001,
11.9035911958841));
#117659=CARTESIAN_POINT('Ctrl Pts',(-10.7498589212496,5.49680016975425,
11.9081952367354));
#117660=CARTESIAN_POINT('Ctrl Pts',(-10.7471925372069,5.49703439950226,
11.9103901924176));
#117661=CARTESIAN_POINT('Ctrl Pts',(-10.7407562084799,5.4975957790995,11.9156412252569));
#117662=CARTESIAN_POINT('Ctrl Pts',(-10.736976904448,5.4979221255154,11.9186858321313));
#117663=CARTESIAN_POINT('Ctrl Pts',(-10.7237487777928,5.49905342925434,
11.9292082449067));
#117664=CARTESIAN_POINT('Ctrl Pts',(-10.7142037360135,5.49985044899447,
11.9365646303574));
#117665=CARTESIAN_POINT('Ctrl Pts',(-10.6902308992104,5.50180956290318,
11.954460862457));
#117666=CARTESIAN_POINT('Ctrl Pts',(-10.6756726646755,5.50296199112549,
11.9648216164006));
#117667=CARTESIAN_POINT('Ctrl Pts',(-10.6099529527165,5.50802826873212,
12.0093753245141));
#117668=CARTESIAN_POINT('Ctrl Pts',(-10.5563912828239,5.51180378374164,
12.0398610279887));
#117669=CARTESIAN_POINT('Ctrl Pts',(-10.4336639918296,5.52020005152387,
12.0975035431772));
#117670=CARTESIAN_POINT('Ctrl Pts',(-10.3638284418439,5.52482421478696,
12.1225886489348));
#117671=CARTESIAN_POINT('Ctrl Pts',(-10.2803235330198,5.53047305218441,
12.143967523567));
#117672=CARTESIAN_POINT('Ctrl Pts',(-10.2684958362515,5.53127547339873,
12.1468011798728));
#117673=CARTESIAN_POINT('Ctrl Pts',(-10.2497874299115,5.53254935365872,
12.1509780231997));
#117674=CARTESIAN_POINT('Ctrl Pts',(-10.2429347690995,5.53301693486544,
12.1524438660627));
#117675=CARTESIAN_POINT('Ctrl Pts',(-10.2301642890874,5.53389030945156,
12.1550566195723));
#117676=CARTESIAN_POINT('Ctrl Pts',(-10.2242499287071,5.53429558693422,
12.1562194262132));
#117677=CARTESIAN_POINT('Ctrl Pts',(-10.211083758798,5.53519967581801,12.1587031720095));
#117678=CARTESIAN_POINT('Ctrl Pts',(-10.2038280000269,5.53569917877641,
12.1600015242181));
#117679=CARTESIAN_POINT('Ctrl Pts',(-10.1825106168296,5.53717067734174,
12.1636098991202));
#117680=CARTESIAN_POINT('Ctrl Pts',(-10.1684191173383,5.53814844299294,
12.165732856474));
#117681=CARTESIAN_POINT('Ctrl Pts',(-10.1362093312238,5.5403958101997,12.1699892364676));
#117682=CARTESIAN_POINT('Ctrl Pts',(-10.118073396393,5.54167014075104,12.171958363703));
#117683=CARTESIAN_POINT('Ctrl Pts',(-10.0559368143059,5.54606738930973,
12.1772480163532));
#117684=CARTESIAN_POINT('Ctrl Pts',(-10.0118024752413,5.54924562590739,
12.1785167910004));
#117685=CARTESIAN_POINT('Ctrl Pts',(-9.90429018920359,5.55708621360699,
12.1755675827569));
#117686=CARTESIAN_POINT('Ctrl Pts',(-9.84112059918129,5.56177996137742,
12.1687073338518));
#117687=CARTESIAN_POINT('Ctrl Pts',(-9.74740744030234,5.56868543722492,
12.150788555779));
#117688=CARTESIAN_POINT('Ctrl Pts',(-9.71625822513954,5.57096933138761,
12.1435070198843));
#117689=CARTESIAN_POINT('Ctrl Pts',(-9.67874669146476,5.57367699045913,
12.1331106007244));
#117690=CARTESIAN_POINT('Ctrl Pts',(-9.67206850815527,5.57415734697159,
12.1311959442064));
#117691=CARTESIAN_POINT('Ctrl Pts',(-9.66162987120367,5.57490512522231,
12.1281029392176));
#117692=CARTESIAN_POINT('Ctrl Pts',(-9.65785785370527,5.57517470532991,
12.1269646571228));
#117693=CARTESIAN_POINT('Ctrl Pts',(-9.65116672815232,5.5756517006279,12.1249087843609));
#117694=CARTESIAN_POINT('Ctrl Pts',(-9.64824547155877,5.57585953156193,
12.1239987441045));
#117695=CARTESIAN_POINT('Ctrl Pts',(-9.64123748255917,5.57635713618037,
12.1217855930865));
#117696=CARTESIAN_POINT('Ctrl Pts',(-9.63715428391033,5.5766462763919,12.1204715295526));
#117697=CARTESIAN_POINT('Ctrl Pts',(-9.62467482199324,5.57752781745608,
12.116379990083));
#117698=CARTESIAN_POINT('Ctrl Pts',(-9.61630235863866,5.57811624329526,
12.113530153603));
#117699=CARTESIAN_POINT('Ctrl Pts',(-9.59678183201735,5.57948287406148,
12.1066393972782));
#117700=CARTESIAN_POINT('Ctrl Pts',(-9.58566094855489,5.58025736744226,
12.1025238411512));
#117701=CARTESIAN_POINT('Ctrl Pts',(-9.54614159833198,5.58300136878465,
12.0872162823073));
#117702=CARTESIAN_POINT('Ctrl Pts',(-9.51811680547734,5.58493202198807,
12.0750886196897));
#117703=CARTESIAN_POINT('Ctrl Pts',(-9.42420774075897,5.59144914596474,
12.0300386123009));
#117704=CARTESIAN_POINT('Ctrl Pts',(-9.36095543944663,5.59593139552262,
11.9920375914384));
#117705=CARTESIAN_POINT('Ctrl Pts',(-9.26639850108618,5.60331870707735,
11.9224109411773));
#117706=CARTESIAN_POINT('Ctrl Pts',(-9.23261182661492,5.60611846080799,
11.8944986564432));
#117707=CARTESIAN_POINT('Ctrl Pts',(-9.19210438609852,5.60974073079378,
11.8570468131491));
#117708=CARTESIAN_POINT('Ctrl Pts',(-9.18386131626456,5.61049269071724,
11.8492009167682));
#117709=CARTESIAN_POINT('Ctrl Pts',(-9.17089913990472,5.61169996255374,
11.8365002296261));
#117710=CARTESIAN_POINT('Ctrl Pts',(-9.16610582873728,5.61215198389991,
11.8317219356774));
#117711=CARTESIAN_POINT('Ctrl Pts',(-9.15710200405896,5.61301190517363,
11.8225902430264));
#117712=CARTESIAN_POINT('Ctrl Pts',(-9.15288335221187,5.61341943243898,
11.8182451479701));
#117713=CARTESIAN_POINT('Ctrl Pts',(-9.14336326768805,5.61434980373827,
11.8082871882457));
#117714=CARTESIAN_POINT('Ctrl Pts',(-9.13808318547892,5.61487353205715,
11.802654389986));
#117715=CARTESIAN_POINT('Ctrl Pts',(-9.12200500521743,5.61649261685196,
11.7851605743406));
#117716=CARTESIAN_POINT('Ctrl Pts',(-9.11139391342923,5.61759563504772,
11.7731309833368));
#117717=CARTESIAN_POINT('Ctrl Pts',(-9.08729801504498,5.62018361430836,
11.7446623925145));
#117718=CARTESIAN_POINT('Ctrl Pts',(-9.07400644845524,5.62167560773698,
11.728067880187));
#117719=CARTESIAN_POINT('Ctrl Pts',(-9.02679999702403,5.62721964048393,
11.6657457450799));
#117720=CARTESIAN_POINT('Ctrl Pts',(-8.99576679502239,5.63136388037159,
11.6179401684105));
#117721=CARTESIAN_POINT('Ctrl Pts',(-8.93380240767638,5.64078503571739,
11.5054078317079));
#117722=CARTESIAN_POINT('Ctrl Pts',(-8.90507110211147,5.64606296086224,
11.4397122252583));
#117723=CARTESIAN_POINT('Ctrl Pts',(-8.87922172893789,5.65180725803288,
11.3620188026973));
#117724=CARTESIAN_POINT('Ctrl Pts',(-8.87609272053191,5.65252540285743,
11.3521845987954));
#117725=CARTESIAN_POINT('Ctrl Pts',(-8.87178113502745,5.65354788576446,
11.3379905846795));
#117726=CARTESIAN_POINT('Ctrl Pts',(-8.87049384548747,5.65385773525799,
11.3336634400313));
#117727=CARTESIAN_POINT('Ctrl Pts',(-8.86827676243306,5.65439944181888,
11.3260509659468));
#117728=CARTESIAN_POINT('Ctrl Pts',(-8.86733632707572,5.65463189194131,
11.3227688400012));
#117729=CARTESIAN_POINT('Ctrl Pts',(-8.8653593561261,5.65512629786925,11.3157541400231));
#117730=CARTESIAN_POINT('Ctrl Pts',(-8.86432695123927,5.65538802059525,
11.3120205042513));
#117731=CARTESIAN_POINT('Ctrl Pts',(-8.86152494302682,5.65610847305291,
11.3016890261951));
#117732=CARTESIAN_POINT('Ctrl Pts',(-8.85979425623234,5.65656506332959,
11.2950806520859));
#117733=CARTESIAN_POINT('Ctrl Pts',(-8.8499763500194,5.6592275670099,11.2562157806712));
#117734=CARTESIAN_POINT('Ctrl Pts',(-8.84319993132417,5.66136758416781,
11.2236402782718));
#117735=CARTESIAN_POINT('Ctrl Pts',(-8.82972323400405,5.66663066304444,
11.1415598179796));
#117736=CARTESIAN_POINT('Ctrl Pts',(-8.82477498280083,5.66970516250638,
11.0918343377936));
#117737=CARTESIAN_POINT('Ctrl Pts',(-8.82043547062653,5.67724548475243,
10.970058594321));
#117738=CARTESIAN_POINT('Ctrl Pts',(-8.8244645630676,5.68171858275261,10.8980995038247));
#117739=CARTESIAN_POINT('Ctrl Pts',(-8.83740660917913,5.6874505835615,10.8109679405071));
#117740=CARTESIAN_POINT('Ctrl Pts',(-8.84011127988951,5.6885119512546,10.7950252994599));
#117741=CARTESIAN_POINT('Ctrl Pts',(-8.84459556137706,5.6900967740084,10.7715363682457));
#117742=CARTESIAN_POINT('Ctrl Pts',(-8.84612291358142,5.69061235351592,
10.7639434125485));
#117743=CARTESIAN_POINT('Ctrl Pts',(-8.84897837222354,5.6915354793211,10.7504384150271));
#117744=CARTESIAN_POINT('Ctrl Pts',(-8.85027743478322,5.6919420974047,10.7445204646237));
#117745=CARTESIAN_POINT('Ctrl Pts',(-8.85167500520383,5.69236622608789,
10.7383803797683));
#117746=CARTESIAN_POINT('Ctrl Pts',(-8.85172799934485,5.69238228933724,
10.7381478816677));
#117747=CARTESIAN_POINT('Ctrl Pts',(-8.85183602870579,5.69241499551592,
10.7376745941957));
#117748=CARTESIAN_POINT('Ctrl Pts',(-8.85189106906718,5.69243163860739,
10.737433806021));
#117749=CARTESIAN_POINT('Ctrl Pts',(-8.85199018141113,5.69246157132207,
10.7370008406896));
#117750=CARTESIAN_POINT('Ctrl Pts',(-8.85203422592418,5.69247486007415,
10.7368086572));
#117751=CARTESIAN_POINT('Ctrl Pts',(-8.85211352745354,5.69249876286179,
10.7364630321335));
#117752=CARTESIAN_POINT('Ctrl Pts',(-8.85214876699141,5.69250937634355,
10.7363095865071));
#117753=CARTESIAN_POINT('Ctrl Pts',(-8.85221221141381,5.69252846969523,
10.7360335803762));
#117754=CARTESIAN_POINT('Ctrl Pts',(-8.85224040516692,5.69253694921186,
10.7359110172968));
#117755=CARTESIAN_POINT('Ctrl Pts',(-8.85229116342918,5.692552205703,10.7356905240883));
#117756=CARTESIAN_POINT('Ctrl Pts',(-8.85231372084538,5.69255898245254,
10.7355925923131));
#117757=CARTESIAN_POINT('Ctrl Pts',(-8.85235433179264,5.69257117682672,
10.7354163852431));
#117758=CARTESIAN_POINT('Ctrl Pts',(-8.85237238080182,5.69257659430843,
10.735338108889));
#117759=CARTESIAN_POINT('Ctrl Pts',(-8.85242127803492,5.69259126518817,
10.735126146597));
#117760=CARTESIAN_POINT('Ctrl Pts',(-8.85245214160332,5.69260051907262,
10.7349924642341));
#117761=CARTESIAN_POINT('Ctrl Pts',(-8.85251250030732,5.69261860430856,
10.7347312349951));
#117762=CARTESIAN_POINT('Ctrl Pts',(-8.85254199335314,5.69262743559395,
10.7346036876289));
#117763=CARTESIAN_POINT('Ctrl Pts',(-8.85259968027501,5.69264469802397,
10.7343544007321));
#117764=CARTESIAN_POINT('Ctrl Pts',(-8.85262787225994,5.69265312910793,
10.7342326607714));
#117765=CARTESIAN_POINT('Ctrl Pts',(-8.85268302251681,5.69266961220141,
10.7339946806596));
#117766=CARTESIAN_POINT('Ctrl Pts',(-8.85270997908106,5.69267766415671,
10.7338784401099));
#117767=CARTESIAN_POINT('Ctrl Pts',(-8.85276272034361,5.69269340881282,
10.7336511692175));
#117768=CARTESIAN_POINT('Ctrl Pts',(-8.85278850349565,5.69270110146426,
10.7335401385183));
#117769=CARTESIAN_POINT('Ctrl Pts',(-8.85283895635133,5.69271614615873,
10.7333230150553));
#117770=CARTESIAN_POINT('Ctrl Pts',(-8.85286362465407,5.69272349815682,
10.7332169219713));
#117771=CARTESIAN_POINT('Ctrl Pts',(-8.85291190296945,5.69273787908416,
10.7330094177831));
#117772=CARTESIAN_POINT('Ctrl Pts',(-8.85293551171732,5.6927449079741,10.7329080063678));
#117773=CARTESIAN_POINT('Ctrl Pts',(-8.85298172302272,5.6927586591927,10.7327096247633));
#117774=CARTESIAN_POINT('Ctrl Pts',(-8.85300432442984,5.69276538148475,
10.7326126543057));
#117775=CARTESIAN_POINT('Ctrl Pts',(-8.85304857024886,5.69277853504223,
10.7324229281797));
#117776=CARTESIAN_POINT('Ctrl Pts',(-8.85307021361671,5.69278496627449,
10.7323301722665));
#117777=CARTESIAN_POINT('Ctrl Pts',(-8.85311258982465,5.69279755233854,
10.7321486621492));
#117778=CARTESIAN_POINT('Ctrl Pts',(-8.85313332171459,5.69280370713969,
10.7320599077299));
#117779=CARTESIAN_POINT('Ctrl Pts',(-8.85317391884307,5.6928157541103,10.7318862001128));
#117780=CARTESIAN_POINT('Ctrl Pts',(-8.8531937832242,5.69282164625379,10.7318012466918));
#117781=CARTESIAN_POINT('Ctrl Pts',(-8.85323268682015,5.69283318088917,
10.7316349521619));
#117782=CARTESIAN_POINT('Ctrl Pts',(-8.8532517252439,5.69283882335418,10.7315536108964));
#117783=CARTESIAN_POINT('Ctrl Pts',(-8.85328901609544,5.69284987085508,
10.7313943628751));
#117784=CARTESIAN_POINT('Ctrl Pts',(-8.85330726781337,5.69285527586961,
10.7313164559319));
#117785=CARTESIAN_POINT('Ctrl Pts',(-8.85334302230932,5.6928658600014,10.7311639088761));
#117786=CARTESIAN_POINT('Ctrl Pts',(-8.85336052443384,5.69287103909722,
10.7310892686209));
#117787=CARTESIAN_POINT('Ctrl Pts',(-8.85339481476514,5.69288118226336,
10.7309430969272));
#117788=CARTESIAN_POINT('Ctrl Pts',(-8.85341160238164,5.69288614631579,
10.7308715653344));
#117789=CARTESIAN_POINT('Ctrl Pts',(-8.85512552386732,5.69339276800916,
10.7235716620517));
#117790=CARTESIAN_POINT('Ctrl Pts',(-8.85689093365318,5.69389658491991,
10.7163596464042));
#117791=CARTESIAN_POINT('Ctrl Pts',(-8.8626508373448,5.69548619623917,10.6937570146164));
#117792=CARTESIAN_POINT('Ctrl Pts',(-8.86688873745678,5.6965796559959,10.678430866149));
#117793=CARTESIAN_POINT('Ctrl Pts',(-8.87750057083868,5.69915438054011,
10.6428726980765));
#117794=CARTESIAN_POINT('Ctrl Pts',(-8.88411323373964,5.70064277244283,
10.6227182653889));
#117795=CARTESIAN_POINT('Ctrl Pts',(-8.91038803138248,5.70616623493076,
10.5493838898778));
#117796=CARTESIAN_POINT('Ctrl Pts',(-8.933336674925,5.71029275195161,10.4974691831022));
#117797=CARTESIAN_POINT('Ctrl Pts',(-8.99364865311626,5.71971933949734,
10.3839509507372));
#117798=CARTESIAN_POINT('Ctrl Pts',(-9.03310678545581,5.72502147709497,
10.3237021884467));
#117799=CARTESIAN_POINT('Ctrl Pts',(-9.08423912071204,5.7307886061424,10.2593356009091));
#117800=CARTESIAN_POINT('Ctrl Pts',(-9.09076996775819,5.73150741546516,
10.2513328465132));
#117801=CARTESIAN_POINT('Ctrl Pts',(-9.10030663316379,5.73253066636257,
10.2399557229522));
#117802=CARTESIAN_POINT('Ctrl Pts',(-9.1032276877866,5.73284063040539,10.236511375897));
#117803=CARTESIAN_POINT('Ctrl Pts',(-9.10839187321157,5.73338246695969,
10.2304925805417));
#117804=CARTESIAN_POINT('Ctrl Pts',(-9.1106264920798,5.73361493344824,10.2279109604706));
#117805=CARTESIAN_POINT('Ctrl Pts',(-9.11541965957674,5.73410929384367,
10.2224219127305));
#117806=CARTESIAN_POINT('Ctrl Pts',(-9.11798134673244,5.73437095528417,
10.2195173564808));
#117807=CARTESIAN_POINT('Ctrl Pts',(-9.12509806049707,5.7350910618468,10.2115278941836));
#117808=CARTESIAN_POINT('Ctrl Pts',(-9.12968312862919,5.73554737088737,
10.2064697773408));
#117809=CARTESIAN_POINT('Ctrl Pts',(-9.15677638885022,5.738201483049,10.1770985948259));
#117810=CARTESIAN_POINT('Ctrl Pts',(-9.18026071028634,5.74033388788059,
10.1537017519244));
#117811=CARTESIAN_POINT('Ctrl Pts',(-9.2362193271707,5.74513504297883,10.1024700526257));
#117812=CARTESIAN_POINT('Ctrl Pts',(-9.26928434523316,5.74777729970631,
10.0753509281711));
#117813=CARTESIAN_POINT('Ctrl Pts',(-9.34543318703334,5.75361769611662,
10.0195368060908));
#117814=CARTESIAN_POINT('Ctrl Pts',(-9.3890789741614,5.75681132730609,9.99176347828966));
#117815=CARTESIAN_POINT('Ctrl Pts',(-9.46657858128663,5.76240643889298,
9.94933256948704));
#117816=CARTESIAN_POINT('Ctrl Pts',(-9.49955429327655,5.76476497861299,
9.93323191524651));
#117817=CARTESIAN_POINT('Ctrl Pts',(-9.54314932008757,5.76788657375813,
9.91441289538316));
#117818=CARTESIAN_POINT('Ctrl Pts',(-9.55313174890669,5.76860151782906,
9.91026578519691));
#117819=CARTESIAN_POINT('Ctrl Pts',(-9.56934020589601,5.769763331187,9.90379228493961));
#117820=CARTESIAN_POINT('Ctrl Pts',(-9.57553146730357,5.7702073390646,9.90138010462552));
#117821=CARTESIAN_POINT('Ctrl Pts',(-9.58743144646808,5.77106133528235,
9.89685935465352));
#117822=CARTESIAN_POINT('Ctrl Pts',(-9.59313676059736,5.77147103007217,
9.89474238441067));
#117823=CARTESIAN_POINT('Ctrl Pts',(-9.60443976780258,5.77228330594148,
9.890647752811));
#117824=CARTESIAN_POINT('Ctrl Pts',(-9.61003651976814,5.77268580439191,
9.88866801202665));
#117825=CARTESIAN_POINT('Ctrl Pts',(-9.6229648189787,5.77361634095547,9.88420456478332));
#117826=CARTESIAN_POINT('Ctrl Pts',(-9.63030629636242,5.77414533087923,
9.88175068007574));
#117827=CARTESIAN_POINT('Ctrl Pts',(-9.65663557767925,5.77604480715797,
9.87323774572988));
#117828=CARTESIAN_POINT('Ctrl Pts',(-9.67575140967261,5.77742824655517,
9.86758882331491));
#117829=CARTESIAN_POINT('Ctrl Pts',(-9.73327922432616,5.78160631487507,
9.85216478097923));
#117830=CARTESIAN_POINT('Ctrl Pts',(-9.77203822195782,5.78444156898681,
9.84384320035442));
#117831=CARTESIAN_POINT('Ctrl Pts',(-9.81114942708339,5.78731516233854,
9.83748955978492));
#117832=CARTESIAN_POINT('Origin',(-10.,2.67563288526385,11.));
#117833=CARTESIAN_POINT('',(-9.81114930150155,6.38739526456853,9.83748958018577));
#117834=CARTESIAN_POINT('',(-9.81114930150541,6.28889384320256,9.83748958018515));
#117835=CARTESIAN_POINT('',(-9.81114930150157,2.67563288526385,9.83748958018577));
#117836=CARTESIAN_POINT('',(-9.81108652115608,6.38739074626474,9.83749978064041));
#117837=CARTESIAN_POINT('Ctrl Pts',(-9.81114930150153,6.38739526456853,
9.83748958018578));
#117838=CARTESIAN_POINT('Ctrl Pts',(-9.811125092701,6.38739352228488,9.83749351292377));
#117839=CARTESIAN_POINT('Ctrl Pts',(-9.81111072975194,6.3873924885829,9.83749584659379));
#117840=CARTESIAN_POINT('Ctrl Pts',(-9.81108652115608,6.38739074626474,
9.83749978064041));
#117841=CARTESIAN_POINT('Ctrl Pts',(-9.81108652115747,6.38739074626483,
9.83749978064019));
#117842=CARTESIAN_POINT('Ctrl Pts',(-9.70629422173851,6.37984873400106,
9.85452917771854));
#117843=CARTESIAN_POINT('Ctrl Pts',(-9.60431432144809,6.37191206627698,
9.88564185940446));
#117844=CARTESIAN_POINT('Ctrl Pts',(-9.49156845948395,6.36298003618431,
9.93749594515914));
#117845=CARTESIAN_POINT('Ctrl Pts',(-9.47542747424803,6.36169889764369,
9.94537151866597));
#117846=CARTESIAN_POINT('Ctrl Pts',(-9.44872567109751,6.35958243714402,
9.95916476905495));
#117847=CARTESIAN_POINT('Ctrl Pts',(-9.43806489731962,6.35873824085316,
9.9648814886998));
#117848=CARTESIAN_POINT('Ctrl Pts',(-9.42324552134241,6.35756778761629,
9.97312466021357));
#117849=CARTESIAN_POINT('Ctrl Pts',(-9.41901203223011,6.35723377635244,
9.97551394567556));
#117850=CARTESIAN_POINT('Ctrl Pts',(-9.41179450552945,6.35666509762935,
9.97964648272454));
#117851=CARTESIAN_POINT('Ctrl Pts',(-9.40880315382429,6.35642963396348,
9.98137676529053));
#117852=CARTESIAN_POINT('Ctrl Pts',(-9.40258119724893,6.35594040726098,
9.98501236339502));
#117853=CARTESIAN_POINT('Ctrl Pts',(-9.39935202901517,6.35568679161012,
9.98691997143284));
#117854=CARTESIAN_POINT('Ctrl Pts',(-9.39075257741571,6.35501202541322,
9.99205560705719));
#117855=CARTESIAN_POINT('Ctrl Pts',(-9.38539875879872,6.3545925878495,9.99531117265904));
#117856=CARTESIAN_POINT('Ctrl Pts',(-9.36158592312661,6.35272875821254,
10.0100529393856));
#117857=CARTESIAN_POINT('Ctrl Pts',(-9.34341980893909,6.35131162651471,
10.0220069983552));
#117858=CARTESIAN_POINT('Ctrl Pts',(-9.24218941974319,6.34337931952056,
10.0927138219315));
#117859=CARTESIAN_POINT('Ctrl Pts',(-9.16667897359472,6.33728876670943,
10.1615341306614));
#117860=CARTESIAN_POINT('Ctrl Pts',(-9.0830571195697,6.3291261256659,10.2603528021599));
#117861=CARTESIAN_POINT('Ctrl Pts',(-9.06591773062386,6.32736092092334,
10.2821195240132));
#117862=CARTESIAN_POINT('Ctrl Pts',(-9.04163329601515,6.32469961721259,
10.3153040171819));
#117863=CARTESIAN_POINT('Ctrl Pts',(-9.0338903865228,6.32382455549247,10.3262734082767));
#117864=CARTESIAN_POINT('Ctrl Pts',(-9.02012551203901,6.32221755088553,
10.3464994759808));
#117865=CARTESIAN_POINT('Ctrl Pts',(-9.0140429147898,6.32148788943906,10.3557131386691));
#117866=CARTESIAN_POINT('Ctrl Pts',(-9.00455913802206,6.32031769091186,
10.3705276314881));
#117867=CARTESIAN_POINT('Ctrl Pts',(-9.00107352058646,6.31988025688667,
10.3760738359218));
#117868=CARTESIAN_POINT('Ctrl Pts',(-8.99446021896994,6.31903583900708,
10.3867941924002));
#117869=CARTESIAN_POINT('Ctrl Pts',(-8.99132574703084,6.31862911824801,
10.3919639297122));
#117870=CARTESIAN_POINT('Ctrl Pts',(-8.9843397606953,6.31770765838549,10.4036887208888));
#117871=CARTESIAN_POINT('Ctrl Pts',(-8.98051166841585,6.31719210068422,
10.4102573439408));
#117872=CARTESIAN_POINT('Ctrl Pts',(-8.96911428319043,6.31562414332695,
10.4302567463196));
#117873=CARTESIAN_POINT('Ctrl Pts',(-8.9617451120734,6.31456476942986,10.4437990606441));
#117874=CARTESIAN_POINT('Ctrl Pts',(-8.91330230911327,6.30727536796872,
10.5371414518518));
#117875=CARTESIAN_POINT('Ctrl Pts',(-8.88120873676352,6.30073476276135,
10.6212518246503));
#117876=CARTESIAN_POINT('Ctrl Pts',(-8.84773275981184,6.29082032112359,
10.7521391615196));
#117877=CARTESIAN_POINT('Ctrl Pts',(-8.8390374445294,6.28749335510108,10.7967238379003));
#117878=CARTESIAN_POINT('Ctrl Pts',(-8.82990514995668,6.28262746781723,
10.8640520316427));
#117879=CARTESIAN_POINT('Ctrl Pts',(-8.82751597898316,6.28103227993347,
10.8864870544646));
#117880=CARTESIAN_POINT('Ctrl Pts',(-8.82530126139607,6.27904486070874,
10.9150581385752));
#117881=CARTESIAN_POINT('Ctrl Pts',(-8.82487720426123,6.2786242325543,10.9211414859415));
#117882=CARTESIAN_POINT('Ctrl Pts',(-8.82427095523865,6.27795147363083,
10.9309343406105));
#117883=CARTESIAN_POINT('Ctrl Pts',(-8.82405903284976,6.27769777966777,
10.9346417966469));
#117884=CARTESIAN_POINT('Ctrl Pts',(-8.82368491539028,6.27721139947143,
10.9417790976713));
#117885=CARTESIAN_POINT('Ctrl Pts',(-8.82352017975578,6.27697858525491,
10.9452087175666));
#117886=CARTESIAN_POINT('Ctrl Pts',(-8.82318906649482,6.27646556313903,
10.9527942006495));
#117887=CARTESIAN_POINT('Ctrl Pts',(-8.82302969835505,6.27618573541428,
10.9569503652164));
#117888=CARTESIAN_POINT('Ctrl Pts',(-8.82254172955023,6.27519559324589,
10.9717190176507));
#117889=CARTESIAN_POINT('Ctrl Pts',(-8.82233460898579,6.27449154925881,
10.9823353824679));
#117890=CARTESIAN_POINT('Ctrl Pts',(-8.8219044584418,6.26976718149439,11.0542297909788));
#117891=CARTESIAN_POINT('Ctrl Pts',(-8.82632060487794,6.26595504163347,
11.1154494459901));
#117892=CARTESIAN_POINT('Ctrl Pts',(-8.84163327647415,6.25961129438993,
11.2167359195588));
#117893=CARTESIAN_POINT('Ctrl Pts',(-8.84991122505178,6.25707572594225,
11.2570674084187));
#117894=CARTESIAN_POINT('Ctrl Pts',(-8.87395575485386,6.25111862635543,
11.3493732868182));
#117895=CARTESIAN_POINT('Ctrl Pts',(-8.8912372515358,6.24767731413254,11.4008508397926));
#117896=CARTESIAN_POINT('Ctrl Pts',(-8.91645632861289,6.24335499839081,
11.4616963125574));
#117897=CARTESIAN_POINT('Ctrl Pts',(-8.92106905669942,6.24258666608632,
11.4723752498627));
#117898=CARTESIAN_POINT('Ctrl Pts',(-8.92863748940995,6.24135920285288,
11.489207521536));
#117899=CARTESIAN_POINT('Ctrl Pts',(-8.93148989452805,6.24090355951913,
11.495406680848));
#117900=CARTESIAN_POINT('Ctrl Pts',(-8.93697196258465,6.2400405667787,11.5070532914514));
#117901=CARTESIAN_POINT('Ctrl Pts',(-8.9395900445429,6.23963362339906,11.5125059733628));
#117902=CARTESIAN_POINT('Ctrl Pts',(-8.94560690027989,6.2387098301773,11.5247937903583));
#117903=CARTESIAN_POINT('Ctrl Pts',(-8.94903033056707,6.23819214482194,
11.5316164786036));
#117904=CARTESIAN_POINT('Ctrl Pts',(-8.9594032863729,6.2366463961322,11.55179731025));
#117905=CARTESIAN_POINT('Ctrl Pts',(-8.9665427019263,6.23561180301538,11.5650555448208));
#117906=CARTESIAN_POINT('Ctrl Pts',(-9.01907436029362,6.22819677966362,
11.6582819130233));
#117907=CARTESIAN_POINT('Ctrl Pts',(-9.07343307562128,6.22148788494853,
11.7328148973178));
#117908=CARTESIAN_POINT('Ctrl Pts',(-9.1773578505369,6.21026489252221,11.8450323391692));
#117909=CARTESIAN_POINT('Ctrl Pts',(-9.22224890338372,6.20579768160234,
11.8865238654787));
#117910=CARTESIAN_POINT('Ctrl Pts',(-9.27724317159866,6.20089698559862,
11.9299457598515));
#117911=CARTESIAN_POINT('Ctrl Pts',(-9.28439232458486,6.20027021996111,
11.9354582922272));
#117912=CARTESIAN_POINT('Ctrl Pts',(-9.29506001281054,6.19935095590464,
11.943490003677));
#117913=CARTESIAN_POINT('Ctrl Pts',(-9.29852998299973,6.19905439652207,
11.946072718832));
#117914=CARTESIAN_POINT('Ctrl Pts',(-9.30448243049094,6.19854996474648,
11.9504523993803));
#117915=CARTESIAN_POINT('Ctrl Pts',(-9.3069577816837,6.19834145450866,11.9522588605016));
#117916=CARTESIAN_POINT('Ctrl Pts',(-9.31261301546616,6.19786796688682,
11.9563522030986));
#117917=CARTESIAN_POINT('Ctrl Pts',(-9.31579727962397,6.19760340783684,
11.9586329023276));
#117918=CARTESIAN_POINT('Ctrl Pts',(-9.32457472648706,6.1968795678452,11.9648536512827));
#117919=CARTESIAN_POINT('Ctrl Pts',(-9.33019106076757,6.19642240951869,
11.9687609916347));
#117920=CARTESIAN_POINT('Ctrl Pts',(-9.360758868145,6.19396462558051,11.9896343959691));
#117921=CARTESIAN_POINT('Ctrl Pts',(-9.38632353872697,6.19201756019995,
12.0056873314156));
#117922=CARTESIAN_POINT('Ctrl Pts',(-9.46857154385732,6.18599384250776,
12.0530278343754));
#117923=CARTESIAN_POINT('Ctrl Pts',(-9.52723302750387,6.18203637754222,
12.0806369383949));
#117924=CARTESIAN_POINT('Ctrl Pts',(-9.64690685357045,6.17410845601267,
12.1253408998996));
#117925=CARTESIAN_POINT('Ctrl Pts',(-9.70761252432059,6.17015287263634,
12.142617627114));
#117926=CARTESIAN_POINT('Ctrl Pts',(-9.78341873219423,6.16510613487855,
12.1577529330576));
#117927=CARTESIAN_POINT('Ctrl Pts',(-9.79748253232348,6.16416580695201,
12.1602956287908));
#117928=CARTESIAN_POINT('Ctrl Pts',(-9.81887412787079,6.16272776976035,
12.1637624127615));
#117929=CARTESIAN_POINT('Ctrl Pts',(-9.82617041122119,6.16223592465893,
12.1648745875945));
#117930=CARTESIAN_POINT('Ctrl Pts',(-9.83944562195321,6.16133835370048,
12.1667706334527));
#117931=CARTESIAN_POINT('Ctrl Pts',(-9.84542107699788,6.16093335351449,
12.167577309497));
#117932=CARTESIAN_POINT('Ctrl Pts',(-9.85835005048697,6.16005481325003,
12.1692217092685));
#117933=CARTESIAN_POINT('Ctrl Pts',(-9.86530534269043,6.15958078922281,
12.1700433578527));
#117934=CARTESIAN_POINT('Ctrl Pts',(-9.88433464202471,6.1582798489739,12.1721194215927));
#117935=CARTESIAN_POINT('Ctrl Pts',(-9.89642108615721,6.1574491176511,12.1732492501675));
#117936=CARTESIAN_POINT('Ctrl Pts',(-9.9729680335276,6.15215804231381,12.1792127781107));
#117937=CARTESIAN_POINT('Ctrl Pts',(-10.0377067570292,6.14754052359055,
12.1789186618631));
#117938=CARTESIAN_POINT('Ctrl Pts',(-10.1710445990236,6.13778864143651,
12.167317529738));
#117939=CARTESIAN_POINT('Ctrl Pts',(-10.2393399837693,6.13265920832274,
12.1552501402892));
#117940=CARTESIAN_POINT('Ctrl Pts',(-10.3244485035658,6.12630571835054,
12.1323365883588));
#117941=CARTESIAN_POINT('Ctrl Pts',(-10.3425966403301,6.12495397033817,
12.1269785282937));
#117942=CARTESIAN_POINT('Ctrl Pts',(-10.3725727336541,6.12273439176715,
12.1173372651871));
#117943=CARTESIAN_POINT('Ctrl Pts',(-10.3844749519752,6.12185662009324,
12.1132978258146));
#117944=CARTESIAN_POINT('Ctrl Pts',(-10.4009575402082,6.12064811768897,
12.1074079928679));
#117945=CARTESIAN_POINT('Ctrl Pts',(-10.4055938967586,6.12030896742988,
12.1057183207342));
#117946=CARTESIAN_POINT('Ctrl Pts',(-10.4134709318236,6.11973426652526,
12.1027914044581));
#117947=CARTESIAN_POINT('Ctrl Pts',(-10.4167169836809,6.11949787715479,
12.1015689038777));
#117948=CARTESIAN_POINT('Ctrl Pts',(-10.4234353573576,6.11900959176672,
12.099004739103));
#117949=CARTESIAN_POINT('Ctrl Pts',(-10.4269067770909,6.11875782237371,
12.0976609326531));
#117950=CARTESIAN_POINT('Ctrl Pts',(-10.4360856578786,6.11809337082034,
12.0940576039124));
#117951=CARTESIAN_POINT('Ctrl Pts',(-10.4417820176929,6.11768231092122,
12.0917698450513));
#117952=CARTESIAN_POINT('Ctrl Pts',(-10.4664961426038,6.11590345518523,
12.0816191105415));
#117953=CARTESIAN_POINT('Ctrl Pts',(-10.4853251086725,6.11455999829749,
12.0733024795324));
#117954=CARTESIAN_POINT('Ctrl Pts',(-10.596999059492,6.10660738205377,12.0204365229945));
#117955=CARTESIAN_POINT('Ctrl Pts',(-10.6838971370887,6.10044786928515,
11.9643585897023));
#117956=CARTESIAN_POINT('Ctrl Pts',(-10.7835859986464,6.09220195164302,
11.8796935140586));
#117957=CARTESIAN_POINT('Ctrl Pts',(-10.8041275965974,6.09043068872284,
11.8609566443414));
#117958=CARTESIAN_POINT('Ctrl Pts',(-10.8380157696309,6.08736140424382,
11.8277742309498));
#117959=CARTESIAN_POINT('Ctrl Pts',(-10.8516989095593,6.08607765539683,
11.8136888246224));
#117960=CARTESIAN_POINT('Ctrl Pts',(-10.8706946591815,6.08422611440667,
11.7931303294171));
#117961=CARTESIAN_POINT('Ctrl Pts',(-10.8763007186664,6.08367064232529,
11.7869319878202));
#117962=CARTESIAN_POINT('Ctrl Pts',(-10.8859154404189,6.08270177586815,
11.7760713194669));
#117963=CARTESIAN_POINT('Ctrl Pts',(-10.8899544872706,6.08228965374864,
11.7714362375604));
#117964=CARTESIAN_POINT('Ctrl Pts',(-10.8981801593538,6.081439623963,11.7618461403508));
#117965=CARTESIAN_POINT('Ctrl Pts',(-10.9023625000221,6.08100156215505,
11.7568877432476));
#117966=CARTESIAN_POINT('Ctrl Pts',(-10.9129333354446,6.07987908813245,
11.7441432794363));
#117967=CARTESIAN_POINT('Ctrl Pts',(-10.9192631972995,6.07919237201247,
11.7363094855211));
#117968=CARTESIAN_POINT('Ctrl Pts',(-10.9439864918241,6.07645070848699,
11.7048963358474));
#117969=CARTESIAN_POINT('Ctrl Pts',(-10.9615780516534,6.07436525955523,
11.6807031041947));
#117970=CARTESIAN_POINT('Ctrl Pts',(-11.0294744998208,6.06573414008526,
11.5794354614752));
#117971=CARTESIAN_POINT('Ctrl Pts',(-11.0715807899662,6.05892008917143,
11.4972660251621));
#117972=CARTESIAN_POINT('Ctrl Pts',(-11.1175036907816,6.04932392050498,
11.3739613752723));
#117973=CARTESIAN_POINT('Ctrl Pts',(-11.1294405004094,6.04646795035366,
11.3361939740255));
#117974=CARTESIAN_POINT('Ctrl Pts',(-11.1418431774274,6.04303491028879,
11.2887533171767));
#117975=CARTESIAN_POINT('Ctrl Pts',(-11.1441228329361,6.04237842695314,
11.2795841147672));
#117976=CARTESIAN_POINT('Ctrl Pts',(-11.1473033681052,6.04142430431516,
11.266100452843));
#117977=CARTESIAN_POINT('Ctrl Pts',(-11.1482907015608,6.04112216282071,
11.2618070582505));
#117978=CARTESIAN_POINT('Ctrl Pts',(-11.1499961159496,6.04058959787017,
11.2541958261614));
#117979=CARTESIAN_POINT('Ctrl Pts',(-11.150723971087,6.04035864070637,11.2508803063934));
#117980=CARTESIAN_POINT('Ctrl Pts',(-11.1522768610569,6.03985777636539,
11.2436576349092));
#117981=CARTESIAN_POINT('Ctrl Pts',(-11.1530963675353,6.03958817792172,
11.2397494023623));
#117982=CARTESIAN_POINT('Ctrl Pts',(-11.1553337788786,6.03883680301431,
11.2288022654326));
#117983=CARTESIAN_POINT('Ctrl Pts',(-11.1567072447311,6.03835742072707,
11.22175430904));
#117984=CARTESIAN_POINT('Ctrl Pts',(-11.1646265435953,6.03547599864402,
11.1790392091209));
#117985=CARTESIAN_POINT('Ctrl Pts',(-11.1695873791818,6.03315178173758,
11.1430941929195));
#117986=CARTESIAN_POINT('Ctrl Pts',(-11.1830507830697,6.02380828805878,
10.995479029044));
#117987=CARTESIAN_POINT('Ctrl Pts',(-11.1772710642939,6.01710399785173,
10.883107957809));
#117988=CARTESIAN_POINT('Ctrl Pts',(-11.15177936822,6.00854620343227,10.7531864146719));
#117989=CARTESIAN_POINT('Ctrl Pts',(-11.1473238032225,6.00721130635091,
10.7332404282512));
#117990=CARTESIAN_POINT('Ctrl Pts',(-11.1402866442378,6.0052989923684,10.7051891003853));
#117991=CARTESIAN_POINT('Ctrl Pts',(-11.138132560821,6.00473505819836,10.6969795958973));
#117992=CARTESIAN_POINT('Ctrl Pts',(-11.1342595724544,6.00375625404548,
10.6828433246477));
#117993=CARTESIAN_POINT('Ctrl Pts',(-11.1325824488133,6.0033427313431,10.6769053875374));
#117994=CARTESIAN_POINT('Ctrl Pts',(-11.1292722071328,6.00254569599005,
10.6655278810401));
#117995=CARTESIAN_POINT('Ctrl Pts',(-11.1276462458137,6.00216242366987,
10.6600863955035));
#117996=CARTESIAN_POINT('Ctrl Pts',(-11.1237142616486,6.00125442002403,
10.6472662744635));
#117997=CARTESIAN_POINT('Ctrl Pts',(-11.1213748436088,6.00072862286135,
10.6398982391766));
#117998=CARTESIAN_POINT('Ctrl Pts',(-11.1128600091068,5.99886394203865,
10.6139684874737));
#117999=CARTESIAN_POINT('Ctrl Pts',(-11.1062951536931,5.99751256811168,
10.5955390223871));
#118000=CARTESIAN_POINT('Ctrl Pts',(-11.0577356971366,5.9880659199627,10.469260400461));
#118001=CARTESIAN_POINT('Ctrl Pts',(-11.0005034541431,5.97944263925819,
10.3679620832917));
#118002=CARTESIAN_POINT('Ctrl Pts',(-10.9086570334226,5.968605568674,10.2499441843482));
#118003=CARTESIAN_POINT('Ctrl Pts',(-10.8867187140578,5.96618430723135,
10.2241316361699));
#118004=CARTESIAN_POINT('Ctrl Pts',(-10.8590302048183,5.96335277436182,
10.1942647598513));
#118005=CARTESIAN_POINT('Ctrl Pts',(-10.8543199605625,5.96287840483543,
10.1892721907946));
#118006=CARTESIAN_POINT('Ctrl Pts',(-10.8468780511222,5.962140677148,10.1815211094861));
#118007=CARTESIAN_POINT('Ctrl Pts',(-10.8441760278416,5.96187519937299,
10.1787345357308));
#118008=CARTESIAN_POINT('Ctrl Pts',(-10.8390717898062,5.96137823466725,
10.1735223856035));
#118009=CARTESIAN_POINT('Ctrl Pts',(-10.8366728139832,5.96114653026263,
10.1710939026464));
#118010=CARTESIAN_POINT('Ctrl Pts',(-10.8310838448612,5.9606109700974,10.1654851746107));
#118011=CARTESIAN_POINT('Ctrl Pts',(-10.8278861247826,5.96030771746657,
10.1623127570297));
#118012=CARTESIAN_POINT('Ctrl Pts',(-10.8173475005805,5.95931829342201,
10.151976811946));
#118013=CARTESIAN_POINT('Ctrl Pts',(-10.8099309719718,5.95863771457508,
10.144890590444));
#118014=CARTESIAN_POINT('Ctrl Pts',(-10.7495441853622,5.95321181468442,
10.0886838601736));
#118015=CARTESIAN_POINT('Ctrl Pts',(-10.692242036395,5.94876058173987,10.0444282099289));
#118016=CARTESIAN_POINT('Ctrl Pts',(-10.5835458903057,5.94079626491515,
9.97542178330105));
#118017=CARTESIAN_POINT('Ctrl Pts',(-10.5337394266677,5.937301350591,9.94861617554074));
#118018=CARTESIAN_POINT('Ctrl Pts',(-10.4628930425399,5.93235473993236,
9.9168226588763));
#118019=CARTESIAN_POINT('Ctrl Pts',(-10.4433519336298,5.93099333191455,
9.90867873434603));
#118020=CARTESIAN_POINT('Ctrl Pts',(-10.4086849019479,5.92857495945463,
9.8953157353362));
#118021=CARTESIAN_POINT('Ctrl Pts',(-10.3936520492041,5.92752527597006,
9.88986996340276));
#118022=CARTESIAN_POINT('Ctrl Pts',(-10.3712106766067,5.92595449166869,
9.8822535298701));
#118023=CARTESIAN_POINT('Ctrl Pts',(-10.3638837659836,5.92544105913767,
9.87984682384738));
#118024=CARTESIAN_POINT('Ctrl Pts',(-10.3507613863413,5.92452021417186,
9.87567878436805));
#118025=CARTESIAN_POINT('Ctrl Pts',(-10.3449749183962,5.92411371098358,
9.87388985911269));
#118026=CARTESIAN_POINT('Ctrl Pts',(-10.3326857641733,5.92324932245628,
9.87019419222461));
#118027=CARTESIAN_POINT('Ctrl Pts',(-10.3261799266074,5.92279108867051,
9.86829878804781));
#118028=CARTESIAN_POINT('Ctrl Pts',(-10.3086745537846,5.92155623859653,
9.86336227544526));
#118029=CARTESIAN_POINT('Ctrl Pts',(-10.2976468070993,5.92077634841056,
9.86042478994145));
#118030=CARTESIAN_POINT('Ctrl Pts',(-10.2436175470539,5.91694453892045,
9.84687062917507));
#118031=CARTESIAN_POINT('Ctrl Pts',(-10.2000881977963,5.91382215544051,
9.83852649164516));
#118032=CARTESIAN_POINT('Ctrl Pts',(-10.0834333548866,5.90536608682455,
9.82291747677267));
#118033=CARTESIAN_POINT('Ctrl Pts',(-10.009922120106,5.89993789865148,9.82000658530401));
#118034=CARTESIAN_POINT('Ctrl Pts',(-9.90637557113827,5.89236928612994,
9.82558639901517));
#118035=CARTESIAN_POINT('Ctrl Pts',(-9.87619670925931,5.89017484800594,
9.82838324284337));
#118036=CARTESIAN_POINT('Ctrl Pts',(-9.83446346949928,5.88718191571037,
9.83388171966526));
#118037=CARTESIAN_POINT('Ctrl Pts',(-9.82279274497268,5.88634954765775,
9.835598093972));
#118038=CARTESIAN_POINT('Ctrl Pts',(-9.81114930150087,5.88552497076973,
9.83748958018588));
#118039=CARTESIAN_POINT('Ctrl Pts',(-9.81114942708287,5.78731516233851,
9.837489559785));
#118040=CARTESIAN_POINT('Ctrl Pts',(-9.90947160064604,5.79453912650356,
9.82151705909552));
#118041=CARTESIAN_POINT('Ctrl Pts',(-10.0094102735156,5.80199718996431,
9.8180824094726));
#118042=CARTESIAN_POINT('Ctrl Pts',(-10.1158737937996,5.80950143692189,
9.82794125172127));
#118043=CARTESIAN_POINT('Ctrl Pts',(-10.1231428226069,5.81001136187773,
9.82868266597279));
#118044=CARTESIAN_POINT('Ctrl Pts',(-10.1364257823334,5.8109381422852,9.83016250190705));
#118045=CARTESIAN_POINT('Ctrl Pts',(-10.1424417717871,5.81135600042542,
9.83087977025029));
#118046=CARTESIAN_POINT('Ctrl Pts',(-10.1521266188609,5.81202535872896,
9.83211033300425));
#118047=CARTESIAN_POINT('Ctrl Pts',(-10.1557989617142,5.81227839549757,
9.83259455760698));
#118048=CARTESIAN_POINT('Ctrl Pts',(-10.1628740332343,5.81276432143749,
9.83356143649753));
#118049=CARTESIAN_POINT('Ctrl Pts',(-10.1662770028275,5.81299733261119,
9.83404166807149));
#118050=CARTESIAN_POINT('Ctrl Pts',(-10.1738091880881,5.81351159877274,
9.83513826644664));
#118051=CARTESIAN_POINT('Ctrl Pts',(-10.1779373689123,5.81379246602502,
9.83576171415851));
#118052=CARTESIAN_POINT('Ctrl Pts',(-10.1922349074714,5.81476206868853,
9.83799878668286));
#118053=CARTESIAN_POINT('Ctrl Pts',(-10.2023867043277,5.81544498728578,
9.8397238609111));
#118054=CARTESIAN_POINT('Ctrl Pts',(-10.2801247790684,5.82064096924409,
9.85398512492233));
#118055=CARTESIAN_POINT('Ctrl Pts',(-10.3465284807465,5.82488919782711,
9.87228525326674));
#118056=CARTESIAN_POINT('Ctrl Pts',(-10.4660855137594,5.83278156314981,
9.91680147391089));
#118057=CARTESIAN_POINT('Ctrl Pts',(-10.5195891101423,5.83641337635526,
9.94142487387269));
#118058=CARTESIAN_POINT('Ctrl Pts',(-10.5899678887931,5.84153504657397,
9.98044032716379));
#118059=CARTESIAN_POINT('Ctrl Pts',(-10.6086139186056,5.8429268475616,9.99145994123044));
#118060=CARTESIAN_POINT('Ctrl Pts',(-10.6405808342553,5.84538366108026,
10.0115614719147));
#118061=CARTESIAN_POINT('Ctrl Pts',(-10.6540389683504,5.84644077711937,
10.0204146201527));
#118062=CARTESIAN_POINT('Ctrl Pts',(-10.673259961579,5.84798634290642,10.0336314297363));
#118063=CARTESIAN_POINT('Ctrl Pts',(-10.6791712632499,5.84846670142559,
10.0377767510773));
#118064=CARTESIAN_POINT('Ctrl Pts',(-10.6851680254147,5.84895929271713,
10.0420647920094));
#118065=CARTESIAN_POINT('Ctrl Pts',(-10.6852920634587,5.84896948388425,
10.0421535229907));
#118066=CARTESIAN_POINT('Ctrl Pts',(-10.6855475884722,5.84899048302827,
10.042336388605));
#118067=CARTESIAN_POINT('Ctrl Pts',(-10.6856790732958,5.84900129111814,
10.0424305262309));
#118068=CARTESIAN_POINT('Ctrl Pts',(-10.6859504176161,5.84902360110197,
10.0426248819419));
#118069=CARTESIAN_POINT('Ctrl Pts',(-10.6860902745437,5.84903510313059,
10.0427251035983));
#118070=CARTESIAN_POINT('Ctrl Pts',(-10.6863794437516,5.84905889094312,
10.0429324185521));
#118071=CARTESIAN_POINT('Ctrl Pts',(-10.686528752931,5.84907117688871,10.0430395161439));
#118072=CARTESIAN_POINT('Ctrl Pts',(-10.6916040110387,5.8494889109615,10.0466817339086));
#118073=CARTESIAN_POINT('Ctrl Pts',(-10.6965025329501,5.84989578610632,
10.050254747946));
#118074=CARTESIAN_POINT('Ctrl Pts',(-10.7067823119526,5.85075758464687,
10.0578751869046));
#118075=CARTESIAN_POINT('Ctrl Pts',(-10.7121568676708,5.85121283065427,
10.0619312431805));
#118076=CARTESIAN_POINT('Ctrl Pts',(-10.7263929426214,5.85243140557028,
10.0728677446094));
#118077=CARTESIAN_POINT('Ctrl Pts',(-10.7351912427192,5.85319786122763,
10.0798289574122));
#118078=CARTESIAN_POINT('Ctrl Pts',(-10.7758653243394,5.85680532844437,
10.1129660344793));
#118079=CARTESIAN_POINT('Ctrl Pts',(-10.8064478968707,5.85970689640087,
10.1406762262686));
#118080=CARTESIAN_POINT('Ctrl Pts',(-10.895556579142,5.86876608198137,10.2303690942567));
#118081=CARTESIAN_POINT('Ctrl Pts',(-10.9488640058241,5.87509134210871,
10.2971428844925));
#118082=CARTESIAN_POINT('Ctrl Pts',(-11.0077711710052,5.8830780034626,10.3899947905962));
#118083=CARTESIAN_POINT('Ctrl Pts',(-11.0203829632282,5.88486226307866,
10.4113338370063));
#118084=CARTESIAN_POINT('Ctrl Pts',(-11.0372908443385,5.88735038048038,
10.4421203471628));
#118085=CARTESIAN_POINT('Ctrl Pts',(-11.0421494712075,5.88807782057147,
10.4512500580464));
#118086=CARTESIAN_POINT('Ctrl Pts',(-11.0505319410105,5.88935396544953,
10.4675143279457));
#118087=CARTESIAN_POINT('Ctrl Pts',(-11.0541048699363,5.88990514641565,
10.4746227243214));
#118088=CARTESIAN_POINT('Ctrl Pts',(-11.0594148296537,5.89073489823167,
10.4854592464811));
#118089=CARTESIAN_POINT('Ctrl Pts',(-11.0612047314854,5.89101650016448,
10.4891609965118));
#118090=CARTESIAN_POINT('Ctrl Pts',(-11.0644325507665,5.89152773883546,
10.4959267297449));
#118091=CARTESIAN_POINT('Ctrl Pts',(-11.0658766643162,5.8917577368547,10.4989875709834));
#118092=CARTESIAN_POINT('Ctrl Pts',(-11.0691057930816,5.89227494629921,
10.5059089615551));
#118093=CARTESIAN_POINT('Ctrl Pts',(-11.0708831070205,5.89256169346219,
10.5097729877074));
#118094=CARTESIAN_POINT('Ctrl Pts',(-11.075429587041,5.89330086127631,10.5198001290989));
#118095=CARTESIAN_POINT('Ctrl Pts',(-11.078166765539,5.8937514467997,10.52597769716));
#118096=CARTESIAN_POINT('Ctrl Pts',(-11.0982704139765,5.89710591934993,
10.5724250061464));
#118097=CARTESIAN_POINT('Ctrl Pts',(-11.1134307745713,5.89989462363576,
10.613617925865));
#118098=CARTESIAN_POINT('Ctrl Pts',(-11.1318844536946,5.90384498513094,
10.6739591580923));
#118099=CARTESIAN_POINT('Ctrl Pts',(-11.1370584093556,5.90504028836632,
10.6924886177964));
#118100=CARTESIAN_POINT('Ctrl Pts',(-11.1538881992863,5.90929301887068,
10.7590109600925));
#118101=CARTESIAN_POINT('Ctrl Pts',(-11.162976854303,5.91233058417215,10.8075983550166));
#118102=CARTESIAN_POINT('Ctrl Pts',(-11.1750155459169,5.91852626408267,
10.9057454031004));
#118103=CARTESIAN_POINT('Ctrl Pts',(-11.1779379923034,5.92167863521211,
10.9552042523465));
#118104=CARTESIAN_POINT('Ctrl Pts',(-11.1776952635886,5.92567537975267,
11.0160747781951));
#118105=CARTESIAN_POINT('Ctrl Pts',(-11.1774850013983,5.92642725270317,
11.0274515773558));
#118106=CARTESIAN_POINT('Ctrl Pts',(-11.1768868485671,5.92763441770235,
11.0455874118374));
#118107=CARTESIAN_POINT('Ctrl Pts',(-11.1766054568,5.92808642022136,11.052349424586));
#118108=CARTESIAN_POINT('Ctrl Pts',(-11.175961858709,5.92894632661825,11.0651570948562));
#118109=CARTESIAN_POINT('Ctrl Pts',(-11.1756112669987,5.92935385801442,
11.0712031369153));
#118110=CARTESIAN_POINT('Ctrl Pts',(-11.1747076567851,5.93028426795964,
11.0849505660536));
#118111=CARTESIAN_POINT('Ctrl Pts',(-11.1741255074466,5.93080803107064,
11.0926496920355));
#118112=CARTESIAN_POINT('Ctrl Pts',(-11.1721009181036,5.93242733381381,
11.1163265290887));
#118113=CARTESIAN_POINT('Ctrl Pts',(-11.1704077434366,5.9335305381578,11.1322803605795));
#118114=CARTESIAN_POINT('Ctrl Pts',(-11.1586219860055,5.94002985697228,
11.2252014999871));
#118115=CARTESIAN_POINT('Ctrl Pts',(-11.1412671196536,5.94564998499509,
11.3010416623207));
#118116=CARTESIAN_POINT('Ctrl Pts',(-11.0994558299612,5.95528925424692,
11.4256665548531));
#118117=CARTESIAN_POINT('Ctrl Pts',(-11.078844579872,5.95925571722541,11.4754892218222));
#118118=CARTESIAN_POINT('Ctrl Pts',(-11.0474862437933,5.96432013598574,
11.5386513020983));
#118119=CARTESIAN_POINT('Ctrl Pts',(-11.0397610445403,5.96550642379532,
11.5534163754663));
#118120=CARTESIAN_POINT('Ctrl Pts',(-11.0262058764351,5.96748303446041,
11.5780376347333));
#118121=CARTESIAN_POINT('Ctrl Pts',(-11.0205409367788,5.96828088418374,
11.5879814866216));
#118122=CARTESIAN_POINT('Ctrl Pts',(-11.012317977323,5.96939845561366,11.6019385233083));
#118123=CARTESIAN_POINT('Ctrl Pts',(-11.0098794059447,5.96972505526765,
11.6060208416054));
#118124=CARTESIAN_POINT('Ctrl Pts',(-11.0056354870955,5.97028507328242,
11.6130286662371));
#118125=CARTESIAN_POINT('Ctrl Pts',(-11.0038419520618,5.97051922711342,
11.6159612123169));
#118126=CARTESIAN_POINT('Ctrl Pts',(-11.0000420840315,5.97101001093681,
11.6221135619159));
#118127=CARTESIAN_POINT('Ctrl Pts',(-10.9980330091693,5.97126646210512,
11.6253315659574));
#118128=CARTESIAN_POINT('Ctrl Pts',(-10.9925583583521,5.97195729212957,
11.6340069077107));
#118129=CARTESIAN_POINT('Ctrl Pts',(-10.9890632810347,5.97238981207894,
11.6394456071847));
#118130=CARTESIAN_POINT('Ctrl Pts',(-10.9723353491798,5.97442157832678,
11.6650106716581));
#118131=CARTESIAN_POINT('Ctrl Pts',(-10.958530907186,5.97598710954884,11.6847582879155));
#118132=CARTESIAN_POINT('Ctrl Pts',(-10.9028407971031,5.98194992737554,
11.7594364605432));
#118133=CARTESIAN_POINT('Ctrl Pts',(-10.8567588458612,5.98617139903251,
11.81106783501));
#118134=CARTESIAN_POINT('Ctrl Pts',(-10.7584952246908,5.9945312462484,11.9033841529435));
#118135=CARTESIAN_POINT('Ctrl Pts',(-10.7068970201755,5.99865029955416,
11.9443055507134));
#118136=CARTESIAN_POINT('Ctrl Pts',(-10.6403315529191,6.00387006293588,
11.9885708346382));
#118137=CARTESIAN_POINT('Ctrl Pts',(-10.6283637779072,6.00480471257315,
11.9962207221405));
#118138=CARTESIAN_POINT('Ctrl Pts',(-10.6099876276135,6.00623574767356,
12.0075040195473));
#118139=CARTESIAN_POINT('Ctrl Pts',(-10.6036784065798,6.00672635565561,
12.0112970051144));
#118140=CARTESIAN_POINT('Ctrl Pts',(-10.5921397370371,6.00762252715203,
12.0180873836492));
#118141=CARTESIAN_POINT('Ctrl Pts',(-10.5869220096243,6.00802737479339,
12.0211042753982));
#118142=CARTESIAN_POINT('Ctrl Pts',(-10.5755814230532,6.00890656972139,
12.027545766937));
#118143=CARTESIAN_POINT('Ctrl Pts',(-10.5694506895897,6.00938140858583,
12.0309559574311));
#118144=CARTESIAN_POINT('Ctrl Pts',(-10.5525790327372,6.01068712373316,
12.0401443292468));
#118145=CARTESIAN_POINT('Ctrl Pts',(-10.5417784976248,6.01152186302523,
12.0458106201535));
#118146=CARTESIAN_POINT('Ctrl Pts',(-10.4665999776609,6.01732642989461,
12.0837744660025));
#118147=CARTESIAN_POINT('Ctrl Pts',(-10.3994766430831,6.0224944250484,12.1102691906438));
#118148=CARTESIAN_POINT('Ctrl Pts',(-10.2796567893891,6.03161908203103,
12.1452851907529));
#118149=CARTESIAN_POINT('Ctrl Pts',(-10.2280080506737,6.03551786450257,
12.1566756184141));
#118150=CARTESIAN_POINT('Ctrl Pts',(-10.1515834263136,6.04112962872133,
12.1682105073654));
#118151=CARTESIAN_POINT('Ctrl Pts',(-10.1272885316629,6.04289016423973,
12.1711067860192));
#118152=CARTESIAN_POINT('Ctrl Pts',(-10.0927069711798,6.04534868355793,
12.1741403584893));
#118153=CARTESIAN_POINT('Ctrl Pts',(-10.0824826348186,6.04606969412131,
12.1749028874096));
#118154=CARTESIAN_POINT('Ctrl Pts',(-10.0643622881309,6.04733569457318,
12.1760165805728));
#118155=CARTESIAN_POINT('Ctrl Pts',(-10.0564703610344,6.04788310826346,
12.1764219517979));
#118156=CARTESIAN_POINT('Ctrl Pts',(-10.0444775131329,6.04870837079211,
12.1769170016562));
#118157=CARTESIAN_POINT('Ctrl Pts',(-10.0403794025583,6.04898920282887,
12.1770647319035));
#118158=CARTESIAN_POINT('Ctrl Pts',(-10.0328972549855,6.04949969635539,
12.1772953285025));
#118159=CARTESIAN_POINT('Ctrl Pts',(-10.0295135976092,6.04972971248978,
12.1773850126808));
#118160=CARTESIAN_POINT('Ctrl Pts',(-10.0218649315126,6.0502477731439,12.1775547471037));
#118161=CARTESIAN_POINT('Ctrl Pts',(-10.017599837303,6.05053534615001,12.1776262160832));
#118162=CARTESIAN_POINT('Ctrl Pts',(-10.0065365869644,6.05127810145475,
12.1777514811081));
#118163=CARTESIAN_POINT('Ctrl Pts',(-9.99973807400412,6.05173141895143,
12.1777695933052));
#118164=CARTESIAN_POINT('Ctrl Pts',(-9.94703997528089,6.0552237622368,12.1774536716179));
#118165=CARTESIAN_POINT('Ctrl Pts',(-9.90118981057364,6.05813647379192,
12.1744954204296));
#118166=CARTESIAN_POINT('Ctrl Pts',(-9.83850812105004,6.06208433004872,
12.1667531323157));
#118167=CARTESIAN_POINT('Ctrl Pts',(-9.82144006302314,6.06315570866509,
12.1642632295234));
#118168=CARTESIAN_POINT('Ctrl Pts',(-9.75464996471581,6.06735324763434,
12.1530164804466));
#118169=CARTESIAN_POINT('Ctrl Pts',(-9.7054590877052,6.07045818225584,12.1414416932365));
#118170=CARTESIAN_POINT('Ctrl Pts',(-9.61086941177181,6.07665833042173,
12.1126607684765));
#118171=CARTESIAN_POINT('Ctrl Pts',(-9.565492693937,6.07974261654607,12.0957368116173));
#118172=CARTESIAN_POINT('Ctrl Pts',(-9.51095249436908,6.08366260936188,
12.0714735567464));
#118173=CARTESIAN_POINT('Ctrl Pts',(-9.5006833065229,6.08441023225558,12.0667267085232));
#118174=CARTESIAN_POINT('Ctrl Pts',(-9.48439540958915,6.08561217650794,
12.0589110354723));
#118175=CARTESIAN_POINT('Ctrl Pts',(-9.47833179796513,6.08606325884864,
12.0559370049776));
#118176=CARTESIAN_POINT('Ctrl Pts',(-9.46687748099454,6.08692244306843,
12.0501962451072));
#118177=CARTESIAN_POINT('Ctrl Pts',(-9.46148187561897,6.08733018131324,
12.0474397361521));
#118178=CARTESIAN_POINT('Ctrl Pts',(-9.44923739567313,6.08826250434251,
12.0410646546737));
#118179=CARTESIAN_POINT('Ctrl Pts',(-9.44240252874945,6.08878798738599,
12.0374199326366));
#118180=CARTESIAN_POINT('Ctrl Pts',(-9.42140825397861,6.0904180874743,12.025957239138));
#118181=CARTESIAN_POINT('Ctrl Pts',(-9.40737407563235,6.09153051819662,
12.0179150916901));
#118182=CARTESIAN_POINT('Ctrl Pts',(-9.33379521931331,6.09748777759601,
11.9737140386729));
#118183=CARTESIAN_POINT('Ctrl Pts',(-9.27739000599291,6.10250883656341,
11.9326198247534));
#118184=CARTESIAN_POINT('Ctrl Pts',(-9.17981419023098,6.11199402890588,
11.8473395231834));
#118185=CARTESIAN_POINT('Ctrl Pts',(-9.13775194974572,6.11642177259655,
11.8044984387828));
#118186=CARTESIAN_POINT('Ctrl Pts',(-9.08777731861914,6.12200282642176,
11.7451547875916));
#118187=CARTESIAN_POINT('Ctrl Pts',(-9.07672468994285,6.12326003064341,
11.7314155091281));
#118188=CARTESIAN_POINT('Ctrl Pts',(-9.05871548420487,6.12534130879301,
11.7079695644674));
#118189=CARTESIAN_POINT('Ctrl Pts',(-9.05159069704285,6.12617390861915,
11.6983962093682));
#118190=CARTESIAN_POINT('Ctrl Pts',(-9.04178532445334,6.12733112196246,
11.6847941798981));
#118191=CARTESIAN_POINT('Ctrl Pts',(-9.03898245074212,6.12766326646496,
11.6808551280019));
#118192=CARTESIAN_POINT('Ctrl Pts',(-9.03422079000655,6.12822971748844,
11.6740752814595));
#118193=CARTESIAN_POINT('Ctrl Pts',(-9.03225010613175,6.12846480515564,
11.6712429602783));
#118194=CARTESIAN_POINT('Ctrl Pts',(-9.02815820107811,6.12895425969481,
11.6653064816562));
#118195=CARTESIAN_POINT('Ctrl Pts',(-9.0260393646799,6.12920847189046,11.6622007841338));
#118196=CARTESIAN_POINT('Ctrl Pts',(-9.02040426770968,6.1298867784185,11.6538555491758));
#118197=CARTESIAN_POINT('Ctrl Pts',(-9.01691512223378,6.13030912745391,
11.6485977223077));
#118198=CARTESIAN_POINT('Ctrl Pts',(-9.0012750329835,6.13221435726023,11.6246133343469));
#118199=CARTESIAN_POINT('Ctrl Pts',(-8.98961489105718,6.13366842656563,
11.6055703606862));
#118200=CARTESIAN_POINT('Ctrl Pts',(-8.96763850352448,6.13650225493909,
11.5672752412326));
#118201=CARTESIAN_POINT('Ctrl Pts',(-8.95730253432802,6.13788238655509,
11.5480452025423));
#118202=CARTESIAN_POINT('Ctrl Pts',(-8.9166486186316,6.1435617755003,11.4670898730716));
#118203=CARTESIAN_POINT('Ctrl Pts',(-8.89123096516069,6.14775342711004,
11.4030568239904));
#118204=CARTESIAN_POINT('Ctrl Pts',(-8.85693437350742,6.15525136477062,
11.2882717732334));
#118205=CARTESIAN_POINT('Ctrl Pts',(-8.84551926511867,6.15849743397149,
11.2384804320415));
#118206=CARTESIAN_POINT('Ctrl Pts',(-8.83553832368823,6.16259975366978,
11.1767922684761));
#118207=CARTESIAN_POINT('Ctrl Pts',(-8.83387259266239,6.163357218145,11.1654489545542));
#118208=CARTESIAN_POINT('Ctrl Pts',(-8.83148489797139,6.16457125180627,
11.1473552697741));
#118209=CARTESIAN_POINT('Ctrl Pts',(-8.83065521510991,6.16502446451204,
11.1406196643484));
#118210=CARTESIAN_POINT('Ctrl Pts',(-8.82919577056458,6.165885335354,11.1278638150882));
#118211=CARTESIAN_POINT('Ctrl Pts',(-8.82855411552353,6.16629260945253,
11.121845132331));
#118212=CARTESIAN_POINT('Ctrl Pts',(-8.82720271741023,6.16722057532817,
11.1081698722249));
#118213=CARTESIAN_POINT('Ctrl Pts',(-8.82652151366565,6.16774213412433,
11.100510818159));
#118214=CARTESIAN_POINT('Ctrl Pts',(-8.82466391719549,6.16934766410132,
11.077020519941));
#118215=CARTESIAN_POINT('Ctrl Pts',(-8.82373260712074,6.17043911208709,
11.0611722644537));
#118216=CARTESIAN_POINT('Ctrl Pts',(-8.81994039894409,6.17727679848077,
10.9626752375845));
#118217=CARTESIAN_POINT('Ctrl Pts',(-8.8254716351637,6.18328105719493,10.8799488573848));
#118218=CARTESIAN_POINT('Ctrl Pts',(-8.85145132348145,6.19442286019621,
10.7303393820249));
#118219=CARTESIAN_POINT('Ctrl Pts',(-8.86927084106631,6.19951365297629,
10.6633483482401));
#118220=CARTESIAN_POINT('Ctrl Pts',(-8.89597270092113,6.20499005121681,
10.589754333469));
#118221=CARTESIAN_POINT('Ctrl Pts',(-8.89917383850949,6.20562162857878,
10.5812404522781));
#118222=CARTESIAN_POINT('Ctrl Pts',(-8.90404699459608,6.20654649929942,
10.5687217955917));
#118223=CARTESIAN_POINT('Ctrl Pts',(-8.90564293713968,6.20684392410625,
10.5646880427521));
#118224=CARTESIAN_POINT('Ctrl Pts',(-8.9085251933115,6.20737135213772,10.5575191630085));
#118225=CARTESIAN_POINT('Ctrl Pts',(-8.90980278748786,6.20760185033157,
10.554380674198));
#118226=CARTESIAN_POINT('Ctrl Pts',(-8.91263372108549,6.2081054476046,10.5475113609995));
#118227=CARTESIAN_POINT('Ctrl Pts',(-8.91419272808288,6.20837820795604,
10.5437829875848));
#118228=CARTESIAN_POINT('Ctrl Pts',(-8.91866012672926,6.20914723092183,
10.5332518066875));
#118229=CARTESIAN_POINT('Ctrl Pts',(-8.92161353228926,6.20964091670073,
10.526468131364));
#118230=CARTESIAN_POINT('Ctrl Pts',(-8.94237360183216,6.21301507758722,
10.479986094138));
#118231=CARTESIAN_POINT('Ctrl Pts',(-8.96230639805596,6.21578275798562,
10.4412684457535));
#118232=CARTESIAN_POINT('Ctrl Pts',(-8.99424397426174,6.21973319052331,
10.3868665181161));
#118233=CARTESIAN_POINT('Ctrl Pts',(-9.00456824894697,6.22094906703784,
10.3702432929228));
#118234=CARTESIAN_POINT('Ctrl Pts',(-9.042848454305,6.2252736976786,10.3119031812852));
#118235=CARTESIAN_POINT('Ctrl Pts',(-9.07305070880461,6.2283619059775,10.271727265241));
#118236=CARTESIAN_POINT('Ctrl Pts',(-9.13746595293808,6.23456760567458,
10.1965639886571));
#118237=CARTESIAN_POINT('Ctrl Pts',(-9.17147437984068,6.23767572605648,
10.161537809113));
#118238=CARTESIAN_POINT('Ctrl Pts',(-9.21593957255163,6.24162259097188,
10.12109567214));
#118239=CARTESIAN_POINT('Ctrl Pts',(-9.22443529865826,6.2423717198824,10.1135898517853));
#118240=CARTESIAN_POINT('Ctrl Pts',(-9.23816697858046,6.24357551410664,
10.1018067078392));
#118241=CARTESIAN_POINT('Ctrl Pts',(-9.24333384539688,6.24402692254065,
10.0974496856814));
#118242=CARTESIAN_POINT('Ctrl Pts',(-9.25320244835176,6.24488636155847,
10.0892721710971));
#118243=CARTESIAN_POINT('Ctrl Pts',(-9.25789673572267,6.24529402536646,
10.0854430010735));
#118244=CARTESIAN_POINT('Ctrl Pts',(-9.26865323526619,6.24622566489964,
10.0768061774196));
#118245=CARTESIAN_POINT('Ctrl Pts',(-9.27473364840652,6.24675053399349,
10.0720217466764));
#118246=CARTESIAN_POINT('Ctrl Pts',(-9.2936322345923,6.24837677466826,10.0574504126231));
#118247=CARTESIAN_POINT('Ctrl Pts',(-9.30660416466416,6.24948590651322,
10.0478669653783));
#118248=CARTESIAN_POINT('Ctrl Pts',(-9.37658707831844,6.25543525747671,
9.99835345659297));
#118249=CARTESIAN_POINT('Ctrl Pts',(-9.43684831745196,6.26045148134564,
9.96327594894306));
#118250=CARTESIAN_POINT('Ctrl Pts',(-9.55421430847007,6.26993962622691,
9.9082230851759));
#118251=CARTESIAN_POINT('Ctrl Pts',(-9.61045754356547,6.27437536955614,
9.88691474052568));
#118252=CARTESIAN_POINT('Ctrl Pts',(-9.68501252270141,6.27996531685678,
9.86501571460661));
#118253=CARTESIAN_POINT('Ctrl Pts',(-9.7020536997882,6.28122368640625,9.8604235398414));
#118254=CARTESIAN_POINT('Ctrl Pts',(-9.73078847295159,6.28330667744125,
9.85336894024559));
#118255=CARTESIAN_POINT('Ctrl Pts',(-9.7424276179688,6.28413984170077,9.85069841692303));
#118256=CARTESIAN_POINT('Ctrl Pts',(-9.75883493815722,6.28529769725672,
9.8471956547395));
#118257=CARTESIAN_POINT('Ctrl Pts',(-9.76357024640248,6.28562993036857,
9.84621517639846));
#118258=CARTESIAN_POINT('Ctrl Pts',(-9.77169471585385,6.28619648463342,
9.84458506750503));
#118259=CARTESIAN_POINT('Ctrl Pts',(-9.77508090643458,6.28643158766354,
9.84392112222993));
#118260=CARTESIAN_POINT('Ctrl Pts',(-9.78216200544157,6.28692102306534,
9.84256499064077));
#118261=CARTESIAN_POINT('Ctrl Pts',(-9.78585736253136,6.28717520113481,
9.84187560056085));
#118262=CARTESIAN_POINT('Ctrl Pts',(-9.79576210200434,6.28785331693078,
9.84007684340012));
#118263=CARTESIAN_POINT('Ctrl Pts',(-9.80197730639773,6.2882755110681,9.83899962731526));
#118264=CARTESIAN_POINT('Ctrl Pts',(-9.80918359072738,6.28876150219062,
9.83781019098842));
#118265=CARTESIAN_POINT('Ctrl Pts',(-9.81016634717706,6.28882770338877,
9.83764926186054));
#118266=CARTESIAN_POINT('Ctrl Pts',(-9.81114930150925,6.28889384320256,
9.83748958018452));
#118267=CARTESIAN_POINT('Origin',(-10.,2.67563288526385,11.));
#118268=CARTESIAN_POINT('',(-9.81114930150157,6.88692359881868,9.83748958018577));
#118269=CARTESIAN_POINT('',(-9.81114930155385,6.78711399980274,9.83748958017728));
#118270=CARTESIAN_POINT('',(-9.81114930150157,2.67563288526385,9.83748958018577));
#118271=CARTESIAN_POINT('Ctrl Pts',(-9.81114930150157,6.88692359881869,
9.83748958018577));
#118272=CARTESIAN_POINT('Ctrl Pts',(-9.76179042850999,6.88380575833335,
9.84550796650101));
#118273=CARTESIAN_POINT('Ctrl Pts',(-9.7129624323272,6.8806441789585,9.85666654922391));
#118274=CARTESIAN_POINT('Ctrl Pts',(-9.64974224407113,6.87635091260822,
9.87542603022264));
#118275=CARTESIAN_POINT('Ctrl Pts',(-9.63461569572728,6.87530842991322,
9.88024941152047));
#118276=CARTESIAN_POINT('Ctrl Pts',(-9.61231325242055,6.87374635546162,
9.88786098144651));
#118277=CARTESIAN_POINT('Ctrl Pts',(-9.60505933493838,6.87323430605266,
9.89041625947696));
#118278=CARTESIAN_POINT('Ctrl Pts',(-9.59214058766744,6.87231498885222,
9.89510977083978));
#118279=CARTESIAN_POINT('Ctrl Pts',(-9.5864661895756,6.87190861854475,9.89722100853172));
#118280=CARTESIAN_POINT('Ctrl Pts',(-9.57446415273821,6.87104350070152,
9.90179219024364));
#118281=CARTESIAN_POINT('Ctrl Pts',(-9.56814102279633,6.87058439699561,
9.90426327468967));
#118282=CARTESIAN_POINT('Ctrl Pts',(-9.5511931304261,6.86934469582523,9.91105600927023));
#118283=CARTESIAN_POINT('Ctrl Pts',(-9.54060978228383,6.86856077964798,
9.91547833914255));
#118284=CARTESIAN_POINT('Ctrl Pts',(-9.4832417468298,6.86425654377663,9.94044037423251));
#118285=CARTESIAN_POINT('Ctrl Pts',(-9.43777328038918,6.86064042014211,
9.96385063048835));
#118286=CARTESIAN_POINT('Ctrl Pts',(-9.3345596547659,6.85194779297395,10.0257898499238));
#118287=CARTESIAN_POINT('Ctrl Pts',(-9.27841011587521,6.84682189398038,
10.0666172370726));
#118288=CARTESIAN_POINT('Ctrl Pts',(-9.19493393992593,6.83875158519271,
10.1393714025256));
#118289=CARTESIAN_POINT('Ctrl Pts',(-9.1651440962155,6.83576621817576,10.1682372235315));
#118290=CARTESIAN_POINT('Ctrl Pts',(-9.13233734381287,6.83240784216452,
10.2035690569654));
#118291=CARTESIAN_POINT('Ctrl Pts',(-9.12778158932141,6.83193979573026,
10.208560942762));
#118292=CARTESIAN_POINT('Ctrl Pts',(-9.12042836942682,6.83118197293282,
10.2167587174884));
#118293=CARTESIAN_POINT('Ctrl Pts',(-9.11760493578553,6.83089040770405,
10.2199409560735));
#118294=CARTESIAN_POINT('Ctrl Pts',(-9.11256570719197,6.83036908374168,
10.2256829465782));
#118295=CARTESIAN_POINT('Ctrl Pts',(-9.11034365390934,6.83013887950344,
10.2282370117834));
#118296=CARTESIAN_POINT('Ctrl Pts',(-9.10544625595514,6.8296307827573,10.2339154230651));
#118297=CARTESIAN_POINT('Ctrl Pts',(-9.10277624372192,6.82935327183675,
10.2370442264093));
#118298=CARTESIAN_POINT('Ctrl Pts',(-9.0949880147737,6.8285420897468,10.2462681421888));
#118299=CARTESIAN_POINT('Ctrl Pts',(-9.08991500411405,6.82801152468811,
10.2524013672887));
#118300=CARTESIAN_POINT('Ctrl Pts',(-9.07839110009297,6.82679993981414,
10.2666248246997));
#118301=CARTESIAN_POINT('Ctrl Pts',(-9.07198378166519,6.82612157327325,
10.2747496799778));
#118302=CARTESIAN_POINT('Ctrl Pts',(-9.050587773727,6.82383593427871,10.3026289894329));
#118303=CARTESIAN_POINT('Ctrl Pts',(-9.03611539849764,6.82225483822977,
10.3227729074299));
#118304=CARTESIAN_POINT('Ctrl Pts',(-8.99297176984956,6.8173772938791,10.3870120642228));
#118305=CARTESIAN_POINT('Ctrl Pts',(-8.96660976898363,6.81414729723689,
10.4325802684868));
#118306=CARTESIAN_POINT('Ctrl Pts',(-8.91168687598181,6.80644384007156,
10.5441297845966));
#118307=CARTESIAN_POINT('Ctrl Pts',(-8.88594577952553,6.80195556185637,
10.6112528618167));
#118308=CARTESIAN_POINT('Ctrl Pts',(-8.86316351407304,6.79645588799566,
10.6920284422795));
#118309=CARTESIAN_POINT('Ctrl Pts',(-8.86003677285234,6.79565161104774,
10.7038117172662));
#118310=CARTESIAN_POINT('Ctrl Pts',(-8.85539980489722,6.79437535476795,
10.7224487972974));
#118311=CARTESIAN_POINT('Ctrl Pts',(-8.85376690724421,6.79390727631051,
10.7292714085222));
#118312=CARTESIAN_POINT('Ctrl Pts',(-8.85084421183912,6.79303331594007,
10.7419837497076));
#118313=CARTESIAN_POINT('Ctrl Pts',(-8.84953849442978,6.79262795348139,
10.7478696115752));
#118314=CARTESIAN_POINT('Ctrl Pts',(-8.84673797962109,6.79172411118871,
10.7609685467832));
#118315=CARTESIAN_POINT('Ctrl Pts',(-8.84526555833112,6.79122494322128,
10.7681860913628));
#118316=CARTESIAN_POINT('Ctrl Pts',(-8.84114938812104,6.78975584280423,
10.7893758587363));
#118317=CARTESIAN_POINT('Ctrl Pts',(-8.83869094749129,6.78878017059658,
10.8033822911032));
#118318=CARTESIAN_POINT('Ctrl Pts',(-8.82536651925484,6.78283486572284,
10.8882981462983));
#118319=CARTESIAN_POINT('Ctrl Pts',(-8.82074613153098,6.7776727719978,10.9600225828784));
#118320=CARTESIAN_POINT('Ctrl Pts',(-8.82488830363903,6.76641594566124,
11.1138122572782));
#118321=CARTESIAN_POINT('Ctrl Pts',(-8.8356817974282,6.76032312666523,11.1954628546032));
#118322=CARTESIAN_POINT('Ctrl Pts',(-8.85711033871251,6.75390455613337,
11.2845854857307));
#118323=CARTESIAN_POINT('Ctrl Pts',(-8.85944790637781,6.75324301673536,
11.2938139082215));
#118324=CARTESIAN_POINT('Ctrl Pts',(-8.86302198055884,6.75228621149174,
11.3072379506916));
#118325=CARTESIAN_POINT('Ctrl Pts',(-8.86417029767902,6.75198633959229,
11.3114563595402));
#118326=CARTESIAN_POINT('Ctrl Pts',(-8.86625288273057,6.75145573934282,
11.318942132196));
#118327=CARTESIAN_POINT('Ctrl Pts',(-8.86717783475078,6.75122449892443,
11.3222119684327));
#118328=CARTESIAN_POINT('Ctrl Pts',(-8.86921277893933,6.75072520772989,
11.3292886974684));
#118329=CARTESIAN_POINT('Ctrl Pts',(-8.87032785275883,6.75045744828318,
11.3330940205084));
#118330=CARTESIAN_POINT('Ctrl Pts',(-8.8735368645652,6.74970290661337,11.3438436759775));
#118331=CARTESIAN_POINT('Ctrl Pts',(-8.8756758054223,6.74921860705328,11.3507745443964));
#118332=CARTESIAN_POINT('Ctrl Pts',(-8.89101712500389,6.745868036217,11.3989029284176));
#118333=CARTESIAN_POINT('Ctrl Pts',(-8.90641820536623,6.74311400244167,
11.439370363674));
#118334=CARTESIAN_POINT('Ctrl Pts',(-8.96157880909751,6.73461477932193,
11.5633038306765));
#118335=CARTESIAN_POINT('Ctrl Pts',(-9.00894260295148,6.72902795338409,
11.6429893197167));
#118336=CARTESIAN_POINT('Ctrl Pts',(-9.0830695657527,6.72124872695082,11.7397319874945));
#118337=CARTESIAN_POINT('Ctrl Pts',(-9.10187856883824,6.71934038468655,
11.7624581984725));
#118338=CARTESIAN_POINT('Ctrl Pts',(-9.12819410550953,6.71673831021565,
11.7919280066178));
#118339=CARTESIAN_POINT('Ctrl Pts',(-9.13496373456065,6.71607457323208,
11.7993170426254));
#118340=CARTESIAN_POINT('Ctrl Pts',(-9.14626195848161,6.71497542121608,
11.8113373883223));
#118341=CARTESIAN_POINT('Ctrl Pts',(-9.15073602384149,6.71454231276816,
11.8160194220677));
#118342=CARTESIAN_POINT('Ctrl Pts',(-9.15953609391194,6.71369443898523,
11.8250777834417));
#118343=CARTESIAN_POINT('Ctrl Pts',(-9.16385823894177,6.7132798476198,11.829457581262));
#118344=CARTESIAN_POINT('Ctrl Pts',(-9.17415364035798,6.71229646702617,
11.8397280693911));
#118345=CARTESIAN_POINT('Ctrl Pts',(-9.18015584080465,6.71172641938154,
11.8455891369838));
#118346=CARTESIAN_POINT('Ctrl Pts',(-9.20055381911394,6.70979962182896,
11.8650861421125));
#118347=CARTESIAN_POINT('Ctrl Pts',(-9.21523053033918,6.70843038631718,
11.8784218955218));
#118348=CARTESIAN_POINT('Ctrl Pts',(-9.31376777079229,6.6993419895866,11.9635151153038));
#118349=CARTESIAN_POINT('Ctrl Pts',(-9.40701564978442,6.69114924935245,
12.023541157303));
#118350=CARTESIAN_POINT('Ctrl Pts',(-9.54223638866296,6.68031865963084,
12.085833253133));
#118351=CARTESIAN_POINT('Ctrl Pts',(-9.57802714927119,6.67754861317366,
12.100236758403));
#118352=CARTESIAN_POINT('Ctrl Pts',(-9.6213369515905,6.67435719096461,12.115240903243));
#118353=CARTESIAN_POINT('Ctrl Pts',(-9.6282324977917,6.67385381597231,12.117558458173));
#118354=CARTESIAN_POINT('Ctrl Pts',(-9.6389659699121,6.67307808184156,12.1210555762556));
#118355=CARTESIAN_POINT('Ctrl Pts',(-9.64278905718063,6.67280330578054,
12.1222796084176));
#118356=CARTESIAN_POINT('Ctrl Pts',(-9.64985425857583,6.6722984191618,12.1245019026164));
#118357=CARTESIAN_POINT('Ctrl Pts',(-9.65309443876776,6.67206800729686,
12.1255057091432));
#118358=CARTESIAN_POINT('Ctrl Pts',(-9.66052484702463,6.67154218082568,
12.1277725101334));
#118359=CARTESIAN_POINT('Ctrl Pts',(-9.6647178196377,6.67124730103432,12.1290261623021));
#118360=CARTESIAN_POINT('Ctrl Pts',(-9.67783608168133,6.67033019621591,
12.1328688508746));
#118361=CARTESIAN_POINT('Ctrl Pts',(-9.68678534660256,6.66971242431087,
12.1353757165151));
#118362=CARTESIAN_POINT('Ctrl Pts',(-9.70798118605942,6.66826574547116,
12.1410433886532));
#118363=CARTESIAN_POINT('Ctrl Pts',(-9.72025104788914,6.66744117351677,
12.1441134357934));
#118364=CARTESIAN_POINT('Ctrl Pts',(-9.76545139601389,6.66444268131249,
12.1546523643158));
#118365=CARTESIAN_POINT('Ctrl Pts',(-9.79865124764172,6.66231568911361,
12.1609022946999));
#118366=CARTESIAN_POINT('Ctrl Pts',(-9.90806180388688,6.65542136814449,
12.1766631168506));
#118367=CARTESIAN_POINT('Ctrl Pts',(-9.98493354166135,6.6507460253511,12.1801532290513));
#118368=CARTESIAN_POINT('Ctrl Pts',(-10.0985151286715,6.64354566969613,
12.1742045969359));
#118369=CARTESIAN_POINT('Ctrl Pts',(-10.1353173729581,6.64116920144629,
12.1705342620274));
#118370=CARTESIAN_POINT('Ctrl Pts',(-10.1826064781939,6.63802694301749,
12.1635580858076));
#118371=CARTESIAN_POINT('Ctrl Pts',(-10.1933067058868,6.63731008068205,
12.161828321907));
#118372=CARTESIAN_POINT('Ctrl Pts',(-10.210532889724,6.63614583254991,12.1587990404762));
#118373=CARTESIAN_POINT('Ctrl Pts',(-10.2170745332368,6.63570132919074,
12.1575914468501));
#118374=CARTESIAN_POINT('Ctrl Pts',(-10.2295802899452,6.63484683790583,
12.1551731412115));
#118375=CARTESIAN_POINT('Ctrl Pts',(-10.2355459527948,6.63443714747739,
12.1539714890093));
#118376=CARTESIAN_POINT('Ctrl Pts',(-10.249280783566,6.63348900242105,12.1510939665381));
#118377=CARTESIAN_POINT('Ctrl Pts',(-10.2570427610736,6.63294953842154,
12.1493855934702));
#118378=CARTESIAN_POINT('Ctrl Pts',(-10.2816068545799,6.63123042579049,
12.1437178941811));
#118379=CARTESIAN_POINT('Ctrl Pts',(-10.2983388429721,6.63004168180246,
12.1394678241189));
#118380=CARTESIAN_POINT('Ctrl Pts',(-10.3375236542188,6.62721423210916,
12.1285923373315));
#118381=CARTESIAN_POINT('Ctrl Pts',(-10.3598836497916,6.6255665631354,12.121662388081));
#118382=CARTESIAN_POINT('Ctrl Pts',(-10.4577772599144,6.61820097037958,
12.0880941366478));
#118383=CARTESIAN_POINT('Ctrl Pts',(-10.530679998881,6.61228990679209,12.0544595481455));
#118384=CARTESIAN_POINT('Ctrl Pts',(-10.6414629784819,6.60287674189544,
11.9889319383886));
#118385=CARTESIAN_POINT('Ctrl Pts',(-10.6817603144619,6.5993536170655,11.9615950761432));
#118386=CARTESIAN_POINT('Ctrl Pts',(-10.7256744122961,6.59548644304517,
11.9276522110296));
#118387=CARTESIAN_POINT('Ctrl Pts',(-10.7310572330969,6.59501194937347,
11.9234161059442));
#118388=CARTESIAN_POINT('Ctrl Pts',(-10.7397443081093,6.59424582523743,
11.916456083266));
#118389=CARTESIAN_POINT('Ctrl Pts',(-10.7430711137178,6.59395234260584,
11.9137607538859));
#118390=CARTESIAN_POINT('Ctrl Pts',(-10.7490027680495,6.59342902100396,
11.9089011958108));
#118391=CARTESIAN_POINT('Ctrl Pts',(-10.7516130483494,6.5931987204336,11.9067438208934));
#118392=CARTESIAN_POINT('Ctrl Pts',(-10.7573548594867,6.59269211430589,
11.9019564298167));
#118393=CARTESIAN_POINT('Ctrl Pts',(-10.7604820230539,6.59241617607557,
11.8993213432081));
#118394=CARTESIAN_POINT('Ctrl Pts',(-10.7695668428105,6.59161424881051,
11.8915847987638));
#118395=CARTESIAN_POINT('Ctrl Pts',(-10.7754874800048,6.59109125950153,
11.8864399333479));
#118396=CARTESIAN_POINT('Ctrl Pts',(-10.7889537788866,6.58989968459779,
11.8744999102825));
#118397=CARTESIAN_POINT('Ctrl Pts',(-10.7964639393049,6.58923362999945,
11.8676654694838));
#118398=CARTESIAN_POINT('Ctrl Pts',(-10.8839716782026,6.58144145673279,
11.7859374081227));
#118399=CARTESIAN_POINT('Ctrl Pts',(-10.9532364529416,6.57491599384366,
11.700321474848));
#118400=CARTESIAN_POINT('Ctrl Pts',(-11.031285485609,6.56536422591013,11.5703579361543));
#118401=CARTESIAN_POINT('Ctrl Pts',(-11.0509594657076,6.56267631391967,
11.5332368592667));
#118402=CARTESIAN_POINT('Ctrl Pts',(-11.0733468547502,6.55917913160202,
11.4849212523699));
#118403=CARTESIAN_POINT('Ctrl Pts',(-11.0779380929265,6.55843424845893,
11.4746277963509));
#118404=CARTESIAN_POINT('Ctrl Pts',(-11.0850399464836,6.55723558973298,
11.4580708263394));
#118405=CARTESIAN_POINT('Ctrl Pts',(-11.0876457619713,6.55678502015619,
11.4518487143755));
#118406=CARTESIAN_POINT('Ctrl Pts',(-11.0924917646039,6.55592608960512,
11.4399926849028));
#118407=CARTESIAN_POINT('Ctrl Pts',(-11.0947421871476,6.55551808629213,
11.4343631658178));
#118408=CARTESIAN_POINT('Ctrl Pts',(-11.0997758331871,6.5545841375757,11.421483671792));
#118409=CARTESIAN_POINT('Ctrl Pts',(-11.1025309899034,6.55405728367611,
11.4142231043229));
#118410=CARTESIAN_POINT('Ctrl Pts',(-11.1108366607301,6.5524190081942,11.3916653922981));
#118411=CARTESIAN_POINT('Ctrl Pts',(-11.1161418866876,6.55129966122063,
11.3762806257664));
#118412=CARTESIAN_POINT('Ctrl Pts',(-11.1277621006485,6.54866656244746,
11.3401718808432));
#118413=CARTESIAN_POINT('Ctrl Pts',(-11.1338272455177,6.54714543593486,
11.3193742940431));
#118414=CARTESIAN_POINT('Ctrl Pts',(-11.1542244518601,6.54143304830739,
11.2415019630706));
#118415=CARTESIAN_POINT('Ctrl Pts',(-11.1648456206274,6.53714329020795,
11.1835500173462));
#118416=CARTESIAN_POINT('Ctrl Pts',(-11.1783873291903,6.52778684236313,
11.0567355453575));
#118417=CARTESIAN_POINT('Ctrl Pts',(-11.1796910592591,6.52272683389703,
10.9879042701646));
#118418=CARTESIAN_POINT('Ctrl Pts',(-11.1742798673433,6.51718196869544,
10.9090718243968));
#118419=CARTESIAN_POINT('Ctrl Pts',(-11.1734397746921,6.5164649841199,10.8988058644734));
#118420=CARTESIAN_POINT('Ctrl Pts',(-11.1720699095102,6.51546684018339,
10.8843945108316));
#118421=CARTESIAN_POINT('Ctrl Pts',(-11.1716526217668,6.51518002206189,
10.8802392504279));
#118422=CARTESIAN_POINT('Ctrl Pts',(-11.1708515595871,6.51465928753007,
10.8726677388568));
#118423=CARTESIAN_POINT('Ctrl Pts',(-11.1704749132637,6.51442498922441,
10.8692507822105));
#118424=CARTESIAN_POINT('Ctrl Pts',(-11.1696612221101,6.51393991739212,
10.8621543752526));
#118425=CARTESIAN_POINT('Ctrl Pts',(-11.1692217684653,6.51368927710423,
10.8584752746962));
#118426=CARTESIAN_POINT('Ctrl Pts',(-11.1680177751548,6.5130311350681,10.848784033788));
#118427=CARTESIAN_POINT('Ctrl Pts',(-11.1672241679208,6.51262520103223,
10.8427755196371));
#118428=CARTESIAN_POINT('Ctrl Pts',(-11.1633164929477,6.51074740421205,
10.8148520936329));
#118429=CARTESIAN_POINT('Ctrl Pts',(-11.159631178728,6.50930420512535,10.7930200736271));
#118430=CARTESIAN_POINT('Ctrl Pts',(-11.1467961777879,6.50505804700152,
10.7281800828165));
#118431=CARTESIAN_POINT('Ctrl Pts',(-11.1358516230769,6.5023197365674,10.6855652547127));
#118432=CARTESIAN_POINT('Ctrl Pts',(-11.0947249586194,6.49389633131512,
10.5560074590836));
#118433=CARTESIAN_POINT('Ctrl Pts',(-11.0567345797142,6.48826107279846,
10.4719260396827));
#118434=CARTESIAN_POINT('Ctrl Pts',(-11.0016044054063,6.48128782741805,
10.3802340526167));
#118435=CARTESIAN_POINT('Ctrl Pts',(-10.9936095226019,6.4802996421887,10.367496009589));
#118436=CARTESIAN_POINT('Ctrl Pts',(-10.9811943762407,6.47879683705197,
10.3485317606691));
#118437=CARTESIAN_POINT('Ctrl Pts',(-10.9769536876819,6.47828878401259,
10.3421894205994));
#118438=CARTESIAN_POINT('Ctrl Pts',(-10.9692412522094,6.47737385615558,
10.3308938506353));
#118439=CARTESIAN_POINT('Ctrl Pts',(-10.9657923733862,6.47696784485768,
10.3259252761871));
#118440=CARTESIAN_POINT('Ctrl Pts',(-10.9621551520774,6.47654282839967,
10.3207705882591));
#118441=CARTESIAN_POINT('Ctrl Pts',(-10.9620048021144,6.47652526529023,
10.3205576616433));
#118442=CARTESIAN_POINT('Ctrl Pts',(-10.9617341699507,6.47649366145813,
10.3201746604881));
#118443=CARTESIAN_POINT('Ctrl Pts',(-10.9616139132548,6.4764796217014,10.3200045678625));
#118444=CARTESIAN_POINT('Ctrl Pts',(-10.961397585805,6.47645437224409,10.3196987636674));
#118445=CARTESIAN_POINT('Ctrl Pts',(-10.9613015314006,6.4764431631628,10.319563040485));
#118446=CARTESIAN_POINT('Ctrl Pts',(-10.9611288225856,6.47642301295004,
10.319319115533));
#118447=CARTESIAN_POINT('Ctrl Pts',(-10.9610521786254,6.47641407221492,
10.3192109063426));
#118448=CARTESIAN_POINT('Ctrl Pts',(-10.960914419698,6.47639800482786,10.3190164820757));
#118449=CARTESIAN_POINT('Ctrl Pts',(-10.9608533113843,6.47639087842781,
10.3189302622565));
#118450=CARTESIAN_POINT('Ctrl Pts',(-10.9567595664819,6.47591353043197,
10.313155904505));
#118451=CARTESIAN_POINT('Ctrl Pts',(-10.9526765848592,6.47544140561772,
10.3075037901762));
#118452=CARTESIAN_POINT('Ctrl Pts',(-10.9441014310368,6.4744578185113,10.2958524897032));
#118453=CARTESIAN_POINT('Ctrl Pts',(-10.9396017112942,6.47394608042074,
10.2898592759349));
#118454=CARTESIAN_POINT('Ctrl Pts',(-10.9279345186782,6.47263011900641,
10.2746246752531));
#118455=CARTESIAN_POINT('Ctrl Pts',(-10.9206861767294,6.47182280728793,
10.2654465439755));
#118456=CARTESIAN_POINT('Ctrl Pts',(-10.899010914347,6.46943762440835,10.2388253882844));
#118457=CARTESIAN_POINT('Ctrl Pts',(-10.8842170660407,6.46784588929161,
10.2216893432562));
#118458=CARTESIAN_POINT('Ctrl Pts',(-10.8259012126992,6.46170513764661,
10.1579505000429));
#118459=CARTESIAN_POINT('Ctrl Pts',(-10.7791183195288,6.45704047028252,
10.1144870315301));
#118460=CARTESIAN_POINT('Ctrl Pts',(-10.6806149535299,6.44783599438381,
10.0368476926493));
#118461=CARTESIAN_POINT('Ctrl Pts',(-10.629246720199,6.44331249685648,10.0025286438084));
#118462=CARTESIAN_POINT('Ctrl Pts',(-10.5670520870114,6.43830829164045,
9.96770206869916));
#118463=CARTESIAN_POINT('Ctrl Pts',(-10.5586247063069,6.43763978817619,
9.96311739323915));
#118464=CARTESIAN_POINT('Ctrl Pts',(-10.5456798268929,6.43662847756751,
9.95627874596362));
#118465=CARTESIAN_POINT('Ctrl Pts',(-10.5412025203919,6.43628149125897,
9.9539501140723));
#118466=CARTESIAN_POINT('Ctrl Pts',(-10.5336351595802,6.4356999025399,9.95007594852423));
#118467=CARTESIAN_POINT('Ctrl Pts',(-10.530553054412,6.43546437968896,9.94851511896717));
#118468=CARTESIAN_POINT('Ctrl Pts',(-10.5241794531227,6.43498017951108,
9.94532258068705));
#118469=CARTESIAN_POINT('Ctrl Pts',(-10.5208871266898,6.43473161128179,
9.94369267726372));
#118470=CARTESIAN_POINT('Ctrl Pts',(-10.5122719052983,6.43408506184391,
9.93947768899875));
#118471=CARTESIAN_POINT('Ctrl Pts',(-10.5069369788951,6.43368854995923,
9.93691722798775));
#118472=CARTESIAN_POINT('Ctrl Pts',(-10.4829410806476,6.43192131550433,
9.92562227941228));
#118473=CARTESIAN_POINT('Ctrl Pts',(-10.4640708914842,6.43057530843563,
9.91733758482847));
#118474=CARTESIAN_POINT('Ctrl Pts',(-10.4088184902817,6.42673207738054,
9.89479010534935));
#118475=CARTESIAN_POINT('Ctrl Pts',(-10.3719303602719,6.42428596659195,
9.8818364482973));
#118476=CARTESIAN_POINT('Ctrl Pts',(-10.2760182156491,6.4180720185036,9.85342920792167));
#118477=CARTESIAN_POINT('Ctrl Pts',(-10.2163181946885,6.41433691856388,
9.84068256519486));
#118478=CARTESIAN_POINT('Ctrl Pts',(-10.1134751395846,6.40781166946424,
9.82694822893905));
#118479=CARTESIAN_POINT('Ctrl Pts',(-10.0707767319115,6.40507765948761,
9.82359993246088));
#118480=CARTESIAN_POINT('Ctrl Pts',(-10.0159877731083,6.40148502921441,
9.82229728578206));
#118481=CARTESIAN_POINT('Ctrl Pts',(-10.0039783204683,6.40069248273311,
9.82219549683343));
#118482=CARTESIAN_POINT('Ctrl Pts',(-9.98499530024241,6.39943074911249,
9.82232493155173));
#118483=CARTESIAN_POINT('Ctrl Pts',(-9.97802152927992,6.39896531426812,
9.82243443869749));
#118484=CARTESIAN_POINT('Ctrl Pts',(-9.96503141139489,6.39809459135314,
9.82275385038394));
#118485=CARTESIAN_POINT('Ctrl Pts',(-9.95901487699916,6.39768980472283,
9.82294795511619));
#118486=CARTESIAN_POINT('Ctrl Pts',(-9.94721752970901,6.39689303775286,
9.82341912057908));
#118487=CARTESIAN_POINT('Ctrl Pts',(-9.94143674205579,6.39650117696969,
9.82369268567168));
#118488=CARTESIAN_POINT('Ctrl Pts',(-9.92841544259355,6.3956151669874,9.82440511673336));
#118489=CARTESIAN_POINT('Ctrl Pts',(-9.92117655154485,6.39512028112661,
9.82486828895023));
#118490=CARTESIAN_POINT('Ctrl Pts',(-9.90045467898295,6.39369676742912,
9.82638648165186));
#118491=CARTESIAN_POINT('Ctrl Pts',(-9.88698534657606,6.39276312490249,
9.82760688191719));
#118492=CARTESIAN_POINT('Ctrl Pts',(-9.85267089459624,6.3903625670311,9.8313127805553));
#118493=CARTESIAN_POINT('Ctrl Pts',(-9.8318664609301,6.38888625823141,9.83412406193983));
#118494=CARTESIAN_POINT('Ctrl Pts',(-9.81114930150153,6.38739526456853,
9.83748958018578));
#118495=CARTESIAN_POINT('Ctrl Pts',(-9.81114930150925,6.28889384320256,
9.83748958018452));
#118496=CARTESIAN_POINT('Ctrl Pts',(-9.83217396752733,6.29030852489224,
9.83407410726026));
#118497=CARTESIAN_POINT('Ctrl Pts',(-9.85328916382042,6.29169514151888,
9.83122934520844));
#118498=CARTESIAN_POINT('Ctrl Pts',(-9.89617828576813,6.29446374418358,
9.82663189519018));
#118499=CARTESIAN_POINT('Ctrl Pts',(-9.91794655001183,6.29584420572935,
9.82490894845336));
#118500=CARTESIAN_POINT('Ctrl Pts',(-9.96063918496295,6.29852432224818,
9.82272210337179));
#118501=CARTESIAN_POINT('Ctrl Pts',(-9.98155255812689,6.29982444267296,
9.82220874040484));
#118502=CARTESIAN_POINT('Ctrl Pts',(-10.0524501001525,6.30421865218534,
9.82235736437935));
#118503=CARTESIAN_POINT('Ctrl Pts',(-10.102372720044,6.3072926477863,9.82564363432128));
#118504=CARTESIAN_POINT('Ctrl Pts',(-10.2006291928598,6.3135028030339,9.83842596070636));
#118505=CARTESIAN_POINT('Ctrl Pts',(-10.2488742064699,6.31663088569745,
9.8477990283414));
#118506=CARTESIAN_POINT('Ctrl Pts',(-10.3073797526552,6.32060025391447,
9.86301200751928));
#118507=CARTESIAN_POINT('Ctrl Pts',(-10.3183274550742,6.32135062903676,
9.86602838480624));
#118508=CARTESIAN_POINT('Ctrl Pts',(-10.3357227821993,6.32255595410178,
9.87109300102004));
#118509=CARTESIAN_POINT('Ctrl Pts',(-10.3421995154701,6.32300763235351,
9.87303935861515));
#118510=CARTESIAN_POINT('Ctrl Pts',(-10.3544446705997,6.32386728313721,
9.87683450587686));
#118511=CARTESIAN_POINT('Ctrl Pts',(-10.3602163124535,6.32427488629912,
9.87867223453655));
#118512=CARTESIAN_POINT('Ctrl Pts',(-10.3733205341226,6.325205964905,9.88295631662731));
#118513=CARTESIAN_POINT('Ctrl Pts',(-10.3806436572598,6.32573032970159,
9.88543048084908));
#118514=CARTESIAN_POINT('Ctrl Pts',(-10.4031323625625,6.32735340456808,
9.8932759154381));
#118515=CARTESIAN_POINT('Ctrl Pts',(-10.4182121084477,6.32845983122719,
9.89888579649363));
#118516=CARTESIAN_POINT('Ctrl Pts',(-10.5027427225827,6.33476789642603,
9.93231927577882));
#118517=CARTESIAN_POINT('Ctrl Pts',(-10.5695219883126,6.34017597535457,
9.96639777855707));
#118518=CARTESIAN_POINT('Ctrl Pts',(-10.6729950598149,6.34916657788513,
10.0322886833606));
#118519=CARTESIAN_POINT('Ctrl Pts',(-10.7117765736319,6.35269340505642,
10.0604459187035));
#118520=CARTESIAN_POINT('Ctrl Pts',(-10.7739054899705,6.35851980659507,
10.1116146854433));
#118521=CARTESIAN_POINT('Ctrl Pts',(-10.798204808411,6.3608489191406,10.133381467443));
#118522=CARTESIAN_POINT('Ctrl Pts',(-10.8264410490351,6.36358818697766,
10.1608716172262));
#118523=CARTESIAN_POINT('Ctrl Pts',(-10.8312695829954,6.36405782680935,
10.1656546661223));
#118524=CARTESIAN_POINT('Ctrl Pts',(-10.8387795772585,6.36478980571842,
10.1732238332109));
#118525=CARTESIAN_POINT('Ctrl Pts',(-10.8414890907739,6.36505421310971,
10.1759817232688));
#118526=CARTESIAN_POINT('Ctrl Pts',(-10.8465670431253,6.36555026022516,
10.1812015062211));
#118527=CARTESIAN_POINT('Ctrl Pts',(-10.8489383433094,6.36578210809694,
10.1836603516253));
#118528=CARTESIAN_POINT('Ctrl Pts',(-10.854427909427,6.36631937956946,10.1894023739248));
#118529=CARTESIAN_POINT('Ctrl Pts',(-10.8575379832642,6.36662418651468,
10.1926932598141));
#118530=CARTESIAN_POINT('Ctrl Pts',(-10.8677259934319,6.3676243999898,10.2035988819598));
#118531=CARTESIAN_POINT('Ctrl Pts',(-10.8747223244253,6.36831404309873,
10.2112896515093));
#118532=CARTESIAN_POINT('Ctrl Pts',(-10.9275832057929,6.37355557130202,
10.2709661276993));
#118533=CARTESIAN_POINT('Ctrl Pts',(-10.9688851040908,6.37783792873874,
10.3268245004164));
#118534=CARTESIAN_POINT('Ctrl Pts',(-11.0354983911175,6.38574235523404,
10.4358614179606));
#118535=CARTESIAN_POINT('Ctrl Pts',(-11.0622057174546,6.38935136529559,
10.4879183076003));
#118536=CARTESIAN_POINT('Ctrl Pts',(-11.0933340670707,6.39444393097727,
10.5616152592759));
#118537=CARTESIAN_POINT('Ctrl Pts',(-11.101180893692,6.39583073523075,10.5817164608792));
#118538=CARTESIAN_POINT('Ctrl Pts',(-11.1139528173571,6.39828998263429,
10.6172894549519));
#118539=CARTESIAN_POINT('Ctrl Pts',(-11.1191184439728,6.39935478400995,
10.6326689401085));
#118540=CARTESIAN_POINT('Ctrl Pts',(-11.1262813850154,6.40094375495417,
10.6555505188657));
#118541=CARTESIAN_POINT('Ctrl Pts',(-11.1285249876063,6.40145998777256,
10.6629739611946));
#118542=CARTESIAN_POINT('Ctrl Pts',(-11.1323908979861,6.40238383991421,
10.6762367528507));
#118543=CARTESIAN_POINT('Ctrl Pts',(-11.1340417690815,6.40279052546244,
10.6820675391139));
#118544=CARTESIAN_POINT('Ctrl Pts',(-11.13743582127,6.40365318382968,10.6944180016443));
#118545=CARTESIAN_POINT('Ctrl Pts',(-11.1391681039494,6.40410948881517,
10.7009404191445));
#118546=CARTESIAN_POINT('Ctrl Pts',(-11.1436481533967,6.40533395956629,
10.7184126958472));
#118547=CARTESIAN_POINT('Ctrl Pts',(-11.1462946371025,6.40610530556393,
10.7293875497957));
#118548=CARTESIAN_POINT('Ctrl Pts',(-11.158108550393,6.40979124284393,10.7816662056745));
#118549=CARTESIAN_POINT('Ctrl Pts',(-11.1652026957464,6.41276975924071,
10.8234016250495));
#118550=CARTESIAN_POINT('Ctrl Pts',(-11.1825361006483,6.42364956251278,
10.974102466896));
#118551=CARTESIAN_POINT('Ctrl Pts',(-11.1798333680014,6.43187006434389,
11.0839791656808));
#118552=CARTESIAN_POINT('Ctrl Pts',(-11.1603686901995,6.44032657929434,
11.2018444576054));
#118553=CARTESIAN_POINT('Ctrl Pts',(-11.1585984920666,6.44103526499194,
11.2117692887905));
#118554=CARTESIAN_POINT('Ctrl Pts',(-11.1552331384942,6.44228179030265,
11.2293300709823));
#118555=CARTESIAN_POINT('Ctrl Pts',(-11.153689167492,6.44282195479856,11.2369751013588));
#118556=CARTESIAN_POINT('Ctrl Pts',(-11.1512220756028,6.4436385708266,11.2485949247318));
#118557=CARTESIAN_POINT('Ctrl Pts',(-11.1503540915028,6.44391791434338,
11.252581015481));
#118558=CARTESIAN_POINT('Ctrl Pts',(-11.1487278000906,6.44442698106938,
11.2598672129701));
#118559=CARTESIAN_POINT('Ctrl Pts',(-11.1479759674725,6.44465704604658,
11.2631685881364));
#118560=CARTESIAN_POINT('Ctrl Pts',(-11.1462391511918,6.44517681391507,
11.2706460401156));
#118561=CARTESIAN_POINT('Ctrl Pts',(-11.1452455770436,6.44546603089243,
11.2748200146712));
#118562=CARTESIAN_POINT('Ctrl Pts',(-11.1425990859452,6.44621594308083,
11.2856741963277));
#118563=CARTESIAN_POINT('Ctrl Pts',(-11.1409103644785,6.44667471364137,
11.2923456231267));
#118564=CARTESIAN_POINT('Ctrl Pts',(-11.1259577532096,6.45057671105032,
11.349313340769));
#118565=CARTESIAN_POINT('Ctrl Pts',(-11.109431945306,6.45385723645849,11.3987014531337));
#118566=CARTESIAN_POINT('Ctrl Pts',(-11.0854280758571,6.45779638413193,
11.4572387343791));
#118567=CARTESIAN_POINT('Ctrl Pts',(-11.081015482048,6.45849391788365,11.4675755556586));
#118568=CARTESIAN_POINT('Ctrl Pts',(-11.0557855815724,6.46234744014686,
11.5244113753327));
#118569=CARTESIAN_POINT('Ctrl Pts',(-11.0321166870885,6.4654808309648,11.5695835854562));
#118570=CARTESIAN_POINT('Ctrl Pts',(-10.9807448891762,6.47167249639648,
11.6538455159632));
#118571=CARTESIAN_POINT('Ctrl Pts',(-10.9534389330596,6.47471717707662,
11.6930569124288));
#118572=CARTESIAN_POINT('Ctrl Pts',(-10.9168388029762,6.47859250628929,
11.7393434710986));
#118573=CARTESIAN_POINT('Ctrl Pts',(-10.9097198733394,6.47933758263407,
11.7480854874865));
#118574=CARTESIAN_POINT('Ctrl Pts',(-10.8981428532842,6.48053639877852,
11.7618923644829));
#118575=CARTESIAN_POINT('Ctrl Pts',(-10.893764719189,6.48098692967035,11.76702358732));
#118576=CARTESIAN_POINT('Ctrl Pts',(-10.8853695264092,6.48184568587702,
11.7766933732516));
#118577=CARTESIAN_POINT('Ctrl Pts',(-10.8813610250861,6.48225355288609,
11.7812391026142));
#118578=CARTESIAN_POINT('Ctrl Pts',(-10.8721397774403,6.48318704586131,
11.7915349045038));
#118579=CARTESIAN_POINT('Ctrl Pts',(-10.8669049655136,6.48371357844924,
11.7972647441227));
#118580=CARTESIAN_POINT('Ctrl Pts',(-10.8505321523428,6.48535028959538,
11.8148339331578));
#118581=CARTESIAN_POINT('Ctrl Pts',(-10.8392058027676,6.4864683737595,11.8264943168244));
#118582=CARTESIAN_POINT('Ctrl Pts',(-10.777077899462,6.4925299012312,11.8878604587627));
#118583=CARTESIAN_POINT('Ctrl Pts',(-10.7221048432263,6.49765733572671,
11.9331172455703));
#118584=CARTESIAN_POINT('Ctrl Pts',(-10.6148703370555,6.50716076011914,
12.0062201081526));
#118585=CARTESIAN_POINT('Ctrl Pts',(-10.5639346196445,6.51149630259752,
12.0356266774468));
#118586=CARTESIAN_POINT('Ctrl Pts',(-10.4952995125897,6.51697469563982,
12.0686803852398));
#118587=CARTESIAN_POINT('Ctrl Pts',(-10.4794155378241,6.51821831385074,
12.0758997074673));
#118588=CARTESIAN_POINT('Ctrl Pts',(-10.4524915447586,6.52027960564922,
12.0874220152448));
#118589=CARTESIAN_POINT('Ctrl Pts',(-10.4415367161865,6.52110560947637,
12.09191601888));
#118590=CARTESIAN_POINT('Ctrl Pts',(-10.4260295246585,6.52225531395607,
12.0980059808534));
#118591=CARTESIAN_POINT('Ctrl Pts',(-10.4215327062809,6.52258641956077,
12.099740182698));
#118592=CARTESIAN_POINT('Ctrl Pts',(-10.4138007681067,6.52315166112207,
12.102667617511));
#118593=CARTESIAN_POINT('Ctrl Pts',(-10.410570853343,6.52338656965778,12.1038743252981));
#118594=CARTESIAN_POINT('Ctrl Pts',(-10.4038022880098,6.5238762533397,12.1063692670518));
#118595=CARTESIAN_POINT('Ctrl Pts',(-10.4002627091289,6.52413086939655,
12.1076547330098));
#118596=CARTESIAN_POINT('Ctrl Pts',(-10.3907495202915,6.52481143338115,
12.111058073576));
#118597=CARTESIAN_POINT('Ctrl Pts',(-10.3847647776579,6.52523561574829,
12.1131447797846));
#118598=CARTESIAN_POINT('Ctrl Pts',(-10.3573243603021,6.52716372399278,
12.1224647051404));
#118599=CARTESIAN_POINT('Ctrl Pts',(-10.3356781923197,6.52863797809679,
12.1291271066355));
#118600=CARTESIAN_POINT('Ctrl Pts',(-10.2928662884244,6.53148740729562,
12.1409638269983));
#118601=CARTESIAN_POINT('Ctrl Pts',(-10.2717229373381,6.53286364770264,
12.1461831666583));
#118602=CARTESIAN_POINT('Ctrl Pts',(-10.1835314371377,6.53852065877968,
12.165375865962));
#118603=CARTESIAN_POINT('Ctrl Pts',(-10.1154737109269,6.54269578734149,
12.1740744920734));
#118604=CARTESIAN_POINT('Ctrl Pts',(-9.99608463157067,6.55017420278105,
12.1788472333208));
#118605=CARTESIAN_POINT('Ctrl Pts',(-9.94505199112209,6.55341817142289,
12.1775720315404));
#118606=CARTESIAN_POINT('Ctrl Pts',(-9.88285008625814,6.55751812484059,
12.1719651685598));
#118607=CARTESIAN_POINT('Ctrl Pts',(-9.87144953293953,6.55827546716636,
12.1707694994951));
#118608=CARTESIAN_POINT('Ctrl Pts',(-9.85333053289396,6.55948935077882,
12.1686013781829));
#118609=CARTESIAN_POINT('Ctrl Pts',(-9.8465997156234,6.55994253705385,12.1677368980973));
#118610=CARTESIAN_POINT('Ctrl Pts',(-9.83388019347696,6.56080338665888,
12.1659913848843));
#118611=CARTESIAN_POINT('Ctrl Pts',(-9.82789005624522,6.56121066620264,
12.1651222530967));
#118612=CARTESIAN_POINT('Ctrl Pts',(-9.81430545551029,6.56213868460753,
12.1630441668263));
#118613=CARTESIAN_POINT('Ctrl Pts',(-9.80671566338288,6.56266029086538,
12.1618069367191));
#118614=CARTESIAN_POINT('Ctrl Pts',(-9.78349302348635,6.56426611662105,
12.1577875070688));
#118615=CARTESIAN_POINT('Ctrl Pts',(-9.76790442400641,6.56535781693441,
12.1547635184029));
#118616=CARTESIAN_POINT('Ctrl Pts',(-9.6716195683883,6.57218973020986,12.134057158988));
#118617=CARTESIAN_POINT('Ctrl Pts',(-9.59292224727309,6.5781873523608,12.1082429432195));
#118618=CARTESIAN_POINT('Ctrl Pts',(-9.45440275226747,6.58932858620843,
12.0460476673394));
#118619=CARTESIAN_POINT('Ctrl Pts',(-9.39383852667254,6.59442557723975,
12.0121572030866));
#118620=CARTESIAN_POINT('Ctrl Pts',(-9.32908415561941,6.59990767598515,
11.9680132882963));
#118621=CARTESIAN_POINT('Ctrl Pts',(-9.32162788354656,6.60053930203682,
11.962802721637));
#118622=CARTESIAN_POINT('Ctrl Pts',(-9.31070566703958,6.60146422996624,
11.9549802109705));
#118623=CARTESIAN_POINT('Ctrl Pts',(-9.30719279671884,6.60176166400383,
11.9524348068935));
#118624=CARTESIAN_POINT('Ctrl Pts',(-9.3009610903509,6.60228910188104,11.9478666296448));
#118625=CARTESIAN_POINT('Ctrl Pts',(-9.29823683661112,6.60251960076676,
11.9458514726241));
#118626=CARTESIAN_POINT('Ctrl Pts',(-9.29228283922467,6.60302319188202,
11.9414073573419));
#118627=CARTESIAN_POINT('Ctrl Pts',(-9.2890568732937,6.60329594544645,11.9389735160922));
#118628=CARTESIAN_POINT('Ctrl Pts',(-9.27996082033554,6.60406493081268,
11.9320372151194));
#118629=CARTESIAN_POINT('Ctrl Pts',(-9.27412041406071,6.60455858617302,
11.9274958890501));
#118630=CARTESIAN_POINT('Ctrl Pts',(-9.23431913559704,6.60792510773057,
11.8959413440579));
#118631=CARTESIAN_POINT('Ctrl Pts',(-9.20182695212705,6.61068579222854,
11.8671209595094));
#118632=CARTESIAN_POINT('Ctrl Pts',(-9.15702365623844,6.61463605337505,
11.8227228665574));
#118633=CARTESIAN_POINT('Ctrl Pts',(-9.14339955577342,6.61585857508875,
11.8085281331262));
#118634=CARTESIAN_POINT('Ctrl Pts',(-9.09690669654099,6.62013275218794,
11.7575930127024));
#118635=CARTESIAN_POINT('Ctrl Pts',(-9.06599522280667,6.62316471111318,
11.7191381151035));
#118636=CARTESIAN_POINT('Ctrl Pts',(-9.00898528464385,6.62936134108222,
11.6383154973168));
#118637=CARTESIAN_POINT('Ctrl Pts',(-8.98298004644003,6.63252073355408,
11.5960086909625));
#118638=CARTESIAN_POINT('Ctrl Pts',(-8.95438357439872,6.63652539132615,
11.5421355674871));
#118639=CARTESIAN_POINT('Ctrl Pts',(-8.94919189064131,6.63727769351883,
11.5320028059577));
#118640=CARTESIAN_POINT('Ctrl Pts',(-8.94114895842337,6.63848538580078,
11.5157279879783));
#118641=CARTESIAN_POINT('Ctrl Pts',(-8.93820228517077,6.63893748124079,
11.5096336874575));
#118642=CARTESIAN_POINT('Ctrl Pts',(-8.93271931447399,6.63979746110695,
11.498039832924));
#118643=CARTESIAN_POINT('Ctrl Pts',(-8.93017257208598,6.64020497216094,
11.4925454385248));
#118644=CARTESIAN_POINT('Ctrl Pts',(-8.92447650368585,6.64113519158471,
11.4800040085575));
#118645=CARTESIAN_POINT('Ctrl Pts',(-8.92135388123496,6.64165878315078,
11.4729452240182));
#118646=CARTESIAN_POINT('Ctrl Pts',(-8.91196054369535,6.64327701144146,
11.4511342872184));
#118647=CARTESIAN_POINT('Ctrl Pts',(-8.90592165865342,6.64437929813376,
11.4362849330254));
#118648=CARTESIAN_POINT('Ctrl Pts',(-8.87222635461074,6.65091498288681,
11.3483263388159));
#118649=CARTESIAN_POINT('Ctrl Pts',(-8.85160518327261,6.65657587018532,
11.2727453069239));
#118650=CARTESIAN_POINT('Ctrl Pts',(-8.82642492560129,6.66768942697238,
11.1233083210996));
#118651=CARTESIAN_POINT('Ctrl Pts',(-8.82102086386312,6.67310554175141,
11.0499353294086));
#118652=CARTESIAN_POINT('Ctrl Pts',(-8.82266590935937,6.67888099350935,
10.9673966547548));
#118653=CARTESIAN_POINT('Ctrl Pts',(-8.82295426711707,6.67951549620996,
10.9582639893612));
#118654=CARTESIAN_POINT('Ctrl Pts',(-8.82353657371618,6.68044380326055,
10.9447935235844));
#118655=CARTESIAN_POINT('Ctrl Pts',(-8.82374829339999,6.68074178191599,
10.9404527695534));
#118656=CARTESIAN_POINT('Ctrl Pts',(-8.8241678784361,6.68126980138062,10.9327291285926));
#118657=CARTESIAN_POINT('Ctrl Pts',(-8.82436632319345,6.68150034176889,
10.9293458623558));
#118658=CARTESIAN_POINT('Ctrl Pts',(-8.82483302657028,6.68200357262701,
10.9219363853628));
#118659=CARTESIAN_POINT('Ctrl Pts',(-8.8251073727273,6.68227592811037,10.9179106647281));
#118660=CARTESIAN_POINT('Ctrl Pts',(-8.8259413280288,6.68304270931541,10.9065354415489));
#118661=CARTESIAN_POINT('Ctrl Pts',(-8.82654925886707,6.68353458164326,
10.8991895151856));
#118662=CARTESIAN_POINT('Ctrl Pts',(-8.83096961497361,6.68672542202354,
10.8512555654499));
#118663=CARTESIAN_POINT('Ctrl Pts',(-8.836818688758,6.68932573401529,10.8108784900547));
#118664=CARTESIAN_POINT('Ctrl Pts',(-8.85791915835156,6.69613316472432,
10.7044866323357));
#118665=CARTESIAN_POINT('Ctrl Pts',(-8.87678663683874,6.7002607983372,10.6393491803509));
#118666=CARTESIAN_POINT('Ctrl Pts',(-8.92029880942133,6.70781748696491,
10.5265303502385));
#118667=CARTESIAN_POINT('Ctrl Pts',(-8.94279447390394,6.71119708577969,
10.4782303320154));
#118668=CARTESIAN_POINT('Ctrl Pts',(-8.97406530778238,6.71544978720752,
10.4214784669267));
#118669=CARTESIAN_POINT('Ctrl Pts',(-8.97980285440935,6.71621472292437,
10.4114195674998));
#118670=CARTESIAN_POINT('Ctrl Pts',(-8.98914929746522,6.71743793412615,
10.3955810104814));
#118671=CARTESIAN_POINT('Ctrl Pts',(-8.99266173119407,6.71789276279152,
10.3897450806246));
#118672=CARTESIAN_POINT('Ctrl Pts',(-8.99938844587789,6.71875494623751,
10.3787849278232));
#118673=CARTESIAN_POINT('Ctrl Pts',(-9.00259197809741,6.71916190168266,
10.373654341718));
#118674=CARTESIAN_POINT('Ctrl Pts',(-9.00993541856415,6.7200867254438,10.3620927325341));
#118675=CARTESIAN_POINT('Ctrl Pts',(-9.01409870278219,6.72060543814387,
10.3556769562781));
#118676=CARTESIAN_POINT('Ctrl Pts',(-9.02697588364101,6.72219329228768,
10.3362497807862));
#118677=CARTESIAN_POINT('Ctrl Pts',(-9.03588675289696,6.72326967283151,
10.3233716748229));
#118678=CARTESIAN_POINT('Ctrl Pts',(-9.09593158010532,6.73038361239888,
10.2401891799696));
#118679=CARTESIAN_POINT('Ctrl Pts',(-9.15445050236053,6.73670990898075,
10.1755650998434));
#118680=CARTESIAN_POINT('Ctrl Pts',(-9.27001121821062,6.74803414866175,
10.0733097001899));
#118681=CARTESIAN_POINT('Ctrl Pts',(-9.32423839146912,6.75298227860817,
10.0330528743344));
#118682=CARTESIAN_POINT('Ctrl Pts',(-9.38823085442226,6.75822377886304,
9.9935736680313));
#118683=CARTESIAN_POINT('Ctrl Pts',(-9.3948848540847,6.75876196901004,9.98955894908117));
#118684=CARTESIAN_POINT('Ctrl Pts',(-9.40508687247327,6.75957622831783,
9.9835404448594));
#118685=CARTESIAN_POINT('Ctrl Pts',(-9.40860620521168,6.75985516483237,
9.98148881337406));
#118686=CARTESIAN_POINT('Ctrl Pts',(-9.41507045712849,6.76036384472535,
9.97776521324488));
#118687=CARTESIAN_POINT('Ctrl Pts',(-9.41801196564356,6.76059392634019,
9.97608767082733));
#118688=CARTESIAN_POINT('Ctrl Pts',(-9.42470299523363,6.76111417561724,
9.97230992657975));
#118689=CARTESIAN_POINT('Ctrl Pts',(-9.42845680975917,6.76140385333729,
9.97021754052496));
#118690=CARTESIAN_POINT('Ctrl Pts',(-9.43827161982545,6.76215577507538,
9.96481694025215));
#118691=CARTESIAN_POINT('Ctrl Pts',(-9.44435050565404,6.7626160774822,9.96154134157663));
#118692=CARTESIAN_POINT('Ctrl Pts',(-9.50163282923052,6.76690645690041,
9.93132186900783));
#118693=CARTESIAN_POINT('Ctrl Pts',(-9.55473499849234,6.77053462237589,
9.90812834394334));
#118694=CARTESIAN_POINT('Ctrl Pts',(-9.67495745459185,6.77844663222738,
9.86585658195173));
#118695=CARTESIAN_POINT('Ctrl Pts',(-9.74249234371883,6.78270439926348,
9.84864295499058));
#118696=CARTESIAN_POINT('Ctrl Pts',(-9.81114930160613,6.78711399980274,
9.83748958016879));
#118697=CARTESIAN_POINT('Origin',(-10.,2.67563288526385,11.));
#118698=CARTESIAN_POINT('',(-9.8111493015013,7.38550319809767,9.83748958018582));
#118699=CARTESIAN_POINT('',(-9.81114930363318,7.28726551493505,9.83748957983949));
#118700=CARTESIAN_POINT('',(-9.81114930150157,2.67563288526385,9.83748958018577));
#118701=CARTESIAN_POINT('Ctrl Pts',(-9.81114930150104,7.38550319809767,
9.83748958018586));
#118702=CARTESIAN_POINT('Ctrl Pts',(-9.80456303233157,7.38503940439618,
9.83855952460266));
#118703=CARTESIAN_POINT('Ctrl Pts',(-9.79798577865897,7.38457827590337,
9.83968545392653));
#118704=CARTESIAN_POINT('Ctrl Pts',(-9.78758650275148,7.38385277612494,
9.84155676596716));
#118705=CARTESIAN_POINT('Ctrl Pts',(-9.78375811782733,7.3835864637623,9.842265285228));
#118706=CARTESIAN_POINT('Ctrl Pts',(-9.77691868855482,7.38311216271557,
9.84356616820762));
#118707=CARTESIAN_POINT('Ctrl Pts',(-9.7739064420784,7.38290378759597,9.84415131518379));
#118708=CARTESIAN_POINT('Ctrl Pts',(-9.76661894261053,7.38240088247456,
9.84559653462716));
#118709=CARTESIAN_POINT('Ctrl Pts',(-9.76234613458593,7.38210702485039,
9.84646858708479));
#118710=CARTESIAN_POINT('Ctrl Pts',(-9.74906321936703,7.38119636107075,
9.84925648196381));
#118711=CARTESIAN_POINT('Ctrl Pts',(-9.74007041987291,7.38058391921619,
9.85125436304195));
#118712=CARTESIAN_POINT('Ctrl Pts',(-9.71893001031958,7.37915186468899,
9.85621198660835));
#118713=CARTESIAN_POINT('Ctrl Pts',(-9.70680406467292,7.37833646891464,
9.85926009580439));
#118714=CARTESIAN_POINT('Ctrl Pts',(-9.66270603997496,7.37538554060596,
9.87109471779888));
#118715=CARTESIAN_POINT('Ctrl Pts',(-9.63105843528758,7.37329537089962,
9.88103762883233));
#118716=CARTESIAN_POINT('Ctrl Pts',(-9.52737139324232,7.36641563649889,
9.91849214696055));
#118717=CARTESIAN_POINT('Ctrl Pts',(-9.45762028258616,7.36172300327169,
9.95173416871535));
#118718=CARTESIAN_POINT('Ctrl Pts',(-9.35964020421842,7.35448228980732,
10.0108442617877));
#118719=CARTESIAN_POINT('Ctrl Pts',(-9.32860172672824,7.35208260102111,
10.03164382885));
#118720=CARTESIAN_POINT('Ctrl Pts',(-9.28982078161402,7.3489098308116,10.0603936305447));
#118721=CARTESIAN_POINT('Ctrl Pts',(-9.28112722742756,7.34818668779305,
10.0670280950305));
#118722=CARTESIAN_POINT('Ctrl Pts',(-9.2672795991387,7.34701472896229,10.0779043393385));
#118723=CARTESIAN_POINT('Ctrl Pts',(-9.26206686668539,7.34656886689955,
10.0820706558163));
#118724=CARTESIAN_POINT('Ctrl Pts',(-9.25217315152062,7.34571342628298,
10.0901170238515));
#118725=CARTESIAN_POINT('Ctrl Pts',(-9.24748624403664,7.34530415896303,
10.0939894756124));
#118726=CARTESIAN_POINT('Ctrl Pts',(-9.23677521076191,7.3443594157383,10.1029796753242));
#118727=CARTESIAN_POINT('Ctrl Pts',(-9.23077226108025,7.34382295455406,
10.1081220811151));
#118728=CARTESIAN_POINT('Ctrl Pts',(-9.21200569764494,7.34212332684976,
10.1245287961239));
#118729=CARTESIAN_POINT('Ctrl Pts',(-9.19943478365673,7.34095135453911,
10.1360091832843));
#118730=CARTESIAN_POINT('Ctrl Pts',(-9.17048907591853,7.33817120173341,
10.163618055932));
#118731=CARTESIAN_POINT('Ctrl Pts',(-9.15432929260231,7.33655446075115,
10.1799609376487));
#118732=CARTESIAN_POINT('Ctrl Pts',(-9.05778883399869,7.32648686664703,
10.2834851768497));
#118733=CARTESIAN_POINT('Ctrl Pts',(-8.99049244071223,7.3175536507483,10.3819031745628));
#118734=CARTESIAN_POINT('Ctrl Pts',(-8.93248258652605,7.30808615503733,
10.5022763849072));
#118735=CARTESIAN_POINT('Ctrl Pts',(-8.92620020751459,7.30702911785883,
10.5159790467937));
#118736=CARTESIAN_POINT('Ctrl Pts',(-8.91800188295383,7.30560824256921,
10.5348065309434));
#118737=CARTESIAN_POINT('Ctrl Pts',(-8.91585631079926,7.30523221700577,
10.5398289958871));
#118738=CARTESIAN_POINT('Ctrl Pts',(-8.91250166047466,7.30463776016894,
10.5478354422089));
#118739=CARTESIAN_POINT('Ctrl Pts',(-8.91126977899309,7.30441801459158,
10.5508096925675));
#118740=CARTESIAN_POINT('Ctrl Pts',(-8.90872415355256,7.30396091668772,
10.5570278365203));
#118741=CARTESIAN_POINT('Ctrl Pts',(-8.90741265167142,7.30372370933032,
10.560272587438));
#118742=CARTESIAN_POINT('Ctrl Pts',(-8.90422529158039,7.30314286077923,
10.5682606481716));
#118743=CARTESIAN_POINT('Ctrl Pts',(-8.90236571758186,7.30280016871734,
10.5730104638729));
#118744=CARTESIAN_POINT('Ctrl Pts',(-8.89562932086222,7.30154394081403,
10.5905517553367));
#118745=CARTESIAN_POINT('Ctrl Pts',(-8.89094454521518,7.3006408612127,10.6034164655634));
#118746=CARTESIAN_POINT('Ctrl Pts',(-8.87955002463621,7.29835842348968,
10.6364891133431));
#118747=CARTESIAN_POINT('Ctrl Pts',(-8.87316178153946,7.29699334100039,
10.6568031911077));
#118748=CARTESIAN_POINT('Ctrl Pts',(-8.85191482947508,7.29207805213374,
10.7313751830044));
#118749=CARTESIAN_POINT('Ctrl Pts',(-8.84039641839956,7.28862351479121,
10.7865074311745));
#118750=CARTESIAN_POINT('Ctrl Pts',(-8.8229928731511,7.28057667350593,10.9152737878085));
#118751=CARTESIAN_POINT('Ctrl Pts',(-8.8199990222924,7.27597410674167,10.9890482038267));
#118752=CARTESIAN_POINT('Ctrl Pts',(-8.82456219839563,7.27034923467111,
11.0747594884836));
#118753=CARTESIAN_POINT('Ctrl Pts',(-8.82539693728081,7.26954673764853,
11.0868943824763));
#118754=CARTESIAN_POINT('Ctrl Pts',(-8.82700870101769,7.2682726846099,11.1059981266348));
#118755=CARTESIAN_POINT('Ctrl Pts',(-8.82766028607641,7.26780500676094,
11.1129769088182));
#118756=CARTESIAN_POINT('Ctrl Pts',(-8.82898817684258,7.26693141816832,
11.1259473117257));
#118757=CARTESIAN_POINT('Ctrl Pts',(-8.82964828058892,7.26652602330956,
11.131940387539));
#118758=CARTESIAN_POINT('Ctrl Pts',(-8.83121791404866,7.26562162790229,
11.1452510600789));
#118759=CARTESIAN_POINT('Ctrl Pts',(-8.83215020284632,7.2651219350284,11.1525656642507));
#118760=CARTESIAN_POINT('Ctrl Pts',(-8.83508644983624,7.26364972211495,
11.1739964360923));
#118761=CARTESIAN_POINT('Ctrl Pts',(-8.83727806427532,7.26267142525286,
11.1880851095267));
#118762=CARTESIAN_POINT('Ctrl Pts',(-8.84285733128236,7.26042271956303,
11.2201114531015));
#118763=CARTESIAN_POINT('Ctrl Pts',(-8.84640727737929,7.25914757484266,
11.2380167548423));
#118764=CARTESIAN_POINT('Ctrl Pts',(-8.85996441087032,7.254746660682,11.2989383483794));
#118765=CARTESIAN_POINT('Ctrl Pts',(-8.87197311069318,7.251565476542,11.3414673073801));
#118766=CARTESIAN_POINT('Ctrl Pts',(-8.90701833127548,7.24371355225981,
11.4433113409571));
#118767=CARTESIAN_POINT('Ctrl Pts',(-8.93252652934635,7.23901130237155,
11.5016315926436));
#118768=CARTESIAN_POINT('Ctrl Pts',(-8.97767572207397,7.23211037901414,
11.5856278747216));
#118769=CARTESIAN_POINT('Ctrl Pts',(-8.99386674205704,7.22983842498088,
11.6130278925004));
#118770=CARTESIAN_POINT('Ctrl Pts',(-9.0149183041041,7.22714266082391,11.6455674011038));
#118771=CARTESIAN_POINT('Ctrl Pts',(-9.01873921358551,7.22666283487739,
11.6513604929667));
#118772=CARTESIAN_POINT('Ctrl Pts',(-9.02480889384697,7.22591565596024,
11.6603884339836));
#118773=CARTESIAN_POINT('Ctrl Pts',(-9.02702299585082,7.22564615077735,
11.6636462369345));
#118774=CARTESIAN_POINT('Ctrl Pts',(-9.03098669086085,7.22516915062024,
11.669415893681));
#118775=CARTESIAN_POINT('Ctrl Pts',(-9.03272973832329,7.22496124100921,
11.6719320450926));
#118776=CARTESIAN_POINT('Ctrl Pts',(-9.0369414309462,7.22446326623873,11.6779614228233));
#118777=CARTESIAN_POINT('Ctrl Pts',(-9.03941950144486,7.22417383663789,
11.6814679783453));
#118778=CARTESIAN_POINT('Ctrl Pts',(-9.04707097245005,7.22329075848971,
11.6921704074906));
#118779=CARTESIAN_POINT('Ctrl Pts',(-9.05230660341444,7.22270110406661,
11.6993217014769));
#118780=CARTESIAN_POINT('Ctrl Pts',(-9.06475353300969,7.22133119295638,
11.7159262892428));
#118781=CARTESIAN_POINT('Ctrl Pts',(-9.07202834453338,7.2205546716017,11.7253309835701));
#118782=CARTESIAN_POINT('Ctrl Pts',(-9.09856091545684,7.21780078394325,
11.7585788647495));
#118783=CARTESIAN_POINT('Ctrl Pts',(-9.11860633332818,7.21586256867839,
11.781779882111));
#118784=CARTESIAN_POINT('Ctrl Pts',(-9.14360759288296,7.21357181614479,
11.8085311845212));
#118785=CARTESIAN_POINT('Ctrl Pts',(-9.14771288550749,7.21319951785788,
11.8128574948114));
#118786=CARTESIAN_POINT('Ctrl Pts',(-9.20752073031973,7.20782790407061,
11.8749340009141));
#118787=CARTESIAN_POINT('Ctrl Pts',(-9.26894694508746,7.20294297894025,
11.9268732757477));
#118788=CARTESIAN_POINT('Ctrl Pts',(-9.36234963743888,7.19574876061458,
11.9907476060144));
#118789=CARTESIAN_POINT('Ctrl Pts',(-9.39028839289087,7.19362506594439,
12.008181657977));
#118790=CARTESIAN_POINT('Ctrl Pts',(-9.42797894050415,7.1907738700824,12.0295608128537));
#118791=CARTESIAN_POINT('Ctrl Pts',(-9.43710661876336,7.19008445945855,
12.034579426547));
#118792=CARTESIAN_POINT('Ctrl Pts',(-9.45208992144726,7.1889538847721,12.0425606226484));
#118793=CARTESIAN_POINT('Ctrl Pts',(-9.45790598603467,7.18851529953383,
12.0455965680688));
#118794=CARTESIAN_POINT('Ctrl Pts',(-9.46919212312733,7.18766458165058,
12.0513683768899));
#118795=CARTESIAN_POINT('Ctrl Pts',(-9.47465874941698,7.18725268447713,
12.0541105416839));
#118796=CARTESIAN_POINT('Ctrl Pts',(-9.48746611844015,7.18628792476728,
12.0604105929349));
#118797=CARTESIAN_POINT('Ctrl Pts',(-9.49482288549503,7.18573393550218,
12.0639349992082));
#118798=CARTESIAN_POINT('Ctrl Pts',(-9.5189362651053,7.18391836178151,12.0751805132597));
#118799=CARTESIAN_POINT('Ctrl Pts',(-9.53583707012708,7.1826461769156,12.0825840203608));
#118800=CARTESIAN_POINT('Ctrl Pts',(-9.61267134258743,7.17686084697968,
12.1141118292701));
#118801=CARTESIAN_POINT('Ctrl Pts',(-9.67434632165505,7.17220365495304,
12.1336737027781));
#118802=CARTESIAN_POINT('Ctrl Pts',(-9.81445776863071,7.16168892727099,
12.1657329625074));
#118803=CARTESIAN_POINT('Ctrl Pts',(-9.89319733916668,7.15581990273731,
12.1755653729065));
#118804=CARTESIAN_POINT('Ctrl Pts',(-9.98409275487158,7.14941813920328,
12.1777013300578));
#118805=CARTESIAN_POINT('Ctrl Pts',(-9.99585793830614,7.14859699984235,
12.1778014827138));
#118806=CARTESIAN_POINT('Ctrl Pts',(-10.0120868775894,7.14747636700087,
12.1776964359569));
#118807=CARTESIAN_POINT('Ctrl Pts',(-10.0165504590798,7.14716940792077,
12.1776421662736));
#118808=CARTESIAN_POINT('Ctrl Pts',(-10.024210147981,7.146644933501,12.1775054784091));
#118809=CARTESIAN_POINT('Ctrl Pts',(-10.0274063858961,7.14642676207325,
12.1774354222551));
#118810=CARTESIAN_POINT('Ctrl Pts',(-10.034121785823,7.14596986377546,12.1772608721305));
#118811=CARTESIAN_POINT('Ctrl Pts',(-10.0376408307015,7.14573130037873,
12.1771536117722));
#118812=CARTESIAN_POINT('Ctrl Pts',(-10.0463622095752,7.14514208546159,
12.1768486353545));
#118813=CARTESIAN_POINT('Ctrl Pts',(-10.0515638940641,7.1447924467446,12.1766321992691));
#118814=CARTESIAN_POINT('Ctrl Pts',(-10.07118936976,7.14347945777119,12.1756852084053));
#118815=CARTESIAN_POINT('Ctrl Pts',(-10.0856014246771,7.14252783127494,
12.1747238304073));
#118816=CARTESIAN_POINT('Ctrl Pts',(-10.122859843571,7.14009182309856,12.1715490658749));
#118817=CARTESIAN_POINT('Ctrl Pts',(-10.1456663752112,7.13862425958408,
12.1689325013321));
#118818=CARTESIAN_POINT('Ctrl Pts',(-10.2868212261419,7.12960887434274,
12.1485420864135));
#118819=CARTESIAN_POINT('Ctrl Pts',(-10.4019560768608,7.12247392096375,
12.1134849655821));
#118820=CARTESIAN_POINT('Ctrl Pts',(-10.5252488923081,7.11358759114768,
12.0542774485041));
#118821=CARTESIAN_POINT('Ctrl Pts',(-10.5404964116846,7.11246664629602,
12.0465423632592));
#118822=CARTESIAN_POINT('Ctrl Pts',(-10.5624759697614,7.11081553764283,
12.0347836469239));
#118823=CARTESIAN_POINT('Ctrl Pts',(-10.5693451953029,7.11029439410972,
12.0310201046277));
#118824=CARTESIAN_POINT('Ctrl Pts',(-10.5814859859092,7.10936388936937,
12.0242100247835));
#118825=CARTESIAN_POINT('Ctrl Pts',(-10.586772476655,7.10895549571897,12.0211905722957));
#118826=CARTESIAN_POINT('Ctrl Pts',(-10.5977782287226,7.10809838208765,
12.0147908090029));
#118827=CARTESIAN_POINT('Ctrl Pts',(-10.6034927584972,7.10764939851695,
12.011402829784));
#118828=CARTESIAN_POINT('Ctrl Pts',(-10.6184198350379,7.10646601734254,
12.0023814508891));
#118829=CARTESIAN_POINT('Ctrl Pts',(-10.6275839220843,7.1057288060035,11.9966694902225));
#118830=CARTESIAN_POINT('Ctrl Pts',(-10.671044510002,7.10217991700831,11.9687435166859));
#118831=CARTESIAN_POINT('Ctrl Pts',(-10.704244323729,7.09930842887193,11.9448830536208));
#118832=CARTESIAN_POINT('Ctrl Pts',(-10.7734519043827,7.09296199601663,
11.8894676366601));
#118833=CARTESIAN_POINT('Ctrl Pts',(-10.8089128465887,7.08947263928147,
11.8573446726783));
#118834=CARTESIAN_POINT('Ctrl Pts',(-10.8912209819115,7.0808342880044,11.7731204377217));
#118835=CARTESIAN_POINT('Ctrl Pts',(-10.9355688926824,7.07567801491109,
11.7188202930857));
#118836=CARTESIAN_POINT('Ctrl Pts',(-10.9806512093493,7.07004136477047,
11.6523232630607));
#118837=CARTESIAN_POINT('Ctrl Pts',(-10.9863527140921,7.06932017985713,
11.6436697721853));
#118838=CARTESIAN_POINT('Ctrl Pts',(-10.9943777343327,7.06829413233643,
11.6311326631173));
#118839=CARTESIAN_POINT('Ctrl Pts',(-10.9967940562876,7.0679837081334,11.6273094356312));
#118840=CARTESIAN_POINT('Ctrl Pts',(-11.0009967172374,7.06744129561164,
11.6205741728159));
#118841=CARTESIAN_POINT('Ctrl Pts',(-11.002792498063,7.06720870999565,11.6176681462682));
#118842=CARTESIAN_POINT('Ctrl Pts',(-11.0065961829106,7.06671435078057,
11.6114525091213));
#118843=CARTESIAN_POINT('Ctrl Pts',(-11.0086004360471,7.06645280784112,
11.6081407796282));
#118844=CARTESIAN_POINT('Ctrl Pts',(-11.0140882208431,7.06573358005744,
11.5989712762055));
#118845=CARTESIAN_POINT('Ctrl Pts',(-11.0175373582328,7.06527802195826,
11.5930929433202));
#118846=CARTESIAN_POINT('Ctrl Pts',(-11.0373555230779,7.06263765302235,
11.5586351976354));
#118847=CARTESIAN_POINT('Ctrl Pts',(-11.0525726042463,7.0605174557016,11.5294063825332));
#118848=CARTESIAN_POINT('Ctrl Pts',(-11.0872863988974,7.0553373624199,11.4552957319249));
#118849=CARTESIAN_POINT('Ctrl Pts',(-11.1052505502069,7.05232368682522,
11.4097653219609));
#118850=CARTESIAN_POINT('Ctrl Pts',(-11.1429689238423,7.04475723960945,
11.2934339700671));
#118851=CARTESIAN_POINT('Ctrl Pts',(-11.1590272413713,7.04019787473598,
11.2216654336696));
#118852=CARTESIAN_POINT('Ctrl Pts',(-11.1703393322768,7.0343739957142,11.1328926504938));
#118853=CARTESIAN_POINT('Ctrl Pts',(-11.1720475706517,7.03331642164604,
11.1168719846597));
#118854=CARTESIAN_POINT('Ctrl Pts',(-11.1740887832349,7.03173609823456,
11.0931151166481));
#118855=CARTESIAN_POINT('Ctrl Pts',(-11.1746750049606,7.03122115634786,
11.0854021300784));
#118856=CARTESIAN_POINT('Ctrl Pts',(-11.1755848617806,7.03029863934739,
11.0716380451647));
#118857=CARTESIAN_POINT('Ctrl Pts',(-11.1759378565216,7.0298919863224,11.0655891151254));
#118858=CARTESIAN_POINT('Ctrl Pts',(-11.176586035025,7.02902837012298,11.0527835387011));
#118859=CARTESIAN_POINT('Ctrl Pts',(-11.1768697262391,7.02857106680536,
11.0460265569456));
#118860=CARTESIAN_POINT('Ctrl Pts',(-11.1774736315989,7.02734140247045,
11.0279237540038));
#118861=CARTESIAN_POINT('Ctrl Pts',(-11.177688044813,7.02656581518332,11.0165753621496));
#118862=CARTESIAN_POINT('Ctrl Pts',(-11.1779557546508,7.02241613743726,
10.9562436739114));
#118863=CARTESIAN_POINT('Ctrl Pts',(-11.1751171594198,7.01895439290733,
10.9073021529061));
#118864=CARTESIAN_POINT('Ctrl Pts',(-11.1632335996219,7.01181410622739,
10.8089775920459));
#118865=CARTESIAN_POINT('Ctrl Pts',(-11.1540626107498,7.00813955662012,
10.7597066180039));
#118866=CARTESIAN_POINT('Ctrl Pts',(-11.1366917331144,7.00294220305098,
10.69103667551));
#118867=CARTESIAN_POINT('Ctrl Pts',(-11.1310664800047,7.00141975738431,
10.6710393980602));
#118868=CARTESIAN_POINT('Ctrl Pts',(-11.1184534335279,6.99831450571608,
10.6303609249584));
#118869=CARTESIAN_POINT('Ctrl Pts',(-11.1114134211862,6.99673308923194,
10.6097034187031));
#118870=CARTESIAN_POINT('Ctrl Pts',(-11.0959661819627,6.99355986266214,
10.5681919888782));
#118871=CARTESIAN_POINT('Ctrl Pts',(-11.0875273308079,6.99196975493211,
10.5473583178036));
#118872=CARTESIAN_POINT('Ctrl Pts',(-11.0759557983401,6.98997094654322,
10.5209862460038));
#118873=CARTESIAN_POINT('Ctrl Pts',(-11.0733680939396,6.98953444935822,
10.5152155160713));
#118874=CARTESIAN_POINT('Ctrl Pts',(-11.0691665340739,6.98884247505051,
10.5060443871361));
#118875=CARTESIAN_POINT('Ctrl Pts',(-11.0675826901648,6.98858527729134,
10.5026304937711));
#118876=CARTESIAN_POINT('Ctrl Pts',(-11.0645154094007,6.98809419807456,
10.4961012894803));
#118877=CARTESIAN_POINT('Ctrl Pts',(-11.0630346210165,6.9878601730517,10.4929848501944));
#118878=CARTESIAN_POINT('Ctrl Pts',(-11.0594484023269,6.98730057367608,
10.4855221410046));
#118879=CARTESIAN_POINT('Ctrl Pts',(-11.0573298661109,6.98697578870033,
10.4811821698823));
#118880=CARTESIAN_POINT('Ctrl Pts',(-11.0499006373031,6.98585623485933,
10.466197391157));
#118881=CARTESIAN_POINT('Ctrl Pts',(-11.0444552053208,6.9850691838067,10.4556196879729));
#118882=CARTESIAN_POINT('Ctrl Pts',(-11.0305792035198,6.98313974098937,
10.4296406687201));
#118883=CARTESIAN_POINT('Ctrl Pts',(-11.0219625723902,6.9820066399515,10.4143415430918));
#118884=CARTESIAN_POINT('Ctrl Pts',(-10.9826823537663,6.97708982109436,
10.3481069020108));
#118885=CARTESIAN_POINT('Ctrl Pts',(-10.9485278832279,6.97343637096266,
10.2993395377957));
#118886=CARTESIAN_POINT('Ctrl Pts',(-10.8662458419095,6.96540299895493,
10.1989631295888));
#118887=CARTESIAN_POINT('Ctrl Pts',(-10.8168798587582,6.96102376182901,
10.1486789178639));
#118888=CARTESIAN_POINT('Ctrl Pts',(-10.7510362871584,6.95539728067929,
10.0926411767633));
#118889=CARTESIAN_POINT('Ctrl Pts',(-10.7385324511397,6.95433785198476,
10.0824351158772));
#118890=CARTESIAN_POINT('Ctrl Pts',(-10.7197273612972,6.95275528724952,
10.0677191918045));
#118891=CARTESIAN_POINT('Ctrl Pts',(-10.7135846428599,6.95223999155,10.0630091074995));
#118892=CARTESIAN_POINT('Ctrl Pts',(-10.7025510765595,6.9513170818885,10.054720269492));
#118893=CARTESIAN_POINT('Ctrl Pts',(-10.697678150988,6.9509103930267,10.0511180371731));
#118894=CARTESIAN_POINT('Ctrl Pts',(-10.6873110399871,6.95004695438959,
10.0435773464579));
#118895=CARTESIAN_POINT('Ctrl Pts',(-10.6818103286631,6.9495898663991,10.0396482777969));
#118896=CARTESIAN_POINT('Ctrl Pts',(-10.666995426664,6.94836140172638,10.0292576730323));
#118897=CARTESIAN_POINT('Ctrl Pts',(-10.6576214572477,6.94758680975163,
10.02288303261));
#118898=CARTESIAN_POINT('Ctrl Pts',(-10.6074614629191,6.94345489273674,
9.98982115964472));
#118899=CARTESIAN_POINT('Ctrl Pts',(-10.5651453533168,6.94001082366544,
9.9655531346084));
#118900=CARTESIAN_POINT('Ctrl Pts',(-10.4764056170453,6.93287706764159,
9.92173436529136));
#118901=CARTESIAN_POINT('Ctrl Pts',(-10.4299837702706,6.92919017672033,
9.90239693431866));
#118902=CARTESIAN_POINT('Ctrl Pts',(-10.3637871919489,6.92405463255425,
9.87966780144392));
#118903=CARTESIAN_POINT('Ctrl Pts',(-10.3449433495534,6.92260637095113,
9.87372318469324));
#118904=CARTESIAN_POINT('Ctrl Pts',(-10.2843245442658,6.91800419409123,
9.85626410235194));
#118905=CARTESIAN_POINT('Ctrl Pts',(-10.2420555734649,6.91487905098748,
9.84657805375115));
#118906=CARTESIAN_POINT('Ctrl Pts',(-10.1920496350892,6.91134493418146,
9.83799019486647));
#118907=CARTESIAN_POINT('Ctrl Pts',(-10.1847427200789,6.91083257861849,
9.83680612797481));
#118908=CARTESIAN_POINT('Ctrl Pts',(-10.173428493072,6.91004598123102,9.83508199325979));
#118909=CARTESIAN_POINT('Ctrl Pts',(-10.169428902887,6.90976921817809,9.8344935638392));
#118910=CARTESIAN_POINT('Ctrl Pts',(-10.1620703570259,6.90926250738813,
9.83344963640334));
#118911=CARTESIAN_POINT('Ctrl Pts',(-10.1587124458408,6.90903224088061,
9.83298804140135));
#118912=CARTESIAN_POINT('Ctrl Pts',(-10.1510515128679,6.90850905039826,
9.83196860976443));
#118913=CARTESIAN_POINT('Ctrl Pts',(-10.1467473601533,6.90821663976902,
9.83142004899233));
#118914=CARTESIAN_POINT('Ctrl Pts',(-10.1334104713215,6.90731504648324,
9.82979512273177));
#118915=CARTESIAN_POINT('Ctrl Pts',(-10.1243679709793,6.9067101045831,9.82879957784292));
#118916=CARTESIAN_POINT('Ctrl Pts',(-10.0464839631293,6.90154717067071,
9.82113707127153));
#118917=CARTESIAN_POINT('Ctrl Pts',(-9.97718042366107,6.89726697558048,
9.82044052843688));
#118918=CARTESIAN_POINT('Ctrl Pts',(-9.87568512331888,6.89096809829667,
9.82837501737253));
#118919=CARTESIAN_POINT('Ctrl Pts',(-9.84330458172222,6.88895474394848,
9.83226593055083));
#118920=CARTESIAN_POINT('Ctrl Pts',(-9.81114930150157,6.88692359881869,
9.83748958018577));
#118921=CARTESIAN_POINT('Ctrl Pts',(-9.81114930160613,6.78711399980274,
9.83748958016879));
#118922=CARTESIAN_POINT('Ctrl Pts',(-9.81165865453416,6.78714671379146,
9.83740683539975));
#118923=CARTESIAN_POINT('Ctrl Pts',(-9.81216806925791,6.78717943559225,
9.83732442420086));
#118924=CARTESIAN_POINT('Ctrl Pts',(-9.84739949050416,6.78944276472268,
9.83164857568015));
#118925=CARTESIAN_POINT('Ctrl Pts',(-9.88235162672327,6.79170711495437,
9.82761334767695));
#118926=CARTESIAN_POINT('Ctrl Pts',(-9.92806455013969,6.7947207236186,9.82440057201284));
#118927=CARTESIAN_POINT('Ctrl Pts',(-9.93870889477625,6.79542604679494,
9.8237975887402));
#118928=CARTESIAN_POINT('Ctrl Pts',(-9.95596605151993,6.79657605360612,
9.82305488706229));
#118929=CARTESIAN_POINT('Ctrl Pts',(-9.96257458412418,6.79701798340986,
9.82282621388235));
#118930=CARTESIAN_POINT('Ctrl Pts',(-9.97527772703814,6.79787059677669,
9.8224937267279));
#118931=CARTESIAN_POINT('Ctrl Pts',(-9.9813719199314,6.79828100820676,9.8223815530432));
#118932=CARTESIAN_POINT('Ctrl Pts',(-9.99549397218604,6.79923537918694,
9.82223126038202));
#118933=CARTESIAN_POINT('Ctrl Pts',(-10.0035218188105,6.79978039344215,
9.82222790847409));
#118934=CARTESIAN_POINT('Ctrl Pts',(-10.0292649535235,6.80153642938082,
9.8224803553207));
#118935=CARTESIAN_POINT('Ctrl Pts',(-10.0469739426987,6.80275711069989,
9.82305380715873));
#118936=CARTESIAN_POINT('Ctrl Pts',(-10.0888515527345,6.80567532620799,
9.82535650285618));
#118937=CARTESIAN_POINT('Ctrl Pts',(-10.1129922950995,6.8073826282093,9.8274324986164));
#118938=CARTESIAN_POINT('Ctrl Pts',(-10.2093826906933,6.81429913051286,
9.83872582109171));
#118939=CARTESIAN_POINT('Ctrl Pts',(-10.2807668703331,6.81965942393501,
9.85389060782328));
#118940=CARTESIAN_POINT('Ctrl Pts',(-10.4021546231384,6.82897493337465,
9.89170477922401));
#118941=CARTESIAN_POINT('Ctrl Pts',(-10.4528506143468,6.83292643968186,
9.91143473943408));
#118942=CARTESIAN_POINT('Ctrl Pts',(-10.5082358099888,6.83719281706454,
9.93753173143941));
#118943=CARTESIAN_POINT('Ctrl Pts',(-10.5144380150171,6.83766978855705,
9.94052088527869));
#118944=CARTESIAN_POINT('Ctrl Pts',(-10.5244632017613,6.83843905807482,
9.94546131949502));
#118945=CARTESIAN_POINT('Ctrl Pts',(-10.5283022522786,6.83873323317957,
9.94737936065352));
#118946=CARTESIAN_POINT('Ctrl Pts',(-10.5351514477798,6.839257220031,9.95084822112669));
#118947=CARTESIAN_POINT('Ctrl Pts',(-10.5381654689918,6.83948749962473,
9.95239107675725));
#118948=CARTESIAN_POINT('Ctrl Pts',(-10.5447954655564,6.83999337636174,
9.95582108891341));
#118949=CARTESIAN_POINT('Ctrl Pts',(-10.5484083202271,6.84026861206831,
9.95771404441627));
#118950=CARTESIAN_POINT('Ctrl Pts',(-10.5588972801966,6.8410666461757,9.96327937332951));
#118951=CARTESIAN_POINT('Ctrl Pts',(-10.5657470082468,6.84158648818206,
9.96700137549403));
#118952=CARTESIAN_POINT('Ctrl Pts',(-10.6306056379888,6.84650113723427,
10.00308290321));
#118953=CARTESIAN_POINT('Ctrl Pts',(-10.685824861638,6.85063068201233,10.0402323136601));
#118954=CARTESIAN_POINT('Ctrl Pts',(-10.8062065005216,6.86019183421428,
10.1369439770718));
#118955=CARTESIAN_POINT('Ctrl Pts',(-10.8683930005054,6.86559822922517,
10.1995462634242));
#118956=CARTESIAN_POINT('Ctrl Pts',(-10.9327103267732,6.87234319087347,
10.2807020684408));
#118957=CARTESIAN_POINT('Ctrl Pts',(-10.9421487187703,6.87336717271529,
10.2931097519017));
#118958=CARTESIAN_POINT('Ctrl Pts',(-10.955838415462,6.87490676472398,10.3118675470388));
#118959=CARTESIAN_POINT('Ctrl Pts',(-10.9602789402022,6.87541515073502,
10.3180779357509));
#118960=CARTESIAN_POINT('Ctrl Pts',(-10.9681279744353,6.87633034143428,
10.3292840712264));
#118961=CARTESIAN_POINT('Ctrl Pts',(-10.9715590064366,6.87673627906025,
10.3342637709421));
#118962=CARTESIAN_POINT('Ctrl Pts',(-10.9787774987635,6.87760310387184,
10.3449151345576));
#118963=CARTESIAN_POINT('Ctrl Pts',(-10.9825543348174,6.87806436718427,
10.3505936951545));
#118964=CARTESIAN_POINT('Ctrl Pts',(-10.9926319598948,6.87931649393747,
10.3660348128915));
#118965=CARTESIAN_POINT('Ctrl Pts',(-10.998837804494,6.88011079344423,10.3758581172305));
#118966=CARTESIAN_POINT('Ctrl Pts',(-11.0330680192284,6.88462772834538,
10.4318598079068));
#118967=CARTESIAN_POINT('Ctrl Pts',(-11.0580307929856,6.88845808245707,
10.4798248960721));
#118968=CARTESIAN_POINT('Ctrl Pts',(-11.0924813458439,6.89469673414182,
10.5588463247718));
#118969=CARTESIAN_POINT('Ctrl Pts',(-11.1041340284224,6.897051251909,10.5888796428063));
#118970=CARTESIAN_POINT('Ctrl Pts',(-11.1374642360981,6.90461488750198,
10.686470679371));
#118971=CARTESIAN_POINT('Ctrl Pts',(-11.1542795214332,6.90984485056745,
10.7555290402598));
#118972=CARTESIAN_POINT('Ctrl Pts',(-11.1663055234763,6.91554508812385,
10.8358875516916));
#118973=CARTESIAN_POINT('Ctrl Pts',(-11.1676982350094,6.91626297000211,
10.8461093901593));
#118974=CARTESIAN_POINT('Ctrl Pts',(-11.1695070714827,6.9172851489878,10.8608287152093));
#118975=CARTESIAN_POINT('Ctrl Pts',(-11.1700318741482,6.91759495313364,
10.8653120201424));
#118976=CARTESIAN_POINT('Ctrl Pts',(-11.170908326613,6.91813660824291,10.8731914477863));
#118977=CARTESIAN_POINT('Ctrl Pts',(-11.171271003691,6.91836905189644,10.8765862432607));
#118978=CARTESIAN_POINT('Ctrl Pts',(-11.1720137042958,6.91886347589555,
10.8838365484634));
#118979=CARTESIAN_POINT('Ctrl Pts',(-11.1723894717543,6.91912522291862,
10.8876923950372));
#118980=CARTESIAN_POINT('Ctrl Pts',(-11.1733753756158,6.91984581252435,
10.8983536770298));
#118981=CARTESIAN_POINT('Ctrl Pts',(-11.1739453390482,6.92030251431377,
10.9051628053703));
#118982=CARTESIAN_POINT('Ctrl Pts',(-11.1769438259324,6.92296725598487,
10.9451702951498));
#118983=CARTESIAN_POINT('Ctrl Pts',(-11.1780235384313,6.92510926990228,
10.9784579210194));
#118984=CARTESIAN_POINT('Ctrl Pts',(-11.1771923471998,6.93038075948637,
11.0617692510761));
#118985=CARTESIAN_POINT('Ctrl Pts',(-11.1735071117453,6.93346143365807,
11.1117086315468));
#118986=CARTESIAN_POINT('Ctrl Pts',(-11.1568325932704,6.94099722565733,
11.2323393781032));
#118987=CARTESIAN_POINT('Ctrl Pts',(-11.1405351230815,6.94545963074922,
11.3023593628651));
#118988=CARTESIAN_POINT('Ctrl Pts',(-11.1128757074553,6.951181412913,11.3858302844127));
#118989=CARTESIAN_POINT('Ctrl Pts',(-11.1074652090303,6.95224444402214,
11.4010961458548));
#118990=CARTESIAN_POINT('Ctrl Pts',(-11.0990028766858,6.95383127645805,
11.4234947463477));
#118991=CARTESIAN_POINT('Ctrl Pts',(-11.0961924491044,6.9543471726105,11.4307171146851));
#118992=CARTESIAN_POINT('Ctrl Pts',(-11.0910579929475,6.95527065034166,
11.4435360582521));
#118993=CARTESIAN_POINT('Ctrl Pts',(-11.088761643206,6.95567730101118,11.4491434747255));
#118994=CARTESIAN_POINT('Ctrl Pts',(-11.0838154108504,6.95654012453228,
11.4609607354383));
#118995=CARTESIAN_POINT('Ctrl Pts',(-11.0811552044576,6.95699663136441,
11.4671659929967));
#118996=CARTESIAN_POINT('Ctrl Pts',(-11.0738992235544,6.95822222624694,
11.483697497566));
#118997=CARTESIAN_POINT('Ctrl Pts',(-11.0692080011012,6.9589945047686,11.4939808158791));
#118998=CARTESIAN_POINT('Ctrl Pts',(-11.0437272525085,6.96308793890694,
11.5477714133036));
#118999=CARTESIAN_POINT('Ctrl Pts',(-11.0204310276766,6.96649389541748,
11.5900334905316));
#119000=CARTESIAN_POINT('Ctrl Pts',(-10.9675111489711,6.97361345098019,
11.6734822037529));
#119001=CARTESIAN_POINT('Ctrl Pts',(-10.9376837656646,6.97732685370013,
11.7144261177717));
#119002=CARTESIAN_POINT('Ctrl Pts',(-10.8947538876449,6.98225167017783,
11.7660178318959));
#119003=CARTESIAN_POINT('Ctrl Pts',(-10.8839238386263,6.98346267692399,
11.7784898826693));
#119004=CARTESIAN_POINT('Ctrl Pts',(-10.841498648658,6.98808016313202,11.8253202569992));
#119005=CARTESIAN_POINT('Ctrl Pts',(-10.8081300733243,6.99145557320917,
11.8580211408581));
#119006=CARTESIAN_POINT('Ctrl Pts',(-10.7677639444479,6.99518262035704,
11.8931293356577));
#119007=CARTESIAN_POINT('Ctrl Pts',(-10.7625841326585,6.99565457358155,
11.8975560877365));
#119008=CARTESIAN_POINT('Ctrl Pts',(-10.7540959288575,6.9964173855241,11.9046837162791));
#119009=CARTESIAN_POINT('Ctrl Pts',(-10.7508108360015,6.99671007169759,
11.9074119166069));
#119010=CARTESIAN_POINT('Ctrl Pts',(-10.7448950863615,6.99723249945962,
11.9122707006347));
#119011=CARTESIAN_POINT('Ctrl Pts',(-10.742270018797,6.99746269642173,11.9144078635862));
#119012=CARTESIAN_POINT('Ctrl Pts',(-10.7364475617438,6.99796969578397,
11.9191065414099));
#119013=CARTESIAN_POINT('Ctrl Pts',(-10.7332459971836,6.99824612588312,
11.9216627119199));
#119014=CARTESIAN_POINT('Ctrl Pts',(-10.7238453606961,6.99905116914096,
11.9290883133652));
#119015=CARTESIAN_POINT('Ctrl Pts',(-10.7176105171636,6.99957674605434,
11.9339123910437));
#119016=CARTESIAN_POINT('Ctrl Pts',(-10.7031820669488,7.00077519334837,
11.9448462798436));
#119017=CARTESIAN_POINT('Ctrl Pts',(-10.6949563267502,7.00144549053447,
11.9509128410331));
#119018=CARTESIAN_POINT('Ctrl Pts',(-10.5975028865921,7.00924980231475,
12.0208455488302));
#119019=CARTESIAN_POINT('Ctrl Pts',(-10.4998413897803,7.01578315034754,
12.0720542325587));
#119020=CARTESIAN_POINT('Ctrl Pts',(-10.3571838960684,7.02533078838272,
12.1230570996598));
#119021=CARTESIAN_POINT('Ctrl Pts',(-10.3171614733879,7.02800366797263,
12.1350090800011));
#119022=CARTESIAN_POINT('Ctrl Pts',(-10.265653932376,7.03148385768885,12.1474535624513));
#119023=CARTESIAN_POINT('Ctrl Pts',(-10.2546787816675,7.03222758301654,
12.1499392999861));
#119024=CARTESIAN_POINT('Ctrl Pts',(-10.2370751754345,7.03342473963628,
12.1536619350291));
#119025=CARTESIAN_POINT('Ctrl Pts',(-10.2304686180908,7.03387497794746,
12.1549998753391));
#119026=CARTESIAN_POINT('Ctrl Pts',(-10.2178999354993,7.03473350855163,
12.1574331184898));
#119027=CARTESIAN_POINT('Ctrl Pts',(-10.2119401089706,7.03514144537417,
12.1585392498846));
#119028=CARTESIAN_POINT('Ctrl Pts',(-10.1983226619466,7.03607556639405,
12.1609580286707));
#119029=CARTESIAN_POINT('Ctrl Pts',(-10.1906601264017,7.03660266169847,
12.1622409964259));
#119030=CARTESIAN_POINT('Ctrl Pts',(-10.1668853912186,7.0382429243873,12.1659802562812));
#119031=CARTESIAN_POINT('Ctrl Pts',(-10.1507350783665,7.039364046988,12.1681778896968));
#119032=CARTESIAN_POINT('Ctrl Pts',(-10.1129805475338,7.04200217535782,
12.1725193537282));
#119033=CARTESIAN_POINT('Ctrl Pts',(-10.0913528787889,7.043526596353,12.1744023110127));
#119034=CARTESIAN_POINT('Ctrl Pts',(-10.0107225406934,7.04925876677697,
12.1791815265163));
#119035=CARTESIAN_POINT('Ctrl Pts',(-9.95158498874825,7.05356577982892,
12.1782354034993));
#119036=CARTESIAN_POINT('Ctrl Pts',(-9.82468377092682,7.06291484233857,
12.1666337641989));
#119037=CARTESIAN_POINT('Ctrl Pts',(-9.75725871623206,7.06794945412695,
12.1544905639196));
#119038=CARTESIAN_POINT('Ctrl Pts',(-9.6821665797117,7.0734099639287,12.134092518972));
#119039=CARTESIAN_POINT('Ctrl Pts',(-9.6730992039668,7.07406666543416,12.131512177507));
#119040=CARTESIAN_POINT('Ctrl Pts',(-9.65926876106935,7.07506326109653,
12.1273962525905));
#119041=CARTESIAN_POINT('Ctrl Pts',(-9.65448310569204,7.07540717021679,
12.1259387929861));
#119042=CARTESIAN_POINT('Ctrl Pts',(-9.64641688889671,7.07598507713754,
12.1234259743158));
#119043=CARTESIAN_POINT('Ctrl Pts',(-9.64313144245742,7.07621997000779,
12.1223866401824));
#119044=CARTESIAN_POINT('Ctrl Pts',(-9.63634064170335,7.0767043928802,12.1202055720394));
#119045=CARTESIAN_POINT('Ctrl Pts',(-9.6328360213339,7.07695380308728,12.119061779446));
#119046=CARTESIAN_POINT('Ctrl Pts',(-9.62366193906326,7.07760527364036,
12.1160199238925));
#119047=CARTESIAN_POINT('Ctrl Pts',(-9.61800137057801,7.07800582248132,
12.1140950845841));
#119048=CARTESIAN_POINT('Ctrl Pts',(-9.59228377130419,7.07982020323933,
12.105130925934));
#119049=CARTESIAN_POINT('Ctrl Pts',(-9.5724035481661,7.08120767074359,12.0975920443112));
#119050=CARTESIAN_POINT('Ctrl Pts',(-9.51471206571097,7.08521963830381,
12.0739088568943));
#119051=CARTESIAN_POINT('Ctrl Pts',(-9.47752756285411,7.08778755163321,
12.0563179766644));
#119052=CARTESIAN_POINT('Ctrl Pts',(-9.35620794602017,7.09633855736261,
11.9909479118797));
#119053=CARTESIAN_POINT('Ctrl Pts',(-9.27706171316799,7.10224403132633,
11.9347749660114));
#119054=CARTESIAN_POINT('Ctrl Pts',(-9.19589184900835,7.10941600538715,
11.8606280550987));
#119055=CARTESIAN_POINT('Ctrl Pts',(-9.18626241497194,7.11028651857718,
11.8515290292971));
#119056=CARTESIAN_POINT('Ctrl Pts',(-9.17115188074181,7.11168582274353,
11.8367604113687));
#119057=CARTESIAN_POINT('Ctrl Pts',(-9.16557051385687,7.11221019044671,
11.8311946934718));
#119058=CARTESIAN_POINT('Ctrl Pts',(-9.15577393229354,7.11314429250534,
11.8212274615917));
#119059=CARTESIAN_POINT('Ctrl Pts',(-9.15153618464364,7.11355303155063,
11.8168484245695));
#119060=CARTESIAN_POINT('Ctrl Pts',(-9.14276818517147,7.11440866878137,
11.807646247941));
#119061=CARTESIAN_POINT('Ctrl Pts',(-9.13824422735141,7.11485581406018,
11.8028174334143));
#119062=CARTESIAN_POINT('Ctrl Pts',(-9.12652418455816,7.11602934011728,
11.7900944003536));
#119063=CARTESIAN_POINT('Ctrl Pts',(-9.11939452241287,7.11675845096712,
11.7821401034664));
#119064=CARTESIAN_POINT('Ctrl Pts',(-9.08646289567101,7.12019962205745,
11.7443784032387));
#119065=CARTESIAN_POINT('Ctrl Pts',(-9.06206257805021,7.12296713144085,
11.713387709906));
#119066=CARTESIAN_POINT('Ctrl Pts',(-8.98923021723505,7.13196782840287,
11.6106732760269));
#119067=CARTESIAN_POINT('Ctrl Pts',(-8.94712514452389,7.13838714501175,
11.5348170503302));
#119068=CARTESIAN_POINT('Ctrl Pts',(-8.9061460852412,7.14609857239075,11.4369918889146));
#119069=CARTESIAN_POINT('Ctrl Pts',(-8.89903335609785,7.14751277359536,
11.4187491081265));
#119070=CARTESIAN_POINT('Ctrl Pts',(-8.88545716169023,7.15036611530907,
11.3811875131619));
#119071=CARTESIAN_POINT('Ctrl Pts',(-8.87903314728264,7.15180354467346,
11.3618606002703));
#119072=CARTESIAN_POINT('Ctrl Pts',(-8.87133565921433,7.15364002468118,
11.3365252632519));
#119073=CARTESIAN_POINT('Ctrl Pts',(-8.86960375412886,7.15406180561386,
11.3306611230906));
#119074=CARTESIAN_POINT('Ctrl Pts',(-8.86689269643877,7.15473591586353,
11.32121132087));
#119075=CARTESIAN_POINT('Ctrl Pts',(-8.8658847386127,7.15498981993244,11.3176341431503));
#119076=CARTESIAN_POINT('Ctrl Pts',(-8.86396841716875,7.15547889723786,
11.3107078150592));
#119077=CARTESIAN_POINT('Ctrl Pts',(-8.86305790372677,7.15571418165724,
11.3073593557755));
#119078=CARTESIAN_POINT('Ctrl Pts',(-8.8608854037027,7.15628283562606,11.2992281166866));
#119079=CARTESIAN_POINT('Ctrl Pts',(-8.85963870467275,7.15661534724143,
11.2944412464405));
#119080=CARTESIAN_POINT('Ctrl Pts',(-8.85531094597071,7.15779263077702,
11.2773843429932));
#119081=CARTESIAN_POINT('Ctrl Pts',(-8.85239733680639,7.15862858013191,
11.2650721850143));
#119082=CARTESIAN_POINT('Ctrl Pts',(-8.84558592345296,7.16070455095235,
11.2340677265738));
#119083=CARTESIAN_POINT('Ctrl Pts',(-8.8419430949966,7.1619333543182,11.2153226590861));
#119084=CARTESIAN_POINT('Ctrl Pts',(-8.82697921390544,7.16764214086865,
11.1268899725776));
#119085=CARTESIAN_POINT('Ctrl Pts',(-8.82148249036645,7.17194682567929,
11.0563614794458));
#119086=CARTESIAN_POINT('Ctrl Pts',(-8.82309786245486,7.18024999671284,
10.9227535747313));
#119087=CARTESIAN_POINT('Ctrl Pts',(-8.82891472518208,7.18421814271105,
10.8599164502919));
#119088=CARTESIAN_POINT('Ctrl Pts',(-8.84180773714321,7.18914122931831,
10.7859146325037));
#119089=CARTESIAN_POINT('Ctrl Pts',(-8.84407134684014,7.18994067473012,
10.7740115192775));
#119090=CARTESIAN_POINT('Ctrl Pts',(-8.8479312869556,7.19121087118127,10.7552926112887));
#119091=CARTESIAN_POINT('Ctrl Pts',(-8.84940547147821,7.19167778221233,
10.7484522847466));
#119092=CARTESIAN_POINT('Ctrl Pts',(-8.85226296937522,7.19255053712155,
10.7357442323773));
#119093=CARTESIAN_POINT('Ctrl Pts',(-8.85363055702685,7.1929558710821,10.7298731777575));
#119094=CARTESIAN_POINT('Ctrl Pts',(-8.8567734085209,7.19386089624394,10.7168347772511));
#119095=CARTESIAN_POINT('Ctrl Pts',(-8.85857111351893,7.19436128608009,
10.709673157194));
#119096=CARTESIAN_POINT('Ctrl Pts',(-8.86405124036055,7.19583805048366,
10.6886796608658));
#119097=CARTESIAN_POINT('Ctrl Pts',(-8.86791850177335,7.19682025803088,
10.6748978803393));
#119098=CARTESIAN_POINT('Ctrl Pts',(-8.88661407039467,7.20131612265656,
10.6126566140892));
#119099=CARTESIAN_POINT('Ctrl Pts',(-8.90430756781351,7.20491968977872,
10.5651207077329));
#119100=CARTESIAN_POINT('Ctrl Pts',(-8.95706673317573,7.21427434940384,
10.4472384470748));
#119101=CARTESIAN_POINT('Ctrl Pts',(-8.99620787556259,7.22010496877039,
10.3789880507339));
#119102=CARTESIAN_POINT('Ctrl Pts',(-9.04473955631525,7.22612793207715,
10.3110897557392));
#119103=CARTESIAN_POINT('Ctrl Pts',(-9.04765975988754,7.22648635661377,
10.3070585102653));
#119104=CARTESIAN_POINT('Ctrl Pts',(-9.06511561785741,7.22860498064223,
10.283280050629));
#119105=CARTESIAN_POINT('Ctrl Pts',(-9.08024074262172,7.23034380847114,
10.2639705161614));
#119106=CARTESIAN_POINT('Ctrl Pts',(-9.1001261074507,7.23249841912012,10.2401550730176));
#119107=CARTESIAN_POINT('Ctrl Pts',(-9.10433465808834,7.23294738707613,
10.2351987606793));
#119108=CARTESIAN_POINT('Ctrl Pts',(-9.11106879769303,7.23365440166092,
10.2273999525602));
#119109=CARTESIAN_POINT('Ctrl Pts',(-9.11356740155779,7.2339142969905,10.2245344848482));
#119110=CARTESIAN_POINT('Ctrl Pts',(-9.11834973341286,7.23440704975766,
10.2191032927936));
#119111=CARTESIAN_POINT('Ctrl Pts',(-9.12063080009237,7.23464007276924,
10.2165354695666));
#119112=CARTESIAN_POINT('Ctrl Pts',(-9.12608465351509,7.23519253616889,
10.210449830751));
#119113=CARTESIAN_POINT('Ctrl Pts',(-9.1292674823748,7.23551123513328,10.2069411199333));
#119114=CARTESIAN_POINT('Ctrl Pts',(-9.14013726532212,7.23658750646814,
10.1951027340893));
#119115=CARTESIAN_POINT('Ctrl Pts',(-9.1479235383552,7.23733813586079,10.1868645513261));
#119116=CARTESIAN_POINT('Ctrl Pts',(-9.16729775348845,7.23916068762187,
10.1669498273378));
#119117=CARTESIAN_POINT('Ctrl Pts',(-9.17901395931552,7.24022459647593,
10.1554009245735));
#119118=CARTESIAN_POINT('Ctrl Pts',(-9.22919113742058,7.24464375396235,
10.1079713967805));
#119119=CARTESIAN_POINT('Ctrl Pts',(-9.26979357389781,7.24789398535228,
10.0744403190192));
#119120=CARTESIAN_POINT('Ctrl Pts',(-9.37690190980518,7.25605424897156,
9.99743609743425));
#119121=CARTESIAN_POINT('Ctrl Pts',(-9.44580343115982,7.26095979364624,
9.95776688848817));
#119122=CARTESIAN_POINT('Ctrl Pts',(-9.53276104529315,7.26716279202987,
9.91877905885108));
#119123=CARTESIAN_POINT('Ctrl Pts',(-9.54748918981858,7.26821306132519,
9.91253280909261));
#119124=CARTESIAN_POINT('Ctrl Pts',(-9.56949960935692,7.26978446932996,
9.90372268182108));
#119125=CARTESIAN_POINT('Ctrl Pts',(-9.5766876224835,7.2702979287095,9.90092713116257));
#119126=CARTESIAN_POINT('Ctrl Pts',(-9.58956720381623,7.27121870368291,
9.89606311383766));
#119127=CARTESIAN_POINT('Ctrl Pts',(-9.59524829642875,7.27162510909946,
9.89396754797411));
#119128=CARTESIAN_POINT('Ctrl Pts',(-9.60731743551697,7.27248916316173,
9.88962108376982));
#119129=CARTESIAN_POINT('Ctrl Pts',(-9.61370922310152,7.27294715910361,
9.88738130231654));
#119130=CARTESIAN_POINT('Ctrl Pts',(-9.63091205410315,7.27418105115824,
9.88151926860928));
#119131=CARTESIAN_POINT('Ctrl Pts',(-9.64175673907339,7.27496021373416,
9.8779987484569));
#119132=CARTESIAN_POINT('Ctrl Pts',(-9.70033578511025,7.27917732241226,
9.85991801359534));
#119133=CARTESIAN_POINT('Ctrl Pts',(-9.74890176212053,7.28270643786671,
9.84824740365316));
#119134=CARTESIAN_POINT('Ctrl Pts',(-9.80241649052628,7.28662544021495,
9.83893350277088));
#119135=CARTESIAN_POINT('Ctrl Pts',(-9.8067810654517,7.28694525765071,9.83819920342532));
#119136=CARTESIAN_POINT('Ctrl Pts',(-9.81114930576479,7.28726551493505,
9.83748957949321));
#119137=CARTESIAN_POINT('Origin',(-10.,2.67563288526385,11.));
#119138=CARTESIAN_POINT('',(-9.81114930150157,7.88735883108162,9.83748958018577));
#119139=CARTESIAN_POINT('',(-9.81114930150278,7.78890339972193,9.83748958018558));
#119140=CARTESIAN_POINT('',(-9.81114930150157,2.67563288526385,9.83748958018577));
#119141=CARTESIAN_POINT('Ctrl Pts',(-9.81114930150157,7.88735883108162,
9.83748958018577));
#119142=CARTESIAN_POINT('Ctrl Pts',(-9.74943107542683,7.88290340352557,
9.84751575277368));
#119143=CARTESIAN_POINT('Ctrl Pts',(-9.68857434077757,7.87832101353714,
9.86244662222568));
#119144=CARTESIAN_POINT('Ctrl Pts',(-9.58638890922645,7.87042032301345,
9.89634623793599));
#119145=CARTESIAN_POINT('Ctrl Pts',(-9.54446494224,7.86711755370434,9.91297928531574));
#119146=CARTESIAN_POINT('Ctrl Pts',(-9.48322646397056,7.86228195855108,
9.9414421632336));
#119147=CARTESIAN_POINT('Ctrl Pts',(-9.46313093829663,7.86069357339216,
9.95149089166864));
#119148=CARTESIAN_POINT('Ctrl Pts',(-9.437967233662,7.85871329830822,9.964987287547));
#119149=CARTESIAN_POINT('Ctrl Pts',(-9.43262306370001,7.85829325086483,
9.9679071933588));
#119150=CARTESIAN_POINT('Ctrl Pts',(-9.42405840609558,7.85762119538577,
9.97267331444895));
#119151=CARTESIAN_POINT('Ctrl Pts',(-9.42082366478352,7.85736762980968,
9.97449348508955));
#119152=CARTESIAN_POINT('Ctrl Pts',(-9.41461239925589,7.85688131954688,
9.97802729256199));
#119153=CARTESIAN_POINT('Ctrl Pts',(-9.41163470634162,7.85664844817307,
9.97973869062973));
#119154=CARTESIAN_POINT('Ctrl Pts',(-9.40506443222326,7.85613512220821,
9.98355321742165));
#119155=CARTESIAN_POINT('Ctrl Pts',(-9.40147539334602,7.85585504949519,
9.98566243875509));
#119156=CARTESIAN_POINT('Ctrl Pts',(-9.38875205165487,7.85486308814584,
9.99323078962856));
#119157=CARTESIAN_POINT('Ctrl Pts',(-9.37968031223164,7.85415750027515,
9.99879482537806));
#119158=CARTESIAN_POINT('Ctrl Pts',(-9.32070828520934,7.84957328519771,
10.0360738736426));
#119159=CARTESIAN_POINT('Ctrl Pts',(-9.27317506302755,7.84588793213582,
10.0713891657175));
#119160=CARTESIAN_POINT('Ctrl Pts',(-9.18872929210029,7.83896291861324,
10.1446028521408));
#119161=CARTESIAN_POINT('Ctrl Pts',(-9.15132399448373,7.83572638062435,
10.1817009887514));
#119162=CARTESIAN_POINT('Ctrl Pts',(-9.09645807225226,7.83051274360634,
10.2439391986843));
#119163=CARTESIAN_POINT('Ctrl Pts',(-9.07727925166329,7.8285852224052,10.2674686551036));
#119164=CARTESIAN_POINT('Ctrl Pts',(-9.04643749691965,7.8252728600388,10.3084422316967));
#119165=CARTESIAN_POINT('Ctrl Pts',(-9.03429280986289,7.82390564156193,
10.3255052773521));
#119166=CARTESIAN_POINT('Ctrl Pts',(-9.01782979429182,7.82195502303108,
10.3499921909187));
#119167=CARTESIAN_POINT('Ctrl Pts',(-9.01312743757314,7.82138586783488,
10.3571539811538));
#119168=CARTESIAN_POINT('Ctrl Pts',(-9.00516599340077,7.82040089994723,
10.369572677558));
#119169=CARTESIAN_POINT('Ctrl Pts',(-9.0018693660908,7.8199864812399,10.3748051945668));
#119170=CARTESIAN_POINT('Ctrl Pts',(-8.99563382252948,7.81918974802054,
10.3848774899367));
#119171=CARTESIAN_POINT('Ctrl Pts',(-8.99268829063581,7.818807688374,10.3897129863052));
#119172=CARTESIAN_POINT('Ctrl Pts',(-8.98508569131969,7.81780639150752,
10.4023986938285));
#119173=CARTESIAN_POINT('Ctrl Pts',(-8.9804848905286,7.81718516033154,10.4102820093168));
#119174=CARTESIAN_POINT('Ctrl Pts',(-8.96464819231441,7.81499153345654,
10.4381569681104));
#119175=CARTESIAN_POINT('Ctrl Pts',(-8.95390560423597,7.81340206563585,
10.4584214305627));
#119176=CARTESIAN_POINT('Ctrl Pts',(-8.90422762609893,7.80552306297277,
10.5591321735631));
#119177=CARTESIAN_POINT('Ctrl Pts',(-8.87394936832593,7.79895307775005,
10.6435078764449));
#119178=CARTESIAN_POINT('Ctrl Pts',(-8.84175855188041,7.78864714183354,
10.7804409286624));
#119179=CARTESIAN_POINT('Ctrl Pts',(-8.83329018446766,7.78491312219991,
10.8311250036772));
#119180=CARTESIAN_POINT('Ctrl Pts',(-8.82721547832075,7.78066133481692,
10.8915570254728));
#119181=CARTESIAN_POINT('Ctrl Pts',(-8.8263873231804,7.78000825302077,10.900920679869));
#119182=CARTESIAN_POINT('Ctrl Pts',(-8.82533647356514,7.77905811142901,
10.9146771442689));
#119183=CARTESIAN_POINT('Ctrl Pts',(-8.82502615729278,7.77875660097518,
10.919062613318));
#119184=CARTESIAN_POINT('Ctrl Pts',(-8.82451981918072,7.77822472069115,
10.92683631955));
#119185=CARTESIAN_POINT('Ctrl Pts',(-8.82431387674356,7.77799382238227,
10.9302237845562));
#119186=CARTESIAN_POINT('Ctrl Pts',(-8.82389712328976,7.77749258889408,
10.9376054299811));
#119187=CARTESIAN_POINT('Ctrl Pts',(-8.82369201316351,7.77722256643187,
10.9415998265102));
#119188=CARTESIAN_POINT('Ctrl Pts',(-8.82317424591607,7.77646886041132,
10.9527964512655));
#119189=CARTESIAN_POINT('Ctrl Pts',(-8.82290735365027,7.77598759469651,
10.9600007653021));
#119190=CARTESIAN_POINT('Ctrl Pts',(-8.8216777369192,7.77305877580818,11.0041453287305));
#119191=CARTESIAN_POINT('Ctrl Pts',(-8.82238773403703,7.7706920874923,11.0411154471114));
#119192=CARTESIAN_POINT('Ctrl Pts',(-8.83060896623812,7.76287220682805,
11.1649867825008));
#119193=CARTESIAN_POINT('Ctrl Pts',(-8.8460237164487,7.75760089972407,11.2510691351177));
#119194=CARTESIAN_POINT('Ctrl Pts',(-8.88203763804603,7.74959274599,11.3725849238408));
#119195=CARTESIAN_POINT('Ctrl Pts',(-8.8951783224685,7.74705369044557,11.4099120973305));
#119196=CARTESIAN_POINT('Ctrl Pts',(-8.91422478788929,7.74375009079304,
11.4564007166879));
#119197=CARTESIAN_POINT('Ctrl Pts',(-8.9184135666646,7.74304263426259,11.4662404962497));
#119198=CARTESIAN_POINT('Ctrl Pts',(-8.92541163253317,7.7418899297302,11.4820775227592));
#119199=CARTESIAN_POINT('Ctrl Pts',(-8.928138588902,7.74144745865819,11.4881106532559));
#119200=CARTESIAN_POINT('Ctrl Pts',(-8.93347331432446,7.74059433295124,
11.4996529186084));
#119201=CARTESIAN_POINT('Ctrl Pts',(-8.93607327252425,7.74018395494179,
11.5051654446809));
#119202=CARTESIAN_POINT('Ctrl Pts',(-8.94213257515066,7.73923961335664,
11.517758312413));
#119203=CARTESIAN_POINT('Ctrl Pts',(-8.9456203965101,7.73870468675656,11.5248245470166));
#119204=CARTESIAN_POINT('Ctrl Pts',(-8.9551563016396,7.73726460527448,11.5436652637392));
#119205=CARTESIAN_POINT('Ctrl Pts',(-8.96133226654104,7.73635507936613,
11.5553733769103));
#119206=CARTESIAN_POINT('Ctrl Pts',(-9.01431338981796,7.7287362910599,11.6518366190005));
#119207=CARTESIAN_POINT('Ctrl Pts',(-9.07120114146556,7.7216555510736,11.7306124133267));
#119208=CARTESIAN_POINT('Ctrl Pts',(-9.16499544169033,7.7115472236744,11.8315927996381));
#119209=CARTESIAN_POINT('Ctrl Pts',(-9.19447849853451,7.70854760479785,
11.8601829577406));
#119210=CARTESIAN_POINT('Ctrl Pts',(-9.24139251425142,7.70409517830533,
11.9011441203719));
#119211=CARTESIAN_POINT('Ctrl Pts',(-9.25776551050205,7.7025954618132,11.9146770696243));
#119212=CARTESIAN_POINT('Ctrl Pts',(-9.27920568813946,7.70070865662662,
11.9314431581423));
#119213=CARTESIAN_POINT('Ctrl Pts',(-9.28394275085752,7.70029644460818,
11.9350897371872));
#119214=CARTESIAN_POINT('Ctrl Pts',(-9.29164609525518,7.69963388158351,
11.9409268843436));
#119215=CARTESIAN_POINT('Ctrl Pts',(-9.29459518455639,7.69938204858146,
11.9431398111324));
#119216=CARTESIAN_POINT('Ctrl Pts',(-9.30032161709896,7.69889663068955,
11.9473949050965));
#119217=CARTESIAN_POINT('Ctrl Pts',(-9.30309759307152,7.69866293684108,
11.949438771741));
#119218=CARTESIAN_POINT('Ctrl Pts',(-9.30992657165068,7.69809190192296,
11.9544206535867));
#119219=CARTESIAN_POINT('Ctrl Pts',(-9.3139894702766,7.69775547003068,11.9573451184726));
#119220=CARTESIAN_POINT('Ctrl Pts',(-9.3257648657861,7.69678949781629,11.9657075625778));
#119221=CARTESIAN_POINT('Ctrl Pts',(-9.33352443209061,7.69616411302244,
11.9710790099035));
#119222=CARTESIAN_POINT('Ctrl Pts',(-9.39782834585944,7.6910649793618,12.0144585409606));
#119223=CARTESIAN_POINT('Ctrl Pts',(-9.45751629780706,7.68685210721725,
12.0475928413633));
#119224=CARTESIAN_POINT('Ctrl Pts',(-9.56441427852582,7.67960915107862,
12.0953327314901));
#119225=CARTESIAN_POINT('Ctrl Pts',(-9.6102852064595,7.67658857719186,12.1124795713582));
#119226=CARTESIAN_POINT('Ctrl Pts',(-9.69665170568933,7.67089390940305,
12.1387647625826));
#119227=CARTESIAN_POINT('Ctrl Pts',(-9.73681873110736,7.66824293908909,
12.1487125088813));
#119228=CARTESIAN_POINT('Ctrl Pts',(-9.78806389039291,7.66481243150475,
12.1585748042698));
#119229=CARTESIAN_POINT('Ctrl Pts',(-9.79873254523177,7.66409572875389,
12.160475717325));
#119230=CARTESIAN_POINT('Ctrl Pts',(-9.81598960685156,7.66293167652171,
12.1633054121734));
#119231=CARTESIAN_POINT('Ctrl Pts',(-9.82256246987904,7.6624872076712,12.1643260825989));
#119232=CARTESIAN_POINT('Ctrl Pts',(-9.83516477952391,7.66163274012948,
12.1661738496661));
#119233=CARTESIAN_POINT('Ctrl Pts',(-9.84119269819625,7.66122303858443,
12.1670099982711));
#119234=CARTESIAN_POINT('Ctrl Pts',(-9.85497638860506,7.66028380211372,
12.1688132013588));
#119235=CARTESIAN_POINT('Ctrl Pts',(-9.8627357799825,7.65975333923783,12.169749834939));
#119236=CARTESIAN_POINT('Ctrl Pts',(-9.88343570574244,7.65833334927146,
12.1720397218351));
#119237=CARTESIAN_POINT('Ctrl Pts',(-9.8963900001829,7.65743964055994,12.1732558496495));
#119238=CARTESIAN_POINT('Ctrl Pts',(-10.0078349386093,7.64970516456164,
12.1818580708166));
#119239=CARTESIAN_POINT('Ctrl Pts',(-10.1068561737339,7.64247538467015,
12.1770403367912));
#119240=CARTESIAN_POINT('Ctrl Pts',(-10.2589763085333,7.63114982641165,
12.1502747891218));
#119241=CARTESIAN_POINT('Ctrl Pts',(-10.3131140758385,7.62708576562497,
12.1367329256127));
#119242=CARTESIAN_POINT('Ctrl Pts',(-10.3745458551827,7.62256682567292,
12.1166420805908));
#119243=CARTESIAN_POINT('Ctrl Pts',(-10.3829662981124,7.62194957785701,
12.1137822768003));
#119244=CARTESIAN_POINT('Ctrl Pts',(-10.395409021027,7.62104151562285,12.1093986001857));
#119245=CARTESIAN_POINT('Ctrl Pts',(-10.3994564181847,7.62074677725093,
12.1079477060947));
#119246=CARTESIAN_POINT('Ctrl Pts',(-10.4063721096402,7.62024436770512,
12.10542577497));
#119247=CARTESIAN_POINT('Ctrl Pts',(-10.409244272511,7.62003607314136,12.1043656829349));
#119248=CARTESIAN_POINT('Ctrl Pts',(-10.415798383721,7.61956159847327,12.1019175327269));
#119249=CARTESIAN_POINT('Ctrl Pts',(-10.4194775382595,7.61929584787206,
12.1005222127986));
#119250=CARTESIAN_POINT('Ctrl Pts',(-10.4296087147944,7.61856552379729,
12.0966217748843));
#119251=CARTESIAN_POINT('Ctrl Pts',(-10.4360458780282,7.61810313556992,
12.0940781338228));
#119252=CARTESIAN_POINT('Ctrl Pts',(-10.4716310289381,7.61555418649345,
12.0796527181057));
#119253=CARTESIAN_POINT('Ctrl Pts',(-10.5003187709561,7.61352600618621,
12.0666617707111));
#119254=CARTESIAN_POINT('Ctrl Pts',(-10.5854581331762,7.60748854771771,
12.0239152435637));
#119255=CARTESIAN_POINT('Ctrl Pts',(-10.640045758301,7.60358769934821,11.9907098284495));
#119256=CARTESIAN_POINT('Ctrl Pts',(-10.7274889412229,7.5968819043087,11.9272607647575));
#119257=CARTESIAN_POINT('Ctrl Pts',(-10.7618046919119,7.59411406732138,
11.8992807387113));
#119258=CARTESIAN_POINT('Ctrl Pts',(-10.8079538534198,7.59011040833927,
11.8571111823773));
#119259=CARTESIAN_POINT('Ctrl Pts',(-10.8211549083992,7.58892970881053,
11.8444723627325));
#119260=CARTESIAN_POINT('Ctrl Pts',(-10.8441318053855,7.58680500021843,
11.8214257211127));
#119261=CARTESIAN_POINT('Ctrl Pts',(-10.8540226368043,7.58586598161522,
11.8111374898562));
#119262=CARTESIAN_POINT('Ctrl Pts',(-10.8687385074957,7.58442953984668,
11.7952627743305));
#119263=CARTESIAN_POINT('Ctrl Pts',(-10.8737022306786,7.58393796064214,
11.7898062310485));
#119264=CARTESIAN_POINT('Ctrl Pts',(-10.8826294993968,7.58304066751989,
11.7798054781242));
#119265=CARTESIAN_POINT('Ctrl Pts',(-10.8866100564021,7.5826356770038,11.7752767392976));
#119266=CARTESIAN_POINT('Ctrl Pts',(-10.8951409347728,7.58175691971124,
11.7654194057265));
#119267=CARTESIAN_POINT('Ctrl Pts',(-10.8996788060038,7.58128266708211,
11.7600803918878));
#119268=CARTESIAN_POINT('Ctrl Pts',(-10.9119566425842,7.57998048683745,
11.7453709494854));
#119269=CARTESIAN_POINT('Ctrl Pts',(-10.9195994484237,7.57914873207881,
11.7359209234565));
#119270=CARTESIAN_POINT('Ctrl Pts',(-10.9733837839764,7.5731387209641,11.6672724210527));
#119271=CARTESIAN_POINT('Ctrl Pts',(-11.0139110053601,7.5677438053203,11.6039115574382));
#119272=CARTESIAN_POINT('Ctrl Pts',(-11.0758337722912,7.55780913789568,
11.4830802310864));
#119273=CARTESIAN_POINT('Ctrl Pts',(-11.0993140143457,7.55332132571333,
11.4269589001096));
#119274=CARTESIAN_POINT('Ctrl Pts',(-11.1239259723911,7.54767345631272,
11.3524209442968));
#119275=CARTESIAN_POINT('Ctrl Pts',(-11.1291098421337,7.54640747729846,
11.3354417180618));
#119276=CARTESIAN_POINT('Ctrl Pts',(-11.1371498602182,7.54431326053139,
11.3068046335979));
#119277=CARTESIAN_POINT('Ctrl Pts',(-11.140215154176,7.54347637054082,11.295208939023));
#119278=CARTESIAN_POINT('Ctrl Pts',(-11.1442694027425,7.54231422139191,
11.2788656809099));
#119279=CARTESIAN_POINT('Ctrl Pts',(-11.1454068763686,7.54198134934764,
11.2741562030578));
#119280=CARTESIAN_POINT('Ctrl Pts',(-11.1473052105571,7.54141400011797,
11.2660784444642));
#119281=CARTESIAN_POINT('Ctrl Pts',(-11.1480803708964,7.54117873613198,
11.2627136235878));
#119282=CARTESIAN_POINT('Ctrl Pts',(-11.1496680518051,7.54068927382666,
11.25568055882));
#119283=CARTESIAN_POINT('Ctrl Pts',(-11.1504778310229,7.54043522764607,
11.2520117830932));
#119284=CARTESIAN_POINT('Ctrl Pts',(-11.1525974917259,7.53975805564364,
11.242185293465));
#119285=CARTESIAN_POINT('Ctrl Pts',(-11.1538756030746,7.53933666424317,
11.2360207433045));
#119286=CARTESIAN_POINT('Ctrl Pts',(-11.1594267770394,7.53744388315675,
11.2081230090223));
#119287=CARTESIAN_POINT('Ctrl Pts',(-11.1631359799511,7.53600083947334,
11.1862806485443));
#119288=CARTESIAN_POINT('Ctrl Pts',(-11.1760582182084,7.53005563252371,
11.0945817249614));
#119289=CARTESIAN_POINT('Ctrl Pts',(-11.1796105011957,7.52574958290094,
11.0240710767667));
#119290=CARTESIAN_POINT('Ctrl Pts',(-11.1742170486215,7.5172522330217,10.887097955277));
#119291=CARTESIAN_POINT('Ctrl Pts',(-11.1659541321944,7.51308161537175,
10.8208857684327));
#119292=CARTESIAN_POINT('Ctrl Pts',(-11.1491939774275,7.50780509134025,
10.7418331687425));
#119293=CARTESIAN_POINT('Ctrl Pts',(-11.1459962051112,7.50687017450675,
10.7279897424527));
#119294=CARTESIAN_POINT('Ctrl Pts',(-11.1407620494892,7.50543873167473,
10.7070644571896));
#119295=CARTESIAN_POINT('Ctrl Pts',(-11.1389082708635,7.50494798655903,
10.6999379526993));
#119296=CARTESIAN_POINT('Ctrl Pts',(-11.1354154310126,7.50405156333176,
10.6870092518229));
#119297=CARTESIAN_POINT('Ctrl Pts',(-11.1337983997197,7.50364660150011,
10.6812013238562));
#119298=CARTESIAN_POINT('Ctrl Pts',(-11.1302028513811,7.50276715547185,
10.6686605657566));
#119299=CARTESIAN_POINT('Ctrl Pts',(-11.1282086168535,7.50229217940577,
10.6619325228126));
#119300=CARTESIAN_POINT('Ctrl Pts',(-11.1225829528006,7.50098607288355,
10.6435572738364));
#119301=CARTESIAN_POINT('Ctrl Pts',(-11.1188305686585,7.50015107704404,
10.631948315857));
#119302=CARTESIAN_POINT('Ctrl Pts',(-11.0920525475674,7.49442494220537,
10.553300296523));
#119303=CARTESIAN_POINT('Ctrl Pts',(-11.0631997518326,7.48934234273294,
10.4884118279321));
#119304=CARTESIAN_POINT('Ctrl Pts',(-10.9975180451698,7.47948671327182,
10.3705934060303));
#119305=CARTESIAN_POINT('Ctrl Pts',(-10.9618309628822,7.4747501169921,10.3173021175708));
#119306=CARTESIAN_POINT('Ctrl Pts',(-10.9106490697403,7.46882714053968,
10.2529086745656));
#119307=CARTESIAN_POINT('Ctrl Pts',(-10.8989794028841,7.467526384343,10.2389065214375));
#119308=CARTESIAN_POINT('Ctrl Pts',(-10.8789444381728,7.4653811941965,10.2159711389096));
#119309=CARTESIAN_POINT('Ctrl Pts',(-10.8707566983525,7.46452759484298,
10.2068875351151));
#119310=CARTESIAN_POINT('Ctrl Pts',(-10.8591039732379,7.46334646728263,
10.1943578598798));
#119311=CARTESIAN_POINT('Ctrl Pts',(-10.8557570967964,7.46301100098719,
10.190803677613));
#119312=CARTESIAN_POINT('Ctrl Pts',(-10.8500010354418,7.46244062120765,
10.1847667398202));
#119313=CARTESIAN_POINT('Ctrl Pts',(-10.8476028572891,7.46220489949364,
10.1822736237919));
#119314=CARTESIAN_POINT('Ctrl Pts',(-10.8425874696134,7.46171595909973,
10.1771054605648));
#119315=CARTESIAN_POINT('Ctrl Pts',(-10.8399684556945,7.46146288181669,
10.174432279336));
#119316=CARTESIAN_POINT('Ctrl Pts',(-10.8329566067514,7.46079112356029,
10.1673433189644));
#119317=CARTESIAN_POINT('Ctrl Pts',(-10.828541336462,7.46037412891333,10.1629497534888));
#119318=CARTESIAN_POINT('Ctrl Pts',(-10.8087647728235,7.45853165994443,
10.1435802198638));
#119319=CARTESIAN_POINT('Ctrl Pts',(-10.793029800355,7.45713271717309,10.1289895692622));
#119320=CARTESIAN_POINT('Ctrl Pts',(-10.7591678867197,7.45423697302327,
10.0992691462175));
#119321=CARTESIAN_POINT('Ctrl Pts',(-10.7409671201972,7.45274500648803,
10.0842381354397));
#119322=CARTESIAN_POINT('Ctrl Pts',(-10.7063595370843,7.44999966819764,
10.0573654423217));
#119323=CARTESIAN_POINT('Ctrl Pts',(-10.6900760472545,7.44874325700108,
10.0453802908853));
#119324=CARTESIAN_POINT('Ctrl Pts',(-10.6323821660265,7.44438448625274,
10.005163813606));
#119325=CARTESIAN_POINT('Ctrl Pts',(-10.5894865184984,7.4413024621769,9.9791612565795));
#119326=CARTESIAN_POINT('Ctrl Pts',(-10.5017013264157,7.43509494270162,
9.93333047826263));
#119327=CARTESIAN_POINT('Ctrl Pts',(-10.4569733486797,7.43197825696323,
9.91341701457162));
#119328=CARTESIAN_POINT('Ctrl Pts',(-10.400507908756,7.42802160753003,9.89238218702632));
#119329=CARTESIAN_POINT('Ctrl Pts',(-10.3898188964615,7.4272718114063,9.88857523065238));
#119330=CARTESIAN_POINT('Ctrl Pts',(-10.3726745602887,7.42606711769201,
9.88274691273329));
#119331=CARTESIAN_POINT('Ctrl Pts',(-10.3662537638086,7.42561548428398,
9.8806256362703));
#119332=CARTESIAN_POINT('Ctrl Pts',(-10.3540454888068,7.42475572592515,
9.87670859946695));
#119333=CARTESIAN_POINT('Ctrl Pts',(-10.3482617044017,7.42434796890641,
9.87490197691403));
#119334=CARTESIAN_POINT('Ctrl Pts',(-10.3350620114337,7.42341626688575,
9.87089045431234));
#119335=CARTESIAN_POINT('Ctrl Pts',(-10.3276378651401,7.42289142945741,
9.86871385491808));
#119336=CARTESIAN_POINT('Ctrl Pts',(-10.3046820964827,7.42126584643753,
9.86222863843633));
#119337=CARTESIAN_POINT('Ctrl Pts',(-10.2890836136496,7.42015735168672,
9.85816574280178));
#119338=CARTESIAN_POINT('Ctrl Pts',(-10.2022383123386,7.4139612426353,9.83743892184782));
#119339=CARTESIAN_POINT('Ctrl Pts',(-10.12965318867,7.40867713324825,9.82712518626822));
#119340=CARTESIAN_POINT('Ctrl Pts',(-10.0075903270549,7.3997241386216,9.82125311418582));
#119341=CARTESIAN_POINT('Ctrl Pts',(-9.95848786180473,7.39610887968032,
9.82195977036591));
#119342=CARTESIAN_POINT('Ctrl Pts',(-9.87668310329429,7.39016761705955,
9.82825937951728));
#119343=CARTESIAN_POINT('Ctrl Pts',(-9.84391195329899,7.38781048722023,
9.83217291710457));
#119344=CARTESIAN_POINT('Ctrl Pts',(-9.81128001650616,7.38551240301472,
9.83746835110486));
#119345=CARTESIAN_POINT('Ctrl Pts',(-9.81121465855839,7.38550780042879,
9.83747896288237));
#119346=CARTESIAN_POINT('Ctrl Pts',(-9.81114930150104,7.38550319809767,
9.83748958018586));
#119347=CARTESIAN_POINT('Ctrl Pts',(-9.81114930576479,7.28726551493505,
9.83748957949321));
#119348=CARTESIAN_POINT('Ctrl Pts',(-9.85519968856744,7.29049506618666,
9.83033356159706));
#119349=CARTESIAN_POINT('Ctrl Pts',(-9.89962266941641,7.29377134196203,
9.82568685856417));
#119350=CARTESIAN_POINT('Ctrl Pts',(-9.96506182480563,7.2985783188177,9.82258314744129));
#119351=CARTESIAN_POINT('Ctrl Pts',(-9.98594335352587,7.30010900212892,
9.82214875308509));
#119352=CARTESIAN_POINT('Ctrl Pts',(-10.028665519363,7.30322380343086,9.82239635504111));
#119353=CARTESIAN_POINT('Ctrl Pts',(-10.0504986223138,7.30480659445796,
9.82313041004437));
#119354=CARTESIAN_POINT('Ctrl Pts',(-10.0946051848168,7.30797197528952,
9.82584313524102));
#119355=CARTESIAN_POINT('Ctrl Pts',(-10.1168690011022,7.3095531131394,9.82784972143138));
#119356=CARTESIAN_POINT('Ctrl Pts',(-10.1453318261569,7.31154242376404,
9.83123416982243));
#119357=CARTESIAN_POINT('Ctrl Pts',(-10.1515938824679,7.31197808281688,
9.8320298785049));
#119358=CARTESIAN_POINT('Ctrl Pts',(-10.1615755111745,7.31266899761399,
9.83337985853362));
#119359=CARTESIAN_POINT('Ctrl Pts',(-10.1652992437233,7.31292596585307,
9.8339016502409));
#119360=CARTESIAN_POINT('Ctrl Pts',(-10.1724350044001,7.31341680734857,
9.8349364240891));
#119361=CARTESIAN_POINT('Ctrl Pts',(-10.1758473378235,7.31365082256536,
9.83544657454675));
#119362=CARTESIAN_POINT('Ctrl Pts',(-10.1840342696806,7.31421066878331,
9.83670734142605));
#119363=CARTESIAN_POINT('Ctrl Pts',(-10.1888066473296,7.31453570782569,
9.83747237715991));
#119364=CARTESIAN_POINT('Ctrl Pts',(-10.2053371266664,7.3156574503389,9.84022677520798));
#119365=CARTESIAN_POINT('Ctrl Pts',(-10.2170700803555,7.31644639406028,
9.84236539635367));
#119366=CARTESIAN_POINT('Ctrl Pts',(-10.2460487947011,7.31838152658141,
9.84810358560095));
#119367=CARTESIAN_POINT('Ctrl Pts',(-10.2632505217913,7.31951835213249,
9.85191263910326));
#119368=CARTESIAN_POINT('Ctrl Pts',(-10.3384900116516,7.32446393754164,
9.87035336972859));
#119369=CARTESIAN_POINT('Ctrl Pts',(-10.3954524098334,7.32814088329592,
9.88901151713232));
#119370=CARTESIAN_POINT('Ctrl Pts',(-10.5210572863991,7.33655651133908,
9.94104516928128));
#119371=CARTESIAN_POINT('Ctrl Pts',(-10.5883639569782,7.34130070312863,
9.97691069748441));
#119372=CARTESIAN_POINT('Ctrl Pts',(-10.6618940832352,7.34708549657348,
10.0257618417384));
#119373=CARTESIAN_POINT('Ctrl Pts',(-10.6719454745204,7.34789001319641,
10.032667054387));
#119374=CARTESIAN_POINT('Ctrl Pts',(-10.6876071293454,7.3491664871892,10.0437883563707));
#119375=CARTESIAN_POINT('Ctrl Pts',(-10.693290213132,7.34963453998412,10.0479007674953));
#119376=CARTESIAN_POINT('Ctrl Pts',(-10.7037872067802,7.35050835244923,
10.0556404515272));
#119377=CARTESIAN_POINT('Ctrl Pts',(-10.708610687845,7.35091359202307,10.0592544020934));
#119378=CARTESIAN_POINT('Ctrl Pts',(-10.7192639034136,7.35181703090415,
10.067364647811));
#119379=CARTESIAN_POINT('Ctrl Pts',(-10.7250796041024,7.35231591684206,
10.0718788730091));
#119380=CARTESIAN_POINT('Ctrl Pts',(-10.741992189509,7.35378375748748,10.0852626293453));
#119381=CARTESIAN_POINT('Ctrl Pts',(-10.7529710420379,7.35475843871651,
10.0942784943133));
#119382=CARTESIAN_POINT('Ctrl Pts',(-10.8146467945483,7.36036252513828,
10.1468233154076));
#119383=CARTESIAN_POINT('Ctrl Pts',(-10.8617215715397,7.36515688342821,
10.1943989033175));
#119384=CARTESIAN_POINT('Ctrl Pts',(-10.9498400999013,7.37520603627754,
10.3000644923196));
#119385=CARTESIAN_POINT('Ctrl Pts',(-10.9901836338833,7.380451043011,10.3584060445358));
#119386=CARTESIAN_POINT('Ctrl Pts',(-11.0357146264638,7.38706841774755,
10.4388763534742));
#119387=CARTESIAN_POINT('Ctrl Pts',(-11.0458630622127,7.38860036763467,
10.4580266320085));
#119388=CARTESIAN_POINT('Ctrl Pts',(-11.058260351626,7.3905393158012,10.4830673010665));
#119389=CARTESIAN_POINT('Ctrl Pts',(-11.060997830851,7.39097208422777,10.4887094814884));
#119390=CARTESIAN_POINT('Ctrl Pts',(-11.0653005269334,7.39165949999992,
10.4977610933084));
#119391=CARTESIAN_POINT('Ctrl Pts',(-11.066894701596,7.39191583079058,10.5011565087334));
#119392=CARTESIAN_POINT('Ctrl Pts',(-11.0699256539667,7.39240628402739,
10.5076930958745));
#119393=CARTESIAN_POINT('Ctrl Pts',(-11.0713648617547,7.39264054213048,
10.5108330283381));
#119394=CARTESIAN_POINT('Ctrl Pts',(-11.0747939922603,7.39320212287608,
10.518402125014));
#119395=CARTESIAN_POINT('Ctrl Pts',(-11.0767704049314,7.39352864057986,
10.522837411238));
#119396=CARTESIAN_POINT('Ctrl Pts',(-11.0835623263213,7.39466120180154,
10.5383363386874));
#119397=CARTESIAN_POINT('Ctrl Pts',(-11.0882353917611,7.39545928418995,
10.5494620870147));
#119398=CARTESIAN_POINT('Ctrl Pts',(-11.0994135677282,7.39742156018471,
10.5772645980097));
#119399=CARTESIAN_POINT('Ctrl Pts',(-11.1057112188219,7.39857604753192,
10.5940219427354));
#119400=CARTESIAN_POINT('Ctrl Pts',(-11.1320268859238,7.40365849175708,
10.6692068329938));
#119401=CARTESIAN_POINT('Ctrl Pts',(-11.1478140766051,7.40744723045613,
10.7290149295057));
#119402=CARTESIAN_POINT('Ctrl Pts',(-11.1720056913125,7.41584079796938,
10.8623768700391));
#119403=CARTESIAN_POINT('Ctrl Pts',(-11.1783222942617,7.42044864649759,
10.9360314579091));
#119404=CARTESIAN_POINT('Ctrl Pts',(-11.1776082779531,7.42607917376526,
11.0219468535385));
#119405=CARTESIAN_POINT('Ctrl Pts',(-11.1773189276972,7.42688144202832,
11.0341034497015));
#119406=CARTESIAN_POINT('Ctrl Pts',(-11.1765662293497,7.42815513295858,
11.0532547703275));
#119407=CARTESIAN_POINT('Ctrl Pts',(-11.1762285663683,7.42862267973525,
11.0602537857825));
#119408=CARTESIAN_POINT('Ctrl Pts',(-11.1754842984373,7.42949602241598,
11.073267038325));
#119409=CARTESIAN_POINT('Ctrl Pts',(-11.175093935262,7.4299013027302,11.0792820015953));
#119410=CARTESIAN_POINT('Ctrl Pts',(-11.174123562899,7.43080543937125,11.0926458996963));
#119411=CARTESIAN_POINT('Ctrl Pts',(-11.1735206968037,7.43130498761684,
11.0999928676837));
#119412=CARTESIAN_POINT('Ctrl Pts',(-11.1715499594041,7.43277675482695,
11.1215273945051));
#119413=CARTESIAN_POINT('Ctrl Pts',(-11.1699935045902,7.43375474703828,
11.1356959223877));
#119414=CARTESIAN_POINT('Ctrl Pts',(-11.1658590934259,7.43600272058274,
11.1679302361913));
#119415=CARTESIAN_POINT('Ctrl Pts',(-11.1631176715643,7.43727743456243,
11.185970991878));
#119416=CARTESIAN_POINT('Ctrl Pts',(-11.1523146586199,7.44167655516551,
11.2474157666236));
#119417=CARTESIAN_POINT('Ctrl Pts',(-11.1422334713113,7.44485633235953,
11.2904232018084));
#119418=CARTESIAN_POINT('Ctrl Pts',(-11.111823474531,7.45270276548694,11.3936692006648));
#119419=CARTESIAN_POINT('Ctrl Pts',(-11.0889872088971,7.45740087683083,
11.453027290922));
#119420=CARTESIAN_POINT('Ctrl Pts',(-11.0476609282709,7.4643041727149,11.5389978534609));
#119421=CARTESIAN_POINT('Ctrl Pts',(-11.0326810784807,7.46658208705166,
11.567170426086));
#119422=CARTESIAN_POINT('Ctrl Pts',(-11.0130689804116,7.46928374529891,
11.6006950156024));
#119423=CARTESIAN_POINT('Ctrl Pts',(-11.0095103536734,7.46976379370117,
11.6066565028673));
#119424=CARTESIAN_POINT('Ctrl Pts',(-11.00385034371,7.47051119774183,11.6159505379086));
#119425=CARTESIAN_POINT('Ctrl Pts',(-11.0017846720567,7.47078070836658,
11.6193044886726));
#119426=CARTESIAN_POINT('Ctrl Pts',(-10.9980844729809,7.47125764344715,
11.6252454001082));
#119427=CARTESIAN_POINT('Ctrl Pts',(-10.9964566847459,7.47146548303709,
11.627836365093));
#119428=CARTESIAN_POINT('Ctrl Pts',(-10.9925220474162,7.47196318837868,
11.6340453122912));
#119429=CARTESIAN_POINT('Ctrl Pts',(-10.9902055036909,7.47225241989804,
11.6376570665748));
#119430=CARTESIAN_POINT('Ctrl Pts',(-10.9830502392681,7.47313452422121,
11.6486799090549));
#119431=CARTESIAN_POINT('Ctrl Pts',(-10.9781475431363,7.47372341463591,
11.6560493828098));
#119432=CARTESIAN_POINT('Ctrl Pts',(-10.9664767740408,7.4750913056241,11.6731705472613));
#119433=CARTESIAN_POINT('Ctrl Pts',(-10.9596433381991,7.47586658524173,
11.6828767291657));
#119434=CARTESIAN_POINT('Ctrl Pts',(-10.9346886645188,7.47861449561872,
11.7172076523373));
#119435=CARTESIAN_POINT('Ctrl Pts',(-10.9157558950832,7.48054815310547,
11.741229463679));
#119436=CARTESIAN_POINT('Ctrl Pts',(-10.8940555415662,7.48263984738474,
11.7666602244407));
#119437=CARTESIAN_POINT('Ctrl Pts',(-10.8921947088025,7.48281826351546,
11.7688249559254));
#119438=CARTESIAN_POINT('Ctrl Pts',(-10.8404223914961,7.48775662627848,
11.828611289114));
#119439=CARTESIAN_POINT('Ctrl Pts',(-10.7850427814799,7.49239714324551,
11.8812572533082));
#119440=CARTESIAN_POINT('Ctrl Pts',(-10.6942862226725,7.49967331736426,
11.9521433423309));
#119441=CARTESIAN_POINT('Ctrl Pts',(-10.6624424479499,7.50217150830225,
11.9745664828692));
#119442=CARTESIAN_POINT('Ctrl Pts',(-10.6202249413218,7.50545382701069,
12.0012681013186));
#119443=CARTESIAN_POINT('Ctrl Pts',(-10.6108183454274,7.50618328233104,
12.0070341225404));
#119444=CARTESIAN_POINT('Ctrl Pts',(-10.5955775155201,7.50736291227459,
12.016084288828));
#119445=CARTESIAN_POINT('Ctrl Pts',(-10.5897937219677,7.50781006015288,
12.0194524125259));
#119446=CARTESIAN_POINT('Ctrl Pts',(-10.578708259231,7.50866627415854,12.0257819884076));
#119447=CARTESIAN_POINT('Ctrl Pts',(-10.5734117632605,7.50907501513885,
12.0287521005717));
#119448=CARTESIAN_POINT('Ctrl Pts',(-10.5612085408018,7.51001609675676,
12.0354717746911));
#119449=CARTESIAN_POINT('Ctrl Pts',(-10.5542868419995,7.51054939804968,
12.0391933958879));
#119450=CARTESIAN_POINT('Ctrl Pts',(-10.5324697879892,7.51222915989967,
12.0506438916526));
#119451=CARTESIAN_POINT('Ctrl Pts',(-10.5174467435795,7.51338413810669,
12.0581235653549));
#119452=CARTESIAN_POINT('Ctrl Pts',(-10.4818708143132,7.51611668590152,
12.074897296537));
#119453=CARTESIAN_POINT('Ctrl Pts',(-10.4612011343202,7.51770242286672,
12.0839266946263));
#119454=CARTESIAN_POINT('Ctrl Pts',(-10.3815467789936,7.52380608128021,
12.1160322389629));
#119455=CARTESIAN_POINT('Ctrl Pts',(-10.3209992249661,7.52843811462932,
12.1349289940568));
#119456=CARTESIAN_POINT('Ctrl Pts',(-10.1984958244323,7.53765444871598,
12.162571007012));
#119457=CARTESIAN_POINT('Ctrl Pts',(-10.1367611806452,7.54222271828028,
12.1714391992568));
#119458=CARTESIAN_POINT('Ctrl Pts',(-10.065038971152,7.54726795199432,12.1759919068787));
#119459=CARTESIAN_POINT('Ctrl Pts',(-10.0554606768047,7.54793624946695,
12.1764825372595));
#119460=CARTESIAN_POINT('Ctrl Pts',(-10.040835873149,7.54894725611489,12.1770526523838));
#119461=CARTESIAN_POINT('Ctrl Pts',(-10.0357933267798,7.54929414203913,
12.1772167833914));
#119462=CARTESIAN_POINT('Ctrl Pts',(-10.0272972263487,7.54987556429548,
12.1774386829497));
#119463=CARTESIAN_POINT('Ctrl Pts',(-10.0238442272722,7.55011102054624,
12.1775136706962));
#119464=CARTESIAN_POINT('Ctrl Pts',(-10.0167188985909,7.55059508007801,
12.1776370528487));
#119465=CARTESIAN_POINT('Ctrl Pts',(-10.0130466006967,7.55084357435315,
12.1776834621215));
#119466=CARTESIAN_POINT('Ctrl Pts',(-10.0034589443997,7.55148991746841,
12.1777597757095));
#119467=CARTESIAN_POINT('Ctrl Pts',(-9.99754338211674,7.55188629801649,
12.1777622944516));
#119468=CARTESIAN_POINT('Ctrl Pts',(-9.97103455058822,7.55365275776168,
12.1775738502062));
#119469=CARTESIAN_POINT('Ctrl Pts',(-9.95044706365898,7.55499814457705,
12.1768873352899));
#119470=CARTESIAN_POINT('Ctrl Pts',(-9.89091325727442,7.55883910554718,
12.173336899003));
#119471=CARTESIAN_POINT('Ctrl Pts',(-9.85207646255803,7.56128363162729,
12.1690759062038));
#119472=CARTESIAN_POINT('Ctrl Pts',(-9.71882008265134,7.56966748959021,
12.1477071532082));
#119473=CARTESIAN_POINT('Ctrl Pts',(-9.62633860911317,7.57551203807908,
12.1210126936489));
#119474=CARTESIAN_POINT('Ctrl Pts',(-9.52243717642316,7.58285116080175,
12.0767169669674));
#119475=CARTESIAN_POINT('Ctrl Pts',(-9.50690307542164,7.5839689833877,12.0696920363489));
#119476=CARTESIAN_POINT('Ctrl Pts',(-9.48447152168634,7.58561625695119,
12.0589554493254));
#119477=CARTESIAN_POINT('Ctrl Pts',(-9.47744948836911,7.58613674611029,
12.055508035726));
#119478=CARTESIAN_POINT('Ctrl Pts',(-9.46502701671613,7.58706640900151,
12.0492549735298));
#119479=CARTESIAN_POINT('Ctrl Pts',(-9.45961295183891,7.58747461999549,
12.0464769123747));
#119480=CARTESIAN_POINT('Ctrl Pts',(-9.44833207440883,7.58833168439508,
12.0405775905508));
#119481=CARTESIAN_POINT('Ctrl Pts',(-9.4424696800644,7.58878080374154,12.0374483897113));
#119482=CARTESIAN_POINT('Ctrl Pts',(-9.42713881994972,7.58996530641948,
12.0290976841812));
#119483=CARTESIAN_POINT('Ctrl Pts',(-9.41771541816138,7.59070351455073,
12.0237952077635));
#119484=CARTESIAN_POINT('Ctrl Pts',(-9.37285404803744,7.59426786783325,
11.9977323394992));
#119485=CARTESIAN_POINT('Ctrl Pts',(-9.33844906745561,7.59715447376726,
11.9752597279124));
#119486=CARTESIAN_POINT('Ctrl Pts',(-9.2663042472857,7.60355106637837,11.9225598214281));
#119487=CARTESIAN_POINT('Ctrl Pts',(-9.2291083232013,7.60707620518142,11.8917126486717));
#119488=CARTESIAN_POINT('Ctrl Pts',(-9.14346779251222,7.61569333340251,
11.8113167829369));
#119489=CARTESIAN_POINT('Ctrl Pts',(-9.09728945122025,7.62079035646171,
11.7596036505155));
#119490=CARTESIAN_POINT('Ctrl Pts',(-9.04969565487249,7.62637619838662,
11.6957908910849));
#119491=CARTESIAN_POINT('Ctrl Pts',(-9.04358583168573,7.62710037947976,
11.6873683653177));
#119492=CARTESIAN_POINT('Ctrl Pts',(-9.03497745913946,7.62812983576394,
11.6751644780727));
#119493=CARTESIAN_POINT('Ctrl Pts',(-9.03238806292291,7.6284407231772,11.6714482241731));
#119494=CARTESIAN_POINT('Ctrl Pts',(-9.02788334532991,7.62898360895538,
11.664902957135));
#119495=CARTESIAN_POINT('Ctrl Pts',(-9.02595879918785,7.62921620872815,
11.6620804128033));
#119496=CARTESIAN_POINT('Ctrl Pts',(-9.02188287935203,7.62971020831165,
11.6560464170241));
#119497=CARTESIAN_POINT('Ctrl Pts',(-9.01973501082036,7.62997138056356,
11.6528327159842));
#119498=CARTESIAN_POINT('Ctrl Pts',(-9.01385645676312,7.63068872759903,
11.6439426312588));
#119499=CARTESIAN_POINT('Ctrl Pts',(-9.01015892465356,7.63114279313097,
11.6382443506753));
#119500=CARTESIAN_POINT('Ctrl Pts',(-8.98903637209678,7.63375546439494,
11.605067187394));
#119501=CARTESIAN_POINT('Ctrl Pts',(-8.97270506931862,7.63585102708472,
11.5769049397346));
#119502=CARTESIAN_POINT('Ctrl Pts',(-8.93537468170182,7.64093077034107,
11.5059056353345));
#119503=CARTESIAN_POINT('Ctrl Pts',(-8.91577075809617,7.64387146857802,
11.4624013351057));
#119504=CARTESIAN_POINT('Ctrl Pts',(-8.87221479830077,7.65146665784319,
11.3476136721635));
#119505=CARTESIAN_POINT('Ctrl Pts',(-8.85235207913066,7.65612610292347,
11.2750221382633));
#119506=CARTESIAN_POINT('Ctrl Pts',(-8.83678949046423,7.66205958569363,
11.1851893731293));
#119507=CARTESIAN_POINT('Ctrl Pts',(-8.83436889751725,7.66311553004509,
11.1692864021845));
#119508=CARTESIAN_POINT('Ctrl Pts',(-8.83126851799267,7.66469379887375,
11.1456760963642));
#119509=CARTESIAN_POINT('Ctrl Pts',(-8.83033769030074,7.6652083439785,11.138003183303));
#119510=CARTESIAN_POINT('Ctrl Pts',(-8.82881223362302,7.66613032160656,
11.124301917761));
#119511=CARTESIAN_POINT('Ctrl Pts',(-8.82818845768339,7.6665368347176,11.1182770384605));
#119512=CARTESIAN_POINT('Ctrl Pts',(-8.82696661147169,7.6674003327857,11.105515274149));
#119513=CARTESIAN_POINT('Ctrl Pts',(-8.82638004490823,7.66785765906529,
11.098777534894));
#119514=CARTESIAN_POINT('Ctrl Pts',(-8.82496405541385,7.6690878189272,11.0807129117521));
#119515=CARTESIAN_POINT('Ctrl Pts',(-8.82424040485695,7.66986388469948,
11.0693786996952));
#119516=CARTESIAN_POINT('Ctrl Pts',(-8.82125961410012,7.67402449811763,
11.0089618284884));
#119517=CARTESIAN_POINT('Ctrl Pts',(-8.82191202652291,7.67749727327642,
10.9597907772295));
#119518=CARTESIAN_POINT('Ctrl Pts',(-8.82941569685543,7.68464166316884,
10.8609901001067));
#119519=CARTESIAN_POINT('Ctrl Pts',(-8.83636553731358,7.68830854309182,
10.8114644394558));
#119520=CARTESIAN_POINT('Ctrl Pts',(-8.85814964154146,7.69623600287555,
10.705642174287));
#119521=CARTESIAN_POINT('Ctrl Pts',(-8.87405463299841,7.70048627949963,
10.6496899507921));
#119522=CARTESIAN_POINT('Ctrl Pts',(-8.89759233310584,7.70529304353014,
10.585391678394));
#119523=CARTESIAN_POINT('Ctrl Pts',(-8.90128796778085,7.70601565032005,
10.5756951415607));
#119524=CARTESIAN_POINT('Ctrl Pts',(-8.90667533106688,7.70702415877659,
10.5621024705801));
#119525=CARTESIAN_POINT('Ctrl Pts',(-8.90826058794254,7.70731576572947,
10.5581650358792));
#119526=CARTESIAN_POINT('Ctrl Pts',(-8.91112371990633,7.70783327095792,
10.551163134539));
#119527=CARTESIAN_POINT('Ctrl Pts',(-8.912393327851,7.70805964474647,10.5480953498713));
#119528=CARTESIAN_POINT('Ctrl Pts',(-8.91504615305489,7.70852623311223,
10.5417612041035));
#119529=CARTESIAN_POINT('Ctrl Pts',(-8.91643118149428,7.70876633724323,
10.5384956549827));
#119530=CARTESIAN_POINT('Ctrl Pts',(-8.91930226314544,7.70925705610649,
10.5318105458603));
#119531=CARTESIAN_POINT('Ctrl Pts',(-8.92078984500464,7.70950757811946,
10.5283916819095));
#119532=CARTESIAN_POINT('Ctrl Pts',(-8.92448126239604,7.71012032178206,
10.5200167441402));
#119533=CARTESIAN_POINT('Ctrl Pts',(-8.92670317118583,7.71048152960302,
10.5150686638693));
#119534=CARTESIAN_POINT('Ctrl Pts',(-8.95226235995247,7.71455366154662,
10.4591859432606));
#119535=CARTESIAN_POINT('Ctrl Pts',(-8.97917475356925,7.71807387587225,
10.4099563264487));
#119536=CARTESIAN_POINT('Ctrl Pts',(-9.06038939496961,7.72740206881303,
10.2837060232455));
#119537=CARTESIAN_POINT('Ctrl Pts',(-9.12057561909425,7.73313321001146,
10.2109774769063));
#119538=CARTESIAN_POINT('Ctrl Pts',(-9.20205894599789,7.74041699659072,
10.1335583518798));
#119539=CARTESIAN_POINT('Ctrl Pts',(-9.21563977005296,7.74161636475479,
10.1212451842009));
#119540=CARTESIAN_POINT('Ctrl Pts',(-9.23519198608419,7.74332642162918,
10.1043324453351));
#119541=CARTESIAN_POINT('Ctrl Pts',(-9.24092906785537,7.7438262339833,10.0994651687764));
#119542=CARTESIAN_POINT('Ctrl Pts',(-9.25103840866681,7.74470380011763,
10.091053758916));
#119543=CARTESIAN_POINT('Ctrl Pts',(-9.25539021628676,7.74508056689302,
10.0874853411548));
#119544=CARTESIAN_POINT('Ctrl Pts',(-9.26460000058779,7.74587593122935,
10.0800432034653));
#119545=CARTESIAN_POINT('Ctrl Pts',(-9.26946337762514,7.74629478924844,
10.0761764738583));
#119546=CARTESIAN_POINT('Ctrl Pts',(-9.28123504540855,7.74730602109766,
10.0669682447641));
#119547=CARTESIAN_POINT('Ctrl Pts',(-9.28817250584574,7.74789985363187,
10.0616648105928));
#119548=CARTESIAN_POINT('Ctrl Pts',(-9.31281159390732,7.75000195286584,
10.0432596235438));
#119549=CARTESIAN_POINT('Ctrl Pts',(-9.33082013478496,7.75152601215833,
10.030578394585));
#119550=CARTESIAN_POINT('Ctrl Pts',(-9.37629158006102,7.75534672433294,
10.0004292816455));
#119551=CARTESIAN_POINT('Ctrl Pts',(-9.4041418877605,7.75766335513131,9.98358147941796));
#119552=CARTESIAN_POINT('Ctrl Pts',(-9.51802792521591,7.76703341137145,
9.9209774561804));
#119553=CARTESIAN_POINT('Ctrl Pts',(-9.60889009110396,7.77432048683787,
9.88482364980576));
#119554=CARTESIAN_POINT('Ctrl Pts',(-9.72109540292787,7.78258184088193,
9.85560029742336));
#119555=CARTESIAN_POINT('Ctrl Pts',(-9.73913697270404,7.78388717627685,
9.85135339313152));
#119556=CARTESIAN_POINT('Ctrl Pts',(-9.76293297006085,7.78557253689137,
9.84634158046878));
#119557=CARTESIAN_POINT('Ctrl Pts',(-9.76860237037194,7.78597138913534,
9.84519106945274));
#119558=CARTESIAN_POINT('Ctrl Pts',(-9.77790713634475,7.7866213515191,9.8433740972194));
#119559=CARTESIAN_POINT('Ctrl Pts',(-9.7815374884962,7.78687378639935,9.84268290814946));
#119560=CARTESIAN_POINT('Ctrl Pts',(-9.78833478544891,7.78734419957058,
9.84142188314543));
#119561=CARTESIAN_POINT('Ctrl Pts',(-9.79150087649421,7.7875624007946,9.84084792556047));
#119562=CARTESIAN_POINT('Ctrl Pts',(-9.79724441442967,7.78795664395391,
9.83983101487458));
#119563=CARTESIAN_POINT('Ctrl Pts',(-9.7998210595927,7.78813292929592,9.83938365784728));
#119564=CARTESIAN_POINT('Ctrl Pts',(-9.80531730704864,7.78850777249613,
9.83844824758667));
#119565=CARTESIAN_POINT('Ctrl Pts',(-9.80822746519122,7.78870553243243,
9.83796423470817));
#119566=CARTESIAN_POINT('Ctrl Pts',(-9.81114930150281,7.78890339972193,
9.83748958018557));
#119567=CARTESIAN_POINT('Origin',(-10.,2.67563288526385,11.));
#119568=CARTESIAN_POINT('',(-9.81114929946799,8.38697610116908,9.83748958051613));
#119569=CARTESIAN_POINT('',(-9.81114931542107,8.28715739324099,9.83748957792454));
#119570=CARTESIAN_POINT('',(-9.81114930150157,2.67563288526385,9.83748958018577));
#119571=CARTESIAN_POINT('Ctrl Pts',(-9.8111492994685,8.3869761011691,9.83748958051605));
#119572=CARTESIAN_POINT('Ctrl Pts',(-9.77556036952072,8.38472373587762,
9.84327102921462));
#119573=CARTESIAN_POINT('Ctrl Pts',(-9.74026784148269,8.38244840423991,
9.85068108673375));
#119574=CARTESIAN_POINT('Ctrl Pts',(-9.68692738278437,8.37890183676023,
9.8644634933903));
#119575=CARTESIAN_POINT('Ctrl Pts',(-9.66861095479658,8.37766427285661,
9.86967311841689));
#119576=CARTESIAN_POINT('Ctrl Pts',(-9.64275823187661,8.37588497099228,
9.87770863089574));
#119577=CARTESIAN_POINT('Ctrl Pts',(-9.63511160246356,8.37535460048461,
9.88017141926841));
#119578=CARTESIAN_POINT('Ctrl Pts',(-9.6217623689767,8.37442117849832,9.88462211737458));
#119579=CARTESIAN_POINT('Ctrl Pts',(-9.6160486859111,8.37401922603431,9.88657604089253));
#119580=CARTESIAN_POINT('Ctrl Pts',(-9.60455850842549,8.37320584571282,
9.89060432757954));
#119581=CARTESIAN_POINT('Ctrl Pts',(-9.59878270410538,8.37279438344432,
9.89268007771308));
#119582=CARTESIAN_POINT('Ctrl Pts',(-9.58691541141096,8.37194347296274,
9.89705006792086));
#119583=CARTESIAN_POINT('Ctrl Pts',(-9.58082620253724,8.37150385416781,
9.89934984913751));
#119584=CARTESIAN_POINT('Ctrl Pts',(-9.56526729835222,8.37037265699688,
9.9053739982479));
#119585=CARTESIAN_POINT('Ctrl Pts',(-9.55582640437731,8.36967870390447,
9.90917076896322));
#119586=CARTESIAN_POINT('Ctrl Pts',(-9.5180330990935,8.36686937528555,9.92494177682027));
#119587=CARTESIAN_POINT('Ctrl Pts',(-9.4901080344637,8.36472155024413,9.93790200046723));
#119588=CARTESIAN_POINT('Ctrl Pts',(-9.42177525925837,8.35927994148038,
9.97293197492884));
#119589=CARTESIAN_POINT('Ctrl Pts',(-9.38209521749148,8.35594890082038,
9.99630406285483));
#119590=CARTESIAN_POINT('Ctrl Pts',(-9.29923127863222,8.34865344932402,
10.0518914572739));
#119591=CARTESIAN_POINT('Ctrl Pts',(-9.25667919725604,8.34468453681421,
10.0848711012418));
#119592=CARTESIAN_POINT('Ctrl Pts',(-9.19056427301779,8.33826278624568,
10.1437767738638));
#119593=CARTESIAN_POINT('Ctrl Pts',(-9.16563388113863,8.33577371902835,
10.16805163265));
#119594=CARTESIAN_POINT('Ctrl Pts',(-9.13707791139942,8.33287440325377,
10.1984338343264));
#119595=CARTESIAN_POINT('Ctrl Pts',(-9.13238786957444,8.3323965710423,10.2035126831959));
#119596=CARTESIAN_POINT('Ctrl Pts',(-9.12512747193593,8.33165467008442,
10.2115152059889));
#119597=CARTESIAN_POINT('Ctrl Pts',(-9.12252652107469,8.33138844359755,
10.2144107271394));
#119598=CARTESIAN_POINT('Ctrl Pts',(-9.11767294706688,8.33089088485827,
10.2198681708174));
#119599=CARTESIAN_POINT('Ctrl Pts',(-9.11541710650467,8.33065932822984,
10.2224269782662));
#119600=CARTESIAN_POINT('Ctrl Pts',(-9.11022037385239,8.33012513256885,
10.2283735336706));
#119601=CARTESIAN_POINT('Ctrl Pts',(-9.10728768184697,8.32982308646122,
10.2317683257603));
#119602=CARTESIAN_POINT('Ctrl Pts',(-9.09778120315093,8.32884175804199,
10.2429006760444));
#119603=CARTESIAN_POINT('Ctrl Pts',(-9.09128784721195,8.32816794276472,
10.2507067436001));
#119604=CARTESIAN_POINT('Ctrl Pts',(-9.03833882936707,8.32263438755876,
10.3160609457134));
#119605=CARTESIAN_POINT('Ctrl Pts',(-8.99729122596342,8.31808389526572,
10.3777918201091));
#119606=CARTESIAN_POINT('Ctrl Pts',(-8.93610866554592,8.31008150545563,
10.4917701897934));
#119607=CARTESIAN_POINT('Ctrl Pts',(-8.9133907729591,8.30665195128781,10.5423515549895));
#119608=CARTESIAN_POINT('Ctrl Pts',(-8.88710858139322,8.30178917390322,
10.613987410639));
#119609=CARTESIAN_POINT('Ctrl Pts',(-8.88042563402193,8.30044269590367,
10.6338221867075));
#119610=CARTESIAN_POINT('Ctrl Pts',(-8.86964874752022,8.29805556156961,
10.6688673625453));
#119611=CARTESIAN_POINT('Ctrl Pts',(-8.86532479772586,8.29702210101917,
10.6840017008985));
#119612=CARTESIAN_POINT('Ctrl Pts',(-8.85941664178613,8.29548879372607,
10.7063686473337));
#119613=CARTESIAN_POINT('Ctrl Pts',(-8.85759515350955,8.29499648629831,
10.7135372086045));
#119614=CARTESIAN_POINT('Ctrl Pts',(-8.8558231761747,8.29449691210722,10.7207967332053));
#119615=CARTESIAN_POINT('Ctrl Pts',(-8.85580501912333,8.29449179080672,
10.7208711514294));
#119616=CARTESIAN_POINT('Ctrl Pts',(-8.85576792481073,8.29448132348796,
10.721023250071));
#119617=CARTESIAN_POINT('Ctrl Pts',(-8.85574898819711,8.29447597744853,
10.721100930656));
#119618=CARTESIAN_POINT('Ctrl Pts',(-8.85571029619013,8.29446504914115,
10.7212597208443));
#119619=CARTESIAN_POINT('Ctrl Pts',(-8.85569054151254,8.29445946685143,
10.7213408306099));
#119620=CARTESIAN_POINT('Ctrl Pts',(-8.85565017259324,8.29444805383541,
10.7215066560655));
#119621=CARTESIAN_POINT('Ctrl Pts',(-8.85562955913633,8.29444222308487,
10.7215913719383));
#119622=CARTESIAN_POINT('Ctrl Pts',(-8.85558742951142,8.29443030019162,
10.7217645973198));
#119623=CARTESIAN_POINT('Ctrl Pts',(-8.85556591420485,8.29442420802198,
10.7218531070332));
#119624=CARTESIAN_POINT('Ctrl Pts',(-8.85552193521963,8.29441174853525,
10.7220341193636));
#119625=CARTESIAN_POINT('Ctrl Pts',(-8.85549947248842,8.29440538118856,
10.7221266222053));
#119626=CARTESIAN_POINT('Ctrl Pts',(-8.85545355033533,8.29439235674162,
10.7223158323515));
#119627=CARTESIAN_POINT('Ctrl Pts',(-8.8554300919517,8.29438569960754,10.7224125399213));
#119628=CARTESIAN_POINT('Ctrl Pts',(-8.85538212732569,8.29437208006286,
10.722610384326));
#119629=CARTESIAN_POINT('Ctrl Pts',(-8.85535762223406,8.29436511761703,
10.722711521423));
#119630=CARTESIAN_POINT('Ctrl Pts',(-8.85530751003482,8.29435087095634,
10.722918463683));
#119631=CARTESIAN_POINT('Ctrl Pts',(-8.85528190419233,8.2943435867017,10.7230242691482));
#119632=CARTESIAN_POINT('Ctrl Pts',(-8.85522953315601,8.29432867889302,
10.7232408019257));
#119633=CARTESIAN_POINT('Ctrl Pts',(-8.85520276935465,8.29432105529422,
10.7233515295838));
#119634=CARTESIAN_POINT('Ctrl Pts',(-8.85514802169724,8.29430545015865,
10.7235781765189));
#119635=CARTESIAN_POINT('Ctrl Pts',(-8.85512003938032,8.29429746857302,
10.723694096169));
#119636=CARTESIAN_POINT('Ctrl Pts',(-8.8550627904312,8.29428112764478,10.7239314138862));
#119637=CARTESIAN_POINT('Ctrl Pts',(-8.8550335255047,8.2942727682497,10.724052812343));
#119638=CARTESIAN_POINT('Ctrl Pts',(-8.85497364334648,8.29425565063358,
10.7243013924929));
#119639=CARTESIAN_POINT('Ctrl Pts',(-8.85494302799789,8.29424689235375,
10.7244285746273));
#119640=CARTESIAN_POINT('Ctrl Pts',(-8.85488037307807,8.29422895456967,
10.7246890461119));
#119641=CARTESIAN_POINT('Ctrl Pts',(-8.854848335588,8.29421977499969,10.7248223359591));
#119642=CARTESIAN_POINT('Ctrl Pts',(-8.85479779340273,8.29420528166352,
10.7250327750455));
#119643=CARTESIAN_POINT('Ctrl Pts',(-8.85477927322158,8.2941999683856,10.7251099206018));
#119644=CARTESIAN_POINT('Ctrl Pts',(-8.85473760971123,8.29418800989958,
10.7252835466628));
#119645=CARTESIAN_POINT('Ctrl Pts',(-8.85471447078386,8.29418136455375,
10.7253800281986));
#119646=CARTESIAN_POINT('Ctrl Pts',(-8.85466241491039,8.29416640570187,
10.7255972046706));
#119647=CARTESIAN_POINT('Ctrl Pts',(-8.85463350485297,8.29415809197843,
10.7257179012439));
#119648=CARTESIAN_POINT('Ctrl Pts',(-8.85456846424777,8.29413937440689,
10.7259896288093));
#119649=CARTESIAN_POINT('Ctrl Pts',(-8.85453234449702,8.29412897021821,
10.7261406623607));
#119650=CARTESIAN_POINT('Ctrl Pts',(-8.85445108493201,8.29410554213005,
10.7264807438894));
#119651=CARTESIAN_POINT('Ctrl Pts',(-8.85440596204729,8.2940925176959,10.7266697958807));
#119652=CARTESIAN_POINT('Ctrl Pts',(-8.85430445601056,8.2940631848596,10.7270955438495));
#119653=CARTESIAN_POINT('Ctrl Pts',(-8.85424809941994,8.2940468756198,10.7273322460922));
#119654=CARTESIAN_POINT('Ctrl Pts',(-8.85415859059837,8.29402093487177,
10.7277087081224));
#119655=CARTESIAN_POINT('Ctrl Pts',(-8.85412539055327,8.29401130487389,
10.7278484566327));
#119656=CARTESIAN_POINT('Ctrl Pts',(-8.85396192671454,8.29396385005024,
10.7285370829823));
#119657=CARTESIAN_POINT('Ctrl Pts',(-8.85383203190104,8.29392601357968,
10.7290860475398));
#119658=CARTESIAN_POINT('Ctrl Pts',(-8.85230338138177,8.29347923570598,
10.7355672447981));
#119659=CARTESIAN_POINT('Ctrl Pts',(-8.85095032377587,8.29306885722141,
10.7415100590245));
#119660=CARTESIAN_POINT('Ctrl Pts',(-8.84795378748113,8.29212451211253,
10.7551598816575));
#119661=CARTESIAN_POINT('Ctrl Pts',(-8.84634142619944,8.29158958243961,
10.7628733477612));
#119662=CARTESIAN_POINT('Ctrl Pts',(-8.84222839638118,8.29014948708989,
10.7835856035655));
#119663=CARTESIAN_POINT('Ctrl Pts',(-8.83986932894413,8.28923995025461,
10.7966110167332));
#119664=CARTESIAN_POINT('Ctrl Pts',(-8.82209528764146,8.28162592791745,
10.905151717001));
#119665=CARTESIAN_POINT('Ctrl Pts',(-8.81828779635137,8.27455055149884,
11.0021763687677));
#119666=CARTESIAN_POINT('Ctrl Pts',(-8.8298185325078,8.2644435196521,11.139494176537));
#119667=CARTESIAN_POINT('Ctrl Pts',(-8.83539712749543,8.2614401490568,11.1802327814251));
#119668=CARTESIAN_POINT('Ctrl Pts',(-8.84707469331223,8.25698293784529,
11.2414745303275));
#119669=CARTESIAN_POINT('Ctrl Pts',(-8.85161993797699,8.25548208385647,
11.2622405022161));
#119670=CARTESIAN_POINT('Ctrl Pts',(-8.85816116729086,8.25359407535006,
11.2886778389005));
#119671=CARTESIAN_POINT('Ctrl Pts',(-8.85964150301728,8.25318175958601,
11.2944712493583));
#119672=CARTESIAN_POINT('Ctrl Pts',(-8.86210596052712,8.25251907086765,
11.3038187179651));
#119673=CARTESIAN_POINT('Ctrl Pts',(-8.86306274081926,8.25226721492617,
11.307379778266));
#119674=CARTESIAN_POINT('Ctrl Pts',(-8.86494629057716,8.25178178587113,
11.3142610717138));
#119675=CARTESIAN_POINT('Ctrl Pts',(-8.86587093115574,8.25154810356121,
11.3175818005444));
#119676=CARTESIAN_POINT('Ctrl Pts',(-8.86817379814349,8.25097714500599,
11.3257139228676));
#119677=CARTESIAN_POINT('Ctrl Pts',(-8.86956816086632,8.25064077735985,
11.3305207558966));
#119678=CARTESIAN_POINT('Ctrl Pts',(-8.87367881022585,8.24967511525845,
11.3443611763634));
#119679=CARTESIAN_POINT('Ctrl Pts',(-8.87647310695524,8.24904997251947,
11.3533714425046));
#119680=CARTESIAN_POINT('Ctrl Pts',(-8.90036742997673,8.24394443481163,
11.4272689157817));
#119681=CARTESIAN_POINT('Ctrl Pts',(-8.92696433820455,8.23972572386603,
11.4902524749306));
#119682=CARTESIAN_POINT('Ctrl Pts',(-8.98652447135822,8.2318437015954,11.6028778939458));
#119683=CARTESIAN_POINT('Ctrl Pts',(-9.01807750091479,8.22819215501801,
11.6530099510619));
#119684=CARTESIAN_POINT('Ctrl Pts',(-9.06618489197308,8.22304524692729,
11.7180225855625));
#119685=CARTESIAN_POINT('Ctrl Pts',(-9.0795883688967,8.22164907248295,11.7351254544231));
#119686=CARTESIAN_POINT('Ctrl Pts',(-9.10386867223547,8.21917469201588,
11.7644015508209));
#119687=CARTESIAN_POINT('Ctrl Pts',(-9.11453998748962,8.21810426192985,
11.7767378011318));
#119688=CARTESIAN_POINT('Ctrl Pts',(-9.13066974467157,8.21650840800628,
11.794619648124));
#119689=CARTESIAN_POINT('Ctrl Pts',(-9.13593276951992,8.21599102097178,
11.8003394869624));
#119690=CARTESIAN_POINT('Ctrl Pts',(-9.14540153482438,8.21506578495448,
11.810427844803));
#119691=CARTESIAN_POINT('Ctrl Pts',(-9.14958516104849,8.21465887888075,
11.8148168061963));
#119692=CARTESIAN_POINT('Ctrl Pts',(-9.15849164908155,8.21379646346055,
11.8240171176682));
#119693=CARTESIAN_POINT('Ctrl Pts',(-9.16322229207724,8.2133406271567,11.8288205952672));
#119694=CARTESIAN_POINT('Ctrl Pts',(-9.17595825122229,8.21211913328534,
11.84153246103));
#119695=CARTESIAN_POINT('Ctrl Pts',(-9.18403593992989,8.21135032390752,
11.8493670138083));
#119696=CARTESIAN_POINT('Ctrl Pts',(-9.22257998300997,8.20770814724297,
11.88569358494));
#119697=CARTESIAN_POINT('Ctrl Pts',(-9.25443044085048,8.20477275739549,
11.9126665983159));
#119698=CARTESIAN_POINT('Ctrl Pts',(-9.37506482398508,8.19391375305726,
12.0042923467936));
#119699=CARTESIAN_POINT('Ctrl Pts',(-9.47133148950188,8.18566358757108,
12.0581368006178));
#119700=CARTESIAN_POINT('Ctrl Pts',(-9.58318148769671,8.17716659114382,
12.1015724456768));
#119701=CARTESIAN_POINT('Ctrl Pts',(-9.59275712701194,8.17644782570462,
12.1051483083695));
#119702=CARTESIAN_POINT('Ctrl Pts',(-9.60979913204881,8.17518534133158,
12.1112607684766));
#119703=CARTESIAN_POINT('Ctrl Pts',(-9.61724659686887,8.1746392171673,12.1138478593024));
#119704=CARTESIAN_POINT('Ctrl Pts',(-9.62860371626302,8.17381544488009,
12.1176657161515));
#119705=CARTESIAN_POINT('Ctrl Pts',(-9.63249456933567,8.17353483024211,
12.1189511215168));
#119706=CARTESIAN_POINT('Ctrl Pts',(-9.63961275152208,8.17302447771851,
12.1212615925268));
#119707=CARTESIAN_POINT('Ctrl Pts',(-9.6428378243459,8.17279438756758,12.1222930582728));
#119708=CARTESIAN_POINT('Ctrl Pts',(-9.65014179218854,8.17227583701901,
12.1245943914682));
#119709=CARTESIAN_POINT('Ctrl Pts',(-9.65422318333184,8.17198785130665,
12.1258559878503));
#119710=CARTESIAN_POINT('Ctrl Pts',(-9.66483521445962,8.17124344131276,
12.1290731155613));
#119711=CARTESIAN_POINT('Ctrl Pts',(-9.67137623671441,8.17078889490343,
12.1309942357473));
#119712=CARTESIAN_POINT('Ctrl Pts',(-9.72293768046522,8.16723676432551,
12.1456529070027));
#119713=CARTESIAN_POINT('Ctrl Pts',(-9.76866986137388,8.16427046876545,
12.1557558409163));
#119714=CARTESIAN_POINT('Ctrl Pts',(-9.83105704888142,8.16032424278019,
12.1656849631472));
#119715=CARTESIAN_POINT('Ctrl Pts',(-9.84727920570528,8.15930722514059,
12.1679210288769));
#119716=CARTESIAN_POINT('Ctrl Pts',(-9.91376978636862,8.1551586412886,12.1756770283791));
#119717=CARTESIAN_POINT('Ctrl Pts',(-9.96432054234315,8.15204853487959,
12.1782949303744));
#119718=CARTESIAN_POINT('Ctrl Pts',(-10.0631460941493,8.1458502025093,12.1770460461663));
#119719=CARTESIAN_POINT('Ctrl Pts',(-10.1113214028668,8.14277339313188,
12.1734698690164));
#119720=CARTESIAN_POINT('Ctrl Pts',(-10.1703416913516,8.13886170294202,
12.1654212255078));
#119721=CARTESIAN_POINT('Ctrl Pts',(-10.1815226915575,8.13811442629396,
12.1637321094811));
#119722=CARTESIAN_POINT('Ctrl Pts',(-10.1993400586989,8.13691282746779,
12.1607774189109));
#119723=CARTESIAN_POINT('Ctrl Pts',(-10.2059930411572,8.13646173958394,
12.1596152547496));
#119724=CARTESIAN_POINT('Ctrl Pts',(-10.2185969903339,8.13560240739732,
12.1573016696628));
#119725=CARTESIAN_POINT('Ctrl Pts',(-10.2245498017528,8.13519452576914,
12.1561614000505));
#119726=CARTESIAN_POINT('Ctrl Pts',(-10.2380950000418,8.13426167991051,
12.1534582429777));
#119727=CARTESIAN_POINT('Ctrl Pts',(-10.2456812241632,8.1337358150676,12.1518662589303));
#119728=CARTESIAN_POINT('Ctrl Pts',(-10.2690688831002,8.13210377290235,
12.1467167623073));
#119729=CARTESIAN_POINT('Ctrl Pts',(-10.2848124915868,8.13098975698842,
12.1429082186581));
#119730=CARTESIAN_POINT('Ctrl Pts',(-10.3698947637703,8.12488238159755,
12.1204588314285));
#119731=CARTESIAN_POINT('Ctrl Pts',(-10.4374857565018,8.11970071870876,
12.0958344744591));
#119732=CARTESIAN_POINT('Ctrl Pts',(-10.5476141593115,8.11078291768397,
12.0438929028704));
#119733=CARTESIAN_POINT('Ctrl Pts',(-10.5914213181272,8.10709812416089,
12.0197130373406));
#119734=CARTESIAN_POINT('Ctrl Pts',(-10.6616120180867,8.10106717299453,
11.974921507908));
#119735=CARTESIAN_POINT('Ctrl Pts',(-10.6888954577046,8.09868862901539,
11.9558378013248));
#119736=CARTESIAN_POINT('Ctrl Pts',(-10.7207648882595,8.09589977148649,
11.9314718101271));
#119737=CARTESIAN_POINT('Ctrl Pts',(-10.7261573447767,8.09542751929018,
11.927274109092));
#119738=CARTESIAN_POINT('Ctrl Pts',(-10.734549923372,8.09469234436067,11.9206228799053));
#119739=CARTESIAN_POINT('Ctrl Pts',(-10.7375748882609,8.09442732519014,
11.9182011556447));
#119740=CARTESIAN_POINT('Ctrl Pts',(-10.7432433923885,8.0939307199376,11.9136169797366));
#119741=CARTESIAN_POINT('Ctrl Pts',(-10.7458894692348,8.09369892062497,
11.9114579672218));
#119742=CARTESIAN_POINT('Ctrl Pts',(-10.7520125790718,8.09316250546291,
11.9064174175853));
#119743=CARTESIAN_POINT('Ctrl Pts',(-10.7554824776741,8.09285849911824,
11.9035273551934));
#119744=CARTESIAN_POINT('Ctrl Pts',(-10.7668289374351,8.09186399428393,
11.8939658762343));
#119745=CARTESIAN_POINT('Ctrl Pts',(-10.7746346836783,8.09117916789845,
11.8872106468071));
#119746=CARTESIAN_POINT('Ctrl Pts',(-10.8358071347924,8.08579753893997,
11.8328480184471));
#119747=CARTESIAN_POINT('Ctrl Pts',(-10.8848330255204,8.08138838120861,
11.7805656415313));
#119748=CARTESIAN_POINT('Ctrl Pts',(-10.9638258998428,8.07344124306554,
11.6792471731147));
#119749=CARTESIAN_POINT('Ctrl Pts',(-10.9955312365917,8.06991996865626,
11.6318655206112));
#119750=CARTESIAN_POINT('Ctrl Pts',(-11.0341981948828,8.06493959727346,
11.5638982801113));
#119751=CARTESIAN_POINT('Ctrl Pts',(-11.0442094919244,8.06357223949637,
11.5451363438546));
#119752=CARTESIAN_POINT('Ctrl Pts',(-11.0608737487675,8.06114427115427,
11.5117610145093));
#119753=CARTESIAN_POINT('Ctrl Pts',(-11.0677461051274,8.06009102499601,
11.4972631714739));
#119754=CARTESIAN_POINT('Ctrl Pts',(-11.0774845391716,8.0585159330378,11.4755857098771));
#119755=CARTESIAN_POINT('Ctrl Pts',(-11.0805797182078,8.05800181820763,
11.4685105841374));
#119756=CARTESIAN_POINT('Ctrl Pts',(-11.0859783040471,8.05708021802041,
11.4558320776051));
#119757=CARTESIAN_POINT('Ctrl Pts',(-11.088308497504,8.05667364771427,11.4502403488778));
#119758=CARTESIAN_POINT('Ctrl Pts',(-11.0931513497016,8.05580961131835,
11.4383617515122));
#119759=CARTESIAN_POINT('Ctrl Pts',(-11.095653134681,8.05535180055128,11.4320707160929));
#119760=CARTESIAN_POINT('Ctrl Pts',(-11.1022157988622,8.05411930843729,
11.4151445394574));
#119761=CARTESIAN_POINT('Ctrl Pts',(-11.1061768648162,8.05334137488469,
11.4044717343481));
#119762=CARTESIAN_POINT('Ctrl Pts',(-11.1246360682623,8.04954343197783,
11.3524343236212));
#119763=CARTESIAN_POINT('Ctrl Pts',(-11.1369704328243,8.04645450635206,
11.3103443911239));
#119764=CARTESIAN_POINT('Ctrl Pts',(-11.1636685499137,8.03801779824824,
11.1959463093792));
#119765=CARTESIAN_POINT('Ctrl Pts',(-11.1736415620508,8.03257243928809,
11.1228145197623));
#119766=CARTESIAN_POINT('Ctrl Pts',(-11.1779946282035,8.02497180746589,
11.0187840070013));
#119767=CARTESIAN_POINT('Ctrl Pts',(-11.1780862793021,8.02276344467305,
10.9882890995139));
#119768=CARTESIAN_POINT('Ctrl Pts',(-11.1765702871003,8.01975319249104,
10.9459835267386));
#119769=CARTESIAN_POINT('Ctrl Pts',(-11.1759673801608,8.01891706467461,
10.9341504419125));
#119770=CARTESIAN_POINT('Ctrl Pts',(-11.1746030962002,8.01747091702478,
10.9135086773689));
#119771=CARTESIAN_POINT('Ctrl Pts',(-11.1739209164978,8.01685745661529,
10.9046958766725));
#119772=CARTESIAN_POINT('Ctrl Pts',(-11.1727604269661,8.01595385699603,
10.8916190080917));
#119773=CARTESIAN_POINT('Ctrl Pts',(-11.1723579483332,8.0156598477707,10.8873487643182));
#119774=CARTESIAN_POINT('Ctrl Pts',(-11.1716283226216,8.01515824444408,
10.880035411871));
#119775=CARTESIAN_POINT('Ctrl Pts',(-11.1713126327618,8.01495003274469,
10.8769912772895));
#119776=CARTESIAN_POINT('Ctrl Pts',(-11.1705631440484,8.01447514575751,
10.8700287367744));
#119777=CARTESIAN_POINT('Ctrl Pts',(-11.1701215350591,8.01420890454771,
10.8661112484281));
#119778=CARTESIAN_POINT('Ctrl Pts',(-11.1688465910538,8.01347590622786,
10.8552897112199));
#119779=CARTESIAN_POINT('Ctrl Pts',(-11.1679717506223,8.01301136043032,
10.84839057879));
#119780=CARTESIAN_POINT('Ctrl Pts',(-11.1627181641664,8.01042025516647,
10.8097085582477));
#119781=CARTESIAN_POINT('Ctrl Pts',(-11.1571028554689,8.00835439469295,
10.7781041898662));
#119782=CARTESIAN_POINT('Ctrl Pts',(-11.1365813725998,8.00231024781571,
10.6848945604035));
#119783=CARTESIAN_POINT('Ctrl Pts',(-11.1179889128614,7.99843557217222,
10.6242204245122));
#119784=CARTESIAN_POINT('Ctrl Pts',(-11.0783325469976,7.99176561236707,
10.5243551456662));
#119785=CARTESIAN_POINT('Ctrl Pts',(-11.059772838309,7.98900697270997,10.4843254965805));
#119786=CARTESIAN_POINT('Ctrl Pts',(-11.0304279102795,7.98501539574614,
10.4293460984991));
#119787=CARTESIAN_POINT('Ctrl Pts',(-11.0214698448081,7.98383719326704,
10.4134619732352));
#119788=CARTESIAN_POINT('Ctrl Pts',(-11.004862406242,7.9817165733481,10.3855493721757));
#119789=CARTESIAN_POINT('Ctrl Pts',(-10.9973565239308,7.98077911798206,
10.3734395757147));
#119790=CARTESIAN_POINT('Ctrl Pts',(-10.9856364938995,7.97934458121354,
10.3552751714333));
#119791=CARTESIAN_POINT('Ctrl Pts',(-10.9815819199564,7.97885331969403,
10.3491188027346));
#119792=CARTESIAN_POINT('Ctrl Pts',(-10.9741065406715,7.97795635819017,
10.3379970835156));
#119793=CARTESIAN_POINT('Ctrl Pts',(-10.9707048642027,7.97755137889554,
10.3330191319703));
#119794=CARTESIAN_POINT('Ctrl Pts',(-10.9632652970032,7.97667236070633,
10.322309670439));
#119795=CARTESIAN_POINT('Ctrl Pts',(-10.959214167537,7.97619783367544,10.3165876849829));
#119796=CARTESIAN_POINT('Ctrl Pts',(-10.9479909698979,7.97489416457215,
10.3010319604868));
#119797=CARTESIAN_POINT('Ctrl Pts',(-10.940717338681,7.97406118087562,10.2912729236704));
#119798=CARTESIAN_POINT('Ctrl Pts',(-10.8884637231021,7.96815711651826,
10.2233860466446));
#119799=CARTESIAN_POINT('Ctrl Pts',(-10.8382881672612,7.96287898735427,
10.1694782338457));
#119800=CARTESIAN_POINT('Ctrl Pts',(-10.7371596300048,7.95297393295788,
10.0793858653608));
#119801=CARTESIAN_POINT('Ctrl Pts',(-10.687710650999,7.9483936639308,10.0418825114237));
#119802=CARTESIAN_POINT('Ctrl Pts',(-10.620444846729,7.9426433214011,9.99876840340745));
#119803=CARTESIAN_POINT('Ctrl Pts',(-10.6051303297619,7.94136418514984,
9.98943883309905));
#119804=CARTESIAN_POINT('Ctrl Pts',(-10.5791490245254,7.93925066047584,
9.9744136098997));
#119805=CARTESIAN_POINT('Ctrl Pts',(-10.5685971188126,7.93840742719764,
9.96852611233574));
#119806=CARTESIAN_POINT('Ctrl Pts',(-10.553676949268,7.93723806798522,9.96049987630695));
#119807=CARTESIAN_POINT('Ctrl Pts',(-10.5493836168286,7.93690420644284,
9.95822444118138));
#119808=CARTESIAN_POINT('Ctrl Pts',(-10.5420132816432,7.93633570256747,
9.95437645209557));
#119809=CARTESIAN_POINT('Ctrl Pts',(-10.5389432447222,7.93610026526437,
9.95279076510248));
#119810=CARTESIAN_POINT('Ctrl Pts',(-10.5325256581536,7.93561100817818,
9.94951175249149));
#119811=CARTESIAN_POINT('Ctrl Pts',(-10.529176947732,7.93535733640226,9.94782088325067));
#119812=CARTESIAN_POINT('Ctrl Pts',(-10.5202101482378,7.93468225660047,
9.94334690110892));
#119813=CARTESIAN_POINT('Ctrl Pts',(-10.5145777251602,7.93426256434568,
9.94059255298898));
#119814=CARTESIAN_POINT('Ctrl Pts',(-10.48935751592,7.93240146725709,9.92850804807132));
#119815=CARTESIAN_POINT('Ctrl Pts',(-10.4695347933041,7.93098719496237,
9.91967458575304));
#119816=CARTESIAN_POINT('Ctrl Pts',(-10.3702975115948,7.92408979181832,
9.87870022746897));
#119817=CARTESIAN_POINT('Ctrl Pts',(-10.2877803202513,7.91890732163529,
9.85474082158606));
#119818=CARTESIAN_POINT('Ctrl Pts',(-10.1480111623576,7.91005607855261,
9.83023567037699));
#119819=CARTESIAN_POINT('Ctrl Pts',(-10.0920172380915,7.90649482521806,
9.82450541646872));
#119820=CARTESIAN_POINT('Ctrl Pts',(-10.0241131885421,7.90203748585756,
9.82243849792616));
#119821=CARTESIAN_POINT('Ctrl Pts',(-10.0123893482796,7.90126314686159,
9.82225680856534));
#119822=CARTESIAN_POINT('Ctrl Pts',(-9.99382119583592,7.90002830578992,
9.82224632299599));
#119823=CARTESIAN_POINT('Ctrl Pts',(-9.98697752892163,7.89957136504279,
9.82230211291889));
#119824=CARTESIAN_POINT('Ctrl Pts',(-9.97409001878083,7.89870729013057,
9.82251951785322));
#119825=CARTESIAN_POINT('Ctrl Pts',(-9.96804615437512,7.89830057412994,
9.82266803221052));
#119826=CARTESIAN_POINT('Ctrl Pts',(-9.95440574080568,7.89737916514482,
9.82310832417448));
#119827=CARTESIAN_POINT('Ctrl Pts',(-9.94681039618479,7.89686365393204,
9.82342713168355));
#119828=CARTESIAN_POINT('Ctrl Pts',(-9.923826157997,7.89529598211059,9.82461488221447));
#119829=CARTESIAN_POINT('Ctrl Pts',(-9.90845125909614,7.89423685099825,
9.82571237833746));
#119830=CARTESIAN_POINT('Ctrl Pts',(-9.86565153063747,7.89125793212587,
9.82961314496543));
#119831=CARTESIAN_POINT('Ctrl Pts',(-9.83831699479807,7.88932006193749,
9.8330761678256));
#119832=CARTESIAN_POINT('Ctrl Pts',(-9.81114930150157,7.88735883108162,
9.83748958018577));
#119833=CARTESIAN_POINT('Ctrl Pts',(-9.81114930150278,7.78890339972192,
9.83748958018558));
#119834=CARTESIAN_POINT('Ctrl Pts',(-9.82455959941259,7.78981154754944,
9.83531106712956));
#119835=CARTESIAN_POINT('Ctrl Pts',(-9.83799741169626,7.79070711032302,
9.83336601946057));
#119836=CARTESIAN_POINT('Ctrl Pts',(-9.93521180416505,7.79710149568767,
9.82100785844903));
#119837=CARTESIAN_POINT('Ctrl Pts',(-10.0198595166984,7.80223158742924,
9.81939454282834));
#119838=CARTESIAN_POINT('Ctrl Pts',(-10.1673483502748,7.81141878983337,
9.83246451178699));
#119839=CARTESIAN_POINT('Ctrl Pts',(-10.2301685310679,7.81541166472953,
9.8432089351587));
#119840=CARTESIAN_POINT('Ctrl Pts',(-10.3055645046629,7.82049322285603,
9.86249088603078));
#119841=CARTESIAN_POINT('Ctrl Pts',(-10.3192547339337,7.82142754999622,
9.86625706722847));
#119842=CARTESIAN_POINT('Ctrl Pts',(-10.3399335280042,7.8228581920035,9.87235003793819));
#119843=CARTESIAN_POINT('Ctrl Pts',(-10.3469741886334,7.82334873433376,
9.8744964910309));
#119844=CARTESIAN_POINT('Ctrl Pts',(-10.3597425380678,7.82424483746663,
9.87852031018943));
#119845=CARTESIAN_POINT('Ctrl Pts',(-10.3654768567892,7.82464968295685,
9.88037593219935));
#119846=CARTESIAN_POINT('Ctrl Pts',(-10.3778551841324,7.82552893260949,
9.88448677769641));
#119847=CARTESIAN_POINT('Ctrl Pts',(-10.3844937571763,7.82600382882605,
9.88675751234349));
#119848=CARTESIAN_POINT('Ctrl Pts',(-10.4026191950038,7.82730985537383,
9.8931388131751));
#119849=CARTESIAN_POINT('Ctrl Pts',(-10.4140628291687,7.82814485175348,
9.89736866668973));
#119850=CARTESIAN_POINT('Ctrl Pts',(-10.4913154723831,7.83385479028743,
9.92729536393068));
#119851=CARTESIAN_POINT('Ctrl Pts',(-10.5547511553008,7.83891983013832,
9.95868636168445));
#119852=CARTESIAN_POINT('Ctrl Pts',(-10.6585079027739,7.84780800796341,
10.0222132266455));
#119853=CARTESIAN_POINT('Ctrl Pts',(-10.700254280645,7.85157313324339,10.0516627286598));
#119854=CARTESIAN_POINT('Ctrl Pts',(-10.7704768756123,7.85814043338087,
10.108372721199));
#119855=CARTESIAN_POINT('Ctrl Pts',(-10.7997480578436,7.86095902758692,
10.134530455424));
#119856=CARTESIAN_POINT('Ctrl Pts',(-10.8313209784478,7.86404673599207,
10.1657177045761));
#119857=CARTESIAN_POINT('Ctrl Pts',(-10.8349565970713,7.86440302925653,
10.1693562731244));
#119858=CARTESIAN_POINT('Ctrl Pts',(-10.8416795705965,7.86506308161973,
10.1761734432601));
#119859=CARTESIAN_POINT('Ctrl Pts',(-10.8447730353988,7.86536727369523,
10.1793458612783));
#119860=CARTESIAN_POINT('Ctrl Pts',(-10.8478763011623,7.86567284703338,
10.1825644722537));
#119861=CARTESIAN_POINT('Ctrl Pts',(-10.8479040161325,7.86567557611347,
10.1825932202869));
#119862=CARTESIAN_POINT('Ctrl Pts',(-10.8479594469965,7.86568103443211,
10.182650723164));
#119863=CARTESIAN_POINT('Ctrl Pts',(-10.8479871628904,7.86568376367067,
10.1826794780087));
#119864=CARTESIAN_POINT('Ctrl Pts',(-10.8480426044558,7.86568922317803,
10.1827370036982));
#119865=CARTESIAN_POINT('Ctrl Pts',(-10.8480703300911,7.8656919534433,10.1827657745079));
#119866=CARTESIAN_POINT('Ctrl Pts',(-10.8481258001039,7.86569741588688,
10.1828233414389));
#119867=CARTESIAN_POINT('Ctrl Pts',(-10.8481535444954,7.86570014806661,
10.1828521375793));
#119868=CARTESIAN_POINT('Ctrl Pts',(-10.8482090611459,7.86570561523781,
10.1829097646572));
#119869=CARTESIAN_POINT('Ctrl Pts',(-10.8482368334248,7.86570835023132,
10.1829385956221));
#119870=CARTESIAN_POINT('Ctrl Pts',(-10.8482924151944,7.8657138239504,10.1829963020703));
#119871=CARTESIAN_POINT('Ctrl Pts',(-10.8483202246671,7.86571656267431,
10.1830251775434));
#119872=CARTESIAN_POINT('Ctrl Pts',(-10.8483758903419,7.86572204479174,
10.1830829829172));
#119873=CARTESIAN_POINT('Ctrl Pts',(-10.8484037465364,7.86572478818462,
10.1831119128204));
#119874=CARTESIAN_POINT('Ctrl Pts',(-10.8484595153598,7.86573028059603,
10.1831698371661));
#119875=CARTESIAN_POINT('Ctrl Pts',(-10.8484874279979,7.86573302961562,
10.1831988316308));
#119876=CARTESIAN_POINT('Ctrl Pts',(-10.8485433196438,7.86573853425927,
10.1832568954587));
#119877=CARTESIAN_POINT('Ctrl Pts',(-10.8485712986673,7.86574128988507,
10.1832859648531));
#119878=CARTESIAN_POINT('Ctrl Pts',(-10.8486273332923,7.86574680874696,
10.1833441891921));
#119879=CARTESIAN_POINT('Ctrl Pts',(-10.8486553888782,7.86574957198171,
10.1833733441376));
#119880=CARTESIAN_POINT('Ctrl Pts',(-10.8487115871372,7.86575510709709,
10.1834317505519));
#119881=CARTESIAN_POINT('Ctrl Pts',(-10.848739729728,7.86575787896983,10.1834610019547));
#119882=CARTESIAN_POINT('Ctrl Pts',(-10.8487961126792,7.86576343241388,
10.1835196124461));
#119883=CARTESIAN_POINT('Ctrl Pts',(-10.8488243530778,7.86576621398921,
10.1835489715962));
#119884=CARTESIAN_POINT('Ctrl Pts',(-10.8488809426915,7.86577178792717,
10.1836078091335));
#119885=CARTESIAN_POINT('Ctrl Pts',(-10.8489092918882,7.86577458028827,
10.1836372875256));
#119886=CARTESIAN_POINT('Ctrl Pts',(-10.8489661105019,7.86578017692176,
10.1836963754788));
#119887=CARTESIAN_POINT('Ctrl Pts',(-10.8489945798982,7.86578298119242,
10.183725985045));
#119888=CARTESIAN_POINT('Ctrl Pts',(-10.8490397479066,7.86578743035258,
10.1837729669049));
#119889=CARTESIAN_POINT('Ctrl Pts',(-10.8490564475233,7.86578907531805,
10.1837903382098));
#119890=CARTESIAN_POINT('Ctrl Pts',(-10.8490903572128,7.86579241555501,
10.183825613974));
#119891=CARTESIAN_POINT('Ctrl Pts',(-10.849107567269,7.86579411082561,10.1838435184823));
#119892=CARTESIAN_POINT('Ctrl Pts',(-10.8491425293516,7.8657975547794,10.1838798936415));
#119893=CARTESIAN_POINT('Ctrl Pts',(-10.8491602813417,7.86579930345982,
10.1838983643271));
#119894=CARTESIAN_POINT('Ctrl Pts',(-10.8491963615264,7.86580285760799,
10.1839359076824));
#119895=CARTESIAN_POINT('Ctrl Pts',(-10.849214689642,7.86580466306887,10.1839549803498));
#119896=CARTESIAN_POINT('Ctrl Pts',(-10.8492519591937,7.86580833443686,
10.1839937665355));
#119897=CARTESIAN_POINT('Ctrl Pts',(-10.8492709006929,7.86581020035118,
10.1840134802072));
#119898=CARTESIAN_POINT('Ctrl Pts',(-10.8493094376427,7.86581399663158,
10.1840535909564));
#119899=CARTESIAN_POINT('Ctrl Pts',(-10.8493290329534,7.86581592698497,
10.1840739879852));
#119900=CARTESIAN_POINT('Ctrl Pts',(-10.8516303308932,7.86604263205601,
10.1864696134258));
#119901=CARTESIAN_POINT('Ctrl Pts',(-10.8539020576687,7.86626664103343,
10.1888543983169));
#119902=CARTESIAN_POINT('Ctrl Pts',(-10.8589442226075,7.86676431689917,
10.194192157552));
#119903=CARTESIAN_POINT('Ctrl Pts',(-10.8617094587736,7.86703759542811,
10.1971499103889));
#119904=CARTESIAN_POINT('Ctrl Pts',(-10.8694055213413,7.86779933403846,
10.2054673453715));
#119905=CARTESIAN_POINT('Ctrl Pts',(-10.8743020707884,7.86828533617108,
10.2108586974559));
#119906=CARTESIAN_POINT('Ctrl Pts',(-10.9060015500266,7.87144331735458,
10.2464187080988));
#119907=CARTESIAN_POINT('Ctrl Pts',(-10.931291838951,7.87401856052288,10.2779059452729));
#119908=CARTESIAN_POINT('Ctrl Pts',(-10.9938858617977,7.88073282871563,
10.3646117965544));
#119909=CARTESIAN_POINT('Ctrl Pts',(-11.028207472582,7.88479433127492,10.4217983430664));
#119910=CARTESIAN_POINT('Ctrl Pts',(-11.0815754835307,7.89236417456196,
10.5306625875245));
#119911=CARTESIAN_POINT('Ctrl Pts',(-11.1021879780395,7.89583102351319,
10.581354963265));
#119912=CARTESIAN_POINT('Ctrl Pts',(-11.1228324791063,7.90018195630549,
10.6443625149175));
#119913=CARTESIAN_POINT('Ctrl Pts',(-11.1262954385048,7.90095146918993,
10.6554867690128));
#119914=CARTESIAN_POINT('Ctrl Pts',(-11.1315248528597,7.90218030264611,
10.6732077527523));
#119915=CARTESIAN_POINT('Ctrl Pts',(-11.1334000043344,7.90263612055324,
10.6797718120297));
#119916=CARTESIAN_POINT('Ctrl Pts',(-11.1368281333451,7.90349912087854,
10.6921795739737));
#119917=CARTESIAN_POINT('Ctrl Pts',(-11.1383933864498,7.90390589466667,
10.6980196781309));
#119918=CARTESIAN_POINT('Ctrl Pts',(-11.1418304736136,7.90482886021816,
10.7112503604493));
#119919=CARTESIAN_POINT('Ctrl Pts',(-11.1436756371562,7.90534588293109,
10.7186475216715));
#119920=CARTESIAN_POINT('Ctrl Pts',(-11.1490616225113,7.90692329730635,
10.7411685626707));
#119921=CARTESIAN_POINT('Ctrl Pts',(-11.1523750681196,7.90799078949189,
10.7563445305724));
#119922=CARTESIAN_POINT('Ctrl Pts',(-11.1725964188434,7.91521917885966,
10.8586280082206));
#119923=CARTESIAN_POINT('Ctrl Pts',(-11.1799102402493,7.92168257978313,
10.9473257299318));
#119924=CARTESIAN_POINT('Ctrl Pts',(-11.175794448457,7.93156845030165,11.0819707610842));
#119925=CARTESIAN_POINT('Ctrl Pts',(-11.1716952369856,7.93494244709309,
11.1278379183047));
#119926=CARTESIAN_POINT('Ctrl Pts',(-11.1626773278418,7.93933120050644,
11.1884388919986));
#119927=CARTESIAN_POINT('Ctrl Pts',(-11.1601388780749,7.94041482633825,
11.2034836960619));
#119928=CARTESIAN_POINT('Ctrl Pts',(-11.1553213341638,7.94223835962507,
11.2290031787678));
#119929=CARTESIAN_POINT('Ctrl Pts',(-11.1531903144072,7.94298444720246,
11.2395035697684));
#119930=CARTESIAN_POINT('Ctrl Pts',(-11.1499330595366,7.9440425809472,11.2545004471464));
#119931=CARTESIAN_POINT('Ctrl Pts',(-11.1489231895529,7.94436058267268,
11.2590212835579));
#119932=CARTESIAN_POINT('Ctrl Pts',(-11.1471215490648,7.94491074744287,
11.266868704701));
#119933=CARTESIAN_POINT('Ctrl Pts',(-11.1463419256541,7.94514357528036,
11.2701979729418));
#119934=CARTESIAN_POINT('Ctrl Pts',(-11.1446529155874,7.9456369958904,11.2772717298883));
#119935=CARTESIAN_POINT('Ctrl Pts',(-11.1437396437225,7.94589736917181,
11.2810151914074));
#119936=CARTESIAN_POINT('Ctrl Pts',(-11.1411791956604,7.94661021463223,
11.2912910743716));
#119937=CARTESIAN_POINT('Ctrl Pts',(-11.1394942869817,7.94706062100967,
11.2978140725663));
#119938=CARTESIAN_POINT('Ctrl Pts',(-11.1306855033547,7.94932563932087,
11.3307469838067));
#119939=CARTESIAN_POINT('Ctrl Pts',(-11.1226984854427,7.95109649518949,
11.356919670276));
#119940=CARTESIAN_POINT('Ctrl Pts',(-11.088988099235,7.95770414334222,11.4550063202625));
#119941=CARTESIAN_POINT('Ctrl Pts',(-11.0572042482329,7.96234511825067,
11.5246394917393));
#119942=CARTESIAN_POINT('Ctrl Pts',(-10.9894155815658,7.97076334873772,
11.6415666200688));
#119943=CARTESIAN_POINT('Ctrl Pts',(-10.956168205878,7.97447955965923,11.6901390824437));
#119944=CARTESIAN_POINT('Ctrl Pts',(-10.9120423961465,7.97911120965069,
11.7452608574559));
#119945=CARTESIAN_POINT('Ctrl Pts',(-10.9045090285455,7.97989253965028,
11.7543861602398));
#119946=CARTESIAN_POINT('Ctrl Pts',(-10.8923893047023,7.98113588678859,
11.7686244415405));
#119947=CARTESIAN_POINT('Ctrl Pts',(-10.8878933912457,7.98159425532175,
11.7738136246553));
#119948=CARTESIAN_POINT('Ctrl Pts',(-10.8793570912542,7.98245940580886,
11.7834938795296));
#119949=CARTESIAN_POINT('Ctrl Pts',(-10.8753270072697,7.98286575539433,
11.7879937697824));
#119950=CARTESIAN_POINT('Ctrl Pts',(-10.8661734314228,7.98378414452859,
11.7980575506553));
#119951=CARTESIAN_POINT('Ctrl Pts',(-10.861030641176,7.98429698176375,11.8036034456134));
#119952=CARTESIAN_POINT('Ctrl Pts',(-10.8457184535277,7.98581500406247,
11.8198001031613));
#119953=CARTESIAN_POINT('Ctrl Pts',(-10.8354026282505,7.9868263783012,11.8303097774268));
#119954=CARTESIAN_POINT('Ctrl Pts',(-10.7570588287762,7.99442782051142,
11.9071875813504));
#119955=CARTESIAN_POINT('Ctrl Pts',(-10.6814289663745,8.00137237734009,
11.9652849681981));
#119956=CARTESIAN_POINT('Ctrl Pts',(-10.5869380224639,8.00942628103826,
12.0211843216839));
#119957=CARTESIAN_POINT('Ctrl Pts',(-10.5740721515525,8.01050982666157,
12.0284720878005));
#119958=CARTESIAN_POINT('Ctrl Pts',(-10.5332838187965,8.0138988385519,12.0505723848025));
#119959=CARTESIAN_POINT('Ctrl Pts',(-10.5048985611086,8.01619110933585,
12.0645053651755));
#119960=CARTESIAN_POINT('Ctrl Pts',(-10.4648944824683,8.01930312637977,
12.0821807643669));
#119961=CARTESIAN_POINT('Ctrl Pts',(-10.4537280034242,8.02015937130397,
12.0869098447716));
#119962=CARTESIAN_POINT('Ctrl Pts',(-10.4341519198524,8.02163664500308,
12.0948461643435));
#119963=CARTESIAN_POINT('Ctrl Pts',(-10.4257750404953,8.02226130975367,
12.0981309758894));
#119964=CARTESIAN_POINT('Ctrl Pts',(-10.4133222435431,8.02317805353899,
12.102850143896));
#119965=CARTESIAN_POINT('Ctrl Pts',(-10.4092749875865,8.02347416353389,
12.1043585028967));
#119966=CARTESIAN_POINT('Ctrl Pts',(-10.4023435132963,8.02397804595496,
12.1068984331792));
#119967=CARTESIAN_POINT('Ctrl Pts',(-10.3994634649549,8.02418645297861,
12.1079410566525));
#119968=CARTESIAN_POINT('Ctrl Pts',(-10.3928890943683,8.02465999380218,
12.1102921151401));
#119969=CARTESIAN_POINT('Ctrl Pts',(-10.3891922801295,8.02492470734324,
12.1115933571329));
#119970=CARTESIAN_POINT('Ctrl Pts',(-10.3790117631796,8.02564958545834,
12.1151197846091));
#119971=CARTESIAN_POINT('Ctrl Pts',(-10.3725148991876,8.02610761667849,
12.1173068987812));
#119972=CARTESIAN_POINT('Ctrl Pts',(-10.3370901556295,8.02858224372151,
12.1288889907905));
#119973=CARTESIAN_POINT('Ctrl Pts',(-10.3078230775826,8.03054439582064,
12.1372182869896));
#119974=CARTESIAN_POINT('Ctrl Pts',(-10.2155404363481,8.0365709023081,12.1596569268928));
#119975=CARTESIAN_POINT('Ctrl Pts',(-10.1516661756112,8.04051807760335,
12.1697265493539));
#119976=CARTESIAN_POINT('Ctrl Pts',(-10.0428857337908,8.04728759105127,
12.1778107236893));
#119977=CARTESIAN_POINT('Ctrl Pts',(-9.99833775981535,8.05007201709087,
12.1785898646929));
#119978=CARTESIAN_POINT('Ctrl Pts',(-9.92653781385786,8.05467328388258,
12.1757745271147));
#119979=CARTESIAN_POINT('Ctrl Pts',(-9.8992681945726,8.05644698399625,12.1737526790412));
#119980=CARTESIAN_POINT('Ctrl Pts',(-9.86269184696954,8.05887356706985,
12.1697568172149));
#119981=CARTESIAN_POINT('Ctrl Pts',(-9.85330147482896,8.05950076661409,
12.1686163076164));
#119982=CARTESIAN_POINT('Ctrl Pts',(-9.837625365665,8.06055532761854,12.1665204452778));
#119983=CARTESIAN_POINT('Ctrl Pts',(-9.83133168169488,8.06098075053173,
12.1656270702256));
#119984=CARTESIAN_POINT('Ctrl Pts',(-9.81896063454365,8.06182112571567,
12.1637687371126));
#119985=CARTESIAN_POINT('Ctrl Pts',(-9.81288298623624,8.0622359643735,12.1628070115097));
#119986=CARTESIAN_POINT('Ctrl Pts',(-9.79818915049442,8.06324384590903,
12.1603636822542));
#119987=CARTESIAN_POINT('Ctrl Pts',(-9.78958149270925,8.06383838383765,
12.158833697613));
#119988=CARTESIAN_POINT('Ctrl Pts',(-9.76084233285919,8.06583766239594,
12.1533946498985));
#119989=CARTESIAN_POINT('Ctrl Pts',(-9.74079700728855,8.06725569344303,
12.149055841049));
#119990=CARTESIAN_POINT('Ctrl Pts',(-9.60964016392473,8.07669521747471,
12.1170604569864));
#119991=CARTESIAN_POINT('Ctrl Pts',(-9.50296639463868,8.08522691343523,
12.0738495023957));
#119992=CARTESIAN_POINT('Ctrl Pts',(-9.37510248382612,8.09596763905219,
11.9988686969892));
#119993=CARTESIAN_POINT('Ctrl Pts',(-9.34671561818705,8.09838262646952,
11.9805384020923));
#119994=CARTESIAN_POINT('Ctrl Pts',(-9.31355757967787,8.10120780484132,
11.9570469665376));
#119995=CARTESIAN_POINT('Ctrl Pts',(-9.30799633036576,8.10168177816619,
11.9530335877622));
#119996=CARTESIAN_POINT('Ctrl Pts',(-9.29934438527864,8.10241898268218,
11.946674084668));
#119997=CARTESIAN_POINT('Ctrl Pts',(-9.29622979375232,8.10268432947371,
11.9443609537213));
#119998=CARTESIAN_POINT('Ctrl Pts',(-9.29039683624144,8.10318110837887,
11.9399840743584));
#119999=CARTESIAN_POINT('Ctrl Pts',(-9.28767601930278,8.10341275734486,
11.9379239078558));
#120000=CARTESIAN_POINT('Ctrl Pts',(-9.2813849967981,8.10394825775878,11.9331172636118));
#120001=CARTESIAN_POINT('Ctrl Pts',(-9.27782154431709,8.10425150573368,
11.9303620963278));
#120002=CARTESIAN_POINT('Ctrl Pts',(-9.26619265962072,8.10524118627714,
11.9212638774465));
#120003=CARTESIAN_POINT('Ctrl Pts',(-9.2581940390486,8.10592202104284,11.9148356565452));
#120004=CARTESIAN_POINT('Ctrl Pts',(-9.19463388644543,8.11134248580574,
11.8623726725172));
#120005=CARTESIAN_POINT('Ctrl Pts',(-9.14331820871305,8.11578876267777,
11.8114187535035));
#120006=CARTESIAN_POINT('Ctrl Pts',(-9.0606804886135,8.12375148871338,11.7127215354358));
#120007=CARTESIAN_POINT('Ctrl Pts',(-9.02754788556678,8.12724995818143,
11.6668053763915));
#120008=CARTESIAN_POINT('Ctrl Pts',(-8.98671766308592,8.13220105524531,
11.6006683962578));
#120009=CARTESIAN_POINT('Ctrl Pts',(-8.97608063183501,8.13356319436307,
11.5823509806885));
#120010=CARTESIAN_POINT('Ctrl Pts',(-8.9582878503849,8.13598269385288,11.5497150732665));
#120011=CARTESIAN_POINT('Ctrl Pts',(-8.95091919347303,8.13703276207659,
11.5355187075051));
#120012=CARTESIAN_POINT('Ctrl Pts',(-8.94042951608006,8.13860392694681,
11.5142615338318));
#120013=CARTESIAN_POINT('Ctrl Pts',(-8.93708493779483,8.13911734779618,
11.5073126268758));
#120014=CARTESIAN_POINT('Ctrl Pts',(-8.93123653715304,8.14003808013725,
11.4948498646277));
#120015=CARTESIAN_POINT('Ctrl Pts',(-8.9287065197077,8.14044448177939,11.4893485514305));
#120016=CARTESIAN_POINT('Ctrl Pts',(-8.92343659845646,8.14130855580429,
11.4776527830768));
#120017=CARTESIAN_POINT('Ctrl Pts',(-8.92070749408236,8.14176657569642,
11.4714537327116));
#120018=CARTESIAN_POINT('Ctrl Pts',(-8.91352761370793,8.14300060126082,
11.4547558118809));
#120019=CARTESIAN_POINT('Ctrl Pts',(-8.90917569008422,8.14377987462503,
11.4442154923792));
#120020=CARTESIAN_POINT('Ctrl Pts',(-8.88882767518465,8.14758164296313,
11.3928298504512));
#120021=CARTESIAN_POINT('Ctrl Pts',(-8.87497077232577,8.15067314706299,
11.3511803378975));
#120022=CARTESIAN_POINT('Ctrl Pts',(-8.84416390001624,8.1591104171017,11.2378182849524));
#120023=CARTESIAN_POINT('Ctrl Pts',(-8.83156246872543,8.16455341843918,
11.165126740619));
#120024=CARTESIAN_POINT('Ctrl Pts',(-8.82345615444482,8.17214976019482,
11.0613782627539));
#120025=CARTESIAN_POINT('Ctrl Pts',(-8.82226223582677,8.17435631706544,
11.0309307902424));
#120026=CARTESIAN_POINT('Ctrl Pts',(-8.82224537383291,8.1773643130939,10.9886290527823));
#120027=CARTESIAN_POINT('Ctrl Pts',(-8.82241920929865,8.17819994535925,
10.9767887340886));
#120028=CARTESIAN_POINT('Ctrl Pts',(-8.82303447211169,8.17964529177416,
10.9561223164122));
#120029=CARTESIAN_POINT('Ctrl Pts',(-8.82339671242154,8.18025844228852,
10.9472949697062));
#120030=CARTESIAN_POINT('Ctrl Pts',(-8.82408224553932,8.1811616277269,10.9341905797099));
#120031=CARTESIAN_POINT('Ctrl Pts',(-8.82432961477614,8.18145552867865,
10.9299101161612));
#120032=CARTESIAN_POINT('Ctrl Pts',(-8.82479355294454,8.18195696254556,
10.922577586925));
#120033=CARTESIAN_POINT('Ctrl Pts',(-8.82499864502802,8.18216511252289,
10.9195249118278));
#120034=CARTESIAN_POINT('Ctrl Pts',(-8.8254951551086,8.18263987316357,10.9125416370593));
#120035=CARTESIAN_POINT('Ctrl Pts',(-8.82579440880514,8.18290604988816,
10.9086116710676));
#120036=CARTESIAN_POINT('Ctrl Pts',(-8.82667608214286,8.18363889590926,
10.8977533058052));
#120037=CARTESIAN_POINT('Ctrl Pts',(-8.82730014435008,8.18410335460577,
10.8908283141135));
#120038=CARTESIAN_POINT('Ctrl Pts',(-8.83114773140942,8.18669426191336,
10.8519843922683));
#120039=CARTESIAN_POINT('Ctrl Pts',(-8.83561335391948,8.18876001582665,
10.8201990241753));
#120040=CARTESIAN_POINT('Ctrl Pts',(-8.85274244974931,8.1948043352428,10.7263043808015));
#120041=CARTESIAN_POINT('Ctrl Pts',(-8.86912434214634,8.19867925876159,
10.6649921353747));
#120042=CARTESIAN_POINT('Ctrl Pts',(-8.90513726525193,8.20534962224792,
10.5637490293547));
#120043=CARTESIAN_POINT('Ctrl Pts',(-8.92223496403341,8.20810841112716,
10.5230708675062));
#120044=CARTESIAN_POINT('Ctrl Pts',(-8.94956905684076,8.2121001162128,10.467062509783));
#120045=CARTESIAN_POINT('Ctrl Pts',(-8.95794537512169,8.21327828838946,
10.450864642633));
#120046=CARTESIAN_POINT('Ctrl Pts',(-8.97352961147138,8.21539881153388,
10.422369892323));
#120047=CARTESIAN_POINT('Ctrl Pts',(-8.98059117399518,8.2163362000087,10.40999693485));
#120048=CARTESIAN_POINT('Ctrl Pts',(-8.99164390837769,8.2177705731562,10.3914218424864));
#120049=CARTESIAN_POINT('Ctrl Pts',(-8.99547193252056,8.21826173827777,
10.3851238020341));
#120050=CARTESIAN_POINT('Ctrl Pts',(-9.00253763565448,8.21915849055703,
10.3737410874142));
#120051=CARTESIAN_POINT('Ctrl Pts',(-9.00575574302143,8.21956335708555,
10.3686445145265));
#120052=CARTESIAN_POINT('Ctrl Pts',(-9.01279993431246,8.22044209064721,
10.3576759305739));
#120053=CARTESIAN_POINT('Ctrl Pts',(-9.01663957739453,8.22091644523291,
10.3518129471792));
#120054=CARTESIAN_POINT('Ctrl Pts',(-9.02728669257737,8.22221953176108,
10.3358675764086));
#120055=CARTESIAN_POINT('Ctrl Pts',(-9.03419825434873,8.22305210110015,
10.3258560811101));
#120056=CARTESIAN_POINT('Ctrl Pts',(-9.08393578203363,8.22895380345555,
10.256145609038));
#120057=CARTESIAN_POINT('Ctrl Pts',(-9.13210306648402,8.2342298310506,10.2004724156419));
#120058=CARTESIAN_POINT('Ctrl Pts',(-9.22556636435933,8.24369673948814,
10.110908375121));
#120059=CARTESIAN_POINT('Ctrl Pts',(-9.26871324064937,8.24783168250748,
10.075093935594));
#120060=CARTESIAN_POINT('Ctrl Pts',(-9.33178694130332,8.25344520761053,
10.0299216914241));
#120061=CARTESIAN_POINT('Ctrl Pts',(-9.34967189654596,8.25499261424565,
10.0178421279196));
#120062=CARTESIAN_POINT('Ctrl Pts',(-9.37954098227575,8.25749390594417,
9.99884233009303));
#120063=CARTESIAN_POINT('Ctrl Pts',(-9.39133261651085,8.25846095817066,
9.99162996360394));
#120064=CARTESIAN_POINT('Ctrl Pts',(-9.40766194614922,8.25976972872334,
9.98203296126532));
#120065=CARTESIAN_POINT('Ctrl Pts',(-9.41209175878697,8.26012175735873,
9.97946819533971));
#120066=CARTESIAN_POINT('Ctrl Pts',(-9.41958071637951,8.26071165414091,
9.97519719702706));
#120067=CARTESIAN_POINT('Ctrl Pts',(-9.42263097379942,8.26095046870445,
9.97347560255144));
#120068=CARTESIAN_POINT('Ctrl Pts',(-9.42888391418015,8.2614370062654,9.96998307228857));
#120069=CARTESIAN_POINT('Ctrl Pts',(-9.4320872381885,8.26168465083042,9.96821341802256));
#120070=CARTESIAN_POINT('Ctrl Pts',(-9.44043821854453,8.26232623107853,
9.96365065068852));
#120071=CARTESIAN_POINT('Ctrl Pts',(-9.44559862890257,8.26271873820317,
9.96088090945525));
#120072=CARTESIAN_POINT('Ctrl Pts',(-9.46677776166664,8.26431445062595,
9.94971614665113));
#120073=CARTESIAN_POINT('Ctrl Pts',(-9.48296909531626,8.26549906267782,
9.94165163708398));
#120074=CARTESIAN_POINT('Ctrl Pts',(-9.59831133306932,8.27373696194174,
9.88748171545327));
#120075=CARTESIAN_POINT('Ctrl Pts',(-9.70325428047283,8.28024757132826,
9.85501720676948));
#120076=CARTESIAN_POINT('Ctrl Pts',(-9.81114931547642,8.2871573923531,9.83748957791555));
#120077=CARTESIAN_POINT('Origin',(-10.,2.67563288526385,11.));
#120078=CARTESIAN_POINT('',(-9.81114930149917,8.88548556788545,9.83748958018616));
#120079=CARTESIAN_POINT('',(-9.81114930165995,8.78721751211607,9.83748958016004));
#120080=CARTESIAN_POINT('',(-9.81114930150157,2.67563288526385,9.83748958018577));
#120081=CARTESIAN_POINT('Ctrl Pts',(-9.81114930149677,8.88548556788545,
9.83748958018655));
#120082=CARTESIAN_POINT('Ctrl Pts',(-9.80762618945418,8.88523897046284,
9.83806191240723));
#120083=CARTESIAN_POINT('Ctrl Pts',(-9.80410562708024,8.88499317710299,
9.83865026884476));
#120084=CARTESIAN_POINT('Ctrl Pts',(-9.79682735519712,8.88448640325961,
9.8399006522627));
#120085=CARTESIAN_POINT('Ctrl Pts',(-9.79307007993808,8.88422554748418,
9.84056495246939));
#120086=CARTESIAN_POINT('Ctrl Pts',(-9.78593979417461,8.88373203747368,
9.84186137850437));
#120087=CARTESIAN_POINT('Ctrl Pts',(-9.78256633190168,8.88349920911067,
9.84248998337233));
#120088=CARTESIAN_POINT('Ctrl Pts',(-9.77456755615892,8.88294864188807,
9.84401666348539));
#120089=CARTESIAN_POINT('Ctrl Pts',(-9.76994481043406,8.8826316294304,9.84492776300372));
#120090=CARTESIAN_POINT('Ctrl Pts',(-9.75437541698459,8.88156752609765,
9.84809352145577));
#120091=CARTESIAN_POINT('Ctrl Pts',(-9.74345503743677,8.88082716630944,
9.85047632665062));
#120092=CARTESIAN_POINT('Ctrl Pts',(-9.71685097011188,8.87903453536867,
9.85667930940597));
#120093=CARTESIAN_POINT('Ctrl Pts',(-9.70120837818108,8.87798993734095,
9.86066721525621));
#120094=CARTESIAN_POINT('Ctrl Pts',(-9.6366799752234,8.87370147252014,9.87853853038114));
#120095=CARTESIAN_POINT('Ctrl Pts',(-9.58863338160591,8.87055638592843,
9.89525770444862));
#120096=CARTESIAN_POINT('Ctrl Pts',(-9.46649734425989,8.86235401681429,
9.94683607807214));
#120097=CARTESIAN_POINT('Ctrl Pts',(-9.39470610429211,8.85730647402275,
9.98639422558819));
#120098=CARTESIAN_POINT('Ctrl Pts',(-9.3145279572129,8.85094889821845,10.0421501260401));
#120099=CARTESIAN_POINT('Ctrl Pts',(-9.30164894425003,8.84990399896559,
10.0514990425551));
#120100=CARTESIAN_POINT('Ctrl Pts',(-9.28282703896273,8.84833900102623,
10.0657531029731));
#120101=CARTESIAN_POINT('Ctrl Pts',(-9.27673613712501,8.84782648683882,
10.070460490023));
#120102=CARTESIAN_POINT('Ctrl Pts',(-9.2659373844172,8.84690665673508,10.0789767623831));
#120103=CARTESIAN_POINT('Ctrl Pts',(-9.26121189594785,8.84650024225482,
10.0827629189775));
#120104=CARTESIAN_POINT('Ctrl Pts',(-9.25125403116214,8.84563537182702,
10.0908682342918));
#120105=CARTESIAN_POINT('Ctrl Pts',(-9.24602937887567,8.8451765623171,10.0951964896018));
#120106=CARTESIAN_POINT('Ctrl Pts',(-9.23208833818846,8.84393850204532,
10.1069502521495));
#120107=CARTESIAN_POINT('Ctrl Pts',(-9.2234425482013,8.84315594775777,10.114457973612));
#120108=CARTESIAN_POINT('Ctrl Pts',(-9.17708710588677,8.83887774955211,
10.1559124593417));
#120109=CARTESIAN_POINT('Ctrl Pts',(-9.14149672498564,8.83528770379986,
10.1921384604032));
#120110=CARTESIAN_POINT('Ctrl Pts',(-9.07652347718975,8.82810798254828,
10.2674290495427));
#120111=CARTESIAN_POINT('Ctrl Pts',(-9.04701199219257,8.82453104238795,
10.3062547558313));
#120112=CARTESIAN_POINT('Ctrl Pts',(-9.00697055141908,8.81923397101657,
10.3663291542726));
#120113=CARTESIAN_POINT('Ctrl Pts',(-8.99453650521917,8.8175136341516,10.3862496984175));
#120114=CARTESIAN_POINT('Ctrl Pts',(-8.96300826788446,8.812960324146,10.4402935940919));
#120115=CARTESIAN_POINT('Ctrl Pts',(-8.94500158508196,8.81015037346468,
10.475021797466));
#120116=CARTESIAN_POINT('Ctrl Pts',(-8.92572209310191,8.80691976101814,
10.5172212952883));
#120117=CARTESIAN_POINT('Ctrl Pts',(-8.92275173505512,8.80641482889997,
10.5238860626499));
#120118=CARTESIAN_POINT('Ctrl Pts',(-8.91824150702682,8.80563721013027,
10.5342642611305));
#120119=CARTESIAN_POINT('Ctrl Pts',(-8.9166584466116,8.80536208860369,10.5379585565227));
#120120=CARTESIAN_POINT('Ctrl Pts',(-8.91377438506867,8.80485688769931,
10.5447852382603));
#120121=CARTESIAN_POINT('Ctrl Pts',(-8.91246799714347,8.80462650396821,
10.5479151527524));
#120122=CARTESIAN_POINT('Ctrl Pts',(-8.90950943639207,8.8041011485641,10.5550904736861));
#120123=CARTESIAN_POINT('Ctrl Pts',(-8.90786623904451,8.80380670789217,
10.5591394714559));
#120124=CARTESIAN_POINT('Ctrl Pts',(-8.90281201491224,8.80289237355746,
10.5717952627027));
#120125=CARTESIAN_POINT('Ctrl Pts',(-8.899479811319,8.80227689470087,10.5804334390886));
#120126=CARTESIAN_POINT('Ctrl Pts',(-8.891859307521,8.80083651155446,10.6009039794139));
#120127=CARTESIAN_POINT('Ctrl Pts',(-8.88765803980652,8.80001589118787,
10.6127677455485));
#120128=CARTESIAN_POINT('Ctrl Pts',(-8.87297189302721,8.79703793250479,
10.656452232396));
#120129=CARTESIAN_POINT('Ctrl Pts',(-8.86365523343844,8.79492684340516,
10.6886508131516));
#120130=CARTESIAN_POINT('Ctrl Pts',(-8.83777034136093,8.78810517825263,
10.7948918325602));
#120131=CARTESIAN_POINT('Ctrl Pts',(-8.82697693399025,8.78348579031354,
10.8701385813785));
#120132=CARTESIAN_POINT('Ctrl Pts',(-8.82174874082086,8.77628818621676,
10.9838370535318));
#120133=CARTESIAN_POINT('Ctrl Pts',(-8.82184034095802,8.77384923116895,
11.0218321325642));
#120134=CARTESIAN_POINT('Ctrl Pts',(-8.82432447517397,8.77063170494138,
11.0707314943622));
#120135=CARTESIAN_POINT('Ctrl Pts',(-8.82503579236523,8.76990491460333,
11.0817005594148));
#120136=CARTESIAN_POINT('Ctrl Pts',(-8.82642647241378,8.76872847727069,
11.0993223604917));
#120137=CARTESIAN_POINT('Ctrl Pts',(-8.82700915674939,8.76828182575976,
11.1059822366553));
#120138=CARTESIAN_POINT('Ctrl Pts',(-8.82822964434318,8.76742582096936,
11.1186853853923));
#120139=CARTESIAN_POINT('Ctrl Pts',(-8.82885758339626,8.76701678683107,
11.1247294061596));
#120140=CARTESIAN_POINT('Ctrl Pts',(-8.83040718127812,8.76607395790491,
11.1385994014598));
#120141=CARTESIAN_POINT('Ctrl Pts',(-8.83136065948155,8.76553919141288,
11.1464214542385));
#120142=CARTESIAN_POINT('Ctrl Pts',(-8.8346042786644,8.76385049423788,11.1709769600508));
#120143=CARTESIAN_POINT('Ctrl Pts',(-8.83717582174272,8.7626879180939,11.1876704224937));
#120144=CARTESIAN_POINT('Ctrl Pts',(-8.84405037082682,8.7599341711747,11.2266996496627));
#120145=CARTESIAN_POINT('Ctrl Pts',(-8.84864311485029,8.75833466022537,
11.2489768713147));
#120146=CARTESIAN_POINT('Ctrl Pts',(-8.88020464939812,8.748586905063,11.3824058085627));
#120147=CARTESIAN_POINT('Ctrl Pts',(-8.92259681838964,8.73999294651563,
11.4892569028555));
#120148=CARTESIAN_POINT('Ctrl Pts',(-8.98906906594513,8.73050859717051,
11.6045364872519));
#120149=CARTESIAN_POINT('Ctrl Pts',(-8.99880926448154,8.72918917997709,
11.6205343863147));
#120150=CARTESIAN_POINT('Ctrl Pts',(-9.01213303747131,8.72747980964123,
11.6412870894377));
#120151=CARTESIAN_POINT('Ctrl Pts',(-9.01537635479602,8.72707071770304,
11.6462557912634));
#120152=CARTESIAN_POINT('Ctrl Pts',(-9.02069032290076,8.72641193486082,
11.6542638154006));
#120153=CARTESIAN_POINT('Ctrl Pts',(-9.02273785125503,8.72616079166128,
11.6573182466448));
#120154=CARTESIAN_POINT('Ctrl Pts',(-9.02675831227461,8.72567294687066,
11.6632555179733));
#120155=CARTESIAN_POINT('Ctrl Pts',(-9.0287298078646,8.72543616373811,11.6661392340347));
#120156=CARTESIAN_POINT('Ctrl Pts',(-9.03359227741294,8.72485799696642,
11.673184111837));
#120157=CARTESIAN_POINT('Ctrl Pts',(-9.03649737429108,8.72451754216638,
11.6773355352298));
#120158=CARTESIAN_POINT('Ctrl Pts',(-9.04721404379473,8.72327912575544,
11.692441331472));
#120159=CARTESIAN_POINT('Ctrl Pts',(-9.05518671524618,8.72239123851219,
11.7032808617595));
#120160=CARTESIAN_POINT('Ctrl Pts',(-9.07594258435097,8.72015612409244,
11.7305100008294));
#120161=CARTESIAN_POINT('Ctrl Pts',(-9.08897740306139,8.7188224352027,11.7467026840705));
#120162=CARTESIAN_POINT('Ctrl Pts',(-9.15827921012805,8.71203116242853,
11.8282756757284));
#120163=CARTESIAN_POINT('Ctrl Pts',(-9.22117731224348,8.70681900766609,
11.8876775071258));
#120164=CARTESIAN_POINT('Ctrl Pts',(-9.32655844285437,8.69852451393199,
11.9673007939717));
#120165=CARTESIAN_POINT('Ctrl Pts',(-9.36469164148997,8.6956006205728,11.9927622677969));
#120166=CARTESIAN_POINT('Ctrl Pts',(-9.41420744655112,8.69183332300374,
12.0218006305955));
#120167=CARTESIAN_POINT('Ctrl Pts',(-9.4242928046753,8.69106758265894,12.0275167414853));
#120168=CARTESIAN_POINT('Ctrl Pts',(-9.44043874495223,8.68984330320877,
12.0363554951789));
#120169=CARTESIAN_POINT('Ctrl Pts',(-9.44644506549921,8.68938822008444,
12.0395760875181));
#120170=CARTESIAN_POINT('Ctrl Pts',(-9.45729964499056,8.68856625835707,
12.0452755780688));
#120171=CARTESIAN_POINT('Ctrl Pts',(-9.46213781995304,8.68820005132003,
12.0477733452447));
#120172=CARTESIAN_POINT('Ctrl Pts',(-9.47354942318082,8.68733657947066,
12.0535648580537));
#120173=CARTESIAN_POINT('Ctrl Pts',(-9.48013665672341,8.68683836903946,
12.0568307433259));
#120174=CARTESIAN_POINT('Ctrl Pts',(-9.49949103045295,8.68537493784931,
12.0662017166269));
#120175=CARTESIAN_POINT('Ctrl Pts',(-9.51233776357368,8.68440404454503,
12.0721384435285));
#120176=CARTESIAN_POINT('Ctrl Pts',(-9.57046822454081,8.68001114498712,
12.0977407429037));
#120177=CARTESIAN_POINT('Ctrl Pts',(-9.61684906642373,8.67650404095868,
12.1147764395732));
#120178=CARTESIAN_POINT('Ctrl Pts',(-9.72894838356349,8.66804129298503,
12.1481270129227));
#120179=CARTESIAN_POINT('Ctrl Pts',(-9.79527847381412,8.6630401608305,12.1617887016182));
#120180=CARTESIAN_POINT('Ctrl Pts',(-9.90241328413659,8.65518380094803,
12.1743910778903));
#120181=CARTESIAN_POINT('Ctrl Pts',(-9.9426374825873,8.65228537603638,12.1770419773361));
#120182=CARTESIAN_POINT('Ctrl Pts',(-9.99026985957277,8.64896774822762,
12.1777327303041));
#120183=CARTESIAN_POINT('Ctrl Pts',(-9.99761843418222,8.64845916123766,
12.1777705186655));
#120184=CARTESIAN_POINT('Ctrl Pts',(-10.0089977252712,8.6476771206294,12.17772252657));
#120185=CARTESIAN_POINT('Ctrl Pts',(-10.0130283029126,8.64740118977913,
12.1776848361052));
#120186=CARTESIAN_POINT('Ctrl Pts',(-10.0204488864569,8.64689524780991,
12.177577344142));
#120187=CARTESIAN_POINT('Ctrl Pts',(-10.0238388007892,8.64666492521807,
12.1775135967354));
#120188=CARTESIAN_POINT('Ctrl Pts',(-10.0315816341863,8.64614065210239,
12.1773345414614));
#120189=CARTESIAN_POINT('Ctrl Pts',(-10.0359342316413,8.64584722378039,
12.177209732648));
#120190=CARTESIAN_POINT('Ctrl Pts',(-10.0494579645718,8.64493925685946,
12.1767468688972));
#120191=CARTESIAN_POINT('Ctrl Pts',(-10.0586261714613,8.64432904564143,
12.1763257493064));
#120192=CARTESIAN_POINT('Ctrl Pts',(-10.0802096149529,8.64290310138475,
12.1750813878483));
#120193=CARTESIAN_POINT('Ctrl Pts',(-10.0926187771136,8.64209153644679,
12.1741684883418));
#120194=CARTESIAN_POINT('Ctrl Pts',(-10.137783748469,8.63916034304198,12.1701253426909));
#120195=CARTESIAN_POINT('Ctrl Pts',(-10.1704209283632,8.63708543544754,
12.1658193236148));
#120196=CARTESIAN_POINT('Ctrl Pts',(-10.2784334676807,8.63024111258215,
12.1469347736578));
#120197=CARTESIAN_POINT('Ctrl Pts',(-10.352555209962,8.62556937034821,12.126361132316));
#120198=CARTESIAN_POINT('Ctrl Pts',(-10.4595501234848,8.61831641778901,
12.0850570290388));
#120199=CARTESIAN_POINT('Ctrl Pts',(-10.4942669592658,8.61587926387358,
12.0696891135994));
#120200=CARTESIAN_POINT('Ctrl Pts',(-10.5380014700812,8.61266378793713,
12.0477453157516));
#120201=CARTESIAN_POINT('Ctrl Pts',(-10.5477540234054,8.61193716141169,
12.0426798861601));
#120202=CARTESIAN_POINT('Ctrl Pts',(-10.5633226105629,8.61076092523297,
12.0343149351427));
#120203=CARTESIAN_POINT('Ctrl Pts',(-10.5691840681087,8.61031430918389,
12.03110098542));
#120204=CARTESIAN_POINT('Ctrl Pts',(-10.5803209617273,8.60945832992848,
12.0248705138584));
#120205=CARTESIAN_POINT('Ctrl Pts',(-10.5856010477627,8.60904928550928,
12.0218627105844));
#120206=CARTESIAN_POINT('Ctrl Pts',(-10.5976750166228,8.60810637154452,
12.0148604570776));
#120207=CARTESIAN_POINT('Ctrl Pts',(-10.604452491126,8.60757152969146,12.0108384408905));
#120208=CARTESIAN_POINT('Ctrl Pts',(-10.6256310474118,8.60588234745142,
11.9979811127385));
#120209=CARTESIAN_POINT('Ctrl Pts',(-10.6398821237549,8.60471935452055,
11.9889041032157));
#120210=CARTESIAN_POINT('Ctrl Pts',(-10.6728557531962,8.60196443770187,
11.9668908366225));
#120211=CARTESIAN_POINT('Ctrl Pts',(-10.691407878162,8.60036416394799,11.9537126315116));
#120212=CARTESIAN_POINT('Ctrl Pts',(-10.8009885285493,8.59060311523743,
11.8709954349345));
#120213=CARTESIAN_POINT('Ctrl Pts',(-10.8818388132592,8.58199514799618,
11.789031095193));
#120214=CARTESIAN_POINT('Ctrl Pts',(-10.9605674758953,8.57251176203849,
11.681725758351));
#120215=CARTESIAN_POINT('Ctrl Pts',(-10.9711973409604,8.57120360980147,
11.6664950890417));
#120216=CARTESIAN_POINT('Ctrl Pts',(-10.9847328751874,8.56950645637308,
11.646089169498));
#120217=CARTESIAN_POINT('Ctrl Pts',(-10.9879654151524,8.56909864423396,
11.6411352373319));
#120218=CARTESIAN_POINT('Ctrl Pts',(-10.9931445942054,8.56844141194949,
11.6330658490535));
#120219=CARTESIAN_POINT('Ctrl Pts',(-10.9951141729077,8.56819055162865,
11.6299653467071));
#120220=CARTESIAN_POINT('Ctrl Pts',(-10.9989297929028,8.56770282830961,
11.623896266055));
#120221=CARTESIAN_POINT('Ctrl Pts',(-11.0007771649701,8.56746588680947,
11.6209286178238));
#120222=CARTESIAN_POINT('Ctrl Pts',(-11.0052764737229,8.56688671483245,
11.613628613383));
#120223=CARTESIAN_POINT('Ctrl Pts',(-11.0079136891927,8.56654542079496,
11.6092871747092));
#120224=CARTESIAN_POINT('Ctrl Pts',(-11.0174783722114,8.56530034899717,
11.5933095396261));
#120225=CARTESIAN_POINT('Ctrl Pts',(-11.0242334006939,8.56440678741006,
11.5815706552271));
#120226=CARTESIAN_POINT('Ctrl Pts',(-11.0409292537588,8.5621540379627,11.5513629846424));
#120227=CARTESIAN_POINT('Ctrl Pts',(-11.0505822854791,8.56080866063369,
11.532739915685));
#120228=CARTESIAN_POINT('Ctrl Pts',(-11.0982776164641,8.55387523702402,
11.4343793643923));
#120229=CARTESIAN_POINT('Ctrl Pts',(-11.127757629865,8.54854249131078,11.3508041819735));
#120230=CARTESIAN_POINT('Ctrl Pts',(-11.1574643180958,8.54022787614708,
11.2220168769436));
#120231=CARTESIAN_POINT('Ctrl Pts',(-11.1649216446406,8.53742669604648,
11.1788073089057));
#120232=CARTESIAN_POINT('Ctrl Pts',(-11.1712617350419,8.53380270245219,
11.1239781735694));
#120233=CARTESIAN_POINT('Ctrl Pts',(-11.1724052552642,8.53305052383987,
11.112652306458));
#120234=CARTESIAN_POINT('Ctrl Pts',(-11.1739667728239,8.53184290347931,
11.0945669750115));
#120235=CARTESIAN_POINT('Ctrl Pts',(-11.1744909661526,8.53139075428198,
11.087817217321));
#120236=CARTESIAN_POINT('Ctrl Pts',(-11.1753738848613,8.53053058979536,
11.0750199371686));
#120237=CARTESIAN_POINT('Ctrl Pts',(-11.1757442009273,8.53012294739156,
11.068973413887));
#120238=CARTESIAN_POINT('Ctrl Pts',(-11.1764804572852,8.529192311222,11.0552126556707));
#120239=CARTESIAN_POINT('Ctrl Pts',(-11.1768171966594,8.52866843266695,
11.0474972046805));
#120240=CARTESIAN_POINT('Ctrl Pts',(-11.177619943559,8.52704886336656,11.0237436656819));
#120241=CARTESIAN_POINT('Ctrl Pts',(-11.1778340999152,8.52594550625948,
11.0076994992964));
#120242=CARTESIAN_POINT('Ctrl Pts',(-11.1775697980001,8.52335668895611,
10.9703916001467));
#120243=CARTESIAN_POINT('Ctrl Pts',(-11.176843243716,8.52186419163528,10.9491357725765));
#120244=CARTESIAN_POINT('Ctrl Pts',(-11.1720557862627,8.51631768209624,
10.8710661396924));
#120245=CARTESIAN_POINT('Ctrl Pts',(-11.1644513808421,8.51217138745534,
10.8145534424038));
#120246=CARTESIAN_POINT('Ctrl Pts',(-11.1381470439426,8.50275118543912,
10.6888250374552));
#120247=CARTESIAN_POINT('Ctrl Pts',(-11.117158036718,8.49747639814742,10.6203050939678));
#120248=CARTESIAN_POINT('Ctrl Pts',(-11.0861741516057,8.4917350538909,10.544558198444));
#120249=CARTESIAN_POINT('Ctrl Pts',(-11.0821423242241,8.49101699148367,
10.5350596485392));
#120250=CARTESIAN_POINT('Ctrl Pts',(-11.0761674354496,8.4899945522122,10.5214823949139));
#120251=CARTESIAN_POINT('Ctrl Pts',(-11.0743250657323,8.48968466578908,
10.5173602768911));
#120252=CARTESIAN_POINT('Ctrl Pts',(-11.071047614508,8.48914286379021,10.5101390684957));
#120253=CARTESIAN_POINT('Ctrl Pts',(-11.0696226927823,8.48891035524681,
10.5070354768976));
#120254=CARTESIAN_POINT('Ctrl Pts',(-11.0665520009576,8.48841578335709,
10.5004232698065));
#120255=CARTESIAN_POINT('Ctrl Pts',(-11.0649023977335,8.4881539535437,10.4969165432231));
#120256=CARTESIAN_POINT('Ctrl Pts',(-11.0602954675072,8.48743310686054,
10.487247326179));
#120257=CARTESIAN_POINT('Ctrl Pts',(-11.0573016999778,8.48697623251502,
10.4811022223591));
#120258=CARTESIAN_POINT('Ctrl Pts',(-11.0394045054744,8.48430962612694,
10.4451639370382));
#120259=CARTESIAN_POINT('Ctrl Pts',(-11.0232944593596,8.48216602103481,
10.4159848585458));
#120260=CARTESIAN_POINT('Ctrl Pts',(-10.9496225140483,8.4732028618118,10.2949813702684));
#120261=CARTESIAN_POINT('Ctrl Pts',(-10.8807787398329,8.46671843083733,
10.2106553488865));
#120262=CARTESIAN_POINT('Ctrl Pts',(-10.782753825613,8.45813689749599,10.119638085903));
#120263=CARTESIAN_POINT('Ctrl Pts',(-10.7635807229568,8.45648651170935,
10.1029576474153));
#120264=CARTESIAN_POINT('Ctrl Pts',(-10.7365295478375,8.45418551701674,
10.0809193280543));
#120265=CARTESIAN_POINT('Ctrl Pts',(-10.7291028809892,8.45355654443744,
10.0750167370988));
#120266=CARTESIAN_POINT('Ctrl Pts',(-10.7170792567233,8.45254215513233,
10.0656953345988));
#120267=CARTESIAN_POINT('Ctrl Pts',(-10.7125271476411,8.45215899055984,
10.0622191460015));
#120268=CARTESIAN_POINT('Ctrl Pts',(-10.7030460162611,8.45136263796221,
10.0550878267754));
#120269=CARTESIAN_POINT('Ctrl Pts',(-10.6981134313284,8.45094927144305,
10.051437745511));
#120270=CARTESIAN_POINT('Ctrl Pts',(-10.687239087346,8.45003988621903,10.0435215626047));
#120271=CARTESIAN_POINT('Ctrl Pts',(-10.6812856909329,8.44954326047079,
10.0392719596426));
#120272=CARTESIAN_POINT('Ctrl Pts',(-10.6616341081802,8.44790771690757,
10.0255189487917));
#120273=CARTESIAN_POINT('Ctrl Pts',(-10.6477742111607,8.44676009770651,
10.0162512849215));
#120274=CARTESIAN_POINT('Ctrl Pts',(-10.6146559595049,8.44403020957948,
9.99510955183233));
#120275=CARTESIAN_POINT('Ctrl Pts',(-10.59524349246,8.44243952015611,9.983490368511));
#120276=CARTESIAN_POINT('Ctrl Pts',(-10.5213122654469,8.43641647459734,
9.94208349821359));
#120277=CARTESIAN_POINT('Ctrl Pts',(-10.4648036764495,8.43187538666773,
9.91606741663069));
#120278=CARTESIAN_POINT('Ctrl Pts',(-10.347033757933,8.42266658175131,9.87275601001855));
#120279=CARTESIAN_POINT('Ctrl Pts',(-10.2858793673687,8.41801371882402,
9.85571596757049));
#120280=CARTESIAN_POINT('Ctrl Pts',(-10.2132312943913,8.41281932034774,
9.84166498923229));
#120281=CARTESIAN_POINT('Ctrl Pts',(-10.2027895777748,8.41208074154891,
9.83979140290306));
#120282=CARTESIAN_POINT('Ctrl Pts',(-10.1882217785839,8.41106272329828,
9.83738015247417));
#120283=CARTESIAN_POINT('Ctrl Pts',(-10.1841163829741,8.41077719939434,
9.83672294502803));
#120284=CARTESIAN_POINT('Ctrl Pts',(-10.17661474085,8.41025806943173,9.83556276164537));
#120285=CARTESIAN_POINT('Ctrl Pts',(-10.1732196125569,8.41002408990471,
9.83505286995433));
#120286=CARTESIAN_POINT('Ctrl Pts',(-10.16614682746,8.40953873757135,9.83402226032232));
#120287=CARTESIAN_POINT('Ctrl Pts',(-10.1624688760186,8.40928750473616,
9.83350408359654));
#120288=CARTESIAN_POINT('Ctrl Pts',(-10.1527428500748,8.40862605113666,
9.83218070299519));
#120289=CARTESIAN_POINT('Ctrl Pts',(-10.1466907672967,8.40821742662606,
9.83140506955573));
#120290=CARTESIAN_POINT('Ctrl Pts',(-10.1333138088881,8.40732024756581,
9.82979624301008));
#120291=CARTESIAN_POINT('Ctrl Pts',(-10.1259865324777,8.40683278088396,
9.82898471212525));
#120292=CARTESIAN_POINT('Ctrl Pts',(-10.0161996174005,8.39958173447358,
9.81786771765004));
#120293=CARTESIAN_POINT('Ctrl Pts',(-9.91282441641975,8.39341095337636,
9.82097238054841));
#120294=CARTESIAN_POINT('Ctrl Pts',(-9.81114929946652,8.38697610116898,
9.83748958051637));
#120295=CARTESIAN_POINT('Ctrl Pts',(-9.81114931547642,8.2871573923531,9.83748957791555));
#120296=CARTESIAN_POINT('Ctrl Pts',(-9.81679607853834,8.28751902272957,
9.83657225704743));
#120297=CARTESIAN_POINT('Ctrl Pts',(-9.82245093697995,8.28788160001983,
9.8356958495605));
#120298=CARTESIAN_POINT('Ctrl Pts',(-9.85065399390001,8.28969261320193,
9.83153520975173));
#120299=CARTESIAN_POINT('Ctrl Pts',(-9.8732851306851,8.29115452240905,9.82886489203476));
#120300=CARTESIAN_POINT('Ctrl Pts',(-9.91282461577387,8.2937343285415,9.82535897457222));
#120301=CARTESIAN_POINT('Ctrl Pts',(-9.92970024557085,8.29484346375028,
9.82422834526252));
#120302=CARTESIAN_POINT('Ctrl Pts',(-9.95446843504627,8.29648590351012,
9.82310404953484));
#120303=CARTESIAN_POINT('Ctrl Pts',(-9.96234638984553,8.29701046038242,
9.82282567041498));
#120304=CARTESIAN_POINT('Ctrl Pts',(-9.97629995671946,8.29794364132196,
9.82247281039204));
#120305=CARTESIAN_POINT('Ctrl Pts',(-9.9823745230772,8.29835126059794,9.82236622223877));
#120306=CARTESIAN_POINT('Ctrl Pts',(-9.99513005126263,8.2992101853748,9.82224111995086));
#120307=CARTESIAN_POINT('Ctrl Pts',(-10.0018108708652,8.29966178002077,
9.82223244504251));
#120308=CARTESIAN_POINT('Ctrl Pts',(-10.0194677069978,8.30086004411813,
9.82235974976683));
#120309=CARTESIAN_POINT('Ctrl Pts',(-10.0304421505515,8.30160965887142,
9.82259233401424));
#120310=CARTESIAN_POINT('Ctrl Pts',(-10.0792128906541,8.30496350330611,
9.82430824617389));
#120311=CARTESIAN_POINT('Ctrl Pts',(-10.1169243163701,8.3076180711371,9.82745834118891));
#120312=CARTESIAN_POINT('Ctrl Pts',(-10.2306115288349,8.3158082518639,9.84249372998667));
#120313=CARTESIAN_POINT('Ctrl Pts',(-10.3056328088298,8.32148312800247,
9.86000488135048));
#120314=CARTESIAN_POINT('Ctrl Pts',(-10.409588282637,8.32950916924227,9.89527518704539));
#120315=CARTESIAN_POINT('Ctrl Pts',(-10.4403173673678,8.33190047220863,
9.90715949277119));
#120316=CARTESIAN_POINT('Ctrl Pts',(-10.4819203658134,8.33513209142243,
9.92528945637227));
#120317=CARTESIAN_POINT('Ctrl Pts',(-10.4932519578149,8.33601162716575,
9.93044283711684));
#120318=CARTESIAN_POINT('Ctrl Pts',(-10.5127952712848,8.33752486269641,
9.93970742548203));
#120319=CARTESIAN_POINT('Ctrl Pts',(-10.5210444082844,8.33816243033933,
9.94373674144378));
#120320=CARTESIAN_POINT('Ctrl Pts',(-10.5331355857896,8.33909433586551,
9.94981884059448));
#120321=CARTESIAN_POINT('Ctrl Pts',(-10.5370144712871,8.33939289316836,
9.95179702368593));
#120322=CARTESIAN_POINT('Ctrl Pts',(-10.5438933998816,8.33992153201631,
9.95535339869649));
#120323=CARTESIAN_POINT('Ctrl Pts',(-10.546897695875,8.34015211795317,9.95692307892815));
#120324=CARTESIAN_POINT('Ctrl Pts',(-10.5534578378338,8.34065497254719,
9.9603867478662));
#120325=CARTESIAN_POINT('Ctrl Pts',(-10.5570107713701,8.34092691008848,
9.96228602492832));
#120326=CARTESIAN_POINT('Ctrl Pts',(-10.567011139677,8.34169137963912,9.96769803990997));
#120327=CARTESIAN_POINT('Ctrl Pts',(-10.5734357071145,8.34218138232288,
9.97125296313846));
#120328=CARTESIAN_POINT('Ctrl Pts',(-10.6147894482421,8.34533094511393,
9.99464312567753));
#120329=CARTESIAN_POINT('Ctrl Pts',(-10.6487216450408,8.34789474066395,
10.0161964272414));
#120330=CARTESIAN_POINT('Ctrl Pts',(-10.7390004364148,8.35484580053304,
10.0802468789802));
#120331=CARTESIAN_POINT('Ctrl Pts',(-10.7927317135713,8.35914074423533,
10.1261325001123));
#120332=CARTESIAN_POINT('Ctrl Pts',(-10.8778649470928,8.36676046191007,
10.2131873479139));
#120333=CARTESIAN_POINT('Ctrl Pts',(-10.9112599897202,8.37001928137387,
10.2521194758373));
#120334=CARTESIAN_POINT('Ctrl Pts',(-10.9488997690667,8.3741359637718,10.3022779985991));
#120335=CARTESIAN_POINT('Ctrl Pts',(-10.9556531288595,8.37489416657365,
10.3115569412462));
#120336=CARTESIAN_POINT('Ctrl Pts',(-10.9661840139989,8.37610910719644,
10.3264796931753));
#120337=CARTESIAN_POINT('Ctrl Pts',(-10.9700502936138,8.37656247965453,
10.3320601994038));
#120338=CARTESIAN_POINT('Ctrl Pts',(-10.9772716867776,8.37742347901851,
10.3426783558554));
#120339=CARTESIAN_POINT('Ctrl Pts',(-10.9806366465613,8.37783072036775,
10.3477090689604));
#120340=CARTESIAN_POINT('Ctrl Pts',(-10.9881860080057,8.37875836953882,
10.3591860352838));
#120341=CARTESIAN_POINT('Ctrl Pts',(-10.9923463526853,8.37927964210262,
10.3656477041397));
#120342=CARTESIAN_POINT('Ctrl Pts',(-11.0048941881421,8.3808833890068,10.3855620049134));
#120343=CARTESIAN_POINT('Ctrl Pts',(-11.0130732550673,8.38197331599752,
10.3991431812292));
#120344=CARTESIAN_POINT('Ctrl Pts',(-11.0624569043934,8.38884497066996,
10.4850198300692));
#120345=CARTESIAN_POINT('Ctrl Pts',(-11.096169650088,8.39488833686616,10.5613354085241));
#120346=CARTESIAN_POINT('Ctrl Pts',(-11.1425261878471,8.40603352208812,
10.7059772056802));
#120347=CARTESIAN_POINT('Ctrl Pts',(-11.1577318102823,8.41108787112069,
10.7731203176236));
#120348=CARTESIAN_POINT('Ctrl Pts',(-11.1682224058165,8.4165307433325,10.8502197582763));
#120349=CARTESIAN_POINT('Ctrl Pts',(-11.1693438025817,8.4171620342498,10.8592420722607));
#120350=CARTESIAN_POINT('Ctrl Pts',(-11.1708457290484,8.41808656839774,
10.8725866895361));
#120351=CARTESIAN_POINT('Ctrl Pts',(-11.1713070025415,8.41838393889068,
10.8768993086351));
#120352=CARTESIAN_POINT('Ctrl Pts',(-11.1720862080964,8.4189113089975,10.8845856802864));
#120353=CARTESIAN_POINT('Ctrl Pts',(-11.1724134151022,8.41914180312824,
10.8879583584144));
#120354=CARTESIAN_POINT('Ctrl Pts',(-11.1730989900469,8.4196454366688,10.8953570002676));
#120355=CARTESIAN_POINT('Ctrl Pts',(-11.1734511939247,8.41991823698202,
10.8993834281063));
#120356=CARTESIAN_POINT('Ctrl Pts',(-11.174389635909,8.42068748134716,10.9107877755314));
#120357=CARTESIAN_POINT('Ctrl Pts',(-11.1749270798201,8.42118134624302,
10.9181696761109));
#120358=CARTESIAN_POINT('Ctrl Pts',(-11.1781270633891,8.42453682724228,
10.9686944161239));
#120359=CARTESIAN_POINT('Ctrl Pts',(-11.1784826553976,8.42728717605689,
11.0119554798718));
#120360=CARTESIAN_POINT('Ctrl Pts',(-11.1755303080243,8.43123676183979,
11.0749431308556));
#120361=CARTESIAN_POINT('Ctrl Pts',(-11.1741024823302,8.43246867328965,
11.0947173248053));
#120362=CARTESIAN_POINT('Ctrl Pts',(-11.1673006187578,8.43680691062823,
11.1643829547109));
#120363=CARTESIAN_POINT('Ctrl Pts',(-11.1592391090024,8.43989277293091,
11.2139556748244));
#120364=CARTESIAN_POINT('Ctrl Pts',(-11.1371420866949,8.44609923009376,
11.3104634791576));
#120365=CARTESIAN_POINT('Ctrl Pts',(-11.1232944364729,8.4492106695294,11.3573352011814));
#120366=CARTESIAN_POINT('Ctrl Pts',(-11.1026972240125,8.45316127618904,
11.4138628714252));
#120367=CARTESIAN_POINT('Ctrl Pts',(-11.098661577485,8.45391061325622,11.4244600896895));
#120368=CARTESIAN_POINT('Ctrl Pts',(-11.0919771031511,8.45511466317859,
11.4412785494345));
#120369=CARTESIAN_POINT('Ctrl Pts',(-11.0894265614543,8.45556611668206,
11.447538284379));
#120370=CARTESIAN_POINT('Ctrl Pts',(-11.0844882975585,8.45642559101367,
11.45936575003));
#120371=CARTESIAN_POINT('Ctrl Pts',(-11.0821112165235,8.45683324463233,
11.4649377082649));
#120372=CARTESIAN_POINT('Ctrl Pts',(-11.0766009637549,8.45776479018088,
11.4775827366181));
#120373=CARTESIAN_POINT('Ctrl Pts',(-11.0734409038124,8.45828957480671,
11.4846437109426));
#120374=CARTESIAN_POINT('Ctrl Pts',(-11.0634817468255,8.45991528494975,
11.5063215482407));
#120375=CARTESIAN_POINT('Ctrl Pts',(-11.0564521731293,8.46102396340335,
11.5208298161523));
#120376=CARTESIAN_POINT('Ctrl Pts',(-11.0159326493457,8.4672120375939,11.6002600151921));
#120377=CARTESIAN_POINT('Ctrl Pts',(-10.9767615746854,8.47248722130337,
11.6620912002533));
#120378=CARTESIAN_POINT('Ctrl Pts',(-10.9020840994072,8.48143774327591,
11.758785078553));
#120379=CARTESIAN_POINT('Ctrl Pts',(-10.8696375019692,8.48505963192723,
11.7957646249844));
#120380=CARTESIAN_POINT('Ctrl Pts',(-10.811692936878,8.49100932255054,11.854013727516));
#120381=CARTESIAN_POINT('Ctrl Pts',(-10.7874348360801,8.49336837872976,
11.8764312212767));
#120382=CARTESIAN_POINT('Ctrl Pts',(-10.7570670618802,8.49613764545614,
11.902214504601));
#120383=CARTESIAN_POINT('Ctrl Pts',(-10.7518312583617,8.49660882388745,
11.9065822152277));
#120384=CARTESIAN_POINT('Ctrl Pts',(-10.743563837538,8.49734265846856,11.9133580160886));
#120385=CARTESIAN_POINT('Ctrl Pts',(-10.7405578756893,8.49760739967164,
11.9157969643366));
#120386=CARTESIAN_POINT('Ctrl Pts',(-10.7348775038153,8.49810370516149,
11.9203595918809));
#120387=CARTESIAN_POINT('Ctrl Pts',(-10.7322058921926,8.49833548069488,
11.9224864528827));
#120388=CARTESIAN_POINT('Ctrl Pts',(-10.7259770090227,8.49887211557101,
11.9274011373094));
#120389=CARTESIAN_POINT('Ctrl Pts',(-10.7224128942928,8.49917636298976,
11.9301801432769));
#120390=CARTESIAN_POINT('Ctrl Pts',(-10.710636291383,8.50017278712573,11.9392540611455));
#120391=CARTESIAN_POINT('Ctrl Pts',(-10.7023565678057,8.50085926029323,
11.9454614744132));
#120392=CARTESIAN_POINT('Ctrl Pts',(-10.6372387551582,8.50615896316596,
11.9929535123087));
#120393=CARTESIAN_POINT('Ctrl Pts',(-10.5768839080176,8.51049496240418,
12.0291926744667));
#120394=CARTESIAN_POINT('Ctrl Pts',(-10.4616199292691,8.51841845582033,
12.0850554129716));
#120395=CARTESIAN_POINT('Ctrl Pts',(-10.4078057816376,8.52199152730307,
12.106405008037));
#120396=CARTESIAN_POINT('Ctrl Pts',(-10.3321797296197,8.52703818106705,
12.1301379125482));
#120397=CARTESIAN_POINT('Ctrl Pts',(-10.3115452430198,8.52841704855334,
12.1359993633913));
#120398=CARTESIAN_POINT('Ctrl Pts',(-10.2751137668893,8.53086351430993,
12.1452808718164));
#120399=CARTESIAN_POINT('Ctrl Pts',(-10.2593847254968,8.53192358428407,
12.1489453352583));
#120400=CARTESIAN_POINT('Ctrl Pts',(-10.2360120616192,8.53350683901492,
12.153886171082));
#120401=CARTESIAN_POINT('Ctrl Pts',(-10.2284227698922,8.53402217128693,
12.1554124901795));
#120402=CARTESIAN_POINT('Ctrl Pts',(-10.2148681358126,8.53494502245415,
12.1579997631071));
#120403=CARTESIAN_POINT('Ctrl Pts',(-10.2089085606937,8.53535161523942,
12.1590897195966));
#120404=CARTESIAN_POINT('Ctrl Pts',(-10.1962856641109,8.53621471798645,
12.161297829394));
#120405=CARTESIAN_POINT('Ctrl Pts',(-10.1896206211694,8.53667156498084,
12.1624047174872));
#120406=CARTESIAN_POINT('Ctrl Pts',(-10.1717588021953,8.53789905458422,
12.1652133867625));
#120407=CARTESIAN_POINT('Ctrl Pts',(-10.1605466227965,8.53867290495318,
12.1668110769148));
#120408=CARTESIAN_POINT('Ctrl Pts',(-10.1067668585391,8.54240179143784,
12.1736846619688));
#120409=CARTESIAN_POINT('Ctrl Pts',(-10.0639600438863,8.5454226463176,12.1767936005867));
#120410=CARTESIAN_POINT('Ctrl Pts',(-9.9318331881085,8.55490549544547,12.1791592288951));
#120411=CARTESIAN_POINT('Ctrl Pts',(-9.84270097056296,8.56154883121804,
12.1706058066696));
#120412=CARTESIAN_POINT('Ctrl Pts',(-9.73480427928271,8.56952435227488,
12.1476974326235));
#120413=CARTESIAN_POINT('Ctrl Pts',(-9.71433287150389,8.57103292191426,
12.1427740649778));
#120414=CARTESIAN_POINT('Ctrl Pts',(-9.68089175215072,8.57347873015354,
12.1337765857428));
#120415=CARTESIAN_POINT('Ctrl Pts',(-9.66784146782375,8.5744284653335,12.1300221984775));
#120416=CARTESIAN_POINT('Ctrl Pts',(-9.64999773388478,8.57571786933657,
12.1245529429262));
#120417=CARTESIAN_POINT('Ctrl Pts',(-9.64514669553454,8.57606746816337,
12.1230316301923));
#120418=CARTESIAN_POINT('Ctrl Pts',(-9.63697686435524,8.5766544741878,12.120411301907));
#120419=CARTESIAN_POINT('Ctrl Pts',(-9.63365287252975,8.57689280744138,
12.119328846167));
#120420=CARTESIAN_POINT('Ctrl Pts',(-9.62684893492248,8.57737957068267,
12.1170795922912));
#120421=CARTESIAN_POINT('Ctrl Pts',(-9.62336955301328,8.57762791365505,
12.1159113048154));
#120422=CARTESIAN_POINT('Ctrl Pts',(-9.61430674992187,8.57827340915604,
12.1128210308439));
#120423=CARTESIAN_POINT('Ctrl Pts',(-9.60873213673921,8.57866910049231,
12.1108732567818));
#120424=CARTESIAN_POINT('Ctrl Pts',(-9.58576255012235,8.58029479756681,
12.1026533055393));
#120425=CARTESIAN_POINT('Ctrl Pts',(-9.56850080200281,8.58150532596359,
12.0960134626381));
#120426=CARTESIAN_POINT('Ctrl Pts',(-9.44543084244235,8.59010371441348,
12.0453150666999));
#120427=CARTESIAN_POINT('Ctrl Pts',(-9.34639144423488,8.59690633388872,
11.9864240202187));
#120428=CARTESIAN_POINT('Ctrl Pts',(-9.23974955710112,8.60563475777251,
11.8997956577013));
#120429=CARTESIAN_POINT('Ctrl Pts',(-9.22250624374912,8.60709498584035,
11.8849385992635));
#120430=CARTESIAN_POINT('Ctrl Pts',(-9.19322902106502,8.60967210110284,
11.8581964555101));
#120431=CARTESIAN_POINT('Ctrl Pts',(-9.18100038991453,8.61078025256616,
11.8465342053494));
#120432=CARTESIAN_POINT('Ctrl Pts',(-9.16344315195123,8.61242150769173,
11.8290535552397));
#120433=CARTESIAN_POINT('Ctrl Pts',(-9.15791501478316,8.61294588208986,
11.8234379333706));
#120434=CARTESIAN_POINT('Ctrl Pts',(-9.14822549268473,8.61387885713553,
11.8133954503379));
#120435=CARTESIAN_POINT('Ctrl Pts',(-9.14404118908444,8.61428645455235,
11.8089910268986));
#120436=CARTESIAN_POINT('Ctrl Pts',(-9.13532639241484,8.61514545433638,
11.7996744756803));
#120437=CARTESIAN_POINT('Ctrl Pts',(-9.13080326823792,8.61559714675613,
11.7947557820045));
#120438=CARTESIAN_POINT('Ctrl Pts',(-9.11895700031396,8.61679595447838,
11.7816514092818));
#120439=CARTESIAN_POINT('Ctrl Pts',(-9.11170623169963,8.61754601988317,
11.7734014869193));
#120440=CARTESIAN_POINT('Ctrl Pts',(-9.07964155799004,8.62093844524035,
11.7358725110338));
#120441=CARTESIAN_POINT('Ctrl Pts',(-9.05615485478083,8.62363277251214,
11.705495420198));
#120442=CARTESIAN_POINT('Ctrl Pts',(-8.9903641967241,8.63184698680208,11.6112250466583));
#120443=CARTESIAN_POINT('Ctrl Pts',(-8.95276731990563,8.63750243160193,
11.5442996649155));
#120444=CARTESIAN_POINT('Ctrl Pts',(-8.90875880724403,8.64549274175582,
11.4442508500947));
#120445=CARTESIAN_POINT('Ctrl Pts',(-8.89683491623107,8.6478688791902,11.4137550455752));
#120446=CARTESIAN_POINT('Ctrl Pts',(-8.88216639193007,8.65108222244006,
11.3710752012001));
#120447=CARTESIAN_POINT('Ctrl Pts',(-8.87832183314732,8.65195822724983,
11.3592866501721));
#120448=CARTESIAN_POINT('Ctrl Pts',(-8.87196402145976,8.65346601856556,
11.3386940495358));
#120449=CARTESIAN_POINT('Ctrl Pts',(-8.86936597935487,8.65410163734315,
11.3299174931273));
#120450=CARTESIAN_POINT('Ctrl Pts',(-8.86568472277536,8.65503125497131,
11.316927162763));
#120451=CARTESIAN_POINT('Ctrl Pts',(-8.86452218797081,8.6553294445303,11.3127364937871));
#120452=CARTESIAN_POINT('Ctrl Pts',(-8.86257955839264,8.65583564819996,
11.3055801109436));
#120453=CARTESIAN_POINT('Ctrl Pts',(-8.86178780182369,8.6560443133985,11.302617676156));
#120454=CARTESIAN_POINT('Ctrl Pts',(-8.86001555960837,8.65651678528478,
11.2958812956129));
#120455=CARTESIAN_POINT('Ctrl Pts',(-8.8590422363749,8.65678018411602,11.2921055428348));
#120456=CARTESIAN_POINT('Ctrl Pts',(-8.85643101076055,8.65749792195231,
11.2817637716496));
#120457=CARTESIAN_POINT('Ctrl Pts',(-8.85483088807857,8.6579501957944,11.2751882384675));
#120458=CARTESIAN_POINT('Ctrl Pts',(-8.84667118142944,8.6603264909574,11.2403525367526));
#120459=CARTESIAN_POINT('Ctrl Pts',(-8.84110019414229,8.66220107772388,
11.2118684889089));
#120460=CARTESIAN_POINT('Ctrl Pts',(-8.83453145209203,8.66488543934019,
11.170154822135));
#120461=CARTESIAN_POINT('Ctrl Pts',(-8.83269605008768,8.66571881788552,
11.1570703867563));
#120462=CARTESIAN_POINT('Ctrl Pts',(-8.82285691323287,8.67076928251592,
11.0771776993491));
#120463=CARTESIAN_POINT('Ctrl Pts',(-8.82037024494847,8.67487300323337,
11.0098151051508));
#120464=CARTESIAN_POINT('Ctrl Pts',(-8.82624350914554,8.68240500841242,
10.889433487855));
#120465=CARTESIAN_POINT('Ctrl Pts',(-8.83243976139679,8.68578522600619,
10.8365029577041));
#120466=CARTESIAN_POINT('Ctrl Pts',(-8.84431576322054,8.69003862415664,
10.7727927957167));
#120467=CARTESIAN_POINT('Ctrl Pts',(-8.84660560621155,8.69080359317017,
10.7614407292466));
#120468=CARTESIAN_POINT('Ctrl Pts',(-8.850507560211,8.69202684527201,10.7434681499615));
#120469=CARTESIAN_POINT('Ctrl Pts',(-8.85201040669254,8.6924816811359,10.7368244889986));
#120470=CARTESIAN_POINT('Ctrl Pts',(-8.85495641662997,8.69334387049026,
10.7243066193936));
#120471=CARTESIAN_POINT('Ctrl Pts',(-8.85638737502612,8.69375082457745,
10.7184297430666));
#120472=CARTESIAN_POINT('Ctrl Pts',(-8.85973005102203,8.69467563464132,
10.7051474978714));
#120473=CARTESIAN_POINT('Ctrl Pts',(-8.86166874612947,8.69519433490316,
10.6977492659351));
#120474=CARTESIAN_POINT('Ctrl Pts',(-8.8677959586814,8.69678211205941,10.6752627769738));
#120475=CARTESIAN_POINT('Ctrl Pts',(-8.87221330294783,8.69785842702708,
10.6602392307735));
#120476=CARTESIAN_POINT('Ctrl Pts',(-8.90311345343404,8.7049733097886,10.562398982531));
#120477=CARTESIAN_POINT('Ctrl Pts',(-8.93839419861791,8.71130072579013,
10.4826582039402));
#120478=CARTESIAN_POINT('Ctrl Pts',(-9.0159954478927,8.72262181892624,10.3493343297986));
#120479=CARTESIAN_POINT('Ctrl Pts',(-9.05480819377194,8.72756567297334,
10.2941351553612));
#120480=CARTESIAN_POINT('Ctrl Pts',(-9.10314577822001,8.73280540284141,
10.2365811313431));
#120481=CARTESIAN_POINT('Ctrl Pts',(-9.10821996473862,8.73334546988118,
10.2306598665274));
#120482=CARTESIAN_POINT('Ctrl Pts',(-9.1160376757059,8.73416196959699,10.2217183602025));
#120483=CARTESIAN_POINT('Ctrl Pts',(-9.11873858548639,8.73444129303964,
10.2186613908377));
#120484=CARTESIAN_POINT('Ctrl Pts',(-9.12371041990526,8.73495034065239,
10.2130926998654));
#120485=CARTESIAN_POINT('Ctrl Pts',(-9.12597631203077,8.73518040641653,
10.2105767164225));
#120486=CARTESIAN_POINT('Ctrl Pts',(-9.13113830732347,8.73570019787902,
10.2048944518533));
#120487=CARTESIAN_POINT('Ctrl Pts',(-9.13404088882153,8.73598943746571,
10.2017341965808));
#120488=CARTESIAN_POINT('Ctrl Pts',(-9.14164409642154,8.7367394482269,10.193546296282));
#120489=CARTESIAN_POINT('Ctrl Pts',(-9.14637171564984,8.73719829392061,
10.1885437836248));
#120490=CARTESIAN_POINT('Ctrl Pts',(-9.18750670985272,8.7411296442458,10.1457743171033));
#120491=CARTESIAN_POINT('Ctrl Pts',(-9.22636081116914,8.74443662049366,
10.110432285927));
#120492=CARTESIAN_POINT('Ctrl Pts',(-9.30563774023128,8.75073875225215,
10.0474586856642));
#120493=CARTESIAN_POINT('Ctrl Pts',(-9.34567597300713,8.75373375459912,
10.0195235691197));
#120494=CARTESIAN_POINT('Ctrl Pts',(-9.43392488733558,8.76016685352888,
9.96577058855639));
#120495=CARTESIAN_POINT('Ctrl Pts',(-9.48242921746681,8.76360869313542,
9.94066484789565));
#120496=CARTESIAN_POINT('Ctrl Pts',(-9.54611206531721,8.76813400013127,
9.9131233237625));
#120497=CARTESIAN_POINT('Ctrl Pts',(-9.55983860952306,8.76910947268172,
9.90749229522944));
#120498=CARTESIAN_POINT('Ctrl Pts',(-9.58064747193377,8.77059019873423,
9.89941170799842));
#120499=CARTESIAN_POINT('Ctrl Pts',(-9.58765312108235,8.77108903276959,
9.89676784927144));
#120500=CARTESIAN_POINT('Ctrl Pts',(-9.60029747688905,8.77199017875766,
9.89213326249202));
#120501=CARTESIAN_POINT('Ctrl Pts',(-9.60592708114431,8.77239167893117,
9.89011831827345));
#120502=CARTESIAN_POINT('Ctrl Pts',(-9.61808406746698,8.77325944369891,
9.88587125067659));
#120503=CARTESIAN_POINT('Ctrl Pts',(-9.6246161782072,8.77372615889111,9.88365344429567));
#120504=CARTESIAN_POINT('Ctrl Pts',(-9.64225647317828,8.77498796046651,
9.87783647656071));
#120505=CARTESIAN_POINT('Ctrl Pts',(-9.65339907596273,8.77578649181745,
9.87434499655869));
#120506=CARTESIAN_POINT('Ctrl Pts',(-9.71268718016144,8.78004465563389,
9.85673109983618));
#120507=CARTESIAN_POINT('Ctrl Pts',(-9.76163923892622,8.78359601191732,
9.84553252734959));
#120508=CARTESIAN_POINT('Ctrl Pts',(-9.81114930181833,8.78721751211607,
9.83748958013431));
#120509=CARTESIAN_POINT('Origin',(-10.,2.67563288526385,11.));
#120510=CARTESIAN_POINT('',(-9.81114929159341,9.38732021621766,9.83748958179536));
#120511=CARTESIAN_POINT('',(-9.81114930150155,9.28890850071391,9.83748958018577));
#120512=CARTESIAN_POINT('',(-9.81114930150157,2.67563288526385,9.83748958018577));
#120513=CARTESIAN_POINT('Ctrl Pts',(-9.81114929154307,9.38732021693139,
9.83748958180354));
#120514=CARTESIAN_POINT('Ctrl Pts',(-9.80032443062653,9.38653646503526,
9.83924808875628));
#120515=CARTESIAN_POINT('Ctrl Pts',(-9.7895231070358,9.38574897201044,9.84115795741129));
#120516=CARTESIAN_POINT('Ctrl Pts',(-9.72949114500639,9.38134292685675,
9.85263995832945));
#120517=CARTESIAN_POINT('Ctrl Pts',(-9.68088846556259,9.3776625054019,9.8651972060573));
#120518=CARTESIAN_POINT('Ctrl Pts',(-9.61392716259896,9.37249212111339,
9.88714073354232));
#120519=CARTESIAN_POINT('Ctrl Pts',(-9.59478384343625,9.37100253447649,
9.89396750737397));
#120520=CARTESIAN_POINT('Ctrl Pts',(-9.53605463055195,9.36641123538269,
9.91664072613371));
#120521=CARTESIAN_POINT('Ctrl Pts',(-9.49714120270248,9.36333749679626,
9.93414519946232));
#120522=CARTESIAN_POINT('Ctrl Pts',(-9.45322292166835,9.3598935556402,9.95684322497667));
#120523=CARTESIAN_POINT('Ctrl Pts',(-9.44721364051956,9.35942291712428,
9.96001515549274));
#120524=CARTESIAN_POINT('Ctrl Pts',(-9.43747741296814,9.35866175565437,
9.96526254873928));
#120525=CARTESIAN_POINT('Ctrl Pts',(-9.43373379599942,9.35836941849369,
9.9673065113007));
#120526=CARTESIAN_POINT('Ctrl Pts',(-9.42703847290861,9.35784729267967,
9.97100941970892));
#120527=CARTESIAN_POINT('Ctrl Pts',(-9.42408274486057,9.35761705203515,
9.97266079508712));
#120528=CARTESIAN_POINT('Ctrl Pts',(-9.41756052796343,9.35710956599148,
9.97634177502931));
#120529=CARTESIAN_POINT('Ctrl Pts',(-9.41399749646752,9.35683269637592,
9.97837728722175));
#120530=CARTESIAN_POINT('Ctrl Pts',(-9.40359605239276,9.35602529418844,
9.9843918136961));
#120531=CARTESIAN_POINT('Ctrl Pts',(-9.39678684758696,9.35549782406152,
9.98842125471743));
#120532=CARTESIAN_POINT('Ctrl Pts',(-9.33208877350592,9.35049136239869,
10.0275928432357));
#120533=CARTESIAN_POINT('Ctrl Pts',(-9.27728307350225,9.34628730934923,
10.0676030751559));
#120534=CARTESIAN_POINT('Ctrl Pts',(-9.16114682501842,9.33675164390476,
10.1688142367135));
#120535=CARTESIAN_POINT('Ctrl Pts',(-9.10251686948338,9.33144107663792,
10.2324933681102));
#120536=CARTESIAN_POINT('Ctrl Pts',(-9.04206810367296,9.32479866363295,
10.3146475357289));
#120537=CARTESIAN_POINT('Ctrl Pts',(-9.03301822573962,9.32376758093149,
10.3274765960256));
#120538=CARTESIAN_POINT('Ctrl Pts',(-9.01994002506405,9.32221930463233,
10.346826104499));
#120539=CARTESIAN_POINT('Ctrl Pts',(-9.01571430127629,9.32170945607147,
10.3532115099214));
#120540=CARTESIAN_POINT('Ctrl Pts',(-9.00826120605182,9.32079256083556,
10.3647159364668));
#120541=CARTESIAN_POINT('Ctrl Pts',(-9.00501042877679,9.32038639293661,
10.3698195277322));
#120542=CARTESIAN_POINT('Ctrl Pts',(-8.99818538797317,9.31952007059205,
10.3807190366764));
#120543=CARTESIAN_POINT('Ctrl Pts',(-8.99462178613516,9.31905954745268,
10.3865213352271));
#120544=CARTESIAN_POINT('Ctrl Pts',(-8.98514224464405,9.3178119243831,10.4022604794136));
#120545=CARTESIAN_POINT('Ctrl Pts',(-8.97932214949556,9.31702143201238,
10.4122538753469));
#120546=CARTESIAN_POINT('Ctrl Pts',(-8.947712153106,9.3125867776909,10.4684156433584));
#120547=CARTESIAN_POINT('Ctrl Pts',(-8.92491100156425,9.30883960906149,
10.5161881959716));
#120548=CARTESIAN_POINT('Ctrl Pts',(-8.87689532779373,9.2994320460074,10.637101560905));
#120549=CARTESIAN_POINT('Ctrl Pts',(-8.85552284764237,9.29369959223338,
10.7115029722206));
#120550=CARTESIAN_POINT('Ctrl Pts',(-8.83575232374524,9.28576801412107,
10.8192579941486));
#120551=CARTESIAN_POINT('Ctrl Pts',(-8.8312291121996,9.28345778429272,10.8512877085673));
#120552=CARTESIAN_POINT('Ctrl Pts',(-8.82734011420872,9.28072362762297,
10.8903989177766));
#120553=CARTESIAN_POINT('Ctrl Pts',(-8.82671224417878,9.28024184026102,
10.8973381625369));
#120554=CARTESIAN_POINT('Ctrl Pts',(-8.8258253427327,9.27949227928516,10.9082149180464));
#120555=CARTESIAN_POINT('Ctrl Pts',(-8.82552446578684,9.27922233189707,
10.9121487181704));
#120556=CARTESIAN_POINT('Ctrl Pts',(-8.8250253239318,9.27874494796017,10.9191363058126));
#120557=CARTESIAN_POINT('Ctrl Pts',(-8.82481919167721,9.27853709289594,
10.922189367428));
#120558=CARTESIAN_POINT('Ctrl Pts',(-8.8243529723141,9.27803975674625,10.9295195823278));
#120559=CARTESIAN_POINT('Ctrl Pts',(-8.82410432476527,9.27775090639987,
10.9337973913837));
#120560=CARTESIAN_POINT('Ctrl Pts',(-8.82341543058647,9.27687139981388,
10.9468816565464));
#120561=CARTESIAN_POINT('Ctrl Pts',(-8.82305071412459,9.27628469097743,
10.9556920183317));
#120562=CARTESIAN_POINT('Ctrl Pts',(-8.8224290377103,9.27492276813782,10.9763108857761));
#120563=CARTESIAN_POINT('Ctrl Pts',(-8.82225068144433,9.27415122991986,
10.9881209842543));
#120564=CARTESIAN_POINT('Ctrl Pts',(-8.82224825684961,9.27142209641782,
11.0302662602129));
#120565=CARTESIAN_POINT('Ctrl Pts',(-8.82341843592351,9.26950290299789,
11.060591207284));
#120566=CARTESIAN_POINT('Ctrl Pts',(-8.83141895204983,9.26301117334748,
11.1640107879518));
#120567=CARTESIAN_POINT('Ctrl Pts',(-8.84390629886187,9.25854333736454,
11.236492792907));
#120568=CARTESIAN_POINT('Ctrl Pts',(-8.87460691765328,9.25114500448191,
11.3500626974604));
#120569=CARTESIAN_POINT('Ctrl Pts',(-8.888552746776,9.24831696275417,11.3920941457527));
#120570=CARTESIAN_POINT('Ctrl Pts',(-8.90902603454186,9.24466285719496,
11.4438480047155));
#120571=CARTESIAN_POINT('Ctrl Pts',(-8.9133769642662,9.24390895673842,11.4543958713892));
#120572=CARTESIAN_POINT('Ctrl Pts',(-8.92055486561516,9.24269922125629,
11.4711042093946));
#120573=CARTESIAN_POINT('Ctrl Pts',(-8.92328302895718,9.24224669934713,
11.4773065422678));
#120574=CARTESIAN_POINT('Ctrl Pts',(-8.92855091868038,9.24138623949891,
11.4890077845142));
#120575=CARTESIAN_POINT('Ctrl Pts',(-8.93107985122903,9.24097867801445,
11.4945113349354));
#120576=CARTESIAN_POINT('Ctrl Pts',(-8.93692546247149,9.2400488027501,11.5069783808752));
#120577=CARTESIAN_POINT('Ctrl Pts',(-8.94026829368006,9.23952560963872,
11.5139292332034));
#120578=CARTESIAN_POINT('Ctrl Pts',(-8.95075152700913,9.23791033066491,
11.5351901157291));
#120579=CARTESIAN_POINT('Ctrl Pts',(-8.95811506419071,9.23681063723439,
11.5493874362331));
#120580=CARTESIAN_POINT('Ctrl Pts',(-8.9758952273204,9.23423194000081,11.5820248012439));
#120581=CARTESIAN_POINT('Ctrl Pts',(-8.98652444194508,9.23274597497384,
11.600342112871));
#120582=CARTESIAN_POINT('Ctrl Pts',(-9.02732142156539,9.22723674108767,
11.6664736264289));
#120583=CARTESIAN_POINT('Ctrl Pts',(-9.06042413937132,9.22312255442211,
11.7123809878747));
#120584=CARTESIAN_POINT('Ctrl Pts',(-9.14301221338996,9.21368443866707,
11.8110968882251));
#120585=CARTESIAN_POINT('Ctrl Pts',(-9.1943296466672,9.20835758239048,11.8620923834961));
#120586=CARTESIAN_POINT('Ctrl Pts',(-9.25790848101028,9.20257338460449,
11.9146040155316));
#120587=CARTESIAN_POINT('Ctrl Pts',(-9.26590445004343,9.2018594328693,11.9210342388325));
#120588=CARTESIAN_POINT('Ctrl Pts',(-9.27753084952769,9.20084174649476,
11.930136378442));
#120589=CARTESIAN_POINT('Ctrl Pts',(-9.28109391655605,9.20053257046305,
11.9328930274934));
#120590=CARTESIAN_POINT('Ctrl Pts',(-9.28738465713871,9.19999157366911,
11.9377025587014));
#120591=CARTESIAN_POINT('Ctrl Pts',(-9.29010556524019,9.1997591656601,11.9397641236829));
#120592=CARTESIAN_POINT('Ctrl Pts',(-9.29593909032316,9.19926430700382,
11.944144247833));
#120593=CARTESIAN_POINT('Ctrl Pts',(-9.29905423478611,9.19900209371778,
11.9464592757051));
#120594=CARTESIAN_POINT('Ctrl Pts',(-9.30770867270555,9.19827908156675,
11.952824678683));
#120595=CARTESIAN_POINT('Ctrl Pts',(-9.31327211390171,9.19782044641249,
11.9568421845638));
#120596=CARTESIAN_POINT('Ctrl Pts',(-9.34646771233953,9.19511803832189,
11.9803749105727));
#120597=CARTESIAN_POINT('Ctrl Pts',(-9.37489793246477,9.19294248760269,
11.9987428565288));
#120598=CARTESIAN_POINT('Ctrl Pts',(-9.50352620213314,9.18351288866872,
12.0741977795012));
#120599=CARTESIAN_POINT('Ctrl Pts',(-9.61099325259078,9.17662943643949,
12.1176148326397));
#120600=CARTESIAN_POINT('Ctrl Pts',(-9.74237888128779,9.16789052438256,
12.1494004825394));
#120601=CARTESIAN_POINT('Ctrl Pts',(-9.76181162144749,9.16659228391543,
12.1535841245591));
#120602=CARTESIAN_POINT('Ctrl Pts',(-9.78898579577522,9.16476446451009,
12.1587185217358));
#120603=CARTESIAN_POINT('Ctrl Pts',(-9.79664552326458,9.16424789895686,
12.160087306621));
#120604=CARTESIAN_POINT('Ctrl Pts',(-9.80993083688772,9.16334935247259,
12.162325760217));
#120605=CARTESIAN_POINT('Ctrl Pts',(-9.81555026832102,9.16296848411211,
12.1632307398739));
#120606=CARTESIAN_POINT('Ctrl Pts',(-9.82726513249515,9.16217271205424,
12.1650303348333));
#120607=CARTESIAN_POINT('Ctrl Pts',(-9.83336145262615,9.16175760201808,
12.1659179248929));
#120608=CARTESIAN_POINT('Ctrl Pts',(-9.84781736586806,9.16077077815284,
12.1679069320824));
#120609=CARTESIAN_POINT('Ctrl Pts',(-9.85618228128259,9.16019778146712,
12.168966472367));
#120610=CARTESIAN_POINT('Ctrl Pts',(-9.88451407831968,9.15824999734675,
12.1722464162348));
#120611=CARTESIAN_POINT('Ctrl Pts',(-9.90452520127499,9.15686235036861,
12.1740456275925));
#120612=CARTESIAN_POINT('Ctrl Pts',(-9.95318512760633,9.15345724902068,
12.1771684417553));
#120613=CARTESIAN_POINT('Ctrl Pts',(-9.9818541237806,9.15142503813535,12.1779591148728));
#120614=CARTESIAN_POINT('Ctrl Pts',(-10.0957748296821,9.14325183143161,
12.1769413524686));
#120615=CARTESIAN_POINT('Ctrl Pts',(-10.1806910440417,9.13691853979815,
12.1669243253631));
#120616=CARTESIAN_POINT('Ctrl Pts',(-10.2977059408063,9.12820794110521,
12.1400345203897));
#120617=CARTESIAN_POINT('Ctrl Pts',(-10.3312830901864,9.12571417624412,
12.1307340724643));
#120618=CARTESIAN_POINT('Ctrl Pts',(-10.3711536785797,9.12279631489549,
12.1177613447877));
#120619=CARTESIAN_POINT('Ctrl Pts',(-10.3778857917778,9.12230517062908,
12.1155033893213));
#120620=CARTESIAN_POINT('Ctrl Pts',(-10.3883545561332,9.12154425509543,
12.111886506565));
#120621=CARTESIAN_POINT('Ctrl Pts',(-10.3921053097964,9.12127220597862,
12.1105693548588));
#120622=CARTESIAN_POINT('Ctrl Pts',(-10.3990485585029,9.12076975484328,
12.1080915343766));
#120623=CARTESIAN_POINT('Ctrl Pts',(-10.4022427051574,9.12053907571623,
12.1069360447636));
#120624=CARTESIAN_POINT('Ctrl Pts',(-10.40959222389,9.12000932903487,12.1042413266143));
#120625=CARTESIAN_POINT('Ctrl Pts',(-10.4137439538197,9.11971082769298,
12.1026924501138));
#120626=CARTESIAN_POINT('Ctrl Pts',(-10.4268491618685,9.11877067259253,
12.0977188828527));
#120627=CARTESIAN_POINT('Ctrl Pts',(-10.4357698904588,9.11813379727521,
12.0942081930582));
#120628=CARTESIAN_POINT('Ctrl Pts',(-10.4824230609412,9.11481439641758,
12.0751870949907));
#120629=CARTESIAN_POINT('Ctrl Pts',(-10.5193774715623,9.11222375407902,
12.0578312965337));
#120630=CARTESIAN_POINT('Ctrl Pts',(-10.6199467083064,9.10508549124594,
12.0040544452816));
#120631=CARTESIAN_POINT('Ctrl Pts',(-10.6811708359302,9.10062669633543,
11.9635693210663));
#120632=CARTESIAN_POINT('Ctrl Pts',(-10.7729458945962,9.0932213028762,11.8897380979666));
#120633=CARTESIAN_POINT('Ctrl Pts',(-10.8060375073712,9.09037537518844,
11.8598733036482));
#120634=CARTESIAN_POINT('Ctrl Pts',(-10.8453921815564,9.08670119636175,
11.8200839666402));
#120635=CARTESIAN_POINT('Ctrl Pts',(-10.8533093116708,9.08594613614795,
11.8118428768242));
#120636=CARTESIAN_POINT('Ctrl Pts',(-10.8657303098235,9.08473497601275,
11.798531187456));
#120637=CARTESIAN_POINT('Ctrl Pts',(-10.8703125982674,9.08428220308995,
11.793534501295));
#120638=CARTESIAN_POINT('Ctrl Pts',(-10.8789059294,9.08342154344041,11.7840000674971));
#120639=CARTESIAN_POINT('Ctrl Pts',(-10.8829256228384,9.08301403556718,
11.7794703847859));
#120640=CARTESIAN_POINT('Ctrl Pts',(-10.8919805392111,9.08208466843235,
11.7691067329858));
#120641=CARTESIAN_POINT('Ctrl Pts',(-10.8969937519922,9.0815619334867,11.7632539898746));
#120642=CARTESIAN_POINT('Ctrl Pts',(-10.9122105214732,9.07994951831467,
11.7451319800931));
#120643=CARTESIAN_POINT('Ctrl Pts',(-10.9222220894851,9.07885226963748,
11.7327046319635));
#120644=CARTESIAN_POINT('Ctrl Pts',(-10.9448874849234,9.07628032012166,
11.7033694267971));
#120645=CARTESIAN_POINT('Ctrl Pts',(-10.9573448794097,9.07479870840918,
11.6863174170388));
#120646=CARTESIAN_POINT('Ctrl Pts',(-11.0012854501578,9.069314201956,11.622644799856));
#120647=CARTESIAN_POINT('Ctrl Pts',(-11.0298733643898,9.06522128825756,
11.5741243109414));
#120648=CARTESIAN_POINT('Ctrl Pts',(-11.0871772524861,9.05577279194797,
11.4587092898304));
#120649=CARTESIAN_POINT('Ctrl Pts',(-11.1133890861886,9.05041288245019,
11.3908133955653));
#120650=CARTESIAN_POINT('Ctrl Pts',(-11.1356975369001,9.04467060412752,
11.3120440255709));
#120651=CARTESIAN_POINT('Ctrl Pts',(-11.1381098155511,9.04402741239055,
11.3031277450942));
#120652=CARTESIAN_POINT('Ctrl Pts',(-11.1415318320646,9.0430814385073,11.2898621351395));
#120653=CARTESIAN_POINT('Ctrl Pts',(-11.1426220732322,9.04277453331848,
11.2855342017552));
#120654=CARTESIAN_POINT('Ctrl Pts',(-11.1444509633795,9.04225012659281,
11.2780958001991));
#120655=CARTESIAN_POINT('Ctrl Pts',(-11.1452015887949,9.0420319693341,11.2749883694095));
#120656=CARTESIAN_POINT('Ctrl Pts',(-11.1467523307558,9.04157507176851,
11.2684521384904));
#120657=CARTESIAN_POINT('Ctrl Pts',(-11.1475497398003,9.04133649510714,
11.2650227423568));
#120658=CARTESIAN_POINT('Ctrl Pts',(-11.1494882969301,9.04074719970246,
11.2565128276514));
#120659=CARTESIAN_POINT('Ctrl Pts',(-11.1506111714546,9.04039749437796,
11.2514281411649));
#120660=CARTESIAN_POINT('Ctrl Pts',(-11.1547225321603,9.0390839501421,11.232206207273));
#120661=CARTESIAN_POINT('Ctrl Pts',(-11.1574846318216,9.03813184777235,
11.2180211506746));
#120662=CARTESIAN_POINT('Ctrl Pts',(-11.1639590271024,9.03569431613876,
11.1811681515621));
#120663=CARTESIAN_POINT('Ctrl Pts',(-11.1672706957847,9.03422573141662,
11.1584353796791));
#120664=CARTESIAN_POINT('Ctrl Pts',(-11.183742724702,9.02518357582828,11.0163395930413));
#120665=CARTESIAN_POINT('Ctrl Pts',(-11.179248647086,9.01802501140546,10.8956516867982));
#120666=CARTESIAN_POINT('Ctrl Pts',(-11.1534124868851,9.00912652773981,
10.761217268834));
#120667=CARTESIAN_POINT('Ctrl Pts',(-11.1498875617642,9.00802411922803,
10.7447822360053));
#120668=CARTESIAN_POINT('Ctrl Pts',(-11.1442182103416,9.00639528232526,
10.720857943403));
#120669=CARTESIAN_POINT('Ctrl Pts',(-11.1423491737566,9.00587752541123,
10.7133051081505));
#120670=CARTESIAN_POINT('Ctrl Pts',(-11.138886357589,9.00495087840997,10.6998835176293));
#120671=CARTESIAN_POINT('Ctrl Pts',(-11.1373216871211,9.00454292749327,
10.6940074900681));
#120672=CARTESIAN_POINT('Ctrl Pts',(-11.1339456821418,9.0036844771404,10.6817128180174));
#120673=CARTESIAN_POINT('Ctrl Pts',(-11.1321251943536,9.00323369718965,
10.6752969334643));
#120674=CARTESIAN_POINT('Ctrl Pts',(-11.127181125936,9.00204032905196,10.6584199057474));
#120675=CARTESIAN_POINT('Ctrl Pts',(-11.1239664688353,9.00129483999836,
10.6479863433264));
#120676=CARTESIAN_POINT('Ctrl Pts',(-11.107550429658,8.99762885606164,10.5972250383851));
#120677=CARTESIAN_POINT('Ctrl Pts',(-11.0923227126164,8.99464359061973,
10.5575907389631));
#120678=CARTESIAN_POINT('Ctrl Pts',(-11.0310224673367,8.98388645580076,
10.4206277431398));
#120679=CARTESIAN_POINT('Ctrl Pts',(-10.9738006948832,8.97580669306645,
10.3288900123771));
#120680=CARTESIAN_POINT('Ctrl Pts',(-10.89444504035,8.96700241641876,10.2336246848445));
#120681=CARTESIAN_POINT('Ctrl Pts',(-10.8837056679637,8.96585233314149,
10.2212655059318));
#120682=CARTESIAN_POINT('Ctrl Pts',(-10.8689239135409,8.96432817388114,
10.2049540209413));
#120683=CARTESIAN_POINT('Ctrl Pts',(-10.865106294658,8.96393961009118,10.2008016651149));
#120684=CARTESIAN_POINT('Ctrl Pts',(-10.8590392579699,8.9633302595825,10.1942970735888));
#120685=CARTESIAN_POINT('Ctrl Pts',(-10.8568097312952,8.96310804387674,
10.1919265272448));
#120686=CARTESIAN_POINT('Ctrl Pts',(-10.8521807447933,8.96265025083665,
10.1870454500707));
#120687=CARTESIAN_POINT('Ctrl Pts',(-10.8497799757864,8.96241479143939,
10.1845362576202));
#120688=CARTESIAN_POINT('Ctrl Pts',(-10.8439253374822,8.96184524823,10.1784711445967));
#120689=CARTESIAN_POINT('Ctrl Pts',(-10.8404599976609,8.96151202830936,
10.1749262881278));
#120690=CARTESIAN_POINT('Ctrl Pts',(-10.8280262101665,8.96032973168817,
10.1623668171171));
#120691=CARTESIAN_POINT('Ctrl Pts',(-10.8189339106631,8.95948957535603,
10.1534753187875));
#120692=CARTESIAN_POINT('Ctrl Pts',(-10.7957378982657,8.95740094120697,
10.131515190174));
#120693=CARTESIAN_POINT('Ctrl Pts',(-10.7814545148012,8.95616385566662,
10.1186410536026));
#120694=CARTESIAN_POINT('Ctrl Pts',(-10.7124677317738,8.95037986688048,
10.0594570327741));
#120695=CARTESIAN_POINT('Ctrl Pts',(-10.6539249173861,8.94601280985897,
10.0178519062093));
#120696=CARTESIAN_POINT('Ctrl Pts',(-10.5385745927734,8.93771675750475,
9.95078803646274));
#120697=CARTESIAN_POINT('Ctrl Pts',(-10.4828383023102,8.93382430986824,
9.9240009086476));
#120698=CARTESIAN_POINT('Ctrl Pts',(-10.4139821795683,8.92898486131499,
9.89733950191145));
#120699=CARTESIAN_POINT('Ctrl Pts',(-10.4026342940805,8.92818660108786,
9.89314543563708));
#120700=CARTESIAN_POINT('Ctrl Pts',(-10.3846268725791,8.92691779300244,
9.88680363202755));
#120701=CARTESIAN_POINT('Ctrl Pts',(-10.3780091533756,8.92645106949463,
9.88453908127923));
#120702=CARTESIAN_POINT('Ctrl Pts',(-10.365649144957,8.92557836217799,9.8804321684641));
#120703=CARTESIAN_POINT('Ctrl Pts',(-10.3599120896341,8.92517288573222,
9.87857469618404));
#120704=CARTESIAN_POINT('Ctrl Pts',(-10.3471112000983,8.92426715143396,
9.87453853035606));
#120705=CARTESIAN_POINT('Ctrl Pts',(-10.3400406589412,8.9237661911404,9.87238213438821));
#120706=CARTESIAN_POINT('Ctrl Pts',(-10.3191873207458,8.92228644900763,
9.86623618273146));
#120707=CARTESIAN_POINT('Ctrl Pts',(-10.3053517942695,8.9213018002051,9.86243189683846));
#120708=CARTESIAN_POINT('Ctrl Pts',(-10.2421166925899,8.9167865152561,9.84628114990267));
#120709=CARTESIAN_POINT('Ctrl Pts',(-10.19202410238,8.91316507363937,9.83689502458227));
#120710=CARTESIAN_POINT('Ctrl Pts',(-10.0596815728429,8.90350742160279,
9.8208802736158));
#120711=CARTESIAN_POINT('Ctrl Pts',(-9.97706707226339,8.89737694700525,
9.81959384092877));
#120712=CARTESIAN_POINT('Ctrl Pts',(-9.86991334781599,8.88964401660275,
9.82918544241997));
#120713=CARTESIAN_POINT('Ctrl Pts',(-9.84490652880269,8.88785690149479,
9.83223482927368));
#120714=CARTESIAN_POINT('Ctrl Pts',(-9.81705786206104,8.88589957251103,
9.83654128177284));
#120715=CARTESIAN_POINT('Ctrl Pts',(-9.8141026859178,8.88569228767676,9.83700980064966));
#120716=CARTESIAN_POINT('Ctrl Pts',(-9.81114930149677,8.88548556788545,
9.83748958018655));
#120717=CARTESIAN_POINT('Ctrl Pts',(-9.81114930181833,8.78721751211607,
9.83748958013431));
#120718=CARTESIAN_POINT('Ctrl Pts',(-9.81217914363668,8.78729284169822,
9.83732228155093));
#120719=CARTESIAN_POINT('Ctrl Pts',(-9.81320922699522,8.78736820014809,
9.83715634831394));
#120720=CARTESIAN_POINT('Ctrl Pts',(-9.88853221837043,8.79287945254868,
9.82512545067859));
#120721=CARTESIAN_POINT('Ctrl Pts',(-9.96378569904865,8.79845834619609,
9.82040565303448));
#120722=CARTESIAN_POINT('Ctrl Pts',(-10.0741778762675,8.80647428336804,
9.82406059275664));
#120723=CARTESIAN_POINT('Ctrl Pts',(-10.1093171190298,8.80899797592169,
9.82680516450662));
#120724=CARTESIAN_POINT('Ctrl Pts',(-10.1513650234862,8.81194670009575,
9.83199546181664));
#120725=CARTESIAN_POINT('Ctrl Pts',(-10.1584384678307,8.81244028765832,
9.83293392229028));
#120726=CARTESIAN_POINT('Ctrl Pts',(-10.1694459948495,8.8132041202846,9.83449625635932));
#120727=CARTESIAN_POINT('Ctrl Pts',(-10.173386038307,8.81347667104483,9.83507588036449));
#120728=CARTESIAN_POINT('Ctrl Pts',(-10.1806791570613,8.81397948894335,
9.83618660052427));
#120729=CARTESIAN_POINT('Ctrl Pts',(-10.1840328817114,8.81421003820732,
9.83671220864987));
#120730=CARTESIAN_POINT('Ctrl Pts',(-10.1917458539907,8.81473876154773,
9.83795520478042));
#120731=CARTESIAN_POINT('Ctrl Pts',(-10.1961033845614,8.81503637667364,
9.83868262617167));
#120732=CARTESIAN_POINT('Ctrl Pts',(-10.2098356857319,8.81597112327116,
9.84105451590009));
#120733=CARTESIAN_POINT('Ctrl Pts',(-10.2191949504863,8.81660355255421,
9.84278816202906));
#120734=CARTESIAN_POINT('Ctrl Pts',(-10.2886398676579,8.82126842151982,
9.85652444856068));
#120735=CARTESIAN_POINT('Ctrl Pts',(-10.3477361577329,8.82508622012151,
9.87308790482921));
#120736=CARTESIAN_POINT('Ctrl Pts',(-10.490507686336,8.834506616183,9.92541336061975));
#120737=CARTESIAN_POINT('Ctrl Pts',(-10.57182759508,8.84007346692032,9.96639204573868));
#120738=CARTESIAN_POINT('Ctrl Pts',(-10.6604605161511,8.84698827101984,
10.0247447263933));
#120739=CARTESIAN_POINT('Ctrl Pts',(-10.6731214674889,8.84799742012946,
10.0334399155894));
#120740=CARTESIAN_POINT('Ctrl Pts',(-10.691779799166,8.84951903384249,10.0467983518149));
#120741=CARTESIAN_POINT('Ctrl Pts',(-10.6979083017919,8.85002452518385,
10.0512762939512));
#120742=CARTESIAN_POINT('Ctrl Pts',(-10.708837657432,8.85093655759052,10.0594253049012));
#120743=CARTESIAN_POINT('Ctrl Pts',(-10.7136543864796,8.85134225617695,
10.0630747116284));
#120744=CARTESIAN_POINT('Ctrl Pts',(-10.7238692363989,8.8522107973207,10.0709384898572));
#120745=CARTESIAN_POINT('Ctrl Pts',(-10.7292590903946,8.85267403317879,
10.0751631837498));
#120746=CARTESIAN_POINT('Ctrl Pts',(-10.7437964615153,8.85393719183602,
10.0867640135112));
#120747=CARTESIAN_POINT('Ctrl Pts',(-10.7528707186633,8.85474065505843,
10.0942302683194));
#120748=CARTESIAN_POINT('Ctrl Pts',(-10.8051857487542,8.85946293365098,
10.1386041311387));
#120749=CARTESIAN_POINT('Ctrl Pts',(-10.8458140074639,8.86350173378712,
10.1784625078228));
#120750=CARTESIAN_POINT('Ctrl Pts',(-10.9386581686194,8.87368125311974,
10.2837621182961));
#120751=CARTESIAN_POINT('Ctrl Pts',(-10.9870871983317,8.87990034135288,
10.3521309480626));
#120752=CARTESIAN_POINT('Ctrl Pts',(-11.0390812993549,8.887535395673,10.4450836393841));
#120753=CARTESIAN_POINT('Ctrl Pts',(-11.0497013912911,8.88916074056652,
10.4654447926757));
#120754=CARTESIAN_POINT('Ctrl Pts',(-11.0624977128322,8.89119645197451,
10.4918325153381));
#120755=CARTESIAN_POINT('Ctrl Pts',(-11.0652288145833,8.89163585668405,
10.4975826840628));
#120756=CARTESIAN_POINT('Ctrl Pts',(-11.0695037580035,8.892331304407,10.5067748987938));
#120757=CARTESIAN_POINT('Ctrl Pts',(-11.0710778701415,8.89258909784036,
10.5102026072492));
#120758=CARTESIAN_POINT('Ctrl Pts',(-11.07405838785,8.89308045723284,10.5167759175706));
#120759=CARTESIAN_POINT('Ctrl Pts',(-11.0754674816029,8.89331417324166,
10.5199201830323));
#120760=CARTESIAN_POINT('Ctrl Pts',(-11.0788085483953,8.89387184412986,
10.5274640053804));
#120761=CARTESIAN_POINT('Ctrl Pts',(-11.080727459549,8.89419502332695,10.5318693446502));
#120762=CARTESIAN_POINT('Ctrl Pts',(-11.0872454870586,8.89530327469764,
10.5470868043181));
#120763=CARTESIAN_POINT('Ctrl Pts',(-11.0917099141055,8.89608083444063,
10.5579563357465));
#120764=CARTESIAN_POINT('Ctrl Pts',(-11.1023309611704,8.89798231240072,
10.5849583130967));
#120765=CARTESIAN_POINT('Ctrl Pts',(-11.1082970667748,8.89909728313716,
10.6011631601668));
#120766=CARTESIAN_POINT('Ctrl Pts',(-11.1326041233348,8.90387890045194,
10.6719483590693));
#120767=CARTESIAN_POINT('Ctrl Pts',(-11.1472863828311,8.90742236888328,
10.7277044038575));
#120768=CARTESIAN_POINT('Ctrl Pts',(-11.1711486005192,8.91548468030999,
10.8558001469946));
#120769=CARTESIAN_POINT('Ctrl Pts',(-11.1778150171182,8.92000420582508,
10.9283570916866));
#120770=CARTESIAN_POINT('Ctrl Pts',(-11.1777349892736,8.92578529644395,
11.0171934049905));
#120771=CARTESIAN_POINT('Ctrl Pts',(-11.177388994329,8.92684428617756,11.0333231668098));
#120772=CARTESIAN_POINT('Ctrl Pts',(-11.1763870004886,8.92842623555848,
11.0571713668401));
#120773=CARTESIAN_POINT('Ctrl Pts',(-11.1759859894112,8.9289413618942,11.0648990604175));
#120774=CARTESIAN_POINT('Ctrl Pts',(-11.1751353144204,8.92986398440066,
11.0786686447434));
#120775=CARTESIAN_POINT('Ctrl Pts',(-11.174715121116,8.93027055621383,11.0847121286903));
#120776=CARTESIAN_POINT('Ctrl Pts',(-11.1737275778251,8.93113376175845,
11.0974900395759));
#120777=CARTESIAN_POINT('Ctrl Pts',(-11.173148851033,8.93159073364153,11.1042233409543));
#120778=CARTESIAN_POINT('Ctrl Pts',(-11.1714445329448,8.93281891897082,
11.1222342712521));
#120779=CARTESIAN_POINT('Ctrl Pts',(-11.1702140716586,8.93359334653481,
11.1335010178738));
#120780=CARTESIAN_POINT('Ctrl Pts',(-11.1628316821674,8.93772465065677,
11.1931128841886));
#120781=CARTESIAN_POINT('Ctrl Pts',(-11.1538468086768,8.94116825021961,
11.2410529378607));
#120782=CARTESIAN_POINT('Ctrl Pts',(-11.1296209295448,8.94830194390495,
11.3370107767009));
#120783=CARTESIAN_POINT('Ctrl Pts',(-11.1142172343292,8.95198927789017,
11.3848884305607));
#120784=CARTESIAN_POINT('Ctrl Pts',(-11.0885814999662,8.9571218461473,11.4499709215877));
#120785=CARTESIAN_POINT('Ctrl Pts',(-11.0808990260695,8.95856668779901,
11.4681248023011));
#120786=CARTESIAN_POINT('Ctrl Pts',(-11.0548603356207,8.96316956290856,
11.5255917255573));
#120787=CARTESIAN_POINT('Ctrl Pts',(-11.0347845379642,8.96629876578241,
11.5640911175499));
#120788=CARTESIAN_POINT('Ctrl Pts',(-11.0088492644349,8.9698365090596,11.6077606250268));
#120789=CARTESIAN_POINT('Ctrl Pts',(-11.0050108171361,8.97034870365302,
11.6140871925809));
#120790=CARTESIAN_POINT('Ctrl Pts',(-10.9989840952081,8.97113506074841,
11.6238126102224));
#120791=CARTESIAN_POINT('Ctrl Pts',(-10.9968376054625,8.97141174294187,
11.6272369446348));
#120792=CARTESIAN_POINT('Ctrl Pts',(-10.9928590160677,8.97191830728661,
11.6335120512491));
#120793=CARTESIAN_POINT('Ctrl Pts',(-10.9910322304903,8.9721485080222,11.6363659823849));
#120794=CARTESIAN_POINT('Ctrl Pts',(-10.9868389296037,8.97267154383687,
11.6428551964744));
#120795=CARTESIAN_POINT('Ctrl Pts',(-10.9844646271373,8.97296386591053,
11.6464853254508));
#120796=CARTESIAN_POINT('Ctrl Pts',(-10.9770508895488,8.97386516039381,
11.6576848105663));
#120797=CARTESIAN_POINT('Ctrl Pts',(-10.9719436663379,8.97446989501998,
11.6652091946876));
#120798=CARTESIAN_POINT('Ctrl Pts',(-10.9273617054979,8.97961943163362,
11.7292812366038));
#120799=CARTESIAN_POINT('Ctrl Pts',(-10.8830721135756,8.98388803988168,
11.782328060993));
#120800=CARTESIAN_POINT('Ctrl Pts',(-10.7758658888013,8.99328681619203,
11.8899456242137));
#120801=CARTESIAN_POINT('Ctrl Pts',(-10.7113105864744,8.99840182432431,
11.9423408921894));
#120802=CARTESIAN_POINT('Ctrl Pts',(-10.6284895198859,9.00483260099497,
11.9961664983533));
#120803=CARTESIAN_POINT('Ctrl Pts',(-10.6150140089508,9.00587439486937,
12.0045419349325));
#120804=CARTESIAN_POINT('Ctrl Pts',(-10.5947641559801,9.00743555144133,
12.0165676360184));
#120805=CARTESIAN_POINT('Ctrl Pts',(-10.5881162379497,9.00794738303571,
12.0204280698899));
#120806=CARTESIAN_POINT('Ctrl Pts',(-10.5761675167285,9.00886635981372,
12.0272111220553));
#120807=CARTESIAN_POINT('Ctrl Pts',(-10.5708810300333,9.00927260865949,
12.0301585042232));
#120808=CARTESIAN_POINT('Ctrl Pts',(-10.5596184156277,9.01013752015906,
12.0363244484792));
#120809=CARTESIAN_POINT('Ctrl Pts',(-10.553636732481,9.01059653919139,12.0395323461756));
#120810=CARTESIAN_POINT('Ctrl Pts',(-10.5374734492557,9.01183613629482,
12.0480214244391));
#120811=CARTESIAN_POINT('Ctrl Pts',(-10.5272420975913,9.01262003350744,
12.0532057582191));
#120812=CARTESIAN_POINT('Ctrl Pts',(-10.4709985435536,9.01692645603221,
12.0806800371523));
#120813=CARTESIAN_POINT('Ctrl Pts',(-10.4236541475633,9.02054491464231,
12.1001021948276));
#120814=CARTESIAN_POINT('Ctrl Pts',(-10.309276901016,9.02925880599954,12.1385429850584));
#120815=CARTESIAN_POINT('Ctrl Pts',(-10.2415186556002,9.03440446895688,
12.1548160630736));
#120816=CARTESIAN_POINT('Ctrl Pts',(-10.1601725931716,9.04039695468296,
12.1668765471568));
#120817=CARTESIAN_POINT('Ctrl Pts',(-10.1475887837073,9.04131846547583,
12.1685348527222));
#120818=CARTESIAN_POINT('Ctrl Pts',(-10.1056473190783,9.04436723267493,
12.1733735915057));
#120819=CARTESIAN_POINT('Ctrl Pts',(-10.0761945526865,9.04647166606036,
12.1756537142102));
#120820=CARTESIAN_POINT('Ctrl Pts',(-10.0398888750311,9.04899793501454,
12.1770939621699));
#120821=CARTESIAN_POINT('Ctrl Pts',(-10.0330906607521,9.04946804853283,
12.1773046894365));
#120822=CARTESIAN_POINT('Ctrl Pts',(-10.0223849300082,9.05020337792364,
12.1775437320413));
#120823=CARTESIAN_POINT('Ctrl Pts',(-10.0184785741322,9.05047064086738,
12.1776115103777));
#120824=CARTESIAN_POINT('Ctrl Pts',(-10.0115070684675,9.0509456597272,12.1776977729446));
#120825=CARTESIAN_POINT('Ctrl Pts',(-10.0084421776964,9.05115381097372,
12.1777237311734));
#120826=CARTESIAN_POINT('Ctrl Pts',(-10.0010400613329,9.05165491560924,
12.177757526471));
#120827=CARTESIAN_POINT('Ctrl Pts',(-9.99670284998123,9.05194720930854,
12.1777533711183));
#120828=CARTESIAN_POINT('Ctrl Pts',(-9.98327479863973,9.0528483264862,12.1776663269543));
#120829=CARTESIAN_POINT('Ctrl Pts',(-9.97418456748794,9.05345291457749,
12.1775021383639));
#120830=CARTESIAN_POINT('Ctrl Pts',(-9.89642719078224,9.05858501960186,
12.1751967484587));
#120831=CARTESIAN_POINT('Ctrl Pts',(-9.82805717397522,9.06283844932961,
12.1671559717956));
#120832=CARTESIAN_POINT('Ctrl Pts',(-9.67929824221765,9.07223888232213,
12.1362961018654));
#120833=CARTESIAN_POINT('Ctrl Pts',(-9.59985616958305,9.07737038382616,
12.1108111339311));
#120834=CARTESIAN_POINT('Ctrl Pts',(-9.50926675535917,9.0838190652842,12.0707601354034));
#120835=CARTESIAN_POINT('Ctrl Pts',(-9.49489895759711,9.08486007962245,
12.064057932262));
#120836=CARTESIAN_POINT('Ctrl Pts',(-9.47377365672992,9.08642029299866,
12.0536792491373));
#120837=CARTESIAN_POINT('Ctrl Pts',(-9.46690944300894,9.08693197449629,
12.0502231085752));
#120838=CARTESIAN_POINT('Ctrl Pts',(-9.45470076372537,9.08785078576587,
12.0439254938016));
#120839=CARTESIAN_POINT('Ctrl Pts',(-9.44934340405423,9.08825702047573,
12.0411095065844));
#120840=CARTESIAN_POINT('Ctrl Pts',(-9.43802323661951,9.08912201250749,
12.0350474721965));
#120841=CARTESIAN_POINT('Ctrl Pts',(-9.43206633614897,9.08958112705322,
12.0317909199131));
#120842=CARTESIAN_POINT('Ctrl Pts',(-9.4161165051537,9.09082125697064,12.0228914043181));
#120843=CARTESIAN_POINT('Ctrl Pts',(-9.4061775645365,9.09160559642151,12.0171537049903));
#120844=CARTESIAN_POINT('Ctrl Pts',(-9.35232447110803,9.09592055355682,
11.9850062652558));
#120845=CARTESIAN_POINT('Ctrl Pts',(-9.31009185543225,9.09954756707406,
11.9559008222945));
#120846=CARTESIAN_POINT('Ctrl Pts',(-9.21454110197612,9.10834226466559,
11.8804121310864));
#120847=CARTESIAN_POINT('Ctrl Pts',(-9.16323137527353,9.11356340557285,
11.8317983703183));
#120848=CARTESIAN_POINT('Ctrl Pts',(-9.09003100777206,9.1216238726878,11.7487746871832));
#120849=CARTESIAN_POINT('Ctrl Pts',(-9.06503253792432,9.12451260256411,
11.7173169748328));
#120850=CARTESIAN_POINT('Ctrl Pts',(-9.03742029580544,9.12782058198034,
11.6786672715583));
#120851=CARTESIAN_POINT('Ctrl Pts',(-9.03320870139038,9.12832865533921,
11.6726541043924));
#120852=CARTESIAN_POINT('Ctrl Pts',(-9.02677343916909,9.12911002906179,
11.6632807486305));
#120853=CARTESIAN_POINT('Ctrl Pts',(-9.0245104125778,9.12938580103322,11.6599479951163));
#120854=CARTESIAN_POINT('Ctrl Pts',(-9.02037471234452,9.1298915248187,11.6537896055271));
#120855=CARTESIAN_POINT('Ctrl Pts',(-9.0184971276118,9.13012178723625,11.6509674834636));
#120856=CARTESIAN_POINT('Ctrl Pts',(-9.01423536889355,9.13064600869969,
11.6445014471614));
#120857=CARTESIAN_POINT('Ctrl Pts',(-9.01185919538046,9.13093944504688,
11.6408523816671));
#120858=CARTESIAN_POINT('Ctrl Pts',(-9.00453574923229,9.1318477191234,11.6294682611041));
#120859=CARTESIAN_POINT('Ctrl Pts',(-8.99965851150791,9.1324582241955,11.6216882542368));
#120860=CARTESIAN_POINT('Ctrl Pts',(-8.98838345538847,9.13388502870457,
11.6032263555899));
#120861=CARTESIAN_POINT('Ctrl Pts',(-8.98206294536905,9.13469715239179,
11.5924983111881));
#120862=CARTESIAN_POINT('Ctrl Pts',(-8.95964337146803,9.13763143703435,
11.5530265832466));
#120863=CARTESIAN_POINT('Ctrl Pts',(-8.94458108286684,9.13970877253897,
11.5237094000783));
#120864=CARTESIAN_POINT('Ctrl Pts',(-8.89856897859478,9.14655858600484,
11.4240781093049));
#120865=CARTESIAN_POINT('Ctrl Pts',(-8.87326777545926,9.1512335043338,11.3513787597083));
#120866=CARTESIAN_POINT('Ctrl Pts',(-8.84632791663282,9.15848474035216,
11.2399354704662));
#120867=CARTESIAN_POINT('Ctrl Pts',(-8.83921268181324,9.16091634912756,
11.2027329897751));
#120868=CARTESIAN_POINT('Ctrl Pts',(-8.83236085205739,9.16412539061146,
11.154384053541));
#120869=CARTESIAN_POINT('Ctrl Pts',(-8.83097238584885,9.16485138825542,
11.1434922989329));
#120870=CARTESIAN_POINT('Ctrl Pts',(-8.82898428312476,9.1660267721978,11.1259440168871));
#120871=CARTESIAN_POINT('Ctrl Pts',(-8.82828865127806,9.1664731714854,11.1192988546944));
#120872=CARTESIAN_POINT('Ctrl Pts',(-8.82706852245927,9.16732884364298,
11.1066007565577));
#120873=CARTESIAN_POINT('Ctrl Pts',(-8.82653424564735,9.16773779882173,
11.1005489596915));
#120874=CARTESIAN_POINT('Ctrl Pts',(-8.82541446984163,9.16868066168069,
11.0866372534615));
#120875=CARTESIAN_POINT('Ctrl Pts',(-8.82486100618216,9.16921554265581,
11.0787751314072));
#120876=CARTESIAN_POINT('Ctrl Pts',(-8.8233687001217,9.17090545739777,11.0540336357764));
#120877=CARTESIAN_POINT('Ctrl Pts',(-8.82271438232854,9.1720691565603,11.0371399080642));
#120878=CARTESIAN_POINT('Ctrl Pts',(-8.82203258342463,9.17482616255882,
10.9974698286009));
#120879=CARTESIAN_POINT('Ctrl Pts',(-8.8223017294407,9.1764278383377,10.9746958016619));
#120880=CARTESIAN_POINT('Ctrl Pts',(-8.82791819165112,9.18621444235574,
10.8371597071616));
#120881=CARTESIAN_POINT('Ctrl Pts',(-8.84937208907464,9.1948494406038,10.7236990689699));
#120882=CARTESIAN_POINT('Ctrl Pts',(-8.89287407362688,9.20433134877922,
10.5978791993898));
#120883=CARTESIAN_POINT('Ctrl Pts',(-8.89924652861694,9.20561813660484,
10.5807496693198));
#120884=CARTESIAN_POINT('Ctrl Pts',(-8.90819297292411,9.20729201244887,
10.5583134133446));
#120885=CARTESIAN_POINT('Ctrl Pts',(-8.91041140763523,9.20769729797516,
10.5528687796668));
#120886=CARTESIAN_POINT('Ctrl Pts',(-8.91407869166553,9.20835142407162,
10.5440576755381));
#120887=CARTESIAN_POINT('Ctrl Pts',(-8.91550261325906,9.20860168130448,
10.5406810365197));
#120888=CARTESIAN_POINT('Ctrl Pts',(-8.91831703917647,9.20908904429194,
10.5340930563904));
#120889=CARTESIAN_POINT('Ctrl Pts',(-8.91970612645554,9.20932622276822,
10.5308811930303));
#120890=CARTESIAN_POINT('Ctrl Pts',(-8.92315572034549,9.209907144738,10.5230015800378));
#120891=CARTESIAN_POINT('Ctrl Pts',(-8.92523231546658,9.21024993784047,
10.5183408654161));
#120892=CARTESIAN_POINT('Ctrl Pts',(-8.93299860294191,9.21150737760295,
10.5012105258155));
#120893=CARTESIAN_POINT('Ctrl Pts',(-8.93887580535044,9.21241153989564,
10.4888264442241));
#120894=CARTESIAN_POINT('Ctrl Pts',(-8.9544472459475,9.21469746671847,10.4574418308564));
#120895=CARTESIAN_POINT('Ctrl Pts',(-8.96444411629919,9.21606489826338,
10.4385963583646));
#120896=CARTESIAN_POINT('Ctrl Pts',(-9.00262635101331,9.22097970736207,
10.3711120106389));
#120897=CARTESIAN_POINT('Ctrl Pts',(-9.03377275714509,9.22443176304719,
10.324233839698));
#120898=CARTESIAN_POINT('Ctrl Pts',(-9.11319847588293,9.23247497086787,
10.2214727945865));
#120899=CARTESIAN_POINT('Ctrl Pts',(-9.16360986827574,9.23707643729784,
10.1675511771322));
#120900=CARTESIAN_POINT('Ctrl Pts',(-9.22782401362489,9.24270007268017,
10.1106253613136));
#120901=CARTESIAN_POINT('Ctrl Pts',(-9.2370497229487,9.24350255706174,10.1026985686418));
#120902=CARTESIAN_POINT('Ctrl Pts',(-9.25178173602707,9.24477651551689,
10.0904321891394));
#120903=CARTESIAN_POINT('Ctrl Pts',(-9.25720701603082,9.24524411094678,
10.0859963060825));
#120904=CARTESIAN_POINT('Ctrl Pts',(-9.26737167552583,9.24611749872227,
10.0778356261446));
#120905=CARTESIAN_POINT('Ctrl Pts',(-9.27210071086898,9.24652277504439,
10.0740982682803));
#120906=CARTESIAN_POINT('Ctrl Pts',(-9.28267589301659,9.24742684423489,
10.0658717884464));
#120907=CARTESIAN_POINT('Ctrl Pts',(-9.28853587268803,9.24792632851136,
10.0614009474974));
#120908=CARTESIAN_POINT('Ctrl Pts',(-9.3058460340239,9.24939771624038,10.0484494989833));
#120909=CARTESIAN_POINT('Ctrl Pts',(-9.31740825911904,9.25037538841595,
10.0401215863885));
#120910=CARTESIAN_POINT('Ctrl Pts',(-9.34410875904977,9.25262250546335,
10.0216164376162));
#120911=CARTESIAN_POINT('Ctrl Pts',(-9.35933779205176,9.25389667782512,
10.0115772219069));
#120912=CARTESIAN_POINT('Ctrl Pts',(-9.41217788882717,9.25829315417297,
9.97847846988859));
#120913=CARTESIAN_POINT('Ctrl Pts',(-9.45084518532322,9.26147075531366,
9.95718200696276));
#120914=CARTESIAN_POINT('Ctrl Pts',(-9.54778864323472,9.26930893028266,
9.91067848726169));
#120915=CARTESIAN_POINT('Ctrl Pts',(-9.60708604374026,9.27400087647328,
9.88791408701438));
#120916=CARTESIAN_POINT('Ctrl Pts',(-9.69863510623786,9.28090725149277,
9.86100981115744));
#120917=CARTESIAN_POINT('Ctrl Pts',(-9.72970082172079,9.28319361425112,
9.85324012855308));
#120918=CARTESIAN_POINT('Ctrl Pts',(-9.76785147060816,9.28590375011514,
9.84533537028877));
#120919=CARTESIAN_POINT('Ctrl Pts',(-9.77466819106758,9.28638423353661,
9.84398575765425));
#120920=CARTESIAN_POINT('Ctrl Pts',(-9.78536858929546,9.28713216592202,
9.84196548139005));
#120921=CARTESIAN_POINT('Ctrl Pts',(-9.7892442349903,9.28740177464927,9.84125386843765));
#120922=CARTESIAN_POINT('Ctrl Pts',(-9.79613558635934,9.28787879477103,
9.84002425664583));
#120923=CARTESIAN_POINT('Ctrl Pts',(-9.79914975141056,9.28808662216013,
9.83949855566299));
#120924=CARTESIAN_POINT('Ctrl Pts',(-9.80515848643411,9.28849933375342,
9.83847468308996));
#120925=CARTESIAN_POINT('Ctrl Pts',(-9.8081529288778,9.28870422647288,9.83797634318877));
#120926=CARTESIAN_POINT('Ctrl Pts',(-9.81114930150154,9.28890850071391,
9.83748958018578));
#120927=CARTESIAN_POINT('Origin',(-10.,2.67563288526385,11.));
#120928=CARTESIAN_POINT('',(-9.81114930121628,9.88702732255485,9.83748958023212));
#120929=CARTESIAN_POINT('',(-9.81114931871882,9.78720258982876,9.83748957738882));
#120930=CARTESIAN_POINT('',(-9.81114930150157,2.67563288526385,9.83748958018577));
#120931=CARTESIAN_POINT('Ctrl Pts',(-9.811149300931,9.88702732255485,9.83748958027846));
#120932=CARTESIAN_POINT('Ctrl Pts',(-9.80938824931081,9.8869156335339,9.83777566444935));
#120933=CARTESIAN_POINT('Ctrl Pts',(-9.80762778878882,9.88680387632169,
9.83806575984527));
#120934=CARTESIAN_POINT('Ctrl Pts',(-9.75742776987676,9.88361396124912,
9.84645513374948));
#120935=CARTESIAN_POINT('Ctrl Pts',(-9.70954676787389,9.8804854382945,9.8575714057799));
#120936=CARTESIAN_POINT('Ctrl Pts',(-9.65162148964359,9.8765154451205,9.87489712639537));
#120937=CARTESIAN_POINT('Ctrl Pts',(-9.64078796236252,9.87576491170119,
9.87830897301879));
#120938=CARTESIAN_POINT('Ctrl Pts',(-9.62358365976746,9.87455931229639,
9.88400198881191));
#120939=CARTESIAN_POINT('Ctrl Pts',(-9.61718009036813,9.87410751926147,
9.88618235974566));
#120940=CARTESIAN_POINT('Ctrl Pts',(-9.6050772592325,9.87324763554169,9.89041998859629));
#120941=CARTESIAN_POINT('Ctrl Pts',(-9.59937437796505,9.87283991432368,
9.89246630683284));
#120942=CARTESIAN_POINT('Ctrl Pts',(-9.58643003504639,9.8719085437726,9.89722407751386));
#120943=CARTESIAN_POINT('Ctrl Pts',(-9.57919904028137,9.87138400438727,
9.89996300130681));
#120944=CARTESIAN_POINT('Ctrl Pts',(-9.5570009627198,9.8697602920866,9.90862198605889));
#120945=CARTESIAN_POINT('Ctrl Pts',(-9.54212839488076,9.86865339581668,
9.91477759641596));
#120946=CARTESIAN_POINT('Ctrl Pts',(-9.46390490726167,9.86272700280551,
9.94904775201491));
#120947=CARTESIAN_POINT('Ctrl Pts',(-9.40301170560974,9.85773306371417,
9.98240445600521));
#120948=CARTESIAN_POINT('Ctrl Pts',(-9.29670362250005,9.84837455696655,
10.0534788470948));
#120949=CARTESIAN_POINT('Ctrl Pts',(-9.25049208672881,9.84404770574388,
10.0896339673903));
#120950=CARTESIAN_POINT('Ctrl Pts',(-9.19331958916606,9.83847620862531,
10.1416805933299));
#120951=CARTESIAN_POINT('Ctrl Pts',(-9.17977839627417,9.83713907676591,
10.1546112798479));
#120952=CARTESIAN_POINT('Ctrl Pts',(-9.15773930903832,9.83494077863843,
10.1766850480223));
#120953=CARTESIAN_POINT('Ctrl Pts',(-9.14906838188003,9.83406989640862,
10.1856499561546));
#120954=CARTESIAN_POINT('Ctrl Pts',(-9.13717745249645,9.83286918669891,
10.1983413965465));
#120955=CARTESIAN_POINT('Ctrl Pts',(-9.13383628550524,9.8325310782292,10.2019525785877));
#120956=CARTESIAN_POINT('Ctrl Pts',(-9.12817997426074,9.83195760129593,
10.2081433731584));
#120957=CARTESIAN_POINT('Ctrl Pts',(-9.12585343206928,9.83172140273937,
10.2107124390951));
#120958=CARTESIAN_POINT('Ctrl Pts',(-9.12104807035986,9.83123294197615,
10.216066032842));
#120959=CARTESIAN_POINT('Ctrl Pts',(-9.11857108944876,9.83098081051642,
10.2188521035691));
#120960=CARTESIAN_POINT('Ctrl Pts',(-9.11203413565804,9.83031433618123,
10.2262754542908));
#120961=CARTESIAN_POINT('Ctrl Pts',(-9.10799719766506,9.82990163320605,
10.2309329979921));
#120962=CARTESIAN_POINT('Ctrl Pts',(-9.09048630659057,9.82810541686445,
10.2514592501817));
#120963=CARTESIAN_POINT('Ctrl Pts',(-9.07739697725658,9.82674683075645,
10.2676529502166));
#120964=CARTESIAN_POINT('Ctrl Pts',(-9.05353078340538,9.82422037300306,
10.2988356816681));
#120965=CARTESIAN_POINT('Ctrl Pts',(-9.04266388283144,9.82304877474012,
10.3137471332485));
#120966=CARTESIAN_POINT('Ctrl Pts',(-8.96819436241842,9.81481842660564,
10.4211471059183));
#120967=CARTESIAN_POINT('Ctrl Pts',(-8.91775298506138,9.80809368591901,
10.5220501560005));
#120968=CARTESIAN_POINT('Ctrl Pts',(-8.87619595746399,9.79956484730944,
10.647096763609));
#120969=CARTESIAN_POINT('Ctrl Pts',(-8.87050078497368,9.79828826798496,
10.6657730217614));
#120970=CARTESIAN_POINT('Ctrl Pts',(-8.86303937459166,9.79644526134415,
10.6926156541589));
#120971=CARTESIAN_POINT('Ctrl Pts',(-8.86089153545792,9.79589099534867,
10.7006732556792));
#120972=CARTESIAN_POINT('Ctrl Pts',(-8.85730990284954,9.79492353956979,
10.7147068799046));
#120973=CARTESIAN_POINT('Ctrl Pts',(-8.85583696553106,9.79451161141421,
10.7206726461291));
#120974=CARTESIAN_POINT('Ctrl Pts',(-8.85290378181932,9.7936613347415,10.7329653781374));
#120975=CARTESIAN_POINT('Ctrl Pts',(-8.85144904174875,9.79322282734327,
10.7392934284883));
#120976=CARTESIAN_POINT('Ctrl Pts',(-8.84786508979036,9.79209785469609,
10.7554959175359));
#120977=CARTESIAN_POINT('Ctrl Pts',(-8.84581049053718,9.79140906533196,
10.7653861408711));
#120978=CARTESIAN_POINT('Ctrl Pts',(-8.8381308239319,9.7886481850616,10.8048994545932));
#120979=CARTESIAN_POINT('Ctrl Pts',(-8.83351746386396,9.78654504603491,
10.8347050643838));
#120980=CARTESIAN_POINT('Ctrl Pts',(-8.81950279461284,9.77790934261126,
10.9558483313827));
#120981=CARTESIAN_POINT('Ctrl Pts',(-8.81965306652895,9.77111114552344,
11.0479571288892));
#120982=CARTESIAN_POINT('Ctrl Pts',(-8.83557524991109,9.76127932385518,
11.1818299339724));
#120983=CARTESIAN_POINT('Ctrl Pts',(-8.84299697499609,9.75817718903045,
11.2242586803145));
#120984=CARTESIAN_POINT('Ctrl Pts',(-8.85436350056308,9.75467670583731,
11.2732481884474));
#120985=CARTESIAN_POINT('Ctrl Pts',(-8.85606627222088,9.75417547762376,
11.2802912669989));
#120986=CARTESIAN_POINT('Ctrl Pts',(-8.85880094149647,9.7534054319023,11.291162294782));
#120987=CARTESIAN_POINT('Ctrl Pts',(-8.85978731182509,9.75313419177258,
11.2950013557914));
#120988=CARTESIAN_POINT('Ctrl Pts',(-8.8616553517524,9.75263244678719,11.3021226131765));
#120989=CARTESIAN_POINT('Ctrl Pts',(-8.86253184545969,9.75240167205826,
11.3054059747728));
#120990=CARTESIAN_POINT('Ctrl Pts',(-8.86456900976734,9.75187570795753,
11.3129067935924));
#120991=CARTESIAN_POINT('Ctrl Pts',(-8.86573897534929,9.75158104895785,
11.317121624209));
#120992=CARTESIAN_POINT('Ctrl Pts',(-8.86953295951012,9.75064831401181,
11.33049990041));
#120993=CARTESIAN_POINT('Ctrl Pts',(-8.87224482589534,9.75001498240701,
11.3396383301106));
#120994=CARTESIAN_POINT('Ctrl Pts',(-8.89935199139144,9.74398271811706,
11.4270772666833));
#120995=CARTESIAN_POINT('Ctrl Pts',(-8.93175595000109,9.73897057855183,
11.5026725423464));
#120996=CARTESIAN_POINT('Ctrl Pts',(-9.00678218522363,9.7294448070713,11.637002626922));
#120997=CARTESIAN_POINT('Ctrl Pts',(-9.04746392409348,9.72496551226715,
11.6963671231838));
#120998=CARTESIAN_POINT('Ctrl Pts',(-9.10237112481543,9.71934806547782,
11.7626006015593));
#120999=CARTESIAN_POINT('Ctrl Pts',(-9.11164377099181,9.71841232085094,
11.7733824779468));
#121000=CARTESIAN_POINT('Ctrl Pts',(-9.12601252731676,9.71697986905652,
11.7894904822132));
#121001=CARTESIAN_POINT('Ctrl Pts',(-9.13096738043261,9.71648895547584,
11.7949412719888));
#121002=CARTESIAN_POINT('Ctrl Pts',(-9.14006995512849,9.71559235675428,
11.8047681211574));
#121003=CARTESIAN_POINT('Ctrl Pts',(-9.14420079903002,9.71518738933212,
11.8091595245777));
#121004=CARTESIAN_POINT('Ctrl Pts',(-9.15321082706596,9.71430808338907,
11.8185917009442));
#121005=CARTESIAN_POINT('Ctrl Pts',(-9.15810167538714,9.71383325421941,
11.8236209586879));
#121006=CARTESIAN_POINT('Ctrl Pts',(-9.1716137492505,9.71252794521055,11.8372693067875));
#121007=CARTESIAN_POINT('Ctrl Pts',(-9.18032412316014,9.71169360776905,
11.845798504434));
#121008=CARTESIAN_POINT('Ctrl Pts',(-9.24123195425378,9.70590573268996,
11.9036148668312));
#121009=CARTESIAN_POINT('Ctrl Pts',(-9.29769931890522,9.70075540754787,
11.948166224931));
#121010=CARTESIAN_POINT('Ctrl Pts',(-9.40197001623249,9.69166421459674,
12.0159842333896));
#121011=CARTESIAN_POINT('Ctrl Pts',(-9.44795292833287,9.68778112580812,
12.0416851315213));
#121012=CARTESIAN_POINT('Ctrl Pts',(-9.51786634525496,9.68216169301164,
12.0748278239055));
#121013=CARTESIAN_POINT('Ctrl Pts',(-9.54056239666864,9.68037948953561,
12.0847234462328));
#121014=CARTESIAN_POINT('Ctrl Pts',(-9.57315318296372,9.67789388313698,
12.0977265836197));
#121015=CARTESIAN_POINT('Ctrl Pts',(-9.58280194678847,9.67716694804327,
12.1014298245006));
#121016=CARTESIAN_POINT('Ctrl Pts',(-9.59995898745751,9.67589157060576,
12.1077569580108));
#121017=CARTESIAN_POINT('Ctrl Pts',(-9.60744733867339,9.67534065663029,
12.1104326663095));
#121018=CARTESIAN_POINT('Ctrl Pts',(-9.61884810997145,9.6745111756803,12.1143765989523));
#121019=CARTESIAN_POINT('Ctrl Pts',(-9.6227408417162,9.67422958139862,12.1157004509928));
#121020=CARTESIAN_POINT('Ctrl Pts',(-9.62985133715946,9.67371828228539,
12.1180771400863));
#121021=CARTESIAN_POINT('Ctrl Pts',(-9.63306674281682,9.67348821673665,
12.1191365015956));
#121022=CARTESIAN_POINT('Ctrl Pts',(-9.64033459636005,9.67297075619939,
12.1214963093425));
#121023=CARTESIAN_POINT('Ctrl Pts',(-9.64438955983057,9.67268382662395,
12.1227886669808));
#121024=CARTESIAN_POINT('Ctrl Pts',(-9.65490677957797,9.67194400630748,
12.1260779182545));
#121025=CARTESIAN_POINT('Ctrl Pts',(-9.66137949645554,9.67149295539119,
12.1280412087164));
#121026=CARTESIAN_POINT('Ctrl Pts',(-9.70773442002203,9.66829069942655,
12.1416665260476));
#121027=CARTESIAN_POINT('Ctrl Pts',(-9.74819687954295,9.66564254480248,
12.1512678284537));
#121028=CARTESIAN_POINT('Ctrl Pts',(-9.81005817730761,9.66169899906717,
12.1625280847824));
#121029=CARTESIAN_POINT('Ctrl Pts',(-9.83113008269472,9.66037386493225,
12.1657754661205));
#121030=CARTESIAN_POINT('Ctrl Pts',(-9.90177779370762,9.65596023070978,
12.1747070938877));
#121031=CARTESIAN_POINT('Ctrl Pts',(-9.95162309117121,9.65289167874183,
12.1778131822629));
#121032=CARTESIAN_POINT('Ctrl Pts',(-10.0507397367808,9.64668007169886,
12.1776857268401));
#121033=CARTESIAN_POINT('Ctrl Pts',(-10.0999071147109,9.64354461129797,
12.1745364546185));
#121034=CARTESIAN_POINT('Ctrl Pts',(-10.1600029562102,9.6395667982176,12.1668861415174));
#121035=CARTESIAN_POINT('Ctrl Pts',(-10.1712547301108,9.63881583493078,
12.1652879541012));
#121036=CARTESIAN_POINT('Ctrl Pts',(-10.1891656188076,9.63760970747759,
12.1624789074373));
#121037=CARTESIAN_POINT('Ctrl Pts',(-10.195840656077,9.63715782137835,12.1613730131975));
#121038=CARTESIAN_POINT('Ctrl Pts',(-10.2084740802709,9.63629786443558,
12.1591679461558));
#121039=CARTESIAN_POINT('Ctrl Pts',(-10.2144342571239,9.63589016395301,
12.1580801857217));
#121040=CARTESIAN_POINT('Ctrl Pts',(-10.2279789546812,9.63495898598467,
12.1555000686678));
#121041=CARTESIAN_POINT('Ctrl Pts',(-10.2355576426227,9.63443461982638,
12.1539789445838));
#121042=CARTESIAN_POINT('Ctrl Pts',(-10.25885618064,9.63281199419249,12.1490636047662));
#121043=CARTESIAN_POINT('Ctrl Pts',(-10.2745213486091,9.63170602633101,
12.1454220510301));
#121044=CARTESIAN_POINT('Ctrl Pts',(-10.3632770509769,9.6253511766851,12.1228644725453));
#121045=CARTESIAN_POINT('Ctrl Pts',(-10.4344777476678,9.61989167528658,
12.0972785932153));
#121046=CARTESIAN_POINT('Ctrl Pts',(-10.5455791774064,9.61088622699447,
12.0448366447072));
#121047=CARTESIAN_POINT('Ctrl Pts',(-10.5871702586243,9.60739663019113,
12.022042838848));
#121048=CARTESIAN_POINT('Ctrl Pts',(-10.6457337716462,9.60238843756634,
11.9851896098343));
#121049=CARTESIAN_POINT('Ctrl Pts',(-10.6638666214858,9.600823927387,11.9730631501648));
#121050=CARTESIAN_POINT('Ctrl Pts',(-10.6930108621532,9.59829821309417,
11.9523785905249));
#121051=CARTESIAN_POINT('Ctrl Pts',(-10.7042252179912,9.59732354345189,
11.944116475514));
#121052=CARTESIAN_POINT('Ctrl Pts',(-10.7193700438529,9.59600620759629,
11.9325385598934));
#121053=CARTESIAN_POINT('Ctrl Pts',(-10.723428785002,9.59565306244783,11.9293934695019));
#121054=CARTESIAN_POINT('Ctrl Pts',(-10.7302243973425,9.59506178793847,
11.9240561055544));
#121055=CARTESIAN_POINT('Ctrl Pts',(-10.7329722507951,9.59482270310337,
11.9218779948758));
#121056=CARTESIAN_POINT('Ctrl Pts',(-10.7382184127105,9.59436631045113,
11.9176812916052));
#121057=CARTESIAN_POINT('Ctrl Pts',(-10.7407182402411,9.59414885991354,
11.9156647132149));
#121058=CARTESIAN_POINT('Ctrl Pts',(-10.7474165622467,9.59356616441293,
11.9102158820014));
#121059=CARTESIAN_POINT('Ctrl Pts',(-10.7515997160089,9.59320223059599,
11.9067647650251));
#121060=CARTESIAN_POINT('Ctrl Pts',(-10.7671104385141,9.59185201939796,
11.8937872767119));
#121061=CARTESIAN_POINT('Ctrl Pts',(-10.7782824933457,9.59087791954824,
11.884076088594));
#121062=CARTESIAN_POINT('Ctrl Pts',(-10.8774973694459,9.58218125482287,
11.7944957305467));
#121063=CARTESIAN_POINT('Ctrl Pts',(-10.9531667791192,9.57515033779875,
11.7019301158193));
#121064=CARTESIAN_POINT('Ctrl Pts',(-11.0254070192671,9.5661392839539,11.5797968084552));
#121065=CARTESIAN_POINT('Ctrl Pts',(-11.0365315895107,9.56466423778319,
11.5596660249203));
#121066=CARTESIAN_POINT('Ctrl Pts',(-11.0548575163695,9.56206336091851,
11.5240809007806));
#121067=CARTESIAN_POINT('Ctrl Pts',(-11.0623259920012,9.56094649535609,
11.5087716673341));
#121068=CARTESIAN_POINT('Ctrl Pts',(-11.0727710896248,9.55929466312735,
11.4861273066937));
#121069=CARTESIAN_POINT('Ctrl Pts',(-11.0760101599535,9.5587685887106,11.4789151278091));
#121070=CARTESIAN_POINT('Ctrl Pts',(-11.0816112371478,9.55783359713573,
11.4660999463765));
#121071=CARTESIAN_POINT('Ctrl Pts',(-11.0840029504198,9.55742569707559,
11.4605101838789));
#121072=CARTESIAN_POINT('Ctrl Pts',(-11.0889283883621,9.55656708229574,
11.448747754238));
#121073=CARTESIAN_POINT('Ctrl Pts',(-11.0914531445738,9.5561160850303,11.4425715896387));
#121074=CARTESIAN_POINT('Ctrl Pts',(-11.0979756315731,9.55492150871984,
11.4262206924616));
#121075=CARTESIAN_POINT('Ctrl Pts',(-11.1018843336454,9.55417501819788,
11.4160113790721));
#121076=CARTESIAN_POINT('Ctrl Pts',(-11.1185015566555,9.55086046105451,
11.3707301402732));
#121077=CARTESIAN_POINT('Ctrl Pts',(-11.1296805368603,9.54824352599374,
11.3351237540807));
#121078=CARTESIAN_POINT('Ctrl Pts',(-11.1587413611797,9.54007383858363,
11.2244244284301));
#121079=CARTESIAN_POINT('Ctrl Pts',(-11.1709500611552,9.53437801229778,
11.1480594504365));
#121080=CARTESIAN_POINT('Ctrl Pts',(-11.1776042310567,9.52631363124162,
11.0379739509555));
#121081=CARTESIAN_POINT('Ctrl Pts',(-11.1782066204,9.52390616780706,11.0048159962228));
#121082=CARTESIAN_POINT('Ctrl Pts',(-11.1771087191378,9.52065502650292,
10.9591788541713));
#121083=CARTESIAN_POINT('Ctrl Pts',(-11.1766091740062,9.51977168284805,
10.9466878854261));
#121084=CARTESIAN_POINT('Ctrl Pts',(-11.1753963307118,9.51825254499728,
10.9250109701606));
#121085=CARTESIAN_POINT('Ctrl Pts',(-11.1747739508,9.51761284497638,10.9158212233339));
#121086=CARTESIAN_POINT('Ctrl Pts',(-11.1736981446166,9.51667838729771,
10.9022925691619));
#121087=CARTESIAN_POINT('Ctrl Pts',(-11.1733283391365,9.51637937913493,
10.8979476270582));
#121088=CARTESIAN_POINT('Ctrl Pts',(-11.1726280720717,9.51585019771711,
10.8902276644476));
#121089=CARTESIAN_POINT('Ctrl Pts',(-11.1723071575084,9.51561951675379,
10.8868519089815));
#121090=CARTESIAN_POINT('Ctrl Pts',(-11.1715733453109,9.51511674748456,
10.8794713025378));
#121091=CARTESIAN_POINT('Ctrl Pts',(-11.1711544906633,9.51484498810846,
10.8754671506735));
#121092=CARTESIAN_POINT('Ctrl Pts',(-11.1699154753331,9.51408170758592,
10.8641820091554));
#121093=CARTESIAN_POINT('Ctrl Pts',(-11.1690478752164,9.5135927026095,10.8569062608117));
#121094=CARTESIAN_POINT('Ctrl Pts',(-11.1630311639878,9.51046835065218,
10.8101641641057));
#121095=CARTESIAN_POINT('Ctrl Pts',(-11.1559515967004,9.50792700618369,
10.7709677882233));
#121096=CARTESIAN_POINT('Ctrl Pts',(-11.1416878321562,9.50398642726335,
10.7098804828271));
#121097=CARTESIAN_POINT('Ctrl Pts',(-11.1358253549166,9.50256099574795,
10.6877160602979));
#121098=CARTESIAN_POINT('Ctrl Pts',(-11.1153314344916,9.49808507274521,
10.6184767497435));
#121099=CARTESIAN_POINT('Ctrl Pts',(-11.098390801648,9.49505381190256,10.5721428750308));
#121100=CARTESIAN_POINT('Ctrl Pts',(-11.058501922491,9.48883299390727,10.4811815766583));
#121101=CARTESIAN_POINT('Ctrl Pts',(-11.0355086020152,9.48564782222594,
10.4366884536217));
#121102=CARTESIAN_POINT('Ctrl Pts',(-11.0038844657147,9.48161398404501,
10.3840119663873));
#121103=CARTESIAN_POINT('Ctrl Pts',(-10.997869255619,9.4808599884961,10.3743146063176));
#121104=CARTESIAN_POINT('Ctrl Pts',(-10.9880591204501,9.47965013620202,
10.3590006606479));
#121105=CARTESIAN_POINT('Ctrl Pts',(-10.9843548758562,9.47919759371051,
10.3533266251816));
#121106=CARTESIAN_POINT('Ctrl Pts',(-10.9772473260628,9.47833711750577,
10.342642098877));
#121107=CARTESIAN_POINT('Ctrl Pts',(-10.9738539175789,9.47792956044399,
10.3376252636655));
#121108=CARTESIAN_POINT('Ctrl Pts',(-10.9660518678124,9.47699972697495,
10.3262802278948));
#121109=CARTESIAN_POINT('Ctrl Pts',(-10.961619496813,9.47647657153617,10.3199687646263));
#121110=CARTESIAN_POINT('Ctrl Pts',(-10.9478081524572,9.47486152815741,
10.300707191248));
#121111=CARTESIAN_POINT('Ctrl Pts',(-10.9382275221866,9.47376203587114,
10.287904641652));
#121112=CARTESIAN_POINT('Ctrl Pts',(-10.8794063405429,9.46712951223174,
10.2125505680206));
#121113=CARTESIAN_POINT('Ctrl Pts',(-10.8241956202042,9.46135953916051,
10.1549381568791));
#121114=CARTESIAN_POINT('Ctrl Pts',(-10.7101598844336,9.45037270736284,
10.0578233839667));
#121115=CARTESIAN_POINT('Ctrl Pts',(-10.6527429110041,9.4451979678151,10.0171713005949));
#121116=CARTESIAN_POINT('Ctrl Pts',(-10.5830947380716,9.43954538229104,
9.97667076833222));
#121117=CARTESIAN_POINT('Ctrl Pts',(-10.5740787112456,9.43882503169663,
9.97158576367232));
#121118=CARTESIAN_POINT('Ctrl Pts',(-10.5610299748844,9.43779994810624,
9.96445141798547));
#121119=CARTESIAN_POINT('Ctrl Pts',(-10.557050969699,9.43748966744028,9.96230557615531));
#121120=CARTESIAN_POINT('Ctrl Pts',(-10.5500438966177,9.43694741795186,
9.95857864350278));
#121121=CARTESIAN_POINT('Ctrl Pts',(-10.5470211620447,9.43671485298764,
9.95698773763269));
#121122=CARTESIAN_POINT('Ctrl Pts',(-10.540557163981,9.43622043737663,9.95362147967522));
#121123=CARTESIAN_POINT('Ctrl Pts',(-10.5371140321778,9.43595881815429,
9.95184992827973));
#121124=CARTESIAN_POINT('Ctrl Pts',(-10.5275820135217,9.43523915997629,
9.94700484282948));
#121125=CARTESIAN_POINT('Ctrl Pts',(-10.5214749527171,9.43478325195569,
9.94396711170502));
#121126=CARTESIAN_POINT('Ctrl Pts',(-10.4856374110203,9.43213595062314,
9.92652775980064));
#121127=CARTESIAN_POINT('Ctrl Pts',(-10.4553350358479,9.43000956888852,
9.91332765108223));
#121128=CARTESIAN_POINT('Ctrl Pts',(-10.3786117831148,9.42480384980121,
9.88368019931818));
#121129=CARTESIAN_POINT('Ctrl Pts',(-10.3316398728185,9.4217714470221,9.86883588281473));
#121130=CARTESIAN_POINT('Ctrl Pts',(-10.213079165508,9.41421278653319,9.83939088186083));
#121131=CARTESIAN_POINT('Ctrl Pts',(-10.1408115597129,9.40967965837839,
9.82842557594697));
#121132=CARTESIAN_POINT('Ctrl Pts',(-10.0519013977926,9.403884019448,9.82328368204909));
#121133=CARTESIAN_POINT('Ctrl Pts',(-10.035787476563,9.40282556943374,9.82268344788408));
#121134=CARTESIAN_POINT('Ctrl Pts',(-10.011930228533,9.40124418740033,9.82228500679487));
#121135=CARTESIAN_POINT('Ctrl Pts',(-10.0041926112593,9.40072907836155,
9.82223204627822));
#121136=CARTESIAN_POINT('Ctrl Pts',(-9.99039569824927,9.39980637588931,
9.82227357268185));
#121137=CARTESIAN_POINT('Ctrl Pts',(-9.98433654090951,9.39939970596728,
9.82233857415405));
#121138=CARTESIAN_POINT('Ctrl Pts',(-9.97151793132222,9.39853617381677,
9.82257503350508));
#121139=CARTESIAN_POINT('Ctrl Pts',(-9.96475893638935,9.39807897235682,
9.82275795007639));
#121140=CARTESIAN_POINT('Ctrl Pts',(-9.94666581100367,9.39684987552481,
9.82340355268593));
#121141=CARTESIAN_POINT('Ctrl Pts',(-9.93533640440357,9.39607475907768,
9.82397179482884));
#121142=CARTESIAN_POINT('Ctrl Pts',(-9.88620080417885,9.39268818701886,
9.82714840212198));
#121143=CARTESIAN_POINT('Ctrl Pts',(-9.8485346392725,9.39002702650581,9.83141630341042));
#121144=CARTESIAN_POINT('Ctrl Pts',(-9.81114929154307,9.38732021693139,
9.83748958180354));
#121145=CARTESIAN_POINT('Ctrl Pts',(-9.81114930150154,9.28890850071391,
9.83748958018578));
#121146=CARTESIAN_POINT('Ctrl Pts',(-9.81238629142768,9.28899283107266,
9.83728863023504));
#121147=CARTESIAN_POINT('Ctrl Pts',(-9.81362361031034,9.28907705602562,
9.83708965331073));
#121148=CARTESIAN_POINT('Ctrl Pts',(-9.82359200226222,9.28975459758873,
9.83550292480142));
#121149=CARTESIAN_POINT('Ctrl Pts',(-9.83233844276262,9.29034283247144,
9.83421149710092));
#121150=CARTESIAN_POINT('Ctrl Pts',(-9.85284227527573,9.29170894531513,
9.83141960910498));
#121151=CARTESIAN_POINT('Ctrl Pts',(-9.86460959421868,9.29248311559321,
9.82999786872615));
#121152=CARTESIAN_POINT('Ctrl Pts',(-9.90673070950593,9.29522551132414,
9.8255527714253));
#121153=CARTESIAN_POINT('Ctrl Pts',(-9.93717967547182,9.29715493064775,
9.82353099498969));
#121154=CARTESIAN_POINT('Ctrl Pts',(-10.0412499298315,9.30366930523765,
9.82067354204818));
#121155=CARTESIAN_POINT('Ctrl Pts',(-10.1148519412607,9.30814998712544,
9.82555470571068));
#121156=CARTESIAN_POINT('Ctrl Pts',(-10.2308040256384,9.31553851517843,
9.84425478538658));
#121157=CARTESIAN_POINT('Ctrl Pts',(-10.2736623297318,9.31834136498324,
9.85364674809787));
#121158=CARTESIAN_POINT('Ctrl Pts',(-10.3268599785669,9.32196710360418,
9.86845804913041));
#121159=CARTESIAN_POINT('Ctrl Pts',(-10.3377805921385,9.32271926092387,
9.87166986702973));
#121160=CARTESIAN_POINT('Ctrl Pts',(-10.3551180510158,9.32392677524327,
9.87704316684379));
#121161=CARTESIAN_POINT('Ctrl Pts',(-10.3615659568139,9.32437883932188,
9.87910262069208));
#121162=CARTESIAN_POINT('Ctrl Pts',(-10.3737484558308,9.32523879438062,
9.8831097503593));
#121163=CARTESIAN_POINT('Ctrl Pts',(-10.3794864966331,9.32564631228905,
9.88504630835882));
#121164=CARTESIAN_POINT('Ctrl Pts',(-10.3925041217116,9.32657659596062,
9.8895518171993));
#121165=CARTESIAN_POINT('Ctrl Pts',(-10.3997738333531,9.32710024538058,
9.89214823667424));
#121166=CARTESIAN_POINT('Ctrl Pts',(-10.4220632404085,9.32871883598333,
9.90035698235124));
#121167=CARTESIAN_POINT('Ctrl Pts',(-10.43699373059,9.32982143210397,9.90620450688179));
#121168=CARTESIAN_POINT('Ctrl Pts',(-10.4714222035734,9.33240824503439,
9.92050583338112));
#121169=CARTESIAN_POINT('Ctrl Pts',(-10.4908195203022,9.33389948543975,
9.92918598631351));
#121170=CARTESIAN_POINT('Ctrl Pts',(-10.5612391302604,9.3394392120374,9.96301363600086));
#121171=CARTESIAN_POINT('Ctrl Pts',(-10.6106511984772,9.34357974063689,
9.99132069741985));
#121172=CARTESIAN_POINT('Ctrl Pts',(-10.717221910682,9.35300188196796,10.0630815203742));
#121173=CARTESIAN_POINT('Ctrl Pts',(-10.7728563816388,9.35828472116328,
10.1084181076414));
#121174=CARTESIAN_POINT('Ctrl Pts',(-10.8314057349917,9.36403376904416,
10.165754161119));
#121175=CARTESIAN_POINT('Ctrl Pts',(-10.838685887661,9.36475215224898,10.1730733915267));
#121176=CARTESIAN_POINT('Ctrl Pts',(-10.8490108498607,9.36577491067181,
10.1837304215292));
#121177=CARTESIAN_POINT('Ctrl Pts',(-10.8521339238325,9.36608480126634,
10.1869912513043));
#121178=CARTESIAN_POINT('Ctrl Pts',(-10.857585585026,9.36662655446492,10.1927493055179));
#121179=CARTESIAN_POINT('Ctrl Pts',(-10.8599221778803,9.36685901045488,
10.1952388127088));
#121180=CARTESIAN_POINT('Ctrl Pts',(-10.8648864308651,9.36735340002429,
10.2005742518597));
#121181=CARTESIAN_POINT('Ctrl Pts',(-10.867510905161,9.36761510074435,10.2034230133923));
#121182=CARTESIAN_POINT('Ctrl Pts',(-10.8747238124734,9.36833542899742,
10.2113302625527));
#121183=CARTESIAN_POINT('Ctrl Pts',(-10.8792824622557,9.36879191828701,
10.2164158884212));
#121184=CARTESIAN_POINT('Ctrl Pts',(-10.9057577346191,9.37145239801626,
10.246473682744));
#121185=CARTESIAN_POINT('Ctrl Pts',(-10.9266561299168,9.37359060940483,
10.2723270984589));
#121186=CARTESIAN_POINT('Ctrl Pts',(-10.9760894162227,9.37884609551523,
10.3390711057403));
#121187=CARTESIAN_POINT('Ctrl Pts',(-11.0031746124824,9.3819150234878,10.3809533597151));
#121188=CARTESIAN_POINT('Ctrl Pts',(-11.0627383223666,9.3894569353155,10.4872879247389));
#121189=CARTESIAN_POINT('Ctrl Pts',(-11.0921034161813,9.3939371444805,10.5532396097895));
#121190=CARTESIAN_POINT('Ctrl Pts',(-11.1204557258939,9.39967719255917,
10.6367706329338));
#121191=CARTESIAN_POINT('Ctrl Pts',(-11.1253375165846,9.40073874903828,
10.6521896500369));
#121192=CARTESIAN_POINT('Ctrl Pts',(-11.1320854756154,9.40232379989139,
10.6751345936017));
#121193=CARTESIAN_POINT('Ctrl Pts',(-11.1341974472289,9.40283941534969,
10.6825867011463));
#121194=CARTESIAN_POINT('Ctrl Pts',(-11.1378302078953,9.40376258109945,
10.6959043060874));
#121195=CARTESIAN_POINT('Ctrl Pts',(-11.1393795399129,9.40416920287083,
10.701761781885));
#121196=CARTESIAN_POINT('Ctrl Pts',(-11.1425601881775,9.40503216497761,
10.714173315404));
#121197=CARTESIAN_POINT('Ctrl Pts',(-11.1441804551736,9.40548884081071,
10.7207299515587));
#121198=CARTESIAN_POINT('Ctrl Pts',(-11.1483638524071,9.40671537699297,
10.7383064236898));
#121199=CARTESIAN_POINT('Ctrl Pts',(-11.1508246795661,9.40748843639763,
10.7493496323047));
#121200=CARTESIAN_POINT('Ctrl Pts',(-11.1629723306005,9.4115955565733,10.8078191931531));
#121201=CARTESIAN_POINT('Ctrl Pts',(-11.1698863373508,9.41501511004576,
10.8557677110338));
#121202=CARTESIAN_POINT('Ctrl Pts',(-11.17794527137,9.42213971779147,10.9543077727452));
#121203=CARTESIAN_POINT('Ctrl Pts',(-11.1788210162106,9.42584364395567,
11.0048250846842));
#121204=CARTESIAN_POINT('Ctrl Pts',(-11.1756170966727,9.43085599160356,
11.0730601327088));
#121205=CARTESIAN_POINT('Ctrl Pts',(-11.1743755187243,9.43216400385614,
11.0908597688378));
#121206=CARTESIAN_POINT('Ctrl Pts',(-11.1685499119349,9.43677666740589,
11.153754076008));
#121207=CARTESIAN_POINT('Ctrl Pts',(-11.1617676936868,9.44005090836022,
11.1986100867019));
#121208=CARTESIAN_POINT('Ctrl Pts',(-11.1510155608579,9.44368161513569,
11.2496082848223));
#121209=CARTESIAN_POINT('Ctrl Pts',(-11.1495581366562,9.44415166514316,
11.2562366347419));
#121210=CARTESIAN_POINT('Ctrl Pts',(-11.147092251452,9.44491202646718,11.2670067302964));
#121211=CARTESIAN_POINT('Ctrl Pts',(-11.1461184821012,9.44520414656266,
11.271156142804));
#121212=CARTESIAN_POINT('Ctrl Pts',(-11.1443310072684,9.44572598464449,
11.2785912142597));
#121213=CARTESIAN_POINT('Ctrl Pts',(-11.1435256451383,9.44595615325374,
11.2818787303616));
#121214=CARTESIAN_POINT('Ctrl Pts',(-11.1417124622674,9.44646359308379,
11.2891445259963));
#121215=CARTESIAN_POINT('Ctrl Pts',(-11.1406980143352,9.4467404877925,11.2931210411702));
#121216=CARTESIAN_POINT('Ctrl Pts',(-11.1376657066151,9.4475482652233,11.3047531462902));
#121217=CARTESIAN_POINT('Ctrl Pts',(-11.1355913686239,9.44807608027455,
11.3123939692873));
#121218=CARTESIAN_POINT('Ctrl Pts',(-11.1306476377437,9.44928043925828,
11.32990392391));
#121219=CARTESIAN_POINT('Ctrl Pts',(-11.1277257652357,9.4499543738738,11.3397576988492));
#121220=CARTESIAN_POINT('Ctrl Pts',(-11.1173886278384,9.4522199414502,11.3730152565905));
#121221=CARTESIAN_POINT('Ctrl Pts',(-11.1093704072429,9.45378589460911,
11.3962261742062));
#121222=CARTESIAN_POINT('Ctrl Pts',(-11.0818519377761,9.45866124432687,
11.4684824062941));
#121223=CARTESIAN_POINT('Ctrl Pts',(-11.0597783991114,9.46190256023911,
11.5164780669949));
#121224=CARTESIAN_POINT('Ctrl Pts',(-11.0001925798052,9.4696271910506,11.6260044437626));
#121225=CARTESIAN_POINT('Ctrl Pts',(-10.9601167798413,9.47412503617093,
11.685886694406));
#121226=CARTESIAN_POINT('Ctrl Pts',(-10.9071435538109,9.47963662738325,
11.751222175606));
#121227=CARTESIAN_POINT('Ctrl Pts',(-10.8993060127274,9.48044225257185,
11.7605871821846));
#121228=CARTESIAN_POINT('Ctrl Pts',(-10.8867367344808,9.48172009868814,
11.77514017396));
#121229=CARTESIAN_POINT('Ctrl Pts',(-10.8821016597997,9.48218840086363,
11.7804107788587));
#121230=CARTESIAN_POINT('Ctrl Pts',(-10.8733994507242,9.48306244547943,
11.7901296008024));
#121231=CARTESIAN_POINT('Ctrl Pts',(-10.869344725099,9.48346766560511,11.7945886566156));
#121232=CARTESIAN_POINT('Ctrl Pts',(-10.8602645522863,9.48437076364838,
11.8044215898332));
#121233=CARTESIAN_POINT('Ctrl Pts',(-10.8552226475359,9.48486932560902,
11.8097798546553));
#121234=CARTESIAN_POINT('Ctrl Pts',(-10.8403155372915,9.48633524745779,
11.8253278180035));
#121235=CARTESIAN_POINT('Ctrl Pts',(-10.8303163784592,9.48730831110135,
11.835386671333));
#121236=CARTESIAN_POINT('Ctrl Pts',(-10.7793192723676,9.49222283153462,
11.8848679885892));
#121237=CARTESIAN_POINT('Ctrl Pts',(-10.735690918824,9.49628043828416,11.9214592019986));
#121238=CARTESIAN_POINT('Ctrl Pts',(-10.6426288268623,9.50462518840194,
11.9886758949842));
#121239=CARTESIAN_POINT('Ctrl Pts',(-10.593222306063,9.50890396462073,12.0190872509067));
#121240=CARTESIAN_POINT('Ctrl Pts',(-10.5224185054236,9.51471832836415,
12.0557696286537));
#121241=CARTESIAN_POINT('Ctrl Pts',(-10.5027801228185,9.51629896694799,
12.0652618629947));
#121242=CARTESIAN_POINT('Ctrl Pts',(-10.4623261614532,9.51947685725525,
12.0834472032572));
#121243=CARTESIAN_POINT('Ctrl Pts',(-10.4415008164873,9.52107225972215,
12.0920991298801));
#121244=CARTESIAN_POINT('Ctrl Pts',(-10.4145260736668,9.52307654590144,
12.1024079359971));
#121245=CARTESIAN_POINT('Ctrl Pts',(-10.4085954839624,9.523513412781,12.1046197798526));
#121246=CARTESIAN_POINT('Ctrl Pts',(-10.3991101626343,9.52420578940791,
12.1080705333613));
#121247=CARTESIAN_POINT('Ctrl Pts',(-10.3955669260566,9.52446302384449,
12.1093403611312));
#121248=CARTESIAN_POINT('Ctrl Pts',(-10.3887655488734,9.52495403055696,
12.1117411137708));
#121249=CARTESIAN_POINT('Ctrl Pts',(-10.3855084713862,9.52518794741127,
12.1128747345613));
#121250=CARTESIAN_POINT('Ctrl Pts',(-10.3776835927793,9.52574708342137,
12.1155596967004));
#121251=CARTESIAN_POINT('Ctrl Pts',(-10.3731110897487,9.52607151593239,
12.1170973323241));
#121252=CARTESIAN_POINT('Ctrl Pts',(-10.3572575782142,9.52718884455906,
12.1223203303473));
#121253=CARTESIAN_POINT('Ctrl Pts',(-10.3459299714877,9.52797406230489,
12.1258633941903));
#121254=CARTESIAN_POINT('Ctrl Pts',(-10.3177707674791,9.52989816047619,
12.1342059178023));
#121255=CARTESIAN_POINT('Ctrl Pts',(-10.3008816874889,9.5310278151308,12.138802704707));
#121256=CARTESIAN_POINT('Ctrl Pts',(-10.2265451070646,9.53591896598004,
12.1572658948226));
#121257=CARTESIAN_POINT('Ctrl Pts',(-10.1681998259575,9.53955154362894,
12.167174731793));
#121258=CARTESIAN_POINT('Ctrl Pts',(-10.038871725141,9.54759043266453,12.179234907543));
#121259=CARTESIAN_POINT('Ctrl Pts',(-9.96794915061524,9.55199645186888,
12.1794393019217));
#121260=CARTESIAN_POINT('Ctrl Pts',(-9.88136498698978,9.55765241025506,
12.171870827871));
#121261=CARTESIAN_POINT('Ctrl Pts',(-9.86531935612558,9.55871176965451,
12.1701352857376));
#121262=CARTESIAN_POINT('Ctrl Pts',(-9.84163951467993,9.56029416574665,
12.167080508595));
#121263=CARTESIAN_POINT('Ctrl Pts',(-9.83397407809116,9.56080936256901,
12.1660147277523));
#121264=CARTESIAN_POINT('Ctrl Pts',(-9.82032788384395,9.56173206333001,
12.1639801093673));
#121265=CARTESIAN_POINT('Ctrl Pts',(-9.81434299574059,9.56213864231125,
12.1630405146676));
#121266=CARTESIAN_POINT('Ctrl Pts',(-9.80169826008948,9.56300181262123,
12.1609552732107));
#121267=CARTESIAN_POINT('Ctrl Pts',(-9.79504051250955,9.56345874171839,
12.1597984012973));
#121268=CARTESIAN_POINT('Ctrl Pts',(-9.77724693005966,9.56468668869176,
12.1565485360494));
#121269=CARTESIAN_POINT('Ctrl Pts',(-9.76613096313191,9.56546091850695,
12.1543520712756));
#121270=CARTESIAN_POINT('Ctrl Pts',(-9.70742681919636,9.56958871082519,
12.141869685641));
#121271=CARTESIAN_POINT('Ctrl Pts',(-9.66048501027235,9.57302881705548,
12.1288019709701));
#121272=CARTESIAN_POINT('Ctrl Pts',(-9.56698193258889,9.58016120064225,
12.0964116141803));
#121273=CARTESIAN_POINT('Ctrl Pts',(-9.52057760629516,9.58385095451787,
12.0769292836869));
#121274=CARTESIAN_POINT('Ctrl Pts',(-9.45812615238472,9.58896874711957,
12.0458714257684));
#121275=CARTESIAN_POINT('Ctrl Pts',(-9.44090671964008,9.59039638886854,
12.036768552548));
#121276=CARTESIAN_POINT('Ctrl Pts',(-9.38586246771766,9.5950011854037,12.0058996530843));
#121277=CARTESIAN_POINT('Ctrl Pts',(-9.34901527086668,9.59814925777463,
11.9824554717117));
#121278=CARTESIAN_POINT('Ctrl Pts',(-9.30753739171142,9.60170471643013,
11.9527042382854));
#121279=CARTESIAN_POINT('Ctrl Pts',(-9.30156449979356,9.60221697683924,
11.9483341650216));
#121280=CARTESIAN_POINT('Ctrl Pts',(-9.2923938897724,9.60300341349259,11.9414908335166));
#121281=CARTESIAN_POINT('Ctrl Pts',(-9.28916717104804,9.6032801101994,11.9390570202812));
#121282=CARTESIAN_POINT('Ctrl Pts',(-9.28325824022292,9.60378668801218,
11.9345521893084));
#121283=CARTESIAN_POINT('Ctrl Pts',(-9.28057242145093,9.60401688782949,
11.9324861953485));
#121284=CARTESIAN_POINT('Ctrl Pts',(-9.27446906357078,9.60453990502997,
11.9277492843404));
#121285=CARTESIAN_POINT('Ctrl Pts',(-9.27105732883218,9.60483220956044,
11.9250710556238));
#121286=CARTESIAN_POINT('Ctrl Pts',(-9.26053991250686,9.60573339441751,
11.916720516071));
#121287=CARTESIAN_POINT('Ctrl Pts',(-9.25348486085126,9.60633803844235,
11.91098456903));
#121288=CARTESIAN_POINT('Ctrl Pts',(-9.19362004216394,9.61147679519786,
11.8611503113386));
#121289=CARTESIAN_POINT('Ctrl Pts',(-9.14469421838923,9.61573601777523,
11.8125781180138));
#121290=CARTESIAN_POINT('Ctrl Pts',(-9.04666147102512,9.6251358133601,11.6965242266218));
#121291=CARTESIAN_POINT('Ctrl Pts',(-8.99991314899424,9.63026101880993,
11.627554501938));
#121292=CARTESIAN_POINT('Ctrl Pts',(-8.95335061639721,9.63670286611648,
11.5402514233177));
#121293=CARTESIAN_POINT('Ctrl Pts',(-8.94617166786187,9.63774418015345,
11.5261105779438));
#121294=CARTESIAN_POINT('Ctrl Pts',(-8.93594044338544,9.63930475615475,
11.5049073162581));
#121295=CARTESIAN_POINT('Ctrl Pts',(-8.93266812627908,9.63981649536579,
11.4979526129023));
#121296=CARTESIAN_POINT('Ctrl Pts',(-8.92694109934899,9.64073537026862,
11.4854650250478));
#121297=CARTESIAN_POINT('Ctrl Pts',(-8.92446050673897,9.64114161040775,
11.4799442581331));
#121298=CARTESIAN_POINT('Ctrl Pts',(-8.91928820152738,9.64200657144456,
11.4681913644485));
#121299=CARTESIAN_POINT('Ctrl Pts',(-8.91660760805679,9.64246564924087,
11.4619546155768));
#121300=CARTESIAN_POINT('Ctrl Pts',(-8.90954178747643,9.64370557415027,
11.4451152560814));
#121301=CARTESIAN_POINT('Ctrl Pts',(-8.90525742805021,9.64448974344235,
11.4344713908661));
#121302=CARTESIAN_POINT('Ctrl Pts',(-8.88270771544209,9.6488014127095,11.3759977023578));
#121303=CARTESIAN_POINT('Ctrl Pts',(-8.86742305291574,9.65242513017925,
11.3270848210618));
#121304=CARTESIAN_POINT('Ctrl Pts',(-8.83884901407342,9.66118851389804,
11.2091542571005));
#121305=CARTESIAN_POINT('Ctrl Pts',(-8.82845434770677,9.66638037877928,
11.1396315267862));
#121306=CARTESIAN_POINT('Ctrl Pts',(-8.82191201484686,9.67444408567743,
11.0291231763896));
#121307=CARTESIAN_POINT('Ctrl Pts',(-8.82160750270993,9.67736266253232,
10.9885414829633));
#121308=CARTESIAN_POINT('Ctrl Pts',(-8.82372239782677,9.68070006440941,
10.940668469199));
#121309=CARTESIAN_POINT('Ctrl Pts',(-8.82411613454022,9.68120945654215,
10.9333188952218));
#121310=CARTESIAN_POINT('Ctrl Pts',(-8.82483221621325,9.68199242526599,
10.9219487108479));
#121311=CARTESIAN_POINT('Ctrl Pts',(-8.82510635104722,9.6822684888089,10.9179254079559));
#121312=CARTESIAN_POINT('Ctrl Pts',(-8.8256489176753,9.6827744809635,10.9105232688751));
#121313=CARTESIAN_POINT('Ctrl Pts',(-8.82591127053541,9.68300472273815,
10.9071441663436));
#121314=CARTESIAN_POINT('Ctrl Pts',(-8.82654357041775,9.68352856045989,
10.8994316961168));
#121315=CARTESIAN_POINT('Ctrl Pts',(-8.82692293512729,9.68382163683827,
10.895099202829));
#121316=CARTESIAN_POINT('Ctrl Pts',(-8.82817520730296,9.68472765255914,
10.8816551778761));
#121317=CARTESIAN_POINT('Ctrl Pts',(-8.82913036305045,9.68533629005852,
10.8725513922389));
#121318=CARTESIAN_POINT('Ctrl Pts',(-8.83162912416268,9.68675798246277,
10.8511433260401));
#121319=CARTESIAN_POINT('Ctrl Pts',(-8.83326112528838,9.68756690224357,
10.8388502641155));
#121320=CARTESIAN_POINT('Ctrl Pts',(-8.83990671039832,9.69048472615131,
10.7942086970315));
#121321=CARTESIAN_POINT('Ctrl Pts',(-8.84607437837803,9.6925493375411,10.7620452431849));
#121322=CARTESIAN_POINT('Ctrl Pts',(-8.86413699526466,9.69747139202525,
10.685300279843));
#121323=CARTESIAN_POINT('Ctrl Pts',(-8.87732570999502,9.70030494745551,
10.6410804229618));
#121324=CARTESIAN_POINT('Ctrl Pts',(-8.91572911921611,9.70728282471766,
10.5354012316572));
#121325=CARTESIAN_POINT('Ctrl Pts',(-8.94360883301637,9.71144941376279,
10.4750891845998));
#121326=CARTESIAN_POINT('Ctrl Pts',(-8.98244228216605,9.71659414637436,
10.4068559184069));
#121327=CARTESIAN_POINT('Ctrl Pts',(-8.98863473234494,9.71739824935399,
10.3963578145763));
#121328=CARTESIAN_POINT('Ctrl Pts',(-8.99864542462074,9.7186742113475,10.3799731731409));
#121329=CARTESIAN_POINT('Ctrl Pts',(-9.00235536146342,9.71914217107062,
10.3740212277713));
#121330=CARTESIAN_POINT('Ctrl Pts',(-9.0093519642638,9.72001589700007,10.3630165940065));
#121331=CARTESIAN_POINT('Ctrl Pts',(-9.01262470218902,9.72042114393834,
10.3579552903564));
#121332=CARTESIAN_POINT('Ctrl Pts',(-9.01606784208457,9.72084400708484,
10.3527190496997));
#121333=CARTESIAN_POINT('Ctrl Pts',(-9.01619965170182,9.72086018980727,
10.35251873024));
#121334=CARTESIAN_POINT('Ctrl Pts',(-9.0164529526398,9.72089127837934,10.3521340286093));
#121335=CARTESIAN_POINT('Ctrl Pts',(-9.01657443466254,9.72090618388388,
10.3519496403075));
#121336=CARTESIAN_POINT('Ctrl Pts',(-9.01680845570551,9.72093488907301,
10.3515946549447));
#121337=CARTESIAN_POINT('Ctrl Pts',(-9.01692098730145,9.72094868848224,
10.3514240529745));
#121338=CARTESIAN_POINT('Ctrl Pts',(-9.01713825082408,9.72097532352946,
10.3510948600706));
#121339=CARTESIAN_POINT('Ctrl Pts',(-9.01724297674637,9.72098815894416,
10.3509362651746));
#121340=CARTESIAN_POINT('Ctrl Pts',(-9.01744558753614,9.72101298498382,
10.3506295967978));
#121341=CARTESIAN_POINT('Ctrl Pts',(-9.01754346751164,9.72102497542761,
10.3504815200642));
#121342=CARTESIAN_POINT('Ctrl Pts',(-9.01773319653839,9.72104821198619,
10.35019463143));
#121343=CARTESIAN_POINT('Ctrl Pts',(-9.01782504155932,9.72105945795176,
10.350055816845));
#121344=CARTESIAN_POINT('Ctrl Pts',(-9.01800339037561,9.72108129100874,
10.3497863845396));
#121345=CARTESIAN_POINT('Ctrl Pts',(-9.01808989080319,9.72109187797388,
10.3496557646131));
#121346=CARTESIAN_POINT('Ctrl Pts',(-9.01825814153266,9.72111246621133,
10.3494018077736));
#121347=CARTESIAN_POINT('Ctrl Pts',(-9.01833988902623,9.72112246737942,
10.3492784689915));
#121348=CARTESIAN_POINT('Ctrl Pts',(-9.02241617728978,9.72162107085455,
10.343130773052));
#121349=CARTESIAN_POINT('Ctrl Pts',(-9.02646599233686,9.72211171933589,
10.3371434215258));
#121350=CARTESIAN_POINT('Ctrl Pts',(-9.03977072564902,9.7237088020395,10.3178583123283));
#121351=CARTESIAN_POINT('Ctrl Pts',(-9.04924463038598,9.72482338908638,
10.3047146461059));
#121352=CARTESIAN_POINT('Ctrl Pts',(-9.0720775327723,9.72745936479107,10.2743768893543));
#121353=CARTESIAN_POINT('Ctrl Pts',(-9.0856478372066,9.72898839171479,10.2573499996535));
#121354=CARTESIAN_POINT('Ctrl Pts',(-9.13796206439732,9.73474772757883,
10.1953190792775));
#121355=CARTESIAN_POINT('Ctrl Pts',(-9.17961663506222,9.73907834493517,
10.1528928404179));
#121356=CARTESIAN_POINT('Ctrl Pts',(-9.27539260322614,9.7484170785229,10.0690585304199));
#121357=CARTESIAN_POINT('Ctrl Pts',(-9.33027625887786,9.75341676628223,
10.0288256232234));
#121358=CARTESIAN_POINT('Ctrl Pts',(-9.39639606303814,9.75884661397003,
9.98864124952498));
#121359=CARTESIAN_POINT('Ctrl Pts',(-9.40452474727897,9.75950448171555,
9.98383393483351));
#121360=CARTESIAN_POINT('Ctrl Pts',(-9.41705058008964,9.76050252805791,
9.97662807134143));
#121361=CARTESIAN_POINT('Ctrl Pts',(-9.42140645578641,9.76084673776016,
9.9741590555037));
#121362=CARTESIAN_POINT('Ctrl Pts',(-9.42878724976407,9.76142499916493,
9.9700374105656));
#121363=CARTESIAN_POINT('Ctrl Pts',(-9.43180388728355,9.76165994844305,
9.96837016311263));
#121364=CARTESIAN_POINT('Ctrl Pts',(-9.43806089312858,9.7621443322034,9.96494778775583));
#121365=CARTESIAN_POINT('Ctrl Pts',(-9.44130223938692,9.76239364799356,
9.96319459148318));
#121366=CARTESIAN_POINT('Ctrl Pts',(-9.44981804728157,9.76304459025896,
9.95864004898167));
#121367=CARTESIAN_POINT('Ctrl Pts',(-9.45510576232724,9.76344470970256,
9.95586351363371));
#121368=CARTESIAN_POINT('Ctrl Pts',(-9.47924698774396,9.76525408402404,
9.94342049702607));
#121369=CARTESIAN_POINT('Ctrl Pts',(-9.4983393879207,9.76663715191732,9.93422295496629));
#121370=CARTESIAN_POINT('Ctrl Pts',(-9.61124012854633,9.77459945010247,
9.88354116297366));
#121371=CARTESIAN_POINT('Ctrl Pts',(-9.70989195838233,9.7807355707276,9.8539389107558));
#121372=CARTESIAN_POINT('Ctrl Pts',(-9.81114931872029,9.78720258982885,
9.83748957738858));
#121373=CARTESIAN_POINT('Origin',(-10.,2.67563288526385,11.));
#121374=CARTESIAN_POINT('',(-9.81114930150097,10.385472315614,9.83748958018587));
#121375=CARTESIAN_POINT('',(-9.81114930150157,10.287171250943,9.83748958018577));
#121376=CARTESIAN_POINT('',(-9.81114930150157,2.67563288526385,9.83748958018577));
#121377=CARTESIAN_POINT('Ctrl Pts',(-9.81114930150037,10.385472315614,9.83748958018597));
#121378=CARTESIAN_POINT('Ctrl Pts',(-9.80901865393688,10.3853241363018,
9.83783570549699));
#121379=CARTESIAN_POINT('Ctrl Pts',(-9.80688893621724,10.3851762668984,
9.83818769190922));
#121380=CARTESIAN_POINT('Ctrl Pts',(-9.80137111344281,10.3847938131546,
9.83911523474365));
#121381=CARTESIAN_POINT('Ctrl Pts',(-9.79798450088191,10.3845597242658,
9.83969977499039));
#121382=CARTESIAN_POINT('Ctrl Pts',(-9.79085865717225,10.3840685805468,
9.84096186392286));
#121383=CARTESIAN_POINT('Ctrl Pts',(-9.78712009935092,10.3838117083245,
9.84164269282486));
#121384=CARTESIAN_POINT('Ctrl Pts',(-9.77700493425228,10.383118727767,9.84353539120436));
#121385=CARTESIAN_POINT('Ctrl Pts',(-9.77063483055417,10.3826844973983,
9.84478191906313));
#121386=CARTESIAN_POINT('Ctrl Pts',(-9.74039221174691,10.380631922259,9.8509599405518));
#121387=CARTESIAN_POINT('Ctrl Pts',(-9.71666447833965,10.379048130933,9.85657950056329));
#121388=CARTESIAN_POINT('Ctrl Pts',(-9.68157964884264,10.3767230771455,
9.86604824544442));
#121389=CARTESIAN_POINT('Ctrl Pts',(-9.67008068569605,10.3759637879132,
9.86934029724323));
#121390=CARTESIAN_POINT('Ctrl Pts',(-9.60005324488689,10.3713457699839,
9.89054786214394));
#121391=CARTESIAN_POINT('Ctrl Pts',(-9.54294276551046,10.3676007600548,
9.91282899400435));
#121392=CARTESIAN_POINT('Ctrl Pts',(-9.43275573165214,10.3600018520841,
9.9660423712307));
#121393=CARTESIAN_POINT('Ctrl Pts',(-9.37985172576072,10.3561585951765,
9.99688026163735));
#121394=CARTESIAN_POINT('Ctrl Pts',(-9.31783649874031,10.3512341924403,
10.0398165853582));
#121395=CARTESIAN_POINT('Ctrl Pts',(-9.30623802895158,10.3502940166443,
10.0481630753736));
#121396=CARTESIAN_POINT('Ctrl Pts',(-9.28888383701256,10.348856164818,10.0611372141539));
#121397=CARTESIAN_POINT('Ctrl Pts',(-9.28301478567254,10.3483643506024,
10.0656115763813));
#121398=CARTESIAN_POINT('Ctrl Pts',(-9.27242774770514,10.3474668119295,
10.0738412464389));
#121399=CARTESIAN_POINT('Ctrl Pts',(-9.26769577783842,10.3470618128797,
10.0775782184907));
#121400=CARTESIAN_POINT('Ctrl Pts',(-9.25752961857975,10.3461832474682,
10.0857342554353));
#121401=CARTESIAN_POINT('Ctrl Pts',(-9.25210576233181,10.3457091969369,
10.0901657708273));
#121402=CARTESIAN_POINT('Ctrl Pts',(-9.23738924506434,10.34440811294,10.1024102878799));
#121403=CARTESIAN_POINT('Ctrl Pts',(-9.22817757358346,10.3435772629782,
10.1103188336145));
#121404=CARTESIAN_POINT('Ctrl Pts',(-9.17059101114898,10.3382758630526,
10.1613264229501));
#121405=CARTESIAN_POINT('Ctrl Pts',(-9.12572741545361,10.3336473690437,
10.2082061006038));
#121406=CARTESIAN_POINT('Ctrl Pts',(-9.0301413438192,10.3225841260118,10.3261687593772));
#121407=CARTESIAN_POINT('Ctrl Pts',(-8.98299996017106,10.3161000792904,
10.3996782553392));
#121408=CARTESIAN_POINT('Ctrl Pts',(-8.93849786779084,10.3090165172813,
10.4896228477336));
#121409=CARTESIAN_POINT('Ctrl Pts',(-8.9328071225575,10.3080874931541,10.5016316487003));
#121410=CARTESIAN_POINT('Ctrl Pts',(-8.92523864428582,10.3068212502874,
10.5183273758546));
#121411=CARTESIAN_POINT('Ctrl Pts',(-8.92318621215167,10.3064745484479,
10.5229333828439));
#121412=CARTESIAN_POINT('Ctrl Pts',(-8.91976399584554,10.3058909326453,
10.5307480342843));
#121413=CARTESIAN_POINT('Ctrl Pts',(-8.91837878477369,10.3056531171588,
10.5339498095624));
#121414=CARTESIAN_POINT('Ctrl Pts',(-8.91555962669803,10.3051658888952,
10.5405462826958));
#121415=CARTESIAN_POINT('Ctrl Pts',(-8.91412735710677,10.304916574061,10.5439416200212));
#121416=CARTESIAN_POINT('Ctrl Pts',(-8.91041692483366,10.3042658446329,
10.5528541480393));
#121417=CARTESIAN_POINT('Ctrl Pts',(-8.90816469160973,10.3038659345682,
10.5583821180139));
#121418=CARTESIAN_POINT('Ctrl Pts',(-8.89890668807222,10.3022001189235,
10.5816091455266));
#121419=CARTESIAN_POINT('Ctrl Pts',(-8.8922880690545,10.3009549055186,10.5994606568881));
#121420=CARTESIAN_POINT('Ctrl Pts',(-8.88015178480883,10.2985434794403,
10.6348001258412));
#121421=CARTESIAN_POINT('Ctrl Pts',(-8.87460404174534,10.297376393813,10.652271699045));
#121422=CARTESIAN_POINT('Ctrl Pts',(-8.85231468746043,10.2923578204032,
10.7286010092507));
#121423=CARTESIAN_POINT('Ctrl Pts',(-8.8397657908465,10.2886140266636,10.7885851805867));
#121424=CARTESIAN_POINT('Ctrl Pts',(-8.82638754072009,10.2821221852604,
10.8922618935437));
#121425=CARTESIAN_POINT('Ctrl Pts',(-8.82321816208708,10.2794083401122,
10.9355191768748));
#121426=CARTESIAN_POINT('Ctrl Pts',(-8.82211597393611,10.2754756646011,
10.9968866780313));
#121427=CARTESIAN_POINT('Ctrl Pts',(-8.82220646974194,10.2743097013499,
11.0149271686104));
#121428=CARTESIAN_POINT('Ctrl Pts',(-8.82310657662545,10.2722091344293,
11.0470799920346));
#121429=CARTESIAN_POINT('Ctrl Pts',(-8.82375598102475,10.2712793549658,
11.0611934288648));
#121430=CARTESIAN_POINT('Ctrl Pts',(-8.82512879344959,10.269854175078,11.0826238295905));
#121431=CARTESIAN_POINT('Ctrl Pts',(-8.82566710723015,10.2693644769871,
11.0899516651189));
#121432=CARTESIAN_POINT('Ctrl Pts',(-8.82677182083556,10.2684691421378,
11.1032813645461));
#121433=CARTESIAN_POINT('Ctrl Pts',(-8.82731580772734,10.2680642127124,
11.1092848733099));
#121434=CARTESIAN_POINT('Ctrl Pts',(-8.82859404398805,10.2671838847777,
11.1222807376632));
#121435=CARTESIAN_POINT('Ctrl Pts',(-8.82934486372115,10.2667079867487,
11.1292711908589));
#121436=CARTESIAN_POINT('Ctrl Pts',(-8.83157650266895,10.2653968716313,
11.1484314161075));
#121437=CARTESIAN_POINT('Ctrl Pts',(-8.83318478637407,10.264557740133,11.1605851549259));
#121438=CARTESIAN_POINT('Ctrl Pts',(-8.84550380420088,10.2587672285939,
11.2436826790302));
#121439=CARTESIAN_POINT('Ctrl Pts',(-8.862486347632,10.2536194438306,11.3135316183597));
#121440=CARTESIAN_POINT('Ctrl Pts',(-8.90277680409362,10.2445255288309,
11.4312459212113));
#121441=CARTESIAN_POINT('Ctrl Pts',(-8.92316751660878,10.2406368184134,
11.4798996261221));
#121442=CARTESIAN_POINT('Ctrl Pts',(-8.96310822090906,10.2341549052335,
11.5597206450897));
#121443=CARTESIAN_POINT('Ctrl Pts',(-8.98098407378706,10.2315339282751,
11.5916408262308));
#121444=CARTESIAN_POINT('Ctrl Pts',(-9.00401565860117,10.2285040565285,
11.6286168683901));
#121445=CARTESIAN_POINT('Ctrl Pts',(-9.00776621475628,10.2280205314956,
11.6345203675979));
#121446=CARTESIAN_POINT('Ctrl Pts',(-9.01369505309372,10.2272717736742,
11.6436714217074));
#121447=CARTESIAN_POINT('Ctrl Pts',(-9.01583722032277,10.2270043198606,
11.6469420156628));
#121448=CARTESIAN_POINT('Ctrl Pts',(-9.01987692689434,10.2265057688019,
11.6530432114334));
#121449=CARTESIAN_POINT('Ctrl Pts',(-9.02177045959044,10.2262744359305,
11.6558762391433));
#121450=CARTESIAN_POINT('Ctrl Pts',(-9.02616906100948,10.2257423962922,
11.6623958252496));
#121451=CARTESIAN_POINT('Ctrl Pts',(-9.02868279048243,10.2254422662415,
11.6660764274075));
#121452=CARTESIAN_POINT('Ctrl Pts',(-9.0368979624016,10.2244737006971,11.6779596700908));
#121453=CARTESIAN_POINT('Ctrl Pts',(-9.04268306253631,10.2238105373222,
11.6861043262969));
#121454=CARTESIAN_POINT('Ctrl Pts',(-9.09388370336655,10.2180932540946,
11.7562793942878));
#121455=CARTESIAN_POINT('Ctrl Pts',(-9.14517478797374,10.2133749096299,
11.8138074119133));
#121456=CARTESIAN_POINT('Ctrl Pts',(-9.25195686906547,10.2043889820855,
11.912247829077));
#121457=CARTESIAN_POINT('Ctrl Pts',(-9.30612918828313,10.2001455722198,
11.9540998653966));
#121458=CARTESIAN_POINT('Ctrl Pts',(-9.37997676132295,10.1944644593128,
12.0015208861984));
#121459=CARTESIAN_POINT('Ctrl Pts',(-9.39658964797795,10.1931933308712,
12.0116169133594));
#121460=CARTESIAN_POINT('Ctrl Pts',(-9.42066292059268,10.1913568153999,
12.0254427886401));
#121461=CARTESIAN_POINT('Ctrl Pts',(-9.4279254211099,10.190803469697,12.0295120371455));
#121462=CARTESIAN_POINT('Ctrl Pts',(-9.44062055374436,10.189837089304,12.0364494337988));
#121463=CARTESIAN_POINT('Ctrl Pts',(-9.44603368236305,10.1894253081422,
12.0393527361814));
#121464=CARTESIAN_POINT('Ctrl Pts',(-9.45721943217093,10.1885748378738,
12.0452399448286));
#121465=CARTESIAN_POINT('Ctrl Pts',(-9.46299452244783,10.1881359862442,
12.0482186800673));
#121466=CARTESIAN_POINT('Ctrl Pts',(-9.47782986725035,10.1870090845652,
12.05571583124));
#121467=CARTESIAN_POINT('Ctrl Pts',(-9.4869241182467,10.186318694758,12.0601654080086));
#121468=CARTESIAN_POINT('Ctrl Pts',(-9.52350079821706,10.1835428887661,
12.0774805583007));
#121469=CARTESIAN_POINT('Ctrl Pts',(-9.55141639784078,10.1814259962953,
12.0893981398639));
#121470=CARTESIAN_POINT('Ctrl Pts',(-9.6653653704601,10.1727864107622,12.1329220490494));
#121471=CARTESIAN_POINT('Ctrl Pts',(-9.75448857278884,10.1660001839393,
12.1555140137383));
#121472=CARTESIAN_POINT('Ctrl Pts',(-9.88440660426491,10.1564431663294,
12.1727269753214));
#121473=CARTESIAN_POINT('Ctrl Pts',(-9.92374220836997,10.1535978001401,
12.1759403722289));
#121474=CARTESIAN_POINT('Ctrl Pts',(-9.9725950795899,10.1501759802145,12.1774688878563));
#121475=CARTESIAN_POINT('Ctrl Pts',(-9.98202532438966,10.1495206518886,
12.1776506003725));
#121476=CARTESIAN_POINT('Ctrl Pts',(-9.99585925486454,10.1485678807776,
12.1777509485204));
#121477=CARTESIAN_POINT('Ctrl Pts',(-10.0002616464349,10.1482659533288,
12.1777581991312));
#121478=CARTESIAN_POINT('Ctrl Pts',(-10.0080582213571,10.1477336207909,
12.1777273233041));
#121479=CARTESIAN_POINT('Ctrl Pts',(-10.0114523193918,10.1475026837675,
12.1776992096452));
#121480=CARTESIAN_POINT('Ctrl Pts',(-10.0188413690828,10.1470016950095,
12.1776060579574));
#121481=CARTESIAN_POINT('Ctrl Pts',(-10.0228361440019,10.146731953355,12.1775353653439));
#121482=CARTESIAN_POINT('Ctrl Pts',(-10.0340185504667,10.1459797913893,
12.1772805506011));
#121483=CARTESIAN_POINT('Ctrl Pts',(-10.0412051151877,10.1454997732333,
12.1770509340774));
#121484=CARTESIAN_POINT('Ctrl Pts',(-10.0848526923941,10.1426024266976,
12.1752561027433));
#121485=CARTESIAN_POINT('Ctrl Pts',(-10.1212306846842,10.1402639367501,
12.1720625316576));
#121486=CARTESIAN_POINT('Ctrl Pts',(-10.2682742420256,10.1309134072535,
12.1522323949297));
#121487=CARTESIAN_POINT('Ctrl Pts',(-10.376443399477,10.124213050488,12.1215623876192));
#121488=CARTESIAN_POINT('Ctrl Pts',(-10.4972292166454,10.1156668605729,
12.0678347207529));
#121489=CARTESIAN_POINT('Ctrl Pts',(-10.5155757364185,10.1143394506538,
12.0590984211393));
#121490=CARTESIAN_POINT('Ctrl Pts',(-10.5412354941172,10.1124360206062,
12.0460549311523));
#121491=CARTESIAN_POINT('Ctrl Pts',(-10.5487429254111,10.1118733096992,
12.0421362553317));
#121492=CARTESIAN_POINT('Ctrl Pts',(-10.5616432108252,10.1108959462641,
12.0352246122339));
#121493=CARTESIAN_POINT('Ctrl Pts',(-10.5670560878653,10.1104826301208,
12.0322695795174));
#121494=CARTESIAN_POINT('Ctrl Pts',(-10.5780825109515,10.1096339268534,
12.0261370663789));
#121495=CARTESIAN_POINT('Ctrl Pts',(-10.5836936507828,10.1091984132654,
12.0229557114803));
#121496=CARTESIAN_POINT('Ctrl Pts',(-10.5978500056684,10.1080902677247,
12.0147750706219));
#121497=CARTESIAN_POINT('Ctrl Pts',(-10.6063586987922,10.1074154466459,
12.0097139155532));
#121498=CARTESIAN_POINT('Ctrl Pts',(-10.639127271279,10.1047816295369,11.9896588946422));
#121499=CARTESIAN_POINT('Ctrl Pts',(-10.6629014561146,10.1027951030559,
11.973894150424));
#121500=CARTESIAN_POINT('Ctrl Pts',(-10.7544619628815,10.0948339223381,
11.9082733543169));
#121501=CARTESIAN_POINT('Ctrl Pts',(-10.8173896212803,10.0886374248943,
11.852082107418));
#121502=CARTESIAN_POINT('Ctrl Pts',(-10.8788028811276,10.0819307434755,
11.7841278894994));
#121503=CARTESIAN_POINT('Ctrl Pts',(-10.8837669353067,10.0813834925766,
11.7785287770944));
#121504=CARTESIAN_POINT('Ctrl Pts',(-10.9088181494688,10.0785964622036,
11.7497243463314));
#121505=CARTESIAN_POINT('Ctrl Pts',(-10.9280474112327,10.0763724346722,
11.7257859697885));
#121506=CARTESIAN_POINT('Ctrl Pts',(-10.9534046025276,10.0733431379989,
11.6915607932475));
#121507=CARTESIAN_POINT('Ctrl Pts',(-10.9603435967534,10.0725032124597,
11.6818921226765));
#121508=CARTESIAN_POINT('Ctrl Pts',(-10.9721963356003,10.0710511755734,
11.664836823074));
#121509=CARTESIAN_POINT('Ctrl Pts',(-10.9771753009775,10.0704355872511,
11.6574968890905));
#121510=CARTESIAN_POINT('Ctrl Pts',(-10.9844417902834,10.0695294800027,
11.6465198143342));
#121511=CARTESIAN_POINT('Ctrl Pts',(-10.9867929604971,10.0692350607974,
11.6429254726311));
#121512=CARTESIAN_POINT('Ctrl Pts',(-10.9907860906683,10.0687330044068,
11.6367474813839));
#121513=CARTESIAN_POINT('Ctrl Pts',(-10.992437697833,10.0685247463666,11.6341702052227));
#121514=CARTESIAN_POINT('Ctrl Pts',(-10.9961911124559,10.0680500924463,
11.6282625548572));
#121515=CARTESIAN_POINT('Ctrl Pts',(-10.9982862814403,10.0677841280645,
11.6249280532942));
#121516=CARTESIAN_POINT('Ctrl Pts',(-11.0040250740278,10.0670526390294,
11.6156921423218));
#121517=CARTESIAN_POINT('Ctrl Pts',(-11.0076334262963,10.0665893109604,
11.6097688474448));
#121518=CARTESIAN_POINT('Ctrl Pts',(-11.0274612749347,10.0640221138178,
11.5765637306348));
#121519=CARTESIAN_POINT('Ctrl Pts',(-11.042626660284,10.0619776231043,11.5486642410104));
#121520=CARTESIAN_POINT('Ctrl Pts',(-11.0847374688505,10.0559372745275,
11.4631246474535));
#121521=CARTESIAN_POINT('Ctrl Pts',(-11.1081608318639,10.0520477490289,
11.4038814842948));
#121522=CARTESIAN_POINT('Ctrl Pts',(-11.1395540968116,10.0453574677012,
11.3007710908776));
#121523=CARTESIAN_POINT('Ctrl Pts',(-11.1500325435245,10.0425936214176,
11.2578206525288));
#121524=CARTESIAN_POINT('Ctrl Pts',(-11.161396683861,10.038595204308,11.196433499557));
#121525=CARTESIAN_POINT('Ctrl Pts',(-11.1643019695358,10.0374155875785,
11.178407532631));
#121526=CARTESIAN_POINT('Ctrl Pts',(-11.1687282071296,10.0352926518581,
11.146194385809));
#121527=CARTESIAN_POINT('Ctrl Pts',(-11.1704125890949,10.0343543110073,
11.1320331904748));
#121528=CARTESIAN_POINT('Ctrl Pts',(-11.172577253173,10.0329186951408,11.1105080484999));
#121529=CARTESIAN_POINT('Ctrl Pts',(-11.1732461847603,10.032427253641,11.1031640889303));
#121530=CARTESIAN_POINT('Ctrl Pts',(-11.1743366042695,10.0315301043074,
11.089805097426));
#121531=CARTESIAN_POINT('Ctrl Pts',(-11.1747809539501,10.0311251186999,
11.0837921450878));
#121532=CARTESIAN_POINT('Ctrl Pts',(-11.1756419443467,10.0302462485327,
11.0707827835452));
#121533=CARTESIAN_POINT('Ctrl Pts',(-11.1760423382264,10.0297718771316,
11.0637855687921));
#121534=CARTESIAN_POINT('Ctrl Pts',(-11.1769665991841,10.028469052508,11.0446383274545));
#121535=CARTESIAN_POINT('Ctrl Pts',(-11.1773647549391,10.027636765878,11.0324833880006));
#121536=CARTESIAN_POINT('Ctrl Pts',(-11.1788670097181,10.0216375951394,
10.9454462200042));
#121537=CARTESIAN_POINT('Ctrl Pts',(-11.1730144356616,10.016255100776,10.8706287511743));
#121538=CARTESIAN_POINT('Ctrl Pts',(-11.1496065400018,10.0063241740616,
10.7369326639045));
#121539=CARTESIAN_POINT('Ctrl Pts',(-11.1344779464935,10.001827147489,10.6778823269995));
#121540=CARTESIAN_POINT('Ctrl Pts',(-11.109123790337,9.99616905279425,10.6034458767436));
#121541=CARTESIAN_POINT('Ctrl Pts',(-11.1030148535012,9.9949017499612,10.5867578717978));
#121542=CARTESIAN_POINT('Ctrl Pts',(-11.0921506344577,9.99280558923922,
10.5590395762574));
#121543=CARTESIAN_POINT('Ctrl Pts',(-11.0876001892522,9.99196805981675,
10.5479325716764));
#121544=CARTESIAN_POINT('Ctrl Pts',(-11.0809749711376,9.99080518356035,
10.5324407420751));
#121545=CARTESIAN_POINT('Ctrl Pts',(-11.0790418797436,9.9904722115102,10.527996640135));
#121546=CARTESIAN_POINT('Ctrl Pts',(-11.0756844832104,9.98990474565607,
10.5204065481754));
#121547=CARTESIAN_POINT('Ctrl Pts',(-11.0742736859224,9.98966946422608,
10.5172546888228));
#121548=CARTESIAN_POINT('Ctrl Pts',(-11.071299258808,9.98918002301297,10.5106871438213));
#121549=CARTESIAN_POINT('Ctrl Pts',(-11.069733128387,9.98892601494905,10.5072726837606));
#121550=CARTESIAN_POINT('Ctrl Pts',(-11.0654998021698,9.9882490559596,10.4981585581365));
#121551=CARTESIAN_POINT('Ctrl Pts',(-11.0628031733358,9.98782783755301,
10.4924725817508));
#121552=CARTESIAN_POINT('Ctrl Pts',(-11.050422214748,9.98593709943094,10.4668981762408));
#121553=CARTESIAN_POINT('Ctrl Pts',(-11.0402236369813,9.98449585061446,
10.4472619807246));
#121554=CARTESIAN_POINT('Ctrl Pts',(-11.018858366515,9.98167188384095,10.4088142360255));
#121555=CARTESIAN_POINT('Ctrl Pts',(-11.0077090153751,9.98028923564516,
10.390003598347));
#121556=CARTESIAN_POINT('Ctrl Pts',(-10.9847977925115,9.97759709328722,
10.3536932939783));
#121557=CARTESIAN_POINT('Ctrl Pts',(-10.9730771274872,9.97628726498755,
10.3361777383488));
#121558=CARTESIAN_POINT('Ctrl Pts',(-10.9320107305756,9.97188542225476,
10.2782341718334));
#121559=CARTESIAN_POINT('Ctrl Pts',(-10.9005664146903,9.96881344615436,
10.2393621733329));
#121560=CARTESIAN_POINT('Ctrl Pts',(-10.8334741801638,9.96260284621545,
10.1664345447527));
#121561=CARTESIAN_POINT('Ctrl Pts',(-10.7979709371211,9.95947212324639,
10.1323871331149));
#121562=CARTESIAN_POINT('Ctrl Pts',(-10.7517733962769,9.95549965017358,
10.0933242745445));
#121563=CARTESIAN_POINT('Ctrl Pts',(-10.7429934385777,9.95474898025505,
10.0861155182275));
#121564=CARTESIAN_POINT('Ctrl Pts',(-10.7288207624926,9.953543213175,10.074818328926));
#121565=CARTESIAN_POINT('Ctrl Pts',(-10.7234945635506,9.95309139058837,
10.0706472996617));
#121566=CARTESIAN_POINT('Ctrl Pts',(-10.7133306329849,9.95223148362811,
10.0628280948171));
#121567=CARTESIAN_POINT('Ctrl Pts',(-10.7085000897431,9.95182376900533,
10.0591709016499));
#121568=CARTESIAN_POINT('Ctrl Pts',(-10.6974416438909,9.95089245966032,
10.0509320402588));
#121569=CARTESIAN_POINT('Ctrl Pts',(-10.6911964655906,9.95036797532428,
10.0463741405225));
#121570=CARTESIAN_POINT('Ctrl Pts',(-10.671816708427,9.94874460840205,10.0325206508186));
#121571=CARTESIAN_POINT('Ctrl Pts',(-10.6585366243807,9.94763800722059,
10.0234328231667));
#121572=CARTESIAN_POINT('Ctrl Pts',(-10.5870542269926,9.94170913329293,
9.9766371438205));
#121573=CARTESIAN_POINT('Ctrl Pts',(-10.5258014668674,9.9367121835445,9.94385883884487));
#121574=CARTESIAN_POINT('Ctrl Pts',(-10.4065664149515,9.92722568950665,
9.89300642346206));
#121575=CARTESIAN_POINT('Ctrl Pts',(-10.3493652962279,9.92277150964326,
9.87364511897384));
#121576=CARTESIAN_POINT('Ctrl Pts',(-10.2737964126132,9.91716098639665,
9.85438082680134));
#121577=CARTESIAN_POINT('Ctrl Pts',(-10.2565638544502,9.915899863062,9.85039884223858));
#121578=CARTESIAN_POINT('Ctrl Pts',(-10.2275369426201,9.91381277906313,
9.84437677578661));
#121579=CARTESIAN_POINT('Ctrl Pts',(-10.2157897183693,9.91297823677459,
9.8421256883715));
#121580=CARTESIAN_POINT('Ctrl Pts',(-10.1992433630736,9.91181875781252,
9.83921553878035));
#121581=CARTESIAN_POINT('Ctrl Pts',(-10.1944718062914,9.91148625344596,
9.83840661083375));
#121582=CARTESIAN_POINT('Ctrl Pts',(-10.1862883879155,9.91091933285136,
9.83707110485011));
#121583=CARTESIAN_POINT('Ctrl Pts',(-10.1828789821384,9.91068413285715,
9.83653007868065));
#121584=CARTESIAN_POINT('Ctrl Pts',(-10.175751902392,9.91019459231923,9.83543121182761));
#121585=CARTESIAN_POINT('Ctrl Pts',(-10.1720338830041,9.90994040546051,
9.83487617066981));
#121586=CARTESIAN_POINT('Ctrl Pts',(-10.1620728356242,9.90926244725283,
9.83343786596021));
#121587=CARTESIAN_POINT('Ctrl Pts',(-10.1558251604455,9.9088404173545,9.83258690244145));
#121588=CARTESIAN_POINT('Ctrl Pts',(-10.1274951240876,9.90693994117975,
9.82895970213356));
#121589=CARTESIAN_POINT('Ctrl Pts',(-10.1053420673119,9.90549012543356,
9.82675936551118));
#121590=CARTESIAN_POINT('Ctrl Pts',(-10.0613550350741,9.90265958900217,
9.82364651981266));
#121591=CARTESIAN_POINT('Ctrl Pts',(-10.039532018702,9.9012786418376,9.82271105470953));
#121592=CARTESIAN_POINT('Ctrl Pts',(-9.99674692403357,9.89859585072934,
9.82206817432506));
#121593=CARTESIAN_POINT('Ctrl Pts',(-9.97579404795538,9.89729357032893,
9.82231240126855));
#121594=CARTESIAN_POINT('Ctrl Pts',(-9.90670392384635,9.89300823891411,
9.82496248113367));
#121595=CARTESIAN_POINT('Ctrl Pts',(-9.85871097048288,9.89004376809584,
9.82976315099974));
#121596=CARTESIAN_POINT('Ctrl Pts',(-9.811149300931,9.88702732255485,9.83748958027846));
#121597=CARTESIAN_POINT('Ctrl Pts',(-9.81114931871824,9.78720258982872,
9.83748957738891));
#121598=CARTESIAN_POINT('Ctrl Pts',(-9.8523278733838,9.78983254678884,9.83080009060967));
#121599=CARTESIAN_POINT('Ctrl Pts',(-9.89381879494177,9.79250430083039,
9.82630478299562));
#121600=CARTESIAN_POINT('Ctrl Pts',(-9.94356232370296,9.79577764382975,
9.82357508836557));
#121601=CARTESIAN_POINT('Ctrl Pts',(-9.95166122798493,9.79631274306618,
9.8232144877574));
#121602=CARTESIAN_POINT('Ctrl Pts',(-9.96582342516913,9.79725254629638,
9.82273036422669));
#121603=CARTESIAN_POINT('Ctrl Pts',(-9.97188521447495,9.79765611754449,
9.82257000627575));
#121604=CARTESIAN_POINT('Ctrl Pts',(-9.9836655472331,9.79844308986436,9.82234939334581));
#121605=CARTESIAN_POINT('Ctrl Pts',(-9.98938383241838,9.79882632102659,
9.82228396430817));
#121606=CARTESIAN_POINT('Ctrl Pts',(-10.0007332813967,9.7995894818911,9.82223676679376));
#121607=CARTESIAN_POINT('Ctrl Pts',(-10.0063642896939,9.7999693623216,9.8222537348324));
#121608=CARTESIAN_POINT('Ctrl Pts',(-10.0195317398902,9.80086066579966,
9.82238784660003));
#121609=CARTESIAN_POINT('Ctrl Pts',(-10.0270675365127,9.80137306094949,
9.82253695744159));
#121610=CARTESIAN_POINT('Ctrl Pts',(-10.0530039667011,9.8031448019985,9.82329927544956));
#121611=CARTESIAN_POINT('Ctrl Pts',(-10.0713905314373,9.80441507000134,
9.8242715697791));
#121612=CARTESIAN_POINT('Ctrl Pts',(-10.1324181164698,9.80868100564058,
9.8289355019231));
#121613=CARTESIAN_POINT('Ctrl Pts',(-10.1748762279876,9.81173137673236,
9.83451975368101));
#121614=CARTESIAN_POINT('Ctrl Pts',(-10.311795516664,9.82181489848881,9.86017823505895));
#121615=CARTESIAN_POINT('Ctrl Pts',(-10.4041093057615,9.82903379542414,
9.88954724361765));
#121616=CARTESIAN_POINT('Ctrl Pts',(-10.5054153235497,9.83692809199575,
9.93610394986887));
#121617=CARTESIAN_POINT('Ctrl Pts',(-10.5189067352052,9.83797792414632,
9.94261865595356));
#121618=CARTESIAN_POINT('Ctrl Pts',(-10.5369787281021,9.83937869249076,
9.95177447073537));
#121619=CARTESIAN_POINT('Ctrl Pts',(-10.5416705550233,9.83974184712636,
9.95419125692172));
#121620=CARTESIAN_POINT('Ctrl Pts',(-10.5494772870861,9.84034505006163,
9.95827918027376));
#121621=CARTESIAN_POINT('Ctrl Pts',(-10.552601155317,9.84058613876326,9.95993292548676));
#121622=CARTESIAN_POINT('Ctrl Pts',(-10.5585232240598,9.84104257664747,
9.96310222458633));
#121623=CARTESIAN_POINT('Ctrl Pts',(-10.5613227945275,9.84125809491405,
9.96461509117329));
#121624=CARTESIAN_POINT('Ctrl Pts',(-10.5687422680068,9.84182867680468,
9.96866345622333));
#121625=CARTESIAN_POINT('Ctrl Pts',(-10.5733514098863,9.84218252587693,
9.97121868342542));
#121626=CARTESIAN_POINT('Ctrl Pts',(-10.5899552324494,9.8434555838853,9.98056979818936));
#121627=CARTESIAN_POINT('Ctrl Pts',(-10.601848045967,9.84436433026698,9.98754551590718));
#121628=CARTESIAN_POINT('Ctrl Pts',(-10.6795426477743,9.8502990617593,10.0349702014326));
#121629=CARTESIAN_POINT('Ctrl Pts',(-10.7413588424396,9.85502021041961,
10.0816042601525));
#121630=CARTESIAN_POINT('Ctrl Pts',(-10.8344700822246,9.86286215657187,
10.1674185152224));
#121631=CARTESIAN_POINT('Ctrl Pts',(-10.8686302721791,9.8659355375177,10.2031228682169));
#121632=CARTESIAN_POINT('Ctrl Pts',(-10.913048807546,9.87033822437074,10.2558097441577));
#121633=CARTESIAN_POINT('Ctrl Pts',(-10.9252753294953,9.87159875525423,
10.2710673813529));
#121634=CARTESIAN_POINT('Ctrl Pts',(-10.9461591585574,9.87384668091376,
10.2985010274177));
#121635=CARTESIAN_POINT('Ctrl Pts',(-10.9549752892441,9.87482801611236,
10.3105508530133));
#121636=CARTESIAN_POINT('Ctrl Pts',(-10.9678306337069,9.87631056658614,
10.3288412306251));
#121637=CARTESIAN_POINT('Ctrl Pts',(-10.9720439284502,9.87680522282221,
10.3349580267463));
#121638=CARTESIAN_POINT('Ctrl Pts',(-10.9762546223322,9.87730869480909,
10.341196550739));
#121639=CARTESIAN_POINT('Ctrl Pts',(-10.9763102281505,9.87731534522267,
10.3412789582898));
#121640=CARTESIAN_POINT('Ctrl Pts',(-10.9764240026447,9.87732895591257,
10.3414476175867));
#121641=CARTESIAN_POINT('Ctrl Pts',(-10.9764821703287,9.87733591622579,
10.341533870003));
#121642=CARTESIAN_POINT('Ctrl Pts',(-10.9766012020463,9.87735016316377,
10.3417104235061));
#121643=CARTESIAN_POINT('Ctrl Pts',(-10.9766620649907,9.87735744982969,
10.341800725337));
#121644=CARTESIAN_POINT('Ctrl Pts',(-10.9767866285292,9.87737236691389,
10.3419855945139));
#121645=CARTESIAN_POINT('Ctrl Pts',(-10.9768503279104,9.87737999737614,
10.3420801626625));
#121646=CARTESIAN_POINT('Ctrl Pts',(-10.9769807137374,9.87739562052947,
10.3422737942382));
#121647=CARTESIAN_POINT('Ctrl Pts',(-10.9770473988811,9.8774036132734,10.3423728586042));
#121648=CARTESIAN_POINT('Ctrl Pts',(-10.9771839144923,9.87741998059714,
10.3425757264834));
#121649=CARTESIAN_POINT('Ctrl Pts',(-10.9772537434496,9.87742835522663,
10.3426795309249));
#121650=CARTESIAN_POINT('Ctrl Pts',(-10.9773967138817,9.8774455070784,10.3428921371793));
#121651=CARTESIAN_POINT('Ctrl Pts',(-10.9774698537432,9.87745428436218,
10.343000940099));
#121652=CARTESIAN_POINT('Ctrl Pts',(-10.9776196228563,9.87747226352813,
10.3432238171254));
#121653=CARTESIAN_POINT('Ctrl Pts',(-10.9776962503026,9.87748146547562,
10.3433378924218));
#121654=CARTESIAN_POINT('Ctrl Pts',(-10.9778180379123,9.87749609555491,
10.343519266237));
#121655=CARTESIAN_POINT('Ctrl Pts',(-10.9778632111151,9.8775015232052,10.3435865560364));
#121656=CARTESIAN_POINT('Ctrl Pts',(-10.9779649073965,9.87751374467584,
10.3437380761536));
#121657=CARTESIAN_POINT('Ctrl Pts',(-10.9780214265277,9.87752053864082,
10.3438223090943));
#121658=CARTESIAN_POINT('Ctrl Pts',(-10.9781486559982,9.877535836301,10.3440119777118));
#121659=CARTESIAN_POINT('Ctrl Pts',(-10.9782193601631,9.87754434022368,
10.3441174175063));
#121660=CARTESIAN_POINT('Ctrl Pts',(-10.9783785031417,9.87756348714072,
10.3443548274198));
#121661=CARTESIAN_POINT('Ctrl Pts',(-10.9784669322995,9.87757413049253,
10.3444868039972));
#121662=CARTESIAN_POINT('Ctrl Pts',(-10.9786659356483,9.87759809204481,
10.3447839376166));
#121663=CARTESIAN_POINT('Ctrl Pts',(-10.9787764947074,9.87761141080147,
10.3449491047165));
#121664=CARTESIAN_POINT('Ctrl Pts',(-10.9790252299308,9.87764139010588,
10.3453209004046));
#121665=CARTESIAN_POINT('Ctrl Pts',(-10.9791633824834,9.87765805152672,
10.3455275447418));
#121666=CARTESIAN_POINT('Ctrl Pts',(-10.9794469019112,9.87769226561721,
10.3459519150913));
#121667=CARTESIAN_POINT('Ctrl Pts',(-10.9795922616295,9.87770981855088,
10.3461696458624));
#121668=CARTESIAN_POINT('Ctrl Pts',(-10.9831001393132,9.87813368960713,
10.3514278058397));
#121669=CARTESIAN_POINT('Ctrl Pts',(-10.9864237285865,9.87854143680692,
10.35649397805));
#121670=CARTESIAN_POINT('Ctrl Pts',(-10.9939073677419,9.87947384170192,
10.3680955591872));
#121671=CARTESIAN_POINT('Ctrl Pts',(-10.9980422857103,9.87999939824166,
10.3746467646654));
#121672=CARTESIAN_POINT('Ctrl Pts',(-11.0106126574739,9.88162996072876,
10.3950050379172));
#121673=CARTESIAN_POINT('Ctrl Pts',(-11.0188281461086,9.88274278676537,
10.4089450014902));
#121674=CARTESIAN_POINT('Ctrl Pts',(-11.0628089117876,9.88897389469459,
10.4872140778996));
#121675=CARTESIAN_POINT('Ctrl Pts',(-11.0927642357806,9.89429109071009,
10.5546067557565));
#121676=CARTESIAN_POINT('Ctrl Pts',(-11.1317571717245,9.90324854645872,
10.670470585973));
#121677=CARTESIAN_POINT('Ctrl Pts',(-11.1444073466782,9.90683471397212,
10.7175182015803));
#121678=CARTESIAN_POINT('Ctrl Pts',(-11.1606612122813,9.91273817709745,
10.797415594826));
#121679=CARTESIAN_POINT('Ctrl Pts',(-11.1658621579242,9.91508608094091,
10.8298801871881));
#121680=CARTESIAN_POINT('Ctrl Pts',(-11.1704936316568,9.91784418016715,
10.869286204795));
#121681=CARTESIAN_POINT('Ctrl Pts',(-11.1712298969036,9.91831478905645,
10.8760565769925));
#121682=CARTESIAN_POINT('Ctrl Pts',(-11.1722923280178,9.91904793676694,
10.8866830547739));
#121683=CARTESIAN_POINT('Ctrl Pts',(-11.1726582731051,9.9193125544387,10.8905349005046));
#121684=CARTESIAN_POINT('Ctrl Pts',(-11.1733114952172,9.91980876409739,
10.8977901076806));
#121685=CARTESIAN_POINT('Ctrl Pts',(-11.1736029502361,9.92004056618484,
10.9011929029623));
#121686=CARTESIAN_POINT('Ctrl Pts',(-11.1742459513468,9.92057743569713,
10.9091046694058));
#121687=CARTESIAN_POINT('Ctrl Pts',(-11.1745863336722,9.92088188945316,
10.9136144583462));
#121688=CARTESIAN_POINT('Ctrl Pts',(-11.1756213021207,9.92187970981186,
10.9284664014418));
#121689=CARTESIAN_POINT('Ctrl Pts',(-11.1762053611257,9.92256735084233,
10.9388161115897));
#121690=CARTESIAN_POINT('Ctrl Pts',(-11.1796683774466,9.92784359227748,
11.0189848508572));
#121691=CARTESIAN_POINT('Ctrl Pts',(-11.1764653806438,9.93215805823227,
11.0889369088581));
#121692=CARTESIAN_POINT('Ctrl Pts',(-11.1626694761059,9.93851154953261,
11.1907124679081));
#121693=CARTESIAN_POINT('Ctrl Pts',(-11.1569056978916,9.94053939612312,
11.2230262157098));
#121694=CARTESIAN_POINT('Ctrl Pts',(-11.1380310498144,9.94598213135829,
11.3081135517474));
#121695=CARTESIAN_POINT('Ctrl Pts',(-11.1226047891467,9.94942977090415,
11.3602860059021));
#121696=CARTESIAN_POINT('Ctrl Pts',(-11.0995712052823,9.95375907795563,
11.4221061557952));
#121697=CARTESIAN_POINT('Ctrl Pts',(-11.0953476050538,9.95452760333169,
11.4329480922691));
#121698=CARTESIAN_POINT('Ctrl Pts',(-11.0883934437932,9.95575522382811,
11.4500459222704));
#121699=CARTESIAN_POINT('Ctrl Pts',(-11.0857678665593,9.95621082836442,
11.4563439024372));
#121700=CARTESIAN_POINT('Ctrl Pts',(-11.0807126090511,9.95707365166353,
11.4681793268876));
#121701=CARTESIAN_POINT('Ctrl Pts',(-11.0782947100244,9.95748046379671,
11.4737215864668));
#121702=CARTESIAN_POINT('Ctrl Pts',(-11.0727299135412,9.9584038260772,11.4862137358509));
#121703=CARTESIAN_POINT('Ctrl Pts',(-11.0695579749783,9.95892121004558,
11.4931521040812));
#121704=CARTESIAN_POINT('Ctrl Pts',(-11.0597124394219,9.96050085258223,
11.5141465871658));
#121705=CARTESIAN_POINT('Ctrl Pts',(-11.0528277266683,9.96157024113716,
11.5281012263174));
#121706=CARTESIAN_POINT('Ctrl Pts',(-11.005004702315,9.96877616834009,11.6203796534567));
#121707=CARTESIAN_POINT('Ctrl Pts',(-10.9556451671787,9.97521245360292,
11.6940043920953));
#121708=CARTESIAN_POINT('Ctrl Pts',(-10.8558418246479,9.98654185796914,
11.8117820910479));
#121709=CARTESIAN_POINT('Ctrl Pts',(-10.8089862925539,9.99138505794548,
11.85848615138));
#121710=CARTESIAN_POINT('Ctrl Pts',(-10.7524728406437,9.99653527007772,
11.9060578842726));
#121711=CARTESIAN_POINT('Ctrl Pts',(-10.7464375382498,9.99707714665545,
11.9110363742705));
#121712=CARTESIAN_POINT('Ctrl Pts',(-10.73717635193,9.99789580571806,11.9185220581034));
#121713=CARTESIAN_POINT('Ctrl Pts',(-10.7339864318326,9.99817550161973,
11.9210731047092));
#121714=CARTESIAN_POINT('Ctrl Pts',(-10.7281281629122,9.99868490442716,
11.9257083253272));
#121715=CARTESIAN_POINT('Ctrl Pts',(-10.725464075222,9.998914956155,11.9277976079804));
#121716=CARTESIAN_POINT('Ctrl Pts',(-10.719408138791,9.99943431236045,11.932504878962));
#121717=CARTESIAN_POINT('Ctrl Pts',(-10.7160109838593,9.99972313437981,
11.9351158708311));
#121718=CARTESIAN_POINT('Ctrl Pts',(-10.7071365837252,10.0004713252565,
11.941859859105));
#121719=CARTESIAN_POINT('Ctrl Pts',(-10.7016372443882,10.0009287839368,
11.9459637017154));
#121720=CARTESIAN_POINT('Ctrl Pts',(-10.6561166846949,10.004667726416,11.9793177181599));
#121721=CARTESIAN_POINT('Ctrl Pts',(-10.6143159712585,10.0078016495747,
12.0060663199458));
#121722=CARTESIAN_POINT('Ctrl Pts',(-10.5618754311339,10.0115400676978,
12.0351322030602));
#121723=CARTESIAN_POINT('Ctrl Pts',(-10.5527360003429,10.0121848153562,
12.0400411511428));
#121724=CARTESIAN_POINT('Ctrl Pts',(-10.4827227561273,10.0170807842753,
12.0764629054364));
#121725=CARTESIAN_POINT('Ctrl Pts',(-10.4192701796792,10.021280905765,12.1027264754644));
#121726=CARTESIAN_POINT('Ctrl Pts',(-10.3314743089277,10.0271215432245,
12.1303859642725));
#121727=CARTESIAN_POINT('Ctrl Pts',(-10.3088482741071,10.0286282484068,
12.1367762685141));
#121728=CARTESIAN_POINT('Ctrl Pts',(-10.2692477311084,10.0312796280453,
12.1466911684563));
#121729=CARTESIAN_POINT('Ctrl Pts',(-10.2523582714307,10.0324148327803,
12.1505260663637));
#121730=CARTESIAN_POINT('Ctrl Pts',(-10.2275951058526,10.034088635895,12.1555772740474));
#121731=CARTESIAN_POINT('Ctrl Pts',(-10.2197833835956,10.0346179916649,
12.1570884268811));
#121732=CARTESIAN_POINT('Ctrl Pts',(-10.2059711900595,10.0355566080363,
12.1596154370835));
#121733=CARTESIAN_POINT('Ctrl Pts',(-10.1999769735943,10.0359648227329,
12.1606641636243));
#121734=CARTESIAN_POINT('Ctrl Pts',(-10.1874206812549,10.036821876427,12.1627608126972));
#121735=CARTESIAN_POINT('Ctrl Pts',(-10.1808573424513,10.0372709812275,
12.1637997413075));
#121736=CARTESIAN_POINT('Ctrl Pts',(-10.1635930599042,10.0384554030377,
12.1663829838843));
#121737=CARTESIAN_POINT('Ctrl Pts',(-10.1528792395733,10.039193544145,12.1678355530397));
#121738=CARTESIAN_POINT('Ctrl Pts',(-10.1057119781914,10.0424578006168,
12.1735702759618));
#121739=CARTESIAN_POINT('Ctrl Pts',(-10.0690933233369,10.0450311957578,
12.1762941077919));
#121740=CARTESIAN_POINT('Ctrl Pts',(-9.95543740293148,10.0531413809449,
12.1794229851852));
#121741=CARTESIAN_POINT('Ctrl Pts',(-9.87844784428245,10.0588232812969,
12.1739877377011));
#121742=CARTESIAN_POINT('Ctrl Pts',(-9.76919844508157,10.0669295751954,
12.1554091045433));
#121743=CARTESIAN_POINT('Ctrl Pts',(-9.73610446858114,10.0693882137826,
12.1483026625576));
#121744=CARTESIAN_POINT('Ctrl Pts',(-9.69110731905805,10.0727008095166,
12.1365916959968));
#121745=CARTESIAN_POINT('Ctrl Pts',(-9.67890584703845,10.0735958694567,
12.1332051645396));
#121746=CARTESIAN_POINT('Ctrl Pts',(-9.65784012121549,10.0751330090084,
12.1269907650452));
#121747=CARTESIAN_POINT('Ctrl Pts',(-9.64895053646607,10.0757791147434,
12.124253465524));
#121748=CARTESIAN_POINT('Ctrl Pts',(-9.635926360528,10.0767210347194,12.1200734822325));
#121749=CARTESIAN_POINT('Ctrl Pts',(-9.63176615112178,10.0770211951966,
12.1187126774297));
#121750=CARTESIAN_POINT('Ctrl Pts',(-9.62439622793677,10.0775515576935,
12.1162564086244));
#121751=CARTESIAN_POINT('Ctrl Pts',(-9.62118355133466,10.077782277421,12.1151702392938));
#121752=CARTESIAN_POINT('Ctrl Pts',(-9.6141809173022,10.0782841235858,12.1127689741043));
#121753=CARTESIAN_POINT('Ctrl Pts',(-9.61039295635534,10.0785549294332,
12.1114483825353));
#121754=CARTESIAN_POINT('Ctrl Pts',(-9.59976390686338,10.079313152015,12.1076817746339));
#121755=CARTESIAN_POINT('Ctrl Pts',(-9.59293845562154,10.0797981039373,
12.1051917253199));
#121756=CARTESIAN_POINT('Ctrl Pts',(-9.55022372314629,10.0828233882771,
12.0891592026522));
#121757=CARTESIAN_POINT('Ctrl Pts',(-9.51498703366338,10.0852764778098,
12.0739318136012));
#121758=CARTESIAN_POINT('Ctrl Pts',(-9.40341724966897,10.0930962619891,
12.0191030064842));
#121759=CARTESIAN_POINT('Ctrl Pts',(-9.33066260023107,10.098297230063,11.9728669711294));
#121760=CARTESIAN_POINT('Ctrl Pts',(-9.2328997028319,10.1062143586153,11.8945380307947));
#121761=CARTESIAN_POINT('Ctrl Pts',(-9.20346716003467,10.1087390786546,
11.8684331266418));
#121762=CARTESIAN_POINT('Ctrl Pts',(-9.16777638611086,10.1120262851994,
11.833434364177));
#121763=CARTESIAN_POINT('Ctrl Pts',(-9.16025782038972,10.1127323963158,
11.8258583670641));
#121764=CARTESIAN_POINT('Ctrl Pts',(-9.14824794525244,10.1138833698487,
11.8134231736636));
#121765=CARTESIAN_POINT('Ctrl Pts',(-9.14369268611624,10.1143254696866,
11.8086263682286));
#121766=CARTESIAN_POINT('Ctrl Pts',(-9.13501885193152,10.115178193465,11.7993371113518));
#121767=CARTESIAN_POINT('Ctrl Pts',(-9.13089425444719,10.1155885435035,
11.7948505549792));
#121768=CARTESIAN_POINT('Ctrl Pts',(-9.12151276665089,10.116533267278,11.7844854576798));
#121769=CARTESIAN_POINT('Ctrl Pts',(-9.11627977627321,10.1170686079563,
11.7785857778109));
#121770=CARTESIAN_POINT('Ctrl Pts',(-9.10240657725098,10.1185108256013,
11.7626250588449));
#121771=CARTESIAN_POINT('Ctrl Pts',(-9.09387661543735,10.1194220954155,
11.752470145627));
#121772=CARTESIAN_POINT('Ctrl Pts',(-9.02465384580525,10.1270269828836,
11.6671763377686));
#121773=CARTESIAN_POINT('Ctrl Pts',(-8.97325535110623,10.1340900363597,
11.584989409425));
#121774=CARTESIAN_POINT('Ctrl Pts',(-8.9150803558295,10.1441918107109,11.4601520121544));
#121775=CARTESIAN_POINT('Ctrl Pts',(-8.89965608253601,10.1472017765896,
11.4219409759152));
#121776=CARTESIAN_POINT('Ctrl Pts',(-8.87934460717991,10.1516673060155,
11.3628764650067));
#121777=CARTESIAN_POINT('Ctrl Pts',(-8.87297098728736,10.1531700722691,
11.3425690872504));
#121778=CARTESIAN_POINT('Ctrl Pts',(-8.86551506679084,10.1550600291455,
11.3163459626639));
#121779=CARTESIAN_POINT('Ctrl Pts',(-8.86392321440222,10.1554724463104,
11.310580702532));
#121780=CARTESIAN_POINT('Ctrl Pts',(-8.86142112596248,10.156135212824,11.3012421011723));
#121781=CARTESIAN_POINT('Ctrl Pts',(-8.86048365568388,10.1563870464388,
11.2976762635915));
#121782=CARTESIAN_POINT('Ctrl Pts',(-8.8587024910475,10.1568723600284,11.2907695495652));
#121783=CARTESIAN_POINT('Ctrl Pts',(-8.8578566939894,10.1571059496638,11.2874293022541));
#121784=CARTESIAN_POINT('Ctrl Pts',(-8.85581923698841,10.1576765687429,
11.2792319023384));
#121785=CARTESIAN_POINT('Ctrl Pts',(-8.85464381426869,10.1580126914523,
11.2743707050295));
#121786=CARTESIAN_POINT('Ctrl Pts',(-8.85134348863313,10.1589773496186,
11.2603306437367));
#121787=CARTESIAN_POINT('Ctrl Pts',(-8.84929765658777,10.1596017446629,
11.251133341962));
#121788=CARTESIAN_POINT('Ctrl Pts',(-8.83329312878412,10.1647241202077,
11.1748766409154));
#121789=CARTESIAN_POINT('Ctrl Pts',(-8.82509679049962,10.1689582632367,
11.1067320987606));
#121790=CARTESIAN_POINT('Ctrl Pts',(-8.82095568837646,10.1768457733572,
10.979303972472));
#121791=CARTESIAN_POINT('Ctrl Pts',(-8.82347091754177,10.1804870927864,
10.9202972995075));
#121792=CARTESIAN_POINT('Ctrl Pts',(-8.83294116683044,10.1856208900694,
10.8401902323332));
#121793=CARTESIAN_POINT('Ctrl Pts',(-8.83608190059323,10.1870147651435,
10.818726573289));
#121794=CARTESIAN_POINT('Ctrl Pts',(-8.84261573541903,10.1894853929018,
10.7813175109578));
#121795=CARTESIAN_POINT('Ctrl Pts',(-8.84575062497382,10.1905544019334,
10.765332777549));
#121796=CARTESIAN_POINT('Ctrl Pts',(-8.85086845922819,10.1921484547219,
10.7418293284208));
#121797=CARTESIAN_POINT('Ctrl Pts',(-8.85259605824133,10.1926654864226,
10.7342565461324));
#121798=CARTESIAN_POINT('Ctrl Pts',(-8.85580495739395,10.1935902279562,
10.7208056097592));
#121799=CARTESIAN_POINT('Ctrl Pts',(-8.8572569853549,10.193996997212,10.7149207071626));
#121800=CARTESIAN_POINT('Ctrl Pts',(-8.860419829456,10.1948592682948,10.7025146256794));
#121801=CARTESIAN_POINT('Ctrl Pts',(-8.86214133748237,10.1953150980078,
10.6959964245187));
#121802=CARTESIAN_POINT('Ctrl Pts',(-8.86688668985026,10.1965369223158,
10.6786341284507));
#121803=CARTESIAN_POINT('Ctrl Pts',(-8.87001015262367,10.1973060730905,
10.6678182325631));
#121804=CARTESIAN_POINT('Ctrl Pts',(-8.88546464750051,10.2009557548812,
10.6170448916394));
#121805=CARTESIAN_POINT('Ctrl Pts',(-8.89976164395921,10.203898639096,10.5777222481572));
#121806=CARTESIAN_POINT('Ctrl Pts',(-8.95903547831701,10.214760540718,10.4382856343051));
#121807=CARTESIAN_POINT('Ctrl Pts',(-9.01584269607229,10.2230047644088,
10.3438282343092));
#121808=CARTESIAN_POINT('Ctrl Pts',(-9.09435318104939,10.2318362655084,
10.2469231591729));
#121809=CARTESIAN_POINT('Ctrl Pts',(-9.10403626307838,10.2328895148301,
10.2354282746097));
#121810=CARTESIAN_POINT('Ctrl Pts',(-9.11741813464309,10.2342940610156,
10.2201460185641));
#121811=CARTESIAN_POINT('Ctrl Pts',(-9.12092581791159,10.2346576582772,
10.2161941780932));
#121812=CARTESIAN_POINT('Ctrl Pts',(-9.12682498134826,10.2352613926566,
10.2096374557708));
#121813=CARTESIAN_POINT('Ctrl Pts',(-9.1292017762616,10.2355025739433,10.2070195342156));
#121814=CARTESIAN_POINT('Ctrl Pts',(-9.1337391810844,10.235959028747,10.2020668105704));
#121815=CARTESIAN_POINT('Ctrl Pts',(-9.13589751156172,10.2361744724633,
10.1997300010209));
#121816=CARTESIAN_POINT('Ctrl Pts',(-9.14106649854063,10.2366865323853,
10.194178867366));
#121817=CARTESIAN_POINT('Ctrl Pts',(-9.14408579511978,10.2369825093353,
10.190972600499));
#121818=CARTESIAN_POINT('Ctrl Pts',(-9.15332467460925,10.237879010605,10.181271215327));
#121819=CARTESIAN_POINT('Ctrl Pts',(-9.15960089012562,10.2384755316472,
10.1748301524246));
#121820=CARTESIAN_POINT('Ctrl Pts',(-9.22051271687433,10.2441539608153,
10.1137343983395));
#121821=CARTESIAN_POINT('Ctrl Pts',(-9.28033704181194,10.2488953106951,
10.0645023815691));
#121822=CARTESIAN_POINT('Ctrl Pts',(-9.40126392457704,10.2579010206164,
9.98350217287021));
#121823=CARTESIAN_POINT('Ctrl Pts',(-9.46115375799348,10.2621402473397,
9.95052581331259));
#121824=CARTESIAN_POINT('Ctrl Pts',(-9.5411564253882,10.2678047917668,9.91513690097317));
#121825=CARTESIAN_POINT('Ctrl Pts',(-9.55894219038821,10.2690634563514,
9.90778513538494));
#121826=CARTESIAN_POINT('Ctrl Pts',(-9.58463674049259,10.2708850305245,
9.89789421352575));
#121827=CARTESIAN_POINT('Ctrl Pts',(-9.59240525612902,10.2714361700404,
9.89499759237496));
#121828=CARTESIAN_POINT('Ctrl Pts',(-9.60597488514384,10.2723998853838,
9.89010049203051));
#121829=CARTESIAN_POINT('Ctrl Pts',(-9.61176231837995,10.2728112264164,
9.88806285740814));
#121830=CARTESIAN_POINT('Ctrl Pts',(-9.62372006744907,10.2736619035269,
9.8839575183728));
#121831=CARTESIAN_POINT('Ctrl Pts',(-9.62989211583079,10.2741014102278,
9.88189555068189));
#121832=CARTESIAN_POINT('Ctrl Pts',(-9.64575649916026,10.275232351951,9.87674130084371));
#121833=CARTESIAN_POINT('Ctrl Pts',(-9.6554722211877,10.2759261608883,9.87372331929939));
#121834=CARTESIAN_POINT('Ctrl Pts',(-9.69472931081829,10.2787350804978,
9.8620844257641));
#121835=CARTESIAN_POINT('Ctrl Pts',(-9.7245619785955,10.2808826337338,9.85449764532584));
#121836=CARTESIAN_POINT('Ctrl Pts',(-9.77340835366934,10.2844217488063,
9.84409389574778));
#121837=CARTESIAN_POINT('Ctrl Pts',(-9.79224544531752,10.2857918682406,
9.84056052594576));
#121838=CARTESIAN_POINT('Ctrl Pts',(-9.81114930150156,10.287171250943,9.83748958018577));
#121839=CARTESIAN_POINT('Origin',(-10.,2.67563288526385,11.));
#121840=CARTESIAN_POINT('',(-9.81114929229234,10.8872795026091,9.83748958168182));
#121841=CARTESIAN_POINT('',(-9.81114930150156,10.7889089429636,9.83748958018577));
#121842=CARTESIAN_POINT('',(-9.81114930150157,2.67563288526385,9.83748958018577));
#121843=CARTESIAN_POINT('',(-11.1777495366547,10.524431373431,11.0010447055591));
#121844=CARTESIAN_POINT('Ctrl Pts',(-9.81114928308311,10.8872795026091,
9.83748958317786));
#121845=CARTESIAN_POINT('Ctrl Pts',(-9.80153143050108,10.886581170619,9.83905201077338));
#121846=CARTESIAN_POINT('Ctrl Pts',(-9.79193198703791,10.8858799908288,
9.84073395523692));
#121847=CARTESIAN_POINT('Ctrl Pts',(-9.73454387667587,10.8816639673094,
9.85152507374089));
#121848=CARTESIAN_POINT('Ctrl Pts',(-9.68733980702918,10.878092617641,9.86346810946966));
#121849=CARTESIAN_POINT('Ctrl Pts',(-9.61862962080496,10.8727994259501,
9.88545794616421));
#121850=CARTESIAN_POINT('Ctrl Pts',(-9.59646596281431,10.871077343618,9.89328970252864));
#121851=CARTESIAN_POINT('Ctrl Pts',(-9.53814242378295,10.8665256973153,
9.91588415171789));
#121852=CARTESIAN_POINT('Ctrl Pts',(-9.50245360370961,10.8637190923385,
9.93179223450883));
#121853=CARTESIAN_POINT('Ctrl Pts',(-9.46111108032463,10.8604917661137,
9.95274310511545));
#121854=CARTESIAN_POINT('Ctrl Pts',(-9.45463498253787,10.8599869658328,
9.95610092631087));
#121855=CARTESIAN_POINT('Ctrl Pts',(-9.44464001173203,10.8592095066125,
9.96140166779736));
#121856=CARTESIAN_POINT('Ctrl Pts',(-9.44109931656387,10.8589344143202,
9.96330272524422));
#121857=CARTESIAN_POINT('Ctrl Pts',(-9.43458838920588,10.8584292400594,
9.9668416014475));
#121858=CARTESIAN_POINT('Ctrl Pts',(-9.43161548894146,10.8581988539951,
9.96847413303503));
#121859=CARTESIAN_POINT('Ctrl Pts',(-9.42482808376164,10.8576734589406,
9.9722396059433));
#121860=CARTESIAN_POINT('Ctrl Pts',(-9.4210183597356,10.8573789812727,9.97438095640616));
#121861=CARTESIAN_POINT('Ctrl Pts',(-9.40917292602147,10.8564644137249,
9.98112601609021));
#121862=CARTESIAN_POINT('Ctrl Pts',(-9.40117930666043,10.8558487418699,
9.98580346246934));
#121863=CARTESIAN_POINT('Ctrl Pts',(-9.3824511212313,10.8544078290771,9.99706084809407));
#121864=CARTESIAN_POINT('Ctrl Pts',(-9.37176507247056,10.8535868763449,
10.0037196863953));
#121865=CARTESIAN_POINT('Ctrl Pts',(-9.33302344769064,10.8506071935734,
10.0287321780463));
#121866=CARTESIAN_POINT('Ctrl Pts',(-9.30564659797557,10.8484947695667,
10.0481110469272));
#121867=CARTESIAN_POINT('Ctrl Pts',(-9.21909402639469,10.841666990973,10.1151017832191));
#121868=CARTESIAN_POINT('Ctrl Pts',(-9.16369123535825,10.8370428942522,
10.1672655872992));
#121869=CARTESIAN_POINT('Ctrl Pts',(-9.0887470444682,10.8298456373801,10.2529068388566));
#121870=CARTESIAN_POINT('Ctrl Pts',(-9.0651919648464,10.8274125294662,10.2825993906165));
#121871=CARTESIAN_POINT('Ctrl Pts',(-9.03670650156127,10.824201660183,10.3222970124379));
#121872=CARTESIAN_POINT('Ctrl Pts',(-9.03042836863093,10.8234754028843,
10.3313098312222));
#121873=CARTESIAN_POINT('Ctrl Pts',(-9.02053430677979,10.8222996200945,
10.3459459594557));
#121874=CARTESIAN_POINT('Ctrl Pts',(-9.01683850421292,10.8218530839732,
10.3515146861777));
#121875=CARTESIAN_POINT('Ctrl Pts',(-9.00987316797461,10.8209971622053,
10.3622062644311));
#121876=CARTESIAN_POINT('Ctrl Pts',(-9.00659548694875,10.8205880945474,
10.3673235710855));
#121877=CARTESIAN_POINT('Ctrl Pts',(-8.99915710356788,10.8196449885876,
10.3791371260857));
#121878=CARTESIAN_POINT('Ctrl Pts',(-8.99502377827826,10.8191099766161,
10.3858501810727));
#121879=CARTESIAN_POINT('Ctrl Pts',(-8.98223805815542,10.8174196990585,
10.4070905700987));
#121880=CARTESIAN_POINT('Ctrl Pts',(-8.97383126500324,10.816255764924,10.421762472407));
#121881=CARTESIAN_POINT('Ctrl Pts',(-8.95484813297215,10.8134982057211,
10.4566111793496));
#121882=CARTESIAN_POINT('Ctrl Pts',(-8.94453585665193,10.8118962088725,
10.4769233705708));
#121883=CARTESIAN_POINT('Ctrl Pts',(-8.88578020292007,10.8021048689982,
10.6014765030514));
#121884=CARTESIAN_POINT('Ctrl Pts',(-8.8522305608705,10.7934649515813,10.712031056074));
#121885=CARTESIAN_POINT('Ctrl Pts',(-8.83252593215987,10.7839836806918,
10.8436953957469));
#121886=CARTESIAN_POINT('Ctrl Pts',(-8.83024808484026,10.7827010860466,
10.8617705748012));
#121887=CARTESIAN_POINT('Ctrl Pts',(-8.82779138592134,10.7810317029888,
10.8857348701571));
#121888=CARTESIAN_POINT('Ctrl Pts',(-8.82723614640671,10.7806268377514,
10.8915818183274));
#121889=CARTESIAN_POINT('Ctrl Pts',(-8.82640557873414,10.7799731757505,
10.9010827583738));
#121890=CARTESIAN_POINT('Ctrl Pts',(-8.82610353136468,10.7797229665814,
10.9047342234988));
#121891=CARTESIAN_POINT('Ctrl Pts',(-8.82554615933276,10.7792355110843,
10.9118779327996));
#121892=CARTESIAN_POINT('Ctrl Pts',(-8.82528936169787,10.7789981933083,
10.9153699859307));
#121893=CARTESIAN_POINT('Ctrl Pts',(-8.82469614236506,10.7784166522687,
10.9239604639775));
#121894=CARTESIAN_POINT('Ctrl Pts',(-8.82437731249267,10.7780733833853,
10.9290601112762));
#121895=CARTESIAN_POINT('Ctrl Pts',(-8.82332299153975,10.7768125269855,
10.9478908897555));
#121896=CARTESIAN_POINT('Ctrl Pts',(-8.82279476504904,10.7759054961799,
10.9616331329053));
#121897=CARTESIAN_POINT('Ctrl Pts',(-8.82205953126637,10.7736106941078,
10.9968000460305));
#121898=CARTESIAN_POINT('Ctrl Pts',(-8.82219617177542,10.7722373946901,
11.0182274442435));
#121899=CARTESIAN_POINT('Ctrl Pts',(-8.82481080651115,10.7673141750267,
11.0958664378761));
#121900=CARTESIAN_POINT('Ctrl Pts',(-8.83073061865043,10.7638592873141,
11.1518875045451));
#121901=CARTESIAN_POINT('Ctrl Pts',(-8.85355814146852,10.7558262112603,
11.2795715011196));
#121902=CARTESIAN_POINT('Ctrl Pts',(-8.87321595123649,10.7512377776358,
11.350492253662));
#121903=CARTESIAN_POINT('Ctrl Pts',(-8.90367827560027,10.7456281366656,
11.4304902706779));
#121904=CARTESIAN_POINT('Ctrl Pts',(-8.90818539614777,10.7448251341771,
11.4417963890945));
#121905=CARTESIAN_POINT('Ctrl Pts',(-8.91556357633511,10.7435504554451,
11.4595017496197));
#121906=CARTESIAN_POINT('Ctrl Pts',(-8.91831804225275,10.7430826638112,
11.4659488744341));
#121907=CARTESIAN_POINT('Ctrl Pts',(-8.92354805095531,10.7422089697321,
11.4778939374242));
#121908=CARTESIAN_POINT('Ctrl Pts',(-8.92600858208183,10.741803584186,11.4833982270904));
#121909=CARTESIAN_POINT('Ctrl Pts',(-8.93157117864938,10.7408993464107,
11.4955898069945));
#121910=CARTESIAN_POINT('Ctrl Pts',(-8.93469396357023,10.7403998030501,
11.5022673068844));
#121911=CARTESIAN_POINT('Ctrl Pts',(-8.9440353234591,10.738928477035,11.5217630074455));
#121912=CARTESIAN_POINT('Ctrl Pts',(-8.95042385449657,10.7379509281313,
11.5344978185298));
#121913=CARTESIAN_POINT('Ctrl Pts',(-8.96551232342165,10.7357042241271,
11.5632608740115));
#121914=CARTESIAN_POINT('Ctrl Pts',(-8.97435651781146,10.7344303451847,
11.5792089005859));
#121915=CARTESIAN_POINT('Ctrl Pts',(-9.00584089217265,10.7300356105158,
11.6329983879148));
#121916=CARTESIAN_POINT('Ctrl Pts',(-9.03023208735937,10.7268595116441,
11.6697677160261));
#121917=CARTESIAN_POINT('Ctrl Pts',(-9.09455620556723,10.7190268830814,
11.7558313891755));
#121918=CARTESIAN_POINT('Ctrl Pts',(-9.13652072817729,10.7143390375931,
11.8034382888994));
#121919=CARTESIAN_POINT('Ctrl Pts',(-9.20519247688796,10.7074309187343,
11.8697155240066));
#121920=CARTESIAN_POINT('Ctrl Pts',(-9.22917710046181,10.7051392245171,
11.8910423954008));
#121921=CARTESIAN_POINT('Ctrl Pts',(-9.2593858576292,10.7024236515511,11.9157696817498));
#121922=CARTESIAN_POINT('Ctrl Pts',(-9.26480590931729,10.701942808905,11.9201266612523));
#121923=CARTESIAN_POINT('Ctrl Pts',(-9.27335865475094,10.7011943951677,
11.9268780709642));
#121924=CARTESIAN_POINT('Ctrl Pts',(-9.27646521624351,10.7009246606986,
11.9293051279843));
#121925=CARTESIAN_POINT('Ctrl Pts',(-9.28200511121423,10.7004474618356,
11.9335886507282));
#121926=CARTESIAN_POINT('Ctrl Pts',(-9.28443350408976,10.700239580793,11.9354512383713));
#121927=CARTESIAN_POINT('Ctrl Pts',(-9.2902826891068,10.6997419384228,11.939901482977));
#121928=CARTESIAN_POINT('Ctrl Pts',(-9.29371038808442,10.699452810147,11.9424799438871));
#121929=CARTESIAN_POINT('Ctrl Pts',(-9.30424461500359,10.6985715909525,
11.9503144918047));
#121930=CARTESIAN_POINT('Ctrl Pts',(-9.31139648250242,10.697983469806,11.9555094956221));
#121931=CARTESIAN_POINT('Ctrl Pts',(-9.32827007757079,10.6966177181266,
11.9674783442409));
#121932=CARTESIAN_POINT('Ctrl Pts',(-9.33803702378796,10.6958437918539,
11.9741870850089));
#121933=CARTESIAN_POINT('Ctrl Pts',(-9.37328879626928,10.6931028093784,
11.9976258807716));
#121934=CARTESIAN_POINT('Ctrl Pts',(-9.39932121479374,10.6911745127712,
12.0135134864214));
#121935=CARTESIAN_POINT('Ctrl Pts',(-9.49019137339902,10.6846625222036,
12.0642388996812));
#121936=CARTESIAN_POINT('Ctrl Pts',(-9.55765934409957,10.6801831461707,
12.094003785954));
#121937=CARTESIAN_POINT('Ctrl Pts',(-9.63835134843804,10.6748324453237,
12.1209090144417));
#121938=CARTESIAN_POINT('Ctrl Pts',(-9.64929058076807,10.6741074783455,
12.1243796775402));
#121939=CARTESIAN_POINT('Ctrl Pts',(-9.69287426794037,10.671217023402,12.1375094506139));
#121940=CARTESIAN_POINT('Ctrl Pts',(-9.72587768746345,10.6690230704251,
12.145910376039));
#121941=CARTESIAN_POINT('Ctrl Pts',(-9.76951185348409,10.6660908351589,
12.1550243840701));
#121942=CARTESIAN_POINT('Ctrl Pts',(-9.77985547593401,10.6653935086531,
12.1570404012885));
#121943=CARTESIAN_POINT('Ctrl Pts',(-9.79670622308358,10.6642532300046,
12.1600905534317));
#121944=CARTESIAN_POINT('Ctrl Pts',(-9.80319757083106,10.6638129428923,
12.1612093923107));
#121945=CARTESIAN_POINT('Ctrl Pts',(-9.81572377817318,10.6629612055448,
12.1632603413709));
#121946=CARTESIAN_POINT('Ctrl Pts',(-9.82175718592707,10.6625500090232,
12.1642000878541));
#121947=CARTESIAN_POINT('Ctrl Pts',(-9.83580384266115,10.6615903544599,
12.1662762047317));
#121948=CARTESIAN_POINT('Ctrl Pts',(-9.84382195966752,10.661040805725,12.167376964766));
#121949=CARTESIAN_POINT('Ctrl Pts',(-9.86978787312542,10.6592551208576,
12.1706693737516));
#121950=CARTESIAN_POINT('Ctrl Pts',(-9.88777421279505,10.6580088634585,
12.1725302941356));
#121951=CARTESIAN_POINT('Ctrl Pts',(-9.98358219291365,10.6513173183515,
12.1802183103532));
#121952=CARTESIAN_POINT('Ctrl Pts',(-10.0617841774874,10.6456509560254,
12.1787127307168));
#121953=CARTESIAN_POINT('Ctrl Pts',(-10.2072553001873,10.634903055233,12.1613917014821));
#121954=CARTESIAN_POINT('Ctrl Pts',(-10.2744314189326,10.6298598732395,
12.1473772335697));
#121955=CARTESIAN_POINT('Ctrl Pts',(-10.3490350731491,10.6243918157777,
12.1248814923333));
#121956=CARTESIAN_POINT('Ctrl Pts',(-10.3580241556568,10.62373537929,12.1220528381882));
#121957=CARTESIAN_POINT('Ctrl Pts',(-10.3717318398115,10.6227390654846,
12.1175578391822));
#121958=CARTESIAN_POINT('Ctrl Pts',(-10.3764751520759,10.6223951773419,
12.1159688825327));
#121959=CARTESIAN_POINT('Ctrl Pts',(-10.3844692567733,10.6218172470295,
12.1132341763298));
#121960=CARTESIAN_POINT('Ctrl Pts',(-10.3877253718202,10.6215823102871,
12.1121043017626));
#121961=CARTESIAN_POINT('Ctrl Pts',(-10.3944555622792,10.6210977307217,
12.1097357677851));
#121962=CARTESIAN_POINT('Ctrl Pts',(-10.3979288436736,10.6208482082355,
12.108495061437));
#121963=CARTESIAN_POINT('Ctrl Pts',(-10.4070213558203,10.6201963169081,
12.1051988409286));
#121964=CARTESIAN_POINT('Ctrl Pts',(-10.4126309382986,10.6197954624359,
12.1031167547413));
#121965=CARTESIAN_POINT('Ctrl Pts',(-10.4378768845288,10.6179963720566,
12.0935267894348));
#121966=CARTESIAN_POINT('Ctrl Pts',(-10.4573272872385,10.6166238660957,
12.0855362214911));
#121967=CARTESIAN_POINT('Ctrl Pts',(-10.5135890942475,10.6126647079295,
12.060641962421));
#121968=CARTESIAN_POINT('Ctrl Pts',(-10.549756490421,10.6101330615061,12.0423547473091));
#121969=CARTESIAN_POINT('Ctrl Pts',(-10.6694055598791,10.6015767872125,
11.973893085681));
#121970=CARTESIAN_POINT('Ctrl Pts',(-10.7475699967837,10.5956360590842,
11.9152642954634));
#121971=CARTESIAN_POINT('Ctrl Pts',(-10.8281670359103,10.588332451929,11.8375253964328));
#121972=CARTESIAN_POINT('Ctrl Pts',(-10.8385142832949,10.587369857886,11.8271657603227));
#121973=CARTESIAN_POINT('Ctrl Pts',(-10.8538982195933,10.5858984230248,
11.8111780631434));
#121974=CARTESIAN_POINT('Ctrl Pts',(-10.8590785766533,10.5853957396488,
11.8056897754421));
#121975=CARTESIAN_POINT('Ctrl Pts',(-10.8683098558573,10.5844866465242,
11.7957195166096));
#121976=CARTESIAN_POINT('Ctrl Pts',(-10.872379750164,10.5840810546809,11.7912554101402));
#121977=CARTESIAN_POINT('Ctrl Pts',(-10.8810112988154,10.583210408159,11.7816402585063));
#121978=CARTESIAN_POINT('Ctrl Pts',(-10.885562498689,10.5827449418544,11.7764801734794));
#121979=CARTESIAN_POINT('Ctrl Pts',(-10.8970210576773,10.5815564274281,
11.7632568429367));
#121980=CARTESIAN_POINT('Ctrl Pts',(-10.9038649516957,10.5808308452378,
11.7551396708653));
#121981=CARTESIAN_POINT('Ctrl Pts',(-10.9399341336241,10.5769202644692,
11.7111670539386));
#121982=CARTESIAN_POINT('Ctrl Pts',(-10.9671340813768,10.5736570979384,
11.6737102112708));
#121983=CARTESIAN_POINT('Ctrl Pts',(-11.0230820954715,10.5661896681983,
11.5862690988688));
#121984=CARTESIAN_POINT('Ctrl Pts',(-11.0505072397248,10.5619584967098,
11.5355764471843));
#121985=CARTESIAN_POINT('Ctrl Pts',(-11.096154081084,10.5537977302198,11.4340833091441));
#121986=CARTESIAN_POINT('Ctrl Pts',(-11.1148163967447,10.5498772141991,
11.3836243613011));
#121987=CARTESIAN_POINT('Ctrl Pts',(-11.1329455086723,10.5453638767865,
11.3219332329409));
#121988=CARTESIAN_POINT('Ctrl Pts',(-11.1357860654532,10.5446288134673,
11.3117636362784));
#121989=CARTESIAN_POINT('Ctrl Pts',(-11.139552127202,10.5436147947911,11.2975453453061));
#121990=CARTESIAN_POINT('Ctrl Pts',(-11.1405934667704,10.5433298157008,
11.2935282405269));
#121991=CARTESIAN_POINT('Ctrl Pts',(-11.1424570178325,10.5428113598447,
11.2861796611299));
#121992=CARTESIAN_POINT('Ctrl Pts',(-11.1432859438448,10.5425775131625,
11.2828499387873));
#121993=CARTESIAN_POINT('Ctrl Pts',(-11.1449827410332,10.542092036483,11.2759047103736));
#121994=CARTESIAN_POINT('Ctrl Pts',(-11.1458480588564,10.5418405493249,
11.2722886583205));
#121995=CARTESIAN_POINT('Ctrl Pts',(-11.147581113616,10.5413286144644,11.2648918576034));
#121996=CARTESIAN_POINT('Ctrl Pts',(-11.1484473265979,10.5410682527546,
11.2611107956759));
#121997=CARTESIAN_POINT('Ctrl Pts',(-11.1505613326278,10.5404212435453,
11.2516689927708));
#121998=CARTESIAN_POINT('Ctrl Pts',(-11.1517860611162,10.5400357985367,
11.2460031192622));
#121999=CARTESIAN_POINT('Ctrl Pts',(-11.1551432723351,10.5389474879925,
11.2298969834078));
#122000=CARTESIAN_POINT('Ctrl Pts',(-11.1571760272035,10.5382494113297,
11.2194362368922));
#122001=CARTESIAN_POINT('Ctrl Pts',(-11.1714346956862,10.5330273145064,
11.140341574944));
#122002=CARTESIAN_POINT('Ctrl Pts',(-11.1776876846325,10.5287459337407,
11.0707736257504));
#122003=CARTESIAN_POINT('Ctrl Pts',(-11.1777495366547,10.5244313734309,
11.001044705558));
#122004=CARTESIAN_POINT('Ctrl Pts',(-11.1777495366547,10.524431373431,11.0010447055599));
#122005=CARTESIAN_POINT('Ctrl Pts',(-11.1778014625253,10.5208092234631,
10.9425060392978));
#122006=CARTESIAN_POINT('Ctrl Pts',(-11.1734900406971,10.5171760859007,
10.8840597268698));
#122007=CARTESIAN_POINT('Ctrl Pts',(-11.1614407031938,10.5119409805812,
10.8033164228629));
#122008=CARTESIAN_POINT('Ctrl Pts',(-11.1573588302156,10.5104425498072,
10.7805703663003));
#122009=CARTESIAN_POINT('Ctrl Pts',(-11.150974721311,10.5084003519483,10.7501687844275));
#122010=CARTESIAN_POINT('Ctrl Pts',(-11.149259657729,10.5078746211142,10.7423943334408));
#122011=CARTESIAN_POINT('Ctrl Pts',(-11.1457910342312,10.5068532469504,
10.7273954729512));
#122012=CARTESIAN_POINT('Ctrl Pts',(-11.1440476297423,10.5063579412863,
10.7201690886765));
#122013=CARTESIAN_POINT('Ctrl Pts',(-11.1407656902538,10.5054567320525,
10.7071090723435));
#122014=CARTESIAN_POINT('Ctrl Pts',(-11.1392505067385,10.505051583652,10.7012697937131));
#122015=CARTESIAN_POINT('Ctrl Pts',(-11.1358902237492,10.5041757601692,
10.6887172797469));
#122016=CARTESIAN_POINT('Ctrl Pts',(-11.1340303318796,10.5037046253151,
10.6820082782195));
#122017=CARTESIAN_POINT('Ctrl Pts',(-11.1288157203648,10.5024193294463,
10.6638259078731));
#122018=CARTESIAN_POINT('Ctrl Pts',(-11.1253457076169,10.5016015038199,
10.652386751018));
#122019=CARTESIAN_POINT('Ctrl Pts',(-11.1043786990478,10.4968630574732,
10.586874434735));
#122020=CARTESIAN_POINT('Ctrl Pts',(-11.0831625836609,10.4928229155626,
10.5340792737668));
#122021=CARTESIAN_POINT('Ctrl Pts',(-11.0278595206646,10.4836838374943,
10.4208759623487));
#122022=CARTESIAN_POINT('Ctrl Pts',(-10.9920816027849,10.4785602159411,
10.3615225610974));
#122023=CARTESIAN_POINT('Ctrl Pts',(-10.9309621471302,10.471036847189,10.2777846963343));
#122024=CARTESIAN_POINT('Ctrl Pts',(-10.9094043283811,10.4685644605243,
10.2508206447563));
#122025=CARTESIAN_POINT('Ctrl Pts',(-10.8818106844505,10.4656432975802,
10.2192567823819));
#122026=CARTESIAN_POINT('Ctrl Pts',(-10.8768771136236,10.4651298141408,
10.2137197766276));
#122027=CARTESIAN_POINT('Ctrl Pts',(-10.8691372000435,10.4643382643406,
10.2051966442339));
#122028=CARTESIAN_POINT('Ctrl Pts',(-10.8663671232169,10.4640576992096,
10.2021780550008));
#122029=CARTESIAN_POINT('Ctrl Pts',(-10.8612788985222,10.4635473943146,
10.1966911011804));
#122030=CARTESIAN_POINT('Ctrl Pts',(-10.8589658351801,10.463317302713,10.194218253757));
#122031=CARTESIAN_POINT('Ctrl Pts',(-10.8537098982712,10.4627986961576,
10.1886475935271));
#122032=CARTESIAN_POINT('Ctrl Pts',(-10.8507608068258,10.4625106563633,
10.1855557914169));
#122033=CARTESIAN_POINT('Ctrl Pts',(-10.8430610771185,10.4617660111174,
10.177570920186));
#122034=CARTESIAN_POINT('Ctrl Pts',(-10.8382845706704,10.4613112854978,
10.172702861725));
#122035=CARTESIAN_POINT('Ctrl Pts',(-10.8003082299016,10.457749557439,10.1346652593722));
#122036=CARTESIAN_POINT('Ctrl Pts',(-10.7651908179347,10.4547746531926,
10.103461333031));
#122037=CARTESIAN_POINT('Ctrl Pts',(-10.6664374598311,10.4469257599335,
10.0257552737279));
#122038=CARTESIAN_POINT('Ctrl Pts',(-10.5998516165015,10.4421380705178,
9.98340285229885));
#122039=CARTESIAN_POINT('Ctrl Pts',(-10.4971142958291,10.4348584924731,
9.93168818361229));
#122040=CARTESIAN_POINT('Ctrl Pts',(-10.4639558608616,10.43252635496,9.91687612547961));
#122041=CARTESIAN_POINT('Ctrl Pts',(-10.4196031719364,10.4293978659463,
9.89947419113913));
#122042=CARTESIAN_POINT('Ctrl Pts',(-10.4089785677588,10.4286478604088,
9.89548182706895));
#122043=CARTESIAN_POINT('Ctrl Pts',(-10.3919338614074,10.4274429094518,
9.88935665192368));
#122044=CARTESIAN_POINT('Ctrl Pts',(-10.3855500367186,10.4269912307043,
9.88712446144455));
#122045=CARTESIAN_POINT('Ctrl Pts',(-10.3734107658169,10.4261314367687,
9.88299678738927));
#122046=CARTESIAN_POINT('Ctrl Pts',(-10.3676592054947,10.4257236899488,
9.88109049370623));
#122047=CARTESIAN_POINT('Ctrl Pts',(-10.3545321260789,10.4247920822244,
9.87685180393833));
#122048=CARTESIAN_POINT('Ctrl Pts',(-10.3471478878776,10.4242673295688,
9.8745475408788));
#122049=CARTESIAN_POINT('Ctrl Pts',(-10.3243150668196,10.4226422787787,
9.86766860884956));
#122050=CARTESIAN_POINT('Ctrl Pts',(-10.3087954522306,10.4215342388315,
9.86333823581042));
#122051=CARTESIAN_POINT('Ctrl Pts',(-10.2171369372544,10.4149666843821,
9.83977880192476));
#122052=CARTESIAN_POINT('Ctrl Pts',(-10.1393298372915,10.4092775572933,
9.82788871955721));
#122053=CARTESIAN_POINT('Ctrl Pts',(-10.0079361810192,10.3996280394529,
9.82108174312774));
#122054=CARTESIAN_POINT('Ctrl Pts',(-9.95481241391698,10.3957208987762,
9.82192113401668));
#122055=CARTESIAN_POINT('Ctrl Pts',(-9.88545199811531,10.3907234091425,
9.82771716130987));
#122056=CARTESIAN_POINT('Ctrl Pts',(-9.86900947669093,10.3895467188059,
9.82944037382131));
#122057=CARTESIAN_POINT('Ctrl Pts',(-9.84132069371484,10.3875842958606,
9.83293300639602));
#122058=CARTESIAN_POINT('Ctrl Pts',(-9.8300542156052,10.3867911682803,9.83452029446056));
#122059=CARTESIAN_POINT('Ctrl Pts',(-9.81625646134559,10.3858278533388,
9.8366685495508));
#122060=CARTESIAN_POINT('Ctrl Pts',(-9.81370221395765,10.3856498620175,
9.83707485762302));
#122061=CARTESIAN_POINT('Ctrl Pts',(-9.81114930150037,10.385472315614,9.83748958018597));
#122062=CARTESIAN_POINT('Ctrl Pts',(-9.81114930150156,10.287171250943,9.83748958018577));
#122063=CARTESIAN_POINT('Ctrl Pts',(-9.8822558631217,10.292359777568,9.82593826537525));
#122064=CARTESIAN_POINT('Ctrl Pts',(-9.95430619677359,10.2976918666623,
9.82092997109078));
#122065=CARTESIAN_POINT('Ctrl Pts',(-10.0656605648505,10.3058135681201,
9.82342593242662));
#122066=CARTESIAN_POINT('Ctrl Pts',(-10.1048644736454,10.3086470262399,
9.82627009030703));
#122067=CARTESIAN_POINT('Ctrl Pts',(-10.1531977265903,10.3120561606732,
9.83221829899421));
#122068=CARTESIAN_POINT('Ctrl Pts',(-10.1625253172695,10.3127101124164,
9.8334798845329));
#122069=CARTESIAN_POINT('Ctrl Pts',(-10.1761879738484,10.3136612222668,
9.83549486825425));
#122070=CARTESIAN_POINT('Ctrl Pts',(-10.1805352679866,10.3139628446267,
9.83616091208098));
#122071=CARTESIAN_POINT('Ctrl Pts',(-10.1882297125398,10.3144947882491,
9.83738391977375));
#122072=CARTESIAN_POINT('Ctrl Pts',(-10.1915783048973,10.3147256393405,
9.83793101375094));
#122073=CARTESIAN_POINT('Ctrl Pts',(-10.1988658090097,10.3152266079621,
9.83915400550776));
#122074=CARTESIAN_POINT('Ctrl Pts',(-10.2028036771766,10.3154964142574,
9.83983548467139));
#122075=CARTESIAN_POINT('Ctrl Pts',(-10.2138236043379,10.3162491340243,
9.84180039301222));
#122076=CARTESIAN_POINT('Ctrl Pts',(-10.2208976233688,10.3167296388762,
9.84312874107009));
#122077=CARTESIAN_POINT('Ctrl Pts',(-10.2639683208791,10.3196412690377,
9.85162597113228));
#122078=CARTESIAN_POINT('Ctrl Pts',(-10.2996296432167,10.3219926312374,
9.8604102313947));
#122079=CARTESIAN_POINT('Ctrl Pts',(-10.441995630875,10.331348659916,9.90262578346285));
#122080=CARTESIAN_POINT('Ctrl Pts',(-10.5440916072857,10.3380446635281,
9.94949733627392));
#122081=CARTESIAN_POINT('Ctrl Pts',(-10.655052839223,10.3465801570331,10.0210158899088));
#122082=CARTESIAN_POINT('Ctrl Pts',(-10.6717666783701,10.3479016175868,
10.0324083703543));
#122083=CARTESIAN_POINT('Ctrl Pts',(-10.695037332062,10.3497978935837,10.0491637318292));
#122084=CARTESIAN_POINT('Ctrl Pts',(-10.7018429804912,10.3503595359576,
10.0541760595204));
#122085=CARTESIAN_POINT('Ctrl Pts',(-10.7135165484209,10.3513355529462,
10.0629689557677));
#122086=CARTESIAN_POINT('Ctrl Pts',(-10.7184098905328,10.351748600042,10.0667153331077));
#122087=CARTESIAN_POINT('Ctrl Pts',(-10.7277602072342,10.3525455621152,
10.0739911111412));
#122088=CARTESIAN_POINT('Ctrl Pts',(-10.7322214817457,10.3529292429321,
10.0775147257552));
#122089=CARTESIAN_POINT('Ctrl Pts',(-10.7427099497199,10.3538395357452,
10.0859227733466));
#122090=CARTESIAN_POINT('Ctrl Pts',(-10.7487146751093,10.3543672275123,
10.0908346817073));
#122091=CARTESIAN_POINT('Ctrl Pts',(-10.7698230334699,10.3562459062084,
10.1084524073393));
#122092=CARTESIAN_POINT('Ctrl Pts',(-10.7846546037202,10.3576096319008,
10.1214775560349));
#122093=CARTESIAN_POINT('Ctrl Pts',(-10.8839942794638,10.3670548098794,
10.2132409732851));
#122094=CARTESIAN_POINT('Ctrl Pts',(-10.956837739388,10.3756609084894,10.3036616795177));
#122095=CARTESIAN_POINT('Ctrl Pts',(-11.0324911879688,10.3864797851252,
10.4323714859524));
#122096=CARTESIAN_POINT('Ctrl Pts',(-11.048375278236,10.3888997911129,10.4622733747698));
#122097=CARTESIAN_POINT('Ctrl Pts',(-11.0659054601722,10.3917299785873,
10.4990132830507));
#122098=CARTESIAN_POINT('Ctrl Pts',(-11.0688061076328,10.3922041977594,
10.5052317204052));
#122099=CARTESIAN_POINT('Ctrl Pts',(-11.0732618410511,10.3929416986472,
10.515006041832));
#122100=CARTESIAN_POINT('Ctrl Pts',(-11.0748539238431,10.3932070986589,
10.5185447451649));
#122101=CARTESIAN_POINT('Ctrl Pts',(-11.0778133172067,10.3937039194524,
10.5252104022605));
#122102=CARTESIAN_POINT('Ctrl Pts',(-11.0791845221947,10.3939355575783,
10.5283354197459));
#122103=CARTESIAN_POINT('Ctrl Pts',(-11.0823335246481,10.3944709595313,
10.5355977174437));
#122104=CARTESIAN_POINT('Ctrl Pts',(-11.0841012021118,10.39477412062,10.5397392870799));
#122105=CARTESIAN_POINT('Ctrl Pts',(-11.0898158919151,10.3957632164203,
10.5533440783053));
#122106=CARTESIAN_POINT('Ctrl Pts',(-11.093663216687,10.3964435624502,10.5628490231141));
#122107=CARTESIAN_POINT('Ctrl Pts',(-11.1238760031118,10.401916838432,10.6403872692997));
#122108=CARTESIAN_POINT('Ctrl Pts',(-11.1439949601166,10.406409666529,10.7106955278433));
#122109=CARTESIAN_POINT('Ctrl Pts',(-11.167820599171,10.4143875245765,10.8374438994735));
#122110=CARTESIAN_POINT('Ctrl Pts',(-11.1742264520675,10.4178526365535,
10.8931305790753));
#122111=CARTESIAN_POINT('Ctrl Pts',(-11.1775585844599,10.422760974927,10.9700959178083));
#122112=CARTESIAN_POINT('Ctrl Pts',(-11.1779049748196,10.4241155330458,
10.9911531855618));
#122113=CARTESIAN_POINT('Ctrl Pts',(-11.1775216859798,10.4265228001002,
11.0281298659052));
#122114=CARTESIAN_POINT('Ctrl Pts',(-11.1770337598879,10.4275683225547,
11.0440465569254));
#122115=CARTESIAN_POINT('Ctrl Pts',(-11.1758314714931,10.4291339897832,
11.067636379727));
#122116=CARTESIAN_POINT('Ctrl Pts',(-11.1753642482087,10.4296465384176,
11.075320704655));
#122117=CARTESIAN_POINT('Ctrl Pts',(-11.1743951046497,10.4305663065676,
11.0890384683117));
#122118=CARTESIAN_POINT('Ctrl Pts',(-11.1739219299493,10.4309726236499,
11.0950737120102));
#122119=CARTESIAN_POINT('Ctrl Pts',(-11.1728201305206,10.4318371538744,
11.1078609593253));
#122120=CARTESIAN_POINT('Ctrl Pts',(-11.1721796795132,10.4322957193756,
11.1146116953859));
#122121=CARTESIAN_POINT('Ctrl Pts',(-11.1703022486991,10.4335327869764,
11.1327349621216));
#122122=CARTESIAN_POINT('Ctrl Pts',(-11.1689578388091,10.4343145848187,
11.1440953801079));
#122123=CARTESIAN_POINT('Ctrl Pts',(-11.1615402081611,10.4381810954351,
11.1998083865065));
#122124=CARTESIAN_POINT('Ctrl Pts',(-11.1531078234111,10.4413378830274,
11.2438042452301));
#122125=CARTESIAN_POINT('Ctrl Pts',(-11.1208717102869,10.4508392694634,
11.3720031245035));
#122126=CARTESIAN_POINT('Ctrl Pts',(-11.0901766388471,10.4573447157126,
11.4541504932501));
#122127=CARTESIAN_POINT('Ctrl Pts',(-11.0412388012425,10.4651745503363,
11.5507750310746));
#122128=CARTESIAN_POINT('Ctrl Pts',(-11.0313063147132,10.4666711852939,
11.5691561860265));
#122129=CARTESIAN_POINT('Ctrl Pts',(-11.0141567372982,10.4690999003144,
11.5989686936526));
#122130=CARTESIAN_POINT('Ctrl Pts',(-11.0072227350167,10.4700442738613,
11.6105569462091));
#122131=CARTESIAN_POINT('Ctrl Pts',(-10.997411347687,10.4713276728443,11.6263317020142));
#122132=CARTESIAN_POINT('Ctrl Pts',(-10.9947042170087,10.4716765118662,
11.6306221693421));
#122133=CARTESIAN_POINT('Ctrl Pts',(-10.9900860704306,10.472262615208,11.6378376289855));
#122134=CARTESIAN_POINT('Ctrl Pts',(-10.9881896276822,10.4725007992281,
11.6407718227033));
#122135=CARTESIAN_POINT('Ctrl Pts',(-10.9845178957631,10.4729571170824,
11.6463976881193));
#122136=CARTESIAN_POINT('Ctrl Pts',(-10.9827445797068,10.4731753820059,
11.6490905560654));
#122137=CARTESIAN_POINT('Ctrl Pts',(-10.9779217700138,10.4737633902271,
11.6563491591512));
#122138=CARTESIAN_POINT('Ctrl Pts',(-10.9748513254613,10.4741317785629,
11.6609009783329));
#122139=CARTESIAN_POINT('Ctrl Pts',(-10.9631138726958,10.4755183581334,
11.6780415299478));
#122140=CARTESIAN_POINT('Ctrl Pts',(-10.9542335140878,10.4765235096128,
11.6904832382428));
#122141=CARTESIAN_POINT('Ctrl Pts',(-10.8745257732511,10.4852058857344,
11.797680535715));
#122142=CARTESIAN_POINT('Ctrl Pts',(-10.7900328601207,10.4922062853714,
11.8814448889436));
#122143=CARTESIAN_POINT('Ctrl Pts',(-10.6759144941456,10.5011795155759,
11.9647601165845));
#122144=CARTESIAN_POINT('Ctrl Pts',(-10.6569749062222,10.5026526648774,
11.9777557773459));
#122145=CARTESIAN_POINT('Ctrl Pts',(-10.6233635567393,10.5052504532086,
11.9994010354373));
#122146=CARTESIAN_POINT('Ctrl Pts',(-10.6088614147608,10.5063661556958,
12.0083016828432));
#122147=CARTESIAN_POINT('Ctrl Pts',(-10.5873498777719,10.5080165017209,
12.0208710091174));
#122148=CARTESIAN_POINT('Ctrl Pts',(-10.5804878206124,10.508542274165,12.0247884568163));
#122149=CARTESIAN_POINT('Ctrl Pts',(-10.5682785916075,10.5094768281883,
12.0315965519764));
#122150=CARTESIAN_POINT('Ctrl Pts',(-10.5629474338271,10.5098845945755,
12.0345154363843));
#122151=CARTESIAN_POINT('Ctrl Pts',(-10.5517175285242,10.5107430270575,
12.0405514599651));
#122152=CARTESIAN_POINT('Ctrl Pts',(-10.5458144255501,10.51119397629,12.0436599933981));
#122153=CARTESIAN_POINT('Ctrl Pts',(-10.5301678785782,10.5123886520457,
12.0517303046131));
#122154=CARTESIAN_POINT('Ctrl Pts',(-10.5203813924906,10.5131352922613,
12.0566067411761));
#122155=CARTESIAN_POINT('Ctrl Pts',(-10.4768731673793,10.5164530272218,
12.0775350684553));
#122156=CARTESIAN_POINT('Ctrl Pts',(-10.442470186839,10.5190731147247,12.0921123798651));
#122157=CARTESIAN_POINT('Ctrl Pts',(-10.3350675051766,10.5272445997452,
12.1317128675599));
#122158=CARTESIAN_POINT('Ctrl Pts',(-10.2602579016275,10.5329387616071,
12.1512201603543));
#122159=CARTESIAN_POINT('Ctrl Pts',(-10.151365695603,10.5410002008411,12.1684524512969));
#122160=CARTESIAN_POINT('Ctrl Pts',(-10.1184360468283,10.5434064844935,
12.1722482226635));
#122161=CARTESIAN_POINT('Ctrl Pts',(-10.0729260691632,10.5466561430441,
12.1755564540803));
#122162=CARTESIAN_POINT('Ctrl Pts',(-10.0604497383667,10.5475391541488,
12.1762640199792));
#122163=CARTESIAN_POINT('Ctrl Pts',(-10.0387645628158,10.5490577455538,
12.1771478841248));
#122164=CARTESIAN_POINT('Ctrl Pts',(-10.0295607028759,10.5496972288833,
12.1774149694714));
#122165=CARTESIAN_POINT('Ctrl Pts',(-10.0159957339912,10.5506313826146,
12.1776494392883));
#122166=CARTESIAN_POINT('Ctrl Pts',(-10.0116366852185,10.5509303007438,
12.1777005792833));
#122167=CARTESIAN_POINT('Ctrl Pts',(-10.0038874455616,10.5514593265673,
12.177748463072));
#122168=CARTESIAN_POINT('Ctrl Pts',(-10.0004974442092,10.5516899416526,
12.1777547741499));
#122169=CARTESIAN_POINT('Ctrl Pts',(-9.99308262972192,10.5521925649602,
12.1777365625432));
#122170=CARTESIAN_POINT('Ctrl Pts',(-9.98905793755075,10.5524642444608,
12.1777060470415));
#122171=CARTESIAN_POINT('Ctrl Pts',(-9.97770945961987,10.5532272880305,
12.1775618213777));
#122172=CARTESIAN_POINT('Ctrl Pts',(-9.97038631254256,10.5537161375682,
12.1774004193765));
#122173=CARTESIAN_POINT('Ctrl Pts',(-9.92330816030469,10.5568387602093,
12.1759232884624));
#122174=CARTESIAN_POINT('Ctrl Pts',(-9.8836354588537,10.5593786414759,12.1726624518815));
#122175=CARTESIAN_POINT('Ctrl Pts',(-9.82253681388627,10.5632508353322,
12.1645082756874));
#122176=CARTESIAN_POINT('Ctrl Pts',(-9.80095791407728,10.5646106390706,
12.1610146440701));
#122177=CARTESIAN_POINT('Ctrl Pts',(-9.73363879272821,10.5688600877953,
12.1481834829735));
#122178=CARTESIAN_POINT('Ctrl Pts',(-9.6883501272944,10.571731118984,12.1367268285679));
#122179=CARTESIAN_POINT('Ctrl Pts',(-9.59294936299341,10.5779851341149,
12.1064618020151));
#122180=CARTESIAN_POINT('Ctrl Pts',(-9.54320120686809,10.5813760060638,
12.0868678553168));
#122181=CARTESIAN_POINT('Ctrl Pts',(-9.48448844479286,10.5856414004614,
12.0589982103215));
#122182=CARTESIAN_POINT('Ctrl Pts',(-9.4740930775466,10.5864069409019,12.0538744073007));
#122183=CARTESIAN_POINT('Ctrl Pts',(-9.45770904950382,10.5876308949159,
12.0454960593669));
#122184=CARTESIAN_POINT('Ctrl Pts',(-9.45166993447215,10.5880858543134,
12.0423414129229));
#122185=CARTESIAN_POINT('Ctrl Pts',(-9.44032220527155,10.5889481451443,
12.0362878028507));
#122186=CARTESIAN_POINT('Ctrl Pts',(-9.43500786965713,10.5893550760111,
12.0333999876922));
#122187=CARTESIAN_POINT('Ctrl Pts',(-9.42302716809412,10.5902796514208,
12.0267696230198));
#122188=CARTESIAN_POINT('Ctrl Pts',(-9.4163745813716,10.5907981385546,12.0230028707085));
#122189=CARTESIAN_POINT('Ctrl Pts',(-9.39622287864518,10.5923845968865,
12.0113322603697));
#122190=CARTESIAN_POINT('Ctrl Pts',(-9.38284460710379,10.5934597885788,
12.0032242687634));
#122191=CARTESIAN_POINT('Ctrl Pts',(-9.29597862485375,10.6005905617704,
11.9481834421076));
#122192=CARTESIAN_POINT('Ctrl Pts',(-9.22774829709035,10.6069368624258,
11.8934874740305));
#122193=CARTESIAN_POINT('Ctrl Pts',(-9.11877638770217,10.6182605058637,
11.7842493365551));
#122194=CARTESIAN_POINT('Ctrl Pts',(-9.0755086792396,10.6231879643457,11.7327481310584));
#122195=CARTESIAN_POINT('Ctrl Pts',(-9.03237766019328,10.6284123542835,
11.6714631679281));
#122196=CARTESIAN_POINT('Ctrl Pts',(-9.02795627252195,10.6289520339248,
11.6650464482634));
#122197=CARTESIAN_POINT('Ctrl Pts',(-9.02131839222845,10.6297680712681,
11.6552053135649));
#122198=CARTESIAN_POINT('Ctrl Pts',(-9.01905556464106,10.6300473148976,
11.6518126328265));
#122199=CARTESIAN_POINT('Ctrl Pts',(-9.01494619491756,10.6305562865526,
11.6455815430454));
#122200=CARTESIAN_POINT('Ctrl Pts',(-9.01309425486463,10.6307863554798,
11.6427469007652));
#122201=CARTESIAN_POINT('Ctrl Pts',(-9.00892242291732,10.6313062409033,
11.6363008106253));
#122202=CARTESIAN_POINT('Ctrl Pts',(-9.00661002683278,10.6315955705008,
11.6326846355474));
#122203=CARTESIAN_POINT('Ctrl Pts',(-9.00063882496331,10.6323459737338,
11.6232332935644));
#122204=CARTESIAN_POINT('Ctrl Pts',(-8.99701128075046,10.6328051185808,
11.6173784341347));
#122205=CARTESIAN_POINT('Ctrl Pts',(-8.96460145395669,10.6369405581506,
11.5640292570794));
#122206=CARTESIAN_POINT('Ctrl Pts',(-8.93915674306324,10.6404309797261,
11.5145798361444));
#122207=CARTESIAN_POINT('Ctrl Pts',(-8.89925486206284,10.6467321821857,
11.4213743181669));
#122208=CARTESIAN_POINT('Ctrl Pts',(-8.8836904635516,10.6495496716591,11.3782184703491));
#122209=CARTESIAN_POINT('Ctrl Pts',(-8.85379889377512,10.6561070903127,
11.2772294633044));
#122210=CARTESIAN_POINT('Ctrl Pts',(-8.84126401347867,10.6598651851965,
11.2190038811722));
#122211=CARTESIAN_POINT('Ctrl Pts',(-8.83156835102912,10.6645439927616,
11.1483348257683));
#122212=CARTESIAN_POINT('Ctrl Pts',(-8.83013383291588,10.6653271303463,
11.1365608776609));
#122213=CARTESIAN_POINT('Ctrl Pts',(-8.82814942484362,10.6665726972816,
11.1179343681861));
#122214=CARTESIAN_POINT('Ctrl Pts',(-8.82748126609069,10.6670314554784,
11.1110950086928));
#122215=CARTESIAN_POINT('Ctrl Pts',(-8.82633837094896,10.6678969397748,
11.0982340292899));
#122216=CARTESIAN_POINT('Ctrl Pts',(-8.82585002949443,10.6683032299063,
11.0922138192027));
#122217=CARTESIAN_POINT('Ctrl Pts',(-8.82485517237363,10.6692209458802,
11.0786560016849));
#122218=CARTESIAN_POINT('Ctrl Pts',(-8.82437483500912,10.6697331644927,
11.0711168006841));
#122219=CARTESIAN_POINT('Ctrl Pts',(-8.82317449755367,10.671247616402,11.0489120604837));
#122220=CARTESIAN_POINT('Ctrl Pts',(-8.82265620555464,10.6722559954407,
11.0342375355609));
#122221=CARTESIAN_POINT('Ctrl Pts',(-8.82082804806691,10.6798795027076,
10.9241625131865));
#122222=CARTESIAN_POINT('Ctrl Pts',(-8.83084171807125,10.6868523262554,
10.8289451005862));
#122223=CARTESIAN_POINT('Ctrl Pts',(-8.86160456831754,10.6969196260929,
10.6951988981057));
#122224=CARTESIAN_POINT('Ctrl Pts',(-8.87315872536738,10.6999815748667,
10.6549245923035));
#122225=CARTESIAN_POINT('Ctrl Pts',(-8.89385403063312,10.7045132595249,
10.5950331161816));
#122226=CARTESIAN_POINT('Ctrl Pts',(-8.90142954844151,10.7060316547431,
10.5749115550463));
#122227=CARTESIAN_POINT('Ctrl Pts',(-8.91181951610866,10.707938130686,10.5494511036793));
#122228=CARTESIAN_POINT('Ctrl Pts',(-8.91412935227894,10.7083519622754,
10.5439122740749));
#122229=CARTESIAN_POINT('Ctrl Pts',(-8.91792828598864,10.7090164424341,
10.5349951672435));
#122230=CARTESIAN_POINT('Ctrl Pts',(-8.9193910715358,10.709268588812,10.5316058994573));
#122231=CARTESIAN_POINT('Ctrl Pts',(-8.92224906389396,10.7097540569526,
10.5250685964608));
#122232=CARTESIAN_POINT('Ctrl Pts',(-8.92364216928187,10.7099874916057,
10.5219197358682));
#122233=CARTESIAN_POINT('Ctrl Pts',(-8.9270871418914,10.7105570805657,10.5142243920073));
#122234=CARTESIAN_POINT('Ctrl Pts',(-8.92915415204224,10.7108923359316,
10.5096846784443));
#122235=CARTESIAN_POINT('Ctrl Pts',(-8.93630399369179,10.7120305775245,
10.4942425870194));
#122236=CARTESIAN_POINT('Ctrl Pts',(-8.94152517004917,10.7128257778488,
10.4834045912768));
#122237=CARTESIAN_POINT('Ctrl Pts',(-8.98223900118111,10.7187773744916,
10.4021016714969));
#122238=CARTESIAN_POINT('Ctrl Pts',(-9.0245704751313,10.7236001869118,10.3352741847902));
#122239=CARTESIAN_POINT('Ctrl Pts',(-9.1132685123151,10.7324999027994,10.2221809461214));
#122240=CARTESIAN_POINT('Ctrl Pts',(-9.15740015321717,10.7365403265275,
10.1745792647244));
#122241=CARTESIAN_POINT('Ctrl Pts',(-9.21867823586108,10.7419254490531,
10.1185444088313));
#122242=CARTESIAN_POINT('Ctrl Pts',(-9.2324202294947,10.7431196426774,10.10655224203));
#122243=CARTESIAN_POINT('Ctrl Pts',(-9.2526742612774,10.7448642044167,10.0896894899659));
#122244=CARTESIAN_POINT('Ctrl Pts',(-9.25896741171793,10.7454041602719,
10.0845592962692));
#122245=CARTESIAN_POINT('Ctrl Pts',(-9.27008738376275,10.7463549107081,
10.0756840632185));
#122246=CARTESIAN_POINT('Ctrl Pts',(-9.27489129054688,10.7467645679853,
10.0719107071985));
#122247=CARTESIAN_POINT('Ctrl Pts',(-9.2842910225191,10.7475641829805,10.0646449667689));
#122248=CARTESIAN_POINT('Ctrl Pts',(-9.28888360357225,10.7479539717054,
10.0611486553634));
#122249=CARTESIAN_POINT('Ctrl Pts',(-9.30128566488355,10.7490043161214,
10.0518502273855));
#122250=CARTESIAN_POINT('Ctrl Pts',(-9.30914150517322,10.7496672585339,
10.0461109898473));
#122251=CARTESIAN_POINT('Ctrl Pts',(-9.33921292896529,10.7521966381418,
10.0247080585079));
#122252=CARTESIAN_POINT('Ctrl Pts',(-9.36189582820236,10.754087879968,10.0097188369469));
#122253=CARTESIAN_POINT('Ctrl Pts',(-9.45786738299857,10.7620274195192,
9.95096626927944));
#122254=CARTESIAN_POINT('Ctrl Pts',(-9.53527964146946,10.7683110628135,
9.91445376356915));
#122255=CARTESIAN_POINT('Ctrl Pts',(-9.66159725545541,10.7780965895773,
9.87088038894103));
#122256=CARTESIAN_POINT('Ctrl Pts',(-9.70818308542766,10.7816070953586,
9.85795300187527));
#122257=CARTESIAN_POINT('Ctrl Pts',(-9.76558789828214,10.7857245918511,
9.84576703056778));
#122258=CARTESIAN_POINT('Ctrl Pts',(-9.77576890968408,10.7864469620291,
9.84374604101449));
#122259=CARTESIAN_POINT('Ctrl Pts',(-9.79047333763238,10.7874776997161,
9.84102866319185));
#122260=CARTESIAN_POINT('Ctrl Pts',(-9.79497584213038,10.7877916203952,
9.84022369474705));
#122261=CARTESIAN_POINT('Ctrl Pts',(-9.80284477362347,10.788337169576,9.83886412595221));
#122262=CARTESIAN_POINT('Ctrl Pts',(-9.80620908263723,10.788569429329,9.83829789411524));
#122263=CARTESIAN_POINT('Ctrl Pts',(-9.81010032997558,10.7888369096174,
9.83766035075839));
#122264=CARTESIAN_POINT('Ctrl Pts',(-9.81062478641594,10.788872936198,9.83757478805884));
#122265=CARTESIAN_POINT('Ctrl Pts',(-9.81114930150155,10.7889089429636,
9.83748958018577));
#122266=CARTESIAN_POINT('Origin',(-10.,2.67563288526385,11.));
#122267=CARTESIAN_POINT('',(-9.81114930150156,11.3870771460943,9.83748958018577));
#122268=CARTESIAN_POINT('',(-9.81114930150157,11.2872494929995,9.83748958018577));
#122269=CARTESIAN_POINT('',(-9.81114930150157,2.67563288526385,9.83748958018577));
#122270=CARTESIAN_POINT('Ctrl Pts',(-9.81114930150155,11.3870771460943,
9.83748958018577));
#122271=CARTESIAN_POINT('Ctrl Pts',(-9.79272746796521,11.3859061337436,
9.84048222100143));
#122272=CARTESIAN_POINT('Ctrl Pts',(-9.7743691874173,11.3847269668944,9.84391397489799));
#122273=CARTESIAN_POINT('Ctrl Pts',(-9.72569745290075,11.3815573166116,
9.85421717594312));
#122274=CARTESIAN_POINT('Ctrl Pts',(-9.69557359308454,11.3795499570249,
9.86185041831245));
#122275=CARTESIAN_POINT('Ctrl Pts',(-9.65599864501995,11.3768330240802,
9.87356208966352));
#122276=CARTESIAN_POINT('Ctrl Pts',(-9.64624710610495,11.376157038407,9.87658637297539));
#122277=CARTESIAN_POINT('Ctrl Pts',(-9.63033811278735,11.3750429059349,
9.88174796488936));
#122278=CARTESIAN_POINT('Ctrl Pts',(-9.62415676711958,11.3746071942134,
9.88381032691575));
#122279=CARTESIAN_POINT('Ctrl Pts',(-9.6121903838679,11.373758058577,9.88791349585017));
#122280=CARTESIAN_POINT('Ctrl Pts',(-9.60640353951357,11.3733448384497,
9.88994841789864));
#122281=CARTESIAN_POINT('Ctrl Pts',(-9.59284943961911,11.3723707621606,
9.89483397725119));
#122282=CARTESIAN_POINT('Ctrl Pts',(-9.58509588766303,11.3718087134616,
9.89772141081544));
#122283=CARTESIAN_POINT('Ctrl Pts',(-9.55951523736213,11.3699379487286,
9.90755581714999));
#122284=CARTESIAN_POINT('Ctrl Pts',(-9.54182781918716,11.3686177170514,
9.91485517215457));
#122285=CARTESIAN_POINT('Ctrl Pts',(-9.46398871692444,11.3626842815403,
9.94922062592171));
#122286=CARTESIAN_POINT('Ctrl Pts',(-9.40600385123646,11.3579218238942,
9.98087705193931));
#122287=CARTESIAN_POINT('Ctrl Pts',(-9.28416219350759,11.3472324609399,
10.0613397514326));
#122288=CARTESIAN_POINT('Ctrl Pts',(-9.22201389194342,11.3412985578297,
10.1121676349345));
#122289=CARTESIAN_POINT('Ctrl Pts',(-9.1586272881331,11.3350052465293,10.1758143939991));
#122290=CARTESIAN_POINT('Ctrl Pts',(-9.15183895734867,11.3343280044603,
10.1828018511508));
#122291=CARTESIAN_POINT('Ctrl Pts',(-9.14210276620221,11.3333529041161,
10.1930756742565));
#122292=CARTESIAN_POINT('Ctrl Pts',(-9.13908565519734,11.3330501961127,
10.196295437537));
#122293=CARTESIAN_POINT('Ctrl Pts',(-9.13377420425991,11.3325164583443,
10.2020278768188));
#122294=CARTESIAN_POINT('Ctrl Pts',(-9.13147256388948,11.3322848935339,
10.2045336384126));
#122295=CARTESIAN_POINT('Ctrl Pts',(-9.12653041968114,11.3317870959178,
10.2099611009863));
#122296=CARTESIAN_POINT('Ctrl Pts',(-9.12389368625927,11.3315211371819,
10.2128860960097));
#122297=CARTESIAN_POINT('Ctrl Pts',(-9.11652737105877,11.3307768789678,
10.221140611296));
#122298=CARTESIAN_POINT('Ctrl Pts',(-9.11183131522705,11.3303009559553,
10.2265000148463));
#122299=CARTESIAN_POINT('Ctrl Pts',(-9.08129755363035,11.3271942630137,
10.2619916120838));
#122300=CARTESIAN_POINT('Ctrl Pts',(-9.05694569003653,11.3246578082542,
10.2933743205045));
#122301=CARTESIAN_POINT('Ctrl Pts',(-9.00520173043543,11.3189755801465,
10.3675107705387));
#122302=CARTESIAN_POINT('Ctrl Pts',(-8.97889512240055,11.3158605820624,
10.4109232619296));
#122303=CARTESIAN_POINT('Ctrl Pts',(-8.92291456639828,11.308350612603,10.5183910309816));
#122304=CARTESIAN_POINT('Ctrl Pts',(-8.89603948827621,11.3039385307278,
10.583671384167));
#122305=CARTESIAN_POINT('Ctrl Pts',(-8.87154388323513,11.2985224291015,
10.6626118351759));
#122306=CARTESIAN_POINT('Ctrl Pts',(-8.86810875893508,11.2977173423505,
10.6743219664268));
#122307=CARTESIAN_POINT('Ctrl Pts',(-8.86298571508327,11.2964400837106,
10.6928472172144));
#122308=CARTESIAN_POINT('Ctrl Pts',(-8.86117564954436,11.2959718230462,
10.6996278786175));
#122309=CARTESIAN_POINT('Ctrl Pts',(-8.85792353649532,11.2950976932142,
10.7122626884846));
#122310=CARTESIAN_POINT('Ctrl Pts',(-8.8564656241279,11.2946923451227,10.7181125440605));
#122311=CARTESIAN_POINT('Ctrl Pts',(-8.85332711594917,11.2937887526367,
10.7311309429709));
#122312=CARTESIAN_POINT('Ctrl Pts',(-8.85166871262495,11.2932898220047,
10.7383045223447));
#122313=CARTESIAN_POINT('Ctrl Pts',(-8.84700850419926,11.2918221278411,
10.7593604398945));
#122314=CARTESIAN_POINT('Ctrl Pts',(-8.84419051911569,11.2908476412599,
10.7732816711453));
#122315=CARTESIAN_POINT('Ctrl Pts',(-8.82992302083362,11.2853847642603,
10.8509649057126));
#122316=CARTESIAN_POINT('Ctrl Pts',(-8.82349952669627,11.280742163358,10.9155263878737));
#122317=CARTESIAN_POINT('Ctrl Pts',(-8.82128489779045,11.2710903312503,
11.0477676259102));
#122318=CARTESIAN_POINT('Ctrl Pts',(-8.82595839374699,11.2660917158784,
11.1152283383518));
#122319=CARTESIAN_POINT('Ctrl Pts',(-8.84044223454589,11.2593432209551,
11.2078724492724));
#122320=CARTESIAN_POINT('Ctrl Pts',(-8.84536754271233,11.2574768950459,
11.2336863150586));
#122321=CARTESIAN_POINT('Ctrl Pts',(-8.85261869556331,11.2551886982754,
11.2658111016204));
#122322=CARTESIAN_POINT('Ctrl Pts',(-8.85413988014996,11.2547287197831,
11.2722939411926));
#122323=CARTESIAN_POINT('Ctrl Pts',(-8.85662413841964,11.2540083558031,
11.2824914554336));
#122324=CARTESIAN_POINT('Ctrl Pts',(-8.85755049499621,11.2537460061904,
11.2862148018765));
#122325=CARTESIAN_POINT('Ctrl Pts',(-8.85933823718161,11.2532514223385,
11.2932533666002));
#122326=CARTESIAN_POINT('Ctrl Pts',(-8.86019588497293,11.2530189998139,
11.2965693407176));
#122327=CARTESIAN_POINT('Ctrl Pts',(-8.86225654724447,11.252471749424,11.3043956088194));
#122328=CARTESIAN_POINT('Ctrl Pts',(-8.86347192693217,11.2521576229194,
11.3089025605685));
#122329=CARTESIAN_POINT('Ctrl Pts',(-8.86761921668051,11.2511135674627,
11.3239259351954));
#122330=CARTESIAN_POINT('Ctrl Pts',(-8.87067065077571,11.2503900302297,
11.3344091682097));
#122331=CARTESIAN_POINT('Ctrl Pts',(-8.8784476400569,11.2486459915908,11.359805565952));
#122332=CARTESIAN_POINT('Ctrl Pts',(-8.88332547588599,11.2476326300367,
11.3746702515226));
#122333=CARTESIAN_POINT('Ctrl Pts',(-8.90438899898507,11.2435480306065,
11.4347886260867));
#122334=CARTESIAN_POINT('Ctrl Pts',(-8.92304212565801,11.2405662064929,
11.4791315488177));
#122335=CARTESIAN_POINT('Ctrl Pts',(-8.98233876458414,11.2322890143681,
11.5989987525076));
#122336=CARTESIAN_POINT('Ctrl Pts',(-9.0285826415389,11.2270154786977,11.6714016635962));
#122337=CARTESIAN_POINT('Ctrl Pts',(-9.0921286174542,11.2204129489149,11.7504080386997));
#122338=CARTESIAN_POINT('Ctrl Pts',(-9.1022351409386,11.2193795033654,11.7624702562932));
#122339=CARTESIAN_POINT('Ctrl Pts',(-9.11761871959068,11.2178283662472,
11.7801006831076));
#122340=CARTESIAN_POINT('Ctrl Pts',(-9.12271367120461,11.2173180604035,
11.7858259937624));
#122341=CARTESIAN_POINT('Ctrl Pts',(-9.13193104138223,11.2164006628796,
11.7959823920354));
#122342=CARTESIAN_POINT('Ctrl Pts',(-9.13603245714807,11.215994453862,11.8004322381772));
#122343=CARTESIAN_POINT('Ctrl Pts',(-9.14481828769405,11.2151283863368,
11.8098182566846));
#122344=CARTESIAN_POINT('Ctrl Pts',(-9.14951153879956,11.2146681617618,
11.8147458155361));
#122345=CARTESIAN_POINT('Ctrl Pts',(-9.16228133093817,11.2134222056775,
11.8279225627887));
#122346=CARTESIAN_POINT('Ctrl Pts',(-9.17043671795362,11.2126330972982,
11.8360939439518));
#122347=CARTESIAN_POINT('Ctrl Pts',(-9.21633715964392,11.2082265685633,
11.8807516670098));
#122348=CARTESIAN_POINT('Ctrl Pts',(-9.25636370237924,11.2045077203375,
11.9147975774346));
#122349=CARTESIAN_POINT('Ctrl Pts',(-9.36225645454631,11.1949779082525,
11.9933144294481));
#122350=CARTESIAN_POINT('Ctrl Pts',(-9.43059862275343,11.1890842163386,
12.0340075001627));
#122351=CARTESIAN_POINT('Ctrl Pts',(-9.53042256950844,11.1811217645572,
12.0805278330715));
#122352=CARTESIAN_POINT('Ctrl Pts',(-9.55883707669991,11.1789243982566,
12.0924371825522));
#122353=CARTESIAN_POINT('Ctrl Pts',(-9.59413595809878,11.1763036470834,
12.1056296038588));
#122354=CARTESIAN_POINT('Ctrl Pts',(-9.6006048061927,11.1758277648368,12.1079828185775));
#122355=CARTESIAN_POINT('Ctrl Pts',(-9.61079534325875,11.1750853773126,
12.1115890483473));
#122356=CARTESIAN_POINT('Ctrl Pts',(-9.61450317690428,11.1748167629088,
12.1128803519465));
#122357=CARTESIAN_POINT('Ctrl Pts',(-9.62111497469947,11.1743405287551,
12.1151459910997));
#122358=CARTESIAN_POINT('Ctrl Pts',(-9.62401629098665,11.174132502201,12.1161275441228));
#122359=CARTESIAN_POINT('Ctrl Pts',(-9.63101119437675,11.1736332095339,
12.1184636403855));
#122360=CARTESIAN_POINT('Ctrl Pts',(-9.63510843031541,11.1733425888863,
12.119807035779));
#122361=CARTESIAN_POINT('Ctrl Pts',(-9.64773799338084,11.1724521404418,
12.1238713193084));
#122362=CARTESIAN_POINT('Ctrl Pts',(-9.65629428472368,11.171856404055,12.1265174906952));
#122363=CARTESIAN_POINT('Ctrl Pts',(-9.6764334797956,11.1704699667828,12.1324950356505));
#122364=CARTESIAN_POINT('Ctrl Pts',(-9.68803915802647,11.1696831261186,
12.1357467834655));
#122365=CARTESIAN_POINT('Ctrl Pts',(-9.72996032999592,11.1668776194249,
12.1468013964896));
#122366=CARTESIAN_POINT('Ctrl Pts',(-9.76053584938151,11.1648996891446,
12.1535736052226));
#122367=CARTESIAN_POINT('Ctrl Pts',(-9.80670408327826,11.161966914709,12.161884347791));
#122368=CARTESIAN_POINT('Ctrl Pts',(-9.82211498184402,11.1609968521491,
12.1643433706988));
#122369=CARTESIAN_POINT('Ctrl Pts',(-9.93122761341439,11.154165377668,12.1795368450491));
#122370=CARTESIAN_POINT('Ctrl Pts',(-10.0261035645613,11.1483817612358,
12.181250781766));
#122371=CARTESIAN_POINT('Ctrl Pts',(-10.1348632709454,11.1412526725535,
12.1700963246834));
#122372=CARTESIAN_POINT('Ctrl Pts',(-10.1495358962874,11.140281135277,12.1683118141402));
#122373=CARTESIAN_POINT('Ctrl Pts',(-10.1716725003214,11.1387987313983,
12.1651956958818));
#122374=CARTESIAN_POINT('Ctrl Pts',(-10.179163942804,11.1382941638889,12.1640673237334));
#122375=CARTESIAN_POINT('Ctrl Pts',(-10.1926108222015,11.1373830321057,
12.1619090566164));
#122376=CARTESIAN_POINT('Ctrl Pts',(-10.1985702534752,11.1369773017429,
12.1609054383492));
#122377=CARTESIAN_POINT('Ctrl Pts',(-10.2112783240323,11.1361078551258,
12.1586645783361));
#122378=CARTESIAN_POINT('Ctrl Pts',(-10.2180243781897,11.1356437388738,
12.1574141447096));
#122379=CARTESIAN_POINT('Ctrl Pts',(-10.2363462909496,11.1343760208711,
12.153852171281));
#122380=CARTESIAN_POINT('Ctrl Pts',(-10.2478986783004,11.1335688366078,
12.1514254774599));
#122381=CARTESIAN_POINT('Ctrl Pts',(-10.3160322140127,11.1287600229732,
12.1360404827966));
#122382=CARTESIAN_POINT('Ctrl Pts',(-10.3716207032903,11.1246330203112,
12.1190891564534));
#122383=CARTESIAN_POINT('Ctrl Pts',(-10.4963313629057,11.1149267169187,
12.0707401985779));
#122384=CARTESIAN_POINT('Ctrl Pts',(-10.5641290084596,11.1093050131847,
12.0366230969395));
#122385=CARTESIAN_POINT('Ctrl Pts',(-10.6523989116582,11.1017761560084,
11.980964019803));
#122386=CARTESIAN_POINT('Ctrl Pts',(-10.6760539964246,11.0997374268553,
11.9648139930955));
#122387=CARTESIAN_POINT('Ctrl Pts',(-10.7045273187046,11.0972778822531,
11.943812385895));
#122388=CARTESIAN_POINT('Ctrl Pts',(-10.709921447103,11.0968116881393,11.9397617287672));
#122389=CARTESIAN_POINT('Ctrl Pts',(-10.7183748560127,11.0960810817562,
11.9332994150732));
#122390=CARTESIAN_POINT('Ctrl Pts',(-10.7214573842745,11.0958146646942,
11.9309186192726));
#122391=CARTESIAN_POINT('Ctrl Pts',(-10.7269471251834,11.0953402772547,
11.9266349628011));
#122392=CARTESIAN_POINT('Ctrl Pts',(-10.7293587158861,11.0951319195112,
11.9247379850288));
#122393=CARTESIAN_POINT('Ctrl Pts',(-10.7351780436037,11.094629185484,11.920123525881));
#122394=CARTESIAN_POINT('Ctrl Pts',(-10.7385781451713,11.0943354803106,
11.9173965247727));
#122395=CARTESIAN_POINT('Ctrl Pts',(-10.7491073078336,11.0934257747851,
11.9088552854706));
#122396=CARTESIAN_POINT('Ctrl Pts',(-10.7561836443658,11.0928141255971,
11.9029761887233));
#122397=CARTESIAN_POINT('Ctrl Pts',(-10.7726960913151,11.0913842430596,
11.8889272028956));
#122398=CARTESIAN_POINT('Ctrl Pts',(-10.7820728106409,11.090570209226,11.8806889162199));
#122399=CARTESIAN_POINT('Ctrl Pts',(-10.8158073448324,11.0876263052474,
11.8500863349232));
#122400=CARTESIAN_POINT('Ctrl Pts',(-10.8393528450589,11.0855415689328,
11.8268467299764));
#122401=CARTESIAN_POINT('Ctrl Pts',(-10.9143410623074,11.0786744622705,
11.7463234589442));
#122402=CARTESIAN_POINT('Ctrl Pts',(-10.9611433970977,11.0739892884291,
11.6849975471589));
#122403=CARTESIAN_POINT('Ctrl Pts',(-11.0213865364239,11.0667442577068,
11.5876013288456));
#122404=CARTESIAN_POINT('Ctrl Pts',(-11.0396032752786,11.0643312433426,
11.5547345085694));
#122405=CARTESIAN_POINT('Ctrl Pts',(-11.0610643460701,11.0611432712156,
11.5112313846294));
#122406=CARTESIAN_POINT('Ctrl Pts',(-11.0657735785254,11.0604188728548,
11.5013399457858));
#122407=CARTESIAN_POINT('Ctrl Pts',(-11.0731299533268,11.0592453726583,
11.4853161366395));
#122408=CARTESIAN_POINT('Ctrl Pts',(-11.0758641813459,11.0587992389096,
11.4792242788184));
#122409=CARTESIAN_POINT('Ctrl Pts',(-11.0809882343679,11.0579436051517,
11.4675429919504));
#122410=CARTESIAN_POINT('Ctrl Pts',(-11.0833868833319,11.0575344191036,
11.4619576504541));
#122411=CARTESIAN_POINT('Ctrl Pts',(-11.0888016531507,11.0565903397104,
11.4490750137273));
#122412=CARTESIAN_POINT('Ctrl Pts',(-11.0917878117162,11.0560544657919,
11.4417655224118));
#122413=CARTESIAN_POINT('Ctrl Pts',(-11.100962218157,11.0543586312355,11.4186471822516));
#122414=CARTESIAN_POINT('Ctrl Pts',(-11.1068820398805,11.0531899206166,
11.4027348592538));
#122415=CARTESIAN_POINT('Ctrl Pts',(-11.1199736667424,11.0504189415259,
11.3650730484422));
#122416=CARTESIAN_POINT('Ctrl Pts',(-11.1268589372337,11.0488081894755,
11.3432319351265));
#122417=CARTESIAN_POINT('Ctrl Pts',(-11.1650240896711,11.0388568114994,
11.2085982426991));
#122418=CARTESIAN_POINT('Ctrl Pts',(-11.1799769951264,11.0300474056564,
11.0918834662697));
#122419=CARTESIAN_POINT('Ctrl Pts',(-11.1771332988819,11.0205753676004,
10.9585233022005));
#122420=CARTESIAN_POINT('Ctrl Pts',(-11.1764429523605,11.0194251399042,
10.9421625932513));
#122421=CARTESIAN_POINT('Ctrl Pts',(-11.1750563531718,11.0179008211877,
10.9201911895189));
#122422=CARTESIAN_POINT('Ctrl Pts',(-11.174660636672,11.0175122386487,10.9145642275563));
#122423=CARTESIAN_POINT('Ctrl Pts',(-11.1739728896703,11.0169028658525,
10.905695668058));
#122424=CARTESIAN_POINT('Ctrl Pts',(-11.17370783061,11.0166806464345,10.9024521567633));
#122425=CARTESIAN_POINT('Ctrl Pts',(-11.1731321422063,11.0162228520569,
10.8957498262941));
#122426=CARTESIAN_POINT('Ctrl Pts',(-11.1728196555916,11.0159873949953,
10.8922912371738));
#122427=CARTESIAN_POINT('Ctrl Pts',(-11.1720239975761,11.0154178674021,
10.8838992565372));
#122428=CARTESIAN_POINT('Ctrl Pts',(-11.1715249619692,11.0150846606449,
10.8789673630975));
#122429=CARTESIAN_POINT('Ctrl Pts',(-11.1696349682116,11.0139024641359,
10.8613971084884));
#122430=CARTESIAN_POINT('Ctrl Pts',(-11.1680704565681,11.0130623927603,
10.8487777760091));
#122431=CARTESIAN_POINT('Ctrl Pts',(-11.1636281513183,11.0109740164168,
10.8171500932583));
#122432=CARTESIAN_POINT('Ctrl Pts',(-11.1604887097481,11.009737100129,10.7981817626773));
#122433=CARTESIAN_POINT('Ctrl Pts',(-11.1434602758955,11.0039546723689,
10.7089214109206));
#122434=CARTESIAN_POINT('Ctrl Pts',(-11.1236399454783,10.9995889118622,
10.6399128527113));
#122435=CARTESIAN_POINT('Ctrl Pts',(-11.0752779747691,10.9912927308428,
10.5155530809471));
#122436=CARTESIAN_POINT('Ctrl Pts',(-11.0483945116772,10.9873987249763,
10.4598342649403));
#122437=CARTESIAN_POINT('Ctrl Pts',(-11.0111714760072,10.9825575506522,
10.3960350369925));
#122438=CARTESIAN_POINT('Ctrl Pts',(-11.004914218444,10.9817592599538,10.3856801921034));
#122439=CARTESIAN_POINT('Ctrl Pts',(-10.9947894379346,10.9804904141443,
10.3694938854948));
#122440=CARTESIAN_POINT('Ctrl Pts',(-10.9910274523769,10.9800236837695,
10.3635971626855));
#122441=CARTESIAN_POINT('Ctrl Pts',(-10.9839247349748,10.9791509701349,
10.3526797219019));
#122442=CARTESIAN_POINT('Ctrl Pts',(-10.9805975180125,10.9787454942994,
10.3476504526822));
#122443=CARTESIAN_POINT('Ctrl Pts',(-10.9731061311413,10.9778397697463,
10.3365136320482));
#122444=CARTESIAN_POINT('Ctrl Pts',(-10.9689228169994,10.977338818661,10.3304193302415));
#122445=CARTESIAN_POINT('Ctrl Pts',(-10.9564516846754,10.9758591312999,
10.312612849279));
#122446=CARTESIAN_POINT('Ctrl Pts',(-10.9480071430515,10.9748745287189,
10.3010126286232));
#122447=CARTESIAN_POINT('Ctrl Pts',(-10.9086419514347,10.9703596274273,
10.2489627222537));
#122448=CARTESIAN_POINT('Ctrl Pts',(-10.8753341775915,10.9667385411551,
10.2103950176387));
#122449=CARTESIAN_POINT('Ctrl Pts',(-10.7818982931113,10.9570856641998,
10.1154038814592));
#122450=CARTESIAN_POINT('Ctrl Pts',(-10.7181625000867,10.9509598380189,
10.0629208912601));
#122451=CARTESIAN_POINT('Ctrl Pts',(-10.6284213187806,10.9432267710343,
10.0035971179078));
#122452=CARTESIAN_POINT('Ctrl Pts',(-10.6069232326493,10.941435618148,9.99035825081243));
#122453=CARTESIAN_POINT('Ctrl Pts',(-10.5793148119248,10.9392260709056,
9.97455739320516));
#122454=CARTESIAN_POINT('Ctrl Pts',(-10.5735876910458,10.9387725074589,
9.97134293528797));
#122455=CARTESIAN_POINT('Ctrl Pts',(-10.5644899632893,10.9380598930056,
9.96633626767257));
#122456=CARTESIAN_POINT('Ctrl Pts',(-10.5611371215611,10.9377989456487,
9.96451230715521));
#122457=CARTESIAN_POINT('Ctrl Pts',(-10.5547534261991,10.9373053710769,
9.9610796606097));
#122458=CARTESIAN_POINT('Ctrl Pts',(-10.551724422581,10.9370725688616,9.95946792586443));
#122459=CARTESIAN_POINT('Ctrl Pts',(-10.5445217493021,10.9365222107504,
9.95567567313349));
#122460=CARTESIAN_POINT('Ctrl Pts',(-10.5403419802501,10.9362053796808,
9.95350691286821));
#122461=CARTESIAN_POINT('Ctrl Pts',(-10.5262128007504,10.9351425447922,
9.94628291603847));
#122462=CARTESIAN_POINT('Ctrl Pts',(-10.5162042222657,10.9344032503157,
9.94134385759972));
#122463=CARTESIAN_POINT('Ctrl Pts',(-10.4915811537853,10.9326137074118,
9.92962505603652));
#122464=CARTESIAN_POINT('Ctrl Pts',(-10.4768945548228,10.9315710975809,
9.92300130560755));
#122465=CARTESIAN_POINT('Ctrl Pts',(-10.415500051688,10.9272958590718,9.89681426892766));
#122466=CARTESIAN_POINT('Ctrl Pts',(-10.3676878529283,10.9241613900453,
9.87997077982901));
#122467=CARTESIAN_POINT('Ctrl Pts',(-10.2399934623775,10.9159544989636,
9.84404868849485));
#122468=CARTESIAN_POINT('Ctrl Pts',(-10.1589562433228,10.910892454728,9.83014905191553));
#122469=CARTESIAN_POINT('Ctrl Pts',(-10.0612671311687,10.9045191209752,
9.82373713324707));
#122470=CARTESIAN_POINT('Ctrl Pts',(-10.0453786679518,10.903474847725,9.82301710697184));
#122471=CARTESIAN_POINT('Ctrl Pts',(-10.0217874163671,10.9019106070592,
9.82242639266425));
#122472=CARTESIAN_POINT('Ctrl Pts',(-10.0140921974884,10.9013982132125,
9.82230916727659));
#122473=CARTESIAN_POINT('Ctrl Pts',(-10.0003416268194,10.9004785159569,
9.82223448481794));
#122474=CARTESIAN_POINT('Ctrl Pts',(-9.99428665641062,10.9000721129608,
9.82224829406564));
#122475=CARTESIAN_POINT('Ctrl Pts',(-9.98144680430788,10.8992071787009,
9.8223765937133));
#122476=CARTESIAN_POINT('Ctrl Pts',(-9.97466229012247,10.8987482932007,
9.8225030338731));
#122477=CARTESIAN_POINT('Ctrl Pts',(-9.95642824684165,10.8975098091194,
9.82300051376034));
#122478=CARTESIAN_POINT('Ctrl Pts',(-9.94498265842873,10.896726903093,9.82347997707295));
#122479=CARTESIAN_POINT('Ctrl Pts',(-9.89253117305323,10.8931127066122,
9.82644424029201));
#122480=CARTESIAN_POINT('Ctrl Pts',(-9.85167674298975,10.8902221159927,
9.83090586595053));
#122481=CARTESIAN_POINT('Ctrl Pts',(-9.81114928308311,10.8872795026091,
9.83748958317786));
#122482=CARTESIAN_POINT('Ctrl Pts',(-9.81114930150155,10.7889089429636,
9.83748958018577));
#122483=CARTESIAN_POINT('Ctrl Pts',(-9.8144593237119,10.7891361684467,9.8369518645698));
#122484=CARTESIAN_POINT('Ctrl Pts',(-9.81777168141626,10.7893626048123,
9.83642827959523));
#122485=CARTESIAN_POINT('Ctrl Pts',(-9.827712887307,10.7900394733218,9.83490036371816));
#122486=CARTESIAN_POINT('Ctrl Pts',(-9.83434825740727,10.790487630429,9.83393845916146));
#122487=CARTESIAN_POINT('Ctrl Pts',(-9.86875879015411,10.7927946712871,
9.82924975546467));
#122488=CARTESIAN_POINT('Ctrl Pts',(-9.89665466635841,10.794607506475,9.82645817476321));
#122489=CARTESIAN_POINT('Ctrl Pts',(-10.0038528350274,10.8014447613579,
9.81958357764544));
#122490=CARTESIAN_POINT('Ctrl Pts',(-10.0833946392679,10.8062607968729,
9.82252611025464));
#122491=CARTESIAN_POINT('Ctrl Pts',(-10.2122743425764,10.814381625533,9.84042814460704));
#122492=CARTESIAN_POINT('Ctrl Pts',(-10.2620005807527,10.8175921965828,
9.8506427437954));
#122493=CARTESIAN_POINT('Ctrl Pts',(-10.3247215447131,10.8218373602538,
9.86780919294558));
#122494=CARTESIAN_POINT('Ctrl Pts',(-10.3384622984233,10.8227795059351,
9.87184072538561));
#122495=CARTESIAN_POINT('Ctrl Pts',(-10.3591728371484,10.8242196756507,
9.8783296057735));
#122496=CARTESIAN_POINT('Ctrl Pts',(-10.3661989455015,10.8247118067191,
9.88060376613859));
#122497=CARTESIAN_POINT('Ctrl Pts',(-10.3789207118352,10.8256095685739,
9.88485404674034));
#122498=CARTESIAN_POINT('Ctrl Pts',(-10.3846235101295,10.8260144704899,
9.88680812252446));
#122499=CARTESIAN_POINT('Ctrl Pts',(-10.3969120176277,10.8268924168771,
9.89112450529975));
#122500=CARTESIAN_POINT('Ctrl Pts',(-10.4034921508497,10.8273659419933,
9.89350187842935));
#122501=CARTESIAN_POINT('Ctrl Pts',(-10.4214047022346,10.8286645296677,
9.90015463003992));
#122502=CARTESIAN_POINT('Ctrl Pts',(-10.4326927044636,10.829493385962,9.90454631982017));
#122503=CARTESIAN_POINT('Ctrl Pts',(-10.5111654495748,10.8353314633858,
9.9364788905191));
#122504=CARTESIAN_POINT('Ctrl Pts',(-10.5757332186308,10.8405424995343,
9.97000238888947));
#122505=CARTESIAN_POINT('Ctrl Pts',(-10.6814364158687,10.8497287349869,
10.0379419583048));
#122506=CARTESIAN_POINT('Ctrl Pts',(-10.7240880825547,10.8536451428551,
10.0696195402373));
#122507=CARTESIAN_POINT('Ctrl Pts',(-10.7912349182959,10.86005092236,10.1269127512082));
#122508=CARTESIAN_POINT('Ctrl Pts',(-10.8169766463867,10.8625727204107,
10.1509512934915));
#122509=CARTESIAN_POINT('Ctrl Pts',(-10.8465956363163,10.8655195731447,
10.1812071173854));
#122510=CARTESIAN_POINT('Ctrl Pts',(-10.8515399137799,10.8660130843019,
10.1863503594516));
#122511=CARTESIAN_POINT('Ctrl Pts',(-10.8591708012771,10.8667768243067,
10.1944340784882));
#122512=CARTESIAN_POINT('Ctrl Pts',(-10.8618896488329,10.8670493579885,
10.1973436886935));
#122513=CARTESIAN_POINT('Ctrl Pts',(-10.8668988871079,10.8675521607834,
10.2027591917504));
#122514=CARTESIAN_POINT('Ctrl Pts',(-10.8691932052722,10.8677827118702,
10.2052612006607));
#122515=CARTESIAN_POINT('Ctrl Pts',(-10.8744486211256,10.8683114604281,
10.211042339073));
#122516=CARTESIAN_POINT('Ctrl Pts',(-10.8774021178296,10.8686090987479,
10.2143282447963));
#122517=CARTESIAN_POINT('Ctrl Pts',(-10.8866609276319,10.8695439936189,
10.2247464379767));
#122518=CARTESIAN_POINT('Ctrl Pts',(-10.8928984840552,10.8701765458684,
10.2319388062561));
#122519=CARTESIAN_POINT('Ctrl Pts',(-10.9386339562835,10.8748420891566,
10.2859855236954));
#122520=CARTESIAN_POINT('Ctrl Pts',(-10.9745136452726,10.8786603880657,
10.3357895456284));
#122521=CARTESIAN_POINT('Ctrl Pts',(-11.0535043594221,10.8880804548332,
10.4657151140089));
#122522=CARTESIAN_POINT('Ctrl Pts',(-11.0915251390269,10.893646528456,10.5484442323766));
#122523=CARTESIAN_POINT('Ctrl Pts',(-11.1244341133799,10.9005605155922,
10.6493165169617));
#122524=CARTESIAN_POINT('Ctrl Pts',(-11.1289116907196,10.9015697454868,
10.6640099111066));
#122525=CARTESIAN_POINT('Ctrl Pts',(-11.135170650419,10.9030914571677,10.6860887533817));
#122526=CARTESIAN_POINT('Ctrl Pts',(-11.1371701273765,10.9035969643369,
10.6934110680076));
#122527=CARTESIAN_POINT('Ctrl Pts',(-11.1406341138578,10.9045090139546,
10.7065968639862));
#122528=CARTESIAN_POINT('Ctrl Pts',(-11.14212454616,10.9049147137898,10.7124533069996));
#122529=CARTESIAN_POINT('Ctrl Pts',(-11.1452076572052,10.9057832452661,
10.7249702184464));
#122530=CARTESIAN_POINT('Ctrl Pts',(-11.1467874397167,10.9062464701126,
10.7316336020427));
#122531=CARTESIAN_POINT('Ctrl Pts',(-11.150919788985,10.9075095671303,10.7497665785463));
#122532=CARTESIAN_POINT('Ctrl Pts',(-11.1533589090503,10.908312979138,10.7612609468987));
#122533=CARTESIAN_POINT('Ctrl Pts',(-11.1665897087619,10.913034048415,10.8285547238772));
#122534=CARTESIAN_POINT('Ctrl Pts',(-11.1735014294451,10.9170716159459,
10.885031825212));
#122535=CARTESIAN_POINT('Ctrl Pts',(-11.1804451077102,10.9272568225237,
11.0253254308749));
#122536=CARTESIAN_POINT('Ctrl Pts',(-11.1756680193083,10.9334833199346,
11.1090702660529));
#122537=CARTESIAN_POINT('Ctrl Pts',(-11.158336334938,10.9411198425625,11.2141867536234));
#122538=CARTESIAN_POINT('Ctrl Pts',(-11.1539544793022,10.9427403094235,
11.2366606330973));
#122539=CARTESIAN_POINT('Ctrl Pts',(-11.1475214520918,10.9447709004562,
11.2651980843082));
#122540=CARTESIAN_POINT('Ctrl Pts',(-11.1460726737853,10.9452098898798,
11.2713907475448));
#122541=CARTESIAN_POINT('Ctrl Pts',(-11.1436851393827,10.9459048350956,
11.2812358102571));
#122542=CARTESIAN_POINT('Ctrl Pts',(-11.1427789075989,10.946162537087,11.2848958553062));
#122543=CARTESIAN_POINT('Ctrl Pts',(-11.1410108050414,10.9466538382636,
11.2918925840473));
#122544=CARTESIAN_POINT('Ctrl Pts',(-11.1401518526684,10.9468875866058,
11.2952298951571));
#122545=CARTESIAN_POINT('Ctrl Pts',(-11.1380593964943,10.9474454947647,
11.3032144289846));
#122546=CARTESIAN_POINT('Ctrl Pts',(-11.1368120431204,10.9477688771236,
11.3078580200561));
#122547=CARTESIAN_POINT('Ctrl Pts',(-11.1324137013399,10.9488785959615,
11.3238406549219));
#122548=CARTESIAN_POINT('Ctrl Pts',(-11.1291211003856,10.9496573933126,
11.3351404589956));
#122549=CARTESIAN_POINT('Ctrl Pts',(-11.1205704794178,10.9515625215844,
11.3629273495246));
#122550=CARTESIAN_POINT('Ctrl Pts',(-11.1151173285943,10.952679860437,11.3793519044553));
#122551=CARTESIAN_POINT('Ctrl Pts',(-11.0898808950359,10.9574789713828,
11.4501083624561));
#122552=CARTESIAN_POINT('Ctrl Pts',(-11.0664727513307,10.9610366562839,
11.5030653410641));
#122553=CARTESIAN_POINT('Ctrl Pts',(-11.0052148020642,10.9690935171345,
11.6179622217489));
#122554=CARTESIAN_POINT('Ctrl Pts',(-10.9653508562184,10.9735932756457,
11.6785500139398));
#122555=CARTESIAN_POINT('Ctrl Pts',(-10.9101012266667,10.9793535925768,
11.7477109429893));
#122556=CARTESIAN_POINT('Ctrl Pts',(-10.8997629076585,10.9804137361944,
11.7601200998497));
#122557=CARTESIAN_POINT('Ctrl Pts',(-10.8840966259385,10.9819970799163,
11.7781568918825));
#122558=CARTESIAN_POINT('Ctrl Pts',(-10.8789627613031,10.9825124262236,
11.7839511795043));
#122559=CARTESIAN_POINT('Ctrl Pts',(-10.8697099841708,10.9834352929785,
11.7941890901225));
#122560=CARTESIAN_POINT('Ctrl Pts',(-10.8656131645881,10.9838418871966,
11.7986523739334));
#122561=CARTESIAN_POINT('Ctrl Pts',(-10.856875235057,10.9847049829542,11.808025705275));
#122562=CARTESIAN_POINT('Ctrl Pts',(-10.8522259604238,10.9851618214502,
11.8129278061044));
#122563=CARTESIAN_POINT('Ctrl Pts',(-10.8396714015447,10.9863892637121,
11.8259390095289));
#122564=CARTESIAN_POINT('Ctrl Pts',(-10.8316910701045,10.9871630748054,
11.8339743751608));
#122565=CARTESIAN_POINT('Ctrl Pts',(-10.7888658749981,10.991283449389,11.8758688518904));
#122566=CARTESIAN_POINT('Ctrl Pts',(-10.7520710145602,10.9947161786266,
11.9076583514454));
#122567=CARTESIAN_POINT('Ctrl Pts',(-10.6733618378722,11.0018457784109,
11.9675815230439));
#122568=CARTESIAN_POINT('Ctrl Pts',(-10.6313883231267,11.0055406254961,
11.9954789746541));
#122569=CARTESIAN_POINT('Ctrl Pts',(-10.57134985927,11.0106243083954,12.0300548876868));
#122570=CARTESIAN_POINT('Ctrl Pts',(-10.5547124072893,11.0120127402581,
12.0391091848679));
#122571=CARTESIAN_POINT('Ctrl Pts',(-10.4985494486609,11.0166204464434,
12.0679402708649));
#122572=CARTESIAN_POINT('Ctrl Pts',(-10.4581258493629,11.0198101379962,
12.0858957395375));
#122573=CARTESIAN_POINT('Ctrl Pts',(-10.410458730477,11.0233601789877,12.1039313549433));
#122574=CARTESIAN_POINT('Ctrl Pts',(-10.4041123207451,11.0238286104358,
12.1062703301498));
#122575=CARTESIAN_POINT('Ctrl Pts',(-10.3937407970433,11.0245868870124,
12.1099916006046));
#122576=CARTESIAN_POINT('Ctrl Pts',(-10.3897278236745,11.0248785250987,
12.1114069432687));
#122577=CARTESIAN_POINT('Ctrl Pts',(-10.382509348481,11.0253998624469,12.1139089350421));
#122578=CARTESIAN_POINT('Ctrl Pts',(-10.3793067593123,11.0256300082825,
12.1150035427895));
#122579=CARTESIAN_POINT('Ctrl Pts',(-10.3722047134575,11.0261378292643,
12.1173967981541));
#122580=CARTESIAN_POINT('Ctrl Pts',(-10.3683031477281,11.0264151242766,
12.1186888512445));
#122581=CARTESIAN_POINT('Ctrl Pts',(-10.3568383159114,11.0272252609451,
12.1224190948198));
#122582=CARTESIAN_POINT('Ctrl Pts',(-10.3492568645201,11.0277550076889,
12.1248012531785));
#122583=CARTESIAN_POINT('Ctrl Pts',(-10.3317693823475,11.0289644734875,
12.1301021066745));
#122584=CARTESIAN_POINT('Ctrl Pts',(-10.3218477920664,11.0296415517963,
12.1329676558844));
#122585=CARTESIAN_POINT('Ctrl Pts',(-10.2880462969432,11.0319214656636,
12.1422503065539));
#122586=CARTESIAN_POINT('Ctrl Pts',(-10.2640013017299,11.0334982650823,
12.1480461235296));
#122587=CARTESIAN_POINT('Ctrl Pts',(-10.1882547885436,11.038375355526,12.1637980723468));
#122588=CARTESIAN_POINT('Ctrl Pts',(-10.1360568300788,11.0416087234541,
12.171048597162));
#122589=CARTESIAN_POINT('Ctrl Pts',(-10.0120533944585,11.0493107767507,
12.1798673576524));
#122590=CARTESIAN_POINT('Ctrl Pts',(-9.94025454983669,11.0537940229939,
12.1784145241942));
#122591=CARTESIAN_POINT('Ctrl Pts',(-9.8568507494053,11.0592927079498,12.1690824397815));
#122592=CARTESIAN_POINT('Ctrl Pts',(-9.84468561160191,11.0601017044701,
12.1675285355699));
#122593=CARTESIAN_POINT('Ctrl Pts',(-9.8255883191371,11.0613837231064,12.164785411527));
#122594=CARTESIAN_POINT('Ctrl Pts',(-9.81863854099204,11.0618527832158,
12.1637235526157));
#122595=CARTESIAN_POINT('Ctrl Pts',(-9.80575001255119,11.0627275359033,
12.1616360537669));
#122596=CARTESIAN_POINT('Ctrl Pts',(-9.79980879365612,11.0631326994353,
12.160626924394));
#122597=CARTESIAN_POINT('Ctrl Pts',(-9.78664565985859,11.064034773709,12.1582870597943));
#122598=CARTESIAN_POINT('Ctrl Pts',(-9.77942796904358,11.0645323607029,
12.1569342947126));
#122599=CARTESIAN_POINT('Ctrl Pts',(-9.7583769236949,11.0659925158156,12.1527846851136));
#122600=CARTESIAN_POINT('Ctrl Pts',(-9.74458103501503,11.0669607195338,
12.1498066635739));
#122601=CARTESIAN_POINT('Ctrl Pts',(-9.71330299284559,11.0691825278767,
12.1424642118172));
#122602=CARTESIAN_POINT('Ctrl Pts',(-9.69586113915025,11.0704407090283,
12.1379451403868));
#122603=CARTESIAN_POINT('Ctrl Pts',(-9.63691182354621,11.0747595160042,
12.1212196909126));
#122604=CARTESIAN_POINT('Ctrl Pts',(-9.59597932292998,11.077873305584,12.1071283804173));
#122605=CARTESIAN_POINT('Ctrl Pts',(-9.49947310251629,11.085464492693,12.067839860856));
#122606=CARTESIAN_POINT('Ctrl Pts',(-9.44489799808155,11.0899706133088,
12.0405146790893));
#122607=CARTESIAN_POINT('Ctrl Pts',(-9.36233027863264,11.0969654688663,
11.9908215694962));
#122608=CARTESIAN_POINT('Ctrl Pts',(-9.33281399558934,11.0995040147299,
11.9711917455431));
#122609=CARTESIAN_POINT('Ctrl Pts',(-9.29846126704067,11.102467409513,11.9460388466418));
#122610=CARTESIAN_POINT('Ctrl Pts',(-9.29273585919675,11.1029615962512,
11.9417661783215));
#122611=CARTESIAN_POINT('Ctrl Pts',(-9.28387819621269,11.1037261551844,
11.9350296781316));
#122612=CARTESIAN_POINT('Ctrl Pts',(-9.28071908400707,11.1039988398429,
11.9326016844901));
#122613=CARTESIAN_POINT('Ctrl Pts',(-9.27489142543986,11.1045017762716,
11.9280755034191));
#122614=CARTESIAN_POINT('Ctrl Pts',(-9.2722196233885,11.1047323113588,11.9259818080442));
#122615=CARTESIAN_POINT('Ctrl Pts',(-9.26609352574576,11.105260837501,11.9211383399846));
#122616=CARTESIAN_POINT('Ctrl Pts',(-9.26264560281176,11.1055582711769,
11.9183806666404));
#122617=CARTESIAN_POINT('Ctrl Pts',(-9.25182539224047,11.1064918583267,
11.9096263661507));
#122618=CARTESIAN_POINT('Ctrl Pts',(-9.24450991058488,11.1071233261193,
11.9035596873271));
#122619=CARTESIAN_POINT('Ctrl Pts',(-9.20673439790415,11.1103903856575,
11.8714531340525));
#122620=CARTESIAN_POINT('Ctrl Pts',(-9.17754145612012,11.1129372616593,
11.843957051111));
#122621=CARTESIAN_POINT('Ctrl Pts',(-9.08483336891261,11.1213279952747,
11.7472481667146));
#122622=CARTESIAN_POINT('Ctrl Pts',(-9.02820134341422,11.1270042573511,
11.6719503984445));
#122623=CARTESIAN_POINT('Ctrl Pts',(-8.96708243901817,11.1347964440785,
11.5665320148384));
#122624=CARTESIAN_POINT('Ctrl Pts',(-8.95392220947762,11.1366086433628,
11.5418470942804));
#122625=CARTESIAN_POINT('Ctrl Pts',(-8.93734161571641,11.1390987676831,
11.5078866208787));
#122626=CARTESIAN_POINT('Ctrl Pts',(-8.93314037037807,11.1397499794866,
11.4990011847919));
#122627=CARTESIAN_POINT('Ctrl Pts',(-8.92637376313749,11.140833757778,11.4842139621393));
#122628=CARTESIAN_POINT('Ctrl Pts',(-8.92374463302754,11.141264145885,11.4783417605577));
#122629=CARTESIAN_POINT('Ctrl Pts',(-8.91868733941256,11.1421107105515,
11.4667934277452));
#122630=CARTESIAN_POINT('Ctrl Pts',(-8.91625542921269,11.1425267442592,
11.4611191569752));
#122631=CARTESIAN_POINT('Ctrl Pts',(-8.91057630777647,11.1435200909674,
11.4475751952879));
#122632=CARTESIAN_POINT('Ctrl Pts',(-8.90736963220345,11.1440987344948,
11.4396889916674));
#122633=CARTESIAN_POINT('Ctrl Pts',(-8.89669452749624,11.146087814776,11.4125975107195));
#122634=CARTESIAN_POINT('Ctrl Pts',(-8.88964512756509,11.1475118667593,
11.3932322932649));
#122635=CARTESIAN_POINT('Ctrl Pts',(-8.87368895003519,11.1510263661408,
11.3455425441044));
#122636=CARTESIAN_POINT('Ctrl Pts',(-8.86533859051338,11.1531328585483,
11.3170480581416));
#122637=CARTESIAN_POINT('Ctrl Pts',(-8.84499918826781,11.15910264228,11.2364775756994));
#122638=CARTESIAN_POINT('Ctrl Pts',(-8.83546410649209,11.1630197180775,
11.1838584316372));
#122639=CARTESIAN_POINT('Ctrl Pts',(-8.82293588981713,11.1712990794932,
11.0717305397439));
#122640=CARTESIAN_POINT('Ctrl Pts',(-8.82081545381712,11.1756506918968,
11.01226257693));
#122641=CARTESIAN_POINT('Ctrl Pts',(-8.82361997367075,11.1805727147056,
10.9422150672314));
#122642=CARTESIAN_POINT('Ctrl Pts',(-8.82419219630213,11.1813162300303,
10.9315522572618));
#122643=CARTESIAN_POINT('Ctrl Pts',(-8.82518929670315,11.1823398133931,
10.9167399006612));
#122644=CARTESIAN_POINT('Ctrl Pts',(-8.82549129422022,11.1826260520454,
10.9125829874173));
#122645=CARTESIAN_POINT('Ctrl Pts',(-8.82608242579897,11.1831460213998,
10.9050032114331));
#122646=CARTESIAN_POINT('Ctrl Pts',(-8.82636447943263,11.1833801305476,
10.9015798448634));
#122647=CARTESIAN_POINT('Ctrl Pts',(-8.82698210887803,11.1838651664396,
10.8944640578267));
#122648=CARTESIAN_POINT('Ctrl Pts',(-8.82732014744257,11.184115957482,10.8907719251042));
#122649=CARTESIAN_POINT('Ctrl Pts',(-8.8282579717746,11.1847751490537,10.8810354052362));
#122650=CARTESIAN_POINT('Ctrl Pts',(-8.82888710013355,11.1851819721369,
10.8749938593626));
#122651=CARTESIAN_POINT('Ctrl Pts',(-8.83204392164894,11.1870714275878,
10.8467980071097));
#122652=CARTESIAN_POINT('Ctrl Pts',(-8.83515387707686,11.1885249577439,
10.8247119081072));
#122653=CARTESIAN_POINT('Ctrl Pts',(-8.84634500104037,11.1928158873806,
10.7588435220824));
#122654=CARTESIAN_POINT('Ctrl Pts',(-8.85628293923035,11.1955870238585,
10.7154157750965));
#122655=CARTESIAN_POINT('Ctrl Pts',(-8.89396411720842,11.2039865621445,
10.5851862525209));
#122656=CARTESIAN_POINT('Ctrl Pts',(-8.92932579221778,11.2095696708637,
10.5009603958658));
#122657=CARTESIAN_POINT('Ctrl Pts',(-8.98156221155184,11.2165015554414,
10.4082951756153));
#122658=CARTESIAN_POINT('Ctrl Pts',(-8.98935089181854,11.2175089957556,
10.3950880451457));
#122659=CARTESIAN_POINT('Ctrl Pts',(-9.00137470629132,11.2190285370869,
10.3755801753981));
#122660=CARTESIAN_POINT('Ctrl Pts',(-9.00541673844993,11.2195336934714,
10.3691618861101));
#122661=CARTESIAN_POINT('Ctrl Pts',(-9.01278975502116,11.2204453618026,
10.3577013869853));
#122662=CARTESIAN_POINT('Ctrl Pts',(-9.01609811198099,11.2208510341149,
10.3526448822301));
#122663=CARTESIAN_POINT('Ctrl Pts',(-9.02324046569379,11.2217197805876,
10.3419097180139));
#122664=CARTESIAN_POINT('Ctrl Pts',(-9.02708538487016,11.2221832500721,
10.336238630722));
#122665=CARTESIAN_POINT('Ctrl Pts',(-9.03766716634926,11.2234477166518,
10.3209204556042));
#122666=CARTESIAN_POINT('Ctrl Pts',(-9.04449931818464,11.2242522666304,
10.3113404760051));
#122667=CARTESIAN_POINT('Ctrl Pts',(-9.08538431838967,11.2290003874276,
10.2557917829051));
#122668=CARTESIAN_POINT('Ctrl Pts',(-9.12260148474596,11.2330655416056,
10.2122577939222));
#122669=CARTESIAN_POINT('Ctrl Pts',(-9.21989597293735,11.2430980929595,
10.1139325299781));
#122670=CARTESIAN_POINT('Ctrl Pts',(-9.28276766226697,11.2491322247577,
10.0623139069738));
#122671=CARTESIAN_POINT('Ctrl Pts',(-9.37104826978553,11.2567349955457,
10.0039453485187));
#122672=CARTESIAN_POINT('Ctrl Pts',(-9.39207716277581,11.2584869077926,
9.99097315477275));
#122673=CARTESIAN_POINT('Ctrl Pts',(-9.41915158789648,11.2606551767727,
9.97542562214886));
#122674=CARTESIAN_POINT('Ctrl Pts',(-9.42483003208833,11.2611052125408,
9.97222714257835));
#122675=CARTESIAN_POINT('Ctrl Pts',(-9.43386560808367,11.2618135180266,
9.96723604273454));
#122676=CARTESIAN_POINT('Ctrl Pts',(-9.43720527916555,11.2620736475487,
9.96541233122933));
#122677=CARTESIAN_POINT('Ctrl Pts',(-9.44357529998175,11.2625665614581,
9.961973793474));
#122678=CARTESIAN_POINT('Ctrl Pts',(-9.44660386016015,11.2627995136631,
9.96035603934288));
#122679=CARTESIAN_POINT('Ctrl Pts',(-9.45382122468548,11.2633514243431,
9.95654124209201));
#122680=CARTESIAN_POINT('Ctrl Pts',(-9.45801625725096,11.2636696455486,
9.95435615118438));
#122681=CARTESIAN_POINT('Ctrl Pts',(-9.47226945304297,11.2647425489247,
9.94704082977616));
#122682=CARTESIAN_POINT('Ctrl Pts',(-9.48238854890885,11.2654903467187,
9.94202979577966));
#122683=CARTESIAN_POINT('Ctrl Pts',(-9.50734571199425,11.2673046553543,
9.93011468490168));
#122684=CARTESIAN_POINT('Ctrl Pts',(-9.52225892809573,11.2683632469225,
9.92337269303126));
#122685=CARTESIAN_POINT('Ctrl Pts',(-9.58522062988033,11.2727461682114,
9.89647489275286));
#122686=CARTESIAN_POINT('Ctrl Pts',(-9.63444177812688,11.2759672246033,
9.8792067198233));
#122687=CARTESIAN_POINT('Ctrl Pts',(-9.72630295517816,11.281865198734,9.85367799378828));
#122688=CARTESIAN_POINT('Ctrl Pts',(-9.76853434469116,11.2845348228597,
9.84441241220771));
#122689=CARTESIAN_POINT('Ctrl Pts',(-9.81114930150156,11.2872494929995,
9.83748958018577));
#122690=CARTESIAN_POINT('Origin',(-10.,2.67563288526385,11.));
#122691=CARTESIAN_POINT('',(-9.81114930150145,11.8854636688711,9.83748958018579));
#122692=CARTESIAN_POINT('',(-9.81114930150157,11.7871268320303,9.83748958018577));
#122693=CARTESIAN_POINT('',(-9.81114930150157,2.67563288526385,9.83748958018577));
#122694=CARTESIAN_POINT('Ctrl Pts',(-9.81114930150134,11.8854636688711,
9.83748958018581));
#122695=CARTESIAN_POINT('Ctrl Pts',(-9.81028034253745,11.8854036452282,
9.83763074322788));
#122696=CARTESIAN_POINT('Ctrl Pts',(-9.80941153764504,11.8853436757721,
9.83777288125349));
#122697=CARTESIAN_POINT('Ctrl Pts',(-9.8051592648706,11.8850503775531,9.83847345699382));
#122698=CARTESIAN_POINT('Ctrl Pts',(-9.80177808428253,11.8848178402371,
9.83904569658545));
#122699=CARTESIAN_POINT('Ctrl Pts',(-9.79431956583179,11.8843063002129,
9.84034152911374));
#122700=CARTESIAN_POINT('Ctrl Pts',(-9.7902434079324,11.8840276693685,9.84107188166586));
#122701=CARTESIAN_POINT('Ctrl Pts',(-9.77584363062652,11.8830463778862,
9.8437304479553));
#122702=CARTESIAN_POINT('Ctrl Pts',(-9.76554167624368,11.8823498413611,
9.84577529568974));
#122703=CARTESIAN_POINT('Ctrl Pts',(-9.68979036946538,11.8772595760648,
9.86186738544853));
#122704=CARTESIAN_POINT('Ctrl Pts',(-9.62560862157251,11.8731161131964,
9.88133590927951));
#122705=CARTESIAN_POINT('Ctrl Pts',(-9.4895706949893,11.8640534254544,9.9356317142924));
#122706=CARTESIAN_POINT('Ctrl Pts',(-9.41890224580094,11.8591486421966,
9.97250712471857));
#122707=CARTESIAN_POINT('Ctrl Pts',(-9.33740316682762,11.8528193148595,
10.0261484995713));
#122708=CARTESIAN_POINT('Ctrl Pts',(-9.32254677400131,11.8516363426646,
10.0364241709241));
#122709=CARTESIAN_POINT('Ctrl Pts',(-9.30138719889297,11.8499051317427,
10.0517908114712));
#122710=CARTESIAN_POINT('Ctrl Pts',(-9.29489053862493,11.8493670766408,
10.0566118756708));
#122711=CARTESIAN_POINT('Ctrl Pts',(-9.28357883487237,11.8484184213404,
10.0651882243561));
#122712=CARTESIAN_POINT('Ctrl Pts',(-9.27874231461894,11.8480089413352,
10.0689147780067));
#122713=CARTESIAN_POINT('Ctrl Pts',(-9.26874756454997,11.8471545321851,
10.0767403694604));
#122714=CARTESIAN_POINT('Ctrl Pts',(-9.26359432985219,11.8467093763934,
10.0808454125286));
#122715=CARTESIAN_POINT('Ctrl Pts',(-9.2502838525281,11.8455472845629,10.091632263477));
#122716=CARTESIAN_POINT('Ctrl Pts',(-9.24218157301851,11.844827717133,10.0983806425474));
#122717=CARTESIAN_POINT('Ctrl Pts',(-9.20826274022853,11.8417623484875,
10.1274118051074));
#122718=CARTESIAN_POINT('Ctrl Pts',(-9.18333211589294,11.8393761168736,
10.1506995763677));
#122719=CARTESIAN_POINT('Ctrl Pts',(-9.10395718997506,11.8313155425491,
10.2315740540055));
#122720=CARTESIAN_POINT('Ctrl Pts',(-9.05431675740454,11.8254727493145,
10.2935640824585));
#122721=CARTESIAN_POINT('Ctrl Pts',(-9.00960631724414,11.8194516363058,
10.3626422498798));
#122722=CARTESIAN_POINT('Ctrl Pts',(-9.0079429460058,11.8192263878441,10.3652344131719));
#122723=CARTESIAN_POINT('Ctrl Pts',(-8.98893583222473,11.8166383092667,
10.3951119076177));
#122724=CARTESIAN_POINT('Ctrl Pts',(-8.97271134679763,11.8142918187697,
10.4230956290713));
#122725=CARTESIAN_POINT('Ctrl Pts',(-8.95193045769536,11.8111141827451,
10.4626019474309));
#122726=CARTESIAN_POINT('Ctrl Pts',(-8.94637355575669,11.8102450593589,
10.4735802296974));
#122727=CARTESIAN_POINT('Ctrl Pts',(-8.93700799218333,11.8087478526672,
10.4928256271242));
#122728=CARTESIAN_POINT('Ctrl Pts',(-8.93312130133838,11.8081160065524,
10.5010534015022));
#122729=CARTESIAN_POINT('Ctrl Pts',(-8.9275223659849,11.8071907708689,10.5132704891912));
#122730=CARTESIAN_POINT('Ctrl Pts',(-8.92573629903351,11.8068932463396,
10.5172253171035));
#122731=CARTESIAN_POINT('Ctrl Pts',(-8.9225940982975,11.8063656524613,10.5242867730151));
#122732=CARTESIAN_POINT('Ctrl Pts',(-8.92122947480075,11.8061350877485,
10.5273894771897));
#122733=CARTESIAN_POINT('Ctrl Pts',(-8.9182668239128,11.8056313511507,10.5342052625401));
#122734=CARTESIAN_POINT('Ctrl Pts',(-8.91667450368135,11.8053585181383,
10.5379207081678));
#122735=CARTESIAN_POINT('Ctrl Pts',(-8.91222132012836,11.8045892987304,
10.548461110488));
#122736=CARTESIAN_POINT('Ctrl Pts',(-8.90940554724136,11.8040954903982,
10.5553050802943));
#122737=CARTESIAN_POINT('Ctrl Pts',(-8.89046314763234,11.8007181830896,
10.6026084688807));
#122738=CARTESIAN_POINT('Ctrl Pts',(-8.87652527228846,11.7979477180871,
10.64391364079));
#122739=CARTESIAN_POINT('Ctrl Pts',(-8.8597009490363,11.7939973870626,10.7047134290204));
#122740=CARTESIAN_POINT('Ctrl Pts',(-8.8549635257435,11.7927843266876,10.7236531378988));
#122741=CARTESIAN_POINT('Ctrl Pts',(-8.8397277432039,11.7884620453546,10.7917085209231));
#122742=CARTESIAN_POINT('Ctrl Pts',(-8.83190244486421,11.7853733852593,
10.8413651900117));
#122743=CARTESIAN_POINT('Ctrl Pts',(-8.82277260143998,11.7791679894831,
10.9399267378273));
#122744=CARTESIAN_POINT('Ctrl Pts',(-8.82129526246719,11.7760606716317,
10.9887115453498));
#122745=CARTESIAN_POINT('Ctrl Pts',(-8.82320581161219,11.7721145824843,
11.0487753805916));
#122746=CARTESIAN_POINT('Ctrl Pts',(-8.82372985148856,11.7713653725679,
11.0601009375571));
#122747=CARTESIAN_POINT('Ctrl Pts',(-8.82482722149161,11.7701613985238,
11.0781645903157));
#122748=CARTESIAN_POINT('Ctrl Pts',(-8.82529522992912,11.7697098916066,
11.084908553678));
#122749=CARTESIAN_POINT('Ctrl Pts',(-8.82629281142983,11.7688502316105,
11.0976894001496));
#122750=CARTESIAN_POINT('Ctrl Pts',(-8.82681097183119,11.7684424452403,
11.1037269744835));
#122751=CARTESIAN_POINT('Ctrl Pts',(-8.82809702725269,11.7675104766752,
11.1174665635128));
#122752=CARTESIAN_POINT('Ctrl Pts',(-8.82889429644162,11.7669854001541,
11.1251654793574));
#122753=CARTESIAN_POINT('Ctrl Pts',(-8.83158762091886,11.76535831786,11.1488890628285));
#122754=CARTESIAN_POINT('Ctrl Pts',(-8.83373709420384,11.7642485422381,
11.1648824748614));
#122755=CARTESIAN_POINT('Ctrl Pts',(-8.84679718553935,11.7583452385116,
11.2489364556803));
#122756=CARTESIAN_POINT('Ctrl Pts',(-8.86333697585634,11.7533794604482,
11.3159753838638));
#122757=CARTESIAN_POINT('Ctrl Pts',(-8.90524442624838,11.7439043163671,
11.4384917550157));
#122758=CARTESIAN_POINT('Ctrl Pts',(-8.92924369472445,11.7394290007836,
11.4942126197188));
#122759=CARTESIAN_POINT('Ctrl Pts',(-8.96566871418012,11.7337950029776,
11.5635317501745));
#122760=CARTESIAN_POINT('Ctrl Pts',(-8.9742673410289,11.7325308236331,11.5790352517634));
#122761=CARTESIAN_POINT('Ctrl Pts',(-8.98925894164514,11.7304392497548,
11.6046826502418));
#122762=CARTESIAN_POINT('Ctrl Pts',(-8.99546253674041,11.7296032292092,
11.6149334167827));
#122763=CARTESIAN_POINT('Ctrl Pts',(-9.00439207257219,11.7284420684382,
11.6291926335334));
#122764=CARTESIAN_POINT('Ctrl Pts',(-9.00698772801648,11.7281093320967,
11.6332812526857));
#122765=CARTESIAN_POINT('Ctrl Pts',(-9.01147697085825,11.7275421408303,
11.6402571384975));
#122766=CARTESIAN_POINT('Ctrl Pts',(-9.01335815202916,11.7273069002274,
11.6431522740763));
#122767=CARTESIAN_POINT('Ctrl Pts',(-9.01731338322248,11.7268174085978,
11.6491811739911));
#122768=CARTESIAN_POINT('Ctrl Pts',(-9.01938972912648,11.7265633102804,
11.6523133304703));
#122769=CARTESIAN_POINT('Ctrl Pts',(-9.0249865416234,11.7258858470152,11.6606689757945));
#122770=CARTESIAN_POINT('Ctrl Pts',(-9.02853404065055,11.7254642190908,
11.6658743378164));
#122771=CARTESIAN_POINT('Ctrl Pts',(-9.04476545377029,11.7235686142606,
11.6892853821426));
#122772=CARTESIAN_POINT('Ctrl Pts',(-9.05792142102435,11.7221230874706,
11.7071601500283));
#122773=CARTESIAN_POINT('Ctrl Pts',(-9.08501927550016,11.7192958439277,
11.7418778447711));
#122774=CARTESIAN_POINT('Ctrl Pts',(-9.09894033775112,11.7179140488507,
11.758725272201));
#122775=CARTESIAN_POINT('Ctrl Pts',(-9.15150426656147,11.7129066822172,
11.8188499664151));
#122776=CARTESIAN_POINT('Ctrl Pts',(-9.19286110719524,11.7093554758552,
11.8596437846266));
#122777=CARTESIAN_POINT('Ctrl Pts',(-9.28317543329782,11.7019802131619,
11.9364414023846));
#122778=CARTESIAN_POINT('Ctrl Pts',(-9.33224345092774,11.6981607195572,
11.972038963412));
#122779=CARTESIAN_POINT('Ctrl Pts',(-9.39411452647769,11.6934021673654,
12.0100215886035));
#122780=CARTESIAN_POINT('Ctrl Pts',(-9.40449948119461,11.6926055214441,
12.0161790841453));
#122781=CARTESIAN_POINT('Ctrl Pts',(-9.42104261215629,11.6913387120742,
12.025647234455));
#122782=CARTESIAN_POINT('Ctrl Pts',(-9.42713893860623,11.6908723525591,
12.0290646759476));
#122783=CARTESIAN_POINT('Ctrl Pts',(-9.43855173667663,11.689999979859,12.0353295508228));
#122784=CARTESIAN_POINT('Ctrl Pts',(-9.44386038758146,11.6895944707809,
12.0381908111614));
#122785=CARTESIAN_POINT('Ctrl Pts',(-9.45573075577258,11.6886882183188,
12.0444715405973));
#122786=CARTESIAN_POINT('Ctrl Pts',(-9.46230314780352,11.6881867685885,
12.047870173327));
#122787=CARTESIAN_POINT('Ctrl Pts',(-9.48174513550563,11.6867041131371,
12.0576926989053));
#122788=CARTESIAN_POINT('Ctrl Pts',(-9.49470049620781,11.6857170053869,
12.0639428225465));
#122789=CARTESIAN_POINT('Ctrl Pts',(-9.59853530514978,11.677809068555,12.1117121355898));
#122790=CARTESIAN_POINT('Ctrl Pts',(-9.69423296583647,11.6704904530913,
12.1417426824959));
#122791=CARTESIAN_POINT('Ctrl Pts',(-9.84835908816711,11.6590120022976,
12.1693224725322));
#122792=CARTESIAN_POINT('Ctrl Pts',(-9.90482820035644,11.654880916073,12.1752675551682));
#122793=CARTESIAN_POINT('Ctrl Pts',(-9.96840185063562,11.6504484221341,
12.1773462305951));
#122794=CARTESIAN_POINT('Ctrl Pts',(-9.97529421870459,11.6499707885057,
12.1775110274237));
#122795=CARTESIAN_POINT('Ctrl Pts',(-9.98648217224949,11.6492006250307,
12.1776802521799));
#122796=CARTESIAN_POINT('Ctrl Pts',(-9.9907769170129,11.6489062118566,12.1777217176579));
#122797=CARTESIAN_POINT('Ctrl Pts',(-9.99845886655501,11.6483819139084,
12.1777538619372));
#122798=CARTESIAN_POINT('Ctrl Pts',(-10.0018458942518,11.6481515597413,
12.1777534240991));
#122799=CARTESIAN_POINT('Ctrl Pts',(-10.0093110125854,11.6476456463955,
12.1777202545384));
#122800=CARTESIAN_POINT('Ctrl Pts',(-10.013388966867,11.6473704478051,12.1776809541314));
#122801=CARTESIAN_POINT('Ctrl Pts',(-10.0252549566938,11.6465728558468,
12.1775049553073));
#122802=CARTESIAN_POINT('Ctrl Pts',(-10.0330421209843,11.6460534129845,
12.1773121756059));
#122803=CARTESIAN_POINT('Ctrl Pts',(-10.0508847032444,11.6448711830845,
12.1766932852275));
#122804=CARTESIAN_POINT('Ctrl Pts',(-10.060937839997,11.6442108710305,12.1762155138652));
#122805=CARTESIAN_POINT('Ctrl Pts',(-10.1801453303351,11.6364368577523,
12.1690176931791));
#122806=CARTESIAN_POINT('Ctrl Pts',(-10.2878685893985,11.6299235233656,
12.1472544420701));
#122807=CARTESIAN_POINT('Ctrl Pts',(-10.4309949411495,11.6203661613851,
12.0968735333952));
#122808=CARTESIAN_POINT('Ctrl Pts',(-10.470146632485,11.6176560439965,12.0806709661132));
#122809=CARTESIAN_POINT('Ctrl Pts',(-10.5185255479391,11.6141339782369,
12.0575225114229));
#122810=CARTESIAN_POINT('Ctrl Pts',(-10.5286419979848,11.6133876161545,
12.0525018905266));
#122811=CARTESIAN_POINT('Ctrl Pts',(-10.5446875665734,11.6121871408178,
12.0442490549877));
#122812=CARTESIAN_POINT('Ctrl Pts',(-10.5506639616384,11.6117362510378,
12.0411099039856));
#122813=CARTESIAN_POINT('Ctrl Pts',(-10.5619549162205,11.6108770728547,
12.0350548190162));
#122814=CARTESIAN_POINT('Ctrl Pts',(-10.5672746121441,11.610469145213,12.0321488837836));
#122815=CARTESIAN_POINT('Ctrl Pts',(-10.5793500626143,11.6095358801171,
12.0254310003598));
#122816=CARTESIAN_POINT('Ctrl Pts',(-10.5860910056058,11.6090096390513,
12.021593147842));
#122817=CARTESIAN_POINT('Ctrl Pts',(-10.6068139275105,11.6073752272377,
12.0095222590645));
#122818=CARTESIAN_POINT('Ctrl Pts',(-10.6206635399159,11.6062591849552,
12.0010669602879));
#122819=CARTESIAN_POINT('Ctrl Pts',(-10.6525152694905,11.6036352530459,
11.9807061458023));
#122820=CARTESIAN_POINT('Ctrl Pts',(-10.6703731332381,11.6021200593224,
11.9685868483809));
#122821=CARTESIAN_POINT('Ctrl Pts',(-10.735326987072,11.5964423902016,11.9218487286979));
#122822=CARTESIAN_POINT('Ctrl Pts',(-10.7801553403127,11.5921827378486,
11.884232529541));
#122823=CARTESIAN_POINT('Ctrl Pts',(-10.871635127332,11.5828120529406,11.7950788411472));
#122824=CARTESIAN_POINT('Ctrl Pts',(-10.9169056414725,11.5777062882203,
11.7424176065636));
#122825=CARTESIAN_POINT('Ctrl Pts',(-10.963342348769,11.5721128936166,11.6776243170531));
#122826=CARTESIAN_POINT('Ctrl Pts',(-10.9692879906955,11.5713891086367,
11.6690919260951));
#122827=CARTESIAN_POINT('Ctrl Pts',(-10.9776599766469,11.570360057979,11.6567317145132));
#122828=CARTESIAN_POINT('Ctrl Pts',(-10.9801782665281,11.5700491872053,
11.6529671831796));
#122829=CARTESIAN_POINT('Ctrl Pts',(-10.9845582736125,11.5695062670896,
11.6463371749579));
#122830=CARTESIAN_POINT('Ctrl Pts',(-10.9864293288907,11.5692736168557,
11.6434779857766));
#122831=CARTESIAN_POINT('Ctrl Pts',(-10.9903915232622,11.5687794313835,
11.6373653969942));
#122832=CARTESIAN_POINT('Ctrl Pts',(-10.9924791038739,11.568518124435,11.6341098075936));
#122833=CARTESIAN_POINT('Ctrl Pts',(-10.9981922777561,11.5678002278441,
11.6251027609012));
#122834=CARTESIAN_POINT('Ctrl Pts',(-11.0017842334639,11.5673457520091,
11.6193299928529));
#122835=CARTESIAN_POINT('Ctrl Pts',(-11.0223236699117,11.5647266329988,
11.5856740071272));
#122836=CARTESIAN_POINT('Ctrl Pts',(-11.038158195742,11.5626253912577,11.5571245088472));
#122837=CARTESIAN_POINT('Ctrl Pts',(-11.074280868677,11.5575229601613,11.4850922935149));
#122838=CARTESIAN_POINT('Ctrl Pts',(-11.093137695031,11.5545658575668,11.4409584619326));
#122839=CARTESIAN_POINT('Ctrl Pts',(-11.1343591547775,11.5469774721492,
11.325431796728));
#122840=CARTESIAN_POINT('Ctrl Pts',(-11.1527112385436,11.5423407892761,
11.2528469091625));
#122841=CARTESIAN_POINT('Ctrl Pts',(-11.1665110259867,11.5364322625477,
11.1631134822439));
#122842=CARTESIAN_POINT('Ctrl Pts',(-11.1686305574301,11.5353759422225,
11.1471616854395));
#122843=CARTESIAN_POINT('Ctrl Pts',(-11.1712836518244,11.5337971340684,
11.1234886472789));
#122844=CARTESIAN_POINT('Ctrl Pts',(-11.1720690548649,11.5332824315019,
11.1157970850563));
#122845=CARTESIAN_POINT('Ctrl Pts',(-11.1733347591155,11.5323601798707,
11.1020652482584));
#122846=CARTESIAN_POINT('Ctrl Pts',(-11.1738442881375,11.5319535508573,
11.096027895525));
#122847=CARTESIAN_POINT('Ctrl Pts',(-11.1748240914353,11.5310898135671,
11.083241710955));
#122848=CARTESIAN_POINT('Ctrl Pts',(-11.175282843281,11.5306323638384,11.0764922431001));
#122849=CARTESIAN_POINT('Ctrl Pts',(-11.1763560799771,11.5294018839892,
11.0583993417979));
#122850=CARTESIAN_POINT('Ctrl Pts',(-11.1768646212295,11.5286256201298,
11.047050586153));
#122851=CARTESIAN_POINT('Ctrl Pts',(-11.1786985582833,11.5244637888941,
10.9865706553073));
#122852=CARTESIAN_POINT('Ctrl Pts',(-11.1771115125317,11.5209899416152,
10.9374063274741));
#122853=CARTESIAN_POINT('Ctrl Pts',(-11.1677298832601,11.5138452869112,
10.8387639577073));
#122854=CARTESIAN_POINT('Ctrl Pts',(-11.1598420688603,11.5101792909591,
10.7893914178048));
#122855=CARTESIAN_POINT('Ctrl Pts',(-11.1441481672073,11.5049495662789,
10.7198661592634));
#122856=CARTESIAN_POINT('Ctrl Pts',(-11.1388872966125,11.5033861636991,
10.6991914999717));
#122857=CARTESIAN_POINT('Ctrl Pts',(-11.1217262736686,11.4988016062291,
10.638678472675));
#122858=CARTESIAN_POINT('Ctrl Pts',(-11.1082740554659,11.4958071327588,
10.5993100265784));
#122859=CARTESIAN_POINT('Ctrl Pts',(-11.0902436760273,11.4924397732825,
10.5544559066076));
#122860=CARTESIAN_POINT('Ctrl Pts',(-11.0876668533149,11.4919713084939,
10.5482017775917));
#122861=CARTESIAN_POINT('Ctrl Pts',(-11.0833810922463,11.4912129467006,
10.538049154046));
#122862=CARTESIAN_POINT('Ctrl Pts',(-11.0817046920236,11.4909212567509,
10.5341372135572));
#122863=CARTESIAN_POINT('Ctrl Pts',(-11.0786567521532,11.4903998034251,
10.5271298965851));
#122864=CARTESIAN_POINT('Ctrl Pts',(-11.0772930410664,11.4901695934959,
10.5240312739366));
#122865=CARTESIAN_POINT('Ctrl Pts',(-11.0742435335754,11.4896615963059,
10.5171824386257));
#122866=CARTESIAN_POINT('Ctrl Pts',(-11.0725514481381,11.4893841896893,
10.5134351437081));
#122867=CARTESIAN_POINT('Ctrl Pts',(-11.067529607272,11.4885736229485,10.5024672653557));
#122868=CARTESIAN_POINT('Ctrl Pts',(-11.0641462356961,11.4880435618061,
10.4952712788427));
#122869=CARTESIAN_POINT('Ctrl Pts',(-11.0561987926366,11.4868333099497,
10.4788033417617));
#122870=CARTESIAN_POINT('Ctrl Pts',(-11.0515849937768,11.4861557642648,
10.4695559756348));
#122871=CARTESIAN_POINT('Ctrl Pts',(-11.0355099155894,11.4838738785624,
10.4383712746884));
#122872=CARTESIAN_POINT('Ctrl Pts',(-11.023478547636,11.4822956212471,10.4167338254846));
#122873=CARTESIAN_POINT('Ctrl Pts',(-10.9837657092893,11.4774184344919,
10.3503317725675));
#122874=CARTESIAN_POINT('Ctrl Pts',(-10.9537608836166,11.4741862626555,
10.3070321714718));
#122875=CARTESIAN_POINT('Ctrl Pts',(-10.8762133085991,11.466478373831,10.2097476904082));
#122876=CARTESIAN_POINT('Ctrl Pts',(-10.8264344633927,11.4619878827328,
10.1578286485053));
#122877=CARTESIAN_POINT('Ctrl Pts',(-10.7630395090095,11.4564857835986,
10.1027740680207));
#122878=CARTESIAN_POINT('Ctrl Pts',(-10.7537122722784,11.4556815352609,
10.0949246120226));
#122879=CARTESIAN_POINT('Ctrl Pts',(-10.7388282493376,11.4544053144119,
10.0827884140839));
#122880=CARTESIAN_POINT('Ctrl Pts',(-10.7333519480492,11.4539372424099,
10.0784039973656));
#122881=CARTESIAN_POINT('Ctrl Pts',(-10.7230970101861,11.4530632880664,
10.0703430069087));
#122882=CARTESIAN_POINT('Ctrl Pts',(-10.718328655482,11.4526579251219,10.0666536809176));
#122883=CARTESIAN_POINT('Ctrl Pts',(-10.707671741214,11.4517540740552,10.058538353549));
#122884=CARTESIAN_POINT('Ctrl Pts',(-10.7017696004514,11.4512548977326,
10.0541306915479));
#122885=CARTESIAN_POINT('Ctrl Pts',(-10.6843533233893,11.4497857477098,
10.0413771255962));
#122886=CARTESIAN_POINT('Ctrl Pts',(-10.6727292639847,11.4488100336609,
10.0331843023129));
#122887=CARTESIAN_POINT('Ctrl Pts',(-10.6013896376719,11.4428482757219,
9.98481247704116));
#122888=CARTESIAN_POINT('Ctrl Pts',(-10.5382523279102,11.4376683850679,
9.94997315892713));
#122889=CARTESIAN_POINT('Ctrl Pts',(-10.3973679283859,11.4264144039185,
9.88829307529733));
#122890=CARTESIAN_POINT('Ctrl Pts',(-10.3191723352072,11.4203438064807,
9.86337145383154));
#122891=CARTESIAN_POINT('Ctrl Pts',(-10.2296669637638,11.4139425911536,
9.84482062648191));
#122892=CARTESIAN_POINT('Ctrl Pts',(-10.2202903317901,11.4132787433372,
9.84299590170522));
#122893=CARTESIAN_POINT('Ctrl Pts',(-10.2065851413353,11.4123192455857,
9.84050148473441));
#122894=CARTESIAN_POINT('Ctrl Pts',(-10.2022736854918,11.4120189541285,
9.83974158687715));
#122895=CARTESIAN_POINT('Ctrl Pts',(-10.1946076552545,11.4114878916562,
9.83843447270111));
#122896=CARTESIAN_POINT('Ctrl Pts',(-10.1912548237236,11.4112566051693,
9.83787771419009));
#122897=CARTESIAN_POINT('Ctrl Pts',(-10.1839891377179,11.4107575435465,
9.8367034986869));
#122898=CARTESIAN_POINT('Ctrl Pts',(-10.1800755451406,11.4104900571378,
9.8360912613264));
#122899=CARTESIAN_POINT('Ctrl Pts',(-10.1690066092292,11.4097370778158,
9.83441681809528));
#122900=CARTESIAN_POINT('Ctrl Pts',(-10.1618443149665,11.4092540512951,
9.83340074915521));
#122901=CARTESIAN_POINT('Ctrl Pts',(-10.1123660199937,11.4059433222284,
9.82684603568829));
#122902=CARTESIAN_POINT('Ctrl Pts',(-10.069780552609,11.4032248161534,9.82354435486669));
#122903=CARTESIAN_POINT('Ctrl Pts',(-9.95477429478815,11.3960138560923,
9.82089685127928));
#122904=CARTESIAN_POINT('Ctrl Pts',(-9.88248499963884,11.3916117101161,
9.82590104197443));
#122905=CARTESIAN_POINT('Ctrl Pts',(-9.81114930150155,11.3870771460943,
9.83748958018577));
#122906=CARTESIAN_POINT('Ctrl Pts',(-9.81114930150156,11.2872494929995,
9.83748958018577));
#122907=CARTESIAN_POINT('Ctrl Pts',(-9.84737765306304,11.2895573217892,
9.83160425702546));
#122908=CARTESIAN_POINT('Ctrl Pts',(-9.88388323073177,11.2918974625956,
9.82741207842403));
#122909=CARTESIAN_POINT('Ctrl Pts',(-9.93648744901483,11.2953294482307,
9.82385526598519));
#122910=CARTESIAN_POINT('Ctrl Pts',(-9.95244618936399,11.2963783388013,
9.82310201164768));
#122911=CARTESIAN_POINT('Ctrl Pts',(-9.97612035696641,11.2979480795901,
9.82246688166452));
#122912=CARTESIAN_POINT('Ctrl Pts',(-9.9838276837551,11.2984612746864,9.82233581458947));
#122913=CARTESIAN_POINT('Ctrl Pts',(-9.99759026902171,11.2993817573054,
9.8222369012787));
#122914=CARTESIAN_POINT('Ctrl Pts',(-10.0036450934907,11.2997881368981,
9.82224007774416));
#122915=CARTESIAN_POINT('Ctrl Pts',(-10.0164745205632,11.3006523282061,
9.82234573991638));
#122916=CARTESIAN_POINT('Ctrl Pts',(-10.0232487790928,11.3011104886817,
9.82245999767215));
#122917=CARTESIAN_POINT('Ctrl Pts',(-10.0414303567718,11.3023452979655,
9.82292360764631));
#122918=CARTESIAN_POINT('Ctrl Pts',(-10.0528339655797,11.3031252216827,
9.82338032308687));
#122919=CARTESIAN_POINT('Ctrl Pts',(-10.1142520899508,11.3073564423581,
9.82673476292573));
#122920=CARTESIAN_POINT('Ctrl Pts',(-10.1640431863648,11.3108996521448,
9.83265537772922));
#122921=CARTESIAN_POINT('Ctrl Pts',(-10.2617303421977,11.3180671460305,
9.85064484445307));
#122922=CARTESIAN_POINT('Ctrl Pts',(-10.309550676165,11.3216819135494,9.86259157721101));
#122923=CARTESIAN_POINT('Ctrl Pts',(-10.3785054858079,11.3269902754965,
9.88448993357294));
#122924=CARTESIAN_POINT('Ctrl Pts',(-10.4003207728054,11.3286838311987,
9.89213158164503));
#122925=CARTESIAN_POINT('Ctrl Pts',(-10.4588805260113,11.3332499026083,
9.91460015488255));
#122926=CARTESIAN_POINT('Ctrl Pts',(-10.4951283317902,11.3360985983244,
9.93064843363919));
#122927=CARTESIAN_POINT('Ctrl Pts',(-10.5370345252153,11.3393671864089,
9.95179080266278));
#122928=CARTESIAN_POINT('Ctrl Pts',(-10.5435366569285,11.339873580824,9.95514761234966));
#122929=CARTESIAN_POINT('Ctrl Pts',(-10.5535647013223,11.3406529234632,
9.96044366727162));
#122930=CARTESIAN_POINT('Ctrl Pts',(-10.5571125371895,11.3409283238183,
9.96234067749375));
#122931=CARTESIAN_POINT('Ctrl Pts',(-10.5636320683037,11.3414337067903,
9.96586971446952));
#122932=CARTESIAN_POINT('Ctrl Pts',(-10.5666064507902,11.3416639967443,
9.96749639888724));
#122933=CARTESIAN_POINT('Ctrl Pts',(-10.5733913623308,11.3421887127709,
9.97124520410875));
#122934=CARTESIAN_POINT('Ctrl Pts',(-10.5771971655063,11.3424826121209,
9.97337566845887));
#122935=CARTESIAN_POINT('Ctrl Pts',(-10.5890099645021,11.3433937960387,
9.98007485245793));
#122936=CARTESIAN_POINT('Ctrl Pts',(-10.5969754435782,11.3440067080817,
9.98471660235024));
#122937=CARTESIAN_POINT('Ctrl Pts',(-10.6156245664929,11.3454401073032,
9.99587944344701));
#122938=CARTESIAN_POINT('Ctrl Pts',(-10.6262605592423,11.3462563659961,
10.0024783522059));
#122939=CARTESIAN_POINT('Ctrl Pts',(-10.6647318611005,11.3492119686065,
10.0272051036391));
#122940=CARTESIAN_POINT('Ctrl Pts',(-10.6919037488671,11.3513057926237,
10.0463397482413));
#122941=CARTESIAN_POINT('Ctrl Pts',(-10.7793868342499,11.3581939011251,
10.1136560958946));
#122942=CARTESIAN_POINT('Ctrl Pts',(-10.8357674185423,11.3628914289487,
10.166608049354));
#122943=CARTESIAN_POINT('Ctrl Pts',(-10.9110578605448,11.3701295113591,
10.2527028130505));
#122944=CARTESIAN_POINT('Ctrl Pts',(-10.9342085710923,11.3725206633456,
10.2818541695447));
#122945=CARTESIAN_POINT('Ctrl Pts',(-10.9623187454,11.3756835687085,10.3209146080355));
#122946=CARTESIAN_POINT('Ctrl Pts',(-10.968574328312,11.3764057774505,10.3298671066322));
#122947=CARTESIAN_POINT('Ctrl Pts',(-10.9784476832123,11.3775765091303,
10.3444241715335));
#122948=CARTESIAN_POINT('Ctrl Pts',(-10.9821440160531,11.3780220883544,
10.3499748741026));
#122949=CARTESIAN_POINT('Ctrl Pts',(-10.989119077439,11.3788771761367,10.3606444938674));
#122950=CARTESIAN_POINT('Ctrl Pts',(-10.9924057139585,11.379286375225,10.365758004305));
#122951=CARTESIAN_POINT('Ctrl Pts',(-10.9998761760139,11.3802312349034,
10.3775811565477));
#122952=CARTESIAN_POINT('Ctrl Pts',(-11.0040322698802,11.3807678829423,
10.3843078855408));
#122953=CARTESIAN_POINT('Ctrl Pts',(-11.0169328871182,11.3824692034622,
10.4056658370025));
#122954=CARTESIAN_POINT('Ctrl Pts',(-11.025427352653,11.3836427088733,10.4204447514974));
#122955=CARTESIAN_POINT('Ctrl Pts',(-11.0446332872541,11.3864272842217,
10.4556046635634));
#122956=CARTESIAN_POINT('Ctrl Pts',(-11.0550734578732,11.3880469536531,
10.4761251440827));
#122957=CARTESIAN_POINT('Ctrl Pts',(-11.1158941464383,11.3981747865419,
10.6048730140338));
#122958=CARTESIAN_POINT('Ctrl Pts',(-11.1501694862814,11.4071725039487,
10.7199125012477));
#122959=CARTESIAN_POINT('Ctrl Pts',(-11.1685549326109,11.4166392397871,
10.8524113895528));
#122960=CARTESIAN_POINT('Ctrl Pts',(-11.17027458303,11.4176497058772,10.8667315675298));
#122961=CARTESIAN_POINT('Ctrl Pts',(-11.172272172983,11.4190180611896,10.8864141054624));
#122962=CARTESIAN_POINT('Ctrl Pts',(-11.1727770738069,11.4193870614828,
10.8917514854352));
#122963=CARTESIAN_POINT('Ctrl Pts',(-11.173525067366,11.4199731503686,10.9002793186423));
#122964=CARTESIAN_POINT('Ctrl Pts',(-11.1737916281222,11.4201914906954,
10.903467557794));
#122965=CARTESIAN_POINT('Ctrl Pts',(-11.1743238849418,11.4206482720651,
10.9101621448309));
#122966=CARTESIAN_POINT('Ctrl Pts',(-11.1745868751823,11.4208865525349,
10.9136686608159));
#122967=CARTESIAN_POINT('Ctrl Pts',(-11.1751990015863,11.4214742877395,
10.9223515302462));
#122968=CARTESIAN_POINT('Ctrl Pts',(-11.1755296520104,11.4218227402786,
10.9275291926398));
#122969=CARTESIAN_POINT('Ctrl Pts',(-11.1766441184479,11.423126302074,10.947003097274));
#122970=CARTESIAN_POINT('Ctrl Pts',(-11.1772014760199,11.4240699014457,
10.961311721003));
#122971=CARTESIAN_POINT('Ctrl Pts',(-11.1779669827714,11.4264803765638,
10.9982956403654));
#122972=CARTESIAN_POINT('Ctrl Pts',(-11.1777815345476,11.4279308704364,
11.0209738158883));
#122973=CARTESIAN_POINT('Ctrl Pts',(-11.1739088223258,11.4345415591004,
11.1254330503157));
#122974=CARTESIAN_POINT('Ctrl Pts',(-11.1623569097417,11.4394997797624,
11.2066954818918));
#122975=CARTESIAN_POINT('Ctrl Pts',(-11.1310138725775,11.4475945646869,
11.3318534979501));
#122976=CARTESIAN_POINT('Ctrl Pts',(-11.1168213836361,11.450601323583,11.3768664737534));
#122977=CARTESIAN_POINT('Ctrl Pts',(-11.0958245075684,11.4544571393744,
11.4317386765184));
#122978=CARTESIAN_POINT('Ctrl Pts',(-11.0915189657757,11.4552234156293,
11.4425109805742));
#122979=CARTESIAN_POINT('Ctrl Pts',(-11.0844322685834,11.4564482734834,
11.4595086216701));
#122980=CARTESIAN_POINT('Ctrl Pts',(-11.0817548970428,11.456903391947,11.4657766181));
#122981=CARTESIAN_POINT('Ctrl Pts',(-11.0768418599362,11.4577252592851,
11.4770076492949));
#122982=CARTESIAN_POINT('Ctrl Pts',(-11.074625890852,11.4580913354805,11.4819791300507));
#122983=CARTESIAN_POINT('Ctrl Pts',(-11.0693381116814,11.4589542879358,
11.4936243911195));
#122984=CARTESIAN_POINT('Ctrl Pts',(-11.0662381873348,11.4594521073703,
11.500285078974));
#122985=CARTESIAN_POINT('Ctrl Pts',(-11.056994662952,11.4609136362439,11.5196700796031));
#122986=CARTESIAN_POINT('Ctrl Pts',(-11.0506843346093,11.4618829974824,
11.5323129794422));
#122987=CARTESIAN_POINT('Ctrl Pts',(-11.0358012395096,11.4641078965645,
11.5608354666634));
#122988=CARTESIAN_POINT('Ctrl Pts',(-11.0270880674437,11.4653680292247,
11.5766373816398));
#122989=CARTESIAN_POINT('Ctrl Pts',(-10.9962096752762,11.4696962733487,
11.6297156994075));
#122990=CARTESIAN_POINT('Ctrl Pts',(-10.9723521561183,11.4728178054089,
11.6659626106579));
#122991=CARTESIAN_POINT('Ctrl Pts',(-10.9101071357254,11.4804393990128,
11.7500343470243));
#122992=CARTESIAN_POINT('Ctrl Pts',(-10.8698777641322,11.4849685248226,
11.7963410656411));
#122993=CARTESIAN_POINT('Ctrl Pts',(-10.8012883862133,11.4919522840426,
11.8638616262008));
#122994=CARTESIAN_POINT('Ctrl Pts',(-10.7752621139751,11.4944592893511,
11.8872931541492));
#122995=CARTESIAN_POINT('Ctrl Pts',(-10.7427274959838,11.4973913356088,
11.9140578015892));
#122996=CARTESIAN_POINT('Ctrl Pts',(-10.7371856497686,11.4978840667946,
11.9185331360155));
#122997=CARTESIAN_POINT('Ctrl Pts',(-10.7284847002826,11.4986468612334,
11.925430138526));
#122998=CARTESIAN_POINT('Ctrl Pts',(-10.7253534586762,11.4989192205252,
11.9278864483328));
#122999=CARTESIAN_POINT('Ctrl Pts',(-10.7195279406223,11.4994218692902,
11.9324087792665));
#123000=CARTESIAN_POINT('Ctrl Pts',(-10.7168371780232,11.4996524391839,
11.9344790257941));
#123001=CARTESIAN_POINT('Ctrl Pts',(-10.7106213271886,11.5001814461097,
11.93921879393));
#123002=CARTESIAN_POINT('Ctrl Pts',(-10.7070901203066,11.5004793219339,
11.9418801287149));
#123003=CARTESIAN_POINT('Ctrl Pts',(-10.6958939667679,11.5014157359894,
11.9502197857745));
#123004=CARTESIAN_POINT('Ctrl Pts',(-10.6881747505092,11.5020495482404,
11.9558250787929));
#123005=CARTESIAN_POINT('Ctrl Pts',(-10.6474206251142,11.5053395038155,
11.9846689086053));
#123006=CARTESIAN_POINT('Ctrl Pts',(-10.6132712003313,11.5079055495045,
12.006292926449));
#123007=CARTESIAN_POINT('Ctrl Pts',(-10.4948425329033,11.5164166735068,
12.0730107881803));
#123008=CARTESIAN_POINT('Ctrl Pts',(-10.4062185334783,11.5221906341204,
12.1095980781174));
#123009=CARTESIAN_POINT('Ctrl Pts',(-10.2887057980497,11.5300029672657,
12.1421212301156));
#123010=CARTESIAN_POINT('Ctrl Pts',(-10.2630358667609,11.5317160423217,
12.1483047982117));
#123011=CARTESIAN_POINT('Ctrl Pts',(-10.2277561606616,11.534090457461,12.1555582123499));
#123012=CARTESIAN_POINT('Ctrl Pts',(-10.2183078612519,11.5347282606841,
12.157380369424));
#123013=CARTESIAN_POINT('Ctrl Pts',(-10.2031777601195,11.535753128282,12.1601064368247));
#123014=CARTESIAN_POINT('Ctrl Pts',(-10.1975096900724,11.5361378501152,
12.1610848665412));
#123015=CARTESIAN_POINT('Ctrl Pts',(-10.1857971963802,11.5369345662467,
12.1630184478343));
#123016=CARTESIAN_POINT('Ctrl Pts',(-10.179752052067,11.5373467199077,12.1639680861339));
#123017=CARTESIAN_POINT('Ctrl Pts',(-10.1656010048259,11.5383138699707,
12.1660782220364));
#123018=CARTESIAN_POINT('Ctrl Pts',(-10.1574899393363,11.5388700112702,
12.1672013647407));
#123019=CARTESIAN_POINT('Ctrl Pts',(-10.1308804302874,11.5407007349562,
12.1706035848899));
#123020=CARTESIAN_POINT('Ctrl Pts',(-10.1123403324389,11.5419861674889,
12.1725280470613));
#123021=CARTESIAN_POINT('Ctrl Pts',(-10.0463734096412,11.5465973844078,
12.1777965410393));
#123022=CARTESIAN_POINT('Ctrl Pts',(-9.99880352294367,11.5499936547528,
12.1787081006965));
#123023=CARTESIAN_POINT('Ctrl Pts',(-9.87540882230567,11.5589582085281,
12.1736027842035));
#123024=CARTESIAN_POINT('Ctrl Pts',(-9.79998893187672,11.5645986856286,
12.1631258146078));
#123025=CARTESIAN_POINT('Ctrl Pts',(-9.69886376144277,11.5720955987445,
12.1389453515556));
#123026=CARTESIAN_POINT('Ctrl Pts',(-9.67186149244443,11.5740888713974,
12.1314614224299));
#123027=CARTESIAN_POINT('Ctrl Pts',(-9.63875764468439,11.5765019656518,
12.121001319763));
#123028=CARTESIAN_POINT('Ctrl Pts',(-9.6323829091429,11.5769652116153,12.1189270208291));
#123029=CARTESIAN_POINT('Ctrl Pts',(-9.62234252296618,11.5776921852624,
12.1155648714268));
#123030=CARTESIAN_POINT('Ctrl Pts',(-9.61866505518231,11.5779578867409,
12.1143131576352));
#123031=CARTESIAN_POINT('Ctrl Pts',(-9.61176952407692,11.578454945639,12.1119279651843));
#123032=CARTESIAN_POINT('Ctrl Pts',(-9.60855020269497,11.5786865231849,
12.1107987030642));
#123033=CARTESIAN_POINT('Ctrl Pts',(-9.6010260105442,11.5792266930345,12.1081226201327));
#123034=CARTESIAN_POINT('Ctrl Pts',(-9.59672518649246,11.5795346370998,
12.1065646894959));
#123035=CARTESIAN_POINT('Ctrl Pts',(-9.58269378679182,11.5805369654304,
12.1013892834332));
#123036=CARTESIAN_POINT('Ctrl Pts',(-9.57300162682791,11.5812256337594,
12.0976680903849));
#123037=CARTESIAN_POINT('Ctrl Pts',(-9.5184848746513,11.5850851702012,12.0759056065092));
#123038=CARTESIAN_POINT('Ctrl Pts',(-9.47474970872814,11.5881280663859,
12.0552454188835));
#123039=CARTESIAN_POINT('Ctrl Pts',(-9.35756823855235,11.5964521188397,
11.9907931234771));
#123040=CARTESIAN_POINT('Ctrl Pts',(-9.28743670762614,11.6016514627571,
11.941616979577));
#123041=CARTESIAN_POINT('Ctrl Pts',(-9.20286309537365,11.6088539030606,
11.8674114858105));
#123042=CARTESIAN_POINT('Ctrl Pts',(-9.18311095506994,11.610611865583,11.8488356970984));
#123043=CARTESIAN_POINT('Ctrl Pts',(-9.1571719101485,11.613038909656,11.8226969945064));
#123044=CARTESIAN_POINT('Ctrl Pts',(-9.15041133136488,11.6136830442357,
11.8157135640854));
#123045=CARTESIAN_POINT('Ctrl Pts',(-9.13977623696417,11.6147154896804,
11.8044522583644));
#123046=CARTESIAN_POINT('Ctrl Pts',(-9.1358452959118,11.6151013927654,11.8002280949062));
#123047=CARTESIAN_POINT('Ctrl Pts',(-9.12781650904053,11.6158985999246,
11.7914722656048));
#123048=CARTESIAN_POINT('Ctrl Pts',(-9.12372257469971,11.6163100503583,
11.7869372660002));
#123049=CARTESIAN_POINT('Ctrl Pts',(-9.11426674051005,11.6172721449325,
11.7762974124336));
#123050=CARTESIAN_POINT('Ctrl Pts',(-9.10893241836143,11.6178238982919,
11.7701685781332));
#123051=CARTESIAN_POINT('Ctrl Pts',(-9.0918100279115,11.6196248991335,11.7500799050643));
#123052=CARTESIAN_POINT('Ctrl Pts',(-9.08028379731052,11.6208845143538,
11.7359014412764));
#123053=CARTESIAN_POINT('Ctrl Pts',(-9.02120635476934,11.6276006886583,
11.6596733291351));
#123054=CARTESIAN_POINT('Ctrl Pts',(-8.9795984126393,11.6332786326552,11.5932812812547));
#123055=CARTESIAN_POINT('Ctrl Pts',(-8.91464383613043,11.6440048148759,
11.4623069537105));
#123056=CARTESIAN_POINT('Ctrl Pts',(-8.88974766899018,11.6490145302144,
11.3988322295689));
#123057=CARTESIAN_POINT('Ctrl Pts',(-8.86779844645613,11.6544532113663,
11.3245054614217));
#123058=CARTESIAN_POINT('Ctrl Pts',(-8.8652340559233,11.6551107690279,11.3154210173819));
#123059=CARTESIAN_POINT('Ctrl Pts',(-8.86147720265792,11.6561084296883,
11.301472982271));
#123060=CARTESIAN_POINT('Ctrl Pts',(-8.86020614117336,11.6564525594978,
11.2966312201322));
#123061=CARTESIAN_POINT('Ctrl Pts',(-8.85811213037243,11.6570307266812,
11.2884424265208));
#123062=CARTESIAN_POINT('Ctrl Pts',(-8.8572729420207,11.6572656609644,11.2850996534163));
#123063=CARTESIAN_POINT('Ctrl Pts',(-8.85556675661982,11.6577500551445,
11.2781747583257));
#123064=CARTESIAN_POINT('Ctrl Pts',(-8.85470188250704,11.657999396056,11.2745921843961));
#123065=CARTESIAN_POINT('Ctrl Pts',(-8.85247921495593,11.658650478696,11.2651920007702));
#123066=CARTESIAN_POINT('Ctrl Pts',(-8.85114882102701,11.6590507122057,
11.2593679272472));
#123067=CARTESIAN_POINT('Ctrl Pts',(-8.84529792086333,11.6608614141788,
11.2328257569416));
#123068=CARTESIAN_POINT('Ctrl Pts',(-8.84129283448115,11.6622456486791,
11.2119966110721));
#123069=CARTESIAN_POINT('Ctrl Pts',(-8.83120988733393,11.6662443009451,
11.1506686885803));
#123070=CARTESIAN_POINT('Ctrl Pts',(-8.8266783404924,11.6688025740083,11.1099461855073));
#123071=CARTESIAN_POINT('Ctrl Pts',(-8.81858974836313,11.6773615717492,
10.9722559879378));
#123072=CARTESIAN_POINT('Ctrl Pts',(-8.82488134758213,11.6832828811689,
10.8751236524719));
#123073=CARTESIAN_POINT('Ctrl Pts',(-8.84547627315186,11.6904714295353,
10.766880497118));
#123074=CARTESIAN_POINT('Ctrl Pts',(-8.84816488988286,11.6913399246038,
10.7539398548229));
#123075=CARTESIAN_POINT('Ctrl Pts',(-8.85280171489664,11.6927366039603,
10.7333670216105));
#123076=CARTESIAN_POINT('Ctrl Pts',(-8.85460974623558,11.6932603915929,
10.7257041522808));
#123077=CARTESIAN_POINT('Ctrl Pts',(-8.85795291110962,11.6941938282056,
10.7121447796497));
#123078=CARTESIAN_POINT('Ctrl Pts',(-8.85945724162704,11.6946024867538,
10.7062409234189));
#123079=CARTESIAN_POINT('Ctrl Pts',(-8.86269186422105,11.6954583297614,
10.6939459110035));
#123080=CARTESIAN_POINT('Ctrl Pts',(-8.86443037680246,11.6959057640935,
10.6875571590109));
#123081=CARTESIAN_POINT('Ctrl Pts',(-8.86911936164415,11.6970808974177,
10.6708821589855));
#123082=CARTESIAN_POINT('Ctrl Pts',(-8.87215626215684,11.6978113402741,
10.6606210651866));
#123083=CARTESIAN_POINT('Ctrl Pts',(-8.88710455624572,11.7012701546579,
10.6125317967769));
#123084=CARTESIAN_POINT('Ctrl Pts',(-8.90078065262895,11.7040546783059,
10.5752835335413));
#123085=CARTESIAN_POINT('Ctrl Pts',(-8.95068483610588,11.7131663121917,
10.458022696459));
#123086=CARTESIAN_POINT('Ctrl Pts',(-8.99398468694034,11.7196859427481,
10.3813464724914));
#123087=CARTESIAN_POINT('Ctrl Pts',(-9.06664531773832,11.7286966156065,
10.2807914684039));
#123088=CARTESIAN_POINT('Ctrl Pts',(-9.08924909719492,11.7312988749648,
10.2523736130383));
#123089=CARTESIAN_POINT('Ctrl Pts',(-9.11785583177452,11.7343251456023,
10.21963580256));
#123090=CARTESIAN_POINT('Ctrl Pts',(-9.12262971704901,11.7348218905809,
10.2142723072423));
#123091=CARTESIAN_POINT('Ctrl Pts',(-9.13013404744714,11.7355895498571,
10.205994819601));
#123092=CARTESIAN_POINT('Ctrl Pts',(-9.13283066776027,11.7358628056026,
10.2030505961355));
#123093=CARTESIAN_POINT('Ctrl Pts',(-9.13784696551319,11.7363662498549,
10.1976293105576));
#123094=CARTESIAN_POINT('Ctrl Pts',(-9.14016238147055,11.7365967267529,
10.1951485550823));
#123095=CARTESIAN_POINT('Ctrl Pts',(-9.14550698442549,11.7371244220209,
10.1894716918284));
#123096=CARTESIAN_POINT('Ctrl Pts',(-9.14854340469529,11.7374210896485,
10.1862825306759));
#123097=CARTESIAN_POINT('Ctrl Pts',(-9.15814594165178,11.7383497920389,
10.1763095618233));
#123098=CARTESIAN_POINT('Ctrl Pts',(-9.16477597425506,11.7389772103389,
10.1695874313731));
#123099=CARTESIAN_POINT('Ctrl Pts',(-9.19958163621376,11.742204983061,10.1351369088079));
#123100=CARTESIAN_POINT('Ctrl Pts',(-9.22906223050449,11.7447189675293,
10.1087574198106));
#123101=CARTESIAN_POINT('Ctrl Pts',(-9.33126768899329,11.7529528192789,
10.0261775106796));
#123102=CARTESIAN_POINT('Ctrl Pts',(-9.40922467466743,11.7585083363272,
9.97700540371097));
#123103=CARTESIAN_POINT('Ctrl Pts',(-9.51924025581333,11.7662860210077,
9.92442122786862));
#123104=CARTESIAN_POINT('Ctrl Pts',(-9.54686074132296,11.7682311333758,
9.91249634420751));
#123105=CARTESIAN_POINT('Ctrl Pts',(-9.58431589752778,11.7708757963589,
9.89800017810766));
#123106=CARTESIAN_POINT('Ctrl Pts',(-9.59377235482036,11.7715440415593,
9.89447932158377));
#123107=CARTESIAN_POINT('Ctrl Pts',(-9.60938298536954,11.7726486234302,
9.88889445805193));
#123108=CARTESIAN_POINT('Ctrl Pts',(-9.61551117991129,11.7730826059062,
9.88675900100521));
#123109=CARTESIAN_POINT('Ctrl Pts',(-9.62747493976373,11.7739307019252,
9.88270062628271));
#123110=CARTESIAN_POINT('Ctrl Pts',(-9.6333085304097,11.7743446300591,9.88077250985911));
#123111=CARTESIAN_POINT('Ctrl Pts',(-9.64709703031774,11.7753240626958,
9.87633450959071));
#123112=CARTESIAN_POINT('Ctrl Pts',(-9.65506395787159,11.7758907989115,
9.87386334710656));
#123113=CARTESIAN_POINT('Ctrl Pts',(-9.68178563886909,11.7777948077483,
9.86588504009686));
#123114=CARTESIAN_POINT('Ctrl Pts',(-9.70065026233228,11.7791441691292,
9.86076043892263));
#123115=CARTESIAN_POINT('Ctrl Pts',(-9.74989433953818,11.7826819746355,
9.84869074533714));
#123116=CARTESIAN_POINT('Ctrl Pts',(-9.78042408017642,11.7848906446434,
9.84248091566963));
#123117=CARTESIAN_POINT('Ctrl Pts',(-9.81114930150157,11.7871268320303,
9.83748958018577));
#123118=CARTESIAN_POINT('Origin',(-10.,2.67563288526385,11.));
#123119=CARTESIAN_POINT('',(-9.81114930150157,12.3872370429983,9.83748958018577));
#123120=CARTESIAN_POINT('',(-9.81114930148955,12.2889045666398,9.83748958018772));
#123121=CARTESIAN_POINT('',(-9.81114930150157,2.67563288526385,9.83748958018577));
#123122=CARTESIAN_POINT('Ctrl Pts',(-9.81114930150156,12.3872370429983,
9.83748958018577));
#123123=CARTESIAN_POINT('Ctrl Pts',(-9.76160618676258,12.3836299704724,
9.84553789671247));
#123124=CARTESIAN_POINT('Ctrl Pts',(-9.71259593242639,12.3799506740213,
9.85675028810344));
#123125=CARTESIAN_POINT('Ctrl Pts',(-9.60051589314023,12.3713694093543,
9.89006659515214));
#123126=CARTESIAN_POINT('Ctrl Pts',(-9.5383324439195,12.3664776583828,9.91445648855665));
#123127=CARTESIAN_POINT('Ctrl Pts',(-9.47156323397072,12.3612864710941,
9.9474268553019));
#123128=CARTESIAN_POINT('Ctrl Pts',(-9.46461859660247,12.3607474111369,
9.95094213619925));
#123129=CARTESIAN_POINT('Ctrl Pts',(-9.45409035715892,12.3599320821303,
9.95640317032562));
#123130=CARTESIAN_POINT('Ctrl Pts',(-9.45048132415873,12.3596529347779,
9.95829903176879));
#123131=CARTESIAN_POINT('Ctrl Pts',(-9.44389215466269,12.3591440130093,
9.96180416266418));
#123132=CARTESIAN_POINT('Ctrl Pts',(-9.44090909019244,12.3589138987812,
9.96340755961084));
#123133=CARTESIAN_POINT('Ctrl Pts',(-9.43415813589313,12.3583937505195,
9.9670738176633));
#123134=CARTESIAN_POINT('Ctrl Pts',(-9.43039458061039,12.3581042050758,
9.96914444222949));
#123135=CARTESIAN_POINT('Ctrl Pts',(-9.42061782363,12.3573529379019,9.97459328799913));
#123136=CARTESIAN_POINT('Ctrl Pts',(-9.4146227179992,12.3568931521619,9.9780038774287));
#123137=CARTESIAN_POINT('Ctrl Pts',(-9.35929643656635,12.3526549918194,
10.0101253393834));
#123138=CARTESIAN_POINT('Ctrl Pts',(-9.31207660422203,12.3490731043331,
10.0423382167819));
#123139=CARTESIAN_POINT('Ctrl Pts',(-9.21382384177081,12.3412796944708,
10.120397932985));
#123140=CARTESIAN_POINT('Ctrl Pts',(-9.16408324747363,12.3370940171404,
10.1675244238099));
#123141=CARTESIAN_POINT('Ctrl Pts',(-9.09359345634885,12.3303691242148,
10.2470350989005));
#123142=CARTESIAN_POINT('Ctrl Pts',(-9.06985658776819,12.3279348188222,
10.2765625456223));
#123143=CARTESIAN_POINT('Ctrl Pts',(-9.04137712998696,12.3247502769696,
10.3157130677671));
#123144=CARTESIAN_POINT('Ctrl Pts',(-9.03528482380032,12.3240520331408,
10.3243292003439));
#123145=CARTESIAN_POINT('Ctrl Pts',(-9.02557750442845,12.3229106656835,
10.3384568907643));
#123146=CARTESIAN_POINT('Ctrl Pts',(-9.02189144904224,12.3224702177506,
10.3439191019275));
#123147=CARTESIAN_POINT('Ctrl Pts',(-9.01487952046986,12.321618455429,10.3545002208894));
#123148=CARTESIAN_POINT('Ctrl Pts',(-9.01154721912971,12.3212073970195,
10.3596146303947));
#123149=CARTESIAN_POINT('Ctrl Pts',(-9.00396891372762,12.3202578312103,
10.3714458814049));
#123150=CARTESIAN_POINT('Ctrl Pts',(-8.99975086971297,12.3197183242605,
10.3781801894225));
#123151=CARTESIAN_POINT('Ctrl Pts',(-8.98633682708029,12.3179662054654,
10.400086032539));
#123152=CARTESIAN_POINT('Ctrl Pts',(-8.97741576718902,12.3167438485322,
10.4154221830435));
#123153=CARTESIAN_POINT('Ctrl Pts',(-8.90792220272462,12.3067358560587,
10.5413497053976));
#123154=CARTESIAN_POINT('Ctrl Pts',(-8.8651307789173,12.2972936991391,10.6608064093586));
#123155=CARTESIAN_POINT('Ctrl Pts',(-8.83872097472247,12.2868863269254,
10.8028545894888));
#123156=CARTESIAN_POINT('Ctrl Pts',(-8.83577568455388,12.2855693372387,
10.8210667549098));
#123157=CARTESIAN_POINT('Ctrl Pts',(-8.83157646988353,12.2834004419215,
10.8515624724007));
#123158=CARTESIAN_POINT('Ctrl Pts',(-8.8300856969844,12.282539125307,10.8638096958764));
#123159=CARTESIAN_POINT('Ctrl Pts',(-8.82827216159539,12.281349273821,10.8809498861448));
#123160=CARTESIAN_POINT('Ctrl Pts',(-8.82778714093373,12.281012647343,10.8858243805658));
#123161=CARTESIAN_POINT('Ctrl Pts',(-8.82701126419884,12.2804409248086,
10.894148817342));
#123162=CARTESIAN_POINT('Ctrl Pts',(-8.82670518463172,12.2802050107709,
10.8975972427542));
#123163=CARTESIAN_POINT('Ctrl Pts',(-8.8261004356901,12.2797163121981,10.9047695897608));
#123164=CARTESIAN_POINT('Ctrl Pts',(-8.82580427299882,12.2794636643636,
10.9084936407075));
#123165=CARTESIAN_POINT('Ctrl Pts',(-8.82506383113207,12.2787943266036,
10.9184004641199));
#123166=CARTESIAN_POINT('Ctrl Pts',(-8.82465062681548,12.2783793015423,
10.9245855433403));
#123167=CARTESIAN_POINT('Ctrl Pts',(-8.82304265437537,12.2765582970677,
10.9518947740142));
#123168=CARTESIAN_POINT('Ctrl Pts',(-8.82236831893546,12.2751780967448,
10.9730470419396));
#123169=CARTESIAN_POINT('Ctrl Pts',(-8.82176079990173,12.2672352272143,
11.096568239539));
#123170=CARTESIAN_POINT('Ctrl Pts',(-8.83460347680853,12.2611097242201,
11.1985648931698));
#123171=CARTESIAN_POINT('Ctrl Pts',(-8.86748809725854,12.2529048434168,
11.3244716322836));
#123172=CARTESIAN_POINT('Ctrl Pts',(-8.87544655877457,12.2511365022331,
11.3510618857467));
#123173=CARTESIAN_POINT('Ctrl Pts',(-8.89061932964242,12.2480717700565,
11.3959219253569));
#123174=CARTESIAN_POINT('Ctrl Pts',(-8.89736519180978,12.2467895917852,
11.414338087863));
#123175=CARTESIAN_POINT('Ctrl Pts',(-8.907635585877,12.2449398987945,11.4403462653681));
#123176=CARTESIAN_POINT('Ctrl Pts',(-8.9107863294314,12.2443846683976,11.4480830509423));
#123177=CARTESIAN_POINT('Ctrl Pts',(-8.9163981836012,12.243416063109,11.4614541799711));
#123178=CARTESIAN_POINT('Ctrl Pts',(-8.91882163285402,12.2430039581116,
11.4671040491092));
#123179=CARTESIAN_POINT('Ctrl Pts',(-8.92358150785358,12.2422061301025,
11.4779653839331));
#123180=CARTESIAN_POINT('Ctrl Pts',(-8.92591183119203,12.2418206223042,
11.4831793477809));
#123181=CARTESIAN_POINT('Ctrl Pts',(-8.93217599057848,12.2407974642004,
11.4969257729409));
#123182=CARTESIAN_POINT('Ctrl Pts',(-8.93617409987834,12.2401576483642,
11.5054283176445));
#123183=CARTESIAN_POINT('Ctrl Pts',(-8.95107974154006,12.2378185686096,
11.5361667120886));
#123184=CARTESIAN_POINT('Ctrl Pts',(-8.96258555552996,12.2360990675684,
11.5581035419926));
#123185=CARTESIAN_POINT('Ctrl Pts',(-9.02848478904072,12.2266815042326,
11.6746574360618));
#123186=CARTESIAN_POINT('Ctrl Pts',(-9.09513620131377,12.2185489611787,
11.7617206611963));
#123187=CARTESIAN_POINT('Ctrl Pts',(-9.19654843196857,12.2082290057327,
11.8617856141624));
#123188=CARTESIAN_POINT('Ctrl Pts',(-9.22129259980168,12.2058433375341,
11.8842081768844));
#123189=CARTESIAN_POINT('Ctrl Pts',(-9.25221649396252,12.2030473209367,
11.9099239861014));
#123190=CARTESIAN_POINT('Ctrl Pts',(-9.25751291115199,12.2025746835896,
11.9142509288193));
#123191=CARTESIAN_POINT('Ctrl Pts',(-9.26586999042197,12.2018390284918,
11.9209577715589));
#123192=CARTESIAN_POINT('Ctrl Pts',(-9.26890512099231,12.2015739104187,
11.9233690307438));
#123193=CARTESIAN_POINT('Ctrl Pts',(-9.27463657024989,12.2010772123813,
11.9278764034622));
#123194=CARTESIAN_POINT('Ctrl Pts',(-9.27733009134492,12.2008454184038,
11.929975767847));
#123195=CARTESIAN_POINT('Ctrl Pts',(-9.28360515273213,12.2003091217246,
11.9348229037928));
#123196=CARTESIAN_POINT('Ctrl Pts',(-9.28719340575597,12.2000052274908,
11.937561837704));
#123197=CARTESIAN_POINT('Ctrl Pts',(-9.29903021931046,12.1990114978714,
11.9464897080238));
#123198=CARTESIAN_POINT('Ctrl Pts',(-9.30734459172771,12.198327322217,11.9525911525848));
#123199=CARTESIAN_POINT('Ctrl Pts',(-9.37380488351564,12.1929575165845,
12.0000322548688));
#123200=CARTESIAN_POINT('Ctrl Pts',(-9.43552586671782,12.188558202979,12.0361257586735));
#123201=CARTESIAN_POINT('Ctrl Pts',(-9.55181707138373,12.1806135455869,
12.090634733429));
#123202=CARTESIAN_POINT('Ctrl Pts',(-9.60518201256105,12.1770845328358,
12.1110671480051));
#123203=CARTESIAN_POINT('Ctrl Pts',(-9.68019777018182,12.1720942643174,
12.1336996489631));
#123204=CARTESIAN_POINT('Ctrl Pts',(-9.70074309402364,12.1707251744367,
12.1392952137203));
#123205=CARTESIAN_POINT('Ctrl Pts',(-9.73703147357809,12.168294416076,12.1481291374567));
#123206=CARTESIAN_POINT('Ctrl Pts',(-9.75271045092133,12.1672401363712,
12.1516079197754));
#123207=CARTESIAN_POINT('Ctrl Pts',(-9.77602981215884,12.1656637961893,
12.1562837459332));
#123208=CARTESIAN_POINT('Ctrl Pts',(-9.78361916552548,12.1651494849072,
12.1577279800865));
#123209=CARTESIAN_POINT('Ctrl Pts',(-9.79718422374252,12.1642276684945,
12.1601713340948));
#123210=CARTESIAN_POINT('Ctrl Pts',(-9.80315451783919,12.1638210800972,
12.1611992151948));
#123211=CARTESIAN_POINT('Ctrl Pts',(-9.81581135089552,12.1629571487377,
12.1632778755968));
#123212=CARTESIAN_POINT('Ctrl Pts',(-9.82249952755908,12.1624994621919,
12.1643171618146));
#123213=CARTESIAN_POINT('Ctrl Pts',(-9.84045162724924,12.1612676574012,
12.1669484934057));
#123214=CARTESIAN_POINT('Ctrl Pts',(-9.85173003757058,12.1604902932226,
12.1684350525478));
#123215=CARTESIAN_POINT('Ctrl Pts',(-9.90642727011608,12.1567022851152,
12.1748397929032));
#123216=CARTESIAN_POINT('Ctrl Pts',(-9.95007055226927,12.1536231753417,
12.1775018556463));
#123217=CARTESIAN_POINT('Ctrl Pts',(-10.0822327231451,12.1441324235055,
12.1782024956472));
#123218=CARTESIAN_POINT('Ctrl Pts',(-10.1704703770715,12.1375483179575,
12.1687005907656));
#123219=CARTESIAN_POINT('Ctrl Pts',(-10.277284797482,12.1296352259838,12.1448355623733));
#123220=CARTESIAN_POINT('Ctrl Pts',(-10.2976376480873,12.1281316364459,
12.1397136737628));
#123221=CARTESIAN_POINT('Ctrl Pts',(-10.3308884024165,12.1256929074211,
12.1303943795055));
#123222=CARTESIAN_POINT('Ctrl Pts',(-10.3438695621243,12.1247453572993,
12.1265133605033));
#123223=CARTESIAN_POINT('Ctrl Pts',(-10.3616230051352,12.1234583453713,
12.1208700517526));
#123224=CARTESIAN_POINT('Ctrl Pts',(-10.3664545803885,12.1231090014807,
12.1192997425349));
#123225=CARTESIAN_POINT('Ctrl Pts',(-10.3745933695163,12.1225222540686,
12.1165962070587));
#123226=CARTESIAN_POINT('Ctrl Pts',(-10.3779059390047,12.1222839269008,
12.115479441579));
#123227=CARTESIAN_POINT('Ctrl Pts',(-10.3846886416362,12.1217969972243,
12.1131591084982));
#123228=CARTESIAN_POINT('Ctrl Pts',(-10.3881581871568,12.1215484830556,
12.111954034352));
#123229=CARTESIAN_POINT('Ctrl Pts',(-10.3971993600612,12.1209022231358,
12.1087662979927));
#123230=CARTESIAN_POINT('Ctrl Pts',(-10.4027618763469,12.1205059443577,
12.1067578370105));
#123231=CARTESIAN_POINT('Ctrl Pts',(-10.425717156149,12.1188751709447,12.0982733728524));
#123232=CARTESIAN_POINT('Ctrl Pts',(-10.4429718010844,12.1176603032386,
12.091428226678));
#123233=CARTESIAN_POINT('Ctrl Pts',(-10.5654896064493,12.1090637331105,
12.039439178034));
#123234=CARTESIAN_POINT('Ctrl Pts',(-10.6638393220722,12.1022654180125,
11.9795588689531));
#123235=CARTESIAN_POINT('Ctrl Pts',(-10.7695148938815,12.0935422836262,
11.8918854219308));
#123236=CARTESIAN_POINT('Ctrl Pts',(-10.7866006344376,12.0920823108362,
11.8768535360224));
#123237=CARTESIAN_POINT('Ctrl Pts',(-10.8155959013439,12.0895055517145,
11.849814006072));
#123238=CARTESIAN_POINT('Ctrl Pts',(-10.8277023275361,12.0883974962961,
11.838027045896));
#123239=CARTESIAN_POINT('Ctrl Pts',(-10.8450776886567,12.0867562754594,
11.8203663040466));
#123240=CARTESIAN_POINT('Ctrl Pts',(-10.8505481796238,12.0862318369102,
11.814693170332));
#123241=CARTESIAN_POINT('Ctrl Pts',(-10.8601350855913,12.0852986985181,
11.8045493287245));
#123242=CARTESIAN_POINT('Ctrl Pts',(-10.864274647321,12.0848910018274,11.8001008183075));
#123243=CARTESIAN_POINT('Ctrl Pts',(-10.8728952696353,12.0840317411773,
11.7906918455874));
#123244=CARTESIAN_POINT('Ctrl Pts',(-10.8773688806839,12.0835798866288,
11.7857248821697));
#123245=CARTESIAN_POINT('Ctrl Pts',(-10.889084344015,12.0823805230305,11.7724926200048));
#123246=CARTESIAN_POINT('Ctrl Pts',(-10.8962530700152,12.0816300601922,
11.7641637514572));
#123247=CARTESIAN_POINT('Ctrl Pts',(-10.9282116623612,12.0782071396007,
11.7259647996493));
#123248=CARTESIAN_POINT('Ctrl Pts',(-10.9516295951193,12.0754814110671,
11.6949836738548));
#123249=CARTESIAN_POINT('Ctrl Pts',(-11.0158313995291,12.0673279635601,
11.600703713481));
#123250=CARTESIAN_POINT('Ctrl Pts',(-11.0521269596415,12.0617731517375,
11.5345888625871));
#123251=CARTESIAN_POINT('Ctrl Pts',(-11.0950387527641,12.0538329611891,
11.434852144938));
#123252=CARTESIAN_POINT('Ctrl Pts',(-11.1069082669311,12.0514114164991,
11.4036838342042));
#123253=CARTESIAN_POINT('Ctrl Pts',(-11.1214028844627,12.0481433357976,
11.3601499651524));
#123254=CARTESIAN_POINT('Ctrl Pts',(-11.1251754630735,12.047256740384,11.3481847663827));
#123255=CARTESIAN_POINT('Ctrl Pts',(-11.1313923435413,12.0457325955713,
11.3273098237242));
#123256=CARTESIAN_POINT('Ctrl Pts',(-11.1339242811537,12.045091107214,11.3184275325967));
#123257=CARTESIAN_POINT('Ctrl Pts',(-11.1374987802191,12.0441545540402,
11.3053041816845));
#123258=CARTESIAN_POINT('Ctrl Pts',(-11.1386225913124,12.0438552121324,
11.3010858921274));
#123259=CARTESIAN_POINT('Ctrl Pts',(-11.1405699313925,12.0433277893603,
11.2936095802436));
#123260=CARTESIAN_POINT('Ctrl Pts',(-11.1414029999692,12.0430991829534,
11.2903541744859));
#123261=CARTESIAN_POINT('Ctrl Pts',(-11.1431993802867,12.0425996066937,
11.2832071863056));
#123262=CARTESIAN_POINT('Ctrl Pts',(-11.1441567641818,12.0423289708863,
11.2793142202481));
#123263=CARTESIAN_POINT('Ctrl Pts',(-11.1467897791724,12.0415718925514,
11.268366975604));
#123264=CARTESIAN_POINT('Ctrl Pts',(-11.1484202092392,12.0410879022624,
11.2613018574454));
#123265=CARTESIAN_POINT('Ctrl Pts',(-11.1581805386689,12.0380894738549,
11.2171505273887));
#123266=CARTESIAN_POINT('Ctrl Pts',(-11.1645792960949,12.035660472511,11.1797003268119));
#123267=CARTESIAN_POINT('Ctrl Pts',(-11.177616044113,12.0288564643399,11.0723641484136));
#123268=CARTESIAN_POINT('Ctrl Pts',(-11.1798357227347,12.0245834694337,
11.0021078021566));
#123269=CARTESIAN_POINT('Ctrl Pts',(-11.1726904199467,12.0168441277723,
10.8784315146374));
#123270=CARTESIAN_POINT('Ctrl Pts',(-11.1659252744894,12.0134341036479,
10.8250746186215));
#123271=CARTESIAN_POINT('Ctrl Pts',(-11.1532996379893,12.0091470098148,
10.7609817329291));
#123272=CARTESIAN_POINT('Ctrl Pts',(-11.1508881132562,12.0083803117057,
10.7496276331002));
#123273=CARTESIAN_POINT('Ctrl Pts',(-11.1467942107791,12.0071548529186,
10.7316632848213));
#123274=CARTESIAN_POINT('Ctrl Pts',(-11.1452215037937,12.0066995598358,
10.7250286223171));
#123275=CARTESIAN_POINT('Ctrl Pts',(-11.1421448934489,12.0058368513597,
10.7125339983493));
#123276=CARTESIAN_POINT('Ctrl Pts',(-11.1406532704289,12.0054298386628,
10.7066712184983));
#123277=CARTESIAN_POINT('Ctrl Pts',(-11.1371752440153,12.0045053693404,
10.6934287515461));
#123278=CARTESIAN_POINT('Ctrl Pts',(-11.1351620615146,12.0039870723721,
10.6860564456525));
#123279=CARTESIAN_POINT('Ctrl Pts',(-11.1288156789064,12.0024022516808,
10.6636753666599));
#123280=CARTESIAN_POINT('Ctrl Pts',(-11.1242556373257,12.0013285313511,
10.6487332675562));
#123281=CARTESIAN_POINT('Ctrl Pts',(-11.0921914514131,11.9941764058379,
10.550696223028));
#123282=CARTESIAN_POINT('Ctrl Pts',(-11.0557988317536,11.9878047673149,
10.4708124694543));
#123283=CARTESIAN_POINT('Ctrl Pts',(-10.9868933004128,11.9779490414106,
10.3555413842839));
#123284=CARTESIAN_POINT('Ctrl Pts',(-10.9605065471821,11.9745153010447,
10.3168360781675));
#123285=CARTESIAN_POINT('Ctrl Pts',(-10.9178430745701,11.9695162311914,
10.2616325709469));
#123286=CARTESIAN_POINT('Ctrl Pts',(-10.9032714747041,11.9678914882944,
10.2438762132457));
#123287=CARTESIAN_POINT('Ctrl Pts',(-10.8841609560181,11.9658730698953,
10.2219305396354));
#123288=CARTESIAN_POINT('Ctrl Pts',(-10.8800968795151,11.9654499477349,
10.2173364911799));
#123289=CARTESIAN_POINT('Ctrl Pts',(-10.8735096161487,11.9647741656414,
10.2100064170602));
#123290=CARTESIAN_POINT('Ctrl Pts',(-10.871009093925,11.9645199181846,10.207250310715));
#123291=CARTESIAN_POINT('Ctrl Pts',(-10.8661788724575,11.9640332282865,
10.2019768253969));
#123292=CARTESIAN_POINT('Ctrl Pts',(-10.8638511952463,11.9638006523242,
10.1994577218648));
#123293=CARTESIAN_POINT('Ctrl Pts',(-10.8586873093338,11.9632889094237,
10.1939179102763));
#123294=CARTESIAN_POINT('Ctrl Pts',(-10.8558460696825,11.9630101154695,
10.1909018991006));
#123295=CARTESIAN_POINT('Ctrl Pts',(-10.8457366470507,11.9620276252861,
10.1802834593454));
#123296=CARTESIAN_POINT('Ctrl Pts',(-10.8383823525459,11.9613300728391,
10.1727631941769));
#123297=CARTESIAN_POINT('Ctrl Pts',(-10.7842260796503,11.9563073169715,
10.1188489312276));
#123298=CARTESIAN_POINT('Ctrl Pts',(-10.7336978726762,11.95222440841,10.0763509967901));
#123299=CARTESIAN_POINT('Ctrl Pts',(-10.6492435429015,11.945824342893,10.0166460731715));
#123300=CARTESIAN_POINT('Ctrl Pts',(-10.6175972558304,11.9435091201759,
9.99646840346917));
#123301=CARTESIAN_POINT('Ctrl Pts',(-10.538634092459,11.9378242182725,9.95127329475322));
#123302=CARTESIAN_POINT('Ctrl Pts',(-10.490475817117,11.9344296907177,9.92790541937281));
#123303=CARTESIAN_POINT('Ctrl Pts',(-10.4301495466326,11.9301600496171,
9.90355079556771));
#123304=CARTESIAN_POINT('Ctrl Pts',(-10.4193351523102,11.9293941806119,
9.89936949668968));
#123305=CARTESIAN_POINT('Ctrl Pts',(-10.40206841981,11.9281697435367,9.89298486817855));
#123306=CARTESIAN_POINT('Ctrl Pts',(-10.3956554613296,11.9277146330197,
9.89067666168918));
#123307=CARTESIAN_POINT('Ctrl Pts',(-10.3835129428983,11.9268520805812,
9.8864249074562));
#123308=CARTESIAN_POINT('Ctrl Pts',(-10.3777877166424,11.9264450396826,
9.88446958673505));
#123309=CARTESIAN_POINT('Ctrl Pts',(-10.3647928012099,11.9255202463072,
9.88014298057294));
#123310=CARTESIAN_POINT('Ctrl Pts',(-10.3575146327765,11.925001651077,9.87779822921384));
#123311=CARTESIAN_POINT('Ctrl Pts',(-10.335277688365,11.9234149678473,9.87087260369048));
#123312=CARTESIAN_POINT('Ctrl Pts',(-10.320250533029,11.9223396582804,9.86651891909287));
#123313=CARTESIAN_POINT('Ctrl Pts',(-10.2209285725711,11.9152090249127,
9.83987595763394));
#123314=CARTESIAN_POINT('Ctrl Pts',(-10.1344820533132,11.9088630166077,
9.82671127663411));
#123315=CARTESIAN_POINT('Ctrl Pts',(-10.0004037138852,11.8990152681782,
9.82131154142789));
#123316=CARTESIAN_POINT('Ctrl Pts',(-9.9533405998498,11.8955643517526,9.82223515717757));
#123317=CARTESIAN_POINT('Ctrl Pts',(-9.88350163733715,11.8905439357649,
9.82779973108206));
#123318=CARTESIAN_POINT('Ctrl Pts',(-9.86060333633592,11.8889145105641,
9.83030171476413));
#123319=CARTESIAN_POINT('Ctrl Pts',(-9.83171100865946,11.8868911932928,
9.83431927009611));
#123320=CARTESIAN_POINT('Ctrl Pts',(-9.82563714228905,11.8864676858942,
9.83521231693964));
#123321=CARTESIAN_POINT('Ctrl Pts',(-9.81676178105942,11.8858518067123,
9.83658825199385));
#123322=CARTESIAN_POINT('Ctrl Pts',(-9.81395473831848,11.8856574553958,
9.83703383484927));
#123323=CARTESIAN_POINT('Ctrl Pts',(-9.81114930150134,11.8854636688711,
9.83748958018581));
#123324=CARTESIAN_POINT('',(-11.1777499019438,11.9246914705086,10.999519405199));
#123325=CARTESIAN_POINT('Ctrl Pts',(-9.81114930150157,11.7871268320303,
9.83748958018577));
#123326=CARTESIAN_POINT('Ctrl Pts',(-9.84265146749419,11.7894195655962,
9.83237202945201));
#123327=CARTESIAN_POINT('Ctrl Pts',(-9.87435912257571,11.7917412401712,
9.82853536515747));
#123328=CARTESIAN_POINT('Ctrl Pts',(-9.98527968920542,11.7998816896544,
9.81967259576722));
#123329=CARTESIAN_POINT('Ctrl Pts',(-10.0648050142063,11.8057649315899,
9.82136040255806));
#123330=CARTESIAN_POINT('Ctrl Pts',(-10.1550366002715,11.8121633871668,
9.83244168935296));
#123331=CARTESIAN_POINT('Ctrl Pts',(-10.1664921428589,11.8129702070396,
9.83402009134467));
#123332=CARTESIAN_POINT('Ctrl Pts',(-10.1823104429231,11.8140750097516,
9.8364375121008));
#123333=CARTESIAN_POINT('Ctrl Pts',(-10.1866940499209,11.8143801839975,
9.8371328131946));
#123334=CARTESIAN_POINT('Ctrl Pts',(-10.1942212173553,11.8149023794814,
9.83837038784229));
#123335=CARTESIAN_POINT('Ctrl Pts',(-10.1973666585246,11.8151200449309,
9.83890067615568));
#123336=CARTESIAN_POINT('Ctrl Pts',(-10.2039846100336,11.815576798188,9.84004406334225));
#123337=CARTESIAN_POINT('Ctrl Pts',(-10.2074565894794,11.8158157171866,
9.84065998940724));
#123338=CARTESIAN_POINT('Ctrl Pts',(-10.2160776666166,11.816407319433,9.84222932935155));
#123339=CARTESIAN_POINT('Ctrl Pts',(-10.2212233495161,11.8167589708983,
9.84320152316361));
#123340=CARTESIAN_POINT('Ctrl Pts',(-10.2407621989008,11.8180892745941,
9.84702821761173));
#123341=CARTESIAN_POINT('Ctrl Pts',(-10.2551087502112,11.819055798924,9.85011742292053));
#123342=CARTESIAN_POINT('Ctrl Pts',(-10.3756227967875,11.8271166942065,
9.87843412671235));
#123343=CARTESIAN_POINT('Ctrl Pts',(-10.4778785581854,11.8336170388484,
9.9180383766846));
#123344=CARTESIAN_POINT('Ctrl Pts',(-10.6105288401802,11.8431785937721,
9.99194600455481));
#123345=CARTESIAN_POINT('Ctrl Pts',(-10.6466680962014,11.8459105610676,
10.0147395834394));
#123346=CARTESIAN_POINT('Ctrl Pts',(-10.6907264483452,11.8494578862955,
10.0459977160656));
#123347=CARTESIAN_POINT('Ctrl Pts',(-10.6998700224752,11.8502064793528,
10.052685204765));
#123348=CARTESIAN_POINT('Ctrl Pts',(-10.7143112199105,11.8514096152484,
10.0635705047728));
#123349=CARTESIAN_POINT('Ctrl Pts',(-10.7196717830395,11.8518609075647,
10.0676839377596));
#123350=CARTESIAN_POINT('Ctrl Pts',(-10.7295537597395,11.8527017723064,
10.0754028911907));
#123351=CARTESIAN_POINT('Ctrl Pts',(-10.7340846082483,11.8530908519899,
10.0789960435164));
#123352=CARTESIAN_POINT('Ctrl Pts',(-10.7387516881056,11.8534953766363,
10.0827535502482));
#123353=CARTESIAN_POINT('Ctrl Pts',(-10.7389145973676,11.8535095017477,
10.0828847814707));
#123354=CARTESIAN_POINT('Ctrl Pts',(-10.7392304080557,11.8535368934708,
10.0831393208946));
#123355=CARTESIAN_POINT('Ctrl Pts',(-10.7393833136292,11.8535501598788,
10.08326262397));
#123356=CARTESIAN_POINT('Ctrl Pts',(-10.7396804447232,11.853575947763,10.0835023532217));
#123357=CARTESIAN_POINT('Ctrl Pts',(-10.7398246736243,11.853588469072,10.0836187752072));
#123358=CARTESIAN_POINT('Ctrl Pts',(-10.7401055694787,11.85361286249,10.0838456246905));
#123359=CARTESIAN_POINT('Ctrl Pts',(-10.7402422392278,11.8536247344621,
10.0839560487427));
#123360=CARTESIAN_POINT('Ctrl Pts',(-10.7405089669717,11.853647910642,10.0841716534674));
#123361=CARTESIAN_POINT('Ctrl Pts',(-10.7406390272939,11.8536592147363,
10.0842768312819));
#123362=CARTESIAN_POINT('Ctrl Pts',(-10.740893350656,11.8536813250315,10.0844825883626));
#123363=CARTESIAN_POINT('Ctrl Pts',(-10.7410176156344,11.8536921311366,
10.0845831652318));
#123364=CARTESIAN_POINT('Ctrl Pts',(-10.7468050480192,11.8541955373455,
10.0892693144007));
#123365=CARTESIAN_POINT('Ctrl Pts',(-10.7524254437942,11.8546902167318,
10.0939072294525));
#123366=CARTESIAN_POINT('Ctrl Pts',(-10.7645657177112,11.8557716403079,
10.1041161538132));
#123367=CARTESIAN_POINT('Ctrl Pts',(-10.7710684716705,11.8563591590664,
10.1097067854797));
#123368=CARTESIAN_POINT('Ctrl Pts',(-10.7883004863567,11.8579386431096,
10.1248521241998));
#123369=CARTESIAN_POINT('Ctrl Pts',(-10.7989166558257,11.8589356570113,
10.1345327231335));
#123370=CARTESIAN_POINT('Ctrl Pts',(-10.8315936402043,11.8620813772571,
10.1654436068719));
#123371=CARTESIAN_POINT('Ctrl Pts',(-10.8530040435193,11.8642562988166,
10.1873400525553));
#123372=CARTESIAN_POINT('Ctrl Pts',(-10.9086430416007,11.8702228956226,
10.2488658358855));
#123373=CARTESIAN_POINT('Ctrl Pts',(-10.9411211754113,11.8740622688413,
10.2899824195799));
#123374=CARTESIAN_POINT('Ctrl Pts',(-11.004141723145,11.8822292665767,10.3817192587976));
#123375=CARTESIAN_POINT('Ctrl Pts',(-11.0338349729055,11.8865463788711,
10.4327625850547));
#123376=CARTESIAN_POINT('Ctrl Pts',(-11.0641677695136,11.8914240980274,
10.4952700153881));
#123377=CARTESIAN_POINT('Ctrl Pts',(-11.0686272091642,11.8921555920061,
10.5047815574599));
#123378=CARTESIAN_POINT('Ctrl Pts',(-11.0746948828354,11.893170360402,10.5181870764257));
#123379=CARTESIAN_POINT('Ctrl Pts',(-11.0764102427971,11.8934595379611,
10.5220316170766));
#123380=CARTESIAN_POINT('Ctrl Pts',(-11.0794918679213,11.8939831633869,
10.5290390263095));
#123381=CARTESIAN_POINT('Ctrl Pts',(-11.0808649384155,11.8942180087875,
10.5321988480658));
#123382=CARTESIAN_POINT('Ctrl Pts',(-11.0836789956021,11.894702465733,10.5387533240788));
#123383=CARTESIAN_POINT('Ctrl Pts',(-11.0851179316682,11.894951956546,10.5421487830395));
#123384=CARTESIAN_POINT('Ctrl Pts',(-11.0888499908174,11.8956038766535,
10.5510717535225));
#123385=CARTESIAN_POINT('Ctrl Pts',(-11.0911170114148,11.89600479064,10.5566101668512));
#123386=CARTESIAN_POINT('Ctrl Pts',(-11.1012658035289,11.8978234365716,
10.5819533161184));
#123387=CARTESIAN_POINT('Ctrl Pts',(-11.1086517891863,11.8992146525209,
10.6019538392975));
#123388=CARTESIAN_POINT('Ctrl Pts',(-11.1287388301803,11.9032420952576,
10.6612541955722));
#123389=CARTESIAN_POINT('Ctrl Pts',(-11.1399214754789,11.905821219531,10.7010357803265));
#123390=CARTESIAN_POINT('Ctrl Pts',(-11.1680716632431,11.9137731768417,
10.8260744062333));
#123391=CARTESIAN_POINT('Ctrl Pts',(-11.1777144565469,11.9190828918736,
10.912656599808));
#123392=CARTESIAN_POINT('Ctrl Pts',(-11.1777499019438,11.9246914705086,
10.999519405199));
#123393=CARTESIAN_POINT('Ctrl Pts',(-11.1777498978294,11.9246908261691,
10.9995094259802));
#123394=CARTESIAN_POINT('Ctrl Pts',(-11.177755783503,11.9256221251925,11.0139329102706));
#123395=CARTESIAN_POINT('Ctrl Pts',(-11.1774969546123,11.9265603664752,
11.0283547832212));
#123396=CARTESIAN_POINT('Ctrl Pts',(-11.1765976782018,11.9281847721749,
11.05310294073));
#123397=CARTESIAN_POINT('Ctrl Pts',(-11.1760860245079,11.9288670704794,
11.0634324098018));
#123398=CARTESIAN_POINT('Ctrl Pts',(-11.1750659675478,11.9299483060232,
11.0796894479493));
#123399=CARTESIAN_POINT('Ctrl Pts',(-11.1746485629377,11.9303444502281,
11.085622354684));
#123400=CARTESIAN_POINT('Ctrl Pts',(-11.1737358034003,11.9311292975541,
11.0973288444902));
#123401=CARTESIAN_POINT('Ctrl Pts',(-11.1732427391017,11.9315179193461,
11.1031024405907));
#123402=CARTESIAN_POINT('Ctrl Pts',(-11.1721020706597,11.9323483230663,
11.1153890619231));
#123403=CARTESIAN_POINT('Ctrl Pts',(-11.1714427420018,11.9327904558006,
11.1219007747635));
#123404=CARTESIAN_POINT('Ctrl Pts',(-11.169600899152,11.9339360666646,11.138693526422));
#123405=CARTESIAN_POINT('Ctrl Pts',(-11.1683371110564,11.9346420393839,
11.1489648973813));
#123406=CARTESIAN_POINT('Ctrl Pts',(-11.1625629445594,11.9375732936573,
11.1912848306329));
#123407=CARTESIAN_POINT('Ctrl Pts',(-11.1568682277918,11.9398347315364,
11.2231547514224));
#123408=CARTESIAN_POINT('Ctrl Pts',(-11.1309316339241,11.9483475855106,
11.3402264047285));
#123409=CARTESIAN_POINT('Ctrl Pts',(-11.1025228833957,11.9548253680828,
11.4233203497335));
#123410=CARTESIAN_POINT('Ctrl Pts',(-11.0477701047596,11.9641915610551,
11.5393862919074));
#123411=CARTESIAN_POINT('Ctrl Pts',(-11.0284548957363,11.9671388187079,
11.5753615891282));
#123412=CARTESIAN_POINT('Ctrl Pts',(-11.002342464544,11.9706681875444,11.6184630363119));
#123413=CARTESIAN_POINT('Ctrl Pts',(-10.997275546867,11.9713344153117,11.6266007036261));
#123414=CARTESIAN_POINT('Ctrl Pts',(-10.9897222057876,11.9722998795227,
11.6384078989193));
#123415=CARTESIAN_POINT('Ctrl Pts',(-10.9873136822041,11.972603767704,11.6421264552732));
#123416=CARTESIAN_POINT('Ctrl Pts',(-10.9830388154057,11.9731360928222,
11.6486455694762));
#123417=CARTESIAN_POINT('Ctrl Pts',(-10.9811813821827,11.9733650931529,
11.6514518276092));
#123418=CARTESIAN_POINT('Ctrl Pts',(-10.9771114986351,11.9738618776224,
11.6575438170293));
#123419=CARTESIAN_POINT('Ctrl Pts',(-10.974894483174,11.9741293569372,11.6608263765228));
#123420=CARTESIAN_POINT('Ctrl Pts',(-10.9686911439102,11.9748693177498,
11.6699120052822));
#123421=CARTESIAN_POINT('Ctrl Pts',(-10.9646692060127,11.9753395186303,
11.6756907251419));
#123422=CARTESIAN_POINT('Ctrl Pts',(-10.94105563891,11.9780476849214,11.7089780493033));
#123423=CARTESIAN_POINT('Ctrl Pts',(-10.9203379243412,11.9802182581707,
11.7356725906976));
#123424=CARTESIAN_POINT('Ctrl Pts',(-10.8583184335943,11.986281452752,11.8088553959763));
#123425=CARTESIAN_POINT('Ctrl Pts',(-10.814445961821,11.9900833427241,11.8530158829485));
#123426=CARTESIAN_POINT('Ctrl Pts',(-10.734158915249,11.9966541211329,11.9219615217974));
#123427=CARTESIAN_POINT('Ctrl Pts',(-10.699471781803,11.9993877000918,11.9485468609408));
#123428=CARTESIAN_POINT('Ctrl Pts',(-10.6484148802514,12.0033462675896,
11.9833522724646));
#123429=CARTESIAN_POINT('Ctrl Pts',(-10.6332063257463,12.0045175673697,
11.99321359521));
#123430=CARTESIAN_POINT('Ctrl Pts',(-10.6092298225601,12.0063565016424,
12.0079855489864));
#123431=CARTESIAN_POINT('Ctrl Pts',(-10.6006160131888,12.0070156599234,
12.0131417662491));
#123432=CARTESIAN_POINT('Ctrl Pts',(-10.5860439692757,12.0081289233563,
12.0216134310379));
#123433=CARTESIAN_POINT('Ctrl Pts',(-10.5801208579939,12.0085809297365,
12.0249884503267));
#123434=CARTESIAN_POINT('Ctrl Pts',(-10.5684882613395,12.0094678686641,
12.0314836349629));
#123435=CARTESIAN_POINT('Ctrl Pts',(-10.5627815547245,12.0099026242601,
12.0346082888091));
#123436=CARTESIAN_POINT('Ctrl Pts',(-10.5519870830568,12.0107244620246,
12.0404029671566));
#123437=CARTESIAN_POINT('Ctrl Pts',(-10.5469050796694,12.0111111659204,
12.0430833647204));
#123438=CARTESIAN_POINT('Ctrl Pts',(-10.534942891162,12.0120210122996,12.0492811219235));
#123439=CARTESIAN_POINT('Ctrl Pts',(-10.5280473678224,12.012545188239,12.0527681330866));
#123440=CARTESIAN_POINT('Ctrl Pts',(-10.5067032116947,12.0141670816505,
12.0632992491961));
#123441=CARTESIAN_POINT('Ctrl Pts',(-10.4921448112291,12.0152724994744,
12.0701153576629));
#123442=CARTESIAN_POINT('Ctrl Pts',(-10.4156241274805,12.0210811593774,
12.1040498772558));
#123443=CARTESIAN_POINT('Ctrl Pts',(-10.3515591641075,12.0259497534578,
12.1260874852991));
#123444=CARTESIAN_POINT('Ctrl Pts',(-10.2296581922039,12.0351408608072,
12.1565991328903));
#123445=CARTESIAN_POINT('Ctrl Pts',(-10.1723834217287,12.0394281145099,
12.1665113126214));
#123446=CARTESIAN_POINT('Ctrl Pts',(-10.0946230140934,12.0450699135368,
12.1741145026504));
#123447=CARTESIAN_POINT('Ctrl Pts',(-10.0745876484128,12.0465072395938,
12.17555738105));
#123448=CARTESIAN_POINT('Ctrl Pts',(-10.0414134024463,12.0488507038394,
12.1770948355798));
#123449=CARTESIAN_POINT('Ctrl Pts',(-10.0282927796975,12.0497681473157,
12.177483280649));
#123450=CARTESIAN_POINT('Ctrl Pts',(-10.0101505326263,12.0510213198357,
12.1777169463803));
#123451=CARTESIAN_POINT('Ctrl Pts',(-10.0051328431663,12.0513662872969,
12.1777495044828));
#123452=CARTESIAN_POINT('Ctrl Pts',(-9.99663190605569,12.0519478005035,
12.1777503344473));
#123453=CARTESIAN_POINT('Ctrl Pts',(-9.99314876233222,12.0521852336447,
12.1777352232711));
#123454=CARTESIAN_POINT('Ctrl Pts',(-9.98597419991665,12.0526725168494,
12.1776722664624));
#123455=CARTESIAN_POINT('Ctrl Pts',(-9.9822828707635,12.0529222630283,12.1776225178468));
#123456=CARTESIAN_POINT('Ctrl Pts',(-9.97259087563087,12.0535756159525,
12.1774463151537));
#123457=CARTESIAN_POINT('Ctrl Pts',(-9.96659074260276,12.0539776951973,
12.1772913447698));
#123458=CARTESIAN_POINT('Ctrl Pts',(-9.94126799028439,12.0556654757494,
12.1764435581702));
#123459=CARTESIAN_POINT('Ctrl Pts',(-9.92196159372133,12.0569297979229,
12.1753208092634));
#123460=CARTESIAN_POINT('Ctrl Pts',(-9.78940226119842,12.0655095478397,
12.1643307320265));
#123461=CARTESIAN_POINT('Ctrl Pts',(-9.67806281472448,12.0722618928368,
12.1385866300699));
#123462=CARTESIAN_POINT('Ctrl Pts',(-9.55098066558749,12.0809281388331,
12.0890326041522));
#123463=CARTESIAN_POINT('Ctrl Pts',(-9.5300751057532,12.082384837017,12.0801763161222));
#123464=CARTESIAN_POINT('Ctrl Pts',(-9.49410723281759,12.0849563013698,
12.0636973212264));
#123465=CARTESIAN_POINT('Ctrl Pts',(-9.47892836256622,12.0860623861987,
12.0563445391701));
#123466=CARTESIAN_POINT('Ctrl Pts',(-9.45690205494621,12.0877011519974,
12.0450845356525));
#123467=CARTESIAN_POINT('Ctrl Pts',(-9.449927186539,12.0882251422958,12.0414302470411));
#123468=CARTESIAN_POINT('Ctrl Pts',(-9.43763752884214,12.0891576836301,
12.0348335188372));
#123469=CARTESIAN_POINT('Ctrl Pts',(-9.43230782683142,12.0895652347138,
12.0319193548158));
#123470=CARTESIAN_POINT('Ctrl Pts',(-9.42116035067936,12.0904243917137,
12.0257116624776));
#123471=CARTESIAN_POINT('Ctrl Pts',(-9.41534761603547,12.0908762895932,
12.0224095759113));
#123472=CARTESIAN_POINT('Ctrl Pts',(-9.40004830274959,12.0920762416338,
12.0135452401849));
#123473=CARTESIAN_POINT('Ctrl Pts',(-9.39061116625172,12.0928272560223,
12.0078994136458));
#123474=CARTESIAN_POINT('Ctrl Pts',(-9.34887399634329,12.0961984938383,
11.9821294326415));
#123475=CARTESIAN_POINT('Ctrl Pts',(-9.31748475768185,12.0988697118025,
11.9605809100776));
#123476=CARTESIAN_POINT('Ctrl Pts',(-9.22611556104383,12.1070689614915,
11.8911146442338));
#123477=CARTESIAN_POINT('Ctrl Pts',(-9.16972353488591,12.1127345751575,
11.8388213722552));
#123478=CARTESIAN_POINT('Ctrl Pts',(-9.0970389146401,12.1207435873642,11.756858242238));
#123479=CARTESIAN_POINT('Ctrl Pts',(-9.0762893776164,12.1231276652709,11.7313905178527));
#123480=CARTESIAN_POINT('Ctrl Pts',(-9.04919225619578,12.1263505797081,
11.695135993109));
#123481=CARTESIAN_POINT('Ctrl Pts',(-9.04191202747868,12.127228435146,11.6850670612147));
#123482=CARTESIAN_POINT('Ctrl Pts',(-9.02953933581988,12.1287390804252,
11.6673718546581));
#123483=CARTESIAN_POINT('Ctrl Pts',(-9.02437416920066,12.1293757211598,
11.6597979571697));
#123484=CARTESIAN_POINT('Ctrl Pts',(-9.01688813918409,12.1303065389456,
11.6485407217811));
#123485=CARTESIAN_POINT('Ctrl Pts',(-9.01449856289214,12.1306049217407,
11.644903804967));
#123486=CARTESIAN_POINT('Ctrl Pts',(-9.01045939897434,12.1311113430238,
11.6386813495417));
#123487=CARTESIAN_POINT('Ctrl Pts',(-9.0087996868492,12.1313200341171,11.6361025132408));
#123488=CARTESIAN_POINT('Ctrl Pts',(-9.00505360680032,12.1317924158358,
11.6302316450915));
#123489=CARTESIAN_POINT('Ctrl Pts',(-9.00297348896896,12.1320556997121,
11.6269357137844));
#123490=CARTESIAN_POINT('Ctrl Pts',(-8.99733062128461,12.1327728043524,
11.6178955151367));
#123491=CARTESIAN_POINT('Ctrl Pts',(-8.99380083400843,12.1332245660208,
11.6121307003452));
#123492=CARTESIAN_POINT('Ctrl Pts',(-8.97544608101233,12.1355925424366,
11.5815660900498));
#123493=CARTESIAN_POINT('Ctrl Pts',(-8.96148649992685,12.1374597346795,
11.556255218153));
#123494=CARTESIAN_POINT('Ctrl Pts',(-8.91890851729149,12.1434701021332,
11.4718521116726));
#123495=CARTESIAN_POINT('Ctrl Pts',(-8.89429493792555,12.14748307587,11.4108778434292));
#123496=CARTESIAN_POINT('Ctrl Pts',(-8.86160825660064,12.1543435571037,
11.3052499953245));
#123497=CARTESIAN_POINT('Ctrl Pts',(-8.8507947686932,12.1571521037317,11.2616107710267));
#123498=CARTESIAN_POINT('Ctrl Pts',(-8.83742290097849,12.1617886187591,
11.1904358542441));
#123499=CARTESIAN_POINT('Ctrl Pts',(-8.83329369867413,12.1635725750304,
11.1632407606041));
#123500=CARTESIAN_POINT('Ctrl Pts',(-8.82902616172211,12.1660110556969,
11.1265116242625));
#123501=CARTESIAN_POINT('Ctrl Pts',(-8.82804586633937,12.1666395631766,
11.1170829661049));
#123502=CARTESIAN_POINT('Ctrl Pts',(-8.82659813616777,12.1676957145058,
11.1013093795092));
#123503=CARTESIAN_POINT('Ctrl Pts',(-8.82606809443844,12.1681214070262,
11.0949705366784));
#123504=CARTESIAN_POINT('Ctrl Pts',(-8.82512661032692,12.1689618483157,
11.0824948947301));
#123505=CARTESIAN_POINT('Ctrl Pts',(-8.82471183980364,12.1693764799683,
11.0763585453952));
#123506=CARTESIAN_POINT('Ctrl Pts',(-8.82382487876583,12.1703830435992,
11.0615085022981));
#123507=CARTESIAN_POINT('Ctrl Pts',(-8.82340144064217,12.1709764610019,
11.0527923733429));
#123508=CARTESIAN_POINT('Ctrl Pts',(-8.82231164331672,12.1729669918766,
11.0236901311657));
#123509=CARTESIAN_POINT('Ctrl Pts',(-8.82207803410386,12.1743772326128,
11.0032925061872));
#123510=CARTESIAN_POINT('Ctrl Pts',(-8.82370840560998,12.1822275238111,
10.8910127063675));
#123511=CARTESIAN_POINT('Ctrl Pts',(-8.83579272272953,12.1889767011168,
10.7996103708562));
#123512=CARTESIAN_POINT('Ctrl Pts',(-8.86091117947494,12.1964668745766,
10.7005360134776));
#123513=CARTESIAN_POINT('Ctrl Pts',(-8.86358475794481,12.1972237962367,
10.690544959543));
#123514=CARTESIAN_POINT('Ctrl Pts',(-8.87474132814395,12.200227380788,10.6509494028131));
#123515=CARTESIAN_POINT('Ctrl Pts',(-8.88425296051962,12.2024591397807,
10.621645416623));
#123516=CARTESIAN_POINT('Ctrl Pts',(-8.899026458731,12.2054977715023,10.5815570218364));
#123517=CARTESIAN_POINT('Ctrl Pts',(-8.90331982680242,12.2063395101654,
10.5704305803293));
#123518=CARTESIAN_POINT('Ctrl Pts',(-8.91110486377902,12.2077943255239,
10.5511332648474));
#123519=CARTESIAN_POINT('Ctrl Pts',(-8.91452131498735,12.2084108971433,
10.5429332655042));
#123520=CARTESIAN_POINT('Ctrl Pts',(-8.91972768322518,12.2093181147967,
10.5308249285663));
#123521=CARTESIAN_POINT('Ctrl Pts',(-8.92144665149034,12.209612675519,10.5268866922958));
#123522=CARTESIAN_POINT('Ctrl Pts',(-8.92442681533606,12.2101148382218,
10.5201596581452));
#123523=CARTESIAN_POINT('Ctrl Pts',(-8.9256773693948,12.2103230625142,10.5173662720309));
#123524=CARTESIAN_POINT('Ctrl Pts',(-8.92856047477507,12.2107974460069,
10.51099295887));
#123525=CARTESIAN_POINT('Ctrl Pts',(-8.93020008790359,12.2110631754266,
10.5074163099547));
#123526=CARTESIAN_POINT('Ctrl Pts',(-8.93477403859497,12.2117935932234,
10.4975692683727));
#123527=CARTESIAN_POINT('Ctrl Pts',(-8.93774584242191,12.2122560945969,
10.4913163071968));
#123528=CARTESIAN_POINT('Ctrl Pts',(-8.95455813389338,12.2148087940525,
10.4567315665533));
#123529=CARTESIAN_POINT('Ctrl Pts',(-8.96947822564044,12.216840399407,10.4289356016382));
#123530=CARTESIAN_POINT('Ctrl Pts',(-8.98630223687682,12.2189393077875,
10.40040478847));
#123531=CARTESIAN_POINT('Ctrl Pts',(-8.98710975063993,12.2190396205947,
10.3990416691348));
#123532=CARTESIAN_POINT('Ctrl Pts',(-9.02750329276134,12.2240363217316,
10.3311682669105));
#123533=CARTESIAN_POINT('Ctrl Pts',(-9.07354787411905,12.2287349241803,
10.2687180149885));
#123534=CARTESIAN_POINT('Ctrl Pts',(-9.16026673871962,12.2368331695996,
10.1725610416616));
#123535=CARTESIAN_POINT('Ctrl Pts',(-9.19766711655844,12.240142827333,10.1362476522582));
#123536=CARTESIAN_POINT('Ctrl Pts',(-9.24612314151881,12.2443167639677,
10.095070462418));
#123537=CARTESIAN_POINT('Ctrl Pts',(-9.25501076407317,12.2450778502939,
10.0877397253008));
#123538=CARTESIAN_POINT('Ctrl Pts',(-9.26931178707853,12.2462963285017,
10.0762922443746));
#123539=CARTESIAN_POINT('Ctrl Pts',(-9.27465591979757,12.2467503201409,
10.0720898511411));
#123540=CARTESIAN_POINT('Ctrl Pts',(-9.28482447108847,12.2476118122534,
10.0642352671384));
#123541=CARTESIAN_POINT('Ctrl Pts',(-9.28964125269203,12.2480189212337,
10.0605735152744));
#123542=CARTESIAN_POINT('Ctrl Pts',(-9.30062666834373,12.2489453261507,
10.0523551200946));
#123543=CARTESIAN_POINT('Ctrl Pts',(-9.30681197186335,12.2494654779694,
10.0478213254443));
#123544=CARTESIAN_POINT('Ctrl Pts',(-9.32584927449223,12.2510622804511,
10.0341508878961));
#123545=CARTESIAN_POINT('Ctrl Pts',(-9.33884041434342,12.2521462903062,
10.025211987843));
#123546=CARTESIAN_POINT('Ctrl Pts',(-9.42300176961781,12.2591365574972,
9.96975895831474));
#123547=CARTESIAN_POINT('Ctrl Pts',(-9.49884109879698,12.2653174174141,
9.93081418616209));
#123548=CARTESIAN_POINT('Ctrl Pts',(-9.62349310948899,12.2751148750309,
9.88299886779541));
#123549=CARTESIAN_POINT('Ctrl Pts',(-9.66982461076612,12.2786782176714,
9.86843750990203));
#123550=CARTESIAN_POINT('Ctrl Pts',(-9.73218891383256,12.2832844991724,
9.85299538852081));
#123551=CARTESIAN_POINT('Ctrl Pts',(-9.74752847923379,12.2844024382356,
9.8495216047509));
#123552=CARTESIAN_POINT('Ctrl Pts',(-9.77366965658846,12.2862773438221,
9.84414976543403));
#123553=CARTESIAN_POINT('Ctrl Pts',(-9.78443631302591,12.2870409274326,
9.84209348071059));
#123554=CARTESIAN_POINT('Ctrl Pts',(-9.79983367116159,12.2881192014786,
9.8393750165261));
#123555=CARTESIAN_POINT('Ctrl Pts',(-9.80444166314972,12.2884401526046,
9.83858971495161));
#123556=CARTESIAN_POINT('Ctrl Pts',(-9.80975253265642,12.2888079585808,
9.83771713238524));
#123557=CARTESIAN_POINT('Ctrl Pts',(-9.8104508646595,12.2888562800112,9.83760304177997));
#123558=CARTESIAN_POINT('Ctrl Pts',(-9.81114930147754,12.2889045666398,
9.83748958018968));
#123559=CARTESIAN_POINT('Origin',(-10.,2.67563288526385,11.));
#123560=CARTESIAN_POINT('',(-9.81116440461326,12.8870115174245,9.83777311283111));
#123561=CARTESIAN_POINT('',(-9.81114930150157,12.7872971999427,9.83748958018577));
#123562=CARTESIAN_POINT('',(-9.81114930150157,2.67563288526385,9.83748958018577));
#123563=CARTESIAN_POINT('Ctrl Pts',(-9.81110867807875,12.8871739896041,
9.83749618022011));
#123564=CARTESIAN_POINT('Ctrl Pts',(-9.78406883002272,12.8854478804254,
9.84188979386417));
#123565=CARTESIAN_POINT('Ctrl Pts',(-9.75719191255045,12.8837043151253,
9.84722525463141));
#123566=CARTESIAN_POINT('Ctrl Pts',(-9.71464208644478,12.8808807571287,
9.85722610260996));
#123567=CARTESIAN_POINT('Ctrl Pts',(-9.6988375012299,12.8798178659499,9.86128913730254));
#123568=CARTESIAN_POINT('Ctrl Pts',(-9.67541680943465,12.8782188242581,
9.86783179935482));
#123569=CARTESIAN_POINT('Ctrl Pts',(-9.66773291883104,12.8776903284387,
9.87006298236067));
#123570=CARTESIAN_POINT('Ctrl Pts',(-9.65428623069631,12.876758316912,9.8741165354314));
#123571=CARTESIAN_POINT('Ctrl Pts',(-9.64851355604475,12.8763558722712,
9.87590531380619));
#123572=CARTESIAN_POINT('Ctrl Pts',(-9.63724727043895,12.8755657311629,
9.87949166509802));
#123573=CARTESIAN_POINT('Ctrl Pts',(-9.63175261472048,12.8751781670077,
9.88128541056828));
#123574=CARTESIAN_POINT('Ctrl Pts',(-9.62085616364738,12.8744050867876,
9.88493156132713));
#123575=CARTESIAN_POINT('Ctrl Pts',(-9.61545419425648,12.874019612599,9.88678295338018));
#123576=CARTESIAN_POINT('Ctrl Pts',(-9.60272489802426,12.8731059219586,
9.89124931474804));
#123577=CARTESIAN_POINT('Ctrl Pts',(-9.59540967212191,12.8725766283155,
9.89389772160528));
#123578=CARTESIAN_POINT('Ctrl Pts',(-9.56964082096367,12.8706968345156,
9.9035169128794));
#123579=CARTESIAN_POINT('Ctrl Pts',(-9.55133753045879,12.8693336695691,
9.91087829379931));
#123580=CARTESIAN_POINT('Ctrl Pts',(-9.4936394361986,12.8649439694878,9.93578507714946));
#123581=CARTESIAN_POINT('Ctrl Pts',(-9.45502289944056,12.8618642147492,
9.95503413376984));
#123582=CARTESIAN_POINT('Ctrl Pts',(-9.34485753226269,12.8526743579141,
10.0177175693384));
#123583=CARTESIAN_POINT('Ctrl Pts',(-9.2767791651881,12.8464463114501,10.0667039500517));
#123584=CARTESIAN_POINT('Ctrl Pts',(-9.20219053210713,12.8392573586922,
10.133474468202));
#123585=CARTESIAN_POINT('Ctrl Pts',(-9.1901476222388,12.8380845260397,10.1447189776182));
#123586=CARTESIAN_POINT('Ctrl Pts',(-9.17020981209158,12.8361274115923,
10.1641338556926));
#123587=CARTESIAN_POINT('Ctrl Pts',(-9.16219020899813,12.8353357843607,
10.1721722733547));
#123588=CARTESIAN_POINT('Ctrl Pts',(-9.1509859751738,12.8342250376851,10.183732424297));
#123589=CARTESIAN_POINT('Ctrl Pts',(-9.14770474643366,12.8338991545232,
10.187159073256));
#123590=CARTESIAN_POINT('Ctrl Pts',(-9.14208382321269,12.8333400129505,
10.1931005682813));
#123591=CARTESIAN_POINT('Ctrl Pts',(-9.13973427665814,12.8331060221488,
10.195605976045));
#123592=CARTESIAN_POINT('Ctrl Pts',(-9.13482301230796,12.8326163994766,
10.2008891692449));
#123593=CARTESIAN_POINT('Ctrl Pts',(-9.13226365778701,12.8323609417971,
10.2036690504066));
#123594=CARTESIAN_POINT('Ctrl Pts',(-9.12536779798752,12.8316716507882,
10.2112318126023));
#123595=CARTESIAN_POINT('Ctrl Pts',(-9.12105709168175,12.8312396894337,
10.2160381955358));
#123596=CARTESIAN_POINT('Ctrl Pts',(-9.10074877752226,12.8291981061035,
10.2390597908665));
#123597=CARTESIAN_POINT('Ctrl Pts',(-9.08527534714444,12.8276229199306,
10.2577320123707));
#123598=CARTESIAN_POINT('Ctrl Pts',(-9.02801231419209,12.8216561173945,
10.3313458831917));
#123599=CARTESIAN_POINT('Ctrl Pts',(-8.99050366702705,12.8174403691046,
10.3894452878321));
#123600=CARTESIAN_POINT('Ctrl Pts',(-8.93670766792437,12.8102949624782,
10.4914277525041));
#123601=CARTESIAN_POINT('Ctrl Pts',(-8.91755001937229,12.8074072933221,
10.5335904523836));
#123602=CARTESIAN_POINT('Ctrl Pts',(-8.89418093907903,12.8032480696345,
10.5942768435863));
#123603=CARTESIAN_POINT('Ctrl Pts',(-8.88785833374651,12.8020372321317,
10.6119433909258));
#123604=CARTESIAN_POINT('Ctrl Pts',(-8.87873515882337,12.8001440652263,
10.6394927324995));
#123605=CARTESIAN_POINT('Ctrl Pts',(-8.87563717982932,12.7994709482178,
10.6492742209935));
#123606=CARTESIAN_POINT('Ctrl Pts',(-8.87008619871506,12.798205201327,10.6676306429787));
#123607=CARTESIAN_POINT('Ctrl Pts',(-8.86760202206982,12.7976136034216,
10.6761954290991));
#123608=CARTESIAN_POINT('Ctrl Pts',(-8.86356749968488,12.796608228155,10.6907199562875));
#123609=CARTESIAN_POINT('Ctrl Pts',(-8.86196617240306,12.7961961061597,
10.6966652377317));
#123610=CARTESIAN_POINT('Ctrl Pts',(-8.85886229692574,12.7953702763121,
10.7085596919887));
#123611=CARTESIAN_POINT('Ctrl Pts',(-8.85735947691383,12.7949565917973,
10.7145085937411));
#123612=CARTESIAN_POINT('Ctrl Pts',(-8.85381161860218,12.7939450766861,
10.7290296713489));
#123613=CARTESIAN_POINT('Ctrl Pts',(-8.85181620568938,12.7933456838564,
10.7376134687512));
#123614=CARTESIAN_POINT('Ctrl Pts',(-8.84533941918717,12.7912907079505,
10.7669648761172));
#123615=CARTESIAN_POINT('Ctrl Pts',(-8.8413239538762,12.7898205910628,10.7878299165997));
#123616=CARTESIAN_POINT('Ctrl Pts',(-8.82301373584406,12.7819257423038,
10.8991152661796));
#123617=CARTESIAN_POINT('Ctrl Pts',(-8.81873575341719,12.7751952318128,
10.9908513870907));
#123618=CARTESIAN_POINT('Ctrl Pts',(-8.82580218420936,12.7677644904687,
11.0919287317256));
#123619=CARTESIAN_POINT('Ctrl Pts',(-8.82660909190401,12.7670455778776,
11.1017112713051));
#123620=CARTESIAN_POINT('Ctrl Pts',(-8.83150848004004,12.7632630917765,
11.1532380744841));
#123621=CARTESIAN_POINT('Ctrl Pts',(-8.83770694970566,12.7602288019821,
11.1947560578584));
#123622=CARTESIAN_POINT('Ctrl Pts',(-8.84804808504356,12.7566106430386,
11.2453480428075));
#123623=CARTESIAN_POINT('Ctrl Pts',(-8.85010484295941,12.7559372143641,
11.254813695718));
#123624=CARTESIAN_POINT('Ctrl Pts',(-8.85327184897153,12.7549647920798,
11.2685688394817));
#123625=CARTESIAN_POINT('Ctrl Pts',(-8.8542898249666,12.7546609838712,11.2728788565181));
#123626=CARTESIAN_POINT('Ctrl Pts',(-8.85612129444679,12.7541295406617,
11.2804421754318));
#123627=CARTESIAN_POINT('Ctrl Pts',(-8.85692439301217,12.7539013373118,
11.2836978398858));
#123628=CARTESIAN_POINT('Ctrl Pts',(-8.85870130073373,12.7534067577356,
11.2907711520637));
#123629=CARTESIAN_POINT('Ctrl Pts',(-8.85968036633839,12.7531406813628,
11.2945873691117));
#123630=CARTESIAN_POINT('Ctrl Pts',(-8.86243659423793,12.7524088694713,
11.3051109732266));
#123631=CARTESIAN_POINT('Ctrl Pts',(-8.86425394354386,12.7519453314807,
11.3118078079074));
#123632=CARTESIAN_POINT('Ctrl Pts',(-8.87471855740354,12.7493766430976,
11.3490635061735));
#123633=CARTESIAN_POINT('Ctrl Pts',(-8.88454074511231,12.7473309143182,
11.3792818249036));
#123634=CARTESIAN_POINT('Ctrl Pts',(-8.91767946752626,12.7412864379041,
11.4687515602554));
#123635=CARTESIAN_POINT('Ctrl Pts',(-8.94458787843713,12.7373941136138,
11.5265471321714));
#123636=CARTESIAN_POINT('Ctrl Pts',(-8.9978922417656,12.7306973327199,11.6203483006338));
#123637=CARTESIAN_POINT('Ctrl Pts',(-9.02189624531239,12.7279298144736,
11.6575443469777));
#123638=CARTESIAN_POINT('Ctrl Pts',(-9.05869900724826,12.723925665021,11.7080832733436));
#123639=CARTESIAN_POINT('Ctrl Pts',(-9.06980637550736,12.722744078595,11.7226127930195));
#123640=CARTESIAN_POINT('Ctrl Pts',(-9.09018631039357,12.720617358585,11.7480228922402));
#123641=CARTESIAN_POINT('Ctrl Pts',(-9.09932729003125,12.7196772092936,
11.7590045046177));
#123642=CARTESIAN_POINT('Ctrl Pts',(-9.11349677523994,12.7182386241192,
11.7754106839105));
#123643=CARTESIAN_POINT('Ctrl Pts',(-9.11838054170768,12.7177460313308,
11.7809589123828));
#123644=CARTESIAN_POINT('Ctrl Pts',(-9.12735292660507,12.7168466530045,
11.790960613971));
#123645=CARTESIAN_POINT('Ctrl Pts',(-9.13142425685647,12.716440590624,11.7954293077699));
#123646=CARTESIAN_POINT('Ctrl Pts',(-9.14030393536213,12.7155592116851,
11.8050261829889));
#123647=CARTESIAN_POINT('Ctrl Pts',(-9.14512413407912,12.7150834056182,
11.8101430299815));
#123648=CARTESIAN_POINT('Ctrl Pts',(-9.15843832488758,12.7137760899345,
11.8240254782902));
#123649=CARTESIAN_POINT('Ctrl Pts',(-9.16702303214714,12.7129407275305,
11.8327024640066));
#123650=CARTESIAN_POINT('Ctrl Pts',(-9.22597026455609,12.7072531220207,
11.8904595349904));
#123651=CARTESIAN_POINT('Ctrl Pts',(-9.28049775176035,12.7022133226105,
11.9350687661089));
#123652=CARTESIAN_POINT('Ctrl Pts',(-9.38079887512987,12.6933626049321,
12.0031338172257));
#123653=CARTESIAN_POINT('Ctrl Pts',(-9.42473919570574,12.6896086474711,
12.0289618565023));
#123654=CARTESIAN_POINT('Ctrl Pts',(-9.50503869840875,12.6830707848471,
12.0694058510048));
#123655=CARTESIAN_POINT('Ctrl Pts',(-9.54071801921699,12.680270311077,12.0852079431273));
#123656=CARTESIAN_POINT('Ctrl Pts',(-9.58376087460311,12.6770619886137,
12.1017670779487));
#123657=CARTESIAN_POINT('Ctrl Pts',(-9.5904258092782,12.6765699163905,12.1042620576965));
#123658=CARTESIAN_POINT('Ctrl Pts',(-9.60082143276683,12.6758101553457,
12.1080465277982));
#123659=CARTESIAN_POINT('Ctrl Pts',(-9.604536545226,12.6755401650494,12.109377885747));
#123660=CARTESIAN_POINT('Ctrl Pts',(-9.61147665969136,12.6750387372548,
12.111825670925));
#123661=CARTESIAN_POINT('Ctrl Pts',(-9.6146998235921,12.6748070472628,12.1129467565907));
#123662=CARTESIAN_POINT('Ctrl Pts',(-9.62212289018574,12.6742761320691,
12.1154925458112));
#123663=CARTESIAN_POINT('Ctrl Pts',(-9.62632601298613,12.6739774660465,
12.116907553424));
#123664=CARTESIAN_POINT('Ctrl Pts',(-9.63988607793801,12.6730198803475,
12.1213875195001));
#123665=CARTESIAN_POINT('Ctrl Pts',(-9.64927378385512,12.6723660543991,
12.1243589918728));
#123666=CARTESIAN_POINT('Ctrl Pts',(-9.73424009222725,12.6665209525267,
12.1500854356494));
#123667=CARTESIAN_POINT('Ctrl Pts',(-9.81190144202986,12.6616844429891,
12.165309992578));
#123668=CARTESIAN_POINT('Ctrl Pts',(-9.9645067388448,12.6521978194249,12.1795585383324));
#123669=CARTESIAN_POINT('Ctrl Pts',(-10.0389803970292,12.6475715806278,
12.1794476349033));
#123670=CARTESIAN_POINT('Ctrl Pts',(-10.1271022677888,12.641790889398,12.1709579166111));
#123671=CARTESIAN_POINT('Ctrl Pts',(-10.1412358629588,12.6408547584067,
12.1693373472622));
#123672=CARTESIAN_POINT('Ctrl Pts',(-10.1626409511236,12.6394217093175,
12.1664893004826));
#123673=CARTESIAN_POINT('Ctrl Pts',(-10.1699363157317,12.6389305858136,
12.1654488455468));
#123674=CARTESIAN_POINT('Ctrl Pts',(-10.1831841245349,12.6380335948936,
12.163432429501));
#123675=CARTESIAN_POINT('Ctrl Pts',(-10.1891397928994,12.6376284453887,
12.162479065587));
#123676=CARTESIAN_POINT('Ctrl Pts',(-10.2020092138304,12.636748731592,12.160317455604));
#123677=CARTESIAN_POINT('Ctrl Pts',(-10.2089199825487,12.636273676327,12.1590930754097));
#123678=CARTESIAN_POINT('Ctrl Pts',(-10.227809217088,12.6349677139771,12.1555720561977));
#123679=CARTESIAN_POINT('Ctrl Pts',(-10.2397633177152,12.6341329463958,
12.1531510519288));
#123680=CARTESIAN_POINT('Ctrl Pts',(-10.3221350377745,12.6283214193523,
12.1351325542028));
#123681=CARTESIAN_POINT('Ctrl Pts',(-10.3910154701715,12.6231459202771,
12.1132836192644));
#123682=CARTESIAN_POINT('Ctrl Pts',(-10.5061844216218,12.6140092080635,
12.0647388694548));
#123683=CARTESIAN_POINT('Ctrl Pts',(-10.5534752999921,12.6101061246871,
12.0409402916311));
#123684=CARTESIAN_POINT('Ctrl Pts',(-10.6302833635469,12.6036283621981,
11.9955689279957));
#123685=CARTESIAN_POINT('Ctrl Pts',(-10.6606916634473,12.6010246604386,
11.9756544928696));
#123686=CARTESIAN_POINT('Ctrl Pts',(-10.6957915137623,12.5980119533303,
11.9502725849841));
#123687=CARTESIAN_POINT('Ctrl Pts',(-10.7014132249043,12.5975292135131,
11.9461307046283));
#123688=CARTESIAN_POINT('Ctrl Pts',(-10.7101222787125,12.5967814411074,
11.9395938870652));
#123689=CARTESIAN_POINT('Ctrl Pts',(-10.7132349926306,12.5965141949876,
11.9372332525772));
#123690=CARTESIAN_POINT('Ctrl Pts',(-10.7190391881619,12.5960159873988,
11.932785777303));
#123691=CARTESIAN_POINT('Ctrl Pts',(-10.7217333587641,12.595784790828,11.9307027558118));
#123692=CARTESIAN_POINT('Ctrl Pts',(-10.7279316691233,12.5952529723598,
11.9258673773861));
#123693=CARTESIAN_POINT('Ctrl Pts',(-10.7314292676585,12.5949529278357,
11.9231067887536));
#123694=CARTESIAN_POINT('Ctrl Pts',(-10.7427215690399,12.5939840636808,
11.9140895108106));
#123695=CARTESIAN_POINT('Ctrl Pts',(-10.7504525608679,12.5933205298584,
11.9077532335629));
#123696=CARTESIAN_POINT('Ctrl Pts',(-10.8168158042945,12.5876133517544,
11.8519349026337));
#123697=CARTESIAN_POINT('Ctrl Pts',(-10.8705721164581,12.5829043980112,
11.7969245231313));
#123698=CARTESIAN_POINT('Ctrl Pts',(-10.9614769897654,12.5739180649251,
11.6836307962055));
#123699=CARTESIAN_POINT('Ctrl Pts',(-10.999605153357,12.569664397412,11.6265598352636));
#123700=CARTESIAN_POINT('Ctrl Pts',(-11.0418984916495,12.5639727647234,
11.549472389243));
#123701=CARTESIAN_POINT('Ctrl Pts',(-11.0508185486628,12.5627025572245,
11.5322148829592));
#123702=CARTESIAN_POINT('Ctrl Pts',(-11.0629427979673,12.5608674400674,
11.5072640907305));
#123703=CARTESIAN_POINT('Ctrl Pts',(-11.0664987555512,12.5603145655806,
11.4997445827643));
#123704=CARTESIAN_POINT('Ctrl Pts',(-11.0725393309801,12.5593490475729,
11.486612892755));
#123705=CARTESIAN_POINT('Ctrl Pts',(-11.0750603120424,12.5589376568278,
11.4810177199848));
#123706=CARTESIAN_POINT('Ctrl Pts',(-11.0801576758564,12.5580880373549,
11.4694641580304));
#123707=CARTESIAN_POINT('Ctrl Pts',(-11.082728749645,12.557649646572,11.4635036700718));
#123708=CARTESIAN_POINT('Ctrl Pts',(-11.0891786994473,12.5565240398669,
11.4482042848302));
#123709=CARTESIAN_POINT('Ctrl Pts',(-11.0929867425828,12.5558344881168,
11.4388362903701));
#123710=CARTESIAN_POINT('Ctrl Pts',(-11.1077171039995,12.553063412293,11.401217238985));
#123711=CARTESIAN_POINT('Ctrl Pts',(-11.1176676039105,12.550950501749,11.3726007195488));
#123712=CARTESIAN_POINT('Ctrl Pts',(-11.1532770691595,12.542306526373,11.2558657283896));
#123713=CARTESIAN_POINT('Ctrl Pts',(-11.1696986535704,12.5355104722746,
11.1652758018376));
#123714=CARTESIAN_POINT('Ctrl Pts',(-11.1779106478584,12.5259419186797,
11.0343331401563));
#123715=CARTESIAN_POINT('Ctrl Pts',(-11.178399895203,12.5230946327988,10.9948458127129));
#123716=CARTESIAN_POINT('Ctrl Pts',(-11.1765483314593,12.5196711373701,
10.9459813142326));
#123717=CARTESIAN_POINT('Ctrl Pts',(-11.1760780678809,12.5190158608483,
10.9365619442179));
#123718=CARTESIAN_POINT('Ctrl Pts',(-11.1752225608884,12.5180633386396,
10.9227578478658));
#123719=CARTESIAN_POINT('Ctrl Pts',(-11.1749258202402,12.5177616029668,
10.9183682893257));
#123720=CARTESIAN_POINT('Ctrl Pts',(-11.1743567166375,12.5172295871915,
10.9105971335661));
#123721=CARTESIAN_POINT('Ctrl Pts',(-11.1740943331922,12.5169987760645,
10.9072149354266));
#123722=CARTESIAN_POINT('Ctrl Pts',(-11.1734911804317,12.5164979759127,
10.899852774744));
#123723=CARTESIAN_POINT('Ctrl Pts',(-11.1731447760542,12.5162282974416,
10.8958733805657));
#123724=CARTESIAN_POINT('Ctrl Pts',(-11.1721187025306,12.5154765790728,
10.8847419346606));
#123725=CARTESIAN_POINT('Ctrl Pts',(-11.1713938158466,12.5149969360654,
10.8775940811916));
#123726=CARTESIAN_POINT('Ctrl Pts',(-11.1666061885918,12.5121100609931,
10.8343324279586));
#123727=CARTESIAN_POINT('Ctrl Pts',(-11.1609386913637,12.5097809823345,
10.7984121461238));
#123728=CARTESIAN_POINT('Ctrl Pts',(-11.1310742290487,12.5004343553015,
10.6531619437831));
#123729=CARTESIAN_POINT('Ctrl Pts',(-11.0930159292454,12.4937306902847,
10.5472936672179));
#123730=CARTESIAN_POINT('Ctrl Pts',(-11.0310283513882,12.4851755731495,
10.4303580711809));
#123731=CARTESIAN_POINT('Ctrl Pts',(-11.0210054743986,12.4838426494338,
10.4125826614298));
#123732=CARTESIAN_POINT('Ctrl Pts',(-11.006168568574,12.4819325386807,10.387797532695));
#123733=CARTESIAN_POINT('Ctrl Pts',(-11.0017322669786,12.4813687827273,
10.3805651701695));
#123734=CARTESIAN_POINT('Ctrl Pts',(-10.9939346381446,12.4803900522237,
10.3681558038375));
#123735=CARTESIAN_POINT('Ctrl Pts',(-10.9906099994122,12.4799764218833,
10.3629560613829));
#123736=CARTESIAN_POINT('Ctrl Pts',(-10.9841457227841,12.4791790094774,
10.3530188897202));
#123737=CARTESIAN_POINT('Ctrl Pts',(-10.9810123533457,12.4787954666535,
10.348277573373));
#123738=CARTESIAN_POINT('Ctrl Pts',(-10.9726973661277,12.4777852850294,
10.3358914340319));
#123739=CARTESIAN_POINT('Ctrl Pts',(-10.9674600139073,12.4771565854204,
10.3282846834106));
#123740=CARTESIAN_POINT('Ctrl Pts',(-10.948474968276,12.4749036274125,10.3013934064281));
#123741=CARTESIAN_POINT('Ctrl Pts',(-10.9342365296448,12.4732610391562,
10.2824640038576));
#123742=CARTESIAN_POINT('Ctrl Pts',(-10.8640759169286,12.4653762176606,
10.1948194565096));
#123743=CARTESIAN_POINT('Ctrl Pts',(-10.801094551065,12.4588622807454,10.1321372571497));
#123744=CARTESIAN_POINT('Ctrl Pts',(-10.7261162005275,12.4518530284067,
10.0726914949289));
#123745=CARTESIAN_POINT('Ctrl Pts',(-10.7204945253284,12.4513317459406,
10.0683168776095));
#123746=CARTESIAN_POINT('Ctrl Pts',(-10.6795848309468,12.4475702872252,
10.0370739118507));
#123747=CARTESIAN_POINT('Ctrl Pts',(-10.6428397950433,12.444360791642,10.0121639728208));
#123748=CARTESIAN_POINT('Ctrl Pts',(-10.5969669140284,12.440621295372,9.984712684578));
#123749=CARTESIAN_POINT('Ctrl Pts',(-10.5891061618307,12.4399895537027,
9.98013149278667));
#123750=CARTESIAN_POINT('Ctrl Pts',(-10.5774174254342,12.4390643231345,
9.9734996243037));
#123751=CARTESIAN_POINT('Ctrl Pts',(-10.5736301422479,12.4387667046716,
9.97137841461988));
#123752=CARTESIAN_POINT('Ctrl Pts',(-10.5668634667379,12.4382389180998,
9.96763748059245));
#123753=CARTESIAN_POINT('Ctrl Pts',(-10.5638887156563,12.438008254587,9.96600963315684));
#123754=CARTESIAN_POINT('Ctrl Pts',(-10.5573507053667,12.4375042816974,
9.96246850181343));
#123755=CARTESIAN_POINT('Ctrl Pts',(-10.5537845939901,12.4372313115131,
9.96056070731184));
#123756=CARTESIAN_POINT('Ctrl Pts',(-10.5436588932818,12.4364614474871,
9.9552105732648));
#123757=CARTESIAN_POINT('Ctrl Pts',(-10.5370764158648,12.4359671375187,
9.95181162528969));
#123758=CARTESIAN_POINT('Ctrl Pts',(-10.4920233428744,12.4326226419558,
9.92908373425419));
#123759=CARTESIAN_POINT('Ctrl Pts',(-10.452545484898,12.4298827672595,9.91181248020323));
#123760=CARTESIAN_POINT('Ctrl Pts',(-10.3955466647752,12.426071048336,9.89051625698182));
#123761=CARTESIAN_POINT('Ctrl Pts',(-10.3787481094242,12.4249647734204,
9.88466989890805));
#123762=CARTESIAN_POINT('Ctrl Pts',(-10.317283313217,12.4209588483814,9.86482736107988));
#123763=CARTESIAN_POINT('Ctrl Pts',(-10.2719264923229,12.4180803149453,
9.8531165990746));
#123764=CARTESIAN_POINT('Ctrl Pts',(-10.1731205530919,12.4117912305726,
9.83379814898562));
#123765=CARTESIAN_POINT('Ctrl Pts',(-10.1196068466762,12.4083722814087,
9.8271016259962));
#123766=CARTESIAN_POINT('Ctrl Pts',(-10.0542309563397,12.4040751518198,
9.82344190264234));
#123767=CARTESIAN_POINT('Ctrl Pts',(-10.0426262548855,12.4033079871435,
9.82296434216628));
#123768=CARTESIAN_POINT('Ctrl Pts',(-10.0241990088803,12.4020819532691,
9.82247888177279));
#123769=CARTESIAN_POINT('Ctrl Pts',(-10.0173799932372,12.4016265572039,
9.82235849748672));
#123770=CARTESIAN_POINT('Ctrl Pts',(-10.0045113276275,12.4007637601384,
9.82224310442615));
#123771=CARTESIAN_POINT('Ctrl Pts',(-9.99846199040873,12.4003567627693,
9.82223546948614));
#123772=CARTESIAN_POINT('Ctrl Pts',(-9.98477333157773,12.3994324743206,
9.82232365338146));
#123773=CARTESIAN_POINT('Ctrl Pts',(-9.97713452480975,12.3989143442458,
9.82244720113989));
#123774=CARTESIAN_POINT('Ctrl Pts',(-9.95389411097235,12.3973305713491,
9.82304930340815));
#123775=CARTESIAN_POINT('Ctrl Pts',(-9.9383008709507,12.3962577457753,9.82376368351143));
#123776=CARTESIAN_POINT('Ctrl Pts',(-9.88532245655986,12.3925764129702,
9.82724713746238));
#123777=CARTESIAN_POINT('Ctrl Pts',(-9.84808779705843,12.3899264143302,
9.83148889359536));
#123778=CARTESIAN_POINT('Ctrl Pts',(-9.81114930150156,12.3872370429983,
9.83748958018577));
#123779=CARTESIAN_POINT('Ctrl Pts',(-9.81114930147754,12.2889045666398,
9.83748958018968));
#123780=CARTESIAN_POINT('Ctrl Pts',(-9.81383173227387,12.2890900172582,
9.83705381727436));
#123781=CARTESIAN_POINT('Ctrl Pts',(-9.81651570929456,12.2892749519145,
9.83662733246075));
#123782=CARTESIAN_POINT('Ctrl Pts',(-9.82298737303286,12.2897193534125,
9.83562193711081));
#123783=CARTESIAN_POINT('Ctrl Pts',(-9.82677644394306,12.2899783050531,
9.83505221399412));
#123784=CARTESIAN_POINT('Ctrl Pts',(-9.83713737611941,12.2906831715642,
9.83354601761439));
#123785=CARTESIAN_POINT('Ctrl Pts',(-9.84371460154284,12.2911270965891,
9.83264658026892));
#123786=CARTESIAN_POINT('Ctrl Pts',(-9.87610734113437,12.2932976282326,
9.82849555443918));
#123787=CARTESIAN_POINT('Ctrl Pts',(-9.90202018048166,12.2949847476504,
9.82604419001744));
#123788=CARTESIAN_POINT('Ctrl Pts',(-10.0093483690408,12.3018478843484,
9.81947009334006));
#123789=CARTESIAN_POINT('Ctrl Pts',(-10.0910041442942,12.3067875563781,
9.82294501328452));
#123790=CARTESIAN_POINT('Ctrl Pts',(-10.2264940354,12.3153341786876,9.84290514455523));
#123791=CARTESIAN_POINT('Ctrl Pts',(-10.2806912153051,12.3188477973632,
9.85484528147258));
#123792=CARTESIAN_POINT('Ctrl Pts',(-10.3450495814925,12.3232513836494,
9.87386837710154));
#123793=CARTESIAN_POINT('Ctrl Pts',(-10.3562068552719,12.3240232546126,
9.87734764682795));
#123794=CARTESIAN_POINT('Ctrl Pts',(-10.3738037736563,12.325254983368,9.88312377085827));
#123795=CARTESIAN_POINT('Ctrl Pts',(-10.3802785640701,12.3257113095331,
9.8853117104703));
#123796=CARTESIAN_POINT('Ctrl Pts',(-10.3924436753499,12.3265747313485,
9.88954083070421));
#123797=CARTESIAN_POINT('Ctrl Pts',(-10.3981380585138,12.3269814135963,
9.8915697184646));
#123798=CARTESIAN_POINT('Ctrl Pts',(-10.4109664978768,12.3279034355693,
9.89625205161689));
#123799=CARTESIAN_POINT('Ctrl Pts',(-10.4180908991964,12.3284195994309,
9.89893097798448));
#123800=CARTESIAN_POINT('Ctrl Pts',(-10.4396139290726,12.3299917305461,
9.9072631018026));
#123801=CARTESIAN_POINT('Ctrl Pts',(-10.4539271228197,12.3310547287337,
9.91313088961841));
#123802=CARTESIAN_POINT('Ctrl Pts',(-10.5502698728734,12.3383328789426,
9.95486224856121));
#123803=CARTESIAN_POINT('Ctrl Pts',(-10.6280801335751,12.3448567434955,
9.99969034442004));
#123804=CARTESIAN_POINT('Ctrl Pts',(-10.7366301626911,12.354762618692,10.0799236801379));
#123805=CARTESIAN_POINT('Ctrl Pts',(-10.7716170726544,12.358097575809,10.1090611746994));
#123806=CARTESIAN_POINT('Ctrl Pts',(-10.8213211854691,12.3629733663097,
10.1555850179048));
#123807=CARTESIAN_POINT('Ctrl Pts',(-10.8373640777366,12.3645707057991,
10.171491271185));
#123808=CARTESIAN_POINT('Ctrl Pts',(-10.8571467901598,12.366560312435,10.1922675900918));
#123809=CARTESIAN_POINT('Ctrl Pts',(-10.8613185742236,12.3669810534016,
10.1967176190142));
#123810=CARTESIAN_POINT('Ctrl Pts',(-10.8679741308999,12.3676539068072,
10.203928547089));
#123811=CARTESIAN_POINT('Ctrl Pts',(-10.8704796794235,12.367907583808,10.2066690610299));
#123812=CARTESIAN_POINT('Ctrl Pts',(-10.8752763759233,12.3683938770941,
10.2119656667887));
#123813=CARTESIAN_POINT('Ctrl Pts',(-10.8775693565291,12.3686266217461,
10.2145199751907));
#123814=CARTESIAN_POINT('Ctrl Pts',(-10.8826144134907,12.3691394202105,
10.2201896778483));
#123815=CARTESIAN_POINT('Ctrl Pts',(-10.8853612569619,12.3694190947035,
10.2233097223448));
#123816=CARTESIAN_POINT('Ctrl Pts',(-10.8950573742619,12.3704082953551,
10.2344414871539));
#123817=CARTESIAN_POINT('Ctrl Pts',(-10.9019151334402,12.3711115665998,
10.2425327392474));
#123818=CARTESIAN_POINT('Ctrl Pts',(-10.9487048044757,12.3759445115104,
10.2992749527889));
#123819=CARTESIAN_POINT('Ctrl Pts',(-10.9847951520627,12.3798541930568,
10.3509722981556));
#123820=CARTESIAN_POINT('Ctrl Pts',(-11.0365092950994,12.3861946413552,
10.4393746423769));
#123821=CARTESIAN_POINT('Ctrl Pts',(-11.0547102834317,12.3886280209249,
10.4744160904239));
#123822=CARTESIAN_POINT('Ctrl Pts',(-11.0936826949566,12.394481730254,10.5596609437193));
#123823=CARTESIAN_POINT('Ctrl Pts',(-11.1128066182164,12.3979247438835,
10.6105123319528));
#123824=CARTESIAN_POINT('Ctrl Pts',(-11.1316890345852,12.4022488582423,
10.6736408508139));
#123825=CARTESIAN_POINT('Ctrl Pts',(-11.1348569835265,12.4030171710055,
10.6848334147411));
#123826=CARTESIAN_POINT('Ctrl Pts',(-11.1396192647359,12.4042445492705,
10.7026625717775));
#123827=CARTESIAN_POINT('Ctrl Pts',(-11.1413226362922,12.4047001272313,
10.7092694522982));
#123828=CARTESIAN_POINT('Ctrl Pts',(-11.1444272645068,12.4055629617689,
10.7217593338015));
#123829=CARTESIAN_POINT('Ctrl Pts',(-11.1458408076143,12.4059698122316,
10.7276390752276));
#123830=CARTESIAN_POINT('Ctrl Pts',(-11.1489355190148,12.4068933463511,
10.7409624213983));
#123831=CARTESIAN_POINT('Ctrl Pts',(-11.1505897351065,12.4074108646688,
10.7484119424355));
#123832=CARTESIAN_POINT('Ctrl Pts',(-11.155291028379,12.4089559472228,10.7706003174318));
#123833=CARTESIAN_POINT('Ctrl Pts',(-11.1581280060205,12.4099900338806,
10.7853815944423));
#123834=CARTESIAN_POINT('Ctrl Pts',(-11.1762906896256,12.4174091955278,
10.890899156526));
#123835=CARTESIAN_POINT('Ctrl Pts',(-11.1812156698372,12.4241232825722,
10.9830866878563));
#123836=CARTESIAN_POINT('Ctrl Pts',(-11.1725744385655,12.4340953702116,
11.1187130782638));
#123837=CARTESIAN_POINT('Ctrl Pts',(-11.1673328681741,12.4373115991175,
11.1623515743318));
#123838=CARTESIAN_POINT('Ctrl Pts',(-11.155804320499,12.4420384271522,11.2273779522965));
#123839=CARTESIAN_POINT('Ctrl Pts',(-11.1513297072006,12.4436020800488,
11.2490470190653));
#123840=CARTESIAN_POINT('Ctrl Pts',(-11.1448551867644,12.4455562824911,
11.2764748909272));
#123841=CARTESIAN_POINT('Ctrl Pts',(-11.1434178589975,12.4459741282282,
11.2823603506691));
#123842=CARTESIAN_POINT('Ctrl Pts',(-11.1410286320628,12.4466434761926,
11.2918260500629));
#123843=CARTESIAN_POINT('Ctrl Pts',(-11.1401051675985,12.4468965148387,
11.2954132536908));
#123844=CARTESIAN_POINT('Ctrl Pts',(-11.1382923925061,12.4473824207276,
11.3023198638966));
#123845=CARTESIAN_POINT('Ctrl Pts',(-11.1374054609663,12.4476154100539,
11.3056398021211));
#123846=CARTESIAN_POINT('Ctrl Pts',(-11.1354089212677,12.4481296270556,
11.3129841375192));
#123847=CARTESIAN_POINT('Ctrl Pts',(-11.1342924100443,12.448410467045,11.3170066539719));
#123848=CARTESIAN_POINT('Ctrl Pts',(-11.1303481425142,12.4493800003188,
11.3309292122626));
#123849=CARTESIAN_POINT('Ctrl Pts',(-11.1274118783254,12.4500628765946,
11.340798387688));
#123850=CARTESIAN_POINT('Ctrl Pts',(-11.1038793784072,12.4552594719201,
11.416259184072));
#123851=CARTESIAN_POINT('Ctrl Pts',(-11.0777021179619,12.4595082351514,
11.4799813422831));
#123852=CARTESIAN_POINT('Ctrl Pts',(-11.0190893860017,12.4674010076476,
11.5933054904039));
#123853=CARTESIAN_POINT('Ctrl Pts',(-10.9881945566757,12.4710326836439,
11.6434481234495));
#123854=CARTESIAN_POINT('Ctrl Pts',(-10.9409783680066,12.4761541728011,
11.7086068849954));
#123855=CARTESIAN_POINT('Ctrl Pts',(-10.9277911490262,12.4775459195896,
11.7257875075303));
#123856=CARTESIAN_POINT('Ctrl Pts',(-10.9038809566076,12.4800131027819,
11.7552211165978));
#123857=CARTESIAN_POINT('Ctrl Pts',(-10.893363413515,12.4810808247063,11.7676336941122));
#123858=CARTESIAN_POINT('Ctrl Pts',(-10.8774524296126,12.4826732857733,
11.7856414962697));
#123859=CARTESIAN_POINT('Ctrl Pts',(-10.8722550154339,12.4831900344556,
11.7914079290279));
#123860=CARTESIAN_POINT('Ctrl Pts',(-10.8628993845384,12.4841144160741,
11.8015837082938));
#123861=CARTESIAN_POINT('Ctrl Pts',(-10.8587633859077,12.4845211103968,
11.806013172301));
#123862=CARTESIAN_POINT('Ctrl Pts',(-10.8499538023294,12.4853833745067,
11.8153030481195));
#123863=CARTESIAN_POINT('Ctrl Pts',(-10.8452723087885,12.4858392732942,
11.8201556237085));
#123864=CARTESIAN_POINT('Ctrl Pts',(-10.832659036157,12.4870616482828,11.8330071335704));
#123865=CARTESIAN_POINT('Ctrl Pts',(-10.8246538960569,12.4878312867054,
11.8409327508884));
#123866=CARTESIAN_POINT('Ctrl Pts',(-10.7863150082217,12.4914897826344,
11.8778168680624));
#123867=CARTESIAN_POINT('Ctrl Pts',(-10.7545657022235,12.4944413852421,
11.9052533422834));
#123868=CARTESIAN_POINT('Ctrl Pts',(-10.634773938621,12.5053073404985,11.9980853860355));
#123869=CARTESIAN_POINT('Ctrl Pts',(-10.5391842613604,12.5135454495557,
12.0528008253265));
#123870=CARTESIAN_POINT('Ctrl Pts',(-10.4279657758124,12.5220272348384,
12.097289356547));
#123871=CARTESIAN_POINT('Ctrl Pts',(-10.4184675869722,12.5227428703444,
12.1009466524536));
#123872=CARTESIAN_POINT('Ctrl Pts',(-10.4015548069343,12.5240003686634,
12.1072084397259));
#123873=CARTESIAN_POINT('Ctrl Pts',(-10.3941594166615,12.5245446123103,
12.1098626737236));
#123874=CARTESIAN_POINT('Ctrl Pts',(-10.3828735705865,12.5253660735851,
12.1137861680705));
#123875=CARTESIAN_POINT('Ctrl Pts',(-10.379002319948,12.525646234837,12.1151094304975));
#123876=CARTESIAN_POINT('Ctrl Pts',(-10.3719155598545,12.5261560559811,
12.1174906426592));
#123877=CARTESIAN_POINT('Ctrl Pts',(-10.3687023545423,12.5263860649456,
12.1185549134768));
#123878=CARTESIAN_POINT('Ctrl Pts',(-10.3614199813835,12.5269047844032,
12.1209321746096));
#123879=CARTESIAN_POINT('Ctrl Pts',(-10.3573482163626,12.5271930173748,
12.1222368719274));
#123880=CARTESIAN_POINT('Ctrl Pts',(-10.3467516696572,12.5279386886658,
12.1255687549981));
#123881=CARTESIAN_POINT('Ctrl Pts',(-10.3402160848432,12.5283942375078,
12.1275614234385));
#123882=CARTESIAN_POINT('Ctrl Pts',(-10.2879317211156,12.5320067027754,
12.1430066818791));
#123883=CARTESIAN_POINT('Ctrl Pts',(-10.2414158378224,12.5350271686034,
12.1537280799974));
#123884=CARTESIAN_POINT('Ctrl Pts',(-10.1189054147635,12.5427815828107,
12.1742279749265));
#123885=CARTESIAN_POINT('Ctrl Pts',(-10.0423889904386,12.5474393654137,
12.1794715062008));
#123886=CARTESIAN_POINT('Ctrl Pts',(-9.92748329316009,12.5547059698119,
12.176143617985));
#123887=CARTESIAN_POINT('Ctrl Pts',(-9.88914318632026,12.5571737880781,
12.173150795251));
#123888=CARTESIAN_POINT('Ctrl Pts',(-9.84011850951595,12.5604215082524,
12.1668992078778));
#123889=CARTESIAN_POINT('Ctrl Pts',(-9.8292366569593,12.5611482064698,12.1653564775146));
#123890=CARTESIAN_POINT('Ctrl Pts',(-9.81177436318909,12.5623244558508,
12.162631001767));
#123891=CARTESIAN_POINT('Ctrl Pts',(-9.80517945702542,12.5627710119694,
12.1615440971186));
#123892=CARTESIAN_POINT('Ctrl Pts',(-9.79260891427126,12.5636268060776,
12.159362283235));
#123893=CARTESIAN_POINT('Ctrl Pts',(-9.78663178150155,12.564035724877,12.1582771547397));
#123894=CARTESIAN_POINT('Ctrl Pts',(-9.77292413074451,12.5649782453653,
12.1556788742987));
#123895=CARTESIAN_POINT('Ctrl Pts',(-9.76519993516243,12.5655128178143,
12.1541343228734));
#123896=CARTESIAN_POINT('Ctrl Pts',(-9.74097322673439,12.5672007182818,
12.1490366154183));
#123897=CARTESIAN_POINT('Ctrl Pts',(-9.72453190157307,12.5683626817358,
12.1452062209552));
#123898=CARTESIAN_POINT('Ctrl Pts',(-9.68615936799015,12.5711148316239,
12.1353923165588));
#123899=CARTESIAN_POINT('Ctrl Pts',(-9.66430842761712,12.5727133462199,
12.1291247523341));
#123900=CARTESIAN_POINT('Ctrl Pts',(-9.53385442457937,12.582446407804,12.08758488285));
#123901=CARTESIAN_POINT('Ctrl Pts',(-9.430691227497,12.5910250083356,12.0373110505005));
#123902=CARTESIAN_POINT('Ctrl Pts',(-9.32077732291851,12.6005096726938,
11.962345260387));
#123903=CARTESIAN_POINT('Ctrl Pts',(-9.30542978302708,12.6018408142823,
11.9513275760085));
#123904=CARTESIAN_POINT('Ctrl Pts',(-9.28560293330061,12.6035628564676,
11.9363585407384));
#123905=CARTESIAN_POINT('Ctrl Pts',(-9.28088006361357,12.6039732378647,
11.9327363006486));
#123906=CARTESIAN_POINT('Ctrl Pts',(-9.27328101219053,12.6046335635537,
11.9268161222098));
#123907=CARTESIAN_POINT('Ctrl Pts',(-9.27038786150642,12.6048849723301,
11.9245402857287));
#123908=CARTESIAN_POINT('Ctrl Pts',(-9.26477103355307,12.6053729973934,
11.9200791392653));
#123909=CARTESIAN_POINT('Ctrl Pts',(-9.26204634421165,12.6056096979167,
11.917895232544));
#123910=CARTESIAN_POINT('Ctrl Pts',(-9.25540042905378,12.6061870592657,
11.9125196455374));
#123911=CARTESIAN_POINT('Ctrl Pts',(-9.25148990493053,12.6065267986259,
11.9093147224343));
#123912=CARTESIAN_POINT('Ctrl Pts',(-9.23731268332321,12.6077590530955,
11.897542156968));
#123913=CARTESIAN_POINT('Ctrl Pts',(-9.22717100683596,12.6086416336667,
11.8888246457526));
#123914=CARTESIAN_POINT('Ctrl Pts',(-9.15098072007739,12.6153002315115,
11.8210432057346));
#123915=CARTESIAN_POINT('Ctrl Pts',(-9.09163063385042,12.6206679816203,
11.7548608605004));
#123916=CARTESIAN_POINT('Ctrl Pts',(-9.00370540351625,12.6300950971517,
11.6312447052773));
#123917=CARTESIAN_POINT('Ctrl Pts',(-8.97134151426516,12.634066809928,11.577003457373));
#123918=CARTESIAN_POINT('Ctrl Pts',(-8.93812220494041,12.6389938285286,
11.5095659544643));
#123919=CARTESIAN_POINT('Ctrl Pts',(-8.9329355465158,12.6397934233851,11.4986134254098));
#123920=CARTESIAN_POINT('Ctrl Pts',(-8.92502114557952,12.6410639236338,
11.4812115127273));
#123921=CARTESIAN_POINT('Ctrl Pts',(-8.92218024081496,12.6415309902298,
11.474814301163));
#123922=CARTESIAN_POINT('Ctrl Pts',(-8.91699808661008,12.6424040822049,
11.4628588227457));
#123923=CARTESIAN_POINT('Ctrl Pts',(-8.91464217084767,12.6428095978943,
11.4573071337555));
#123924=CARTESIAN_POINT('Ctrl Pts',(-8.90949529707561,12.6437150930461,
11.4449147534415));
#123925=CARTESIAN_POINT('Ctrl Pts',(-8.90672587948089,12.6442157719862,
11.4380654494884));
#123926=CARTESIAN_POINT('Ctrl Pts',(-8.89877656886888,12.6456936182524,
11.4178602899702));
#123927=CARTESIAN_POINT('Ctrl Pts',(-8.89377585113021,12.6466766265054,
11.404435864322));
#123928=CARTESIAN_POINT('Ctrl Pts',(-8.87217991296978,12.651177705311,11.3430617331618));
#123929=CARTESIAN_POINT('Ctrl Pts',(-8.85845116710635,12.6547858854001,
11.2941675333026));
#123930=CARTESIAN_POINT('Ctrl Pts',(-8.83140579959324,12.6642207392366,
11.1667541177985));
#123931=CARTESIAN_POINT('Ctrl Pts',(-8.82281541907372,12.6701307758134,
11.0874937278619));
#123932=CARTESIAN_POINT('Ctrl Pts',(-8.82208805224753,12.6778756390834,
10.9800691998945));
#123933=CARTESIAN_POINT('Ctrl Pts',(-8.82289093543136,12.6798613753455,
10.9521635765681));
#123934=CARTESIAN_POINT('Ctrl Pts',(-8.82511505088381,12.6822668131692,
10.9176272494007));
#123935=CARTESIAN_POINT('Ctrl Pts',(-8.82560245808805,12.6827296136136,
10.9109475857441));
#123936=CARTESIAN_POINT('Ctrl Pts',(-8.82646247863124,12.6834560664612,
10.9004016588598));
#123937=CARTESIAN_POINT('Ctrl Pts',(-8.82679727333158,12.6837216875961,
10.8965325807228));
#123938=CARTESIAN_POINT('Ctrl Pts',(-8.82746194930453,12.6842185268924,
10.8892696602143));
#123939=CARTESIAN_POINT('Ctrl Pts',(-8.82778742918393,12.6844499655391,
10.8858756044523));
#123940=CARTESIAN_POINT('Ctrl Pts',(-8.82858384972127,12.6849898415465,
10.8779337556712));
#123941=CARTESIAN_POINT('Ctrl Pts',(-8.82906653734369,12.6852976306464,
10.873387232452));
#123942=CARTESIAN_POINT('Ctrl Pts',(-8.83073208749951,12.6862999909181,
10.8585240652326));
#123943=CARTESIAN_POINT('Ctrl Pts',(-8.83202495304457,12.6869888344812,
10.8482198987244));
#123944=CARTESIAN_POINT('Ctrl Pts',(-8.8401121556615,12.6908528267042,10.7900085556355));
#123945=CARTESIAN_POINT('Ctrl Pts',(-8.84971818265734,12.6938994901274,
10.7425334265172));
#123946=CARTESIAN_POINT('Ctrl Pts',(-8.88432411217041,12.7022368463267,
10.6131078186209));
#123947=CARTESIAN_POINT('Ctrl Pts',(-8.91537150895569,12.7074455303491,
10.5330967194049));
#123948=CARTESIAN_POINT('Ctrl Pts',(-8.96724838437296,12.7146511125664,
10.4332133857361));
#123949=CARTESIAN_POINT('Ctrl Pts',(-8.98050195524227,12.7164008428838,
10.4097064064854));
#123950=CARTESIAN_POINT('Ctrl Pts',(-8.99960050817822,12.7188179952596,
10.3783972557602));
#123951=CARTESIAN_POINT('Ctrl Pts',(-9.00475279765119,12.7194607006416,
10.3701808895838));
#123952=CARTESIAN_POINT('Ctrl Pts',(-9.01312728376249,12.7204911812416,
10.3571854775149));
#123953=CARTESIAN_POINT('Ctrl Pts',(-9.01628418375284,12.7208765591536,
10.3523647174228));
#123954=CARTESIAN_POINT('Ctrl Pts',(-9.02285815988468,12.721672919849,10.3424848625733));
#123955=CARTESIAN_POINT('Ctrl Pts',(-9.02627944355355,12.7220840504695,
10.3374287908513));
#123956=CARTESIAN_POINT('Ctrl Pts',(-9.03434531225376,12.7230458007598,
10.3257062222593));
#123957=CARTESIAN_POINT('Ctrl Pts',(-9.03901983408079,12.7235975328591,
10.3190608032694));
#123958=CARTESIAN_POINT('Ctrl Pts',(-9.05444292695788,12.7254001848041,
10.2976100767621));
#123959=CARTESIAN_POINT('Ctrl Pts',(-9.06546733670553,12.7266615174542,
10.2830073787407));
#123960=CARTESIAN_POINT('Ctrl Pts',(-9.12791011315197,12.7336648027364,
10.2041847677976));
#123961=CARTESIAN_POINT('Ctrl Pts',(-9.1856006621458,12.7396550354643,10.1452415614109));
#123962=CARTESIAN_POINT('Ctrl Pts',(-9.29805742075508,12.7503698574778,
10.0521411516742));
#123963=CARTESIAN_POINT('Ctrl Pts',(-9.35039191603067,12.7550519855471,
10.0155353481846));
#123964=CARTESIAN_POINT('Ctrl Pts',(-9.41368114100117,12.7601988112945,
9.97852240813713));
#123965=CARTESIAN_POINT('Ctrl Pts',(-9.42198400478981,12.7608643245444,
9.97380128700313));
#123966=CARTESIAN_POINT('Ctrl Pts',(-9.43474843910004,12.7618717227801,
9.96674733856949));
#123967=CARTESIAN_POINT('Ctrl Pts',(-9.4391688396424,12.7622177496953,9.96434136834038));
#123968=CARTESIAN_POINT('Ctrl Pts',(-9.44664485640826,12.7627980265347,
9.96033416613209));
#123969=CARTESIAN_POINT('Ctrl Pts',(-9.44969229957226,12.7630331905975,
9.95871790705176));
#123970=CARTESIAN_POINT('Ctrl Pts',(-9.45599999319334,12.7635170484619,
9.95540794953687));
#123971=CARTESIAN_POINT('Ctrl Pts',(-9.45926112821108,12.7637656306932,
9.9537160840547));
#123972=CARTESIAN_POINT('Ctrl Pts',(-9.46780137686993,12.7644126480962,
9.94933602795103));
#123973=CARTESIAN_POINT('Ctrl Pts',(-9.4730930301969,12.764809608459,9.94667231810796));
#123974=CARTESIAN_POINT('Ctrl Pts',(-9.49695672178769,12.7665831506817,
9.93488466453105));
#123975=CARTESIAN_POINT('Ctrl Pts',(-9.51574840485089,12.7679347877326,
9.92621057213089));
#123976=CARTESIAN_POINT('Ctrl Pts',(-9.57089692878683,12.7718003172363,
9.9024969585786));
#123977=CARTESIAN_POINT('Ctrl Pts',(-9.60779219707913,12.7742623584784,
9.88877730847137));
#123978=CARTESIAN_POINT('Ctrl Pts',(-9.69961543009393,12.7802429163818,
9.85977733714761));
#123979=CARTESIAN_POINT('Ctrl Pts',(-9.75504250514998,12.7837322841863,
9.84660417176354));
#123980=CARTESIAN_POINT('Ctrl Pts',(-9.81114930150157,12.7872971999427,
9.83748958018577));
#123981=CARTESIAN_POINT('Origin',(-10.,2.67563288526385,11.));
#123982=CARTESIAN_POINT('',(-8.88725970493355,13.15,11.3858809379011));
#123983=CARTESIAN_POINT('Ctrl Pts',(-9.81114930150157,12.7872971999427,
9.83748958018577));
#123984=CARTESIAN_POINT('Ctrl Pts',(-9.85064840761449,12.7898068956463,
9.83107292047043));
#123985=CARTESIAN_POINT('Ctrl Pts',(-9.89048444922047,12.7923530522079,
9.82666770785197));
#123986=CARTESIAN_POINT('Ctrl Pts',(-9.94663828774431,12.7960136030827,
9.82334849075221));
#123987=CARTESIAN_POINT('Ctrl Pts',(-9.96278856564973,12.7970744726786,
9.82272708569078));
#123988=CARTESIAN_POINT('Ctrl Pts',(-9.98669013886237,12.7986588315724,
9.82229973999947));
#123989=CARTESIAN_POINT('Ctrl Pts',(-9.99443538998884,12.799174457132,9.82223767884118));
#123990=CARTESIAN_POINT('Ctrl Pts',(-10.0082416296171,12.8000977904741,
9.82226324036451));
#123991=CARTESIAN_POINT('Ctrl Pts',(-10.0143024454134,12.800504571097,9.82232125043788));
#123992=CARTESIAN_POINT('Ctrl Pts',(-10.027120084049,12.8013680283292,9.82254289129614));
#123993=CARTESIAN_POINT('Ctrl Pts',(-10.0338764643338,12.8018250417664,
9.82271790819828));
#123994=CARTESIAN_POINT('Ctrl Pts',(-10.0519517448613,12.8030528792592,
9.82334185329487));
#123995=CARTESIAN_POINT('Ctrl Pts',(-10.0632660616117,12.803826910191,9.82389593660675));
#123996=CARTESIAN_POINT('Ctrl Pts',(-10.1230689540906,12.8079482890019,
9.82769002283007));
#123997=CARTESIAN_POINT('Ctrl Pts',(-10.1713241722421,12.8113817712899,
9.83376522166938));
#123998=CARTESIAN_POINT('Ctrl Pts',(-10.2684680361244,12.8185071586902,
9.85215484172937));
#123999=CARTESIAN_POINT('Ctrl Pts',(-10.3172227257137,12.8221968221134,
9.86466182323661));
#124000=CARTESIAN_POINT('Ctrl Pts',(-10.3833145208831,12.8272968664482,
9.88620690359202));
#124001=CARTESIAN_POINT('Ctrl Pts',(-10.401454686601,12.8287068810652,9.89261603818782));
#124002=CARTESIAN_POINT('Ctrl Pts',(-10.4603959511511,12.8333092993468,
9.91507944917733));
#124003=CARTESIAN_POINT('Ctrl Pts',(-10.5004630618422,12.8364724544636,
9.93296925254057));
#124004=CARTESIAN_POINT('Ctrl Pts',(-10.5460305082256,12.840042841253,9.95644805498468));
#124005=CARTESIAN_POINT('Ctrl Pts',(-10.5525860006101,12.8405557785544,
9.95990447708994));
#124006=CARTESIAN_POINT('Ctrl Pts',(-10.5626705435065,12.8413432513868,
9.96534387343638));
#124007=CARTESIAN_POINT('Ctrl Pts',(-10.566222591352,12.8416203109166,9.96728347595301));
#124008=CARTESIAN_POINT('Ctrl Pts',(-10.5727400850639,12.8421280067585,
9.97088610161777));
#124009=CARTESIAN_POINT('Ctrl Pts',(-10.5757083385015,12.8423589581212,
9.97254366013215));
#124010=CARTESIAN_POINT('Ctrl Pts',(-10.5824661353693,12.8428841936287,
9.97635588931542));
#124011=CARTESIAN_POINT('Ctrl Pts',(-10.5862509334626,12.8431779586374,
9.97851876732213));
#124012=CARTESIAN_POINT('Ctrl Pts',(-10.5979409157031,12.8440843346478,
9.98528555300132));
#124013=CARTESIAN_POINT('Ctrl Pts',(-10.605804754991,12.8446926752615,9.98996071412177));
#124014=CARTESIAN_POINT('Ctrl Pts',(-10.6241804707968,12.8461128936734,
10.0011771614478));
#124015=CARTESIAN_POINT('Ctrl Pts',(-10.6346454260007,12.8469206797104,
10.007793604037));
#124016=CARTESIAN_POINT('Ctrl Pts',(-10.6722966265972,12.8498305976039,
10.0324379689147));
#124017=CARTESIAN_POINT('Ctrl Pts',(-10.6988368009481,12.8518890116896,
10.0514292516681));
#124018=CARTESIAN_POINT('Ctrl Pts',(-10.7849522050021,12.8587123786858,
10.1186294379401));
#124019=CARTESIAN_POINT('Ctrl Pts',(-10.840604564399,12.8633793432393,10.1715387674165));
#124020=CARTESIAN_POINT('Ctrl Pts',(-10.9154652957684,12.8706186466293,
10.2580778984159));
#124021=CARTESIAN_POINT('Ctrl Pts',(-10.9388117405499,12.8730480455368,
10.2878503040314));
#124022=CARTESIAN_POINT('Ctrl Pts',(-10.9670423297474,12.8762553360454,
10.327657085576));
#124023=CARTESIAN_POINT('Ctrl Pts',(-10.9732743790793,12.8769821251904,
10.3367105972208));
#124024=CARTESIAN_POINT('Ctrl Pts',(-10.9830972662635,12.8781592268787,
10.3514171971944));
#124025=CARTESIAN_POINT('Ctrl Pts',(-10.9867682829658,12.878606559447,10.3570161435543));
#124026=CARTESIAN_POINT('Ctrl Pts',(-10.9936883970188,12.8794643442666,
10.3677693837309));
#124027=CARTESIAN_POINT('Ctrl Pts',(-10.9969456342904,12.8798744806926,
10.3729182011871));
#124028=CARTESIAN_POINT('Ctrl Pts',(-11.0043403187278,12.8808205698479,
10.3848104544928));
#124029=CARTESIAN_POINT('Ctrl Pts',(-11.0084500209594,12.881357503299,10.3915707085629));
#124030=CARTESIAN_POINT('Ctrl Pts',(-11.0211759631318,12.8830560975778,
10.4129874288123));
#124031=CARTESIAN_POINT('Ctrl Pts',(-11.0295427999917,12.884226510488,10.4277887825921));
#124032=CARTESIAN_POINT('Ctrl Pts',(-11.048431563209,12.887000988222,10.46296017347));
#124033=CARTESIAN_POINT('Ctrl Pts',(-11.0586845926314,12.8886135322086,
10.4834660399043));
#124034=CARTESIAN_POINT('Ctrl Pts',(-11.1175969135865,12.8985663482114,
10.6104227826123));
#124035=CARTESIAN_POINT('Ctrl Pts',(-11.1507538847801,12.9073748326706,
10.7233184485896));
#124036=CARTESIAN_POINT('Ctrl Pts',(-11.1689763819234,12.91685604592,10.855566575958));
#124037=CARTESIAN_POINT('Ctrl Pts',(-11.1708835505594,12.9180142777831,
10.8719430840064));
#124038=CARTESIAN_POINT('Ctrl Pts',(-11.1729825308593,12.9195474635182,
10.8939856869771));
#124039=CARTESIAN_POINT('Ctrl Pts',(-11.1734781339901,12.9199371118442,
10.8996200989351));
#124040=CARTESIAN_POINT('Ctrl Pts',(-11.1741951881055,12.9205477696985,
10.9085050033524));
#124041=CARTESIAN_POINT('Ctrl Pts',(-11.1744437680385,12.9207702178147,
10.9117531272488));
#124042=CARTESIAN_POINT('Ctrl Pts',(-11.1749276113275,12.9212264701463,
10.918439901416));
#124043=CARTESIAN_POINT('Ctrl Pts',(-11.1751612545557,12.9214601623584,
10.9218785071881));
#124044=CARTESIAN_POINT('Ctrl Pts',(-11.1756904856625,12.9220240582894,
10.9302078146349));
#124045=CARTESIAN_POINT('Ctrl Pts',(-11.1759706558401,12.9223534136191,
10.9350994148766));
#124046=CARTESIAN_POINT('Ctrl Pts',(-11.1768570537891,12.9235172961872,
10.952473963759));
#124047=CARTESIAN_POINT('Ctrl Pts',(-11.1772951372886,12.9243431390457,
10.9649651632963));
#124048=CARTESIAN_POINT('Ctrl Pts',(-11.1778942756681,12.9263906475012,
10.9962675311418));
#124049=CARTESIAN_POINT('Ctrl Pts',(-11.1778036825287,12.9276013322428,
11.0150804885096));
#124050=CARTESIAN_POINT('Ctrl Pts',(-11.175292968582,12.9331557136721,11.1023119296313));
#124051=CARTESIAN_POINT('Ctrl Pts',(-11.1673611679931,12.9373310189597,
11.1704419972551));
#124052=CARTESIAN_POINT('Ctrl Pts',(-11.1401835166149,12.9456867082197,
11.3024453450685));
#124053=CARTESIAN_POINT('Ctrl Pts',(-11.1213537969094,12.9498491887249,
11.3661360153631));
#124054=CARTESIAN_POINT('Ctrl Pts',(-11.0928648193882,12.95498645553,11.4391906493396));
#124055=CARTESIAN_POINT('Ctrl Pts',(-11.0882877621961,12.9557858698275,
11.450412775935));
#124056=CARTESIAN_POINT('Ctrl Pts',(-11.0808075126212,12.9570540509385,
11.4679730154782));
#124057=CARTESIAN_POINT('Ctrl Pts',(-11.0780197508826,12.9575189298154,
11.4743596059181));
#124058=CARTESIAN_POINT('Ctrl Pts',(-11.0727329168234,12.9583866217539,
11.4861840841294));
#124059=CARTESIAN_POINT('Ctrl Pts',(-11.0702487432218,12.9587889165432,
11.4916284164401));
#124060=CARTESIAN_POINT('Ctrl Pts',(-11.0646402360107,12.9596854728129,
11.5036760802582));
#124061=CARTESIAN_POINT('Ctrl Pts',(-11.0614957605435,12.9601804136823,
11.5102697052732));
#124062=CARTESIAN_POINT('Ctrl Pts',(-11.0521130655825,12.9616353298062,
11.5294821088002));
#124063=CARTESIAN_POINT('Ctrl Pts',(-11.0457099006386,12.9626009636563,
11.5420184314903));
#124064=CARTESIAN_POINT('Ctrl Pts',(-11.0306161470636,12.9648181883696,
11.5703060253895));
#124065=CARTESIAN_POINT('Ctrl Pts',(-11.0217864437812,12.9660743908674,
11.5859786756873));
#124066=CARTESIAN_POINT('Ctrl Pts',(-10.9905093442848,12.9703915323975,
11.6386375013316));
#124067=CARTESIAN_POINT('Ctrl Pts',(-10.9663865323899,12.9735060763644,
11.6745835921664));
#124068=CARTESIAN_POINT('Ctrl Pts',(-10.9036696872257,12.9810974977375,
11.757750775982));
#124069=CARTESIAN_POINT('Ctrl Pts',(-10.8632791638431,12.9856033701052,
11.8034638172549));
#124070=CARTESIAN_POINT('Ctrl Pts',(-10.7940019939752,12.9926084524547,
11.8705858955302));
#124071=CARTESIAN_POINT('Ctrl Pts',(-10.7673595116995,12.9951571567793,
11.8941581907598));
#124072=CARTESIAN_POINT('Ctrl Pts',(-10.7341460224141,12.9981284485604,
11.920964392835));
#124073=CARTESIAN_POINT('Ctrl Pts',(-10.7285627175034,12.9986212835788,
11.9253875772014));
#124074=CARTESIAN_POINT('Ctrl Pts',(-10.7198087418057,12.9993832693491,
11.9321942742457));
#124075=CARTESIAN_POINT('Ctrl Pts',(-10.7166656921114,12.9996547347482,
11.934612795031));
#124076=CARTESIAN_POINT('Ctrl Pts',(-10.7108398683953,13.0001539198479,
11.9390489929892));
#124077=CARTESIAN_POINT('Ctrl Pts',(-10.7081606885353,13.0003819319455,
11.9410710755734));
#124078=CARTESIAN_POINT('Ctrl Pts',(-10.7019566247551,13.0009064149162,
11.9457120287394));
#124079=CARTESIAN_POINT('Ctrl Pts',(-10.6984256969912,13.0012023246584,
11.9483226727575));
#124080=CARTESIAN_POINT('Ctrl Pts',(-10.6873221083331,13.0021250698465,
11.9564366212971));
#124081=CARTESIAN_POINT('Ctrl Pts',(-10.6796981660609,13.002747384879,11.9618695897508));
#124082=CARTESIAN_POINT('Ctrl Pts',(-10.661529779794,13.0042061095415,11.97449282608));
#124083=CARTESIAN_POINT('Ctrl Pts',(-10.6509314775494,13.0050380960689,
11.9816038699702));
#124084=CARTESIAN_POINT('Ctrl Pts',(-10.6115063934171,13.0080722588288,
12.0071371389317));
#124085=CARTESIAN_POINT('Ctrl Pts',(-10.5819948410109,13.0102263456181,
12.024474318512));
#124086=CARTESIAN_POINT('Ctrl Pts',(-10.4827129035858,13.017232897787,12.0771225347248));
#124087=CARTESIAN_POINT('Ctrl Pts',(-10.410185886626,13.0219916803197,12.1067755462806));
#124088=CARTESIAN_POINT('Ctrl Pts',(-10.3006818366798,13.0292317291624,
12.1392920116502));
#124089=CARTESIAN_POINT('Ctrl Pts',(-10.2656570909294,13.0315527336887,
12.1479641872666));
#124090=CARTESIAN_POINT('Ctrl Pts',(-10.219712919835,13.034633686254,12.1571247398477));
#124091=CARTESIAN_POINT('Ctrl Pts',(-10.2091055608103,13.0353474104155,
12.159088556825));
#124092=CARTESIAN_POINT('Ctrl Pts',(-10.1919068403152,13.0365092172225,
12.1620289160807));
#124093=CARTESIAN_POINT('Ctrl Pts',(-10.1853313881247,13.0369544768231,
12.1630957444161));
#124094=CARTESIAN_POINT('Ctrl Pts',(-10.1726969820333,13.0378122427771,
12.1650357440693));
#124095=CARTESIAN_POINT('Ctrl Pts',(-10.1666395613961,13.0382244650599,
12.1659175728696));
#124096=CARTESIAN_POINT('Ctrl Pts',(-10.1526157983865,13.0391812008066,
12.167847609798));
#124097=CARTESIAN_POINT('Ctrl Pts',(-10.1446451314917,13.0397267549422,
12.1688615837893));
#124098=CARTESIAN_POINT('Ctrl Pts',(-10.119159634303,13.0414771061904,12.1718390077806));
#124099=CARTESIAN_POINT('Ctrl Pts',(-10.1016115513385,13.0426913701659,
12.1734908238236));
#124100=CARTESIAN_POINT('Ctrl Pts',(-10.0600501209667,13.0455901138855,
12.1764638564938));
#124101=CARTESIAN_POINT('Ctrl Pts',(-10.0360210437332,13.0472840853127,
12.1774445089455));
#124102=CARTESIAN_POINT('Ctrl Pts',(-9.94017878671836,13.0541112457052,
12.1784194724864));
#124103=CARTESIAN_POINT('Ctrl Pts',(-9.86846703037902,13.0593894184681,
12.1725818323701));
#124104=CARTESIAN_POINT('Ctrl Pts',(-9.74362477992669,13.0686674466244,
12.1508190538728));
#124105=CARTESIAN_POINT('Ctrl Pts',(-9.69022725301103,13.0726615020068,
12.1376093253964));
#124106=CARTESIAN_POINT('Ctrl Pts',(-9.63072331134241,13.0770173006316,
12.1183860409223));
#124107=CARTESIAN_POINT('Ctrl Pts',(-9.62352716063983,13.0775423898841,
12.1159842373226));
#124108=CARTESIAN_POINT('Ctrl Pts',(-9.61247056675385,13.0783460466103,
12.1121748407477));
#124109=CARTESIAN_POINT('Ctrl Pts',(-9.60859359596864,13.0786272512412,
12.1108163512405));
#124110=CARTESIAN_POINT('Ctrl Pts',(-9.60154494387888,13.079137317803,12.1083050203729));
#124111=CARTESIAN_POINT('Ctrl Pts',(-9.59837109712932,13.0793665390039,
12.1071588298828));
#124112=CARTESIAN_POINT('Ctrl Pts',(-9.59516341493462,13.0795977803896,
12.1059848116457));
#124113=CARTESIAN_POINT('Ctrl Pts',(-9.59512471554921,13.0796005701611,
12.1059706452882));
#124114=CARTESIAN_POINT('Ctrl Pts',(-9.5950477604444,13.0796061175977,12.1059424704019));
#124115=CARTESIAN_POINT('Ctrl Pts',(-9.59500950473514,13.0796088752635,
12.1059284619291));
#124116=CARTESIAN_POINT('Ctrl Pts',(-9.59493342020972,13.079614359702,12.105900596826));
#124117=CARTESIAN_POINT('Ctrl Pts',(-9.59489559137832,13.0796170864772,
12.1058867402398));
#124118=CARTESIAN_POINT('Ctrl Pts',(-9.59482034430635,13.0796225103139,
12.1058591730867));
#124119=CARTESIAN_POINT('Ctrl Pts',(-9.59478292608478,13.0796252073753,
12.1058454625741));
#124120=CARTESIAN_POINT('Ctrl Pts',(-9.59470848485319,13.0796305728967,
12.1058181820737));
#124121=CARTESIAN_POINT('Ctrl Pts',(-9.59467146172201,13.0796332413666,
12.1058046120867));
#124122=CARTESIAN_POINT('Ctrl Pts',(-9.59459779528503,13.079638550818,12.1057776071324));
#124123=CARTESIAN_POINT('Ctrl Pts',(-9.59456115205745,13.0796411917948,
12.1057641722367));
#124124=CARTESIAN_POINT('Ctrl Pts',(-9.59448823099611,13.0796464473036,
12.1057374323014));
#124125=CARTESIAN_POINT('Ctrl Pts',(-9.59445195313516,13.0796490618386,
12.1057241272927));
#124126=CARTESIAN_POINT('Ctrl Pts',(-9.59437974878,13.0796542654778,12.1056976421087));
#124127=CARTESIAN_POINT('Ctrl Pts',(-9.59434382223773,13.0796568545867,
12.1056844619546));
#124128=CARTESIAN_POINT('Ctrl Pts',(-9.59427230686273,13.0796620083611,
12.1056582215851));
#124129=CARTESIAN_POINT('Ctrl Pts',(-9.59423671803249,13.0796645730275,
12.1056451614076));
#124130=CARTESIAN_POINT('Ctrl Pts',(-9.59416586484047,13.0796696788744,
12.1056191562425));
#124131=CARTESIAN_POINT('Ctrl Pts',(-9.59413060052028,13.0796722200528,
12.1056062113054));
#124132=CARTESIAN_POINT('Ctrl Pts',(-9.59406038375695,13.079677279834,12.1055804321038));
#124133=CARTESIAN_POINT('Ctrl Pts',(-9.59402543126224,13.0796797984413,
12.105567597854));
#124134=CARTESIAN_POINT('Ctrl Pts',(-9.59395582574197,13.0796848139772,
12.1055420355708));
#124135=CARTESIAN_POINT('Ctrl Pts',(-9.59392117272207,13.0796873109062,
12.1055293075715));
#124136=CARTESIAN_POINT('Ctrl Pts',(-9.59385215419259,13.0796922839496,
12.105503953492));
#124137=CARTESIAN_POINT('Ctrl Pts',(-9.59381778869325,13.0796947600642,
12.105491327446));
#124138=CARTESIAN_POINT('Ctrl Pts',(-9.59374933359598,13.0796996923178,
12.1054661730986));
#124139=CARTESIAN_POINT('Ctrl Pts',(-9.59371524400376,13.0797021484572,
12.1054536448283));
#124140=CARTESIAN_POINT('Ctrl Pts',(-9.5936473296044,13.0797070415638,12.105428682033));
#124141=CARTESIAN_POINT('Ctrl Pts',(-9.59361350472327,13.079709478537,12.1054162475083));
#124142=CARTESIAN_POINT('Ctrl Pts',(-9.59354610876972,13.0797143341044,
12.1053914682515));
#124143=CARTESIAN_POINT('Ctrl Pts',(-9.59351253768661,13.0797167527,12.1053791235415));
#124144=CARTESIAN_POINT('Ctrl Pts',(-9.59344563858582,13.0797215722883,
12.1053545200415));
#124145=CARTESIAN_POINT('Ctrl Pts',(-9.59341231062789,13.0797239732773,
12.1053422612983));
#124146=CARTESIAN_POINT('Ctrl Pts',(-9.58921791840261,13.0800261370001,
12.1037992578247));
#124147=CARTESIAN_POINT('Ctrl Pts',(-9.58506544934563,13.0803245754349,
12.1022450001442));
#124148=CARTESIAN_POINT('Ctrl Pts',(-9.57608135998949,13.080968935501,12.098824315061));
#124149=CARTESIAN_POINT('Ctrl Pts',(-9.57125305169878,13.0813143959228,
12.0969493813793));
#124150=CARTESIAN_POINT('Ctrl Pts',(-9.55813539709362,13.082251073329,12.0917556771422));
#124151=CARTESIAN_POINT('Ctrl Pts',(-9.54987100242236,13.0828391468118,
12.0883743297964));
#124152=CARTESIAN_POINT('Ctrl Pts',(-9.52344263340581,13.0847155577068,
12.0772087218396));
#124153=CARTESIAN_POINT('Ctrl Pts',(-9.5054350839105,13.0859877329996,12.0690608886513));
#124154=CARTESIAN_POINT('Ctrl Pts',(-9.43704259549868,13.090825989417,12.0360172524376));
#124155=CARTESIAN_POINT('Ctrl Pts',(-9.3882567168026,13.0942940031834,12.0079799832356));
#124156=CARTESIAN_POINT('Ctrl Pts',(-9.28734593884398,13.1018644397697,
11.9399518461945));
#124157=CARTESIAN_POINT('Ctrl Pts',(-9.23618980821173,13.1059669657346,
11.8988759157088));
#124158=CARTESIAN_POINT('Ctrl Pts',(-9.17721209272348,13.1112682655371,
11.8428326955974));
#124159=CARTESIAN_POINT('Ctrl Pts',(-9.1659309224605,13.1123109135151,11.8316703849429));
#124160=CARTESIAN_POINT('Ctrl Pts',(-9.14947191171068,13.113877940139,11.8147130211893));
#124161=CARTESIAN_POINT('Ctrl Pts',(-9.14412001994672,13.1143949943733,
11.809088864643));
#124162=CARTESIAN_POINT('Ctrl Pts',(-9.13462853193339,13.115325853258,11.7989149609325));
#124163=CARTESIAN_POINT('Ctrl Pts',(-9.13046820053756,13.1157387788329,
11.7943848814441));
#124164=CARTESIAN_POINT('Ctrl Pts',(-9.12168918886093,13.1166207972181,
11.7846740416978));
#124165=CARTESIAN_POINT('Ctrl Pts',(-9.11708045681241,13.1170902739214,
11.7794846434893));
#124166=CARTESIAN_POINT('Ctrl Pts',(-9.10473320934241,13.1183658661476,
11.765331732753));
#124167=CARTESIAN_POINT('Ctrl Pts',(-9.09708374848399,13.1191754995966,
11.7562919494934));
#124168=CARTESIAN_POINT('Ctrl Pts',(-9.05413802577621,13.1238352859139,
11.7039603190058));
#124169=CARTESIAN_POINT('Ctrl Pts',(-9.02182575853436,13.1277995076865,
11.6583224945081));
#124170=CARTESIAN_POINT('Ctrl Pts',(-8.94984959361929,13.1378578414956,
11.5395993327016));
#124171=CARTESIAN_POINT('Ctrl Pts',(-8.91445128966916,13.1440331934835,
11.4642915797605));
#124172=CARTESIAN_POINT('Ctrl Pts',(-8.88725970493321,13.1500000000001,
11.3858809379001));
#124173=CARTESIAN_POINT('',(-9.99063336962942,13.15,12.1777127530665));
#124174=CARTESIAN_POINT('Origin',(-10.,13.15,11.));
#124175=CARTESIAN_POINT('',(-11.1772954272628,13.0251562212751,10.9995934172276));
#124176=CARTESIAN_POINT('Ctrl Pts',(-11.1777499234177,13.0254177721281,
10.999575277046));
#124177=CARTESIAN_POINT('Ctrl Pts',(-11.1777577176107,13.0269365486979,
11.0211884488591));
#124178=CARTESIAN_POINT('Ctrl Pts',(-11.1771705716744,13.0284370553205,
11.0427989728332));
#124179=CARTESIAN_POINT('Ctrl Pts',(-11.1755995648328,13.0304066396755,
11.0714944569654));
#124180=CARTESIAN_POINT('Ctrl Pts',(-11.1751456864787,13.0308926866991,
11.0786028869611));
#124181=CARTESIAN_POINT('Ctrl Pts',(-11.174225909971,13.0317514363242,11.0912085761244));
#124182=CARTESIAN_POINT('Ctrl Pts',(-11.1737858258318,13.0321249660324,
11.0967074400733));
#124183=CARTESIAN_POINT('Ctrl Pts',(-11.1728329683863,13.0328659682834,
11.107646388824));
#124184=CARTESIAN_POINT('Ctrl Pts',(-11.1723209395147,13.0332334553756,
11.1130863977106));
#124185=CARTESIAN_POINT('Ctrl Pts',(-11.1711460135807,13.0340160535254,
11.1247022642352));
#124186=CARTESIAN_POINT('Ctrl Pts',(-11.1704720799956,13.034430794186,11.130876859675));
#124187=CARTESIAN_POINT('Ctrl Pts',(-11.1685775147471,13.0355138608371,
11.1470478341186));
#124188=CARTESIAN_POINT('Ctrl Pts',(-11.1672774464124,13.0361795957087,
11.1570345419591));
#124189=CARTESIAN_POINT('Ctrl Pts',(-11.1611175719878,13.0390342259051,
11.2000365202171));
#124190=CARTESIAN_POINT('Ctrl Pts',(-11.1549836689483,13.0411817482987,
11.2328554899879));
#124191=CARTESIAN_POINT('Ctrl Pts',(-11.1334691257893,13.0472321972448,
11.3258838813155));
#124192=CARTESIAN_POINT('Ctrl Pts',(-11.1147099243551,13.0510399841972,
11.3851946694449));
#124193=CARTESIAN_POINT('Ctrl Pts',(-11.0656545921376,13.0590870149611,
11.5061133897456));
#124194=CARTESIAN_POINT('Ctrl Pts',(-11.0344844859888,13.0633170379455,
11.5671061022227));
#124195=CARTESIAN_POINT('Ctrl Pts',(-10.9942855312569,13.0683399983489,
11.6313049735448));
#124196=CARTESIAN_POINT('Ctrl Pts',(-10.990304398483,13.0688335867455,11.637531864601));
#124197=CARTESIAN_POINT('Ctrl Pts',(-10.984152320596,13.06959123457,11.6469576602496));
#124198=CARTESIAN_POINT('Ctrl Pts',(-10.9820236867026,13.0698524824746,
11.6501841912838));
#124199=CARTESIAN_POINT('Ctrl Pts',(-10.9780246286169,13.0703417300501,
11.6561814254742));
#124200=CARTESIAN_POINT('Ctrl Pts',(-10.9761582423722,13.0705694354109,
11.6589547195682));
#124201=CARTESIAN_POINT('Ctrl Pts',(-10.9718988496437,13.0710876144093,
11.6652260151153));
#124202=CARTESIAN_POINT('Ctrl Pts',(-10.9694987328802,13.0713785587402,
11.6687190969701));
#124203=CARTESIAN_POINT('Ctrl Pts',(-10.9632425751771,13.0721341151097,
11.6777197105089));
#124204=CARTESIAN_POINT('Ctrl Pts',(-10.9593581969249,13.0726005079692,
11.6832072228588));
#124205=CARTESIAN_POINT('Ctrl Pts',(-10.9322789708401,13.0758318407849,
11.7207761103104));
#124206=CARTESIAN_POINT('Ctrl Pts',(-10.9075287698814,13.0786849341472,
11.7517001383513));
#124207=CARTESIAN_POINT('Ctrl Pts',(-10.8647875565658,13.0833933198988,
11.7999093719809));
#124208=CARTESIAN_POINT('Ctrl Pts',(-10.8477190946205,13.0852238242874,
11.8179760349368));
#124209=CARTESIAN_POINT('Ctrl Pts',(-10.7858840212843,13.0916585834664,
11.8794117228298));
#124210=CARTESIAN_POINT('Ctrl Pts',(-10.7382556912384,13.0962672086525,
11.9197599180347));
#124211=CARTESIAN_POINT('Ctrl Pts',(-10.6468884894268,13.104398508784,11.9854703978618));
#124212=CARTESIAN_POINT('Ctrl Pts',(-10.6042839821358,13.1079515380481,
12.0121554677843));
#124213=CARTESIAN_POINT('Ctrl Pts',(-10.5489750712035,13.1122853104622,
12.0420563217255));
#124214=CARTESIAN_POINT('Ctrl Pts',(-10.5377533754489,13.1131511732929,
12.0478913749513));
#124215=CARTESIAN_POINT('Ctrl Pts',(-10.5197333915153,13.1145211530228,
12.056895673695));
#124216=CARTESIAN_POINT('Ctrl Pts',(-10.5129953123566,13.1150289509163,
12.0601825677283));
#124217=CARTESIAN_POINT('Ctrl Pts',(-10.5007775373901,13.1159419089311,
12.0659987504876));
#124218=CARTESIAN_POINT('Ctrl Pts',(-10.4953089596567,13.1163477538018,
12.0685506607345));
#124219=CARTESIAN_POINT('Ctrl Pts',(-10.4823365812577,13.1173040935237,
12.0744832319354));
#124220=CARTESIAN_POINT('Ctrl Pts',(-10.4748164242994,13.1178534762734,
12.0778275194227));
#124221=CARTESIAN_POINT('Ctrl Pts',(-10.4523443503552,13.1194809504437,
12.0875402281599));
#124222=CARTESIAN_POINT('Ctrl Pts',(-10.4372946874503,13.1205523055852,
12.0936784496696));
#124223=CARTESIAN_POINT('Ctrl Pts',(-10.3584839054224,13.1260769780107,
12.1239355510394));
#124224=CARTESIAN_POINT('Ctrl Pts',(-10.292842380685,13.1303824394693,12.142797549714));
#124225=CARTESIAN_POINT('Ctrl Pts',(-10.1648024768581,13.1386305765498,
12.1678248973038));
#124226=CARTESIAN_POINT('Ctrl Pts',(-10.1028253210713,13.1425625675842,
12.1749044100269));
#124227=CARTESIAN_POINT('Ctrl Pts',(-10.0311209417352,13.1472915530833,
12.1773768473046));
#124228=CARTESIAN_POINT('Ctrl Pts',(-10.0216527151898,13.1479196453913,
12.1775890212404));
#124229=CARTESIAN_POINT('Ctrl Pts',(-10.0082480130816,13.1488151762712,
12.1777276936811));
#124230=CARTESIAN_POINT('Ctrl Pts',(-10.0043126586523,13.1490788555009,
12.1777486787568));
#124231=CARTESIAN_POINT('Ctrl Pts',(-9.9971259392377,13.1495618946493,12.1777509812338));
#124232=CARTESIAN_POINT('Ctrl Pts',(-9.99388457723913,13.1497803175007,
12.1777386106959));
#124233=CARTESIAN_POINT('Ctrl Pts',(-9.99063336962942,13.15,12.1777127530665));
#124234=CARTESIAN_POINT('Ctrl Pts',(-9.81116440461326,12.8870115174245,
9.83777311283111));
#124235=CARTESIAN_POINT('Ctrl Pts',(-9.85764179083828,12.8900321853929,
9.83013029488514));
#124236=CARTESIAN_POINT('Ctrl Pts',(-9.90455116173817,12.8930103398809,
9.82526020590206));
#124237=CARTESIAN_POINT('Ctrl Pts',(-9.9515353357889,12.8959892278449,9.82321108761683));
#124238=CARTESIAN_POINT('Ctrl Pts',(-9.99860896525469,12.8989737874562,
9.82115806791735));
#124239=CARTESIAN_POINT('Ctrl Pts',(-10.045757547291,12.9019596135139,9.82193735631773));
#124240=CARTESIAN_POINT('Ctrl Pts',(-10.092609471857,12.9050053361438,9.8255527815257));
#124241=CARTESIAN_POINT('Ctrl Pts',(-10.1291483434982,12.9073806338346,
9.82837237877439));
#124242=CARTESIAN_POINT('Ctrl Pts',(-10.1655064318549,12.9097928264916,
9.83291619779872));
#124243=CARTESIAN_POINT('Ctrl Pts',(-10.2015038000959,12.912272145452,9.83916325637052));
#124244=CARTESIAN_POINT('Ctrl Pts',(-10.2015210427633,12.9122733330409,
9.83916624869909));
#124245=CARTESIAN_POINT('Ctrl Pts',(-10.2015382853485,12.9122745206451,
9.83916924141816));
#124246=CARTESIAN_POINT('Ctrl Pts',(-10.2015555278514,12.9122757082647,
9.83917223452772));
#124247=CARTESIAN_POINT('Ctrl Pts',(-10.2442282194276,12.9152148944474,
9.84657974618454));
#124248=CARTESIAN_POINT('Ctrl Pts',(-10.2865568592501,12.9182562844301,
9.85641454158234));
#124249=CARTESIAN_POINT('Ctrl Pts',(-10.3282607259639,12.9213410703907,
9.86859966612906));
#124250=CARTESIAN_POINT('Ctrl Pts',(-10.3332038360598,12.9217067064295,
9.87004395455871));
#124251=CARTESIAN_POINT('Ctrl Pts',(-10.3381381277854,12.9220729521418,
9.87152121879118));
#124252=CARTESIAN_POINT('Ctrl Pts',(-10.3430631019052,12.9224397095998,
9.87303129417658));
#124253=CARTESIAN_POINT('Ctrl Pts',(-10.3879237399555,12.925780432449,9.88678627920702));
#124254=CARTESIAN_POINT('Ctrl Pts',(-10.4320158733059,12.9291630655903,
9.90326743373218));
#124255=CARTESIAN_POINT('Ctrl Pts',(-10.4750087718731,12.9325288967133,
9.92233712650969));
#124256=CARTESIAN_POINT('Ctrl Pts',(-10.5179599024573,12.9358914579015,
9.9413882929112));
#124257=CARTESIAN_POINT('Ctrl Pts',(-10.5598141289736,12.9392369577166,
9.96302272516638));
#124258=CARTESIAN_POINT('Ctrl Pts',(-10.6002628671917,12.9425285565809,
9.98707213673965));
#124259=CARTESIAN_POINT('Ctrl Pts',(-10.6406899655252,12.9458183944553,
10.011108681991));
#124260=CARTESIAN_POINT('Ctrl Pts',(-10.6797131310047,12.9490542995934,
10.0375575726317));
#124261=CARTESIAN_POINT('Ctrl Pts',(-10.7170435689573,12.9522239589476,
10.0662218540858));
#124262=CARTESIAN_POINT('Ctrl Pts',(-10.7543703291871,12.955393306033,10.09488331159));
#124263=CARTESIAN_POINT('Ctrl Pts',(-10.7900046053942,12.9584964779604,
10.1257597863454));
#124264=CARTESIAN_POINT('Ctrl Pts',(-10.8236772833654,12.9615458522909,
10.1586253022285));
#124265=CARTESIAN_POINT('Ctrl Pts',(-10.8573843173583,12.9645983378788,
10.1915243505907));
#124266=CARTESIAN_POINT('Ctrl Pts',(-10.8891255088694,12.967597123764,10.2264166559677));
#124267=CARTESIAN_POINT('Ctrl Pts',(-10.9186530064052,12.970577413428,10.2630447536762));
#124268=CARTESIAN_POINT('Ctrl Pts',(-10.9481986928991,12.9735595389524,
10.2996954143172));
#124269=CARTESIAN_POINT('Ctrl Pts',(-10.9755275164772,12.9765235663849,
10.3380842168579));
#124270=CARTESIAN_POINT('Ctrl Pts',(-11.0004182904618,12.9795229212538,
10.3779196065224));
#124271=CARTESIAN_POINT('Ctrl Pts',(-11.0233446274457,12.9822855601536,
10.4146110958227));
#124272=CARTESIAN_POINT('Ctrl Pts',(-11.0442026173884,12.9850787708026,
10.4525303703702));
#124273=CARTESIAN_POINT('Ctrl Pts',(-11.0628454756567,12.987951913143,10.4914199788974));
#124274=CARTESIAN_POINT('Ctrl Pts',(-11.0644790954582,12.9882036783043,
10.4948277629212));
#124275=CARTESIAN_POINT('Ctrl Pts',(-11.0660957352143,12.988456057222,10.498243013967));
#124276=CARTESIAN_POINT('Ctrl Pts',(-11.067695312561,12.9887090831076,10.5016655686762));
#124277=CARTESIAN_POINT('Ctrl Pts',(-11.0727371756071,12.9895066199477,
10.5124534509552));
#124278=CARTESIAN_POINT('Ctrl Pts',(-11.0776094005779,12.9903106007719,
10.5233135115653));
#124279=CARTESIAN_POINT('Ctrl Pts',(-11.0823094096359,12.9911220678411,
10.5342399661854));
#124280=CARTESIAN_POINT('Ctrl Pts',(-11.0823175711111,12.991123476938,10.5342589397633));
#124281=CARTESIAN_POINT('Ctrl Pts',(-11.082325732067,12.9911248860575,10.5342779135414));
#124282=CARTESIAN_POINT('Ctrl Pts',(-11.0823338925038,12.9911262951996,
10.5342968875198));
#124283=CARTESIAN_POINT('Ctrl Pts',(-11.0999253299888,12.9941639800148,
10.5751990553205));
#124284=CARTESIAN_POINT('Ctrl Pts',(-11.1151555993952,12.9973132986395,
10.6171683939075));
#124285=CARTESIAN_POINT('Ctrl Pts',(-11.1279453099112,13.0005094500513,
10.6599293048586));
#124286=CARTESIAN_POINT('Ctrl Pts',(-11.1298768953495,13.0009921536683,
10.666387336322));
#124287=CARTESIAN_POINT('Ctrl Pts',(-11.1317528145371,13.0014759254947,
10.6728633258445));
#124288=CARTESIAN_POINT('Ctrl Pts',(-11.1335727985327,13.0019605423062,
10.6793562208813));
#124289=CARTESIAN_POINT('Ctrl Pts',(-11.1465529134116,13.0054168264831,
10.7256635091205));
#124290=CARTESIAN_POINT('Ctrl Pts',(-11.1566880602086,13.008915125034,10.7728364981445));
#124291=CARTESIAN_POINT('Ctrl Pts',(-11.1639147879019,13.0123938753952,
10.8205348651852));
#124292=CARTESIAN_POINT('Ctrl Pts',(-11.1647785754975,13.0128096792746,
10.8262360980981));
#124293=CARTESIAN_POINT('Ctrl Pts',(-11.1656007929283,13.0132252038757,
10.8319447785655));
#124294=CARTESIAN_POINT('Ctrl Pts',(-11.1663813188882,13.0136403440721,
10.837660277284));
#124295=CARTESIAN_POINT('Ctrl Pts',(-11.1732971651245,13.0173186916377,
10.8883024241616));
#124296=CARTESIAN_POINT('Ctrl Pts',(-11.1769423028602,13.020966755683,10.9394862387593));
#124297=CARTESIAN_POINT('Ctrl Pts',(-11.1772703118677,13.0245435525335,
10.9908036332495));
#124298=CARTESIAN_POINT('Ctrl Pts',(-11.1772890367999,13.0247477398476,
10.9937331708732));
#124299=CARTESIAN_POINT('Ctrl Pts',(-11.1772969587745,13.024951704152,10.9966631424074));
#124300=CARTESIAN_POINT('Ctrl Pts',(-11.1772940717528,13.0251554412139,
10.9995934713297));
#124301=CARTESIAN_POINT('Origin',(-10.,3.5,11.));
#124302=CARTESIAN_POINT('',(-11.288874705773,13.1492342550778,10.3059746432093));
#124303=CARTESIAN_POINT('Ctrl Pts',(-11.463991763927,12.6884918210949,10.9993887619195));
#124304=CARTESIAN_POINT('Ctrl Pts',(-11.4639306072661,12.6916694228865,
11.0548606201258));
#124305=CARTESIAN_POINT('Ctrl Pts',(-11.4606650012394,12.6949287056907,
11.1104413929884));
#124306=CARTESIAN_POINT('Ctrl Pts',(-11.4542247554779,12.6981982648876,
11.1657358244845));
#124307=CARTESIAN_POINT('Ctrl Pts',(-11.4479113119717,12.7014034496033,
11.2199415617167));
#124308=CARTESIAN_POINT('Ctrl Pts',(-11.4385475454018,12.70461814771,11.273872221106));
#124309=CARTESIAN_POINT('Ctrl Pts',(-11.4262011123443,12.7077927824406,
11.3271678981243));
#124310=CARTESIAN_POINT('Ctrl Pts',(-11.4138654318444,12.7109646523692,
11.3804171597257));
#124311=CARTESIAN_POINT('Ctrl Pts',(-11.3985524523269,12.7140963374362,
11.4330325782745));
#124312=CARTESIAN_POINT('Ctrl Pts',(-11.3803645690148,12.7171603245914,
11.4846667322799));
#124313=CARTESIAN_POINT('Ctrl Pts',(-11.3621849539508,12.720222918852,11.536277413296));
#124314=CARTESIAN_POINT('Ctrl Pts',(-11.3411330761592,12.7232178336545,
11.5869076790711));
#124315=CARTESIAN_POINT('Ctrl Pts',(-11.3173446373055,12.7261412311667,
11.6362221723392));
#124316=CARTESIAN_POINT('Ctrl Pts',(-11.2926743352398,12.7291730021933,
11.6873648073233));
#124317=CARTESIAN_POINT('Ctrl Pts',(-11.2650604962163,12.7321277902365,
11.7370920766566));
#124318=CARTESIAN_POINT('Ctrl Pts',(-11.2346929672173,12.7350278368395,
11.7850445538785));
#124319=CARTESIAN_POINT('Ctrl Pts',(-11.2053818388839,12.7378269990023,
11.8313288996941));
#124320=CARTESIAN_POINT('Ctrl Pts',(-11.1735053054335,12.7405755318138,
11.8759596398189));
#124321=CARTESIAN_POINT('Ctrl Pts',(-11.1392707220035,12.7433149314186,
11.9186294430486));
#124322=CARTESIAN_POINT('Ctrl Pts',(-11.1050138117042,12.7460561175857,
11.9613270743697));
#124323=CARTESIAN_POINT('Ctrl Pts',(-11.0683955094785,12.7487885838883,
12.002060812035));
#124324=CARTESIAN_POINT('Ctrl Pts',(-11.0296630300884,12.7515701670991,
12.0405429981061));
#124325=CARTESIAN_POINT('Ctrl Pts',(-10.994277032835,12.7541114218137,12.0757003273569));
#124326=CARTESIAN_POINT('Ctrl Pts',(-10.9571259891997,12.7566942402975,
12.1089786558575));
#124327=CARTESIAN_POINT('Ctrl Pts',(-10.9184321226944,12.7593688259845,
12.1401776686378));
#124328=CARTESIAN_POINT('Ctrl Pts',(-10.9147017991821,12.7596266722732,
12.1431854427748));
#124329=CARTESIAN_POINT('Ctrl Pts',(-10.9109571274964,12.7598853714582,
12.1461739305206));
#124330=CARTESIAN_POINT('Ctrl Pts',(-10.9071983003763,12.7601449685223,
12.1491429772846));
#124331=CARTESIAN_POINT('Ctrl Pts',(-10.9027286881088,12.7604536547654,
12.1526734636345));
#124332=CARTESIAN_POINT('Ctrl Pts',(-10.8982391177638,12.7607636118325,
12.1561764266014));
#124333=CARTESIAN_POINT('Ctrl Pts',(-10.8937299523839,12.7610749150924,
12.1596515912169));
#124334=CARTESIAN_POINT('Ctrl Pts',(-10.8937152925033,12.7610759271796,
12.1596628894271));
#124335=CARTESIAN_POINT('Ctrl Pts',(-10.8937006324156,12.7610769392811,
12.1596741873435));
#124336=CARTESIAN_POINT('Ctrl Pts',(-10.8936859721208,12.7610779513968,
12.1596854849661));
#124337=CARTESIAN_POINT('Ctrl Pts',(-10.8537499481008,12.763835049828,12.1904612730685));
#124338=CARTESIAN_POINT('Ctrl Pts',(-10.8121129634155,12.7667055672991,
12.219173400463));
#124339=CARTESIAN_POINT('Ctrl Pts',(-10.7690278434298,12.7696293657161,
12.2456599611385));
#124340=CARTESIAN_POINT('Ctrl Pts',(-10.7650618919684,12.7698984990644,
12.2480980282497));
#124341=CARTESIAN_POINT('Ctrl Pts',(-10.761083706844,12.7701680838652,12.2505172388233));
#124342=CARTESIAN_POINT('Ctrl Pts',(-10.7570935073437,12.7704380732146,
12.2529174676517));
#124343=CARTESIAN_POINT('Ctrl Pts',(-10.7098389494908,12.7736354640544,
12.2813425506649));
#124344=CARTESIAN_POINT('Ctrl Pts',(-10.6608936219115,12.7768889670954,
12.3071058356523));
#124345=CARTESIAN_POINT('Ctrl Pts',(-10.6105997122338,12.7801339179107,
12.3300427880688));
#124346=CARTESIAN_POINT('Ctrl Pts',(-10.5603556027551,12.7833756556294,
12.3529570286937));
#124347=CARTESIAN_POINT('Ctrl Pts',(-10.5087656730358,12.7866085236495,
12.3730508776882));
#124348=CARTESIAN_POINT('Ctrl Pts',(-10.4561797286586,12.7897883683785,
12.3901984627458));
#124349=CARTESIAN_POINT('Ctrl Pts',(-10.4036251100483,12.7929663188546,
12.4073358328828));
#124350=CARTESIAN_POINT('Ctrl Pts',(-10.3500756848916,12.7960911734393,
12.4215305799771));
#124351=CARTESIAN_POINT('Ctrl Pts',(-10.2958885096565,12.7991426090625,
12.4326916658829));
#124352=CARTESIAN_POINT('Ctrl Pts',(-10.2417122397385,12.802193430576,12.4438505055896));
#124353=CARTESIAN_POINT('Ctrl Pts',(-10.1868984941038,12.8051708661675,
12.4519768687009));
#124354=CARTESIAN_POINT('Ctrl Pts',(-10.1318117243294,12.8080793134399,
12.4570137059567));
#124355=CARTESIAN_POINT('Ctrl Pts',(-10.0766746164422,12.8109904184421,
12.4620551458582));
#124356=CARTESIAN_POINT('Ctrl Pts',(-10.0212640174713,12.8138325374196,
12.4640012238705));
#124357=CARTESIAN_POINT('Ctrl Pts',(-9.96595264511685,12.8166338655913,
12.462830420146));
#124358=CARTESIAN_POINT('Ctrl Pts',(-9.91061622684647,12.8194364622514,
12.461659086262));
#124359=CARTESIAN_POINT('Ctrl Pts',(-9.85537920337594,12.8221985245844,
12.4573677032184));
#124360=CARTESIAN_POINT('Ctrl Pts',(-9.80062128797522,12.8249689650342,
12.4499743785991));
#124361=CARTESIAN_POINT('Ctrl Pts',(-9.74576049243588,12.8277446106364,
12.4425671632709));
#124362=CARTESIAN_POINT('Ctrl Pts',(-9.69138082321311,12.8305291858514,
12.4320458028768));
#124363=CARTESIAN_POINT('Ctrl Pts',(-9.63786857487717,12.8333866006413,
12.4184749302969));
#124364=CARTESIAN_POINT('Ctrl Pts',(-9.59715191586502,12.8355607642632,
12.4081490589587));
#124365=CARTESIAN_POINT('Ctrl Pts',(-9.55693763547138,12.8377775238315,
12.3960585411452));
#124366=CARTESIAN_POINT('Ctrl Pts',(-9.5173957676152,12.8400672357347,12.3822530440279));
#124367=CARTESIAN_POINT('Ctrl Pts',(-9.51737844909782,12.840068238581,12.3822469975067));
#124368=CARTESIAN_POINT('Ctrl Pts',(-9.51736113070901,12.8400692414413,
12.3822409506567));
#124369=CARTESIAN_POINT('Ctrl Pts',(-9.51734381244877,12.8400702443156,
12.3822349034779));
#124370=CARTESIAN_POINT('Ctrl Pts',(-9.46970834541888,12.8428287422249,
12.3656015821447));
#124371=CARTESIAN_POINT('Ctrl Pts',(-9.42287266454677,12.8457003959102,
12.3464124368936));
#124372=CARTESIAN_POINT('Ctrl Pts',(-9.37711103475015,12.8486249916029,
12.3247909965804));
#124373=CARTESIAN_POINT('Ctrl Pts',(-9.3729300008179,12.8488921987343,12.322815542996));
#124374=CARTESIAN_POINT('Ctrl Pts',(-9.36875795172639,12.8491598478073,
12.3208198159464));
#124375=CARTESIAN_POINT('Ctrl Pts',(-9.36459510762443,12.8494278928976,
12.3188039282783));
#124376=CARTESIAN_POINT('Ctrl Pts',(-9.31495778950907,12.852624034547,12.2947666943536));
#124377=CARTESIAN_POINT('Ctrl Pts',(-9.26662576689027,12.8558758586289,
12.2678584206617));
#124378=CARTESIAN_POINT('Ctrl Pts',(-9.21992386854803,12.8591188273359,
12.2382757540587));
#124379=CARTESIAN_POINT('Ctrl Pts',(-9.17326800766399,12.8623585992128,
12.2087222492419));
#124380=CARTESIAN_POINT('Ctrl Pts',(-9.12823881971626,12.8655892004004,
12.1764998869579));
#124381=CARTESIAN_POINT('Ctrl Pts',(-9.08513296385328,12.8687666544394,
12.1418328127599));
#124382=CARTESIAN_POINT('Ctrl Pts',(-9.04205260528417,12.8719422290011,
12.1071862442812));
#124383=CARTESIAN_POINT('Ctrl Pts',(-9.00089320646608,12.8750645846866,
12.0700979443509));
#124384=CARTESIAN_POINT('Ctrl Pts',(-8.96192625110391,12.8781136056907,
12.0308171767114));
#124385=CARTESIAN_POINT('Ctrl Pts',(-8.92296698235448,12.8811620252457,
11.9915441575871));
#124386=CARTESIAN_POINT('Ctrl Pts',(-8.88619933293799,12.8841371435309,
11.9500795295694));
#124387=CARTESIAN_POINT('Ctrl Pts',(-8.85187038717562,12.8870435803164,
11.9066973488058));
#124388=CARTESIAN_POINT('Ctrl Pts',(-8.81750988950394,12.8899526884228,
11.8632752952583));
#124389=CARTESIAN_POINT('Ctrl Pts',(-8.78559275552825,12.8927931183539,
11.8179320859967));
#124390=CARTESIAN_POINT('Ctrl Pts',(-8.75634084620763,12.8955932876637,
11.7709681597297));
#124391=CARTESIAN_POINT('Ctrl Pts',(-8.72707560095911,12.8983947335689,
11.7239828226369));
#124392=CARTESIAN_POINT('Ctrl Pts',(-8.70047834350937,12.9011561774023,
11.6753751666226));
#124393=CARTESIAN_POINT('Ctrl Pts',(-8.67674156563753,12.9039267316423,
11.6254732072825));
#124394=CARTESIAN_POINT('Ctrl Pts',(-8.65296010294484,12.9067025014898,
11.5754773067965));
#124395=CARTESIAN_POINT('Ctrl Pts',(-8.63205046998966,12.9094879388544,
11.524182112466));
#124396=CARTESIAN_POINT('Ctrl Pts',(-8.61416975518133,12.9123470979137,
11.4719466581655));
#124397=CARTESIAN_POINT('Ctrl Pts',(-8.6005777153295,12.9145204899896,11.4322398352481));
#124398=CARTESIAN_POINT('Ctrl Pts',(-8.5887352577041,12.9167369048377,11.3919903307576));
#124399=CARTESIAN_POINT('Ctrl Pts',(-8.57869358592355,12.9190266353551,
11.3513673085708));
#124400=CARTESIAN_POINT('Ctrl Pts',(-8.57868907329069,12.9190276643385,
11.3513490529667));
#124401=CARTESIAN_POINT('Ctrl Pts',(-8.57868456102113,12.9190286933367,
11.3513307972868));
#124402=CARTESIAN_POINT('Ctrl Pts',(-8.57868004911485,12.9190297223496,
11.3513125415313));
#124403=CARTESIAN_POINT('Ctrl Pts',(-8.56660070253902,12.9217846121045,
11.3024379451385));
#124404=CARTESIAN_POINT('Ctrl Pts',(-8.55708741400778,12.924652975869,11.2528372813682));
#124405=CARTESIAN_POINT('Ctrl Pts',(-8.55018686238138,12.9275746380525,
11.2028063462097));
#124406=CARTESIAN_POINT('Ctrl Pts',(-8.54955230728425,12.9278433057955,
11.1982056437386));
#124407=CARTESIAN_POINT('Ctrl Pts',(-8.54893983039631,12.9281124242362,
11.193601335831));
#124408=CARTESIAN_POINT('Ctrl Pts',(-8.54834945817009,12.9283819465821,
11.1889936722351));
#124409=CARTESIAN_POINT('Ctrl Pts',(-8.54135148776675,12.9315767266135,
11.1343767847181));
#124410=CARTESIAN_POINT('Ctrl Pts',(-8.53746133071862,12.9348276337055,
11.0792829802226));
#124411=CARTESIAN_POINT('Ctrl Pts',(-8.53669217238271,12.9380699468489,
11.0240906774086));
#124412=CARTESIAN_POINT('Ctrl Pts',(-8.53592377559064,12.9413090497774,
10.9689530205062));
#124413=CARTESIAN_POINT('Ctrl Pts',(-8.53826984716269,12.944539241719,10.9137170085431));
#124414=CARTESIAN_POINT('Ctrl Pts',(-8.54370509600633,12.9477162716722,
10.8587525388433));
#124415=CARTESIAN_POINT('Ctrl Pts',(-8.54913712565265,12.9508914199293,
10.8038206235819));
#124416=CARTESIAN_POINT('Ctrl Pts',(-8.55765454448063,12.9540133329836,
10.7491598992555));
#124417=CARTESIAN_POINT('Ctrl Pts',(-8.5691972312881,12.9570615499469,10.6951329001681));
#124418=CARTESIAN_POINT('Ctrl Pts',(-8.5807376732402,12.9601091740841,10.641116408409));
#124419=CARTESIAN_POINT('Ctrl Pts',(-8.5953022305721,12.963083133139,10.5877334291422));
#124420=CARTESIAN_POINT('Ctrl Pts',(-8.61279668643374,12.9659876583311,
10.5353395611747));
#124421=CARTESIAN_POINT('Ctrl Pts',(-8.63030756142934,12.9688949095176,
10.4828965198037));
#124422=CARTESIAN_POINT('Ctrl Pts',(-8.65075399173112,12.9717327226785,
10.4314445539024));
#124423=CARTESIAN_POINT('Ctrl Pts',(-8.67400594107476,12.9745291241955,
10.3813324828995));
#124424=CARTESIAN_POINT('Ctrl Pts',(-8.69726867948781,12.9773268232626,
10.3311971595401));
#124425=CARTESIAN_POINT('Ctrl Pts',(-8.72333981954434,12.9800833620599,
10.2824031845639));
#124426=CARTESIAN_POINT('Ctrl Pts',(-8.7520503332962,12.9828475259031,10.235289759722));
#124427=CARTESIAN_POINT('Ctrl Pts',(-8.78081591254253,12.9856169912902,
10.1880859734167));
#124428=CARTESIAN_POINT('Ctrl Pts',(-8.81223139921618,12.9883946255454,
10.1425695998377));
#124429=CARTESIAN_POINT('Ctrl Pts',(-8.84608268313027,12.99124432723,10.0990671209387));
#124430=CARTESIAN_POINT('Ctrl Pts',(-8.87230015811641,12.9934513921916,
10.0653748936287));
#124431=CARTESIAN_POINT('Ctrl Pts',(-8.89997787675521,12.9957021291343,
10.0328905194451));
#124432=CARTESIAN_POINT('Ctrl Pts',(-8.92899589006904,12.9980286231998,
10.0017564676114));
#124433=CARTESIAN_POINT('Ctrl Pts',(-8.9290084654359,12.9980296314189,10.0017429752293));
#124434=CARTESIAN_POINT('Ctrl Pts',(-8.92902104105451,12.9980306396523,
10.0017294831003));
#124435=CARTESIAN_POINT('Ctrl Pts',(-8.92903361692483,12.9980316478999,
10.0017159912244));
#124436=CARTESIAN_POINT('Ctrl Pts',(-8.96342523601557,13.0007889335873,
9.96481934371385));
#124437=CARTESIAN_POINT('Ctrl Pts',(-8.99983258448837,13.0036599961189,
9.92968370963538));
#124438=CARTESIAN_POINT('Ctrl Pts',(-9.03803252860992,13.0065848607624,
9.89650983373753));
#124439=CARTESIAN_POINT('Ctrl Pts',(-9.04159484639477,13.0068576176362,
9.89341621957601));
#124440=CARTESIAN_POINT('Ctrl Pts',(-9.04517271624349,13.0071308423951,
9.89033967081621));
#124441=CARTESIAN_POINT('Ctrl Pts',(-9.04876593431357,13.0074044864008,
9.88728035283533));
#124442=CARTESIAN_POINT('Ctrl Pts',(-9.09081513479617,13.0106067723269,
9.85147905366303));
#124443=CARTESIAN_POINT('Ctrl Pts',(-9.13497186781783,13.0138658422133,
9.81803614812968));
#124444=CARTESIAN_POINT('Ctrl Pts',(-9.18092427701071,13.0171168896996,
9.78717016845008));
#124445=CARTESIAN_POINT('Ctrl Pts',(-9.22683084803429,13.0203646942206,
9.75633497801586));
#124446=CARTESIAN_POINT('Ctrl Pts',(-9.27452936708117,13.0236041548999,
9.72807124327942));
#124447=CARTESIAN_POINT('Ctrl Pts',(-9.3236942342042,13.0267909395546,9.70256050116778));
#124448=CARTESIAN_POINT('Ctrl Pts',(-9.37282928121454,13.0299757913194,
9.67706523216223));
#124449=CARTESIAN_POINT('Ctrl Pts',(-9.42342885733123,13.033107893756,9.65431948756656));
#124450=CARTESIAN_POINT('Ctrl Pts',(-9.47515458758201,13.0361667410128,
9.63447158781853));
#124451=CARTESIAN_POINT('Ctrl Pts',(-9.52686916668666,13.0392249288365,
9.61462796692417));
#124452=CARTESIAN_POINT('Ctrl Pts',(-9.5797094058222,13.0422098962276,9.59768097893714));
#124453=CARTESIAN_POINT('Ctrl Pts',(-9.63332411368873,13.0451258651884,
9.58374662065141));
#124454=CARTESIAN_POINT('Ctrl Pts',(-9.68698584714255,13.0480443917525,
9.56980004050702));
#124455=CARTESIAN_POINT('Ctrl Pts',(-9.74142340983765,13.0508939277508,
9.55887156717953));
#124456=CARTESIAN_POINT('Ctrl Pts',(-9.79627166289408,13.0537024946183,
9.55104350129771));
#124457=CARTESIAN_POINT('Ctrl Pts',(-9.85114376646174,13.0565122827782,
9.54321203141736));
#124458=CARTESIAN_POINT('Ctrl Pts',(-9.90642689820126,13.0592813606473,
9.5384840198725));
#124459=CARTESIAN_POINT('Ctrl Pts',(-9.96174250575976,13.062058455779,9.53690381441628));
#124460=CARTESIAN_POINT('Ctrl Pts',(-10.0171592713773,13.0648406295054,
9.53532071916956));
#124461=CARTESIAN_POINT('Ctrl Pts',(-10.0726085057825,13.0676313713475,
9.53689752043782));
#124462=CARTESIAN_POINT('Ctrl Pts',(-10.1276975482097,13.0704943671667,
9.54163371294026));
#124463=CARTESIAN_POINT('Ctrl Pts',(-10.1688531780977,13.0726332389116,
9.54517200253689));
#124464=CARTESIAN_POINT('Ctrl Pts',(-10.209807456237,13.0748128461259,9.55047277122835));
#124465=CARTESIAN_POINT('Ctrl Pts',(-10.2503935023658,13.0770618128499,
9.55751614721885));
#124466=CARTESIAN_POINT('Ctrl Pts',(-10.2504107598799,13.0770627691287,
9.55751914211912));
#124467=CARTESIAN_POINT('Ctrl Pts',(-10.2504280173278,13.07706372542,9.55752213733427));
#124468=CARTESIAN_POINT('Ctrl Pts',(-10.2504452747094,13.0770646817239,
9.55752513286428));
#124469=CARTESIAN_POINT('Ctrl Pts',(-10.2999283478705,13.0798067462746,
9.5661143866647));
#124470=CARTESIAN_POINT('Ctrl Pts',(-10.3490540963103,13.0826594087948,
9.57733250151461));
#124471=CARTESIAN_POINT('Ctrl Pts',(-10.3975314251549,13.0855635331345,
9.59110550936363));
#124472=CARTESIAN_POINT('Ctrl Pts',(-10.4020023090948,13.0858313697331,
9.59237574270909));
#124473=CARTESIAN_POINT('Ctrl Pts',(-10.4064676540746,13.0860996440499,
9.5936676792684));
#124474=CARTESIAN_POINT('Ctrl Pts',(-10.4109272177777,13.0863683096957,
9.59498124369684));
#124475=CARTESIAN_POINT('Ctrl Pts',(-10.4632663881832,13.0895214739851,
9.61039774563183));
#124476=CARTESIAN_POINT('Ctrl Pts',(-10.5148132490296,13.0927279572486,
9.62879731176444));
#124477=CARTESIAN_POINT('Ctrl Pts',(-10.5652209584256,13.0959256301729,
9.65004411605881));
#124478=CARTESIAN_POINT('Ctrl Pts',(-10.6155809302256,13.099120274806,9.67127079899927));
#124479=CARTESIAN_POINT('Ctrl Pts',(-10.6648040502312,13.1023058064021,
9.69533903076452));
#124480=CARTESIAN_POINT('Ctrl Pts',(-10.7125662975263,13.105439842644,9.72208043911381));
#124481=CARTESIAN_POINT('Ctrl Pts',(-10.7603032011951,13.108572215902,9.74880765792428));
#124482=CARTESIAN_POINT('Ctrl Pts',(-10.8065808261548,13.1116530190775,
9.77820509768527));
#124483=CARTESIAN_POINT('Ctrl Pts',(-10.8510960532976,13.114662790778,9.81007477960554));
#124484=CARTESIAN_POINT('Ctrl Pts',(-10.8964121546961,13.1177267113356,
9.84251782954903));
#124485=CARTESIAN_POINT('Ctrl Pts',(-10.9399017374015,13.120716954681,9.87752295521772));
#124486=CARTESIAN_POINT('Ctrl Pts',(-10.9812669267779,13.1236382711485,
9.91485049741996));
#124487=CARTESIAN_POINT('Ctrl Pts',(-11.0219325646473,13.1265101834826,
9.95154677118628));
#124488=CARTESIAN_POINT('Ctrl Pts',(-11.0605449414042,13.1293156851876,
9.99048755399651));
#124489=CARTESIAN_POINT('Ctrl Pts',(-11.0968436896816,13.1320822444629,
10.031415469163));
#124490=CARTESIAN_POINT('Ctrl Pts',(-11.1340790829517,13.134920191431,10.0733994793363));
#124491=CARTESIAN_POINT('Ctrl Pts',(-11.1688794471558,13.1377173925956,
10.1174747759693));
#124492=CARTESIAN_POINT('Ctrl Pts',(-11.2009922628842,13.1405248625602,
10.1633297738821));
#124493=CARTESIAN_POINT('Ctrl Pts',(-11.2313042754948,13.1431748969169,
10.2066133428706));
#124494=CARTESIAN_POINT('Ctrl Pts',(-11.2592216391798,13.1458345968796,
10.2514830235118));
#124495=CARTESIAN_POINT('Ctrl Pts',(-11.2845607691875,13.148559395597,10.2976452467453));
#124496=CARTESIAN_POINT('Ctrl Pts',(-11.2860661388544,13.1487212728728,
10.3003876933326));
#124497=CARTESIAN_POINT('Ctrl Pts',(-11.2875624218902,13.1488833799093,
10.3031347098596));
#124498=CARTESIAN_POINT('Ctrl Pts',(-11.2890495846627,13.1490457283295,
10.3058862379435));
#124499=CARTESIAN_POINT('',(-10.2623899083091,13.15,9.56021397908664));
#124500=CARTESIAN_POINT('Origin',(-10.,13.15,11.));
#124501=CARTESIAN_POINT('Ctrl Pts',(-10.2623899083091,13.15,9.56021397908663));
#124502=CARTESIAN_POINT('Ctrl Pts',(-10.2066727834959,13.1469204952333,
9.55005996240732));
#124503=CARTESIAN_POINT('Ctrl Pts',(-10.1503209963368,13.1438409904666,
9.54313634185553));
#124504=CARTESIAN_POINT('Ctrl Pts',(-10.093728771318,13.1407614856999,9.53950447880618));
#124505=CARTESIAN_POINT('Ctrl Pts',(-10.0371641637688,13.1376834837567,
9.53587438813576));
#124506=CARTESIAN_POINT('Ctrl Pts',(-9.98035984204682,13.1346054818135,
9.53553290138471));
#124507=CARTESIAN_POINT('Ctrl Pts',(-9.92371509738344,13.1315274798704,
9.53848952667701));
#124508=CARTESIAN_POINT('Ctrl Pts',(-9.8670840125995,13.1284502201874,9.54144543897916));
#124509=CARTESIAN_POINT('Ctrl Pts',(-9.8106129204972,13.1253729605043,9.54769785837776));
#124510=CARTESIAN_POINT('Ctrl Pts',(-9.75469909499313,13.1222957008213,
9.55720420155768));
#124511=CARTESIAN_POINT('Ctrl Pts',(-9.69878134951582,13.1192182253996,
9.56671121120266));
#124512=CARTESIAN_POINT('Ctrl Pts',(-9.64342143405366,13.1161407499779,
9.57947251435366));
#124513=CARTESIAN_POINT('Ctrl Pts',(-9.58900763170072,13.1130632745562,
9.595394175151));
#124514=CARTESIAN_POINT('Ctrl Pts',(-9.53457307596047,13.1099846253874,
9.61132190845896));
#124515=CARTESIAN_POINT('Ctrl Pts',(-9.48108582259361,13.1069059762186,
9.63041225381241));
#124516=CARTESIAN_POINT('Ctrl Pts',(-9.42891835822367,13.1038273270499,
9.65252161114693));
#124517=CARTESIAN_POINT('Ctrl Pts',(-9.37667202481571,13.1007440234456,
9.67466439436798));
#124518=CARTESIAN_POINT('Ctrl Pts',(-9.32574991787845,13.0976607198414,
9.69983510710552));
#124519=CARTESIAN_POINT('Ctrl Pts',(-9.27650306928019,13.0945774162371,
9.72784260359065));
#124520=CARTESIAN_POINT('Ctrl Pts',(-9.22721636945145,13.091491617581,9.755872764129));
#124521=CARTESIAN_POINT('Ctrl Pts',(-9.17960804257342,13.0884058189248,
9.78674401331004));
#124522=CARTESIAN_POINT('Ctrl Pts',(-9.13400044645138,13.0853200202687,
9.82022162112811));
#124523=CARTESIAN_POINT('Ctrl Pts',(-9.08829907787532,13.0822278769915,
9.85376806128348));
#124524=CARTESIAN_POINT('Ctrl Pts',(-9.04460703761997,13.0791357337144,
9.88993125001151));
#124525=CARTESIAN_POINT('Ctrl Pts',(-9.00321327857189,13.0760435904372,
9.92843643119757));
#124526=CARTESIAN_POINT('Ctrl Pts',(-8.98078087256881,13.0743678737348,
9.94930343814382));
#124527=CARTESIAN_POINT('Ctrl Pts',(-8.95902279238694,13.0726921570323,
9.97085761632403));
#124528=CARTESIAN_POINT('Ctrl Pts',(-8.93798015951895,13.0710164403299,
9.9930510894665));
#124529=CARTESIAN_POINT('Ctrl Pts',(-8.90055520974898,13.0680361282269,
10.0325228429675));
#124530=CARTESIAN_POINT('Ctrl Pts',(-8.86523868247035,13.0650558161238,
10.0741844535331));
#124531=CARTESIAN_POINT('Ctrl Pts',(-8.83230144086544,13.0620755040207,
10.1177798885793));
#124532=CARTESIAN_POINT('Ctrl Pts',(-8.7994307085445,13.0591012099815,10.1612872925389));
#124533=CARTESIAN_POINT('Ctrl Pts',(-8.76893005595056,13.0561269159423,
10.2067203504602));
#124534=CARTESIAN_POINT('Ctrl Pts',(-8.74103264624124,13.0531526219032,
10.2537872607831));
#124535=CARTESIAN_POINT('Ctrl Pts',(-8.71316679315608,13.0501816922867,
10.3008009305787));
#124536=CARTESIAN_POINT('Ctrl Pts',(-8.68789862887806,13.0472107626702,
10.3494443336317));
#124537=CARTESIAN_POINT('Ctrl Pts',(-8.6654190612364,13.0442398330538,10.399395331446));
#124538=CARTESIAN_POINT('Ctrl Pts',(-8.64295558404035,13.041271029972,10.4493105752891));
#124539=CARTESIAN_POINT('Ctrl Pts',(-8.62327697216056,13.0383022268903,
10.5005310693765));
#124540=CARTESIAN_POINT('Ctrl Pts',(-8.60652785182188,13.0353334238085,
10.5527108069136));
#124541=CARTESIAN_POINT('Ctrl Pts',(-8.58978376392874,13.0323655127342,
10.6048748665117));
#124542=CARTESIAN_POINT('Ctrl Pts',(-8.57596758709121,13.0293976016599,
10.6579970840582));
#124543=CARTESIAN_POINT('Ctrl Pts',(-8.56517465496131,13.0264296905856,
10.7117145871977));
#124544=CARTESIAN_POINT('Ctrl Pts',(-8.55437249422687,13.0234592417693,
10.7654780220253));
#124545=CARTESIAN_POINT('Ctrl Pts',(-8.54659885225552,13.020488792953,10.8198372291036));
#124546=CARTESIAN_POINT('Ctrl Pts',(-8.54189792310134,13.0175183441366,
10.8744190167907));
#124547=CARTESIAN_POINT('Ctrl Pts',(-8.53719511151245,13.0145467058371,
10.9290226611465));
#124548=CARTESIAN_POINT('Ctrl Pts',(-8.53556748112019,13.0115750675376,
10.9838485227374));
#124549=CARTESIAN_POINT('Ctrl Pts',(-8.53700706325901,13.0086034292382,
11.0385216438637));
#124550=CARTESIAN_POINT('Ctrl Pts',(-8.53844943988335,13.0056260224591,
11.0933008952632));
#124551=CARTESIAN_POINT('Ctrl Pts',(-8.54297087756189,13.00264861568,11.1479262741279));
#124552=CARTESIAN_POINT('Ctrl Pts',(-8.5505114136092,12.9996712089009,11.2020274434893));
#124553=CARTESIAN_POINT('Ctrl Pts',(-8.55695965237494,12.9971250994872,
11.2482916951762));
#124554=CARTESIAN_POINT('Ctrl Pts',(-8.5656147458921,12.9945789900735,11.294172543667));
#124555=CARTESIAN_POINT('Ctrl Pts',(-8.57641011449673,12.9920328806598,
11.3394467379322));
#124556=CARTESIAN_POINT('Ctrl Pts',(-8.58919170728616,12.9890183162744,
11.3930508654206));
#124557=CARTESIAN_POINT('Ctrl Pts',(-8.60503150897651,12.986003751889,11.4460427091708));
#124558=CARTESIAN_POINT('Ctrl Pts',(-8.62385347287675,12.9829891875036,
11.4980491801887));
#124559=CARTESIAN_POINT('Ctrl Pts',(-8.64264201665942,12.9799799757528,
11.5499633089629));
#124560=CARTESIAN_POINT('Ctrl Pts',(-8.6644020355962,12.976970764002,11.6008950465764));
#124561=CARTESIAN_POINT('Ctrl Pts',(-8.68900719273,12.9739615522512,11.6504845188675));
#124562=CARTESIAN_POINT('Ctrl Pts',(-8.71358799874196,12.9709553186437,
11.7000249136715));
#124563=CARTESIAN_POINT('Ctrl Pts',(-8.7410081315262,12.9679490850361,11.7482252058589));
#124564=CARTESIAN_POINT('Ctrl Pts',(-8.77109314757686,12.9649428514286,
11.7947453668109));
#124565=CARTESIAN_POINT('Ctrl Pts',(-8.80116016980837,12.9619384158465,
11.8412377040995));
#124566=CARTESIAN_POINT('Ctrl Pts',(-8.83388863052887,12.9589339802644,
11.8860514611139));
#124567=CARTESIAN_POINT('Ctrl Pts',(-8.86905925543878,12.9559295446822,
11.9288731249699));
#124568=CARTESIAN_POINT('Ctrl Pts',(-8.90422261581189,12.9529257296701,
11.9716859439573));
#124569=CARTESIAN_POINT('Ctrl Pts',(-8.94182680470588,12.9499219146579,
12.0125070805286));
#124570=CARTESIAN_POINT('Ctrl Pts',(-8.98161193394522,12.9469180996457,
12.0510556583346));
#124571=CARTESIAN_POINT('Ctrl Pts',(-9.02143262164391,12.9439115999361,
12.0896386894166));
#124572=CARTESIAN_POINT('Ctrl Pts',(-9.0634377654752,12.9409051002265,12.1259447365983));
#124573=CARTESIAN_POINT('Ctrl Pts',(-9.10733128966854,12.9378986005169,
12.1597304961047));
#124574=CARTESIAN_POINT('Ctrl Pts',(-9.15124428261898,12.9348907672892,
12.1935312411187));
#124575=CARTESIAN_POINT('Ctrl Pts',(-9.19704689074182,12.9318829340614,
12.22480917203));
#124576=CARTESIAN_POINT('Ctrl Pts',(-9.2444133471966,12.9288751008336,12.253363897719));
#124577=CARTESIAN_POINT('Ctrl Pts',(-9.29186728686476,12.925861712305,12.2819713623998));
#124578=CARTESIAN_POINT('Ctrl Pts',(-9.34089037852705,12.9228483237763,
12.3078453275584));
#124579=CARTESIAN_POINT('Ctrl Pts',(-9.39113255506277,12.9198349352477,
12.3308315763069));
#124580=CARTESIAN_POINT('Ctrl Pts',(-9.42884469940513,12.9175730638284,
12.3480852223562));
#124581=CARTESIAN_POINT('Ctrl Pts',(-9.46724317756633,12.915311192409,12.3637128649905));
#124582=CARTESIAN_POINT('Ctrl Pts',(-9.50617417360824,12.9130493209897,
12.3776677041974));
#124583=CARTESIAN_POINT('Ctrl Pts',(-9.55807203035402,12.910034081442,12.3962705225094));
#124584=CARTESIAN_POINT('Ctrl Pts',(-9.61112726852308,12.9070188418942,
12.4119742732251));
#124585=CARTESIAN_POINT('Ctrl Pts',(-9.66498535908375,12.9040036023465,
12.4246394071384));
#124586=CARTESIAN_POINT('Ctrl Pts',(-9.71875086406413,12.9009935461928,
12.4372827688582));
#124587=CARTESIAN_POINT('Ctrl Pts',(-9.77331597410781,12.8979834900391,
12.4468977615394));
#124588=CARTESIAN_POINT('Ctrl Pts',(-9.82830984692722,12.8949734338853,
12.4533942140169));
#124589=CARTESIAN_POINT('Ctrl Pts',(-9.8832511933067,12.8919662527343,12.459884461521));
#124590=CARTESIAN_POINT('Ctrl Pts',(-9.93861997111454,12.8889590715833,
12.4632620088642));
#124591=CARTESIAN_POINT('Ctrl Pts',(-9.99403579492368,12.8859518904323,
12.4634878469799));
#124592=CARTESIAN_POINT('Ctrl Pts',(-10.0494203555223,12.8829464058028,
12.4637135576875));
#124593=CARTESIAN_POINT('Ctrl Pts',(-10.1048513844888,12.8799409211733,
12.4607910818566));
#124594=CARTESIAN_POINT('Ctrl Pts',(-10.1599463280466,12.8769354365438,
12.4547334539854));
#124595=CARTESIAN_POINT('Ctrl Pts',(-10.2150317286662,12.8739304724911,
12.4486768753497));
#124596=CARTESIAN_POINT('Ctrl Pts',(-10.2697806369713,12.8709255084385,
12.4394862810262));
#124597=CARTESIAN_POINT('Ctrl Pts',(-10.3238157568095,12.8679205443859,
12.4272265432095));
#124598=CARTESIAN_POINT('Ctrl Pts',(-10.3779017934463,12.8649127487832,
12.4149552531542));
#124599=CARTESIAN_POINT('Ctrl Pts',(-10.4312721839688,12.8619049531805,
12.3996091590201));
#124600=CARTESIAN_POINT('Ctrl Pts',(-10.4835614183549,12.8588971575778,
12.3813039508662));
#124601=CARTESIAN_POINT('Ctrl Pts',(-10.5358752893579,12.8558879448208,
12.362990118023));
#124602=CARTESIAN_POINT('Ctrl Pts',(-10.5871065022511,12.8528787320639,
12.3417145941067));
#124603=CARTESIAN_POINT('Ctrl Pts',(-10.6369093691016,12.849869519307,12.3176413417735));
#124604=CARTESIAN_POINT('Ctrl Pts',(-10.6868061775791,12.8468546303639,
12.2935226807994));
#124605=CARTESIAN_POINT('Ctrl Pts',(-10.7352687970077,12.8438397414209,
12.2665960053905));
#124606=CARTESIAN_POINT('Ctrl Pts',(-10.781977016144,12.8408248524778,12.2370708129378));
#124607=CARTESIAN_POINT('Ctrl Pts',(-10.8168821283986,12.8385718220917,
12.2150065986312));
#124608=CARTESIAN_POINT('Ctrl Pts',(-10.8508080173204,12.8363187917057,
12.1914921758089));
#124609=CARTESIAN_POINT('Ctrl Pts',(-10.8836331703264,12.8340657613196,
12.1666296200161));
#124610=CARTESIAN_POINT('Ctrl Pts',(-10.9281971894432,12.8310070066757,
12.1328757663345));
#124611=CARTESIAN_POINT('Ctrl Pts',(-10.9709323801074,12.8279482520317,
12.0964827451277));
#124612=CARTESIAN_POINT('Ctrl Pts',(-11.0115060496337,12.8248894973878,
12.0576803683318));
#124613=CARTESIAN_POINT('Ctrl Pts',(-11.0509173035851,12.8219183745523,
12.0199896604496));
#124614=CARTESIAN_POINT('Ctrl Pts',(-11.0882887948641,12.8189472517169,
11.9800261918535));
#124615=CARTESIAN_POINT('Ctrl Pts',(-11.1233463040231,12.8159761288814,
11.9380433525363));
#124616=CARTESIAN_POINT('Ctrl Pts',(-11.1583695041737,12.8130079137334,
11.8961015996974));
#124617=CARTESIAN_POINT('Ctrl Pts',(-11.1910828596685,12.8100396985854,
11.8521448013385));
#124618=CARTESIAN_POINT('Ctrl Pts',(-11.2212495020353,12.8070714834374,
11.8064625867196));
#124619=CARTESIAN_POINT('Ctrl Pts',(-11.2513991981548,12.8041049356976,
11.7608060342907));
#124620=CARTESIAN_POINT('Ctrl Pts',(-11.2790047175845,12.8011383879578,
11.7134264364987));
#124621=CARTESIAN_POINT('Ctrl Pts',(-11.3038714750513,12.798171840218,11.6646438343561));
#124622=CARTESIAN_POINT('Ctrl Pts',(-11.3287346289191,12.7952057223794,
11.6158683016086));
#124623=CARTESIAN_POINT('Ctrl Pts',(-11.3508595646768,12.7922396045408,
11.5656906508641));
#124624=CARTESIAN_POINT('Ctrl Pts',(-11.370097980956,12.7892734867022,11.5144548304568));
#124625=CARTESIAN_POINT('Ctrl Pts',(-11.3893533958098,12.7863047480774,
11.4631737393838));
#124626=CARTESIAN_POINT('Ctrl Pts',(-11.4057170135729,12.7833360094526,
11.4108331211167));
#124627=CARTESIAN_POINT('Ctrl Pts',(-11.4190896270524,12.7803672708279,
11.3577944666878));
#124628=CARTESIAN_POINT('Ctrl Pts',(-11.4324695517042,12.7773969091127,
11.3047268145804));
#124629=CARTESIAN_POINT('Ctrl Pts',(-11.4428551179191,12.7744265473976,
11.2509608986462));
#124630=CARTESIAN_POINT('Ctrl Pts',(-11.4501984059751,12.7714561856825,
11.1968675527031));
#124631=CARTESIAN_POINT('Ctrl Pts',(-11.4575535382614,12.7684810329734,
11.1426869578266));
#124632=CARTESIAN_POINT('Ctrl Pts',(-11.4618565698593,12.7655058802644,
11.0881784184255));
#124633=CARTESIAN_POINT('Ctrl Pts',(-11.4631115929678,12.7625307275554,
11.0337152268741));
#124634=CARTESIAN_POINT('Ctrl Pts',(-11.4633752506757,12.7619057016585,
11.0222734931305));
#124635=CARTESIAN_POINT('Ctrl Pts',(-11.463504569122,12.7612806757617,11.0108337466015));
#124636=CARTESIAN_POINT('Ctrl Pts',(-11.4634998767682,12.7606556498649,
10.9993994174008));
#124637=CARTESIAN_POINT('Origin',(-10.,13.15,11.));
#124638=CARTESIAN_POINT('',(-11.3001231424463,13.15,10.3280535255874));
#124639=CARTESIAN_POINT('',(-11.4635,13.15,11.));
#124640=CARTESIAN_POINT('Origin',(-10.,13.15,11.));
#124641=CARTESIAN_POINT('Ctrl Pts',(-11.3001231424463,13.15,10.3280535255874));
#124642=CARTESIAN_POINT('Ctrl Pts',(-11.3131761773218,13.1500001384125,
10.3600202599267));
#124643=CARTESIAN_POINT('Ctrl Pts',(-11.3249989234091,13.15,10.3924378242408));
#124644=CARTESIAN_POINT('Ctrl Pts',(-11.3355332824938,13.15,10.425267838127));
#124645=CARTESIAN_POINT('Ctrl Pts',(-11.3530400634154,13.15,10.4798271953819));
#124646=CARTESIAN_POINT('Ctrl Pts',(-11.3669904096394,13.15,10.5355261957002));
#124647=CARTESIAN_POINT('Ctrl Pts',(-11.3774433906746,13.15,10.5920302374161));
#124648=CARTESIAN_POINT('Ctrl Pts',(-11.3819168595279,13.15,10.6162117670538));
#124649=CARTESIAN_POINT('Ctrl Pts',(-11.3857491615815,13.15,10.6405407123288));
#124650=CARTESIAN_POINT('Ctrl Pts',(-11.3889422263824,13.15,10.6649903831658));
#124651=CARTESIAN_POINT('Ctrl Pts',(-11.3905331695892,13.15,10.6771724214745));
#124652=CARTESIAN_POINT('Ctrl Pts',(-11.3919652511976,13.15,10.6893842554283));
#124653=CARTESIAN_POINT('Ctrl Pts',(-11.3932374922766,13.15,10.7016085237643));
#124654=CARTESIAN_POINT('Ctrl Pts',(-11.3991939351861,13.15,10.7588407242136));
#124655=CARTESIAN_POINT('Ctrl Pts',(-11.4016617168143,13.15,10.81642392022));
#124656=CARTESIAN_POINT('Ctrl Pts',(-11.4007057393064,13.15,10.8740172395586));
#124657=CARTESIAN_POINT('Ctrl Pts',(-11.4000640964045,13.15,10.9126733211552));
#124658=CARTESIAN_POINT('Ctrl Pts',(-11.397878941981,13.15,10.9513339579117));
#124659=CARTESIAN_POINT('Ctrl Pts',(-11.3941573214885,13.15,10.9898921947642));
#124660=CARTESIAN_POINT('Ctrl Pts',(-11.3925406285891,13.15,11.0066421099846));
#124661=CARTESIAN_POINT('Ctrl Pts',(-11.3906338685773,13.15,11.0233726427463));
#124662=CARTESIAN_POINT('Ctrl Pts',(-11.3884370658247,13.15,11.0400747034851));
#124663=CARTESIAN_POINT('Ctrl Pts',(-11.3869501481743,13.15,11.0513795823056));
#124664=CARTESIAN_POINT('Ctrl Pts',(-11.3853299562707,13.15,11.0626733277691));
#124665=CARTESIAN_POINT('Ctrl Pts',(-11.3835793602485,13.15,11.0739358722133));
#124666=CARTESIAN_POINT('Ctrl Pts',(-11.3749382707088,13.15,11.1295287410149));
#124667=CARTESIAN_POINT('Ctrl Pts',(-11.3631134776978,13.15,11.1844512590875));
#124668=CARTESIAN_POINT('Ctrl Pts',(-11.3481619217541,13.15,11.2383858660144));
#124669=CARTESIAN_POINT('Ctrl Pts',(-11.3335747203039,13.15,11.2910061404084));
#124670=CARTESIAN_POINT('Ctrl Pts',(-11.3160107755577,13.15,11.3426869861088));
#124671=CARTESIAN_POINT('Ctrl Pts',(-11.2954804801254,13.15,11.3931098408422));
#124672=CARTESIAN_POINT('Ctrl Pts',(-11.2831410946931,13.15,11.423415641419));
#124673=CARTESIAN_POINT('Ctrl Pts',(-11.2697293596248,13.15,11.4532664844744));
#124674=CARTESIAN_POINT('Ctrl Pts',(-11.2552409779441,13.15,11.4825868996509));
#124675=CARTESIAN_POINT('Ctrl Pts',(-11.2449747067262,13.15,11.5033629491129));
#124676=CARTESIAN_POINT('Ctrl Pts',(-11.2341677552456,13.15,11.5238725721958));
#124677=CARTESIAN_POINT('Ctrl Pts',(-11.2228172228053,13.15,11.5440871005847));
#124678=CARTESIAN_POINT('Ctrl Pts',(-11.2179779990594,13.15,11.5527054298398));
#124679=CARTESIAN_POINT('Ctrl Pts',(-11.2130398598468,13.15,11.5612700459744));
#124680=CARTESIAN_POINT('Ctrl Pts',(-11.2080101180467,13.15,11.5697664482042));
#124681=CARTESIAN_POINT('Ctrl Pts',(-11.1811395839106,13.15,11.6151570219604));
#124682=CARTESIAN_POINT('Ctrl Pts',(-11.1516077646003,13.15,11.6586941060695));
#124683=CARTESIAN_POINT('Ctrl Pts',(-11.1194321742994,13.15,11.7000869398436));
#124684=CARTESIAN_POINT('Ctrl Pts',(-11.1119483238485,13.15,11.7097146661668));
#124685=CARTESIAN_POINT('Ctrl Pts',(-11.1043212841036,13.15,11.7192262371259));
#124686=CARTESIAN_POINT('Ctrl Pts',(-11.0965509899046,13.15,11.7286176981156));
#124687=CARTESIAN_POINT('Ctrl Pts',(-11.0623201142441,13.15,11.7699903830067));
#124688=CARTESIAN_POINT('Ctrl Pts',(-11.0253109874935,13.15,11.809035775708));
#124689=CARTESIAN_POINT('Ctrl Pts',(-10.9858215050894,13.15,11.8456181550914));
#124690=CARTESIAN_POINT('Ctrl Pts',(-10.9676656385286,13.15,11.8624374385594));
#124691=CARTESIAN_POINT('Ctrl Pts',(-10.948985131905,13.15,11.8787354281648));
#124692=CARTESIAN_POINT('Ctrl Pts',(-10.9298077378061,13.15,11.8944954447994));
#124693=CARTESIAN_POINT('Ctrl Pts',(-10.9162290702529,13.15,11.9056544179847));
#124694=CARTESIAN_POINT('Ctrl Pts',(-10.9024012778973,13.15,11.9165436356749));
#124695=CARTESIAN_POINT('Ctrl Pts',(-10.8883341250136,13.15,11.9271564682047));
#124696=CARTESIAN_POINT('Ctrl Pts',(-10.8801543039317,13.15,11.9333276580669));
#124697=CARTESIAN_POINT('Ctrl Pts',(-10.8719002307745,13.15,11.9394002908066));
#124698=CARTESIAN_POINT('Ctrl Pts',(-10.8635785576173,13.15,11.9453704723774));
#124699=CARTESIAN_POINT('Ctrl Pts',(-10.8209146516277,13.15,11.9759786518223));
#124700=CARTESIAN_POINT('Ctrl Pts',(-10.7764391517408,13.15,12.0039254571033));
#124701=CARTESIAN_POINT('Ctrl Pts',(-10.7304434962769,13.15,12.0291037016939));
#124702=CARTESIAN_POINT('Ctrl Pts',(-10.6846701427477,13.15,12.0541602571286));
#124703=CARTESIAN_POINT('Ctrl Pts',(-10.637390123747,13.15,12.076475205012));
#124704=CARTESIAN_POINT('Ctrl Pts',(-10.5888782659809,13.15,12.0958933837174));
#124705=CARTESIAN_POINT('Ctrl Pts',(-10.5645820655954,13.15,12.1056185928244));
#124706=CARTESIAN_POINT('Ctrl Pts',(-10.5399767966041,13.15,12.114616401565));
#124707=CARTESIAN_POINT('Ctrl Pts',(-10.5150971825505,13.15,12.1228623097433));
#124708=CARTESIAN_POINT('Ctrl Pts',(-10.4967682426672,13.15,12.1289371127911));
#124709=CARTESIAN_POINT('Ctrl Pts',(-10.478290409887,13.15,12.1346037641086));
#124710=CARTESIAN_POINT('Ctrl Pts',(-10.4596778365068,13.15,12.1398512498179));
#124711=CARTESIAN_POINT('Ctrl Pts',(-10.4506803455549,13.15,12.1423879331784));
#124712=CARTESIAN_POINT('Ctrl Pts',(-10.4416523204638,13.15,12.1448262828857));
#124713=CARTESIAN_POINT('Ctrl Pts',(-10.4326078634624,13.15,12.1471621057536));
#124714=CARTESIAN_POINT('Ctrl Pts',(-10.3837777132245,13.15,12.1597729879272));
#124715=CARTESIAN_POINT('Ctrl Pts',(-10.3343722745856,13.15,12.1694272995591));
#124716=CARTESIAN_POINT('Ctrl Pts',(-10.2846451915519,13.15,12.1759981133649));
#124717=CARTESIAN_POINT('Ctrl Pts',(-10.2359330315984,13.15,12.1824348177442));
#124718=CARTESIAN_POINT('Ctrl Pts',(-10.186911278204,13.15,12.1859126350798));
#124719=CARTESIAN_POINT('Ctrl Pts',(-10.1378247727926,13.15,12.1862630676831));
#124720=CARTESIAN_POINT('Ctrl Pts',(-10.0887382673813,13.15,12.1866135002864));
#124721=CARTESIAN_POINT('Ctrl Pts',(-10.0395861028003,13.15,12.18383673007));
#124722=CARTESIAN_POINT('Ctrl Pts',(-9.99063336962942,13.15,12.1777127530665));
#124723=CARTESIAN_POINT('Ctrl Pts',(-8.88725970493454,13.15,11.3858809379032));
#124724=CARTESIAN_POINT('Ctrl Pts',(-8.82376602848846,13.15,11.257038925907));
#124725=CARTESIAN_POINT('Ctrl Pts',(-8.78447134070238,13.15,11.1152741740962));
#124726=CARTESIAN_POINT('Ctrl Pts',(-8.76392545979419,13.15,10.799130945112));
#124727=CARTESIAN_POINT('Ctrl Pts',(-8.78332170790095,13.15,10.6406721133509));
#124728=CARTESIAN_POINT('Ctrl Pts',(-8.87404255296001,13.15,10.3431797244535));
#124729=CARTESIAN_POINT('Ctrl Pts',(-8.94502385990684,13.15,10.2027828893632));
#124730=CARTESIAN_POINT('Ctrl Pts',(-9.13810939903446,13.15,9.95383959518158));
#124731=CARTESIAN_POINT('Ctrl Pts',(-9.26076129175572,13.15,9.84753666691401));
#124732=CARTESIAN_POINT('Ctrl Pts',(-9.52446957852726,13.15,9.68764328331985));
#124733=CARTESIAN_POINT('Ctrl Pts',(-9.66358225430457,13.15,9.63064099380393));
#124734=CARTESIAN_POINT('Ctrl Pts',(-9.95615051730649,13.15,9.55970692742898));
#124735=CARTESIAN_POINT('Ctrl Pts',(-10.110190526121,13.15,9.54703709299416));
#124736=CARTESIAN_POINT('Ctrl Pts',(-10.2623899083091,13.15,9.5602139790866));
#124737=CARTESIAN_POINT('Origin',(-10.,13.15,11.));
#124738=CARTESIAN_POINT('Ctrl Pts',(-10.5090242870262,3.43381032135065,
9.9402163861523));
#124739=CARTESIAN_POINT('Ctrl Pts',(-10.8597543436467,3.46014567915783,
10.1086659006971));
#124740=CARTESIAN_POINT('Ctrl Pts',(-11.3748996206351,3.51280889018836,
10.8179605421406));
#124741=CARTESIAN_POINT('Ctrl Pts',(-10.9029747057089,3.59179995444226,
12.0542997660115));
#124742=CARTESIAN_POINT('Ctrl Pts',(-9.61102705413118,3.67078351411235,
12.3312080230099));
#124743=CARTESIAN_POINT('Ctrl Pts',(-8.67243540897439,3.74976707378244,
11.4024835440384));
#124744=CARTESIAN_POINT('Ctrl Pts',(-8.93744951993946,3.82875063345253,
10.1079392171469));
#124745=CARTESIAN_POINT('Ctrl Pts',(-10.1662184072312,3.90773419312261,
9.62280065437638));
#124746=CARTESIAN_POINT('Ctrl Pts',(-11.244163884115,3.98671775279271,10.3863742247578));
#124747=CARTESIAN_POINT('Ctrl Pts',(-11.1938649654809,4.06570131246279,
11.7065393375666));
#124748=CARTESIAN_POINT('Ctrl Pts',(-10.0608681388599,4.14468487213289,
12.3859082577524));
#124749=CARTESIAN_POINT('Ctrl Pts',(-8.87268420671462,4.22366843180297,
11.8084764549642));
#124750=CARTESIAN_POINT('Ctrl Pts',(-8.70681751959354,4.30265199147307,
10.49784911305));
#124751=CARTESIAN_POINT('Ctrl Pts',(-9.71369639202666,4.38163555114315,
9.64261346806346));
#124752=CARTESIAN_POINT('Ctrl Pts',(-10.9802123564701,4.46061911081324,
10.0183401047257));
#124753=CARTESIAN_POINT('Ctrl Pts',(-11.3578086652279,4.53960267048333,
11.2843023117032));
#124754=CARTESIAN_POINT('Ctrl Pts',(-10.504054987852,4.61858623015341,12.292439426545));
#124755=CARTESIAN_POINT('Ctrl Pts',(-9.19319158814925,4.69756978982351,
12.1285087346752));
#124756=CARTESIAN_POINT('Ctrl Pts',(-8.61399459221431,4.77655334949359,
10.9411723380592));
#124757=CARTESIAN_POINT('Ctrl Pts',(-9.29171783157003,4.85553690916369,
9.80718487427643));
#124758=CARTESIAN_POINT('Ctrl Pts',(-10.6117575376679,4.93452046883377,
9.75491993483644));
#124759=CARTESIAN_POINT('Ctrl Pts',(-11.3770155961763,5.01350402850386,
10.8317749122026));
#124760=CARTESIAN_POINT('Ctrl Pts',(-10.8935060234263,5.09248758817395,
12.0611873555489));
#124761=CARTESIAN_POINT('Ctrl Pts',(-9.59970687324196,5.17147114784404,
12.3282458523706));
#124762=CARTESIAN_POINT('Ctrl Pts',(-8.66891965550706,5.25045470751413,
11.3907643076178));
#124763=CARTESIAN_POINT('Ctrl Pts',(-8.94524297664017,5.32943826718422,
10.0989121864417));
#124764=CARTESIAN_POINT('Ctrl Pts',(-10.1780888111114,5.40842182685431,
9.62422530790764));
#124765=CARTESIAN_POINT('Ctrl Pts',(-11.249432087953,5.48740538652439,10.3971807195104));
#124766=CARTESIAN_POINT('Ctrl Pts',(-11.1877087953521,5.5663889461945,11.7168120009095));
#124767=CARTESIAN_POINT('Ctrl Pts',(-10.0488936440701,5.64537250586456,
12.3863913729684));
#124768=CARTESIAN_POINT('Ctrl Pts',(-8.86573854494997,5.72435606553468,
11.7987005564936));
#124769=CARTESIAN_POINT('Ctrl Pts',(-8.71120576787552,5.80333962520474,
10.4866959433319));
#124770=CARTESIAN_POINT('Ctrl Pts',(-9.72543572159486,5.88232318487485,
9.640188952682));
#124771=CARTESIAN_POINT('Ctrl Pts',(-10.9886584841126,5.96130674454492,
10.026847376226));
#124772=CARTESIAN_POINT('Ctrl Pts',(-11.3553012023303,6.04029030421503,
11.2960241178163));
#124773=CARTESIAN_POINT('Ctrl Pts',(-10.4928683281718,6.1192738638851,12.296746867533));
#124774=CARTESIAN_POINT('Ctrl Pts',(-9.18347028393007,6.1982574235552,12.1214949175736));
#124775=CARTESIAN_POINT('Ctrl Pts',(-8.61455468207693,6.27724098322528,
10.9291981750663));
#124776=CARTESIAN_POINT('Ctrl Pts',(-9.30205132416306,6.35622454289538,
9.80110914872666));
#124777=CARTESIAN_POINT('Ctrl Pts',(-10.62249338143,6.43520810256546,9.76025259933933));
#124778=CARTESIAN_POINT('Ctrl Pts',(-11.3784178095403,6.51419166223555,
10.8436799126432));
#124779=CARTESIAN_POINT('Ctrl Pts',(-10.8843029970064,6.59317522190564,
12.0688684843584));
#124780=CARTESIAN_POINT('Ctrl Pts',(-9.58824450728937,6.67215878157573,
12.3247373481531));
#124781=CARTESIAN_POINT('Ctrl Pts',(-8.66559277412816,6.75114234124581,
11.3792479174763));
#124782=CARTESIAN_POINT('Ctrl Pts',(-8.95306861171804,6.83012590091592,
10.0898317212739));
#124783=CARTESIAN_POINT('Ctrl Pts',(-10.1899701666462,6.90910946058599,
9.62581552797539));
#124784=CARTESIAN_POINT('Ctrl Pts',(-11.2545943748831,6.98809302025609,
10.407999508547));
#124785=CARTESIAN_POINT('Ctrl Pts',(-11.1814705151243,7.06707657992617,
11.7270481753372));
#124786=CARTESIAN_POINT('Ctrl Pts',(-10.0369120762793,7.14606013959627,
12.3867621014413));
#124787=CARTESIAN_POINT('Ctrl Pts',(-8.85887935736957,7.22504369926635,
11.7888696383636));
#124788=CARTESIAN_POINT('Ctrl Pts',(-8.71568931948482,7.30402725893644,
10.4755786967677));
#124789=CARTESIAN_POINT('Ctrl Pts',(-9.73719603516132,7.38301081860653,
9.6378672225388));
#124790=CARTESIAN_POINT('Ctrl Pts',(-10.9970305396777,7.46199437827663,
10.0354266589216));
#124791=CARTESIAN_POINT('Ctrl Pts',(-11.3526926734573,7.5409779379467,11.3077241598318));
#124792=CARTESIAN_POINT('Ctrl Pts',(-10.4816447991026,7.6199614976168,12.3009573070883));
#124793=CARTESIAN_POINT('Ctrl Pts',(-9.17380998339862,7.69894505728688,
12.1143974532622));
#124794=CARTESIAN_POINT('Ctrl Pts',(-8.61521820114381,7.77792861695698,
10.9172292507842));
#124795=CARTESIAN_POINT('Ctrl Pts',(-9.31243694043001,7.85691217662706,
9.79512296623934));
#124796=CARTESIAN_POINT('Ctrl Pts',(-10.6331827401846,7.93589573629716,
9.76567781965101));
#124797=CARTESIAN_POINT('Ctrl Pts',(-11.3797171025569,8.01487929596723,
10.8555965918649));
#124798=CARTESIAN_POINT('Ctrl Pts',(-10.8750339405711,8.09386285563734,
12.0764697999562));
#124799=CARTESIAN_POINT('Ctrl Pts',(-9.57681288677996,8.17284641530742,
12.321129930996));
#124800=CARTESIAN_POINT('Ctrl Pts',(-8.66236552917783,8.2518299749775,11.3677032089028));
#124801=CARTESIAN_POINT('Ctrl Pts',(-8.96097241869386,8.3308135346476,10.0808192165551));
#124802=CARTESIAN_POINT('Ctrl Pts',(-10.2018373374917,8.40979709431769,
9.62750835464715));
#124803=CARTESIAN_POINT('Ctrl Pts',(-11.2596629844915,8.48878065398777,
10.4188625008905));
#124804=CARTESIAN_POINT('Ctrl Pts',(-11.1751440174684,8.56776421365786,
11.7372300628551));
#124805=CARTESIAN_POINT('Ctrl Pts',(-10.0249277523716,8.64674777332795,
12.3870292839486));
#124806=CARTESIAN_POINT('Ctrl Pts',(-8.85210537436044,8.72573133299805,
11.7789798173233));
#124807=CARTESIAN_POINT('Ctrl Pts',(-8.72026876731281,8.80471489266813,
10.4645006074195));
#124808=CARTESIAN_POINT('Ctrl Pts',(-9.74897597163002,8.88369845233822,
9.63564719938351));
#124809=CARTESIAN_POINT('Ctrl Pts',(-11.005328149507,8.96268201200831,10.04407796386));
#124810=CARTESIAN_POINT('Ctrl Pts',(-11.3499831424592,9.0416655716784,11.3194012248648));
#124811=CARTESIAN_POINT('Ctrl Pts',(-10.4703853068404,9.12064913134849,
12.3050706074684));
#124812=CARTESIAN_POINT('Ctrl Pts',(-9.16421137237607,9.19963269101857,
12.1072167797246));
#124813=CARTESIAN_POINT('Ctrl Pts',(-8.61598511834872,9.27861625068866,
10.9052665067839));
#124814=CARTESIAN_POINT('Ctrl Pts',(-9.32287389528337,9.35759981035876,
9.7892267488582));
#124815=CARTESIAN_POINT('Ctrl Pts',(-10.6438248207931,9.43658337002884,
9.77119520366337));
#124816=CARTESIAN_POINT('Ctrl Pts',(-11.3809133756036,9.51556692969893,
10.8675240533223));
#124817=CARTESIAN_POINT('Ctrl Pts',(-10.8656995475751,9.59455048936902,
12.0839907382895));
#124818=CARTESIAN_POINT('Ctrl Pts',(-9.56541286457688,9.67353404903911,
12.3174238684243));
#124819=CARTESIAN_POINT('Ctrl Pts',(-8.6592381619943,9.7525176087092,11.3561310448651));
#124820=CARTESIAN_POINT('Ctrl Pts',(-8.96895380721882,9.83150116837929,
10.0718753447297));
#124821=CARTESIAN_POINT('Ctrl Pts',(-10.2136894376561,9.91048472804938,
9.62930366178233));
#124822=CARTESIAN_POINT('Ctrl Pts',(-11.2646375382657,9.98946828771946,
10.4297688852943));
#124823=CARTESIAN_POINT('Ctrl Pts',(-11.168729774795,10.0684518473895,11.7473569032777));
#124824=CARTESIAN_POINT('Ctrl Pts',(-10.012941567172,10.1474354070596,12.3871929005038));
#124825=CARTESIAN_POINT('Ctrl Pts',(-8.84541710172598,10.2264189667297,
11.7690318318396));
#124826=CARTESIAN_POINT('Ctrl Pts',(-8.72494376942007,10.3054025263998,
10.45346250245));
#124827=CARTESIAN_POINT('Ctrl Pts',(-9.76077465142473,10.3843860860699,
9.6335290489851));
#124828=CARTESIAN_POINT('Ctrl Pts',(-11.0135506940386,10.46336964574,10.0528006450672));
#124829=CARTESIAN_POINT('Ctrl Pts',(-11.3471728116493,10.5423532054101,
11.3310544410212));
#124830=CARTESIAN_POINT('Ctrl Pts',(-10.4590906921049,10.6213367650801,
12.3090864615405));
#124831=CARTESIAN_POINT('Ctrl Pts',(-9.15467516756241,10.7003203247502,
12.0999534331274));
#124832=CARTESIAN_POINT('Ctrl Pts',(-8.61685537643562,10.7793038844203,
10.8933108362856));
#124833=CARTESIAN_POINT('Ctrl Pts',(-9.33336140940735,10.8582874440904,
9.78342093685283));
#124834=CARTESIAN_POINT('Ctrl Pts',(-10.6544188286669,10.9372710037605,
9.77680433938067));
#124835=CARTESIAN_POINT('Ctrl Pts',(-11.3820065393025,11.0162545634306,
10.8794614064728));
#124836=CARTESIAN_POINT('Ctrl Pts',(-10.8563005150997,11.0952381231007,
12.0914307376909));
#124837=CARTESIAN_POINT('Ctrl Pts',(-9.55404529168748,11.1742216827708,
12.3136194373482));
#124838=CARTESIAN_POINT('Ctrl Pts',(-8.65621090648078,11.2532052424409,
11.3445322890657));
#124839=CARTESIAN_POINT('Ctrl Pts',(-8.97701218059255,11.3321888021109,
10.0630007743079));
#124840=CARTESIAN_POINT('Ctrl Pts',(-10.2255255836145,11.4111723617811,
9.63120131399661));
#124841=CARTESIAN_POINT('Ctrl Pts',(-11.2695176620004,11.4901559214511,
10.4407178499673));
#124842=CARTESIAN_POINT('Ctrl Pts',(-11.1622282713562,11.5691394811212,
11.7574279355407));
#124843=CARTESIAN_POINT('Ctrl Pts',(-10.0009544054462,11.6481230407913,
12.3872529483376));
#124844=CARTESIAN_POINT('Ctrl Pts',(-8.83881505847741,11.7271066004614,
11.7590264065578));
#124845=CARTESIAN_POINT('Ctrl Pts',(-8.72971393906159,11.8060901601315,
10.4424652408987));
#124846=CARTESIAN_POINT('Ctrl Pts',(-9.77259126592953,11.8850737198016,
9.63151286255959));
#124847=CARTESIAN_POINT('Ctrl Pts',(-11.0216974203312,11.9640572794716,
10.0615941798161));
#124848=CARTESIAN_POINT('Ctrl Pts',(-11.3442621578162,12.0430408391418,
11.3426826912335));
#124849=CARTESIAN_POINT('Ctrl Pts',(-10.4477612855078,12.1220243988118,
12.3130050437705));
#124850=CARTESIAN_POINT('Ctrl Pts',(-9.14520306579991,12.2010079584819,
12.0926070447803));
#124851=CARTESIAN_POINT('Ctrl Pts',(-8.61782701892134,12.279991518152,10.8813648817977));
#124852=CARTESIAN_POINT('Ctrl Pts',(-9.34390233273922,12.3589750778221,
9.77770260286736));
#124853=CARTESIAN_POINT('Ctrl Pts',(-10.6649569948427,12.4379586374922,
9.78251126319615));
#124854=CARTESIAN_POINT('Ctrl Pts',(-11.3830099145748,12.5169421971623,
10.8913953614281));
#124855=CARTESIAN_POINT('Ctrl Pts',(-10.8468118025409,12.5959257568324,
12.0988130567366));
#124856=CARTESIAN_POINT('Ctrl Pts',(-9.54276046145547,12.6749093165025,
12.3096711804419));
#124857=CARTESIAN_POINT('Ctrl Pts',(-8.65318901050312,12.7538928761726,
11.3329956779777));
#124858=CARTESIAN_POINT('Ctrl Pts',(-8.98532945352617,12.8328764358426,
10.0540272579587));
#124859=CARTESIAN_POINT('Ctrl Pts',(-10.2369934859239,12.9118599955128,
9.6335268605737));
#124860=CARTESIAN_POINT('Ctrl Pts',(-11.2749857449341,12.9908435551828,
10.451071347098));
#124861=CARTESIAN_POINT('Ctrl Pts',(-11.1542469424753,13.0698334244205,
11.7688789796044));
#124862=CARTESIAN_POINT('Ctrl Pts',(-10.3794236209914,13.1224954404349,
12.1788445786523));
#124863=CARTESIAN_POINT('Ctrl Pts',(-9.99037010550519,13.1488296032259,
12.17565058611));
#124864=CARTESIAN_POINT('Ctrl Pts',(-10.5513377582739,3.49023542398123,
9.85212015063649));
#124865=CARTESIAN_POINT('Ctrl Pts',(-10.9312228209415,3.5165707817884,10.0345723048824));
#124866=CARTESIAN_POINT('Ctrl Pts',(-11.4891903864173,3.56923399281895,
10.8028282163118));
#124867=CARTESIAN_POINT('Ctrl Pts',(-10.9780359458523,3.64822505707284,
12.1419401477623));
#124868=CARTESIAN_POINT('Ctrl Pts',(-9.57869304575365,3.72720861674294,
12.4418668537216));
#124869=CARTESIAN_POINT('Ctrl Pts',(-8.56207944446872,3.80619217641302,
11.4359406428495));
#124870=CARTESIAN_POINT('Ctrl Pts',(-8.84912328417233,3.88517573608311,
10.0337852145809));
#124871=CARTESIAN_POINT('Ctrl Pts',(-10.1800355825104,3.9641592957532,9.50831872021641));
#124872=CARTESIAN_POINT('Ctrl Pts',(-11.3475870292958,4.04314285542329,
10.3353655847789));
#124873=CARTESIAN_POINT('Ctrl Pts',(-11.2931069312924,4.12212641509338,
11.7652715684391));
#124874=CARTESIAN_POINT('Ctrl Pts',(-10.0659279018402,4.20110997476347,
12.5011141343889));
#124875=CARTESIAN_POINT('Ctrl Pts',(-8.77897424901355,4.28009353443356,
11.8756823744131));
#124876=CARTESIAN_POINT('Ctrl Pts',(-8.59931962391916,4.35907709410364,
10.4561070043562));
#124877=CARTESIAN_POINT('Ctrl Pts',(-9.68989693924451,4.43806065377374,
9.52977850624579));
#124878=CARTESIAN_POINT('Ctrl Pts',(-11.061694101878,4.51704421344381,9.9367380303017));
#124879=CARTESIAN_POINT('Ctrl Pts',(-11.4706787175616,4.59602777311392,
11.3079354034798));
#124880=CARTESIAN_POINT('Ctrl Pts',(-10.5459553780284,4.67501133278399,
12.3998755546594));
#124881=CARTESIAN_POINT('Ctrl Pts',(-9.12612432749545,4.75399489245409,
12.2223178575684));
#124882=CARTESIAN_POINT('Ctrl Pts',(-8.49878063982344,4.83297845212418,
10.9362821930396));
#124883=CARTESIAN_POINT('Ctrl Pts',(-9.23284072504908,4.91196201179426,
9.70803017810119));
#124884=CARTESIAN_POINT('Ctrl Pts',(-10.6626108773617,4.99094557146436,
9.65142063061672));
#124885=CARTESIAN_POINT('Ctrl Pts',(-11.4914822558648,5.06992913113444,
10.8177909283396));
#124886=CARTESIAN_POINT('Ctrl Pts',(-10.9677801639641,5.14891269080454,
12.1494002793753));
#124887=CARTESIAN_POINT('Ctrl Pts',(-9.56643185642774,5.22789625047462,
12.4386584478327));
#124888=CARTESIAN_POINT('Ctrl Pts',(-8.55827143827977,5.30687981014471,
11.4232472258526));
#124889=CARTESIAN_POINT('Ctrl Pts',(-8.85756458462907,5.3858633698148,10.0240077972755));
#124890=CARTESIAN_POINT('Ctrl Pts',(-10.1928927330077,5.46484692948489,
9.50986180038816));
#124891=CARTESIAN_POINT('Ctrl Pts',(-11.3532931611411,5.54383048915498,
10.3470703869731));
#124892=CARTESIAN_POINT('Ctrl Pts',(-11.2864390195152,5.62281404882507,
11.77639816362));
#124893=CARTESIAN_POINT('Ctrl Pts',(-10.0529580077071,5.70179760849516,
12.5016374093425));
#124894=CARTESIAN_POINT('Ctrl Pts',(-8.77145121782494,5.78078116816525,
11.865093838492));
#124895=CARTESIAN_POINT('Ctrl Pts',(-8.60407265247242,5.85976472783534,
10.4440267092764));
#124896=CARTESIAN_POINT('Ctrl Pts',(-9.70261211966464,5.93874828750542,
9.52715244908236));
#124897=CARTESIAN_POINT('Ctrl Pts',(-11.0708423276095,6.01773184717552,
9.94595248257362));
#124898=CARTESIAN_POINT('Ctrl Pts',(-11.4679628177349,6.0967154068456,11.3206316037791));
#124899=CARTESIAN_POINT('Ctrl Pts',(-10.533838809079,6.17569896651569,12.4045410586809));
#124900=CARTESIAN_POINT('Ctrl Pts',(-9.11559492406168,6.25468252618578,
12.2147210055197));
#124901=CARTESIAN_POINT('Ctrl Pts',(-8.49938728806626,6.33366608585587,
10.9233126582846));
#124902=CARTESIAN_POINT('Ctrl Pts',(-9.24403320601036,6.41264964552595,
9.70144939798937));
#124903=CARTESIAN_POINT('Ctrl Pts',(-10.6742391555871,6.49163320519605,
9.65719658152432));
#124904=CARTESIAN_POINT('Ctrl Pts',(-11.4930010304939,6.57061676486612,
10.8306855512928));
#124905=CARTESIAN_POINT('Ctrl Pts',(-10.9578121210141,6.64960032453624,
12.1577199145024));
#124906=CARTESIAN_POINT('Ctrl Pts',(-9.55401666267395,6.72858388420629,
12.4348582934994));
#124907=CARTESIAN_POINT('Ctrl Pts',(-8.55466800447861,6.80756744387642,
11.4107735170613));
#124908=CARTESIAN_POINT('Ctrl Pts',(-8.86604073834288,6.88655100354648,
10.0141725036809));
#124909=CARTESIAN_POINT('Ctrl Pts',(-10.2057617455338,6.96553456321659,
9.51158421008386));
#124910=CARTESIAN_POINT('Ctrl Pts',(-11.3588845715633,7.04451812288666,
10.3587885054337));
#124911=CARTESIAN_POINT('Ctrl Pts',(-11.2796821721034,7.12350168255676,
11.7874852366852));
#124912=CARTESIAN_POINT('Ctrl Pts',(-10.0399804526184,7.20248524222684,
12.5020389552223));
#124913=CARTESIAN_POINT('Ctrl Pts',(-8.76402184912772,7.28146880189694,
11.8544457093129));
#124914=CARTESIAN_POINT('Ctrl Pts',(-8.60892890659698,7.36045236156703,
10.4319853235212));
#124915=CARTESIAN_POINT('Ctrl Pts',(-9.71535002841199,7.43943592123711,
9.52463772134717));
#124916=CARTESIAN_POINT('Ctrl Pts',(-11.0799103239017,7.51841948090721,
9.9552449320883));
#124917=CARTESIAN_POINT('Ctrl Pts',(-11.4651374506592,7.59740304057729,
11.333304230805));
#124918=CARTESIAN_POINT('Ctrl Pts',(-10.5216823059128,7.67638660024737,
12.4091014978681));
#124919=CARTESIAN_POINT('Ctrl Pts',(-9.1051315953463,7.75537015991747,12.2070335529509));
#124920=CARTESIAN_POINT('Ctrl Pts',(-8.50010596323409,7.83435371958756,
10.9103487977168));
#124921=CARTESIAN_POINT('Ctrl Pts',(-9.25528214351071,7.91333727925765,
9.6949656043526));
#124922=CARTESIAN_POINT('Ctrl Pts',(-10.685817084663,7.99232083892774,9.66307278209282));
#124923=CARTESIAN_POINT('Ctrl Pts',(-11.4944083293544,8.07130439859782,
10.8435928238447));
#124924=CARTESIAN_POINT('Ctrl Pts',(-10.9477725591963,8.15028795826791,
12.1659531018147));
#124925=CARTESIAN_POINT('Ctrl Pts',(-9.54163477012829,8.229271517938,12.4309510039276));
#124926=CARTESIAN_POINT('Ctrl Pts',(-8.55117248954609,8.30825507760809,
11.3982691358224));
#124927=CARTESIAN_POINT('Ctrl Pts',(-8.87460156212072,8.38723863727818,
10.0044108198581));
#124928=CARTESIAN_POINT('Ctrl Pts',(-10.2186153942451,8.46622219694826,
9.51341775572429));
#124929=CARTESIAN_POINT('Ctrl Pts',(-11.3643745175839,8.54520575661836,
10.3705545016729));
#124930=CARTESIAN_POINT('Ctrl Pts',(-11.2728297740467,8.62418931628843,
11.7985135101531));
#124931=CARTESIAN_POINT('Ctrl Pts',(-10.0269999123061,8.70317287595854,
12.5023283477097));
#124932=CARTESIAN_POINT('Ctrl Pts',(-8.75668476777029,8.78215643562862,
11.8437337808233));
#124933=CARTESIAN_POINT('Ctrl Pts',(-8.61388902846928,8.86113999529871,
10.4199863499891));
#124934=CARTESIAN_POINT('Ctrl Pts',(-9.72810919124724,8.94012355496881,
9.5222331551586));
#124935=CARTESIAN_POINT('Ctrl Pts',(-11.0888976860354,9.01910711463889,
9.9646153908119));
#124936=CARTESIAN_POINT('Ctrl Pts',(-11.4622026854927,9.09809067430898,
11.3459519708493));
#124937=CARTESIAN_POINT('Ctrl Pts',(-10.5094868500547,9.17707423397907,
12.4135567230282));
#124938=CARTESIAN_POINT('Ctrl Pts',(-9.09473508418051,9.25605779364916,
12.1992559742537));
#124939=CARTESIAN_POINT('Ctrl Pts',(-8.50093663167824,9.33504135331924,
10.8973916311767));
#124940=CARTESIAN_POINT('Ctrl Pts',(-9.26658668720091,9.41402491298935,
9.68857925431773));
#124941=CARTESIAN_POINT('Ctrl Pts',(-10.6973438055201,9.49300847265941,
9.66904880761934));
#124942=CARTESIAN_POINT('Ctrl Pts',(-11.4957040445425,9.57199203232953,
10.8565117749229));
#124943=CARTESIAN_POINT('Ctrl Pts',(-10.9376622296101,9.6509755919996,12.1740992303717));
#124944=CARTESIAN_POINT('Ctrl Pts',(-9.52928710254954,9.7299591516697,12.4269368688805));
#124945=CARTESIAN_POINT('Ctrl Pts',(-8.54778515488208,9.80894271133978,
11.3857350168392));
#124946=CARTESIAN_POINT('Ctrl Pts',(-8.8832464165401,9.88792627100986,9.9947234741494));
#124947=CARTESIAN_POINT('Ctrl Pts',(-10.2314527195007,9.96690983067997,
9.51536230068326));
#124948=CARTESIAN_POINT('Ctrl Pts',(-11.3697625892266,10.04589339035,10.382367497008));
#124949=CARTESIAN_POINT('Ctrl Pts',(-11.265882337025,10.1248769500202,11.8094821606464));
#124950=CARTESIAN_POINT('Ctrl Pts',(-10.014017355979,10.2038605096902,12.5025055651571));
#124951=CARTESIAN_POINT('Ctrl Pts',(-8.74944052160167,10.2828440693603,
11.8329588528764));
#124952=CARTESIAN_POINT('Ctrl Pts',(-8.61895264772564,10.3618276290304,
10.4080306846023));
#124953=CARTESIAN_POINT('Ctrl Pts',(-9.74088865547793,10.4408111887005,
9.51993893006537));
#124954=CARTESIAN_POINT('Ctrl Pts',(-11.0978037429465,10.5197947483706,
9.97406315907262));
#124955=CARTESIAN_POINT('Ctrl Pts',(-11.4591587413663,10.5987783080407,
11.3585738795403));
#124956=CARTESIAN_POINT('Ctrl Pts',(-10.4972533521105,10.6777618677108,
12.4179064014977));
#124957=CARTESIAN_POINT('Ctrl Pts',(-9.08440616684122,10.7567454273809,
12.1913888501644));
#124958=CARTESIAN_POINT('Ctrl Pts',(-8.50187923138316,10.8357289870509,
10.8844421261351));
#124959=CARTESIAN_POINT('Ctrl Pts',(-9.27794599298326,10.914712546721,9.68229082475239));
#124960=CARTESIAN_POINT('Ctrl Pts',(-10.7088184575185,10.9936961063911,
9.6751242118605));
#124961=CARTESIAN_POINT('Ctrl Pts',(-11.4968880792509,11.0726796660612,
10.8694414399576));
#124962=CARTESIAN_POINT('Ctrl Pts',(-10.9274818872825,11.1516632257313,
12.1821576918168));
#124963=CARTESIAN_POINT('Ctrl Pts',(-9.51697458168635,11.2306467854014,
12.4228161882874));
#124964=CARTESIAN_POINT('Ctrl Pts',(-8.54450625383342,11.3096303450715,
11.373172095611));
#124965=CARTESIAN_POINT('Ctrl Pts',(-8.89197465529891,11.3886139047415,
9.98511119063623));
#124966=CARTESIAN_POINT('Ctrl Pts',(-10.2442727643307,11.4675974644117,
9.51741769832237));
#124967=CARTESIAN_POINT('Ctrl Pts',(-11.375048381179,11.5465810240817,10.3942266121662));
#124968=CARTESIAN_POINT('Ctrl Pts',(-11.2588403855452,11.6255645837519,
11.8203903638361));
#124969=CARTESIAN_POINT('Ctrl Pts',(-10.0010337419502,11.7045481434219,
12.5025706045647));
#124970=CARTESIAN_POINT('Ctrl Pts',(-8.74228967277683,11.783531703092,11.8221217103547));
#124971=CARTESIAN_POINT('Ctrl Pts',(-8.62411934547226,11.8625152627621,
10.3961192578091));
#124972=CARTESIAN_POINT('Ctrl Pts',(-9.7536875452706,11.9414988224322,9.51775514486607));
#124973=CARTESIAN_POINT('Ctrl Pts',(-11.1066276791042,12.0204823821023,
9.98358767069083));
#124974=CARTESIAN_POINT('Ctrl Pts',(-11.4560061347023,12.0994659417724,
11.3711687469525));
#124975=CARTESIAN_POINT('Ctrl Pts',(-10.4849821701748,12.1784495014425,
12.422150722245));
#124976=CARTESIAN_POINT('Ctrl Pts',(-9.07414668122336,12.2574330611125,
12.1834317813448));
#124977=CARTESIAN_POINT('Ctrl Pts',(-8.50293164322984,12.3364166207826,
10.8715031447629));
#124978=CARTESIAN_POINT('Ctrl Pts',(-9.28936314770077,12.4154001804527,
9.67609714495959));
#124979=CARTESIAN_POINT('Ctrl Pts',(-10.7202326258867,12.4943837401228,
9.68130553299437));
#124980=CARTESIAN_POINT('Ctrl Pts',(-11.4979748617236,12.5733672997929,
10.8823674243165));
#124981=CARTESIAN_POINT('Ctrl Pts',(-10.9172044100689,12.652350859463,12.1901536781328));
#124982=CARTESIAN_POINT('Ctrl Pts',(-9.50475168159853,12.7313344191331,
12.4185397261082));
#124983=CARTESIAN_POINT('Ctrl Pts',(-8.54123315784066,12.8103179788032,
11.3606764849742));
#124984=CARTESIAN_POINT('Ctrl Pts',(-8.90098331506439,12.8893015384733,
9.9753917361545));
#124985=CARTESIAN_POINT('Ctrl Pts',(-10.2566939546601,12.9682850981434,
9.51993655973871));
#124986=CARTESIAN_POINT('Ctrl Pts',(-11.3809710073947,13.0472686578134,
10.4054407605748));
#124987=CARTESIAN_POINT('Ctrl Pts',(-11.2501955957278,13.1262585270511,
11.8327932945507));
#124988=CARTESIAN_POINT('Ctrl Pts',(-10.4109638262168,13.1789205430655,
12.276837950394));
#124989=CARTESIAN_POINT('Ctrl Pts',(-9.9895696048725,13.2052547058564,12.2733784520301));
#124990=CARTESIAN_POINT('Ctrl Pts',(-10.5936512295213,3.54666052661181,
9.76402391512065));
#124991=CARTESIAN_POINT('Ctrl Pts',(-11.0026912982362,3.57299588441898,
9.96047870906769));
#124992=CARTESIAN_POINT('Ctrl Pts',(-11.6034811521994,3.62565909544952,
10.787695890483));
#124993=CARTESIAN_POINT('Ctrl Pts',(-11.0530971859957,3.70465015970341,
12.229580529513));
#124994=CARTESIAN_POINT('Ctrl Pts',(-9.54635903737612,3.78363371937351,
12.5525256844331));
#124995=CARTESIAN_POINT('Ctrl Pts',(-8.45172347996309,3.86261727904359,
11.4693977416606));
#124996=CARTESIAN_POINT('Ctrl Pts',(-8.76079704840517,3.94160083871369,
9.95963121201489));
#124997=CARTESIAN_POINT('Ctrl Pts',(-10.1938527577895,4.02058439838376,
9.39383678605651));
#124998=CARTESIAN_POINT('Ctrl Pts',(-11.4510101744767,4.09956795805386,
10.2843569447999));
#124999=CARTESIAN_POINT('Ctrl Pts',(-11.3923488971039,4.17855151772395,
11.8240037993117));
#125000=CARTESIAN_POINT('Ctrl Pts',(-10.0709876648205,4.25753507739404,
12.6163200110253));
#125001=CARTESIAN_POINT('Ctrl Pts',(-8.68526429131249,4.33651863706412,
11.9428882938621));
#125002=CARTESIAN_POINT('Ctrl Pts',(-8.49182172824476,4.41550219673422,
10.4143648956623));
#125003=CARTESIAN_POINT('Ctrl Pts',(-9.66609748646237,4.49448575640431,
9.41694354442816));
#125004=CARTESIAN_POINT('Ctrl Pts',(-11.143175847286,4.57346931607439,9.8551359558777));
#125005=CARTESIAN_POINT('Ctrl Pts',(-11.5835487698954,4.65245287574449,
11.3315684952565));
#125006=CARTESIAN_POINT('Ctrl Pts',(-10.5878557682048,4.73143643541457,
12.5073116827738));
#125007=CARTESIAN_POINT('Ctrl Pts',(-9.05905706684169,4.81041999508466,
12.3161269804615));
#125008=CARTESIAN_POINT('Ctrl Pts',(-8.38356668743254,4.88940355475475,
10.9313920480199));
#125009=CARTESIAN_POINT('Ctrl Pts',(-9.17396361852812,4.96838711442483,
9.60887548192595));
#125010=CARTESIAN_POINT('Ctrl Pts',(-10.7134642170556,5.04737067409493,
9.54792132639699));
#125011=CARTESIAN_POINT('Ctrl Pts',(-11.6059489155532,5.126354233765,10.8038069444767));
#125012=CARTESIAN_POINT('Ctrl Pts',(-11.042054304502,5.20533779343511,12.2376132032017));
#125013=CARTESIAN_POINT('Ctrl Pts',(-9.5331568396135,5.28432135310519,12.5490710432952));
#125014=CARTESIAN_POINT('Ctrl Pts',(-8.44762322105251,5.36330491277529,
11.4557301440873));
#125015=CARTESIAN_POINT('Ctrl Pts',(-8.76988619261797,5.44228847244537,
9.94910340810924));
#125016=CARTESIAN_POINT('Ctrl Pts',(-10.207696654904,5.52127203211547,9.3954982928687));
#125017=CARTESIAN_POINT('Ctrl Pts',(-11.4571542343291,5.60025559178554,
10.2969600544358));
#125018=CARTESIAN_POINT('Ctrl Pts',(-11.3851692436782,5.67923915145565,
11.8359843263305));
#125019=CARTESIAN_POINT('Ctrl Pts',(-10.0570223713442,5.75822271112572,
12.6168834457166));
#125020=CARTESIAN_POINT('Ctrl Pts',(-8.67716389069992,5.83720627079582,
11.9314871204905));
#125021=CARTESIAN_POINT('Ctrl Pts',(-8.49693953706932,5.9161898304659,10.401357475221));
#125022=CARTESIAN_POINT('Ctrl Pts',(-9.6797885177344,5.995173390136,9.41411594548272));
#125023=CARTESIAN_POINT('Ctrl Pts',(-11.1530261711066,6.07415694980609,
9.86505758892115));
#125024=CARTESIAN_POINT('Ctrl Pts',(-11.5806244331394,6.15314050947617,
11.3452390897421));
#125025=CARTESIAN_POINT('Ctrl Pts',(-10.5748092899862,6.23212406914626,
12.5123352498288));
#125026=CARTESIAN_POINT('Ctrl Pts',(-9.04771956419327,6.31110762881636,
12.3079470934657));
#125027=CARTESIAN_POINT('Ctrl Pts',(-8.38421989405561,6.39009118848643,
10.9174271415028));
#125028=CARTESIAN_POINT('Ctrl Pts',(-9.18601508785768,6.46907474815653,
9.60178964725208));
#125029=CARTESIAN_POINT('Ctrl Pts',(-10.725984929744,6.54805830782661,9.55414056370933));
#125030=CARTESIAN_POINT('Ctrl Pts',(-11.6075842514474,6.62704186749671,
10.8176911899423));
#125031=CARTESIAN_POINT('Ctrl Pts',(-11.0313212450217,6.70602542716679,
12.2465713446463));
#125032=CARTESIAN_POINT('Ctrl Pts',(-9.51978881805855,6.78500898683688,
12.5449792388459));
#125033=CARTESIAN_POINT('Ctrl Pts',(-8.44374323482906,6.86399254650697,
11.4422991166463));
#125034=CARTESIAN_POINT('Ctrl Pts',(-8.77901286496774,6.94297610617706,
9.93851328608784));
#125035=CARTESIAN_POINT('Ctrl Pts',(-10.2215533244214,7.02195966584715,
9.39735289219234));
#125036=CARTESIAN_POINT('Ctrl Pts',(-11.4631747682434,7.10094322551724,
10.3095775023202));
#125037=CARTESIAN_POINT('Ctrl Pts',(-11.3778938290828,7.17992678518733,
11.8479222980334));
#125038=CARTESIAN_POINT('Ctrl Pts',(-10.0430488289575,7.25891034485742,
12.6173158090032));
#125039=CARTESIAN_POINT('Ctrl Pts',(-8.66916434088588,7.3378939045275,11.9200217802622));
#125040=CARTESIAN_POINT('Ctrl Pts',(-8.50216849370914,7.41687746419759,
10.3883919502746));
#125041=CARTESIAN_POINT('Ctrl Pts',(-9.69350402166268,7.49586102386769,
9.41140822015553));
#125042=CARTESIAN_POINT('Ctrl Pts',(-11.1627901081258,7.57484458353777,
9.875063205255));
#125043=CARTESIAN_POINT('Ctrl Pts',(-11.5775822278612,7.65382814320786,
11.3588843017781));
#125044=CARTESIAN_POINT('Ctrl Pts',(-10.5617198127228,7.73281170287795,
12.517245688648));
#125045=CARTESIAN_POINT('Ctrl Pts',(-9.03645320729398,7.81179526254804,
12.2996696526396));
#125046=CARTESIAN_POINT('Ctrl Pts',(-8.38499372532438,7.89077882221813,
10.9034683446493));
#125047=CARTESIAN_POINT('Ctrl Pts',(-9.19812734659141,7.96976238188822,
9.59480824246587));
#125048=CARTESIAN_POINT('Ctrl Pts',(-10.7384514291415,8.04874594155832,
9.56046774453458));
#125049=CARTESIAN_POINT('Ctrl Pts',(-11.6090995561519,8.12772950122838,
10.8315890558243));
#125050=CARTESIAN_POINT('Ctrl Pts',(-11.0205111778215,8.20671306089849,
12.2554364036731));
#125051=CARTESIAN_POINT('Ctrl Pts',(-9.50645665347662,8.28569662056857,
12.5407720768592));
#125052=CARTESIAN_POINT('Ctrl Pts',(-8.43997944991436,8.36468018023866,
11.428835062742));
#125053=CARTESIAN_POINT('Ctrl Pts',(-8.78823070554761,8.44366373990875,
9.92800242316098));
#125054=CARTESIAN_POINT('Ctrl Pts',(-10.2353934509987,8.52264729957884,
9.39932715680145));
#125055=CARTESIAN_POINT('Ctrl Pts',(-11.4690860506765,8.60163085924892,
10.3222465024552));
#125056=CARTESIAN_POINT('Ctrl Pts',(-11.3705155306249,8.68061441891903,
11.8597969574513));
#125057=CARTESIAN_POINT('Ctrl Pts',(-10.0290720722405,8.7595979785891,12.6176274114709));
#125058=CARTESIAN_POINT('Ctrl Pts',(-8.6612641611801,8.83858153825921,11.9084877443233));
#125059=CARTESIAN_POINT('Ctrl Pts',(-8.50750928962575,8.91756509792929,
10.3754720925586));
#125060=CARTESIAN_POINT('Ctrl Pts',(-9.70724241086445,8.99654865759937,
9.40881911093368));
#125061=CARTESIAN_POINT('Ctrl Pts',(-11.1724672225638,9.07553221726946,
9.88515281776378));
#125062=CARTESIAN_POINT('Ctrl Pts',(-11.5744222285264,9.15451577693955,
11.3725027168337));
#125063=CARTESIAN_POINT('Ctrl Pts',(-10.548588393269,9.23349933660964,12.5220428385881));
#125064=CARTESIAN_POINT('Ctrl Pts',(-9.02525879598499,9.31248289627973,
12.2912951687828));
#125065=CARTESIAN_POINT('Ctrl Pts',(-8.38588814500775,9.39146645594982,
10.8895167555695));
#125066=CARTESIAN_POINT('Ctrl Pts',(-9.21029947911844,9.47045001561991,
9.58793175977726));
#125067=CARTESIAN_POINT('Ctrl Pts',(-10.7508627902472,9.54943357529,9.56690241157533));
#125068=CARTESIAN_POINT('Ctrl Pts',(-11.6104947134815,9.62841713496008,
10.8454994965235));
#125069=CARTESIAN_POINT('Ctrl Pts',(-11.009624911645,9.70740069463019,12.264207722454));
#125070=CARTESIAN_POINT('Ctrl Pts',(-9.49316134052218,9.78638425430025,
12.5364498693368));
#125071=CARTESIAN_POINT('Ctrl Pts',(-8.43633214776987,9.86536781397036,
11.4153389888133));
#125072=CARTESIAN_POINT('Ctrl Pts',(-8.79753902586138,9.94435137364043,
9.91757160356907));
#125073=CARTESIAN_POINT('Ctrl Pts',(-10.2492160013451,10.0233349333105,
9.4014209395842));
#125074=CARTESIAN_POINT('Ctrl Pts',(-11.4748876401873,10.1023184929806,
10.3349661087214));
#125075=CARTESIAN_POINT('Ctrl Pts',(-11.363034899255,10.1813020526507,11.8716074180152));
#125076=CARTESIAN_POINT('Ctrl Pts',(-10.0150931447859,10.2602856123208,
12.6178182298103));
#125077=CARTESIAN_POINT('Ctrl Pts',(-8.65346394147736,10.3392691719908,
11.8968858739132));
#125078=CARTESIAN_POINT('Ctrl Pts',(-8.51296152603122,10.4182527316609,
10.3625988667544));
#125079=CARTESIAN_POINT('Ctrl Pts',(-9.72100265953115,10.497236291331,9.40634881114567));
#125080=CARTESIAN_POINT('Ctrl Pts',(-11.1820567918543,10.5762198510011,
9.89532567307804));
#125081=CARTESIAN_POINT('Ctrl Pts',(-11.5711446710833,10.6552034106712,
11.3860933180592));
#125082=CARTESIAN_POINT('Ctrl Pts',(-10.5354160121161,10.7341869703413,
12.5267263414547));
#125083=CARTESIAN_POINT('Ctrl Pts',(-9.01413716612003,10.8131705300114,
12.2828242672015));
#125084=CARTESIAN_POINT('Ctrl Pts',(-8.3869030863307,10.8921540896815,10.8755734159845));
#125085=CARTESIAN_POINT('Ctrl Pts',(-9.22253057655917,10.9711376493516,
9.58116071265196));
#125086=CARTESIAN_POINT('Ctrl Pts',(-10.7632180863699,11.0501212090216,
9.5734440843403));
#125087=CARTESIAN_POINT('Ctrl Pts',(-11.6117696191991,11.1291047686917,
10.8594214734424));
#125088=CARTESIAN_POINT('Ctrl Pts',(-10.9986632594654,11.2080883283618,
12.2728846459425));
#125089=CARTESIAN_POINT('Ctrl Pts',(-9.47990387168526,11.2870718880319,
12.5320129392265));
#125090=CARTESIAN_POINT('Ctrl Pts',(-8.43280160118601,11.366055447702,11.4018119021562));
#125091=CARTESIAN_POINT('Ctrl Pts',(-8.80693713000531,11.4450390073721,
9.90722160696449));
#125092=CARTESIAN_POINT('Ctrl Pts',(-10.2630199450469,11.5240225670421,
9.40363408264815));
#125093=CARTESIAN_POINT('Ctrl Pts',(-11.4805791003575,11.6030061267123,
10.3477353743652));
#125094=CARTESIAN_POINT('Ctrl Pts',(-11.3554524997339,11.6819896863823,
11.8833527921317));
#125095=CARTESIAN_POINT('Ctrl Pts',(-10.0011130784543,11.7609732460524,
12.6178882607918));
#125096=CARTESIAN_POINT('Ctrl Pts',(-8.64576428707628,11.8399568057225,
11.885217014152));
#125097=CARTESIAN_POINT('Ctrl Pts',(-8.51852475188289,11.9189403653926,
10.3497732747195));
#125098=CARTESIAN_POINT('Ctrl Pts',(-9.73478382461175,11.9979239250627,
9.40399742717256));
#125099=CARTESIAN_POINT('Ctrl Pts',(-11.1915579378771,12.0769074847328,
9.90558116156562));
#125100=CARTESIAN_POINT('Ctrl Pts',(-11.5677501115883,12.1558910444029,
11.3996548026714));
#125101=CARTESIAN_POINT('Ctrl Pts',(-10.5222030548419,12.234874604073,12.5312964007194));
#125102=CARTESIAN_POINT('Ctrl Pts',(-9.00309029664685,12.313858163743,12.2742565179095));
#125103=CARTESIAN_POINT('Ctrl Pts',(-8.38803626753834,12.3928417234132,
10.861641407728));
#125104=CARTESIAN_POINT('Ctrl Pts',(-9.23482396266229,12.4718252830832,
9.5744916870518));
#125105=CARTESIAN_POINT('Ctrl Pts',(-10.7755082569308,12.5508088427533,
9.58009980279261));
#125106=CARTESIAN_POINT('Ctrl Pts',(-11.6129398088724,12.6297924024234,
10.8733394872047));
#125107=CARTESIAN_POINT('Ctrl Pts',(-10.987597017597,12.7087759620935,12.2814942995286));
#125108=CARTESIAN_POINT('Ctrl Pts',(-9.46674290174155,12.7877595217636,
12.5274082717744));
#125109=CARTESIAN_POINT('Ctrl Pts',(-8.42927730517822,12.8667430814337,
11.3883572919707));
#125110=CARTESIAN_POINT('Ctrl Pts',(-8.8166371766026,12.9457266411038,9.89675621435035));
#125111=CARTESIAN_POINT('Ctrl Pts',(-10.2763944233962,13.0247102007739,
9.40634625890373));
#125112=CARTESIAN_POINT('Ctrl Pts',(-11.4869562698552,13.1036937604439,
10.3598101740517));
#125113=CARTESIAN_POINT('Ctrl Pts',(-11.3461442489803,13.1826836296816,
11.896707609497));
#125114=CARTESIAN_POINT('Ctrl Pts',(-10.442504031442,13.2353456456961,12.3748313221357));
#125115=CARTESIAN_POINT('Ctrl Pts',(-9.98876910423983,13.261679808487,12.3711063179499));
#125116=CARTESIAN_POINT('Ctrl Pts',(-10.6359647007688,3.60308562924238,
9.67592767960482));
#125117=CARTESIAN_POINT('Ctrl Pts',(-11.074159775531,3.62942098704956,9.88638511325299));
#125118=CARTESIAN_POINT('Ctrl Pts',(-11.7177719179817,3.6820841980801,10.7725635646542));
#125119=CARTESIAN_POINT('Ctrl Pts',(-11.1281584261389,3.76107526233399,
12.3172209112638));
#125120=CARTESIAN_POINT('Ctrl Pts',(-9.51402502899859,3.84005882200409,
12.6631845151446));
#125121=CARTESIAN_POINT('Ctrl Pts',(-8.34136751545742,3.91904238167417,
11.5028548404716));
#125122=CARTESIAN_POINT('Ctrl Pts',(-8.67247081263803,3.99802594134427,
9.88547720944895));
#125123=CARTESIAN_POINT('Ctrl Pts',(-10.2076699330686,4.07700950101435,
9.27935485189655));
#125124=CARTESIAN_POINT('Ctrl Pts',(-11.5544333196575,4.15599306068445,
10.233348304821));
#125125=CARTESIAN_POINT('Ctrl Pts',(-11.4915908629155,4.23497662035453,
11.8827360301843));
#125126=CARTESIAN_POINT('Ctrl Pts',(-10.0760474278007,4.31396018002462,
12.7315258876618));
#125127=CARTESIAN_POINT('Ctrl Pts',(-8.59155433361139,4.39294373969471,
12.010094213311));
#125128=CARTESIAN_POINT('Ctrl Pts',(-8.38432383257039,4.47192729936479,
10.3726227869686));
#125129=CARTESIAN_POINT('Ctrl Pts',(-9.64229803368022,4.5509108590349,9.3041085826105));
#125130=CARTESIAN_POINT('Ctrl Pts',(-11.224657592694,4.62989441870496,9.77353388145369));
#125131=CARTESIAN_POINT('Ctrl Pts',(-11.696418822229,4.70887797837507,11.3552015870332));
#125132=CARTESIAN_POINT('Ctrl Pts',(-10.6297561583812,4.78786153804515,
12.6147478108881));
#125133=CARTESIAN_POINT('Ctrl Pts',(-8.99198980618788,4.86684509771525,
12.4099361033547));
#125134=CARTESIAN_POINT('Ctrl Pts',(-8.26835273504166,4.94582865738532,
10.9265019030003));
#125135=CARTESIAN_POINT('Ctrl Pts',(-9.11508651200717,5.02481221705542,
9.50972078575068));
#125136=CARTESIAN_POINT('Ctrl Pts',(-10.7643175567494,5.10379577672551,
9.44442202217728));
#125137=CARTESIAN_POINT('Ctrl Pts',(-11.7204155752416,5.1827793363956,10.7898229606137));
#125138=CARTESIAN_POINT('Ctrl Pts',(-11.1163284450397,5.26176289606569,
12.3258261270282));
#125139=CARTESIAN_POINT('Ctrl Pts',(-9.4998818227993,5.34074645573578,12.6594836387575));
#125140=CARTESIAN_POINT('Ctrl Pts',(-8.33697500382525,5.41973001540587,
11.488213062322));
#125141=CARTESIAN_POINT('Ctrl Pts',(-8.68220780060687,5.49871357507595,
9.87419901894299));
#125142=CARTESIAN_POINT('Ctrl Pts',(-10.2225005768003,5.57769713474605,
9.28113478534924));
#125143=CARTESIAN_POINT('Ctrl Pts',(-11.5610153075171,5.65668069441612,
10.2468497218984));
#125144=CARTESIAN_POINT('Ctrl Pts',(-11.4838994678413,5.73566425408623,
11.8955704890411));
#125145=CARTESIAN_POINT('Ctrl Pts',(-10.0610867349812,5.8146478137563,12.7321294820906));
#125146=CARTESIAN_POINT('Ctrl Pts',(-8.58287656357489,5.89363137342641,
11.9978804024888));
#125147=CARTESIAN_POINT('Ctrl Pts',(-8.3898064216662,5.97261493309648,10.3586882411655));
#125148=CARTESIAN_POINT('Ctrl Pts',(-9.65696491580419,6.05159849276657,
9.30107944188306));
#125149=CARTESIAN_POINT('Ctrl Pts',(-11.2352100146035,6.13058205243667,
9.78416269526869));
#125150=CARTESIAN_POINT('Ctrl Pts',(-11.693286048544,6.20956561210675,11.369846575705));
#125151=CARTESIAN_POINT('Ctrl Pts',(-10.6157797708933,6.28854917177684,
12.6201294409768));
#125152=CARTESIAN_POINT('Ctrl Pts',(-8.97984420432487,6.36753273144694,
12.4011731814118));
#125153=CARTESIAN_POINT('Ctrl Pts',(-8.26905250004494,6.44651629111701,
10.9115416247212));
#125154=CARTESIAN_POINT('Ctrl Pts',(-9.12799696970499,6.52549985078712,
9.5021298965148));
#125155=CARTESIAN_POINT('Ctrl Pts',(-10.7777307039011,6.60448341045719,
9.4510845458943));
#125156=CARTESIAN_POINT('Ctrl Pts',(-11.7221674724009,6.68346697012729,
10.8046968285918));
#125157=CARTESIAN_POINT('Ctrl Pts',(-11.1048303690294,6.76245052979738,
12.3354227747902));
#125158=CARTESIAN_POINT('Ctrl Pts',(-9.48556097344312,6.84143408946747,
12.6551001841922));
#125159=CARTESIAN_POINT('Ctrl Pts',(-8.33281846517953,6.92041764913755,
11.4738247162312));
#125160=CARTESIAN_POINT('Ctrl Pts',(-8.69198499159258,6.99940120880765,
9.86285406849477));
#125161=CARTESIAN_POINT('Ctrl Pts',(-10.2373449033089,7.07838476847773,
9.28312157430081));
#125162=CARTESIAN_POINT('Ctrl Pts',(-11.5674649649235,7.15736832814783,
10.260366499207));
#125163=CARTESIAN_POINT('Ctrl Pts',(-11.4761054860619,7.2363518878179,11.9083593593815));
#125164=CARTESIAN_POINT('Ctrl Pts',(-10.0461172052965,7.31533544748801,
12.7325926627842));
#125165=CARTESIAN_POINT('Ctrl Pts',(-8.57430683264404,7.39431900715809,
11.9855978512114));
#125166=CARTESIAN_POINT('Ctrl Pts',(-8.39540808082131,7.47330256682818,
10.3447985770281));
#125167=CARTESIAN_POINT('Ctrl Pts',(-9.67165801491334,7.55228612649826,
9.2981787189639));
#125168=CARTESIAN_POINT('Ctrl Pts',(-11.2456698923498,7.63126968616836,
9.7948814784217));
#125169=CARTESIAN_POINT('Ctrl Pts',(-11.6900270050633,7.71025324583844,
11.3844643727514));
#125170=CARTESIAN_POINT('Ctrl Pts',(-10.601757319533,7.78923680550853,12.6253898794279));
#125171=CARTESIAN_POINT('Ctrl Pts',(-8.96777481924168,7.86822036517862,
12.3923057523283));
#125172=CARTESIAN_POINT('Ctrl Pts',(-8.26988148741464,7.94720392484871,
10.896587891582));
#125173=CARTESIAN_POINT('Ctrl Pts',(-9.14097254967212,8.0261874845188,9.49465088057913));
#125174=CARTESIAN_POINT('Ctrl Pts',(-10.7910857736198,8.10517104418889,
9.45786270697637));
#125175=CARTESIAN_POINT('Ctrl Pts',(-11.7237907829494,8.18415460385897,
10.8195852878039));
#125176=CARTESIAN_POINT('Ctrl Pts',(-11.0932497964466,8.26313816352907,
12.3449197055317));
#125177=CARTESIAN_POINT('Ctrl Pts',(-9.47127853682493,8.34212172319915,
12.6505931497907));
#125178=CARTESIAN_POINT('Ctrl Pts',(-8.32878641028264,8.42110528286925,
11.4594009896616));
#125179=CARTESIAN_POINT('Ctrl Pts',(-8.70185984897448,8.50008884253932,
9.85159402646389));
#125180=CARTESIAN_POINT('Ctrl Pts',(-10.2521715077521,8.57907240220943,
9.2852365578786));
#125181=CARTESIAN_POINT('Ctrl Pts',(-11.573797583769,8.65805596187951,10.2739385032375));
#125182=CARTESIAN_POINT('Ctrl Pts',(-11.4682012872031,8.7370395215496,11.9210804047493));
#125183=CARTESIAN_POINT('Ctrl Pts',(-10.031144232175,8.81602308121969,12.732926475232));
#125184=CARTESIAN_POINT('Ctrl Pts',(-8.56584355458991,8.89500664088978,
11.9732417078233));
#125185=CARTESIAN_POINT('Ctrl Pts',(-8.40112955078225,8.97399020055985,
10.3309578351283));
#125186=CARTESIAN_POINT('Ctrl Pts',(-9.68637563048165,9.05297376022996,
9.29540506670874));
#125187=CARTESIAN_POINT('Ctrl Pts',(-11.2560367590921,9.13195731990004,
9.80569024471567));
#125188=CARTESIAN_POINT('Ctrl Pts',(-11.68664177156,9.21094087957014,11.3990534628182));
#125189=CARTESIAN_POINT('Ctrl Pts',(-10.5876899364831,9.28992443924022,
12.6305289541479));
#125190=CARTESIAN_POINT('Ctrl Pts',(-8.95578250778944,9.3689079989103,12.3833343633119));
#125191=CARTESIAN_POINT('Ctrl Pts',(-8.27083965833728,9.44789155858041,
10.8816418799623));
#125192=CARTESIAN_POINT('Ctrl Pts',(-9.15401227103596,9.52687511825048,
9.48728426523676));
#125193=CARTESIAN_POINT('Ctrl Pts',(-10.8043817749742,9.60585867792059,
9.46475601553131));
#125194=CARTESIAN_POINT('Ctrl Pts',(-11.7252853824205,9.68484223759066,
10.8344872181243));
#125195=CARTESIAN_POINT('Ctrl Pts',(-11.0815875936799,9.76382579726076,
12.3543162145363));
#125196=CARTESIAN_POINT('Ctrl Pts',(-9.45703557849479,9.84280935693084,
12.6459628697931));
#125197=CARTESIAN_POINT('Ctrl Pts',(-8.32487914065766,9.92179291660094,
11.4449429607874));
#125198=CARTESIAN_POINT('Ctrl Pts',(-8.71183163518266,10.000776476271,9.84041973298876));
#125199=CARTESIAN_POINT('Ctrl Pts',(-10.2669792831896,10.0797600359411,
9.28747957848513));
#125200=CARTESIAN_POINT('Ctrl Pts',(-11.5800126911482,10.1587435956113,
10.2875647204351));
#125201=CARTESIAN_POINT('Ctrl Pts',(-11.4601874614852,10.2377271552814,
11.933732675384));
#125202=CARTESIAN_POINT('Ctrl Pts',(-10.0161689335928,10.3167107149515,
12.7331308944637));
#125203=CARTESIAN_POINT('Ctrl Pts',(-8.55748736135308,10.3956942746215,
11.9608128949501));
#125204=CARTESIAN_POINT('Ctrl Pts',(-8.4069704043368,10.4746778342916,10.3171670489067));
#125205=CARTESIAN_POINT('Ctrl Pts',(-9.70111666358434,10.5536613939617,
9.29275869222594));
#125206=CARTESIAN_POINT('Ctrl Pts',(-11.266309840762,10.6326449536318,9.81658818708347));
#125207=CARTESIAN_POINT('Ctrl Pts',(-11.6831306008003,10.7116285133019,
11.4136127565782));
#125208=CARTESIAN_POINT('Ctrl Pts',(-10.5735786721218,10.7906120729719,
12.6355462814118));
#125209=CARTESIAN_POINT('Ctrl Pts',(-8.94386816539882,10.8695956326421,
12.3742596842385));
#125210=CARTESIAN_POINT('Ctrl Pts',(-8.27192694127825,10.9485791923122,
10.8667047058338));
#125211=CARTESIAN_POINT('Ctrl Pts',(-9.16711516013507,11.0275627519822,
9.48003060055151));
#125212=CARTESIAN_POINT('Ctrl Pts',(-10.8176177152214,11.1065463116523,
9.4717639568201));
#125213=CARTESIAN_POINT('Ctrl Pts',(-11.7266511591474,11.1855298713225,
10.8494015069271));
#125214=CARTESIAN_POINT('Ctrl Pts',(-11.0698446316482,11.2645134309925,
12.3636116000683));
#125215=CARTESIAN_POINT('Ctrl Pts',(-9.44283316168417,11.3434969906625,
12.6412096901657));
#125216=CARTESIAN_POINT('Ctrl Pts',(-8.3210969485386,11.4224805503327,11.4304517087014));
#125217=CARTESIAN_POINT('Ctrl Pts',(-8.72189960471168,11.5014641100028,
9.82933202329279));
#125218=CARTESIAN_POINT('Ctrl Pts',(-10.2817671257633,11.5804476696729,
9.28985046697391));
#125219=CARTESIAN_POINT('Ctrl Pts',(-11.5861098195362,11.659431229343,10.301244136564));
#125220=CARTESIAN_POINT('Ctrl Pts',(-11.4520646139229,11.7384147890131,
11.9463152204272));
#125221=CARTESIAN_POINT('Ctrl Pts',(-10.0011924149583,11.8173983486832,
12.7332059170188));
#125222=CARTESIAN_POINT('Ctrl Pts',(-8.54923890137574,11.8963819083532,
11.9483123179489));
#125223=CARTESIAN_POINT('Ctrl Pts',(-8.41293015829353,11.9753654680233,
10.3034272916299));
#125224=CARTESIAN_POINT('Ctrl Pts',(-9.71588010395286,12.0543490276934,
9.29023970947901));
#125225=CARTESIAN_POINT('Ctrl Pts',(-11.27648819665,12.1333325873634,9.82757465244043));
#125226=CARTESIAN_POINT('Ctrl Pts',(-11.6794940884743,12.2123161470336,
11.4281408583904));
#125227=CARTESIAN_POINT('Ctrl Pts',(-10.5594239395087,12.2912997067037,
12.6404420791938));
#125228=CARTESIAN_POINT('Ctrl Pts',(-8.9320339120703,12.3702832663738,12.365081254474));
#125229=CARTESIAN_POINT('Ctrl Pts',(-8.27314089184689,12.4492668260438,
10.8517796706932));
#125230=CARTESIAN_POINT('Ctrl Pts',(-9.18028477762376,12.5282503857139,
9.47288622914401));
#125231=CARTESIAN_POINT('Ctrl Pts',(-10.8307838879748,12.607233945384,9.47889407259081));
#125232=CARTESIAN_POINT('Ctrl Pts',(-11.7279047560209,12.6862175050541,
10.8643115500932));
#125233=CARTESIAN_POINT('Ctrl Pts',(-11.057989625125,12.7652010647242,12.3728349209246));
#125234=CARTESIAN_POINT('Ctrl Pts',(-9.42873412188459,12.8441846243943,
12.6362768174407));
#125235=CARTESIAN_POINT('Ctrl Pts',(-8.31732145251579,12.9231681840643,
11.4160380989671));
#125236=CARTESIAN_POINT('Ctrl Pts',(-8.7322910381408,13.0021517437345,9.81812069254618));
#125237=CARTESIAN_POINT('Ctrl Pts',(-10.2960948921322,13.0811353034045,
9.29275595806876));
#125238=CARTESIAN_POINT('Ctrl Pts',(-11.5929415323158,13.1601188630747,
10.3141795875286));
#125239=CARTESIAN_POINT('Ctrl Pts',(-11.4420929022327,13.2391087323122,
11.9606219244432));
#125240=CARTESIAN_POINT('Ctrl Pts',(-10.4740442366673,13.2917707483266,
12.4728246938774));
#125241=CARTESIAN_POINT('Ctrl Pts',(-9.98796860360714,13.3181049111175,
12.4688341838699));
#125242=CARTESIAN_POINT('Ctrl Pts',(-11.2892917767063,13.1491947132283,
10.3057978051142));
#125243=CARTESIAN_POINT('Ctrl Pts',(-11.2911267665574,13.1493279265878,
10.3094867913697));
#125244=CARTESIAN_POINT('Ctrl Pts',(-11.2929458237144,13.149461539121,10.3131836711958));
#125245=CARTESIAN_POINT('Ctrl Pts',(-11.2965564276256,13.1497299497203,
10.320602301492));
#125246=CARTESIAN_POINT('Ctrl Pts',(-11.2983478787435,13.1498647487794,
10.3243240595053));
#125247=CARTESIAN_POINT('Ctrl Pts',(-11.3001231424463,13.15,10.3280535255874));
#125248=CARTESIAN_POINT('',(-10.685566134506,3.59949089696024,11.9587436199823));
#125249=CARTESIAN_POINT('Ctrl Pts',(-10.6861228805008,3.60000000000003,
11.9594385981141));
#125250=CARTESIAN_POINT('Ctrl Pts',(-10.7168289554558,3.60000000000002,
11.9427622376919));
#125251=CARTESIAN_POINT('Ctrl Pts',(-10.7466758757264,3.6,11.9246812723241));
#125252=CARTESIAN_POINT('Ctrl Pts',(-10.7755540070869,3.60000000000001,
11.9052191306961));
#125253=CARTESIAN_POINT('Ctrl Pts',(-10.815638348132,3.60000000000003,11.8782046707663));
#125254=CARTESIAN_POINT('Ctrl Pts',(-10.8538575727216,3.6,11.8485313428333));
#125255=CARTESIAN_POINT('Ctrl Pts',(-10.8901406100634,3.6,11.8164948795181));
#125256=CARTESIAN_POINT('Ctrl Pts',(-10.9070437155787,3.60000000000001,
11.80157011689));
#125257=CARTESIAN_POINT('Ctrl Pts',(-10.9235263388988,3.60000000000003,
11.7861317763512));
#125258=CARTESIAN_POINT('Ctrl Pts',(-10.939579659689,3.60000000000001,11.770206417048));
#125259=CARTESIAN_POINT('Ctrl Pts',(-10.9477051990523,3.6,11.7621456465954));
#125260=CARTESIAN_POINT('Ctrl Pts',(-10.955713805174,3.60000000000001,11.7539669214989));
#125261=CARTESIAN_POINT('Ctrl Pts',(-10.9636034932934,3.60000000000001,
11.7456755575237));
#125262=CARTESIAN_POINT('Ctrl Pts',(-10.9985464304682,3.60000000000002,
11.7089536230065));
#125263=CARTESIAN_POINT('Ctrl Pts',(-11.0311665020199,3.60000000000001,
11.6700183235567));
#125264=CARTESIAN_POINT('Ctrl Pts',(-11.0613843951033,3.59999999999998,
11.6291938939893));
#125265=CARTESIAN_POINT('Ctrl Pts',(-11.0826276826682,3.59999999999997,
11.6004941731127));
#125266=CARTESIAN_POINT('Ctrl Pts',(-11.1026833822258,3.59999999999997,
11.5708596481404));
#125267=CARTESIAN_POINT('Ctrl Pts',(-11.1215156636168,3.6,11.5403900792165));
#125268=CARTESIAN_POINT('Ctrl Pts',(-11.1273432021012,3.60000000000001,
11.5309614506919));
#125269=CARTESIAN_POINT('Ctrl Pts',(-11.1330535344873,3.6,11.5214527959592));
#125270=CARTESIAN_POINT('Ctrl Pts',(-11.1386454384173,3.59999999999999,
11.511866904403));
#125271=CARTESIAN_POINT('Ctrl Pts',(-11.1442677649375,3.59999999999998,
11.5022288610837));
#125272=CARTESIAN_POINT('Ctrl Pts',(-11.1497665524814,3.60000000000002,
11.4925191719262));
#125273=CARTESIAN_POINT('Ctrl Pts',(-11.1551378824765,3.60000000000002,
11.4827468583259));
#125274=CARTESIAN_POINT('Ctrl Pts',(-11.1807420222877,3.60000000000001,
11.4361640410485));
#125275=CARTESIAN_POINT('Ctrl Pts',(-11.2034758957147,3.59999999999998,
11.3881218423073));
#125276=CARTESIAN_POINT('Ctrl Pts',(-11.2232531113551,3.59999999999999,
11.3389605141168));
#125277=CARTESIAN_POINT('Ctrl Pts',(-11.2429220523829,3.6,11.2900683301712));
#125278=CARTESIAN_POINT('Ctrl Pts',(-11.2596672308722,3.59999999999998,
11.2400682143317));
#125279=CARTESIAN_POINT('Ctrl Pts',(-11.2733682251147,3.6,11.18925800081));
#125280=CARTESIAN_POINT('Ctrl Pts',(-11.2813293082148,3.60000000000002,
11.159734279756));
#125281=CARTESIAN_POINT('Ctrl Pts',(-11.2882618783691,3.6,11.1299364359319));
#125282=CARTESIAN_POINT('Ctrl Pts',(-11.2941355108101,3.6,11.0999192215127));
#125283=CARTESIAN_POINT('Ctrl Pts',(-11.297245546931,3.6,11.0840253735351));
#125284=CARTESIAN_POINT('Ctrl Pts',(-11.3000586080087,3.60000000000002,
11.0680699868974));
#125285=CARTESIAN_POINT('Ctrl Pts',(-11.3025695287904,3.60000000000002,
11.0520610063241));
#125286=CARTESIAN_POINT('Ctrl Pts',(-11.3040622829494,3.60000000000001,
11.0425435924308));
#125287=CARTESIAN_POINT('Ctrl Pts',(-11.3054480305648,3.60000000000003,
11.0330079228566));
#125288=CARTESIAN_POINT('Ctrl Pts',(-11.3067241767973,3.60000000000002,
11.0234689901208));
#125289=CARTESIAN_POINT('Ctrl Pts',(-11.3139927404417,3.60000000000001,
10.9691379597692));
#125290=CARTESIAN_POINT('Ctrl Pts',(-11.3177273076128,3.60000000000001,
10.9145922890096));
#125291=CARTESIAN_POINT('Ctrl Pts',(-11.3178159451722,3.60000000000002,
10.8601622391978));
#125292=CARTESIAN_POINT('Ctrl Pts',(-11.3178338810166,3.60000000000002,
10.8491482975715));
#125293=CARTESIAN_POINT('Ctrl Pts',(-11.3177023864676,3.60000000000002,
10.8381390007859));
#125294=CARTESIAN_POINT('Ctrl Pts',(-11.3174203038176,3.60000000000002,
10.8271369643882));
#125295=CARTESIAN_POINT('Ctrl Pts',(-11.3160738601558,3.60000000000002,
10.7746217807255));
#125296=CARTESIAN_POINT('Ctrl Pts',(-11.3113006782232,3.60000000000003,
10.7222726280919));
#125297=CARTESIAN_POINT('Ctrl Pts',(-11.3033023704179,3.60000000000001,
10.6703071156347));
#125298=CARTESIAN_POINT('Ctrl Pts',(-11.2993868268145,3.6,10.6448675808169));
#125299=CARTESIAN_POINT('Ctrl Pts',(-11.2946975676707,3.60000000000001,
10.6195198671649));
#125300=CARTESIAN_POINT('Ctrl Pts',(-11.2892538466151,3.60000000000002,
10.5942892822886));
#125301=CARTESIAN_POINT('Ctrl Pts',(-11.2858213458543,3.60000000000003,
10.5783803110358));
#125302=CARTESIAN_POINT('Ctrl Pts',(-11.2820888261831,3.60000000000004,
10.5625179087665));
#125303=CARTESIAN_POINT('Ctrl Pts',(-11.2780605557296,3.60000000000003,
10.5467084764853));
#125304=CARTESIAN_POINT('Ctrl Pts',(-11.2754395971204,3.60000000000003,
10.5364222089364));
#125305=CARTESIAN_POINT('Ctrl Pts',(-11.2726929981706,3.59999999999998,
10.5261572437755));
#125306=CARTESIAN_POINT('Ctrl Pts',(-11.2698269341424,3.59999999999998,
10.5159323008787));
#125307=CARTESIAN_POINT('Ctrl Pts',(-11.2548712899696,3.59999999999998,
10.4625766862987));
#125308=CARTESIAN_POINT('Ctrl Pts',(-11.2366414727183,3.60000000000002,
10.4102056220908));
#125309=CARTESIAN_POINT('Ctrl Pts',(-11.2153854207654,3.60000000000002,
10.359061853025));
#125310=CARTESIAN_POINT('Ctrl Pts',(-11.1941293688125,3.60000000000001,
10.3079180839592));
#125311=CARTESIAN_POINT('Ctrl Pts',(-11.1698466762124,3.59999999999999,
10.2580006758086));
#125312=CARTESIAN_POINT('Ctrl Pts',(-11.1427321020229,3.59999999999999,
10.2095520946345));
#125313=CARTESIAN_POINT('Ctrl Pts',(-11.1273228069325,3.59999999999999,
10.1820186184011));
#125314=CARTESIAN_POINT('Ctrl Pts',(-11.1109979678583,3.59999999999999,
10.1549595972699));
#125315=CARTESIAN_POINT('Ctrl Pts',(-11.0937864439126,3.60000000000001,
10.1284212693692));
#125316=CARTESIAN_POINT('Ctrl Pts',(-11.082565870655,3.60000000000002,10.111120346262));
#125317=CARTESIAN_POINT('Ctrl Pts',(-11.0709683549836,3.6,10.0940407503956));
#125318=CARTESIAN_POINT('Ctrl Pts',(-11.0590008447151,3.60000000000001,
10.077195802441));
#125319=CARTESIAN_POINT('Ctrl Pts',(-11.0529621175772,3.60000000000001,
10.0686959522577));
#125320=CARTESIAN_POINT('Ctrl Pts',(-11.0468278086681,3.59999999999998,
10.0602540260021));
#125321=CARTESIAN_POINT('Ctrl Pts',(-11.0406031296959,3.59999999999998,
10.0518776796523));
#125322=CARTESIAN_POINT('Ctrl Pts',(-11.0058073901279,3.60000000000001,
10.0050541940683));
#125323=CARTESIAN_POINT('Ctrl Pts',(-10.9683118154454,3.59999999999999,
9.96043766150485));
#125324=CARTESIAN_POINT('Ctrl Pts',(-10.9283466012212,3.59999999999999,
9.91828742617033));
#125325=CARTESIAN_POINT('Ctrl Pts',(-10.8887131736399,3.6,9.87648711727444));
#125326=CARTESIAN_POINT('Ctrl Pts',(-10.8466503825228,3.59999999999998,
9.83711131627027));
#125327=CARTESIAN_POINT('Ctrl Pts',(-10.802335053032,3.59999999999999,9.80042995952269));
#125328=CARTESIAN_POINT('Ctrl Pts',(-10.7583691871941,3.6,9.76403786613083));
#125329=CARTESIAN_POINT('Ctrl Pts',(-10.7121856401227,3.6,9.73029690432086));
#125330=CARTESIAN_POINT('Ctrl Pts',(-10.6639180216976,3.59999999999999,
9.6995022572823));
#125331=CARTESIAN_POINT('Ctrl Pts',(-10.6540348801927,3.59999999999999,
9.69319683215035));
#125332=CARTESIAN_POINT('Ctrl Pts',(-10.6440642465189,3.59999999999999,
9.68701506792451));
#125333=CARTESIAN_POINT('Ctrl Pts',(-10.6340070945752,3.6,9.68095972236314));
#125334=CARTESIAN_POINT('Ctrl Pts',(-10.6850489504522,3.59949089696024,
11.9580203536378));
#125335=CARTESIAN_POINT('Ctrl Pts',(-10.6811863241073,3.5996605979735,11.960782391118));
#125336=CARTESIAN_POINT('Ctrl Pts',(-10.6773069932407,3.59983029898676,
11.963521067824));
#125337=CARTESIAN_POINT('Ctrl Pts',(-10.6734112416282,3.60000000000002,
11.9662361834193));
#125338=CARTESIAN_POINT('Origin',(-10.,3.6,11.));
#125339=CARTESIAN_POINT('',(-9.34313799844363,3.6,9.69219093101808));
#125340=CARTESIAN_POINT('',(-10.,3.6,12.4635));
#125341=CARTESIAN_POINT('Origin',(-10.,3.6,11.));
#125342=CARTESIAN_POINT('Ctrl Pts',(-9.34313799844362,3.6,9.69219093101808));
#125343=CARTESIAN_POINT('Ctrl Pts',(-9.31378869772595,3.6,9.71038023888623));
#125344=CARTESIAN_POINT('Ctrl Pts',(-9.28516938078342,3.6,9.72965705355884));
#125345=CARTESIAN_POINT('Ctrl Pts',(-9.25735011406641,3.6,9.75002500446162));
#125346=CARTESIAN_POINT('Ctrl Pts',(-9.21111763578621,3.59999999999999,
9.78387423770362));
#125347=CARTESIAN_POINT('Ctrl Pts',(-9.16709250398103,3.6,9.82073588839211));
#125348=CARTESIAN_POINT('Ctrl Pts',(-9.12542360544964,3.6,9.86030453606564));
#125349=CARTESIAN_POINT('Ctrl Pts',(-9.10759094978497,3.6,9.87723836666707));
#125350=CARTESIAN_POINT('Ctrl Pts',(-9.09019035914315,3.6,9.89466832777773));
#125351=CARTESIAN_POINT('Ctrl Pts',(-9.07323596058201,3.6,9.91257169240983));
#125352=CARTESIAN_POINT('Ctrl Pts',(-9.06478843089223,3.6,9.92149204447843));
#125353=CARTESIAN_POINT('Ctrl Pts',(-9.05645190942788,3.6,9.93052987853001));
#125354=CARTESIAN_POINT('Ctrl Pts',(-9.04823739289588,3.6,9.93967172435648));
#125355=CARTESIAN_POINT('Ctrl Pts',(-9.00977558014081,3.6,9.98247545614571));
#125356=CARTESIAN_POINT('Ctrl Pts',(-8.9739302059633,3.6,10.0276140624936));
#125357=CARTESIAN_POINT('Ctrl Pts',(-8.94084915684911,3.6,10.0747735565802));
#125358=CARTESIAN_POINT('Ctrl Pts',(-8.91864933328807,3.60000000000001,
10.1064210549512));
#125359=CARTESIAN_POINT('Ctrl Pts',(-8.89769530525791,3.60000000000001,
10.1389792938016));
#125360=CARTESIAN_POINT('Ctrl Pts',(-8.87804422253735,3.6,10.1723576312641));
#125361=CARTESIAN_POINT('Ctrl Pts',(-8.8695068037653,3.6,10.1868588599691));
#125362=CARTESIAN_POINT('Ctrl Pts',(-8.86121544633237,3.59999999999999,
10.2015149048055));
#125363=CARTESIAN_POINT('Ctrl Pts',(-8.8531754732434,3.6,10.2163183978135));
#125364=CARTESIAN_POINT('Ctrl Pts',(-8.84773355435015,3.6,10.2263382582527));
#125365=CARTESIAN_POINT('Ctrl Pts',(-8.8424060011833,3.60000000000001,10.2364274486439));
#125366=CARTESIAN_POINT('Ctrl Pts',(-8.83720228730787,3.60000000000001,
10.2465680467474));
#125367=CARTESIAN_POINT('Ctrl Pts',(-8.8115274595799,3.6,10.2966011799283));
#125368=CARTESIAN_POINT('Ctrl Pts',(-8.78881976750809,3.6,10.3479621763596));
#125369=CARTESIAN_POINT('Ctrl Pts',(-8.7692196109522,3.6,10.4003610263812));
#125370=CARTESIAN_POINT('Ctrl Pts',(-8.75005907739917,3.6,10.4515845929438));
#125371=CARTESIAN_POINT('Ctrl Pts',(-8.7338681007161,3.59999999999999,10.5038010286998));
#125372=CARTESIAN_POINT('Ctrl Pts',(-8.72082637361428,3.6,10.5567452659834));
#125373=CARTESIAN_POINT('Ctrl Pts',(-8.71301454821891,3.6,10.5884581774805));
#125374=CARTESIAN_POINT('Ctrl Pts',(-8.70633357038008,3.6,10.6204322521276));
#125375=CARTESIAN_POINT('Ctrl Pts',(-8.70083101793325,3.6,10.6526092818269));
#125376=CARTESIAN_POINT('Ctrl Pts',(-8.69692474994577,3.6,10.6754517903284));
#125377=CARTESIAN_POINT('Ctrl Pts',(-8.69361250137296,3.6,10.6983965579859));
#125378=CARTESIAN_POINT('Ctrl Pts',(-8.69091346972229,3.6,10.7214220966029));
#125379=CARTESIAN_POINT('Ctrl Pts',(-8.68976274983282,3.6,10.7312389304463));
#125380=CARTESIAN_POINT('Ctrl Pts',(-8.68872362682811,3.6,10.7410704505316));
#125381=CARTESIAN_POINT('Ctrl Pts',(-8.68779870785736,3.6,10.7509006268472));
#125382=CARTESIAN_POINT('Ctrl Pts',(-8.68285750441264,3.6,10.8034164715958));
#125383=CARTESIAN_POINT('Ctrl Pts',(-8.68115878076703,3.6,10.8559970701011));
#125384=CARTESIAN_POINT('Ctrl Pts',(-8.68285927325483,3.6,10.9083968961105));
#125385=CARTESIAN_POINT('Ctrl Pts',(-8.68325479933144,3.6,10.9205848344548));
#125386=CARTESIAN_POINT('Ctrl Pts',(-8.68383444403342,3.6,10.9327629652221));
#125387=CARTESIAN_POINT('Ctrl Pts',(-8.68460058457489,3.6,10.9449281273122));
#125388=CARTESIAN_POINT('Ctrl Pts',(-8.68796860980452,3.6,10.9984073137331));
#125389=CARTESIAN_POINT('Ctrl Pts',(-8.69493710285313,3.6,11.0516377258003));
#125390=CARTESIAN_POINT('Ctrl Pts',(-8.70534580022722,3.6,11.1043362828418));
#125391=CARTESIAN_POINT('Ctrl Pts',(-8.71016328866203,3.6,11.1287269130959));
#125392=CARTESIAN_POINT('Ctrl Pts',(-8.71571837394256,3.6,11.153003280269));
#125393=CARTESIAN_POINT('Ctrl Pts',(-8.72199822947561,3.6,11.1771351721407));
#125394=CARTESIAN_POINT('Ctrl Pts',(-8.72642452861774,3.6,11.1941443169733));
#125395=CARTESIAN_POINT('Ctrl Pts',(-8.73121093312169,3.59999999999999,
11.2110816562522));
#125396=CARTESIAN_POINT('Ctrl Pts',(-8.73635344029319,3.6,11.2279360872153));
#125397=CARTESIAN_POINT('Ctrl Pts',(-8.73934372359225,3.6,11.2377366614767));
#125398=CARTESIAN_POINT('Ctrl Pts',(-8.74245200868552,3.6,11.2475011454469));
#125399=CARTESIAN_POINT('Ctrl Pts',(-8.74567520277798,3.6,11.257222478785));
#125400=CARTESIAN_POINT('Ctrl Pts',(-8.76221595659062,3.60000000000001,
11.3071103157765));
#125401=CARTESIAN_POINT('Ctrl Pts',(-8.78179248474627,3.60000000000001,
11.3559077825822));
#125402=CARTESIAN_POINT('Ctrl Pts',(-8.80423153088837,3.60000000000001,
11.4033561009679));
#125403=CARTESIAN_POINT('Ctrl Pts',(-8.82651895693268,3.60000000000001,
11.4504838122017));
#125404=CARTESIAN_POINT('Ctrl Pts',(-8.85163115351329,3.6,11.49628142762));
#125405=CARTESIAN_POINT('Ctrl Pts',(-8.87943737957251,3.6,11.5404626975772));
#125406=CARTESIAN_POINT('Ctrl Pts',(-8.89337708954315,3.6,11.5626114813793));
#125407=CARTESIAN_POINT('Ctrl Pts',(-8.90799439605087,3.6,11.584353452149));
#125408=CARTESIAN_POINT('Ctrl Pts',(-8.92327560787848,3.60000000000001,
11.6056483791132));
#125409=CARTESIAN_POINT('Ctrl Pts',(-8.9345333635161,3.60000000000001,11.6213364728841));
#125410=CARTESIAN_POINT('Ctrl Pts',(-8.94615148182247,3.60000000000001,
11.6367818819636));
#125411=CARTESIAN_POINT('Ctrl Pts',(-8.95812498707744,3.60000000000001,
11.6519673775081));
#125412=CARTESIAN_POINT('Ctrl Pts',(-8.96391308794098,3.60000000000001,
11.659308183563));
#125413=CARTESIAN_POINT('Ctrl Pts',(-8.96978369044831,3.60000000000002,
11.666587383583));
#125414=CARTESIAN_POINT('Ctrl Pts',(-8.9757278503594,3.60000000000002,11.6737932961742));
#125415=CARTESIAN_POINT('Ctrl Pts',(-9.00764475977342,3.60000000000001,
11.7124851320027));
#125416=CARTESIAN_POINT('Ctrl Pts',(-9.04174097252213,3.59999999999999,
11.7491455050258));
#125417=CARTESIAN_POINT('Ctrl Pts',(-9.07788793671881,3.6,11.7835268528966));
#125418=CARTESIAN_POINT('Ctrl Pts',(-9.11359045273366,3.60000000000001,
11.8174854618767));
#125419=CARTESIAN_POINT('Ctrl Pts',(-9.15129431594974,3.60000000000002,
11.8492213840825));
#125420=CARTESIAN_POINT('Ctrl Pts',(-9.19089957566146,3.60000000000002,
11.8784522451599));
#125421=CARTESIAN_POINT('Ctrl Pts',(-9.23050483537317,3.60000000000001,
11.9076831062372));
#125422=CARTESIAN_POINT('Ctrl Pts',(-9.2720121273675,3.60000000000001,11.9344095961519));
#125423=CARTESIAN_POINT('Ctrl Pts',(-9.31533557546052,3.59999999999998,
11.9582951989184));
#125424=CARTESIAN_POINT('Origin',(-10.,3.6,11.));
#125425=CARTESIAN_POINT('Ctrl Pts',(-9.14642233544205,3.43194259932811,
12.1953167142801));
#125426=CARTESIAN_POINT('Ctrl Pts',(-8.75085549718757,3.45827676171174,
11.9128528384984));
#125427=CARTESIAN_POINT('Ctrl Pts',(-8.26877923968405,3.51093877731875,
10.9295236576293));
#125428=CARTESIAN_POINT('Ctrl Pts',(-9.11444842119196,3.58992864614909,
9.50893498064554));
#125429=CARTESIAN_POINT('Ctrl Pts',(-10.7639040357623,3.66891220581921,
9.44485799761825));
#125430=CARTESIAN_POINT('Ctrl Pts',(-11.7201929573756,3.74789576548928,
10.7889917392604));
#125431=CARTESIAN_POINT('Ctrl Pts',(-11.1167118195198,3.82687932515938,
12.3255613683884));
#125432=CARTESIAN_POINT('Ctrl Pts',(-9.50041245587606,3.90586288482946,
12.6594642560973));
#125433=CARTESIAN_POINT('Ctrl Pts',(-8.33722952194777,3.98484644449956,
11.488748736956));
#125434=CARTESIAN_POINT('Ctrl Pts',(-8.68192527117523,4.06383000416964,
9.87465187282243));
#125435=CARTESIAN_POINT('Ctrl Pts',(-10.2219528997697,4.14281356383973,
9.28117333877804));
#125436=CARTESIAN_POINT('Ctrl Pts',(-11.5606909851596,4.22179712350982,
10.2463977718065));
#125437=CARTESIAN_POINT('Ctrl Pts',(-11.4840968696261,4.3007806831799,11.8950593682192));
#125438=CARTESIAN_POINT('Ctrl Pts',(-10.0616246295418,4.37976424284999,
12.7320115256649));
#125439=CARTESIAN_POINT('Ctrl Pts',(-8.5832683061886,4.45874780252009,11.9982684041319));
#125440=CARTESIAN_POINT('Ctrl Pts',(-8.38969615407199,4.53773136219018,
10.3592273034201));
#125441=CARTESIAN_POINT('Ctrl Pts',(-9.65645294854522,4.61671492186027,
9.30128228688353));
#125442=CARTESIAN_POINT('Ctrl Pts',(-11.2347604701799,4.69569848153035,
9.78384454771434));
#125443=CARTESIAN_POINT('Ctrl Pts',(-11.6933066879699,4.77468204120044,
11.3692963807137));
#125444=CARTESIAN_POINT('Ctrl Pts',(-10.6162518328385,4.85366560087053,
12.6198459283292));
#125445=CARTESIAN_POINT('Ctrl Pts',(-8.9803396151964,4.93264916054061,12.4014135749777));
#125446=CARTESIAN_POINT('Ctrl Pts',(-8.26912197695644,5.01163272021071,
10.9120878594701));
#125447=CARTESIAN_POINT('Ctrl Pts',(-9.12757751269249,5.0906162798808,9.50248664260314));
#125448=CARTESIAN_POINT('Ctrl Pts',(-10.7772027007156,5.16959983955088,
9.45092826629134));
#125449=CARTESIAN_POINT('Ctrl Pts',(-11.7220097524849,5.24858339922098,
10.8041692563782));
#125450=CARTESIAN_POINT('Ctrl Pts',(-11.105185962217,5.32756695889107,12.3350023424395));
#125451=CARTESIAN_POINT('Ctrl Pts',(-9.48610740508019,5.40655051856115,
12.6551681695168));
#125452=CARTESIAN_POINT('Ctrl Pts',(-8.33306019515262,5.48553407823123,
11.4743194644961));
#125453=CARTESIAN_POINT('Ctrl Pts',(-8.69170280350843,5.56451763790132,
9.86332691030806));
#125454=CARTESIAN_POINT('Ctrl Pts',(-10.2367947036762,5.64350119757142,
9.28314370551658));
#125455=CARTESIAN_POINT('Ctrl Pts',(-11.567145710715,5.72248475724152,10.2599178499643));
#125456=CARTESIAN_POINT('Ctrl Pts',(-11.4763066978144,5.80146831691158,
11.9078467940089));
#125457=CARTESIAN_POINT('Ctrl Pts',(-10.0466564110688,5.8804518765817,12.7324810090635));
#125458=CARTESIAN_POINT('Ctrl Pts',(-8.57469504544221,5.95943543625176,
11.9859883640002));
#125459=CARTESIAN_POINT('Ctrl Pts',(-8.39529324394348,6.03841899592188,
10.3453371138528));
#125460=CARTESIAN_POINT('Ctrl Pts',(-9.67114426993458,6.11740255559194,
9.29837689947444));
#125461=CARTESIAN_POINT('Ctrl Pts',(-11.2452231367503,6.19638611526205,
9.79455957959906));
#125462=CARTESIAN_POINT('Ctrl Pts',(-11.6900523859804,6.27536967493214,
11.3839143134568));
#125463=CARTESIAN_POINT('Ctrl Pts',(-10.6022318198948,6.35435323460221,
12.6251104893337));
#125464=CARTESIAN_POINT('Ctrl Pts',(-8.96826813114866,6.43333679427231,
12.3925504006075));
#125465=CARTESIAN_POINT('Ctrl Pts',(-8.26994624343055,6.5123203539424,10.8971347152067));
#125466=CARTESIAN_POINT('Ctrl Pts',(-9.14055002481499,6.59130391361249,
9.49500398419459));
#125467=CARTESIAN_POINT('Ctrl Pts',(-10.7905591410088,6.67028747328258,
9.45770187317659));
#125468=CARTESIAN_POINT('Ctrl Pts',(-11.7236376274101,6.74927103295267,
10.8190563711763));
#125469=CARTESIAN_POINT('Ctrl Pts',(-11.0936090094188,6.82825459262274,
12.3445023621971));
#125470=CARTESIAN_POINT('Ctrl Pts',(-9.47182436053907,6.90723815229285,
12.6506658539255));
#125471=CARTESIAN_POINT('Ctrl Pts',(-8.32902385616829,6.98622171196293,
11.4598978084107));
#125472=CARTESIAN_POINT('Ctrl Pts',(-8.70157358560417,7.06520527163302,
9.8520644121577));
#125473=CARTESIAN_POINT('Ctrl Pts',(-10.2516211374348,7.14418883130311,
9.2852539340673));
#125474=CARTESIAN_POINT('Ctrl Pts',(-11.5734822182317,7.2231723909732,10.273487112059));
#125475=CARTESIAN_POINT('Ctrl Pts',(-11.4684069204993,7.3021559506433,11.9205695971871));
#125476=CARTESIAN_POINT('Ctrl Pts',(-10.0316843826099,7.38113951031337,
12.7328194849246));
#125477=CARTESIAN_POINT('Ctrl Pts',(-8.56622837849275,7.46012306998348,
11.9736355605647));
#125478=CARTESIAN_POINT('Ctrl Pts',(-8.40101006472008,7.53910662965354,
10.3314953595456));
#125479=CARTESIAN_POINT('Ctrl Pts',(-9.68586019221467,7.61809018932364,
9.29559880057533));
#125480=CARTESIAN_POINT('Ctrl Pts',(-11.2555928016841,7.69707374899373,
9.80536449751617));
#125481=CARTESIAN_POINT('Ctrl Pts',(-11.686671904566,7.77605730866382,11.398503643375));
#125482=CARTESIAN_POINT('Ctrl Pts',(-10.5881668333267,7.8550408683339,12.6302536746195));
#125483=CARTESIAN_POINT('Ctrl Pts',(-8.95627368728507,7.93402442800401,
12.3835832651425));
#125484=CARTESIAN_POINT('Ctrl Pts',(-8.27089968685849,8.01300798767408,
10.8821892427257));
#125485=CARTESIAN_POINT('Ctrl Pts',(-9.1535867108016,8.09199154734418,9.4876337046522));
#125486=CARTESIAN_POINT('Ctrl Pts',(-10.8038565517817,8.17097510701427,
9.46459063712853));
#125487=CARTESIAN_POINT('Ctrl Pts',(-11.7251368029427,8.24995866668436,
10.8339569978334));
#125488=CARTESIAN_POINT('Ctrl Pts',(-11.0819503994852,8.32894222635443,
12.3539019907251));
#125489=CARTESIAN_POINT('Ctrl Pts',(-9.45758075359829,8.40792578602454,
12.6460402876506));
#125490=CARTESIAN_POINT('Ctrl Pts',(-8.32511228469123,8.48690934569461,
11.4454418127471));
#125491=CARTESIAN_POINT('Ctrl Pts',(-8.71154131791904,8.56589290536471,
9.8408876275331));
#125492=CARTESIAN_POINT('Ctrl Pts',(-10.2664287832729,8.64487646503479,
9.28749219830115));
#125493=CARTESIAN_POINT('Ctrl Pts',(-11.5797012378345,8.7238600247049,10.28711062105));
#125494=CARTESIAN_POINT('Ctrl Pts',(-11.4603975009684,8.80284358437497,
11.9332236637597));
#125495=CARTESIAN_POINT('Ctrl Pts',(-10.0167099883599,8.88182714404506,
12.7330285755649));
#125496=CARTESIAN_POINT('Ctrl Pts',(-8.55786876762613,8.96081070371516,
11.9612100582326));
#125497=CARTESIAN_POINT('Ctrl Pts',(-8.40684627801222,9.03979426338524,
10.3177035207829));
#125498=CARTESIAN_POINT('Ctrl Pts',(-9.70059957051577,9.11877782305534,
9.29294796498165));
#125499=CARTESIAN_POINT('Ctrl Pts',(-11.2658687146942,9.19776138272542,
9.81625861583101));
#125500=CARTESIAN_POINT('Ctrl Pts',(-11.6831654836466,9.27674494239552,
11.4130632180386));
#125501=CARTESIAN_POINT('Ctrl Pts',(-10.5740579298357,9.3557285020656,12.6352751330062));
#125502=CARTESIAN_POINT('Ctrl Pts',(-8.94435717581294,9.43471206173569,
12.3745128210308));
#125503=CARTESIAN_POINT('Ctrl Pts',(-8.27198223781284,9.51369562140577,
10.8672525668748));
#125504=CARTESIAN_POINT('Ctrl Pts',(-9.16668659631767,9.59267918107587,
9.48037634965791));
#125505=CARTESIAN_POINT('Ctrl Pts',(-10.8170939406285,9.67166274074595,
9.47159404619589));
#125506=CARTESIAN_POINT('Ctrl Pts',(-11.7265071668941,9.75064630041605,
10.8488700224994));
#125507=CARTESIAN_POINT('Ctrl Pts',(-11.0702110030647,9.82962986008613,
12.363200526832));
#125508=CARTESIAN_POINT('Ctrl Pts',(-9.44337764772432,9.90861341975623,
12.64129181573));
#125509=CARTESIAN_POINT('Ctrl Pts',(-8.32132577282368,9.98759697942632,
11.4309525570752));
#125510=CARTESIAN_POINT('Ctrl Pts',(-8.72160525616959,10.0665805390964,
9.82979739088376));
#125511=CARTESIAN_POINT('Ctrl Pts',(-10.2812165355508,10.1455640987665,
9.28985833114085));
#125512=CARTESIAN_POINT('Ctrl Pts',(-11.5858023051603,10.2245476584366,
10.3007873596792));
#125513=CARTESIAN_POINT('Ctrl Pts',(-11.4522790372668,10.3035312181067,
11.945808048893));
#125514=CARTESIAN_POINT('Ctrl Pts',(-10.0017343464181,10.3825147777768,
12.7331082653652));
#125515=CARTESIAN_POINT('Ctrl Pts',(-8.54961683703311,10.4614983374469,
11.9487127847886));
#125516=CARTESIAN_POINT('Ctrl Pts',(-8.41280144804587,10.540481897117,10.3039626273635));
#125517=CARTESIAN_POINT('Ctrl Pts',(-9.71536130428307,10.6194654567871,
9.29042459062748));
#125518=CARTESIAN_POINT('Ctrl Pts',(-11.2760501085098,10.6984490164571,
9.82724112110314));
#125519=CARTESIAN_POINT('Ctrl Pts',(-11.6795333850265,10.7774325761272,
11.4275919503285));
#125520=CARTESIAN_POINT('Ctrl Pts',(-10.5599061629194,10.8564161357973,
12.6401744895403));
#125521=CARTESIAN_POINT('Ctrl Pts',(-8.93251948646677,10.9353996954674,
12.3653397455663));
#125522=CARTESIAN_POINT('Ctrl Pts',(-8.27319381554146,11.0143832551375,
10.8523258028859));
#125523=CARTESIAN_POINT('Ctrl Pts',(-9.17984870307604,11.0933668148076,
9.47323246119838));
#125524=CARTESIAN_POINT('Ctrl Pts',(-10.8302703194389,11.1723503744777,
9.47871157726292));
#125525=CARTESIAN_POINT('Ctrl Pts',(-11.7277486163822,11.2513339341478,
10.8637943320196));
#125526=CARTESIAN_POINT('Ctrl Pts',(-11.0583916977844,11.3303174938179,
12.3723972755227));
#125527=CARTESIAN_POINT('Ctrl Pts',(-9.42921610136029,11.4093010534879,
12.6364207940589));
#125528=CARTESIAN_POINT('Ctrl Pts',(-8.31766460726359,11.488284613158,11.4164311207011));
#125529=CARTESIAN_POINT('Ctrl Pts',(-8.73176464128558,11.5672681728281,
9.81879453522508));
#125530=CARTESIAN_POINT('Ctrl Pts',(-10.2959833047406,11.6462517324982,
9.29235214643519));
#125531=CARTESIAN_POINT('Ctrl Pts',(-11.5917849365506,11.7252352921683,
10.314516324941));
#125532=CARTESIAN_POINT('Ctrl Pts',(-11.444052189557,11.8042188518384,11.9583217779886));
#125533=CARTESIAN_POINT('Ctrl Pts',(-9.98675847132022,11.8832024115085,
12.7330586155007));
#125534=CARTESIAN_POINT('Ctrl Pts',(-8.5414734019267,11.9621859711786,11.936144544465));
#125535=CARTESIAN_POINT('Ctrl Pts',(-8.41887474788645,12.0411695308487,
10.2902739528369));
#125536=CARTESIAN_POINT('Ctrl Pts',(-9.7301450254167,12.1201530905188,9.28802839053024));
#125537=CARTESIAN_POINT('Ctrl Pts',(-11.2861348131133,12.1991366501888,
9.83831210624346));
#125538=CARTESIAN_POINT('Ctrl Pts',(-11.6757785872691,12.2781202098589,
11.4420870022078));
#125539=CARTESIAN_POINT('Ctrl Pts',(-10.5457073900601,12.357103769529,12.6449547452531));
#125540=CARTESIAN_POINT('Ctrl Pts',(-8.92077148761818,12.4360873291991,
12.3560582580058));
#125541=CARTESIAN_POINT('Ctrl Pts',(-8.27451515546233,12.5150708888692,
10.8374224819375));
#125542=CARTESIAN_POINT('Ctrl Pts',(-9.19310887025665,12.5940544485393,
9.46617872771973));
#125543=CARTESIAN_POINT('Ctrl Pts',(-10.8433139901639,12.6730380082094,
9.48598849228214));
#125544=CARTESIAN_POINT('Ctrl Pts',(-11.7289968730589,12.7520215678794,
10.8786408546047));
#125545=CARTESIAN_POINT('Ctrl Pts',(-11.0462324066889,12.8310051275496,
12.381660612415));
#125546=CARTESIAN_POINT('Ctrl Pts',(-9.41559963367022,12.9099886872196,
12.6311015404504));
#125547=CARTESIAN_POINT('Ctrl Pts',(-8.31315199305088,12.9889722468897,
11.4025174432538));
#125548=CARTESIAN_POINT('Ctrl Pts',(-8.74406409137945,13.0679662885069,
9.80632444093873));
#125549=CARTESIAN_POINT('Ctrl Pts',(-9.78568267619791,13.1206324769007,
9.46773891403626));
#125550=CARTESIAN_POINT('Ctrl Pts',(-10.263911338604,13.1469708120712,9.55510288757666));
#125551=CARTESIAN_POINT('Ctrl Pts',(-9.20320175027983,3.48835183995636,
12.1158050466245));
#125552=CARTESIAN_POINT('Ctrl Pts',(-8.83394775330262,3.51468600234,11.8521304787705));
#125553=CARTESIAN_POINT('Ctrl Pts',(-8.38393888573301,3.567348017947,10.934211696745));
#125554=CARTESIAN_POINT('Ctrl Pts',(-9.17335471940146,3.64633788677736,
9.60811962757268));
#125555=CARTESIAN_POINT('Ctrl Pts',(-10.7130896506819,3.72532144644745,
9.54830500256142));
#125556=CARTESIAN_POINT('Ctrl Pts',(-11.6057668733959,3.80430500611754,
10.8030278675101));
#125557=CARTESIAN_POINT('Ctrl Pts',(-11.0424288968432,3.88328856578762,
12.2373859135307));
#125558=CARTESIAN_POINT('Ctrl Pts',(-9.5336446848734,3.96227212545772,12.5490778046731));
#125559=CARTESIAN_POINT('Ctrl Pts',(-8.44783590104305,4.0412556851278,11.4562374981555));
#125560=CARTESIAN_POINT('Ctrl Pts',(-8.76960271978085,4.1202392447979,9.949509276903));
#125561=CARTESIAN_POINT('Ctrl Pts',(-10.2071887414586,4.19922280446798,
9.39550853765221));
#125562=CARTESIAN_POINT('Ctrl Pts',(-11.4568748655967,4.27820636413808,
10.2965268875437));
#125563=CARTESIAN_POINT('Ctrl Pts',(-11.3853757393542,4.35718992380815,
11.8355206182229));
#125564=CARTESIAN_POINT('Ctrl Pts',(-10.0575254004378,4.43617348347826,
12.6167992784344));
#125565=CARTESIAN_POINT('Ctrl Pts',(-8.67750835006137,4.51515704314833,
11.9318642581576));
#125566=CARTESIAN_POINT('Ctrl Pts',(-8.49681248792099,4.59414060281844,
10.4018510742455));
#125567=CARTESIAN_POINT('Ctrl Pts',(-9.67930546842809,4.67312416248851,
9.41427985199122));
#125568=CARTESIAN_POINT('Ctrl Pts',(-11.1526250302863,4.75210772215862,
9.86474239427214));
#125569=CARTESIAN_POINT('Ctrl Pts',(-11.5806690606327,4.83109128182869,
11.3447310326858));
#125570=CARTESIAN_POINT('Ctrl Pts',(-10.5752591734542,4.91007484149879,
12.5120948615465));
#125571=CARTESIAN_POINT('Ctrl Pts',(-9.04816674140454,4.98905840116887,
12.3081924821154));
#125572=CARTESIAN_POINT('Ctrl Pts',(-8.38425882435147,5.06804196083896,
10.9179357162072));
#125573=CARTESIAN_POINT('Ctrl Pts',(-9.18561047252433,5.14702552050905,
9.60210022866015));
#125574=CARTESIAN_POINT('Ctrl Pts',(-10.7255036973451,5.22600908017914,
9.55397148102599));
#125575=CARTESIAN_POINT('Ctrl Pts',(-11.6074628165108,5.30499263984923,
10.8171957863493));
#125576=CARTESIAN_POINT('Ctrl Pts',(-11.0316697318524,5.38397619951932,
12.2461988803081));
#125577=CARTESIAN_POINT('Ctrl Pts',(-9.52029119648024,5.46295975918941,
12.545067490896));
#125578=CARTESIAN_POINT('Ctrl Pts',(-8.44394391507526,5.54194331885949,
11.4427680512404));
#125579=CARTESIAN_POINT('Ctrl Pts',(-8.77872985720856,5.62092687852959,
9.93893764331382));
#125580=CARTESIAN_POINT('Ctrl Pts',(-10.2210432785046,5.69991043819968,
9.39734783691432));
#125581=CARTESIAN_POINT('Ctrl Pts',(-11.4629002271292,5.77889399786976,
10.3091476191532));
#125582=CARTESIAN_POINT('Ctrl Pts',(-11.3781037645566,5.85787755753985,
11.8474574330094));
#125583=CARTESIAN_POINT('Ctrl Pts',(-10.0435528578375,5.93686111720994,
12.6172375321114));
#125584=CARTESIAN_POINT('Ctrl Pts',(-8.66950537688066,6.01584467688004,
11.9204010780749));
#125585=CARTESIAN_POINT('Ctrl Pts',(-8.50203726312108,6.09482823655011,
10.3888848507898));
#125586=CARTESIAN_POINT('Ctrl Pts',(-9.69301953295339,6.17381179622021,
9.41156772900764));
#125587=CARTESIAN_POINT('Ctrl Pts',(-11.1623917272807,6.25279535589029,
9.87474466940886));
#125588=CARTESIAN_POINT('Ctrl Pts',(-11.577631232633,6.33177891556039,11.3583765903286));
#125589=CARTESIAN_POINT('Ctrl Pts',(-10.5621717623862,6.41076247523047,
12.5170092274773));
#125590=CARTESIAN_POINT('Ctrl Pts',(-9.03689824439466,6.48974603490056,
12.2999188801709));
#125591=CARTESIAN_POINT('Ctrl Pts',(-8.38502826117153,6.56872959457065,
10.9039772450903));
#125592=CARTESIAN_POINT('Ctrl Pts',(-9.1977200618246,6.64771315424074,9.59511531167981));
#125593=CARTESIAN_POINT('Ctrl Pts',(-10.7379716761712,6.72669671391083,
9.56029451211568));
#125594=CARTESIAN_POINT('Ctrl Pts',(-11.6089824062857,6.80568027358092,
10.8310926202371));
#125595=CARTESIAN_POINT('Ctrl Pts',(-11.0208628702045,6.88466383325101,
12.2550669651111));
#125596=CARTESIAN_POINT('Ctrl Pts',(-9.50695825050053,6.96364739292109,
12.5408646663239));
#125597=CARTESIAN_POINT('Ctrl Pts',(-8.44017607065814,7.04263095259119,
11.4293057140636));
#125598=CARTESIAN_POINT('Ctrl Pts',(-8.78794404148706,7.12161451226127,
9.92842431900101));
#125599=CARTESIAN_POINT('Ctrl Pts',(-10.2348834678149,7.20059807193137,
9.39931769447449));
#125600=CARTESIAN_POINT('Ctrl Pts',(-11.4688152344077,7.27958163160145,
10.321814263017));
#125601=CARTESIAN_POINT('Ctrl Pts',(-11.3707294751401,7.35856519127155,
11.8593339238371));
#125602=CARTESIAN_POINT('Ctrl Pts',(-10.029576758689,7.43754875094163,12.6175534927849));
#125603=CARTESIAN_POINT('Ctrl Pts',(-8.66160190694888,7.51653231061172,
11.9088699748546));
#125604=CARTESIAN_POINT('Ctrl Pts',(-8.50737380480662,7.59551587028181,
10.375963840713));
#125605=CARTESIAN_POINT('Ctrl Pts',(-9.70675656193467,7.67449942995189,
9.40897442738754));
#125606=CARTESIAN_POINT('Ctrl Pts',(-11.1720716090448,7.75348298962199,
9.88483085141924));
#125607=CARTESIAN_POINT('Ctrl Pts',(-11.5744756185794,7.83246654929207,
11.3719954477872));
#125608=CARTESIAN_POINT('Ctrl Pts',(-10.549042369309,7.91145010896217,12.5218102915208));
#125609=CARTESIAN_POINT('Ctrl Pts',(-9.02570166290748,7.99043366863225,
12.2915482325542));
#125610=CARTESIAN_POINT('Ctrl Pts',(-8.38591828218086,8.06941722830234,
10.8900259354338));
#125611=CARTESIAN_POINT('Ctrl Pts',(-9.20988955618653,8.14840078797243,
9.58823529819872));
#125612=CARTESIAN_POINT('Ctrl Pts',(-10.7503845520812,8.22738434764252,
9.56672504010109));
#125613=CARTESIAN_POINT('Ctrl Pts',(-11.6103818576654,8.30636790731261,
10.8450020671837));
#125614=CARTESIAN_POINT('Ctrl Pts',(-11.0099797831991,8.38535146698271,
12.2638413366418));
#125615=CARTESIAN_POINT('Ctrl Pts',(-9.49366211875843,8.46433502665278,
12.5365467896212));
#125616=CARTESIAN_POINT('Ctrl Pts',(-8.43652469429721,8.54331858632288,
11.4158113215543));
#125617=CARTESIAN_POINT('Ctrl Pts',(-8.79724872692107,8.62230214599295,
9.91799100660755));
#125618=CARTESIAN_POINT('Ctrl Pts',(-10.2487061189644,8.70128570566306,
9.40140707086987));
#125619=CARTESIAN_POINT('Ctrl Pts',(-11.4746205689897,8.78026926533314,
10.3345315453099));
#125620=CARTESIAN_POINT('Ctrl Pts',(-11.3632528368346,8.85925282500323,
11.8711462503722));
#125621=CARTESIAN_POINT('Ctrl Pts',(-10.0155984511203,8.93823638467332,
12.6177486748559));
#125622=CARTESIAN_POINT('Ctrl Pts',(-8.65379837180093,9.01721994434341,
11.8972710086197));
#125623=CARTESIAN_POINT('Ctrl Pts',(-8.51282179709749,9.0962035040135,10.3630894258321));
#125624=CARTESIAN_POINT('Ctrl Pts',(-9.72051548665811,9.17518706368359,
9.40649992360301));
#125625=CARTESIAN_POINT('Ctrl Pts',(-11.1816639752003,9.25417062335368,
9.89500030027658));
#125626=CARTESIAN_POINT('Ctrl Pts',(-11.5712024424322,9.33315418302377,
11.3855865292906));
#125627=CARTESIAN_POINT('Ctrl Pts',(-10.5358719806333,9.41213774269386,
12.5264977258571));
#125628=CARTESIAN_POINT('Ctrl Pts',(-9.01457782980123,9.49112130236393,
12.2830811483128));
#125629=CARTESIAN_POINT('Ctrl Pts',(-8.38692882257045,9.57010486203404,
10.8760828372614));
#125630=CARTESIAN_POINT('Ctrl Pts',(-9.22211804608748,9.64908842170412,
9.58146069760038));
#125631=CARTESIAN_POINT('Ctrl Pts',(-10.7627413986833,9.72807198137422,
9.57326258708555));
#125632=CARTESIAN_POINT('Ctrl Pts',(-11.611661065924,9.80705554104429,10.8589230874321));
#125633=CARTESIAN_POINT('Ctrl Pts',(-10.9990212835699,9.8860391007144,12.2725213403514));
#125634=CARTESIAN_POINT('Ctrl Pts',(-9.4804037939792,9.96502266038446,12.5321141828741));
#125635=CARTESIAN_POINT('Ctrl Pts',(-8.43299005866429,10.0440062200546,
11.4022858814703));
#125636=CARTESIAN_POINT('Ctrl Pts',(-8.80664321873624,10.1229897797246,
9.90763848507602));
#125637=CARTESIAN_POINT('Ctrl Pts',(-10.2625101998601,10.2019733393947,
9.40361581013704));
#125638=CARTESIAN_POINT('Ctrl Pts',(-11.4803157974012,10.2809568990648,
10.3472985164411));
#125639=CARTESIAN_POINT('Ctrl Pts',(-11.3556744079037,10.3599404587349,
11.8828935306307));
#125640=CARTESIAN_POINT('Ctrl Pts',(-10.0016189788554,10.438924018405,12.6178230637439));
#125641=CARTESIAN_POINT('Ctrl Pts',(-8.64609535410689,10.5179075780751,
11.885605045439));
#125642=CARTESIAN_POINT('Ctrl Pts',(-8.51838083320707,10.5968911377452,
10.3502625674444));
#125643=CARTESIAN_POINT('Ctrl Pts',(-9.73429527977711,10.6758746974153,
9.40414440242168));
#125644=CARTESIAN_POINT('Ctrl Pts',(-11.1911681095151,10.7548582570854,
9.90525225664998));
#125645=CARTESIAN_POINT('Ctrl Pts',(-11.5678119485809,10.8338418167554,
11.3991488200345));
#125646=CARTESIAN_POINT('Ctrl Pts',(-10.5226615797786,10.9128253764255,
12.5310711804745));
#125647=CARTESIAN_POINT('Ctrl Pts',(-9.00352757562587,10.9918089360956,
12.2745182596877));
#125648=CARTESIAN_POINT('Ctrl Pts',(-8.38805980695961,11.0707924957657,
10.8621489916208));
#125649=CARTESIAN_POINT('Ctrl Pts',(-9.23440461831537,11.1497760554358,
9.57479201581885));
#125650=CARTESIAN_POINT('Ctrl Pts',(-10.7750412935959,11.2287596151059,
9.57990666475067));
#125651=CARTESIAN_POINT('Ctrl Pts',(-11.6128199350233,11.307743174776,10.8728546418738));
#125652=CARTESIAN_POINT('Ctrl Pts',(-10.9879881905645,11.3867267344461,
12.2811063274758));
#125653=CARTESIAN_POINT('Ctrl Pts',(-9.46718426419918,11.4657102941162,
12.5275671783037));
#125654=CARTESIAN_POINT('Ctrl Pts',(-8.42957243138638,11.5446938537862,
11.3887304013226));
#125655=CARTESIAN_POINT('Ctrl Pts',(-8.81612680835525,11.6236774134563,
9.89736753201015));
#125656=CARTESIAN_POINT('Ctrl Pts',(-10.2762946934488,11.7026609731264,
9.40594373850743));
#125657=CARTESIAN_POINT('Ctrl Pts',(-11.4859004681562,11.7816445327965,
10.3601142401241));
#125658=CARTESIAN_POINT('Ctrl Pts',(-11.3479948045963,11.8606280924666,
11.8945748548441));
#125659=CARTESIAN_POINT('Ctrl Pts',(-9.98763928894373,11.9396116521367,
12.6177767165552));
#125660=CARTESIAN_POINT('Ctrl Pts',(-8.63849361485231,12.0185952118068,
11.8738728360483));
#125661=CARTESIAN_POINT('Ctrl Pts',(-8.52405014120789,12.0975787714769,
10.3374844543838));
#125662=CARTESIAN_POINT('Ctrl Pts',(-9.74809559767757,12.176562331147,9.40190759595083));
#125663=CARTESIAN_POINT('Ctrl Pts',(-11.2005819863195,12.2555458908171,
9.91558680727001));
#125664=CARTESIAN_POINT('Ctrl Pts',(-11.5643069174567,12.3345294504871,
11.4126796707663));
#125665=CARTESIAN_POINT('Ctrl Pts',(-10.509407299785,12.4135130101572,12.5355334567773));
#125666=CARTESIAN_POINT('Ctrl Pts',(-8.99256104579626,12.4924965698273,
12.2658541704664));
#125667=CARTESIAN_POINT('Ctrl Pts',(-8.38929325223351,12.5714801294974,
10.8482370296052));
#125668=CARTESIAN_POINT('Ctrl Pts',(-9.24678272805185,12.6504636891675,
9.56820749196923));
#125669=CARTESIAN_POINT('Ctrl Pts',(-10.7872173080761,12.7294472488376,
9.58669952425418));
#125670=CARTESIAN_POINT('Ctrl Pts',(-11.6139851585015,12.8084308085077,
10.8867135837151));
#125671=CARTESIAN_POINT('Ctrl Pts',(-10.9766377273729,12.8874143681777,
12.2897534733992));
#125672=CARTESIAN_POINT('Ctrl Pts',(-9.45447355482463,12.9663979278479,
12.5226017578842));
#125673=CARTESIAN_POINT('Ctrl Pts',(-8.42535999325021,13.0453814875179,
11.375742252385));
#125674=CARTESIAN_POINT('Ctrl Pts',(-8.82760810726251,13.1243755291351,
9.8857269400479));
#125675=CARTESIAN_POINT('Ctrl Pts',(-9.79993892110727,13.177041717529,9.56966389573644));
#125676=CARTESIAN_POINT('Ctrl Pts',(-10.2463561330297,13.2033800526994,
9.65121647624079));
#125677=CARTESIAN_POINT('Ctrl Pts',(-9.25998116511762,3.54476108058462,
12.0362933789687));
#125678=CARTESIAN_POINT('Ctrl Pts',(-8.91704000941767,3.57109524296825,
11.7914081190427));
#125679=CARTESIAN_POINT('Ctrl Pts',(-8.49909853178196,3.62375725857524,
10.9388997358606));
#125680=CARTESIAN_POINT('Ctrl Pts',(-9.23226101761095,3.7027471274056,9.70730427449976));
#125681=CARTESIAN_POINT('Ctrl Pts',(-10.6622752656016,3.7817306870757,9.65175200750462));
#125682=CARTESIAN_POINT('Ctrl Pts',(-11.4913407894162,3.86071424674578,
10.8170639957596));
#125683=CARTESIAN_POINT('Ctrl Pts',(-10.9681459741666,3.93969780641587,
12.1492104586732));
#125684=CARTESIAN_POINT('Ctrl Pts',(-9.56687691387072,4.01868136608596,
12.4386913532491));
#125685=CARTESIAN_POINT('Ctrl Pts',(-8.55844228013835,4.09766492575605,
11.4237262593553));
#125686=CARTESIAN_POINT('Ctrl Pts',(-8.85728016838641,4.17664848542614,
10.0243666809836));
#125687=CARTESIAN_POINT('Ctrl Pts',(-10.1924245831472,4.25563204509622,
9.50984373652637));
#125688=CARTESIAN_POINT('Ctrl Pts',(-11.3530587460338,4.33461560476632,
10.3466560032809));
#125689=CARTESIAN_POINT('Ctrl Pts',(-11.2866546090824,4.4135991644364,11.7759818682266));
#125690=CARTESIAN_POINT('Ctrl Pts',(-10.053426171334,4.49258272410649,12.5015870312037));
#125691=CARTESIAN_POINT('Ctrl Pts',(-8.77174839393416,4.57156628377659,
11.8654601121833));
#125692=CARTESIAN_POINT('Ctrl Pts',(-8.60392882177002,4.65054984344667,
10.4444748450709));
#125693=CARTESIAN_POINT('Ctrl Pts',(-9.70215798831091,4.72953340311676,
9.52727741709888));
#125694=CARTESIAN_POINT('Ctrl Pts',(-11.070489590393,4.80851696278685,9.94564024082997));
#125695=CARTESIAN_POINT('Ctrl Pts',(-11.4680314332955,4.88750052245693,
11.3201656846581));
#125696=CARTESIAN_POINT('Ctrl Pts',(-10.5342665140699,4.96648408212703,
12.4043437947639));
#125697=CARTESIAN_POINT('Ctrl Pts',(-9.11599386761268,5.04546764179711,
12.214971389253));
#125698=CARTESIAN_POINT('Ctrl Pts',(-8.49939567174651,5.12445120146722,
10.9237835729444));
#125699=CARTESIAN_POINT('Ctrl Pts',(-9.2436434323562,5.20343476113729,9.70171381471713));
#125700=CARTESIAN_POINT('Ctrl Pts',(-10.6738046939746,5.28241832080739,
9.65701469576066));
#125701=CARTESIAN_POINT('Ctrl Pts',(-11.4929158805367,5.36140188047747,
10.8302223163206));
#125702=CARTESIAN_POINT('Ctrl Pts',(-10.958153501488,5.44038544014756,12.1573954181767));
#125703=CARTESIAN_POINT('Ctrl Pts',(-9.55447498788032,5.51936899981765,
12.4349668122754));
#125704=CARTESIAN_POINT('Ctrl Pts',(-8.5548276349979,5.59835255948773,11.4112166379848));
#125705=CARTESIAN_POINT('Ctrl Pts',(-8.86575691090871,5.67733611915783,
10.0145483763196));
#125706=CARTESIAN_POINT('Ctrl Pts',(-10.2052918533331,5.75631967882791,
9.51155196831206));
#125707=CARTESIAN_POINT('Ctrl Pts',(-11.3586547435432,5.83530323849801,
10.3583773883419));
#125708=CARTESIAN_POINT('Ctrl Pts',(-11.2799008312987,5.91428679816809,
11.7870680720098));
#125709=CARTESIAN_POINT('Ctrl Pts',(-10.0404493046063,5.99327035783819,
12.5019940551594));
#125710=CARTESIAN_POINT('Ctrl Pts',(-8.76431570831911,6.07225391750827,
11.8548137921496));
#125711=CARTESIAN_POINT('Ctrl Pts',(-8.60878128229869,6.15123747717835,
10.4324325877267));
#125712=CARTESIAN_POINT('Ctrl Pts',(-9.71489479597219,6.23022103684846,
9.52475855854082));
#125713=CARTESIAN_POINT('Ctrl Pts',(-11.079560317811,6.30920459651853,9.95492975921862));
#125714=CARTESIAN_POINT('Ctrl Pts',(-11.4652100792857,6.38818815618863,
11.3328388672004));
#125715=CARTESIAN_POINT('Ctrl Pts',(-10.5221117048774,6.46717171585871,
12.408907965621));
#125716=CARTESIAN_POINT('Ctrl Pts',(-9.10552835764069,6.54615527552881,
12.2072873597345));
#125717=CARTESIAN_POINT('Ctrl Pts',(-8.50011027891247,6.6251388351989,10.9108197749738));
#125718=CARTESIAN_POINT('Ctrl Pts',(-9.25489009883425,6.70412239486898,
9.69522663916505));
#125719=CARTESIAN_POINT('Ctrl Pts',(-10.6853842113335,6.78310595453907,
9.66288715105476));
#125720=CARTESIAN_POINT('Ctrl Pts',(-11.4943271851612,6.86208951420916,
10.8431288692977));
#125721=CARTESIAN_POINT('Ctrl Pts',(-10.9481167309902,6.94107307387926,
12.1656315680248));
#125722=CARTESIAN_POINT('Ctrl Pts',(-9.54209214046203,7.02005663354933,
12.4310634787225));
#125723=CARTESIAN_POINT('Ctrl Pts',(-8.55132828514797,7.09904019321943,
11.3987136197164));
#125724=CARTESIAN_POINT('Ctrl Pts',(-8.87431449736998,7.17802375288952,
10.0047842258442));
#125725=CARTESIAN_POINT('Ctrl Pts',(-10.2181457981948,7.2570073125596,9.51338145488168));
#125726=CARTESIAN_POINT('Ctrl Pts',(-11.3641482505836,7.3359908722297,10.3701414139749));
#125727=CARTESIAN_POINT('Ctrl Pts',(-11.2730520297809,7.41497443189978,
11.798098250487));
#125728=CARTESIAN_POINT('Ctrl Pts',(-10.0274691347682,7.49395799156988,
12.5022875006452));
#125729=CARTESIAN_POINT('Ctrl Pts',(-8.75697543540498,7.57294155123996,
11.8441043891445));
#125730=CARTESIAN_POINT('Ctrl Pts',(-8.61373754489317,7.65192511091005,
10.4204323218805));
#125731=CARTESIAN_POINT('Ctrl Pts',(-9.72765293165465,7.73090867058014,
9.52235005419975));
#125732=CARTESIAN_POINT('Ctrl Pts',(-11.0885504164055,7.80989223025023,
9.96429720532229));
#125733=CARTESIAN_POINT('Ctrl Pts',(-11.4622793325926,7.88887578992031,
11.3454872521992));
#125734=CARTESIAN_POINT('Ctrl Pts',(-10.5099179052913,7.96785934959041,
12.4133669084223));
#125735=CARTESIAN_POINT('Ctrl Pts',(-9.09512963852988,8.04684290926049,
12.199513199966));
#125736=CARTESIAN_POINT('Ctrl Pts',(-8.50093687750326,8.12582646893058,
10.8978626281419));
#125737=CARTESIAN_POINT('Ctrl Pts',(-9.26619240157147,8.20481002860068,
9.68883689174524));
#125738=CARTESIAN_POINT('Ctrl Pts',(-10.6969125523805,8.28379358827076,
9.66885944307361));
#125739=CARTESIAN_POINT('Ctrl Pts',(-11.4956269123882,8.36277714794085,
10.856047136534));
#125740=CARTESIAN_POINT('Ctrl Pts',(-10.938009166913,8.44176070761094,12.1737806825583));
#125741=CARTESIAN_POINT('Ctrl Pts',(-9.52974348391854,8.52074426728103,
12.4270532915916));
#125742=CARTESIAN_POINT('Ctrl Pts',(-8.54793710390317,8.59972782695112,
11.3861808303615));
#125743=CARTESIAN_POINT('Ctrl Pts',(-8.88295613592307,8.67871138662121,
9.99509438568203));
#125744=CARTESIAN_POINT('Ctrl Pts',(-10.2309834546559,8.7576949462913,9.51532194343859));
#125745=CARTESIAN_POINT('Ctrl Pts',(-11.3695399001448,8.83667850596138,
10.3819524695695));
#125746=CARTESIAN_POINT('Ctrl Pts',(-11.2661081727008,8.91566206563147,
11.8090688369849));
#125747=CARTESIAN_POINT('Ctrl Pts',(-10.0144869138808,8.99464562530156,
12.5024687741467));
#125748=CARTESIAN_POINT('Ctrl Pts',(-8.74972797597572,9.07362918497165,
11.8333319590067));
#125749=CARTESIAN_POINT('Ctrl Pts',(-8.61879731618278,9.15261274464173,
10.4084753308814));
#125750=CARTESIAN_POINT('Ctrl Pts',(-9.74043140280046,9.23159630431184,
9.52005188222438));
#125751=CARTESIAN_POINT('Ctrl Pts',(-11.0974592357066,9.31057986398191,
9.97374198472214));
#125752=CARTESIAN_POINT('Ctrl Pts',(-11.4592394012177,9.38956342365202,
11.3581098405426));
#125753=CARTESIAN_POINT('Ctrl Pts',(-10.4976860314311,9.46854698332209,
12.4177203187083));
#125754=CARTESIAN_POINT('Ctrl Pts',(-9.08479848378951,9.5475305429922,12.191649475595));
#125755=CARTESIAN_POINT('Ctrl Pts',(-8.50187540732805,9.62651410266227,
10.8849131076482));
#125756=CARTESIAN_POINT('Ctrl Pts',(-9.27754949585731,9.70549766233236,
9.68254504554283));
#125757=CARTESIAN_POINT('Ctrl Pts',(-10.708388856738,9.78448122200245,9.67493112797522));
#125758=CARTESIAN_POINT('Ctrl Pts',(-11.4968149649541,9.86346478167254,
10.8689761523649));
#125759=CARTESIAN_POINT('Ctrl Pts',(-10.9278315640749,9.94244834134262,
12.1818421538707));
#125760=CARTESIAN_POINT('Ctrl Pts',(-9.51742994023411,10.0214319010127,
12.422936550018));
#125761=CARTESIAN_POINT('Ctrl Pts',(-8.54465434450489,10.1004154606828,
11.3736192058652));
#125762=CARTESIAN_POINT('Ctrl Pts',(-8.89168118130291,10.1793990203529,
9.98547957926833));
#125763=CARTESIAN_POINT('Ctrl Pts',(-10.2438038641694,10.2583825800229,
9.5173732891332));
#125764=CARTESIAN_POINT('Ctrl Pts',(-11.374829289642,10.337366139693,10.3938096732028));
#125765=CARTESIAN_POINT('Ctrl Pts',(-11.2590697785407,10.4163496993631,
11.8199790123686));
#125766=CARTESIAN_POINT('Ctrl Pts',(-10.0015036112926,10.4953332590332,
12.5025378621227));
#125767=CARTESIAN_POINT('Ctrl Pts',(-8.74257387118066,10.5743168187033,
11.8224973060896));
#125768=CARTESIAN_POINT('Ctrl Pts',(-8.62396021836827,10.6533003783734,
10.3965625075255));
#125769=CARTESIAN_POINT('Ctrl Pts',(-9.75322925527118,10.7322839380435,
9.51786421421587));
#125770=CARTESIAN_POINT('Ctrl Pts',(-11.1062861105205,10.8112674977136,
9.98326339219686));
#125771=CARTESIAN_POINT('Ctrl Pts',(-11.4560905121352,10.8902510573837,
11.3707056897407));
#125772=CARTESIAN_POINT('Ctrl Pts',(-10.4854169966381,10.9692346170537,
12.4219678714086));
#125773=CARTESIAN_POINT('Ctrl Pts',(-9.07453566478498,11.0482181767238,
12.183696773809));
#125774=CARTESIAN_POINT('Ctrl Pts',(-8.50292579837776,11.1272017363939,
10.8719721803556));
#125775=CARTESIAN_POINT('Ctrl Pts',(-9.28896053355473,11.206185296064,9.67635157043933));
#125776=CARTESIAN_POINT('Ctrl Pts',(-10.7198122677529,11.2851688557341,
9.68110175223841));
#125777=CARTESIAN_POINT('Ctrl Pts',(-11.4978912536645,11.3641524154042,
10.881914951728));
#125778=CARTESIAN_POINT('Ctrl Pts',(-10.9175846833448,11.4431359750743,
12.1898153794288));
#125779=CARTESIAN_POINT('Ctrl Pts',(-9.50515242703808,11.5221195347444,
12.4187135625483));
#125780=CARTESIAN_POINT('Ctrl Pts',(-8.54148025550917,11.6011030944145,
11.3610296819441));
#125781=CARTESIAN_POINT('Ctrl Pts',(-8.900488975425,11.6800866540846,9.97594052879524));
#125782=CARTESIAN_POINT('Ctrl Pts',(-10.2566060821569,11.7590702137546,
9.51953533057963));
#125783=CARTESIAN_POINT('Ctrl Pts',(-11.3800159997619,11.8380537734247,
10.4057121553073));
#125784=CARTESIAN_POINT('Ctrl Pts',(-11.2519374196356,11.9170373330948,
11.8308279316994));
#125785=CARTESIAN_POINT('Ctrl Pts',(-9.98852010656727,11.9960208927649,
12.5024948176097));
#125786=CARTESIAN_POINT('Ctrl Pts',(-8.73551382777791,12.075004452435,11.8116011276316));
#125787=CARTESIAN_POINT('Ctrl Pts',(-8.62922553452934,12.1539880121051,
10.3846949559309));
#125788=CARTESIAN_POINT('Ctrl Pts',(-9.76604616993845,12.2329715717752,
9.51578680137141));
#125789=CARTESIAN_POINT('Ctrl Pts',(-11.1150291595255,12.3119551314453,
9.99286150829657));
#125790=CARTESIAN_POINT('Ctrl Pts',(-11.4528352476442,12.3909386911153,
11.3832723393248));
#125791=CARTESIAN_POINT('Ctrl Pts',(-10.4731072095099,12.4699222507854,
12.4261121683014));
#125792=CARTESIAN_POINT('Ctrl Pts',(-9.06435060397434,12.5489058104555,
12.1756500829267));
#125793=CARTESIAN_POINT('Ctrl Pts',(-8.50407134900466,12.6278893701256,
10.8590515772727));
#125794=CARTESIAN_POINT('Ctrl Pts',(-9.30045658584705,12.7068729297957,
9.67023625621872));
#125795=CARTESIAN_POINT('Ctrl Pts',(-10.7311206259883,12.7858564894658,
9.68741055622625));
#125796=CARTESIAN_POINT('Ctrl Pts',(-11.4989734439442,12.8648400491359,
10.8947863128256));
#125797=CARTESIAN_POINT('Ctrl Pts',(-10.907043048057,12.943823608806,12.1978463343832));
#125798=CARTESIAN_POINT('Ctrl Pts',(-9.49334747597901,13.022807168476,12.4141019753182));
#125799=CARTESIAN_POINT('Ctrl Pts',(-8.53756799344957,13.1017907281462,
11.3489670615161));
#125800=CARTESIAN_POINT('Ctrl Pts',(-8.91115212314558,13.1807847697633,
9.96512943915707));
#125801=CARTESIAN_POINT('Ctrl Pts',(-9.81419516601662,13.2334509581573,
9.67158887743661));
#125802=CARTESIAN_POINT('Ctrl Pts',(-10.2288009274554,13.2597892933277,
9.74733006490493));
#125803=CARTESIAN_POINT('Ctrl Pts',(-9.31676057995541,3.60117032121287,
11.956781711313));
#125804=CARTESIAN_POINT('Ctrl Pts',(-9.00013226553272,3.6275044835965,11.7306857593148));
#125805=CARTESIAN_POINT('Ctrl Pts',(-8.61425817783089,3.6801664992035,10.9435877749763));
#125806=CARTESIAN_POINT('Ctrl Pts',(-9.29116731582048,3.75915636803385,
9.80648892142689));
#125807=CARTESIAN_POINT('Ctrl Pts',(-10.6114608805213,3.83813992770395,
9.75519901244778));
#125808=CARTESIAN_POINT('Ctrl Pts',(-11.3769147054366,3.91712348737403,
10.8311001240093));
#125809=CARTESIAN_POINT('Ctrl Pts',(-10.8938630514901,3.99610704704413,
12.0610350038155));
#125810=CARTESIAN_POINT('Ctrl Pts',(-9.60010914286806,4.07509060671421,
12.3283049018249));
#125811=CARTESIAN_POINT('Ctrl Pts',(-8.66904865923364,4.1540741663843,11.3912150205549));
#125812=CARTESIAN_POINT('Ctrl Pts',(-8.94495761699203,4.23305772605439,
10.0992240850642));
#125813=CARTESIAN_POINT('Ctrl Pts',(-10.1776604248361,4.31204128572447,
9.62417893540055));
#125814=CARTESIAN_POINT('Ctrl Pts',(-11.2492426264709,4.39102484539457,
10.3967851190181));
#125815=CARTESIAN_POINT('Ctrl Pts',(-11.1879334788104,4.47000840506465,
11.7164431182301));
#125816=CARTESIAN_POINT('Ctrl Pts',(-10.0493269422301,4.54899196473475,
12.3863747839732));
#125817=CARTESIAN_POINT('Ctrl Pts',(-8.86598843780693,4.62797552440483,
11.7990559662091));
#125818=CARTESIAN_POINT('Ctrl Pts',(-8.71104515561903,4.70695908407493,
10.4870986158965));
#125819=CARTESIAN_POINT('Ctrl Pts',(-9.72501050819376,4.78594264374501,
9.64027498220657));
#125820=CARTESIAN_POINT('Ctrl Pts',(-10.9883541504996,4.8649262034151,10.0265380873878));
#125821=CARTESIAN_POINT('Ctrl Pts',(-11.3553938059582,4.94390976308519,
11.2956003366303));
#125822=CARTESIAN_POINT('Ctrl Pts',(-10.4932738546855,5.02289332275529,
12.2965927279814));
#125823=CARTESIAN_POINT('Ctrl Pts',(-9.18382099382081,5.10187688242537,
12.1217502963907));
#125824=CARTESIAN_POINT('Ctrl Pts',(-8.61453251914156,5.18086044209545,
10.9296314296816));
#125825=CARTESIAN_POINT('Ctrl Pts',(-9.30167639218805,5.25984400176556,
9.80132740077414));
#125826=CARTESIAN_POINT('Ctrl Pts',(-10.6221056906041,5.33882756143563,
9.7600579104953));
#125827=CARTESIAN_POINT('Ctrl Pts',(-11.3783689445625,5.41781112110573,
10.8432488462917));
#125828=CARTESIAN_POINT('Ctrl Pts',(-10.8846372711235,5.49679468077581,
12.0685919560453));
#125829=CARTESIAN_POINT('Ctrl Pts',(-9.5886587792804,5.5757782404459,12.3248661336547));
#125830=CARTESIAN_POINT('Ctrl Pts',(-8.66571135492052,5.65476180011599,
11.3796652247291));
#125831=CARTESIAN_POINT('Ctrl Pts',(-8.95278396460887,5.73374535978609,
10.0901591093253));
#125832=CARTESIAN_POINT('Ctrl Pts',(-10.1895404281615,5.81272891945616,
9.6257560997098));
#125833=CARTESIAN_POINT('Ctrl Pts',(-11.2544092599574,5.89171247912627,
10.4076071575309));
#125834=CARTESIAN_POINT('Ctrl Pts',(-11.1816978980407,5.97069603879634,
11.7266787110101));
#125835=CARTESIAN_POINT('Ctrl Pts',(-10.0373457513751,6.04967959846644,
12.3867505782075));
#125836=CARTESIAN_POINT('Ctrl Pts',(-8.85912603975755,6.12866315813652,
11.7892265062243));
#125837=CARTESIAN_POINT('Ctrl Pts',(-8.71552530147632,6.20764671780661,
10.4759803246637));
#125838=CARTESIAN_POINT('Ctrl Pts',(-9.73677005899099,6.28663027747671,
9.63794938807401));
#125839=CARTESIAN_POINT('Ctrl Pts',(-10.9967289083413,6.36561383714679,
10.0351148490284));
#125840=CARTESIAN_POINT('Ctrl Pts',(-11.3527889259383,6.44459739681688,
11.3073011440721));
#125841=CARTESIAN_POINT('Ctrl Pts',(-10.4820516473687,6.52358095648697,
12.3008067037646));
#125842=CARTESIAN_POINT('Ctrl Pts',(-9.17415847088668,6.60256451615705,
12.114655839298));
#125843=CARTESIAN_POINT('Ctrl Pts',(-8.61519229665345,6.68154807582715,
10.9176623048574));
#125844=CARTESIAN_POINT('Ctrl Pts',(-9.31206013584387,6.76053163549724,
9.79533796665029));
#125845=CARTESIAN_POINT('Ctrl Pts',(-10.6327967464959,6.83951519516732,
9.76547978999385));
#125846=CARTESIAN_POINT('Ctrl Pts',(-11.3796719640369,6.91849875483742,
10.8551651183584));
#125847=CARTESIAN_POINT('Ctrl Pts',(-10.8753705917758,6.99748231450749,
12.0761961709388));
#125848=CARTESIAN_POINT('Ctrl Pts',(-9.5772260304235,7.0764658741776,12.3212622911209));
#125849=CARTESIAN_POINT('Ctrl Pts',(-8.66248049963781,7.15544943384768,
11.3681215253693));
#125850=CARTESIAN_POINT('Ctrl Pts',(-8.96068495325288,7.23443299351777,
10.0811441326875));
#125851=CARTESIAN_POINT('Ctrl Pts',(-10.2014081285749,7.31341655318785,
9.6274452152889));
#125852=CARTESIAN_POINT('Ctrl Pts',(-11.2594812667594,7.39240011285795,
10.4184685649329));
#125853=CARTESIAN_POINT('Ctrl Pts',(-11.1753745844216,7.47138367252803,
11.7368625771371));
#125854=CARTESIAN_POINT('Ctrl Pts',(-10.0253615108474,7.55036723219812,
12.3870215085055));
#125855=CARTESIAN_POINT('Ctrl Pts',(-8.85234896386109,7.62935079186821,
11.7793388034344));
#125856=CARTESIAN_POINT('Ctrl Pts',(-8.72010128497971,7.70833435153831,
10.4649008030479));
#125857=CARTESIAN_POINT('Ctrl Pts',(-9.74854930137463,7.78731791120839,
9.63572568101198));
#125858=CARTESIAN_POINT('Ctrl Pts',(-11.0050292237662,7.86630147087847,
10.0437635592253));
#125859=CARTESIAN_POINT('Ctrl Pts',(-11.3500830466059,7.94528503054858,
11.3189790566114));
#125860=CARTESIAN_POINT('Ctrl Pts',(-10.4707934412737,8.02426859021864,
12.3049235253236));
#125861=CARTESIAN_POINT('Ctrl Pts',(-9.16455761415227,8.10325214988876,
12.1074781673778));
#125862=CARTESIAN_POINT('Ctrl Pts',(-8.61595547282566,8.18223570955883,
10.90569932085));
#125863=CARTESIAN_POINT('Ctrl Pts',(-9.32249524695637,8.26121926922893,
9.78943848529178));
#125864=CARTESIAN_POINT('Ctrl Pts',(-10.6434405526799,8.34020282889902,
9.77099384604614));
#125865=CARTESIAN_POINT('Ctrl Pts',(-11.3808719671109,8.4191863885691,10.8670922058844));
#125866=CARTESIAN_POINT('Ctrl Pts',(-10.8660385506269,8.49816994823921,
12.0837200284748));
#125867=CARTESIAN_POINT('Ctrl Pts',(-9.56582484907866,8.57715350790928,
12.3175597935623));
#125868=CARTESIAN_POINT('Ctrl Pts',(-8.65934951350916,8.65613706757937,
11.3565503391687));
#125869=CARTESIAN_POINT('Ctrl Pts',(-8.96866354492507,8.73512062724947,
10.0721977647565));
#125870=CARTESIAN_POINT('Ctrl Pts',(-10.2132607903475,8.81410418691954,
9.62923681600733));
#125871=CARTESIAN_POINT('Ctrl Pts',(-11.2644592313,8.89308774658964,10.4293733938294));
#125872=CARTESIAN_POINT('Ctrl Pts',(-11.168963508567,8.97207130625972,11.7469914235974));
#125873=CARTESIAN_POINT('Ctrl Pts',(-10.0133753766411,9.05105486592982,
12.3871888734376));
#125874=CARTESIAN_POINT('Ctrl Pts',(-8.84565758015053,9.1300384255999,11.7693929093938));
#125875=CARTESIAN_POINT('Ctrl Pts',(-8.72477283526805,9.20902198526999,
10.4538612359307));
#125876=CARTESIAN_POINT('Ctrl Pts',(-9.76034731894279,9.28800554494009,
9.63360384084576));
#125877=CARTESIAN_POINT('Ctrl Pts',(-11.0132544962128,9.36698910461016,
10.0524836691677));
#125878=CARTESIAN_POINT('Ctrl Pts',(-11.3472763600032,9.44597266428026,
11.3306331517947));
#125879=CARTESIAN_POINT('Ctrl Pts',(-10.4595000822287,9.52495622395034,
12.3089429115593));
#125880=CARTESIAN_POINT('Ctrl Pts',(-9.1550191377778,9.60393978362044,12.1002178028771));
#125881=CARTESIAN_POINT('Ctrl Pts',(-8.61682199208564,9.68292334329052,
10.8937433780347));
#125882=CARTESIAN_POINT('Ctrl Pts',(-9.33298094562714,9.76190690296061,
9.78362939348532));
#125883=CARTESIAN_POINT('Ctrl Pts',(-10.6540363147928,9.84089046263071,
9.77659966886485));
#125884=CARTESIAN_POINT('Ctrl Pts',(-11.3819688639842,9.91987402230078,
10.8790292172976));
#125885=CARTESIAN_POINT('Ctrl Pts',(-10.85664184458,9.99885758197089,12.0911629673903));
#125886=CARTESIAN_POINT('Ctrl Pts',(-9.55445608648902,10.077841141641,12.313758917162));
#125887=CARTESIAN_POINT('Ctrl Pts',(-8.65631863034551,10.1568247013111,
11.3449525302601));
#125888=CARTESIAN_POINT('Ctrl Pts',(-8.97671914386957,10.2358082609812,
10.0633206734606));
#125889=CARTESIAN_POINT('Ctrl Pts',(-10.2250975284787,10.3147918206513,
9.63113076812937));
#125890=CARTESIAN_POINT('Ctrl Pts',(-11.2693427818829,10.3937753803214,
10.4403208299646));
#125891=CARTESIAN_POINT('Ctrl Pts',(-11.1624651491776,10.4727589399914,
11.7570644941064));
#125892=CARTESIAN_POINT('Ctrl Pts',(-10.00138824373,10.5517424996615,12.3872526605013));
#125893=CARTESIAN_POINT('Ctrl Pts',(-8.83905238825443,10.6307260593316,
11.7593895667401));
#125894=CARTESIAN_POINT('Ctrl Pts',(-8.72953960352947,10.7097096190017,
10.4428624476065));
#125895=CARTESIAN_POINT('Ctrl Pts',(-9.77216323076523,10.7886931786718,
9.63158402601005));
#125896=CARTESIAN_POINT('Ctrl Pts',(-11.0214041115258,10.8676767383419,
10.0612745277437));
#125897=CARTESIAN_POINT('Ctrl Pts',(-11.3443690756895,10.946660298012,11.3422625594467));
#125898=CARTESIAN_POINT('Ctrl Pts',(-10.4481724134973,11.0256438576821,
12.3128645623428));
#125899=CARTESIAN_POINT('Ctrl Pts',(-9.1455437539441,11.1046274173521,12.0928752879302));
#125900=CARTESIAN_POINT('Ctrl Pts',(-8.61779178979594,11.1836109770222,
10.8817953690904));
#125901=CARTESIAN_POINT('Ctrl Pts',(-9.34351644879403,11.2625945366923,
9.7779111250598));
#125902=CARTESIAN_POINT('Ctrl Pts',(-10.6645832419098,11.3415780963624,
9.78229683972616));
#125903=CARTESIAN_POINT('Ctrl Pts',(-11.3829625723056,11.4205616560325,
10.8909752615822));
#125904=CARTESIAN_POINT('Ctrl Pts',(-10.8471811761249,11.4995452157026,
12.0985244313819));
#125905=CARTESIAN_POINT('Ctrl Pts',(-9.54312058987698,11.5785287753727,
12.3098599467931));
#125906=CARTESIAN_POINT('Ctrl Pts',(-8.65338807963194,11.6575123350428,
11.3333289625656));
#125907=CARTESIAN_POINT('Ctrl Pts',(-8.98485114249471,11.7364958947129,
10.0545135255803));
#125908=CARTESIAN_POINT('Ctrl Pts',(-10.236917470865,11.8154794543829,9.63312692265186));
#125909=CARTESIAN_POINT('Ctrl Pts',(-11.2741315313676,11.894463014053,10.4513100704904));
#125910=CARTESIAN_POINT('Ctrl Pts',(-11.1558800346749,11.9734465737231,
11.7670810085549));
#125911=CARTESIAN_POINT('Ctrl Pts',(-9.98940092419077,12.0524301333932,
12.387212918664));
#125912=CARTESIAN_POINT('Ctrl Pts',(-8.83253404070354,12.1314136930633,
11.749329419215));
#125913=CARTESIAN_POINT('Ctrl Pts',(-8.73440092785076,12.2103972527334,
10.4319054574778));
#125914=CARTESIAN_POINT('Ctrl Pts',(-9.78399674219934,12.2893808124035,
9.62966600679198));
#125915=CARTESIAN_POINT('Ctrl Pts',(-11.0294763327316,12.3683643720736,
10.0701362093231));
#125916=CARTESIAN_POINT('Ctrl Pts',(-11.3413635778319,12.4473479317437,
11.3538650078832));
#125917=CARTESIAN_POINT('Ctrl Pts',(-10.4368071192347,12.5263314914137,
12.3166908798255));
#125918=CARTESIAN_POINT('Ctrl Pts',(-9.13614016215244,12.6053150510838,
12.0854459953874));
#125919=CARTESIAN_POINT('Ctrl Pts',(-8.61884944577582,12.6842986107539,
10.8698661249404));
#125920=CARTESIAN_POINT('Ctrl Pts',(-9.35413044364226,12.763282170424,9.77226502046828));
#125921=CARTESIAN_POINT('Ctrl Pts',(-10.6750239439003,12.8422657300941,
9.78812158819826));
#125922=CARTESIAN_POINT('Ctrl Pts',(-11.3839617293869,12.9212492897642,
10.9028590419362));
#125923=CARTESIAN_POINT('Ctrl Pts',(-10.8374483687411,13.0002328494343,
12.1059391953675));
#125924=CARTESIAN_POINT('Ctrl Pts',(-9.53222139713344,13.0792164091044,
12.3056021927521));
#125925=CARTESIAN_POINT('Ctrl Pts',(-8.6497759936489,13.1581999687745,11.3221918706472));
#125926=CARTESIAN_POINT('Ctrl Pts',(-8.99469613902865,13.2371940103917,
10.0445319382663));
#125927=CARTESIAN_POINT('Ctrl Pts',(-9.82845141092598,13.2898601987855,
9.77351385913679));
#125928=CARTESIAN_POINT('Ctrl Pts',(-10.211245721881,13.316198533956,9.84344365356907));
#125929=CARTESIAN_POINT('Ctrl Pts',(-9.36562697413928,3.60128171446242,
9.68112655748337));
#125930=CARTESIAN_POINT('Ctrl Pts',(-9.36187623516791,3.60107085989914,
9.68293364760113));
#125931=CARTESIAN_POINT('Ctrl Pts',(-9.35813300790377,3.60085902115538,
9.68475611302156));
#125932=CARTESIAN_POINT('Ctrl Pts',(-9.35063355176791,3.60043166338206,
9.68844553523053));
#125933=CARTESIAN_POINT('Ctrl Pts',(-9.34688639229947,3.60021664372616,
9.69030825750773));
#125934=CARTESIAN_POINT('Ctrl Pts',(-9.34313799844363,3.6,9.69219093101808));
#125935=CARTESIAN_POINT('Origin',(-10.,3.6,11.));
#125936=CARTESIAN_POINT('',(-10.,3.5,12.5635));
#125937=CARTESIAN_POINT('Origin',(-10.,3.5,11.));
#125938=CARTESIAN_POINT('Origin',(-10.,3.6,12.5635));
#125939=CARTESIAN_POINT('Origin',(-10.,3.5,11.));
#125940=CARTESIAN_POINT('',(-10.,3.5,8.45));
#125941=CARTESIAN_POINT('Origin',(-10.,3.5,11.));
#125942=CARTESIAN_POINT('Origin',(-10.,13.325,11.));
#125943=CARTESIAN_POINT('',(-11.1135,13.5,11.));
#125944=CARTESIAN_POINT('',(-11.2885,13.325,11.));
#125945=CARTESIAN_POINT('Origin',(-10.,13.5,11.));
#125946=CARTESIAN_POINT('Origin',(-10.,13.5,11.));
#125947=CARTESIAN_POINT('Origin',(-7.21791809774051,2.9,11.4905561019091));
#125948=CARTESIAN_POINT('',(-7.30151407930766,2.9,11.5297865002293));
#125949=CARTESIAN_POINT('',(-7.28305503829031,2.9,11.4251000765));
#125950=CARTESIAN_POINT('Origin',(-10.,2.9,11.));
#125951=CARTESIAN_POINT('',(-7.43949984216826,2.9,11.451485261934));
#125952=CARTESIAN_POINT('',(-7.02412006173947,2.9,11.6871961823661));
#125953=CARTESIAN_POINT('',(-7.43949984216826,2.9,11.451485261934));
#125954=CARTESIAN_POINT('Origin',(-6.96855264488606,0.5,11.3720577014022));
#125955=CARTESIAN_POINT('',(-7.28305503829031,0.8,11.4251000765));
#125956=CARTESIAN_POINT('',(-7.28305503829031,3.5,11.4251000765));
#125957=CARTESIAN_POINT('',(-7.43949984216826,0.65,11.451485261934));
#125958=CARTESIAN_POINT('',(-7.43949984216826,0.5,11.451485261934));
#125959=CARTESIAN_POINT('Ctrl Pts',(-7.28305503829031,0.800000000000006,
11.4251000765));
#125960=CARTESIAN_POINT('Ctrl Pts',(-7.36347059168579,0.722647555637982,
11.4386625549942));
#125961=CARTESIAN_POINT('Ctrl Pts',(-7.43949984216826,0.65,11.451485261934));
#125962=CARTESIAN_POINT('Origin',(-7.43949984216826,0.5,11.451485261934));
#125963=CARTESIAN_POINT('',(-7.30151407930766,0.8,11.5297865002293));
#125964=CARTESIAN_POINT('',(-7.30151407930766,3.5,11.5297865002293));
#125965=CARTESIAN_POINT('Ctrl Pts',(-7.43949984216826,0.65,11.451485261934));
#125966=CARTESIAN_POINT('Ctrl Pts',(-7.37244134059104,0.722647555638358,
11.489538200171));
#125967=CARTESIAN_POINT('Ctrl Pts',(-7.30151407930765,0.800000000000005,
11.5297865002293));
#125968=CARTESIAN_POINT('Origin',(-10.,3.5,11.));
#125969=CARTESIAN_POINT('',(-12.7494863164095,2.9,10.9468493097211));
#125970=CARTESIAN_POINT('',(-12.75,2.9,11.));
#125971=CARTESIAN_POINT('Origin',(-10.,2.9,11.));
#125972=CARTESIAN_POINT('',(-12.75,3.3,11.));
#125973=CARTESIAN_POINT('',(-12.75,3.5,11.));
#125974=CARTESIAN_POINT('',(-10.,3.3,8.25));
#125975=CARTESIAN_POINT('Origin',(-10.,3.3,11.));
#125976=CARTESIAN_POINT('Origin',(-10.,3.3,11.));
#125977=CARTESIAN_POINT('',(-12.7494863164095,2.9,11.0531506902789));
#125978=CARTESIAN_POINT('Origin',(-10.,2.9,11.));
#125979=CARTESIAN_POINT('',(-12.7494863164095,0.8,11.0531506902789));
#125980=CARTESIAN_POINT('',(-12.7494863164095,3.5,11.0531506902789));
#125981=CARTESIAN_POINT('',(-12.7169449617097,0.8,11.4251000765));
#125982=CARTESIAN_POINT('Origin',(-10.,0.8,11.));
#125983=CARTESIAN_POINT('',(-12.7169449617097,2.9,11.4251000765));
#125984=CARTESIAN_POINT('',(-12.7169449617097,3.5,11.4251000765));
#125985=CARTESIAN_POINT('',(-12.6984859206923,2.9,11.5297865002293));
#125986=CARTESIAN_POINT('Origin',(-10.,2.9,11.));
#125987=CARTESIAN_POINT('',(-12.6984859206923,0.8,11.5297865002293));
#125988=CARTESIAN_POINT('',(-12.6984859206923,3.5,11.5297865002293));
#125989=CARTESIAN_POINT('',(-12.6018506091889,0.8,11.8904343925655));
#125990=CARTESIAN_POINT('Origin',(-10.,0.8,11.));
#125991=CARTESIAN_POINT('',(-12.6018506091889,2.9,11.8904343925656));
#125992=CARTESIAN_POINT('',(-12.6018506091889,3.5,11.8904343925655));
#125993=CARTESIAN_POINT('',(-12.5654933957747,2.9,11.9903250154551));
#125994=CARTESIAN_POINT('Origin',(-10.,2.9,11.));
#125995=CARTESIAN_POINT('',(-12.5654933957747,0.8,11.9903250154551));
#125996=CARTESIAN_POINT('',(-12.5654933957747,3.5,11.9903250154551));
#125997=CARTESIAN_POINT('',(-12.4077003425078,0.8,12.3287133101945));
#125998=CARTESIAN_POINT('Origin',(-10.,0.8,11.));
#125999=CARTESIAN_POINT('',(-12.4077003425078,2.9,12.3287133101945));
#126000=CARTESIAN_POINT('',(-12.4077003425078,3.5,12.3287133101945));
#126001=CARTESIAN_POINT('',(-12.3545496522288,2.9,12.420773006215));
#126002=CARTESIAN_POINT('Origin',(-10.,2.9,11.));
#126003=CARTESIAN_POINT('',(-12.3545496522288,0.8,12.420773006215));
#126004=CARTESIAN_POINT('',(-12.3545496522288,3.5,12.420773006215));
#126005=CARTESIAN_POINT('',(-12.1403933192747,0.8,12.7266199462546));
#126006=CARTESIAN_POINT('Origin',(-10.,0.8,11.));
#126007=CARTESIAN_POINT('',(-12.1403933192747,2.9,12.7266199462546));
#126008=CARTESIAN_POINT('',(-12.1403933192747,3.5,12.7266199462546));
#126009=CARTESIAN_POINT('',(-12.0720641089596,2.9,12.8080515281268));
#126010=CARTESIAN_POINT('Origin',(-10.,2.9,11.));
#126011=CARTESIAN_POINT('',(-12.0720641089596,0.8,12.8080515281268));
#126012=CARTESIAN_POINT('',(-12.0720641089596,3.5,12.8080515281268));
#126013=CARTESIAN_POINT('',(-11.8080515281268,0.8,13.0720641089596));
#126014=CARTESIAN_POINT('Origin',(-10.,0.8,11.));
#126015=CARTESIAN_POINT('',(-11.8080515281268,2.9,13.0720641089596));
#126016=CARTESIAN_POINT('',(-11.8080515281268,3.5,13.0720641089596));
#126017=CARTESIAN_POINT('',(-11.7266199462546,2.9,13.1403933192747));
#126018=CARTESIAN_POINT('Origin',(-10.,2.9,11.));
#126019=CARTESIAN_POINT('',(-11.7266199462546,0.8,13.1403933192747));
#126020=CARTESIAN_POINT('',(-11.7266199462546,3.5,13.1403933192747));
#126021=CARTESIAN_POINT('',(-11.420773006215,0.8,13.3545496522288));
#126022=CARTESIAN_POINT('Origin',(-10.,0.8,11.));
#126023=CARTESIAN_POINT('',(-11.420773006215,2.9,13.3545496522288));
#126024=CARTESIAN_POINT('',(-11.420773006215,3.5,13.3545496522288));
#126025=CARTESIAN_POINT('',(-11.3287133101945,2.9,13.4077003425078));
#126026=CARTESIAN_POINT('Origin',(-10.,2.9,11.));
#126027=CARTESIAN_POINT('',(-11.3287133101945,0.8,13.4077003425078));
#126028=CARTESIAN_POINT('',(-11.3287133101945,3.5,13.4077003425078));
#126029=CARTESIAN_POINT('',(-10.9903250154551,0.8,13.5654933957747));
#126030=CARTESIAN_POINT('Origin',(-10.,0.8,11.));
#126031=CARTESIAN_POINT('',(-10.9903250154551,2.9,13.5654933957747));
#126032=CARTESIAN_POINT('',(-10.9903250154551,3.5,13.5654933957747));
#126033=CARTESIAN_POINT('',(-10.8904343925656,2.9,13.6018506091889));
#126034=CARTESIAN_POINT('Origin',(-10.,2.9,11.));
#126035=CARTESIAN_POINT('',(-10.8904343925656,0.8,13.6018506091889));
#126036=CARTESIAN_POINT('',(-10.8904343925656,3.5,13.6018506091889));
#126037=CARTESIAN_POINT('',(-10.5297865002293,0.8,13.6984859206923));
#126038=CARTESIAN_POINT('Origin',(-10.,0.8,11.));
#126039=CARTESIAN_POINT('',(-10.5297865002293,2.9,13.6984859206923));
#126040=CARTESIAN_POINT('',(-10.5297865002293,3.5,13.6984859206923));
#126041=CARTESIAN_POINT('',(-10.4251000765,2.9,13.7169449617097));
#126042=CARTESIAN_POINT('Origin',(-10.,2.9,11.));
#126043=CARTESIAN_POINT('',(-10.4251000765,0.8,13.7169449617097));
#126044=CARTESIAN_POINT('',(-10.4251000765,3.5,13.7169449617097));
#126045=CARTESIAN_POINT('',(-10.0531506902789,0.8,13.7494863164095));
#126046=CARTESIAN_POINT('Origin',(-10.,0.8,11.));
#126047=CARTESIAN_POINT('',(-10.0531506902789,2.9,13.7494863164095));
#126048=CARTESIAN_POINT('',(-10.0531506902789,3.5,13.7494863164095));
#126049=CARTESIAN_POINT('',(-9.94684930972108,2.9,13.7494863164095));
#126050=CARTESIAN_POINT('Origin',(-10.,2.9,11.));
#126051=CARTESIAN_POINT('',(-9.94684930972108,0.8,13.7494863164095));
#126052=CARTESIAN_POINT('',(-9.94684930972108,3.5,13.7494863164095));
#126053=CARTESIAN_POINT('',(-9.57489992349997,0.8,13.7169449617097));
#126054=CARTESIAN_POINT('Origin',(-10.,0.8,11.));
#126055=CARTESIAN_POINT('',(-9.57489992349997,2.9,13.7169449617097));
#126056=CARTESIAN_POINT('',(-9.57489992349997,3.5,13.7169449617097));
#126057=CARTESIAN_POINT('',(-9.4702134997707,2.9,13.6984859206923));
#126058=CARTESIAN_POINT('Origin',(-10.,2.9,11.));
#126059=CARTESIAN_POINT('',(-9.47021349977071,0.8,13.6984859206923));
#126060=CARTESIAN_POINT('',(-9.47021349977071,3.5,13.6984859206923));
#126061=CARTESIAN_POINT('',(-9.10956560743445,0.8,13.6018506091889));
#126062=CARTESIAN_POINT('Origin',(-10.,0.8,11.));
#126063=CARTESIAN_POINT('',(-9.10956560743445,2.9,13.6018506091889));
#126064=CARTESIAN_POINT('',(-9.10956560743445,3.5,13.6018506091889));
#126065=CARTESIAN_POINT('',(-9.0096749845449,2.9,13.5654933957747));
#126066=CARTESIAN_POINT('Origin',(-10.,2.9,11.));
#126067=CARTESIAN_POINT('',(-9.0096749845449,0.8,13.5654933957747));
#126068=CARTESIAN_POINT('',(-9.0096749845449,3.5,13.5654933957747));
#126069=CARTESIAN_POINT('',(-8.67128668980549,0.8,13.4077003425078));
#126070=CARTESIAN_POINT('Origin',(-10.,0.8,11.));
#126071=CARTESIAN_POINT('',(-8.67128668980549,2.9,13.4077003425078));
#126072=CARTESIAN_POINT('',(-8.67128668980549,3.5,13.4077003425078));
#126073=CARTESIAN_POINT('',(-8.57922699378505,2.9,13.3545496522288));
#126074=CARTESIAN_POINT('Origin',(-10.,2.9,11.));
#126075=CARTESIAN_POINT('',(-8.57922699378505,0.8,13.3545496522288));
#126076=CARTESIAN_POINT('',(-8.57922699378505,3.5,13.3545496522288));
#126077=CARTESIAN_POINT('',(-8.27338005374542,0.8,13.1403933192747));
#126078=CARTESIAN_POINT('Origin',(-10.,0.8,11.));
#126079=CARTESIAN_POINT('',(-8.27338005374542,2.9,13.1403933192747));
#126080=CARTESIAN_POINT('',(-8.27338005374542,3.5,13.1403933192747));
#126081=CARTESIAN_POINT('',(-8.19194847187321,2.9,13.0720641089596));
#126082=CARTESIAN_POINT('Origin',(-10.,2.9,11.));
#126083=CARTESIAN_POINT('',(-8.19194847187321,0.8,13.0720641089596));
#126084=CARTESIAN_POINT('',(-8.19194847187321,3.5,13.0720641089596));
#126085=CARTESIAN_POINT('',(-7.92793589104044,0.8,12.8080515281268));
#126086=CARTESIAN_POINT('Origin',(-10.,0.8,11.));
#126087=CARTESIAN_POINT('',(-7.92793589104044,2.9,12.8080515281268));
#126088=CARTESIAN_POINT('',(-7.92793589104044,3.5,12.8080515281268));
#126089=CARTESIAN_POINT('',(-7.85960668072529,2.9,12.7266199462546));
#126090=CARTESIAN_POINT('Origin',(-10.,2.9,11.));
#126091=CARTESIAN_POINT('',(-7.85960668072529,0.8,12.7266199462546));
#126092=CARTESIAN_POINT('',(-7.85960668072529,3.5,12.7266199462546));
#126093=CARTESIAN_POINT('',(-7.64545034777117,0.8,12.420773006215));
#126094=CARTESIAN_POINT('Origin',(-10.,0.8,11.));
#126095=CARTESIAN_POINT('',(-7.64545034777117,2.9,12.420773006215));
#126096=CARTESIAN_POINT('',(-7.64545034777117,3.5,12.420773006215));
#126097=CARTESIAN_POINT('',(-7.59229965749225,2.9,12.3287133101945));
#126098=CARTESIAN_POINT('Origin',(-10.,2.9,11.));
#126099=CARTESIAN_POINT('',(-7.59229965749225,0.8,12.3287133101945));
#126100=CARTESIAN_POINT('',(-7.59229965749225,3.5,12.3287133101945));
#126101=CARTESIAN_POINT('',(-7.43450660422525,0.8,11.9903250154551));
#126102=CARTESIAN_POINT('Origin',(-10.,0.8,11.));
#126103=CARTESIAN_POINT('',(-7.43450660422525,2.9,11.9903250154551));
#126104=CARTESIAN_POINT('',(-7.43450660422525,3.5,11.9903250154551));
#126105=CARTESIAN_POINT('',(-7.39814939081115,2.9,11.8904343925656));
#126106=CARTESIAN_POINT('Origin',(-10.,2.9,11.));
#126107=CARTESIAN_POINT('',(-7.39814939081115,0.8,11.8904343925656));
#126108=CARTESIAN_POINT('',(-7.39814939081115,3.5,11.8904343925656));
#126109=CARTESIAN_POINT('Origin',(-10.,0.8,11.));
#126110=CARTESIAN_POINT('',(-7.25051368359054,0.8,11.0531506902789));
#126111=CARTESIAN_POINT('Origin',(-10.,0.8,11.));
#126112=CARTESIAN_POINT('',(-7.25051368359054,2.9,11.0531506902789));
#126113=CARTESIAN_POINT('',(-7.25051368359054,3.5,11.0531506902789));
#126114=CARTESIAN_POINT('',(-7.25051368359054,2.9,10.9468493097211));
#126115=CARTESIAN_POINT('Origin',(-10.,2.9,11.));
#126116=CARTESIAN_POINT('',(-7.25051368359054,0.8,10.9468493097211));
#126117=CARTESIAN_POINT('',(-7.25051368359054,3.5,10.9468493097211));
#126118=CARTESIAN_POINT('',(-7.28305503829031,0.8,10.5748999235));
#126119=CARTESIAN_POINT('Origin',(-10.,0.8,11.));
#126120=CARTESIAN_POINT('',(-7.28305503829031,2.9,10.5748999235));
#126121=CARTESIAN_POINT('',(-7.28305503829031,3.5,10.5748999235));
#126122=CARTESIAN_POINT('',(-7.30151407930766,2.9,10.4702134997707));
#126123=CARTESIAN_POINT('Origin',(-10.,2.9,11.));
#126124=CARTESIAN_POINT('',(-7.30151407930766,0.8,10.4702134997707));
#126125=CARTESIAN_POINT('',(-7.30151407930766,3.5,10.4702134997707));
#126126=CARTESIAN_POINT('',(-7.39814939081114,0.8,10.1095656074345));
#126127=CARTESIAN_POINT('Origin',(-10.,0.8,11.));
#126128=CARTESIAN_POINT('',(-7.39814939081114,2.9,10.1095656074344));
#126129=CARTESIAN_POINT('',(-7.39814939081114,3.5,10.1095656074345));
#126130=CARTESIAN_POINT('',(-7.43450660422525,2.9,10.0096749845449));
#126131=CARTESIAN_POINT('Origin',(-10.,2.9,11.));
#126132=CARTESIAN_POINT('',(-7.43450660422525,0.8,10.0096749845449));
#126133=CARTESIAN_POINT('',(-7.43450660422525,3.5,10.0096749845449));
#126134=CARTESIAN_POINT('',(-7.59229965749225,0.8,9.67128668980549));
#126135=CARTESIAN_POINT('Origin',(-10.,0.8,11.));
#126136=CARTESIAN_POINT('',(-7.59229965749225,2.9,9.67128668980549));
#126137=CARTESIAN_POINT('',(-7.59229965749225,3.5,9.67128668980549));
#126138=CARTESIAN_POINT('',(-7.64545034777117,2.9,9.57922699378505));
#126139=CARTESIAN_POINT('Origin',(-10.,2.9,11.));
#126140=CARTESIAN_POINT('',(-7.64545034777117,0.8,9.57922699378504));
#126141=CARTESIAN_POINT('',(-7.64545034777117,3.5,9.57922699378504));
#126142=CARTESIAN_POINT('',(-7.85960668072529,0.8,9.27338005374542));
#126143=CARTESIAN_POINT('Origin',(-10.,0.8,11.));
#126144=CARTESIAN_POINT('',(-7.85960668072529,2.9,9.27338005374542));
#126145=CARTESIAN_POINT('',(-7.85960668072529,3.5,9.27338005374542));
#126146=CARTESIAN_POINT('',(-7.92793589104044,2.9,9.19194847187321));
#126147=CARTESIAN_POINT('Origin',(-10.,2.9,11.));
#126148=CARTESIAN_POINT('',(-7.92793589104044,0.8,9.19194847187321));
#126149=CARTESIAN_POINT('',(-7.92793589104044,3.5,9.19194847187321));
#126150=CARTESIAN_POINT('',(-8.19194847187321,0.8,8.92793589104044));
#126151=CARTESIAN_POINT('Origin',(-10.,0.8,11.));
#126152=CARTESIAN_POINT('',(-8.19194847187321,2.9,8.92793589104044));
#126153=CARTESIAN_POINT('',(-8.19194847187321,3.5,8.92793589104044));
#126154=CARTESIAN_POINT('',(-8.27338005374542,2.9,8.85960668072529));
#126155=CARTESIAN_POINT('Origin',(-10.,2.9,11.));
#126156=CARTESIAN_POINT('',(-8.27338005374542,0.8,8.85960668072529));
#126157=CARTESIAN_POINT('',(-8.27338005374542,3.5,8.85960668072529));
#126158=CARTESIAN_POINT('',(-8.57922699378504,0.8,8.64545034777117));
#126159=CARTESIAN_POINT('Origin',(-10.,0.8,11.));
#126160=CARTESIAN_POINT('',(-8.57922699378504,2.9,8.64545034777117));
#126161=CARTESIAN_POINT('',(-8.57922699378504,3.5,8.64545034777117));
#126162=CARTESIAN_POINT('',(-8.67128668980549,2.9,8.59229965749225));
#126163=CARTESIAN_POINT('Origin',(-10.,2.9,11.));
#126164=CARTESIAN_POINT('',(-8.67128668980549,0.8,8.59229965749225));
#126165=CARTESIAN_POINT('',(-8.67128668980549,3.5,8.59229965749225));
#126166=CARTESIAN_POINT('',(-9.00967498454489,0.8,8.43450660422525));
#126167=CARTESIAN_POINT('Origin',(-10.,0.8,11.));
#126168=CARTESIAN_POINT('',(-9.00967498454489,2.9,8.43450660422525));
#126169=CARTESIAN_POINT('',(-9.00967498454489,3.5,8.43450660422525));
#126170=CARTESIAN_POINT('',(-9.10956560743445,2.9,8.39814939081115));
#126171=CARTESIAN_POINT('Origin',(-10.,2.9,11.));
#126172=CARTESIAN_POINT('',(-9.10956560743445,0.8,8.39814939081115));
#126173=CARTESIAN_POINT('',(-9.10956560743445,3.5,8.39814939081115));
#126174=CARTESIAN_POINT('',(-9.47021349977071,0.8,8.30151407930766));
#126175=CARTESIAN_POINT('Origin',(-10.,0.8,11.));
#126176=CARTESIAN_POINT('',(-9.4702134997707,2.9,8.30151407930766));
#126177=CARTESIAN_POINT('',(-9.47021349977071,3.5,8.30151407930766));
#126178=CARTESIAN_POINT('',(-9.57489992349996,2.9,8.28305503829031));
#126179=CARTESIAN_POINT('Origin',(-10.,2.9,11.));
#126180=CARTESIAN_POINT('',(-9.57489992349997,0.8,8.28305503829031));
#126181=CARTESIAN_POINT('',(-9.57489992349997,3.5,8.28305503829031));
#126182=CARTESIAN_POINT('',(-9.94684930972108,0.8,8.25051368359054));
#126183=CARTESIAN_POINT('Origin',(-10.,0.8,11.));
#126184=CARTESIAN_POINT('',(-9.94684930972108,2.9,8.25051368359054));
#126185=CARTESIAN_POINT('',(-9.94684930972108,3.5,8.25051368359054));
#126186=CARTESIAN_POINT('',(-10.0531506902789,2.9,8.25051368359054));
#126187=CARTESIAN_POINT('Origin',(-10.,2.9,11.));
#126188=CARTESIAN_POINT('',(-10.0531506902789,0.8,8.25051368359054));
#126189=CARTESIAN_POINT('',(-10.0531506902789,3.5,8.25051368359054));
#126190=CARTESIAN_POINT('',(-10.4251000765,0.8,8.28305503829031));
#126191=CARTESIAN_POINT('Origin',(-10.,0.8,11.));
#126192=CARTESIAN_POINT('',(-10.4251000765,2.9,8.28305503829031));
#126193=CARTESIAN_POINT('',(-10.4251000765,3.5,8.28305503829031));
#126194=CARTESIAN_POINT('',(-10.5297865002293,2.9,8.30151407930766));
#126195=CARTESIAN_POINT('Origin',(-10.,2.9,11.));
#126196=CARTESIAN_POINT('',(-10.5297865002293,0.8,8.30151407930766));
#126197=CARTESIAN_POINT('',(-10.5297865002293,3.5,8.30151407930766));
#126198=CARTESIAN_POINT('',(-10.8904343925655,0.8,8.39814939081115));
#126199=CARTESIAN_POINT('Origin',(-10.,0.8,11.));
#126200=CARTESIAN_POINT('',(-10.8904343925656,2.9,8.39814939081115));
#126201=CARTESIAN_POINT('',(-10.8904343925655,3.5,8.39814939081115));
#126202=CARTESIAN_POINT('',(-10.9903250154551,2.9,8.43450660422526));
#126203=CARTESIAN_POINT('Origin',(-10.,2.9,11.));
#126204=CARTESIAN_POINT('',(-10.9903250154551,0.8,8.43450660422526));
#126205=CARTESIAN_POINT('',(-10.9903250154551,3.5,8.43450660422526));
#126206=CARTESIAN_POINT('',(-11.3287133101945,0.8,8.59229965749225));
#126207=CARTESIAN_POINT('Origin',(-10.,0.8,11.));
#126208=CARTESIAN_POINT('',(-11.3287133101945,2.9,8.59229965749225));
#126209=CARTESIAN_POINT('',(-11.3287133101945,3.5,8.59229965749225));
#126210=CARTESIAN_POINT('',(-11.420773006215,2.9,8.64545034777117));
#126211=CARTESIAN_POINT('Origin',(-10.,2.9,11.));
#126212=CARTESIAN_POINT('',(-11.420773006215,0.8,8.64545034777117));
#126213=CARTESIAN_POINT('',(-11.420773006215,3.5,8.64545034777117));
#126214=CARTESIAN_POINT('',(-11.7266199462546,0.8,8.85960668072529));
#126215=CARTESIAN_POINT('Origin',(-10.,0.8,11.));
#126216=CARTESIAN_POINT('',(-11.7266199462546,2.9,8.85960668072529));
#126217=CARTESIAN_POINT('',(-11.7266199462546,3.5,8.85960668072529));
#126218=CARTESIAN_POINT('',(-11.8080515281268,2.9,8.92793589104044));
#126219=CARTESIAN_POINT('Origin',(-10.,2.9,11.));
#126220=CARTESIAN_POINT('',(-11.8080515281268,0.8,8.92793589104044));
#126221=CARTESIAN_POINT('',(-11.8080515281268,3.5,8.92793589104044));
#126222=CARTESIAN_POINT('',(-12.0720641089596,0.8,9.19194847187321));
#126223=CARTESIAN_POINT('Origin',(-10.,0.8,11.));
#126224=CARTESIAN_POINT('',(-12.0720641089596,2.9,9.19194847187321));
#126225=CARTESIAN_POINT('',(-12.0720641089596,3.5,9.19194847187321));
#126226=CARTESIAN_POINT('',(-12.1403933192747,2.9,9.27338005374542));
#126227=CARTESIAN_POINT('Origin',(-10.,2.9,11.));
#126228=CARTESIAN_POINT('',(-12.1403933192747,0.8,9.27338005374542));
#126229=CARTESIAN_POINT('',(-12.1403933192747,3.5,9.27338005374542));
#126230=CARTESIAN_POINT('',(-12.3545496522288,0.8,9.57922699378505));
#126231=CARTESIAN_POINT('Origin',(-10.,0.8,11.));
#126232=CARTESIAN_POINT('',(-12.3545496522288,2.9,9.57922699378505));
#126233=CARTESIAN_POINT('',(-12.3545496522288,3.5,9.57922699378505));
#126234=CARTESIAN_POINT('',(-12.4077003425078,2.9,9.67128668980549));
#126235=CARTESIAN_POINT('Origin',(-10.,2.9,11.));
#126236=CARTESIAN_POINT('',(-12.4077003425078,0.8,9.67128668980549));
#126237=CARTESIAN_POINT('',(-12.4077003425078,3.5,9.67128668980549));
#126238=CARTESIAN_POINT('',(-12.5654933957747,0.8,10.0096749845449));
#126239=CARTESIAN_POINT('Origin',(-10.,0.8,11.));
#126240=CARTESIAN_POINT('',(-12.5654933957747,2.9,10.0096749845449));
#126241=CARTESIAN_POINT('',(-12.5654933957747,3.5,10.0096749845449));
#126242=CARTESIAN_POINT('',(-12.6018506091889,2.9,10.1095656074344));
#126243=CARTESIAN_POINT('Origin',(-10.,2.9,11.));
#126244=CARTESIAN_POINT('',(-12.6018506091889,0.8,10.1095656074345));
#126245=CARTESIAN_POINT('',(-12.6018506091889,3.5,10.1095656074345));
#126246=CARTESIAN_POINT('',(-12.6984859206923,0.8,10.4702134997707));
#126247=CARTESIAN_POINT('Origin',(-10.,0.8,11.));
#126248=CARTESIAN_POINT('',(-12.6984859206923,2.9,10.4702134997707));
#126249=CARTESIAN_POINT('',(-12.6984859206923,3.5,10.4702134997707));
#126250=CARTESIAN_POINT('',(-12.7169449617097,2.9,10.5748999235));
#126251=CARTESIAN_POINT('Origin',(-10.,2.9,11.));
#126252=CARTESIAN_POINT('',(-12.7169449617097,0.8,10.5748999235));
#126253=CARTESIAN_POINT('',(-12.7169449617097,3.5,10.5748999235));
#126254=CARTESIAN_POINT('',(-12.7494863164095,0.8,10.9468493097211));
#126255=CARTESIAN_POINT('Origin',(-10.,0.8,11.));
#126256=CARTESIAN_POINT('',(-12.7494863164095,3.5,10.9468493097211));
#126257=CARTESIAN_POINT('Origin',(-7.07921428367087,0.5,11.8928106178175));
#126258=CARTESIAN_POINT('',(-7.55679918595664,2.9,11.8892523726467));
#126259=CARTESIAN_POINT('',(-7.55679918595664,2.9,11.8892523726467));
#126260=CARTESIAN_POINT('',(-7.55679918595664,0.650000000000001,11.8892523726467));
#126261=CARTESIAN_POINT('',(-7.55679918595664,0.5,11.8892523726467));
#126262=CARTESIAN_POINT('Ctrl Pts',(-7.39814939081114,0.800000000000006,
11.8904343925656));
#126263=CARTESIAN_POINT('Ctrl Pts',(-7.47969835093276,0.722647555638146,
11.8898268122335));
#126264=CARTESIAN_POINT('Ctrl Pts',(-7.55679918595664,0.650000000000001,
11.8892523726467));
#126265=CARTESIAN_POINT('Origin',(-7.55679918595664,0.5,11.8892523726467));
#126266=CARTESIAN_POINT('Ctrl Pts',(-7.55679918595664,0.650000000000001,
11.8892523726467));
#126267=CARTESIAN_POINT('Ctrl Pts',(-7.49736727707775,0.722647555638346,
11.9383717878434));
#126268=CARTESIAN_POINT('Ctrl Pts',(-7.43450660422525,0.800000000000006,
11.9903250154551));
#126269=CARTESIAN_POINT('',(-7.18866072953509,2.9,12.193512256469));
#126270=CARTESIAN_POINT('Origin',(-7.34536834627981,2.9,11.966206904895));
#126271=CARTESIAN_POINT('Origin',(-10.,0.65,11.));
#126272=CARTESIAN_POINT('',(-12.6,0.649999999999998,11.));
#126273=CARTESIAN_POINT('Ctrl Pts',(-12.6,0.649999999999998,11.));
#126274=CARTESIAN_POINT('Ctrl Pts',(-12.6726475556382,0.722647555638152,
10.9741697579953));
#126275=CARTESIAN_POINT('Ctrl Pts',(-12.7494863164095,0.800000000000003,
10.9468493097211));
#126276=CARTESIAN_POINT('',(-12.5605001578317,0.650000000000002,10.548514738066));
#126277=CARTESIAN_POINT('Ctrl Pts',(-12.7169449617097,0.800000000000003,
10.5748999235));
#126278=CARTESIAN_POINT('Ctrl Pts',(-12.6365294083145,0.722647555638305,
10.5613374450059));
#126279=CARTESIAN_POINT('Ctrl Pts',(-12.5605001578317,0.650000000000002,
10.548514738066));
#126280=CARTESIAN_POINT('Ctrl Pts',(-12.5605001578317,0.650000000000002,
10.548514738066));
#126281=CARTESIAN_POINT('Ctrl Pts',(-12.6275586594091,0.722647555638513,
10.5104617998289));
#126282=CARTESIAN_POINT('Ctrl Pts',(-12.6984859206923,0.800000000000003,
10.4702134997707));
#126283=CARTESIAN_POINT('',(-12.4432008140434,0.649999999999998,10.1107476273533));
#126284=CARTESIAN_POINT('Ctrl Pts',(-12.6018506091889,0.800000000000003,
10.1095656074344));
#126285=CARTESIAN_POINT('Ctrl Pts',(-12.5203016490671,0.722647555638048,
10.1101731877666));
#126286=CARTESIAN_POINT('Ctrl Pts',(-12.4432008140434,0.649999999999998,
10.1107476273533));
#126287=CARTESIAN_POINT('Ctrl Pts',(-12.4432008140434,0.649999999999998,
10.1107476273533));
#126288=CARTESIAN_POINT('Ctrl Pts',(-12.5026327229224,0.722647555638522,
10.0616282121565));
#126289=CARTESIAN_POINT('Ctrl Pts',(-12.5654933957747,0.800000000000003,
10.0096749845449));
#126290=CARTESIAN_POINT('',(-12.2516660498395,0.65,9.7));
#126291=CARTESIAN_POINT('Ctrl Pts',(-12.4077003425078,0.800000000000003,
9.67128668980549));
#126292=CARTESIAN_POINT('Ctrl Pts',(-12.3274957995475,0.722647555638263,
9.68604586794285));
#126293=CARTESIAN_POINT('Ctrl Pts',(-12.2516660498395,0.65,9.7));
#126294=CARTESIAN_POINT('Ctrl Pts',(-12.2516660498395,0.65,9.7));
#126295=CARTESIAN_POINT('Ctrl Pts',(-12.3016655575427,0.722647555638126,
9.641306576419));
#126296=CARTESIAN_POINT('Ctrl Pts',(-12.3545496522288,0.800000000000003,
9.57922699378504));
#126297=CARTESIAN_POINT('',(-11.9917155521093,0.649999999999998,9.328752214815));
#126298=CARTESIAN_POINT('Ctrl Pts',(-12.1403933192747,0.800000000000003,
9.27338005374542));
#126299=CARTESIAN_POINT('Ctrl Pts',(-12.0639701679277,0.722647555637942,
9.30184237952896));
#126300=CARTESIAN_POINT('Ctrl Pts',(-11.9917155521093,0.649999999999998,
9.328752214815));
#126301=CARTESIAN_POINT('Ctrl Pts',(-11.9917155521093,0.649999999999998,
9.328752214815));
#126302=CARTESIAN_POINT('Ctrl Pts',(-12.0307634488962,0.722647555637936,
9.26226815282488));
#126303=CARTESIAN_POINT('Ctrl Pts',(-12.0720641089596,0.800000000000003,
9.19194847187321));
#126304=CARTESIAN_POINT('',(-11.671247785185,0.649999999999999,9.00828444789066));
#126305=CARTESIAN_POINT('Ctrl Pts',(-11.8080515281268,0.800000000000002,
8.92793589104044));
#126306=CARTESIAN_POINT('Ctrl Pts',(-11.7377318471751,0.722647555637865,
8.96923655110384));
#126307=CARTESIAN_POINT('Ctrl Pts',(-11.671247785185,0.649999999999999,
9.00828444789066));
#126308=CARTESIAN_POINT('Ctrl Pts',(-11.671247785185,0.649999999999999,
9.00828444789066));
#126309=CARTESIAN_POINT('Ctrl Pts',(-11.6981576204713,0.722647555638571,
8.93602983207164));
#126310=CARTESIAN_POINT('Ctrl Pts',(-11.7266199462546,0.800000000000002,
8.85960668072529));
#126311=CARTESIAN_POINT('',(-11.3,0.65,8.74833395016046));
#126312=CARTESIAN_POINT('Ctrl Pts',(-11.420773006215,0.800000000000002,
8.64545034777117));
#126313=CARTESIAN_POINT('Ctrl Pts',(-11.3586934235809,0.722647555637949,
8.69833444245745));
#126314=CARTESIAN_POINT('Ctrl Pts',(-11.3,0.65,8.74833395016046));
#126315=CARTESIAN_POINT('Ctrl Pts',(-11.3,0.65,8.74833395016046));
#126316=CARTESIAN_POINT('Ctrl Pts',(-11.3139541320571,0.722647555638201,
8.67250420045259));
#126317=CARTESIAN_POINT('Ctrl Pts',(-11.3287133101945,0.800000000000003,
8.59229965749224));
#126318=CARTESIAN_POINT('',(-10.8892523726467,0.65,8.55679918595664));
#126319=CARTESIAN_POINT('Ctrl Pts',(-10.9903250154551,0.800000000000002,
8.43450660422526));
#126320=CARTESIAN_POINT('Ctrl Pts',(-10.9383717878433,0.722647555638172,
8.49736727707789));
#126321=CARTESIAN_POINT('Ctrl Pts',(-10.8892523726467,0.65,8.55679918595664));
#126322=CARTESIAN_POINT('Ctrl Pts',(-10.8892523726467,0.65,8.55679918595664));
#126323=CARTESIAN_POINT('Ctrl Pts',(-10.8898268122335,0.722647555638392,
8.4796983509325));
#126324=CARTESIAN_POINT('Ctrl Pts',(-10.8904343925655,0.800000000000002,
8.39814939081114));
#126325=CARTESIAN_POINT('',(-10.451485261934,0.649999999999999,8.43949984216826));
#126326=CARTESIAN_POINT('Ctrl Pts',(-10.5297865002293,0.800000000000002,
8.30151407930766));
#126327=CARTESIAN_POINT('Ctrl Pts',(-10.4895382001709,0.72264755563816,
8.37244134059122));
#126328=CARTESIAN_POINT('Ctrl Pts',(-10.451485261934,0.649999999999999,
8.43949984216826));
#126329=CARTESIAN_POINT('Ctrl Pts',(-10.451485261934,0.649999999999999,
8.43949984216826));
#126330=CARTESIAN_POINT('Ctrl Pts',(-10.4386625549942,0.722647555637904,
8.36347059168587));
#126331=CARTESIAN_POINT('Ctrl Pts',(-10.4251000765,0.800000000000002,8.28305503829031));
#126332=CARTESIAN_POINT('',(-10.,0.649999999999999,8.4));
#126333=CARTESIAN_POINT('Ctrl Pts',(-10.0531506902789,0.800000000000002,
8.25051368359054));
#126334=CARTESIAN_POINT('Ctrl Pts',(-10.0258302420047,0.722647555638087,
8.32735244436191));
#126335=CARTESIAN_POINT('Ctrl Pts',(-10.,0.649999999999999,8.4));
#126336=CARTESIAN_POINT('Ctrl Pts',(-10.,0.649999999999999,8.4));
#126337=CARTESIAN_POINT('Ctrl Pts',(-9.97416975799538,0.722647555637996,
8.32735244436201));
#126338=CARTESIAN_POINT('Ctrl Pts',(-9.94684930972108,0.800000000000002,
8.25051368359054));
#126339=CARTESIAN_POINT('',(-9.54851473806598,0.65,8.43949984216826));
#126340=CARTESIAN_POINT('Ctrl Pts',(-9.57489992349997,0.800000000000002,
8.28305503829031));
#126341=CARTESIAN_POINT('Ctrl Pts',(-9.56133744500582,0.722647555637995,
8.36347059168578));
#126342=CARTESIAN_POINT('Ctrl Pts',(-9.54851473806598,0.65,8.43949984216826));
#126343=CARTESIAN_POINT('Ctrl Pts',(-9.54851473806598,0.65,8.43949984216826));
#126344=CARTESIAN_POINT('Ctrl Pts',(-9.51046179982906,0.72264755563816,
8.37244134059122));
#126345=CARTESIAN_POINT('Ctrl Pts',(-9.4702134997707,0.800000000000002,
8.30151407930766));
#126346=CARTESIAN_POINT('',(-9.11074762735326,0.65,8.55679918595664));
#126347=CARTESIAN_POINT('Ctrl Pts',(-9.10956560743445,0.800000000000002,
8.39814939081114));
#126348=CARTESIAN_POINT('Ctrl Pts',(-9.11017318776655,0.722647555638322,
8.47969835093257));
#126349=CARTESIAN_POINT('Ctrl Pts',(-9.11074762735326,0.65,8.55679918595664));
#126350=CARTESIAN_POINT('Ctrl Pts',(-9.11074762735326,0.65,8.55679918595664));
#126351=CARTESIAN_POINT('Ctrl Pts',(-9.06162821215674,0.722647555638138,
8.49736727707792));
#126352=CARTESIAN_POINT('Ctrl Pts',(-9.00967498454489,0.800000000000001,
8.43450660422525));
#126353=CARTESIAN_POINT('',(-8.7,0.649999999999997,8.74833395016046));
#126354=CARTESIAN_POINT('Ctrl Pts',(-8.67128668980549,0.800000000000001,
8.59229965749225));
#126355=CARTESIAN_POINT('Ctrl Pts',(-8.68604586794282,0.722647555638445,
8.67250420045233));
#126356=CARTESIAN_POINT('Ctrl Pts',(-8.7,0.649999999999997,8.74833395016046));
#126357=CARTESIAN_POINT('Ctrl Pts',(-8.7,0.649999999999997,8.74833395016046));
#126358=CARTESIAN_POINT('Ctrl Pts',(-8.64130657641892,0.722647555638218,
8.69833444245727));
#126359=CARTESIAN_POINT('Ctrl Pts',(-8.57922699378504,0.800000000000001,
8.64545034777117));
#126360=CARTESIAN_POINT('',(-8.328752214815,0.65,9.00828444789066));
#126361=CARTESIAN_POINT('Ctrl Pts',(-8.27338005374542,0.800000000000001,
8.85960668072529));
#126362=CARTESIAN_POINT('Ctrl Pts',(-8.3018423795288,0.722647555638374,
8.93602983207184));
#126363=CARTESIAN_POINT('Ctrl Pts',(-8.328752214815,0.65,9.00828444789066));
#126364=CARTESIAN_POINT('Ctrl Pts',(-8.328752214815,0.65,9.00828444789066));
#126365=CARTESIAN_POINT('Ctrl Pts',(-8.26226815282474,0.722647555638093,
8.96923655110372));
#126366=CARTESIAN_POINT('Ctrl Pts',(-8.19194847187321,0.800000000000001,
8.92793589104044));
#126367=CARTESIAN_POINT('',(-8.00828444789066,0.65,9.328752214815));
#126368=CARTESIAN_POINT('Ctrl Pts',(-7.92793589104044,0.800000000000001,
9.19194847187321));
#126369=CARTESIAN_POINT('Ctrl Pts',(-7.96923655110365,0.722647555638209,
9.26226815282463));
#126370=CARTESIAN_POINT('Ctrl Pts',(-8.00828444789066,0.65,9.328752214815));
#126371=CARTESIAN_POINT('Ctrl Pts',(-8.00828444789066,0.65,9.328752214815));
#126372=CARTESIAN_POINT('Ctrl Pts',(-7.93602983207193,0.722647555638282,
9.30184237952883));
#126373=CARTESIAN_POINT('Ctrl Pts',(-7.85960668072529,0.8,9.27338005374542));
#126374=CARTESIAN_POINT('',(-7.74833395016046,0.65,9.7));
#126375=CARTESIAN_POINT('Ctrl Pts',(-7.64545034777117,0.800000000000001,
9.57922699378505));
#126376=CARTESIAN_POINT('Ctrl Pts',(-7.69833444245722,0.722647555638291,
9.64130657641886));
#126377=CARTESIAN_POINT('Ctrl Pts',(-7.74833395016046,0.65,9.7));
#126378=CARTESIAN_POINT('Ctrl Pts',(-7.74833395016046,0.65,9.7));
#126379=CARTESIAN_POINT('Ctrl Pts',(-7.67250420045258,0.722647555638207,
9.68604586794286));
#126380=CARTESIAN_POINT('Ctrl Pts',(-7.59229965749225,0.800000000000001,
9.67128668980549));
#126381=CARTESIAN_POINT('',(-7.55679918595664,0.65,10.1107476273533));
#126382=CARTESIAN_POINT('Ctrl Pts',(-7.43450660422525,0.800000000000001,
10.0096749845449));
#126383=CARTESIAN_POINT('Ctrl Pts',(-7.49736727707791,0.722647555638159,
10.0616282121567));
#126384=CARTESIAN_POINT('Ctrl Pts',(-7.55679918595664,0.65,10.1107476273533));
#126385=CARTESIAN_POINT('Ctrl Pts',(-7.55679918595664,0.65,10.1107476273533));
#126386=CARTESIAN_POINT('Ctrl Pts',(-7.47969835093245,0.722647555638439,
10.1101731877665));
#126387=CARTESIAN_POINT('Ctrl Pts',(-7.39814939081114,0.800000000000001,
10.1095656074345));
#126388=CARTESIAN_POINT('',(-7.43949984216826,0.65,10.548514738066));
#126389=CARTESIAN_POINT('Ctrl Pts',(-7.30151407930766,0.800000000000001,
10.4702134997707));
#126390=CARTESIAN_POINT('Ctrl Pts',(-7.37244134059127,0.722647555638108,
10.5104617998291));
#126391=CARTESIAN_POINT('Ctrl Pts',(-7.43949984216826,0.65,10.548514738066));
#126392=CARTESIAN_POINT('Ctrl Pts',(-7.43949984216826,0.65,10.548514738066));
#126393=CARTESIAN_POINT('Ctrl Pts',(-7.36347059168572,0.72264755563805,
10.5613374450058));
#126394=CARTESIAN_POINT('Ctrl Pts',(-7.28305503829031,0.800000000000001,
10.5748999235));
#126395=CARTESIAN_POINT('',(-7.4,0.65,11.));
#126396=CARTESIAN_POINT('Ctrl Pts',(-7.25051368359054,0.800000000000001,
10.9468493097211));
#126397=CARTESIAN_POINT('Ctrl Pts',(-7.3273524443617,0.722647555638303,
10.9741697579953));
#126398=CARTESIAN_POINT('Ctrl Pts',(-7.4,0.65,11.));
#126399=CARTESIAN_POINT('Ctrl Pts',(-7.4,0.65,11.));
#126400=CARTESIAN_POINT('Ctrl Pts',(-7.3273524443617,0.722647555638303,
11.0258302420047));
#126401=CARTESIAN_POINT('Ctrl Pts',(-7.25051368359054,0.800000000000001,
11.0531506902789));
#126402=CARTESIAN_POINT('',(-7.74833395016046,0.65,12.3));
#126403=CARTESIAN_POINT('Ctrl Pts',(-7.59229965749224,0.800000000000005,
12.3287133101945));
#126404=CARTESIAN_POINT('Ctrl Pts',(-7.67250420045221,0.722647555638561,
12.3139541320572));
#126405=CARTESIAN_POINT('Ctrl Pts',(-7.74833395016046,0.65,12.3));
#126406=CARTESIAN_POINT('Ctrl Pts',(-7.74833395016046,0.65,12.3));
#126407=CARTESIAN_POINT('Ctrl Pts',(-7.69833444245715,0.722647555638393,
12.3586934235812));
#126408=CARTESIAN_POINT('Ctrl Pts',(-7.64545034777116,0.800000000000006,
12.420773006215));
#126409=CARTESIAN_POINT('',(-8.00828444789066,0.649999999999997,12.671247785185));
#126410=CARTESIAN_POINT('Ctrl Pts',(-7.85960668072528,0.800000000000005,
12.7266199462546));
#126411=CARTESIAN_POINT('Ctrl Pts',(-7.93602983207192,0.722647555638297,
12.6981576204712));
#126412=CARTESIAN_POINT('Ctrl Pts',(-8.00828444789066,0.649999999999997,
12.671247785185));
#126413=CARTESIAN_POINT('Ctrl Pts',(-8.00828444789066,0.649999999999997,
12.671247785185));
#126414=CARTESIAN_POINT('Ctrl Pts',(-7.96923655110345,0.722647555638591,
12.7377318471757));
#126415=CARTESIAN_POINT('Ctrl Pts',(-7.92793589104044,0.800000000000006,
12.8080515281268));
#126416=CARTESIAN_POINT('',(-8.328752214815,0.65,12.9917155521093));
#126417=CARTESIAN_POINT('Ctrl Pts',(-8.19194847187321,0.800000000000005,
13.0720641089596));
#126418=CARTESIAN_POINT('Ctrl Pts',(-8.26226815282437,0.722647555638491,
13.0307634488965));
#126419=CARTESIAN_POINT('Ctrl Pts',(-8.328752214815,0.65,12.9917155521093));
#126420=CARTESIAN_POINT('Ctrl Pts',(-8.328752214815,0.65,12.9917155521093));
#126421=CARTESIAN_POINT('Ctrl Pts',(-8.301842379529,0.722647555637846,13.0639701679276));
#126422=CARTESIAN_POINT('Ctrl Pts',(-8.27338005374542,0.800000000000006,
13.1403933192747));
#126423=CARTESIAN_POINT('',(-8.7,0.650000000000003,13.2516660498395));
#126424=CARTESIAN_POINT('Ctrl Pts',(-8.57922699378504,0.800000000000005,
13.3545496522288));
#126425=CARTESIAN_POINT('Ctrl Pts',(-8.64130657641873,0.72264755563846,
13.3016655575429));
#126426=CARTESIAN_POINT('Ctrl Pts',(-8.7,0.650000000000003,13.2516660498395));
#126427=CARTESIAN_POINT('Ctrl Pts',(-8.7,0.650000000000003,13.2516660498395));
#126428=CARTESIAN_POINT('Ctrl Pts',(-8.68604586794285,0.722647555638247,
13.3274957995475));
#126429=CARTESIAN_POINT('Ctrl Pts',(-8.67128668980549,0.800000000000006,
13.4077003425078));
#126430=CARTESIAN_POINT('',(-9.11074762735326,0.65,13.4432008140434));
#126431=CARTESIAN_POINT('Ctrl Pts',(-9.00967498454489,0.800000000000005,
13.5654933957748));
#126432=CARTESIAN_POINT('Ctrl Pts',(-9.06162821215681,0.722647555638048,
13.502632722922));
#126433=CARTESIAN_POINT('Ctrl Pts',(-9.11074762735326,0.65,13.4432008140434));
#126434=CARTESIAN_POINT('Ctrl Pts',(-9.11074762735326,0.65,13.4432008140434));
#126435=CARTESIAN_POINT('Ctrl Pts',(-9.11017318776655,0.722647555638307,
13.5203016490674));
#126436=CARTESIAN_POINT('Ctrl Pts',(-9.10956560743445,0.800000000000005,
13.6018506091889));
#126437=CARTESIAN_POINT('',(-9.54851473806598,0.65,13.5605001578317));
#126438=CARTESIAN_POINT('Ctrl Pts',(-9.4702134997707,0.800000000000004,
13.6984859206923));
#126439=CARTESIAN_POINT('Ctrl Pts',(-9.51046179982905,0.722647555638188,
13.6275586594088));
#126440=CARTESIAN_POINT('Ctrl Pts',(-9.54851473806598,0.65,13.5605001578317));
#126441=CARTESIAN_POINT('Ctrl Pts',(-9.54851473806598,0.65,13.5605001578317));
#126442=CARTESIAN_POINT('Ctrl Pts',(-9.5613374450058,0.722647555637915,
13.6365294083141));
#126443=CARTESIAN_POINT('Ctrl Pts',(-9.57489992349997,0.800000000000005,
13.7169449617097));
#126444=CARTESIAN_POINT('',(-10.,0.650000000000002,13.6));
#126445=CARTESIAN_POINT('Ctrl Pts',(-9.94684930972108,0.800000000000004,
13.7494863164095));
#126446=CARTESIAN_POINT('Ctrl Pts',(-9.97416975799544,0.722647555637832,
13.6726475556378));
#126447=CARTESIAN_POINT('Ctrl Pts',(-10.,0.650000000000002,13.6));
#126448=CARTESIAN_POINT('Ctrl Pts',(-10.,0.650000000000002,13.6));
#126449=CARTESIAN_POINT('Ctrl Pts',(-10.0258302420048,0.722647555638509,
13.6726475556385));
#126450=CARTESIAN_POINT('Ctrl Pts',(-10.0531506902789,0.800000000000005,
13.7494863164095));
#126451=CARTESIAN_POINT('',(-10.451485261934,0.650000000000004,13.5605001578317));
#126452=CARTESIAN_POINT('Ctrl Pts',(-10.4251000765,0.800000000000005,13.7169449617097));
#126453=CARTESIAN_POINT('Ctrl Pts',(-10.4386625549942,0.722647555638063,
13.6365294083143));
#126454=CARTESIAN_POINT('Ctrl Pts',(-10.451485261934,0.650000000000004,
13.5605001578317));
#126455=CARTESIAN_POINT('Ctrl Pts',(-10.451485261934,0.650000000000004,
13.5605001578317));
#126456=CARTESIAN_POINT('Ctrl Pts',(-10.4895382001709,0.722647555638065,
13.6275586594087));
#126457=CARTESIAN_POINT('Ctrl Pts',(-10.5297865002293,0.800000000000005,
13.6984859206923));
#126458=CARTESIAN_POINT('',(-10.8892523726467,0.65,13.4432008140434));
#126459=CARTESIAN_POINT('Ctrl Pts',(-10.8904343925656,0.800000000000004,
13.6018506091889));
#126460=CARTESIAN_POINT('Ctrl Pts',(-10.8898268122335,0.72264755563811,
13.5203016490672));
#126461=CARTESIAN_POINT('Ctrl Pts',(-10.8892523726467,0.65,13.4432008140434));
#126462=CARTESIAN_POINT('Ctrl Pts',(-10.8892523726467,0.65,13.4432008140434));
#126463=CARTESIAN_POINT('Ctrl Pts',(-10.9383717878432,0.722647555638111,
13.5026327229221));
#126464=CARTESIAN_POINT('Ctrl Pts',(-10.9903250154551,0.800000000000004,
13.5654933957747));
#126465=CARTESIAN_POINT('',(-11.3,0.649999999999998,13.2516660498395));
#126466=CARTESIAN_POINT('Ctrl Pts',(-11.3287133101945,0.800000000000004,
13.4077003425078));
#126467=CARTESIAN_POINT('Ctrl Pts',(-11.3139541320572,0.722647555638314,
13.3274957995475));
#126468=CARTESIAN_POINT('Ctrl Pts',(-11.3,0.649999999999998,13.2516660498395));
#126469=CARTESIAN_POINT('Ctrl Pts',(-11.3,0.649999999999998,13.2516660498395));
#126470=CARTESIAN_POINT('Ctrl Pts',(-11.3586934235808,0.72264755563789,
13.3016655575425));
#126471=CARTESIAN_POINT('Ctrl Pts',(-11.420773006215,0.800000000000004,
13.3545496522288));
#126472=CARTESIAN_POINT('',(-11.671247785185,0.649999999999997,12.9917155521093));
#126473=CARTESIAN_POINT('Ctrl Pts',(-11.7266199462546,0.800000000000004,
13.1403933192747));
#126474=CARTESIAN_POINT('Ctrl Pts',(-11.6981576204711,0.722647555638155,
13.0639701679279));
#126475=CARTESIAN_POINT('Ctrl Pts',(-11.671247785185,0.649999999999997,
12.9917155521093));
#126476=CARTESIAN_POINT('Ctrl Pts',(-11.671247785185,0.649999999999997,
12.9917155521093));
#126477=CARTESIAN_POINT('Ctrl Pts',(-11.7377318471753,0.722647555638136,
13.0307634488963));
#126478=CARTESIAN_POINT('Ctrl Pts',(-11.8080515281268,0.800000000000004,
13.0720641089596));
#126479=CARTESIAN_POINT('',(-11.9917155521093,0.65,12.671247785185));
#126480=CARTESIAN_POINT('Ctrl Pts',(-12.0720641089596,0.800000000000004,
12.8080515281268));
#126481=CARTESIAN_POINT('Ctrl Pts',(-12.0307634488962,0.72264755563786,
12.7377318471751));
#126482=CARTESIAN_POINT('Ctrl Pts',(-11.9917155521093,0.65,12.671247785185));
#126483=CARTESIAN_POINT('Ctrl Pts',(-11.9917155521093,0.65,12.671247785185));
#126484=CARTESIAN_POINT('Ctrl Pts',(-12.0639701679277,0.722647555637912,
12.698157620471));
#126485=CARTESIAN_POINT('Ctrl Pts',(-12.1403933192747,0.800000000000003,
12.7266199462546));
#126486=CARTESIAN_POINT('',(-12.2516660498395,0.649999999999997,12.3));
#126487=CARTESIAN_POINT('Ctrl Pts',(-12.3545496522288,0.800000000000003,
12.420773006215));
#126488=CARTESIAN_POINT('Ctrl Pts',(-12.301665557543,0.722647555638627,
12.3586934235814));
#126489=CARTESIAN_POINT('Ctrl Pts',(-12.2516660498395,0.649999999999997,
12.3));
#126490=CARTESIAN_POINT('Ctrl Pts',(-12.2516660498395,0.649999999999997,
12.3));
#126491=CARTESIAN_POINT('Ctrl Pts',(-12.3274957995473,0.722647555638123,
12.3139541320571));
#126492=CARTESIAN_POINT('Ctrl Pts',(-12.4077003425078,0.800000000000004,
12.3287133101945));
#126493=CARTESIAN_POINT('',(-12.4432008140434,0.65,11.8892523726467));
#126494=CARTESIAN_POINT('Ctrl Pts',(-12.5654933957747,0.800000000000004,
11.9903250154551));
#126495=CARTESIAN_POINT('Ctrl Pts',(-12.5026327229221,0.722647555638167,
11.9383717878433));
#126496=CARTESIAN_POINT('Ctrl Pts',(-12.4432008140434,0.65,11.8892523726467));
#126497=CARTESIAN_POINT('Ctrl Pts',(-12.4432008140434,0.65,11.8892523726467));
#126498=CARTESIAN_POINT('Ctrl Pts',(-12.5203016490672,0.722647555638142,
11.8898268122335));
#126499=CARTESIAN_POINT('Ctrl Pts',(-12.6018506091889,0.800000000000003,
11.8904343925656));
#126500=CARTESIAN_POINT('',(-12.5605001578317,0.65,11.451485261934));
#126501=CARTESIAN_POINT('Ctrl Pts',(-12.6984859206923,0.800000000000003,
11.5297865002293));
#126502=CARTESIAN_POINT('Ctrl Pts',(-12.6275586594089,0.722647555638257,
11.489538200171));
#126503=CARTESIAN_POINT('Ctrl Pts',(-12.5605001578317,0.65,11.451485261934));
#126504=CARTESIAN_POINT('Ctrl Pts',(-12.5605001578317,0.65,11.451485261934));
#126505=CARTESIAN_POINT('Ctrl Pts',(-12.6365294083144,0.72264755563821,
11.4386625549941));
#126506=CARTESIAN_POINT('Ctrl Pts',(-12.7169449617097,0.800000000000003,
11.4251000765));
#126507=CARTESIAN_POINT('Ctrl Pts',(-12.7494863164095,0.800000000000002,
11.0531506902789));
#126508=CARTESIAN_POINT('Ctrl Pts',(-12.6726475556382,0.722647555638153,
11.0258302420047));
#126509=CARTESIAN_POINT('Ctrl Pts',(-12.6,0.649999999999998,11.));
#126510=CARTESIAN_POINT('',(-12.45,0.5,11.));
#126511=CARTESIAN_POINT('',(-12.6,0.65,11.));
#126512=CARTESIAN_POINT('Origin',(-10.,0.5,11.));
#126513=CARTESIAN_POINT('Origin',(-7.55347823430896,2.9,12.4125));
#126514=CARTESIAN_POINT('',(-7.74833395016046,2.9,12.3));
#126515=CARTESIAN_POINT('',(-7.43862251845746,2.9,12.6635640646055));
#126516=CARTESIAN_POINT('',(-7.74833395016046,2.9,12.3));
#126517=CARTESIAN_POINT('Origin',(-7.27862251845746,0.5,12.3864359353945));
#126518=CARTESIAN_POINT('',(-7.74833395016046,0.5,12.3));
#126519=CARTESIAN_POINT('Origin',(-7.74833395016046,0.5,12.3));
#126520=CARTESIAN_POINT('Origin',(-7.56071843093727,0.5,12.8379350986449));
#126521=CARTESIAN_POINT('',(-8.00828444789066,2.9,12.671247785185));
#126522=CARTESIAN_POINT('',(-8.00828444789066,2.9,12.671247785185));
#126523=CARTESIAN_POINT('',(-8.00828444789066,0.5,12.671247785185));
#126524=CARTESIAN_POINT('Origin',(-8.00828444789066,0.5,12.671247785185));
#126525=CARTESIAN_POINT('',(-7.76641046603697,2.9,13.083069320443));
#126526=CARTESIAN_POINT('Origin',(-7.83592444818889,2.9,12.8158749973645));
#126527=CARTESIAN_POINT('Origin',(-8.18412500263553,2.9,13.1640755518111));
#126528=CARTESIAN_POINT('',(-8.328752214815,2.9,12.9917155521093));
#126529=CARTESIAN_POINT('',(-8.16206490135509,2.9,13.4392815690627));
#126530=CARTESIAN_POINT('',(-8.328752214815,2.9,12.9917155521093));
#126531=CARTESIAN_POINT('Origin',(-7.91693067955702,0.5,13.233589533963));
#126532=CARTESIAN_POINT('',(-8.328752214815,0.5,12.9917155521093));
#126533=CARTESIAN_POINT('Origin',(-8.328752214815,0.5,12.9917155521093));
#126534=CARTESIAN_POINT('Origin',(-8.33643593539449,0.5,13.5613774815425));
#126535=CARTESIAN_POINT('',(-8.7,2.9,13.2516660498395));
#126536=CARTESIAN_POINT('',(-8.7,2.9,13.2516660498395));
#126537=CARTESIAN_POINT('',(-8.7,0.5,13.2516660498395));
#126538=CARTESIAN_POINT('Origin',(-8.7,0.5,13.2516660498395));
#126539=CARTESIAN_POINT('',(-8.61356406460551,2.9,13.7213774815425));
#126540=CARTESIAN_POINT('Origin',(-8.5875,2.9,13.446521765691));
#126541=CARTESIAN_POINT('Origin',(-9.03379309510499,2.9,13.6546316537202));
#126542=CARTESIAN_POINT('',(-9.11074762735326,2.9,13.4432008140434));
#126543=CARTESIAN_POINT('',(-9.10718938218246,2.9,13.9207857163291));
#126544=CARTESIAN_POINT('',(-9.11074762735326,2.9,13.4432008140434));
#126545=CARTESIAN_POINT('Origin',(-8.80648774353097,0.5,13.8113392704649));
#126546=CARTESIAN_POINT('',(-9.11074762735326,0.5,13.4432008140434));
#126547=CARTESIAN_POINT('Origin',(-9.11074762735326,0.5,13.4432008140434));
#126548=CARTESIAN_POINT('Origin',(-9.31280381763391,0.5,13.9758799382605));
#126549=CARTESIAN_POINT('',(-9.54851473806598,2.9,13.5605001578317));
#126550=CARTESIAN_POINT('',(-9.54851473806598,2.9,13.5605001578317));
#126551=CARTESIAN_POINT('',(-9.54851473806598,0.5,13.5605001578317));
#126552=CARTESIAN_POINT('Origin',(-9.54851473806598,0.5,13.5605001578317));
#126553=CARTESIAN_POINT('',(-9.62794229859782,2.9,14.0314473551139));
#126554=CARTESIAN_POINT('Origin',(-9.50944389809092,2.9,13.7820819022595));
#126555=CARTESIAN_POINT('Origin',(-10.,2.9,13.825));
#126556=CARTESIAN_POINT('',(-10.,2.9,13.6));
#126557=CARTESIAN_POINT('',(-10.16,2.9,14.05));
#126558=CARTESIAN_POINT('',(-10.,2.9,13.6));
#126559=CARTESIAN_POINT('Origin',(-9.84,0.5,14.05));
#126560=CARTESIAN_POINT('',(-10.,0.5,13.6));
#126561=CARTESIAN_POINT('Origin',(-10.,0.5,13.6));
#126562=CARTESIAN_POINT('Origin',(-10.3720577014022,0.5,14.0314473551139));
#126563=CARTESIAN_POINT('',(-10.451485261934,2.9,13.5605001578317));
#126564=CARTESIAN_POINT('',(-10.451485261934,2.9,13.5605001578317));
#126565=CARTESIAN_POINT('',(-10.451485261934,0.5,13.5605001578317));
#126566=CARTESIAN_POINT('Origin',(-10.451485261934,0.5,13.5605001578317));
#126567=CARTESIAN_POINT('',(-10.6871961823661,2.9,13.9758799382605));
#126568=CARTESIAN_POINT('Origin',(-10.4905561019091,2.9,13.7820819022595));
#126569=CARTESIAN_POINT('Origin',(-10.966206904895,2.9,13.6546316537202));
#126570=CARTESIAN_POINT('',(-10.8892523726467,2.9,13.4432008140434));
#126571=CARTESIAN_POINT('',(-11.193512256469,2.9,13.8113392704649));
#126572=CARTESIAN_POINT('',(-10.8892523726467,2.9,13.4432008140434));
#126573=CARTESIAN_POINT('Origin',(-10.8928106178175,0.5,13.9207857163291));
#126574=CARTESIAN_POINT('',(-10.8892523726467,0.5,13.4432008140434));
#126575=CARTESIAN_POINT('Origin',(-10.8892523726467,0.5,13.4432008140434));
#126576=CARTESIAN_POINT('Origin',(-11.3864359353945,0.5,13.7213774815425));
#126577=CARTESIAN_POINT('',(-11.3,2.9,13.2516660498395));
#126578=CARTESIAN_POINT('',(-11.3,2.9,13.2516660498395));
#126579=CARTESIAN_POINT('',(-11.3,0.5,13.2516660498395));
#126580=CARTESIAN_POINT('Origin',(-11.3,0.5,13.2516660498395));
#126581=CARTESIAN_POINT('',(-11.6635640646055,2.9,13.5613774815425));
#126582=CARTESIAN_POINT('Origin',(-11.4125,2.9,13.446521765691));
#126583=CARTESIAN_POINT('Origin',(-11.8158749973645,2.9,13.1640755518111));
#126584=CARTESIAN_POINT('',(-11.671247785185,2.9,12.9917155521093));
#126585=CARTESIAN_POINT('',(-12.083069320443,2.9,13.233589533963));
#126586=CARTESIAN_POINT('',(-11.671247785185,2.9,12.9917155521093));
#126587=CARTESIAN_POINT('Origin',(-11.8379350986449,0.5,13.4392815690627));
#126588=CARTESIAN_POINT('',(-11.671247785185,0.5,12.9917155521093));
#126589=CARTESIAN_POINT('Origin',(-11.671247785185,0.5,12.9917155521093));
#126590=CARTESIAN_POINT('Origin',(-12.233589533963,0.5,13.083069320443));
#126591=CARTESIAN_POINT('',(-11.9917155521093,2.9,12.671247785185));
#126592=CARTESIAN_POINT('',(-11.9917155521093,2.9,12.671247785185));
#126593=CARTESIAN_POINT('',(-11.9917155521093,0.5,12.671247785185));
#126594=CARTESIAN_POINT('Origin',(-11.9917155521093,0.5,12.671247785185));
#126595=CARTESIAN_POINT('',(-12.4392815690627,2.9,12.8379350986449));
#126596=CARTESIAN_POINT('Origin',(-12.1640755518111,2.9,12.8158749973645));
#126597=CARTESIAN_POINT('Origin',(-12.446521765691,2.9,12.4125));
#126598=CARTESIAN_POINT('',(-12.2516660498395,2.9,12.3));
#126599=CARTESIAN_POINT('',(-12.7213774815425,2.9,12.3864359353945));
#126600=CARTESIAN_POINT('',(-12.2516660498395,2.9,12.3));
#126601=CARTESIAN_POINT('Origin',(-12.5613774815425,0.5,12.6635640646055));
#126602=CARTESIAN_POINT('',(-12.2516660498395,0.5,12.3));
#126603=CARTESIAN_POINT('Origin',(-12.2516660498395,0.5,12.3));
#126604=CARTESIAN_POINT('Origin',(-12.8113392704649,0.5,12.193512256469));
#126605=CARTESIAN_POINT('',(-12.4432008140434,2.9,11.8892523726467));
#126606=CARTESIAN_POINT('',(-12.4432008140434,2.9,11.8892523726467));
#126607=CARTESIAN_POINT('',(-12.4432008140434,0.5,11.8892523726467));
#126608=CARTESIAN_POINT('Origin',(-12.4432008140434,0.5,11.8892523726467));
#126609=CARTESIAN_POINT('',(-12.9207857163291,2.9,11.8928106178175));
#126610=CARTESIAN_POINT('Origin',(-12.6546316537202,2.9,11.966206904895));
#126611=CARTESIAN_POINT('Origin',(-12.7820819022595,2.9,11.4905561019091));
#126612=CARTESIAN_POINT('',(-12.5605001578317,2.9,11.451485261934));
#126613=CARTESIAN_POINT('',(-13.0314473551139,2.9,11.3720577014022));
#126614=CARTESIAN_POINT('',(-12.5605001578317,2.9,11.451485261934));
#126615=CARTESIAN_POINT('Origin',(-12.9758799382605,0.5,11.6871961823661));
#126616=CARTESIAN_POINT('',(-12.5605001578317,0.5,11.451485261934));
#126617=CARTESIAN_POINT('Origin',(-12.5605001578317,0.5,11.451485261934));
#126618=CARTESIAN_POINT('Origin',(-13.05,0.5,11.16));
#126619=CARTESIAN_POINT('',(-12.6,2.9,11.));
#126620=CARTESIAN_POINT('',(-12.6,2.9,11.));
#126621=CARTESIAN_POINT('',(-12.6,0.5,11.));
#126622=CARTESIAN_POINT('Origin',(-12.6,0.5,11.));
#126623=CARTESIAN_POINT('',(-13.05,2.9,10.84));
#126624=CARTESIAN_POINT('Origin',(-12.825,2.9,11.));
#126625=CARTESIAN_POINT('Origin',(-12.7820819022595,2.9,10.5094438980909));
#126626=CARTESIAN_POINT('',(-12.5605001578317,2.9,10.548514738066));
#126627=CARTESIAN_POINT('',(-12.9758799382605,2.9,10.3128038176339));
#126628=CARTESIAN_POINT('',(-12.5605001578317,2.9,10.548514738066));
#126629=CARTESIAN_POINT('Origin',(-13.0314473551139,0.5,10.6279422985978));
#126630=CARTESIAN_POINT('',(-12.5605001578317,0.5,10.548514738066));
#126631=CARTESIAN_POINT('Origin',(-12.5605001578317,0.5,10.548514738066));
#126632=CARTESIAN_POINT('Origin',(-12.9207857163291,0.5,10.1071893821825));
#126633=CARTESIAN_POINT('',(-12.4432008140434,2.9,10.1107476273533));
#126634=CARTESIAN_POINT('',(-12.4432008140434,2.9,10.1107476273533));
#126635=CARTESIAN_POINT('',(-12.4432008140434,0.5,10.1107476273533));
#126636=CARTESIAN_POINT('Origin',(-12.4432008140434,0.5,10.1107476273533));
#126637=CARTESIAN_POINT('',(-12.8113392704649,2.9,9.80648774353097));
#126638=CARTESIAN_POINT('Origin',(-12.6546316537202,2.9,10.033793095105));
#126639=CARTESIAN_POINT('Origin',(-12.446521765691,2.9,9.5875));
#126640=CARTESIAN_POINT('',(-12.2516660498395,2.9,9.7));
#126641=CARTESIAN_POINT('',(-12.5613774815425,2.9,9.33643593539449));
#126642=CARTESIAN_POINT('',(-12.2516660498395,2.9,9.7));
#126643=CARTESIAN_POINT('Origin',(-12.7213774815425,0.5,9.61356406460551));
#126644=CARTESIAN_POINT('',(-12.2516660498395,0.5,9.7));
#126645=CARTESIAN_POINT('Origin',(-12.2516660498395,0.5,9.7));
#126646=CARTESIAN_POINT('Origin',(-12.4392815690627,0.5,9.16206490135509));
#126647=CARTESIAN_POINT('',(-11.9917155521093,2.9,9.328752214815));
#126648=CARTESIAN_POINT('',(-11.9917155521093,2.9,9.328752214815));
#126649=CARTESIAN_POINT('',(-11.9917155521093,0.5,9.328752214815));
#126650=CARTESIAN_POINT('Origin',(-11.9917155521093,0.5,9.328752214815));
#126651=CARTESIAN_POINT('',(-12.233589533963,2.9,8.91693067955702));
#126652=CARTESIAN_POINT('Origin',(-12.1640755518111,2.9,9.18412500263553));
#126653=CARTESIAN_POINT('Origin',(-11.8158749973645,2.9,8.83592444818889));
#126654=CARTESIAN_POINT('',(-11.671247785185,2.9,9.00828444789066));
#126655=CARTESIAN_POINT('',(-11.8379350986449,2.9,8.56071843093727));
#126656=CARTESIAN_POINT('',(-11.671247785185,2.9,9.00828444789066));
#126657=CARTESIAN_POINT('Origin',(-12.083069320443,0.5,8.76641046603697));
#126658=CARTESIAN_POINT('',(-11.671247785185,0.5,9.00828444789066));
#126659=CARTESIAN_POINT('Origin',(-11.671247785185,0.5,9.00828444789066));
#126660=CARTESIAN_POINT('Origin',(-11.6635640646055,0.5,8.43862251845746));
#126661=CARTESIAN_POINT('',(-11.3,2.9,8.74833395016046));
#126662=CARTESIAN_POINT('',(-11.3,2.9,8.74833395016046));
#126663=CARTESIAN_POINT('',(-11.3,0.5,8.74833395016046));
#126664=CARTESIAN_POINT('Origin',(-11.3,0.5,8.74833395016046));
#126665=CARTESIAN_POINT('',(-11.3864359353945,2.9,8.27862251845746));
#126666=CARTESIAN_POINT('Origin',(-11.4125,2.9,8.55347823430896));
#126667=CARTESIAN_POINT('Origin',(-10.966206904895,2.9,8.34536834627981));
#126668=CARTESIAN_POINT('',(-10.8892523726467,2.9,8.55679918595664));
#126669=CARTESIAN_POINT('',(-10.8928106178175,2.9,8.07921428367087));
#126670=CARTESIAN_POINT('',(-10.8892523726467,2.9,8.55679918595664));
#126671=CARTESIAN_POINT('Origin',(-11.193512256469,0.5,8.18866072953509));
#126672=CARTESIAN_POINT('',(-10.8892523726467,0.5,8.55679918595664));
#126673=CARTESIAN_POINT('Origin',(-10.8892523726467,0.5,8.55679918595664));
#126674=CARTESIAN_POINT('Origin',(-10.6871961823661,0.5,8.02412006173947));
#126675=CARTESIAN_POINT('',(-10.451485261934,2.9,8.43949984216826));
#126676=CARTESIAN_POINT('',(-10.451485261934,2.9,8.43949984216826));
#126677=CARTESIAN_POINT('',(-10.451485261934,0.5,8.43949984216826));
#126678=CARTESIAN_POINT('Origin',(-10.451485261934,0.5,8.43949984216826));
#126679=CARTESIAN_POINT('',(-10.3720577014022,2.9,7.96855264488606));
#126680=CARTESIAN_POINT('Origin',(-10.4905561019091,2.9,8.21791809774051));
#126681=CARTESIAN_POINT('Origin',(-10.,2.9,8.175));
#126682=CARTESIAN_POINT('',(-10.,2.9,8.4));
#126683=CARTESIAN_POINT('',(-9.84,2.9,7.95));
#126684=CARTESIAN_POINT('',(-10.,2.9,8.4));
#126685=CARTESIAN_POINT('Origin',(-10.16,0.5,7.95));
#126686=CARTESIAN_POINT('',(-10.,0.5,8.4));
#126687=CARTESIAN_POINT('Origin',(-10.,0.5,8.4));
#126688=CARTESIAN_POINT('Origin',(-9.62794229859782,0.5,7.96855264488606));
#126689=CARTESIAN_POINT('',(-9.54851473806598,2.9,8.43949984216826));
#126690=CARTESIAN_POINT('',(-9.54851473806598,2.9,8.43949984216826));
#126691=CARTESIAN_POINT('',(-9.54851473806598,0.5,8.43949984216826));
#126692=CARTESIAN_POINT('Origin',(-9.54851473806598,0.5,8.43949984216826));
#126693=CARTESIAN_POINT('',(-9.31280381763391,2.9,8.02412006173947));
#126694=CARTESIAN_POINT('Origin',(-9.50944389809092,2.9,8.21791809774051));
#126695=CARTESIAN_POINT('Origin',(-9.03379309510498,2.9,8.34536834627981));
#126696=CARTESIAN_POINT('',(-9.11074762735326,2.9,8.55679918595664));
#126697=CARTESIAN_POINT('',(-8.80648774353097,2.9,8.18866072953509));
#126698=CARTESIAN_POINT('',(-9.11074762735326,2.9,8.55679918595664));
#126699=CARTESIAN_POINT('Origin',(-9.10718938218246,0.5,8.07921428367087));
#126700=CARTESIAN_POINT('',(-9.11074762735326,0.5,8.55679918595664));
#126701=CARTESIAN_POINT('Origin',(-9.11074762735326,0.5,8.55679918595664));
#126702=CARTESIAN_POINT('Origin',(-8.61356406460551,0.5,8.27862251845747));
#126703=CARTESIAN_POINT('',(-8.7,2.9,8.74833395016046));
#126704=CARTESIAN_POINT('',(-8.7,2.9,8.74833395016046));
#126705=CARTESIAN_POINT('',(-8.7,0.5,8.74833395016046));
#126706=CARTESIAN_POINT('Origin',(-8.7,0.5,8.74833395016046));
#126707=CARTESIAN_POINT('',(-8.33643593539449,2.9,8.43862251845747));
#126708=CARTESIAN_POINT('Origin',(-8.5875,2.9,8.55347823430897));
#126709=CARTESIAN_POINT('Origin',(-8.18412500263553,2.9,8.83592444818889));
#126710=CARTESIAN_POINT('',(-8.328752214815,2.9,9.00828444789066));
#126711=CARTESIAN_POINT('',(-7.91693067955702,2.9,8.76641046603697));
#126712=CARTESIAN_POINT('',(-8.328752214815,2.9,9.00828444789066));
#126713=CARTESIAN_POINT('Origin',(-8.16206490135509,0.5,8.56071843093727));
#126714=CARTESIAN_POINT('',(-8.328752214815,0.5,9.00828444789066));
#126715=CARTESIAN_POINT('Origin',(-8.328752214815,0.5,9.00828444789066));
#126716=CARTESIAN_POINT('Origin',(-7.76641046603696,0.5,8.91693067955702));
#126717=CARTESIAN_POINT('',(-8.00828444789066,2.9,9.328752214815));
#126718=CARTESIAN_POINT('',(-8.00828444789066,2.9,9.328752214815));
#126719=CARTESIAN_POINT('',(-8.00828444789066,0.5,9.328752214815));
#126720=CARTESIAN_POINT('Origin',(-8.00828444789066,0.5,9.328752214815));
#126721=CARTESIAN_POINT('',(-7.56071843093727,2.9,9.16206490135509));
#126722=CARTESIAN_POINT('Origin',(-7.83592444818889,2.9,9.18412500263553));
#126723=CARTESIAN_POINT('Origin',(-7.55347823430896,2.9,9.5875));
#126724=CARTESIAN_POINT('',(-7.74833395016046,2.9,9.7));
#126725=CARTESIAN_POINT('',(-7.27862251845746,2.9,9.61356406460551));
#126726=CARTESIAN_POINT('',(-7.74833395016046,2.9,9.7));
#126727=CARTESIAN_POINT('Origin',(-7.43862251845746,0.5,9.33643593539449));
#126728=CARTESIAN_POINT('',(-7.74833395016046,0.5,9.7));
#126729=CARTESIAN_POINT('Origin',(-7.74833395016046,0.5,9.7));
#126730=CARTESIAN_POINT('Origin',(-7.18866072953509,0.5,9.80648774353097));
#126731=CARTESIAN_POINT('',(-7.55679918595664,2.9,10.1107476273533));
#126732=CARTESIAN_POINT('',(-7.55679918595664,2.9,10.1107476273533));
#126733=CARTESIAN_POINT('',(-7.55679918595664,0.5,10.1107476273533));
#126734=CARTESIAN_POINT('Origin',(-7.55679918595664,0.5,10.1107476273533));
#126735=CARTESIAN_POINT('',(-7.07921428367087,2.9,10.1071893821825));
#126736=CARTESIAN_POINT('Origin',(-7.34536834627981,2.9,10.033793095105));
#126737=CARTESIAN_POINT('Origin',(-7.21791809774051,2.9,10.5094438980909));
#126738=CARTESIAN_POINT('',(-7.43949984216826,2.9,10.548514738066));
#126739=CARTESIAN_POINT('',(-6.96855264488606,2.9,10.6279422985978));
#126740=CARTESIAN_POINT('',(-7.43949984216826,2.9,10.548514738066));
#126741=CARTESIAN_POINT('Origin',(-7.02412006173947,0.5,10.3128038176339));
#126742=CARTESIAN_POINT('',(-7.43949984216826,0.5,10.548514738066));
#126743=CARTESIAN_POINT('Origin',(-7.43949984216826,0.5,10.548514738066));
#126744=CARTESIAN_POINT('Origin',(-6.95,0.5,10.84));
#126745=CARTESIAN_POINT('',(-7.4,2.9,11.));
#126746=CARTESIAN_POINT('',(-7.4,2.9,11.));
#126747=CARTESIAN_POINT('',(-7.4,0.5,11.));
#126748=CARTESIAN_POINT('Origin',(-7.4,0.5,11.));
#126749=CARTESIAN_POINT('',(-6.95,2.9,11.16));
#126750=CARTESIAN_POINT('Origin',(-7.175,2.9,11.));
#126751=CARTESIAN_POINT('Origin',(-10.,3.3,11.));
#126752=CARTESIAN_POINT('Origin',(-10.,3.3,8.45));
#126753=CARTESIAN_POINT('Origin',(-10.,0.5,11.));
#126754=CARTESIAN_POINT('',(-11.5933756729741,0.5,11.));
#126755=CARTESIAN_POINT('Origin',(-10.,0.5,11.));
#126756=CARTESIAN_POINT('Origin',(-10.,0.6,11.));
#126757=CARTESIAN_POINT('',(-11.3903449147952,0.7,11.0918519675297));
#126758=CARTESIAN_POINT('',(-11.4433756729741,0.650000000000001,11.));
#126759=CARTESIAN_POINT('Ctrl Pts',(-11.3903449147952,0.699999999999999,
11.0918519675297));
#126760=CARTESIAN_POINT('Ctrl Pts',(-11.4163929392269,0.676982733747201,
11.0467354657773));
#126761=CARTESIAN_POINT('Ctrl Pts',(-11.4433756729741,0.650000000000001,
11.));
#126762=CARTESIAN_POINT('',(-10.7747185946659,0.7,12.1581480324703));
#126763=CARTESIAN_POINT('Origin',(-10.,0.7,11.));
#126764=CARTESIAN_POINT('',(-10.721687836487,0.65,12.25));
#126765=CARTESIAN_POINT('Ctrl Pts',(-10.721687836487,0.65,12.25));
#126766=CARTESIAN_POINT('Ctrl Pts',(-10.7486705702342,0.676982733747207,
12.2032645342227));
#126767=CARTESIAN_POINT('Ctrl Pts',(-10.7747185946659,0.7,12.1581480324703));
#126768=CARTESIAN_POINT('',(-10.6156263201293,0.7,12.25));
#126769=CARTESIAN_POINT('Ctrl Pts',(-10.6156263201293,0.7,12.25));
#126770=CARTESIAN_POINT('Ctrl Pts',(-10.6677223689926,0.67698273374721,
12.25));
#126771=CARTESIAN_POINT('Ctrl Pts',(-10.721687836487,0.65,12.25));
#126772=CARTESIAN_POINT('',(-9.38437367987071,0.7,12.25));
#126773=CARTESIAN_POINT('Origin',(-10.,0.7,11.));
#126774=CARTESIAN_POINT('',(-9.27831216351297,0.65,12.25));
#126775=CARTESIAN_POINT('Ctrl Pts',(-9.27831216351297,0.65,12.25));
#126776=CARTESIAN_POINT('Ctrl Pts',(-9.3322776310074,0.676982733747216,
12.25));
#126777=CARTESIAN_POINT('Ctrl Pts',(-9.38437367987071,0.7,12.25));
#126778=CARTESIAN_POINT('',(-9.2252814053341,0.7,12.1581480324703));
#126779=CARTESIAN_POINT('Ctrl Pts',(-9.22528140533409,0.700000000000001,
12.1581480324703));
#126780=CARTESIAN_POINT('Ctrl Pts',(-9.25132942976576,0.676982733747215,
12.2032645342227));
#126781=CARTESIAN_POINT('Ctrl Pts',(-9.27831216351297,0.65,12.25));
#126782=CARTESIAN_POINT('',(-8.60965508520481,0.7,11.0918519675297));
#126783=CARTESIAN_POINT('Origin',(-10.,0.7,11.));
#126784=CARTESIAN_POINT('',(-8.55662432702594,0.650000000000001,11.));
#126785=CARTESIAN_POINT('Ctrl Pts',(-8.55662432702594,0.650000000000001,
11.));
#126786=CARTESIAN_POINT('Ctrl Pts',(-8.58360706077315,0.676982733747216,
11.0467354657773));
#126787=CARTESIAN_POINT('Ctrl Pts',(-8.60965508520481,0.7,11.0918519675297));
#126788=CARTESIAN_POINT('',(-8.60965508520481,0.7,10.9081480324703));
#126789=CARTESIAN_POINT('Ctrl Pts',(-8.60965508520481,0.7,10.9081480324703));
#126790=CARTESIAN_POINT('Ctrl Pts',(-8.58360706077314,0.676982733747203,
10.9532645342227));
#126791=CARTESIAN_POINT('Ctrl Pts',(-8.55662432702594,0.650000000000001,
11.));
#126792=CARTESIAN_POINT('',(-9.22528140533409,0.7,9.84185196752971));
#126793=CARTESIAN_POINT('Origin',(-10.,0.7,11.));
#126794=CARTESIAN_POINT('',(-9.27831216351297,0.649999999999999,9.75));
#126795=CARTESIAN_POINT('Ctrl Pts',(-9.27831216351297,0.649999999999999,
9.75));
#126796=CARTESIAN_POINT('Ctrl Pts',(-9.25132942976575,0.676982733747217,
9.79673546577728));
#126797=CARTESIAN_POINT('Ctrl Pts',(-9.22528140533409,0.7,9.84185196752971));
#126798=CARTESIAN_POINT('',(-9.38437367987072,0.7,9.75));
#126799=CARTESIAN_POINT('Ctrl Pts',(-9.38437367987071,0.7,9.75));
#126800=CARTESIAN_POINT('Ctrl Pts',(-9.33227763100738,0.676982733747206,
9.75));
#126801=CARTESIAN_POINT('Ctrl Pts',(-9.27831216351297,0.649999999999999,
9.75));
#126802=CARTESIAN_POINT('',(-10.6156263201293,0.7,9.75));
#126803=CARTESIAN_POINT('Origin',(-10.,0.7,11.));
#126804=CARTESIAN_POINT('',(-10.721687836487,0.649999999999999,9.75));
#126805=CARTESIAN_POINT('Ctrl Pts',(-10.721687836487,0.649999999999999,
9.75));
#126806=CARTESIAN_POINT('Ctrl Pts',(-10.6677223689926,0.67698273374721,
9.75));
#126807=CARTESIAN_POINT('Ctrl Pts',(-10.6156263201293,0.7,9.75));
#126808=CARTESIAN_POINT('',(-10.7747185946659,0.7,9.84185196752971));
#126809=CARTESIAN_POINT('Ctrl Pts',(-10.7747185946659,0.7,9.84185196752971));
#126810=CARTESIAN_POINT('Ctrl Pts',(-10.7486705702342,0.676982733747205,
9.79673546577726));
#126811=CARTESIAN_POINT('Ctrl Pts',(-10.721687836487,0.649999999999999,
9.75));
#126812=CARTESIAN_POINT('',(-11.3903449147952,0.7,10.9081480324703));
#126813=CARTESIAN_POINT('Origin',(-10.,0.7,11.));
#126814=CARTESIAN_POINT('Ctrl Pts',(-11.4433756729741,0.650000000000001,
11.));
#126815=CARTESIAN_POINT('Ctrl Pts',(-11.4163929392269,0.676982733747204,
10.9532645342227));
#126816=CARTESIAN_POINT('Ctrl Pts',(-11.3903449147952,0.7,10.9081480324703));
#126817=CARTESIAN_POINT('',(-11.4933756729741,0.6,11.));
#126818=CARTESIAN_POINT('Origin',(-10.,0.6,11.));
#126819=CARTESIAN_POINT('',(-11.3903449147952,0.5,10.9081480324703));
#126820=CARTESIAN_POINT('',(-11.3903449147952,0.6,10.9081480324703));
#126821=CARTESIAN_POINT('',(-10.7747185946659,0.5,9.84185196752971));
#126822=CARTESIAN_POINT('',(-10.7747185946659,0.6,9.84185196752971));
#126823=CARTESIAN_POINT('Origin',(-10.,0.5,11.));
#126824=CARTESIAN_POINT('Origin',(-10.,0.6,11.));
#126825=CARTESIAN_POINT('',(-9.38437367987072,0.5,9.75));
#126826=CARTESIAN_POINT('',(-9.38437367987072,0.6,9.75));
#126827=CARTESIAN_POINT('',(-10.6156263201293,0.5,9.75));
#126828=CARTESIAN_POINT('Origin',(-10.,0.5,11.));
#126829=CARTESIAN_POINT('',(-10.6156263201293,0.6,9.75));
#126830=CARTESIAN_POINT('Origin',(-10.,0.6,11.));
#126831=CARTESIAN_POINT('',(-10.7747185946659,0.5,12.1581480324703));
#126832=CARTESIAN_POINT('',(-10.7747185946659,0.6,12.1581480324703));
#126833=CARTESIAN_POINT('',(-11.3903449147952,0.5,11.0918519675297));
#126834=CARTESIAN_POINT('',(-11.3903449147952,0.6,11.0918519675297));
#126835=CARTESIAN_POINT('Origin',(-10.,0.5,11.));
#126836=CARTESIAN_POINT('Origin',(-10.,0.6,11.));
#126837=CARTESIAN_POINT('',(-8.60965508520481,0.5,10.9081480324703));
#126838=CARTESIAN_POINT('',(-8.60965508520481,0.6,10.9081480324703));
#126839=CARTESIAN_POINT('',(-9.22528140533409,0.5,9.84185196752971));
#126840=CARTESIAN_POINT('Origin',(-10.,0.5,11.));
#126841=CARTESIAN_POINT('',(-9.22528140533409,0.6,9.84185196752971));
#126842=CARTESIAN_POINT('Origin',(-10.,0.6,11.));
#126843=CARTESIAN_POINT('',(-9.38437367987071,0.5,12.25));
#126844=CARTESIAN_POINT('',(-9.38437367987071,0.6,12.25));
#126845=CARTESIAN_POINT('',(-10.6156263201293,0.5,12.25));
#126846=CARTESIAN_POINT('',(-10.6156263201293,0.6,12.25));
#126847=CARTESIAN_POINT('Origin',(-10.,0.5,11.));
#126848=CARTESIAN_POINT('Origin',(-10.,0.6,11.));
#126849=CARTESIAN_POINT('',(-9.2252814053341,0.5,12.1581480324703));
#126850=CARTESIAN_POINT('',(-9.2252814053341,0.6,12.1581480324703));
#126851=CARTESIAN_POINT('',(-8.60965508520481,0.5,11.0918519675297));
#126852=CARTESIAN_POINT('Origin',(-10.,0.5,11.));
#126853=CARTESIAN_POINT('',(-8.60965508520481,0.6,11.0918519675297));
#126854=CARTESIAN_POINT('Origin',(-10.721687836487,0.5,12.25));
#126855=CARTESIAN_POINT('',(-10.3608439182435,0.5,12.25));
#126856=CARTESIAN_POINT('',(-10.721687836487,1.8,12.25));
#126857=CARTESIAN_POINT('',(-10.721687836487,0.5,12.25));
#126858=CARTESIAN_POINT('',(-9.27831216351297,1.8,12.25));
#126859=CARTESIAN_POINT('',(-9.27831216351297,1.8,12.25));
#126860=CARTESIAN_POINT('',(-9.27831216351297,0.5,12.25));
#126861=CARTESIAN_POINT('Origin',(-11.4433756729741,0.5,11.));
#126862=CARTESIAN_POINT('',(-11.2629537138523,0.5,11.3125));
#126863=CARTESIAN_POINT('',(-11.4433756729741,1.8,11.));
#126864=CARTESIAN_POINT('',(-11.4433756729741,0.5,11.));
#126865=CARTESIAN_POINT('',(-10.721687836487,1.8,12.25));
#126866=CARTESIAN_POINT('Origin',(-10.721687836487,0.5,9.75));
#126867=CARTESIAN_POINT('',(-10.9021097956088,0.5,10.0625));
#126868=CARTESIAN_POINT('',(-10.721687836487,1.8,9.75));
#126869=CARTESIAN_POINT('',(-10.721687836487,0.5,9.75));
#126870=CARTESIAN_POINT('',(-11.4433756729741,1.8,11.));
#126871=CARTESIAN_POINT('Origin',(-10.,0.5,11.));
#126872=CARTESIAN_POINT('Origin',(-10.,0.5,11.));
#126873=CARTESIAN_POINT('Origin',(-10.,0.5,11.));
#126874=CARTESIAN_POINT('',(-9.63915608175648,0.5,9.75));
#126875=CARTESIAN_POINT('Origin',(-10.,0.5,11.));
#126876=CARTESIAN_POINT('Origin',(-10.,0.5,11.));
#126877=CARTESIAN_POINT('',(-8.73704628614769,0.5,10.6875));
#126878=CARTESIAN_POINT('Origin',(-10.,0.5,11.));
#126879=CARTESIAN_POINT('',(-9.09789020439121,0.5,11.9375));
#126880=CARTESIAN_POINT('Origin',(-10.,1.8,11.));
#126881=CARTESIAN_POINT('',(-8.55662432702594,1.8,11.));
#126882=CARTESIAN_POINT('',(-9.27831216351297,1.8,9.75));
#126883=CARTESIAN_POINT('',(-9.27831216351297,1.8,9.75));
#126884=CARTESIAN_POINT('Origin',(-10.,1.8,11.));
#126885=CARTESIAN_POINT('Origin',(-10.,1.8,11.));
#126886=CARTESIAN_POINT('',(-10.721687836487,1.8,9.75));
#126887=CARTESIAN_POINT('Origin',(-10.,1.8,11.));
#126888=CARTESIAN_POINT('Origin',(-10.,1.8,11.));
#126889=CARTESIAN_POINT('Origin',(-10.,1.8,11.));
#126890=CARTESIAN_POINT('Origin',(-10.,1.8,11.));
#126891=CARTESIAN_POINT('Origin',(-10.,1.8,11.));
#126892=CARTESIAN_POINT('Origin',(-10.,1.8,11.));
#126893=CARTESIAN_POINT('Origin',(-10.,1.8,11.));
#126894=CARTESIAN_POINT('Origin',(-10.,1.8,11.));
#126895=CARTESIAN_POINT('',(-8.55662432702594,1.8,11.));
#126896=CARTESIAN_POINT('Origin',(-10.,1.8,11.));
#126897=CARTESIAN_POINT('Origin',(-10.,2.23363380017626,11.));
#126898=CARTESIAN_POINT('',(-10.,2.66726760035252,11.));
#126899=CARTESIAN_POINT('',(-10.721687836487,2.23363380017626,11.));
#126900=CARTESIAN_POINT('Origin',(-8.55662432702594,0.5,11.));
#126901=CARTESIAN_POINT('',(-8.55662432702594,0.5,11.));
#126902=CARTESIAN_POINT('',(-9.27831216351297,0.5,9.75));
#126903=CARTESIAN_POINT('Origin',(-9.27831216351297,0.5,12.25));
#126904=CARTESIAN_POINT('Origin',(-9.27831216351297,0.5,9.75));
#135265=UNCERTAINTY_MEASURE_WITH_UNIT(LENGTH_MEASURE(0.01),#135283,
'DISTANCE_ACCURACY_VALUE',
'Maximum model space distance between geometric entities at asserted c
onnectivities');
#135267=UNCERTAINTY_MEASURE_WITH_UNIT(LENGTH_MEASURE(0.01),#135283,
'DISTANCE_ACCURACY_VALUE',
'Maximum model space distance between geometric entities at asserted c
onnectivities');
#135280=(
GEOMETRIC_REPRESENTATION_CONTEXT(3)
GLOBAL_UNCERTAINTY_ASSIGNED_CONTEXT((#135265))
GLOBAL_UNIT_ASSIGNED_CONTEXT((#135283,#135285,#135286))
REPRESENTATION_CONTEXT('','3D')
);
#135282=(
GEOMETRIC_REPRESENTATION_CONTEXT(3)
GLOBAL_UNCERTAINTY_ASSIGNED_CONTEXT((#135267))
GLOBAL_UNIT_ASSIGNED_CONTEXT((#135283,#135285,#135286))
REPRESENTATION_CONTEXT('','3D')
);
#135283=(
LENGTH_UNIT()
NAMED_UNIT(*)
SI_UNIT(.MILLI.,.METRE.)
);
#135285=(
NAMED_UNIT(*)
PLANE_ANGLE_UNIT()
SI_UNIT($,.RADIAN.)
);
#135286=(
NAMED_UNIT(*)
SI_UNIT($,.STERADIAN.)
SOLID_ANGLE_UNIT()
);
#135299=SHAPE_DEFINITION_REPRESENTATION(#135313,#135348);
#135313=PRODUCT_DEFINITION_SHAPE('',$,#135363);
#135348=SHAPE_REPRESENTATION('',(#33856),#135280);
#135350=PRODUCT_DEFINITION_CONTEXT('part definition',#135394,'design');
#135363=PRODUCT_DEFINITION('2026-10-15-19-09-11-265',
'ISO 4762 - M3 x 10 - 12.9',#135377,#135350);
#135377=PRODUCT_DEFINITION_FORMATION('',$,#135408);
#135394=APPLICATION_CONTEXT(
'Core Data for Automotive Mechanical Design Process');
#135395=PRODUCT_CONTEXT('part definition',#135394,'mechanical');
#135408=PRODUCT('2026-10-15-19-09-11-265','ISO 4762 - M3 x 10 - 12.9',$,
(#135395));
#135422=PRESENTATION_STYLE_ASSIGNMENT((#135436));
#135436=SURFACE_STYLE_USAGE(.BOTH.,#135450);
#135450=SURFACE_SIDE_STYLE('',(#135464));
#135464=SURFACE_STYLE_FILL_AREA(#135478);
#135478=FILL_AREA_STYLE('Opaque(201,205,211)',(#135492));
#135492=FILL_AREA_STYLE_COLOUR('Opaque(201,205,211)',#135506);
#135506=COLOUR_RGB('Opaque(201,205,211)', 0.08235294, 0.09019608, 0.10196078);
ENDSEC;
END-ISO-10303-21;
